ISO-10303-21;
HEADER;
/* Generated by software containing ST-Developer
 * from STEP Tools, Inc. (www.steptools.com) 
 */

FILE_DESCRIPTION(
/* description */ (
'Independent manual bench leaf bending machine,200mm work width. Fabri
cated welded frame and folding leaf, repeated bushed and fully retaine
d hinge hardware, two handles with bonded grips, beveled clamping beam
 and modeledM12 clamp screws.2mm omitted-workpiece assembly reference 
gap, not a capacity claim. Native135deg hinge travel. Weld sizing, pro
duction fits, material condition, bending capacity, strength and life 
unassigned.'),
/* implementation_level */ '2;1');

FILE_NAME(
/* name */ 'Socket head cap screw M12x50.step',
/* time_stamp */ '2026-11-14T09:11:34-08:00',
/* author */ (''),
/* organization */ (''),
/* preprocessor_version */ 'ST-DEVELOPER v20.2',
/* originating_system */ 'Autodesk Translation Framework v15.17.0.0',
/* authorisation */ '');

FILE_SCHEMA (('AUTOMOTIVE_DESIGN { 1 0 10303 214 3 1 1 }'));
ENDSEC;

DATA;
#10=MECHANICAL_DESIGN_GEOMETRIC_PRESENTATION_REPRESENTATION('',(#454),#37701);
#147=CONICAL_SURFACE('',#4560,5.5,0.78539816339745);
#150=B_SPLINE_SURFACE_WITH_KNOTS('',3,3,((#34220,#34221,#34222,#34223,#34224,
#34225,#34226,#34227,#34228,#34229,#34230,#34231,#34232,#34233,#34234,#34235,
#34236,#34237,#34238,#34239,#34240,#34241,#34242,#34243,#34244,#34245,#34246,
#34247,#34248,#34249,#34250,#34251,#34252,#34253,#34254,#34255,#34256,#34257,
#34258,#34259,#34260,#34261,#34262,#34263,#34264,#34265,#34266,#34267,#34268,
#34269,#34270,#34271,#34272,#34273,#34274,#34275,#34276,#34277,#34278,#34279,
#34280,#34281,#34282,#34283,#34284,#34285,#34286,#34287,#34288,#34289,#34290,
#34291,#34292,#34293,#34294,#34295,#34296,#34297,#34298,#34299,#34300,#34301,
#34302,#34303,#34304,#34305,#34306,#34307,#34308,#34309,#34310,#34311,#34312,
#34313,#34314,#34315,#34316,#34317,#34318,#34319,#34320,#34321,#34322,#34323,
#34324,#34325,#34326,#34327,#34328,#34329,#34330,#34331,#34332,#34333,#34334,
#34335,#34336,#34337,#34338,#34339,#34340,#34341,#34342,#34343,#34344,#34345,
#34346,#34347,#34348,#34349,#34350,#34351,#34352,#34353,#34354,#34355,#34356,
#34357,#34358,#34359,#34360,#34361,#34362,#34363,#34364,#34365,#34366,#34367,
#34368,#34369,#34370,#34371,#34372,#34373,#34374,#34375,#34376,#34377,#34378,
#34379,#34380,#34381,#34382,#34383,#34384,#34385,#34386,#34387,#34388,#34389,
#34390,#34391,#34392,#34393,#34394,#34395,#34396,#34397,#34398,#34399,#34400,
#34401,#34402,#34403,#34404,#34405,#34406,#34407,#34408,#34409,#34410,#34411,
#34412,#34413,#34414,#34415,#34416,#34417,#34418,#34419,#34420,#34421,#34422,
#34423,#34424,#34425,#34426,#34427,#34428,#34429,#34430,#34431,#34432,#34433,
#34434,#34435,#34436,#34437,#34438,#34439,#34440,#34441,#34442,#34443,#34444,
#34445,#34446,#34447,#34448,#34449,#34450,#34451,#34452,#34453,#34454,#34455,
#34456,#34457,#34458,#34459,#34460,#34461,#34462,#34463,#34464,#34465,#34466,
#34467,#34468,#34469,#34470,#34471,#34472,#34473,#34474,#34475,#34476,#34477,
#34478,#34479,#34480,#34481,#34482,#34483,#34484,#34485,#34486,#34487,#34488,
#34489,#34490,#34491,#34492,#34493,#34494,#34495,#34496,#34497,#34498,#34499,
#34500,#34501,#34502,#34503,#34504,#34505,#34506,#34507,#34508,#34509,#34510,
#34511,#34512,#34513,#34514,#34515,#34516,#34517,#34518,#34519,#34520,#34521,
#34522,#34523,#34524,#34525,#34526,#34527,#34528,#34529,#34530,#34531,#34532,
#34533,#34534,#34535,#34536,#34537,#34538,#34539,#34540,#34541,#34542,#34543,
#34544,#34545,#34546,#34547,#34548,#34549,#34550,#34551,#34552,#34553,#34554,
#34555,#34556,#34557,#34558,#34559,#34560,#34561,#34562,#34563,#34564,#34565,
#34566,#34567,#34568,#34569,#34570,#34571,#34572,#34573,#34574,#34575,#34576,
#34577,#34578,#34579,#34580,#34581,#34582),(#34583,#34584,#34585,#34586,
#34587,#34588,#34589,#34590,#34591,#34592,#34593,#34594,#34595,#34596,#34597,
#34598,#34599,#34600,#34601,#34602,#34603,#34604,#34605,#34606,#34607,#34608,
#34609,#34610,#34611,#34612,#34613,#34614,#34615,#34616,#34617,#34618,#34619,
#34620,#34621,#34622,#34623,#34624,#34625,#34626,#34627,#34628,#34629,#34630,
#34631,#34632,#34633,#34634,#34635,#34636,#34637,#34638,#34639,#34640,#34641,
#34642,#34643,#34644,#34645,#34646,#34647,#34648,#34649,#34650,#34651,#34652,
#34653,#34654,#34655,#34656,#34657,#34658,#34659,#34660,#34661,#34662,#34663,
#34664,#34665,#34666,#34667,#34668,#34669,#34670,#34671,#34672,#34673,#34674,
#34675,#34676,#34677,#34678,#34679,#34680,#34681,#34682,#34683,#34684,#34685,
#34686,#34687,#34688,#34689,#34690,#34691,#34692,#34693,#34694,#34695,#34696,
#34697,#34698,#34699,#34700,#34701,#34702,#34703,#34704,#34705,#34706,#34707,
#34708,#34709,#34710,#34711,#34712,#34713,#34714,#34715,#34716,#34717,#34718,
#34719,#34720,#34721,#34722,#34723,#34724,#34725,#34726,#34727,#34728,#34729,
#34730,#34731,#34732,#34733,#34734,#34735,#34736,#34737,#34738,#34739,#34740,
#34741,#34742,#34743,#34744,#34745,#34746,#34747,#34748,#34749,#34750,#34751,
#34752,#34753,#34754,#34755,#34756,#34757,#34758,#34759,#34760,#34761,#34762,
#34763,#34764,#34765,#34766,#34767,#34768,#34769,#34770,#34771,#34772,#34773,
#34774,#34775,#34776,#34777,#34778,#34779,#34780,#34781,#34782,#34783,#34784,
#34785,#34786,#34787,#34788,#34789,#34790,#34791,#34792,#34793,#34794,#34795,
#34796,#34797,#34798,#34799,#34800,#34801,#34802,#34803,#34804,#34805,#34806,
#34807,#34808,#34809,#34810,#34811,#34812,#34813,#34814,#34815,#34816,#34817,
#34818,#34819,#34820,#34821,#34822,#34823,#34824,#34825,#34826,#34827,#34828,
#34829,#34830,#34831,#34832,#34833,#34834,#34835,#34836,#34837,#34838,#34839,
#34840,#34841,#34842,#34843,#34844,#34845,#34846,#34847,#34848,#34849,#34850,
#34851,#34852,#34853,#34854,#34855,#34856,#34857,#34858,#34859,#34860,#34861,
#34862,#34863,#34864,#34865,#34866,#34867,#34868,#34869,#34870,#34871,#34872,
#34873,#34874,#34875,#34876,#34877,#34878,#34879,#34880,#34881,#34882,#34883,
#34884,#34885,#34886,#34887,#34888,#34889,#34890,#34891,#34892,#34893,#34894,
#34895,#34896,#34897,#34898,#34899,#34900,#34901,#34902,#34903,#34904,#34905,
#34906,#34907,#34908,#34909,#34910,#34911,#34912,#34913,#34914,#34915,#34916,
#34917,#34918,#34919,#34920,#34921,#34922,#34923,#34924,#34925,#34926,#34927,
#34928,#34929,#34930,#34931,#34932,#34933,#34934,#34935,#34936,#34937,#34938,
#34939,#34940,#34941,#34942,#34943,#34944,#34945),(#34946,#34947,#34948,
#34949,#34950,#34951,#34952,#34953,#34954,#34955,#34956,#34957,#34958,#34959,
#34960,#34961,#34962,#34963,#34964,#34965,#34966,#34967,#34968,#34969,#34970,
#34971,#34972,#34973,#34974,#34975,#34976,#34977,#34978,#34979,#34980,#34981,
#34982,#34983,#34984,#34985,#34986,#34987,#34988,#34989,#34990,#34991,#34992,
#34993,#34994,#34995,#34996,#34997,#34998,#34999,#35000,#35001,#35002,#35003,
#35004,#35005,#35006,#35007,#35008,#35009,#35010,#35011,#35012,#35013,#35014,
#35015,#35016,#35017,#35018,#35019,#35020,#35021,#35022,#35023,#35024,#35025,
#35026,#35027,#35028,#35029,#35030,#35031,#35032,#35033,#35034,#35035,#35036,
#35037,#35038,#35039,#35040,#35041,#35042,#35043,#35044,#35045,#35046,#35047,
#35048,#35049,#35050,#35051,#35052,#35053,#35054,#35055,#35056,#35057,#35058,
#35059,#35060,#35061,#35062,#35063,#35064,#35065,#35066,#35067,#35068,#35069,
#35070,#35071,#35072,#35073,#35074,#35075,#35076,#35077,#35078,#35079,#35080,
#35081,#35082,#35083,#35084,#35085,#35086,#35087,#35088,#35089,#35090,#35091,
#35092,#35093,#35094,#35095,#35096,#35097,#35098,#35099,#35100,#35101,#35102,
#35103,#35104,#35105,#35106,#35107,#35108,#35109,#35110,#35111,#35112,#35113,
#35114,#35115,#35116,#35117,#35118,#35119,#35120,#35121,#35122,#35123,#35124,
#35125,#35126,#35127,#35128,#35129,#35130,#35131,#35132,#35133,#35134,#35135,
#35136,#35137,#35138,#35139,#35140,#35141,#35142,#35143,#35144,#35145,#35146,
#35147,#35148,#35149,#35150,#35151,#35152,#35153,#35154,#35155,#35156,#35157,
#35158,#35159,#35160,#35161,#35162,#35163,#35164,#35165,#35166,#35167,#35168,
#35169,#35170,#35171,#35172,#35173,#35174,#35175,#35176,#35177,#35178,#35179,
#35180,#35181,#35182,#35183,#35184,#35185,#35186,#35187,#35188,#35189,#35190,
#35191,#35192,#35193,#35194,#35195,#35196,#35197,#35198,#35199,#35200,#35201,
#35202,#35203,#35204,#35205,#35206,#35207,#35208,#35209,#35210,#35211,#35212,
#35213,#35214,#35215,#35216,#35217,#35218,#35219,#35220,#35221,#35222,#35223,
#35224,#35225,#35226,#35227,#35228,#35229,#35230,#35231,#35232,#35233,#35234,
#35235,#35236,#35237,#35238,#35239,#35240,#35241,#35242,#35243,#35244,#35245,
#35246,#35247,#35248,#35249,#35250,#35251,#35252,#35253,#35254,#35255,#35256,
#35257,#35258,#35259,#35260,#35261,#35262,#35263,#35264,#35265,#35266,#35267,
#35268,#35269,#35270,#35271,#35272,#35273,#35274,#35275,#35276,#35277,#35278,
#35279,#35280,#35281,#35282,#35283,#35284,#35285,#35286,#35287,#35288,#35289,
#35290,#35291,#35292,#35293,#35294,#35295,#35296,#35297,#35298,#35299,#35300,
#35301,#35302,#35303,#35304,#35305,#35306,#35307,#35308),(#35309,#35310,
#35311,#35312,#35313,#35314,#35315,#35316,#35317,#35318,#35319,#35320,#35321,
#35322,#35323,#35324,#35325,#35326,#35327,#35328,#35329,#35330,#35331,#35332,
#35333,#35334,#35335,#35336,#35337,#35338,#35339,#35340,#35341,#35342,#35343,
#35344,#35345,#35346,#35347,#35348,#35349,#35350,#35351,#35352,#35353,#35354,
#35355,#35356,#35357,#35358,#35359,#35360,#35361,#35362,#35363,#35364,#35365,
#35366,#35367,#35368,#35369,#35370,#35371,#35372,#35373,#35374,#35375,#35376,
#35377,#35378,#35379,#35380,#35381,#35382,#35383,#35384,#35385,#35386,#35387,
#35388,#35389,#35390,#35391,#35392,#35393,#35394,#35395,#35396,#35397,#35398,
#35399,#35400,#35401,#35402,#35403,#35404,#35405,#35406,#35407,#35408,#35409,
#35410,#35411,#35412,#35413,#35414,#35415,#35416,#35417,#35418,#35419,#35420,
#35421,#35422,#35423,#35424,#35425,#35426,#35427,#35428,#35429,#35430,#35431,
#35432,#35433,#35434,#35435,#35436,#35437,#35438,#35439,#35440,#35441,#35442,
#35443,#35444,#35445,#35446,#35447,#35448,#35449,#35450,#35451,#35452,#35453,
#35454,#35455,#35456,#35457,#35458,#35459,#35460,#35461,#35462,#35463,#35464,
#35465,#35466,#35467,#35468,#35469,#35470,#35471,#35472,#35473,#35474,#35475,
#35476,#35477,#35478,#35479,#35480,#35481,#35482,#35483,#35484,#35485,#35486,
#35487,#35488,#35489,#35490,#35491,#35492,#35493,#35494,#35495,#35496,#35497,
#35498,#35499,#35500,#35501,#35502,#35503,#35504,#35505,#35506,#35507,#35508,
#35509,#35510,#35511,#35512,#35513,#35514,#35515,#35516,#35517,#35518,#35519,
#35520,#35521,#35522,#35523,#35524,#35525,#35526,#35527,#35528,#35529,#35530,
#35531,#35532,#35533,#35534,#35535,#35536,#35537,#35538,#35539,#35540,#35541,
#35542,#35543,#35544,#35545,#35546,#35547,#35548,#35549,#35550,#35551,#35552,
#35553,#35554,#35555,#35556,#35557,#35558,#35559,#35560,#35561,#35562,#35563,
#35564,#35565,#35566,#35567,#35568,#35569,#35570,#35571,#35572,#35573,#35574,
#35575,#35576,#35577,#35578,#35579,#35580,#35581,#35582,#35583,#35584,#35585,
#35586,#35587,#35588,#35589,#35590,#35591,#35592,#35593,#35594,#35595,#35596,
#35597,#35598,#35599,#35600,#35601,#35602,#35603,#35604,#35605,#35606,#35607,
#35608,#35609,#35610,#35611,#35612,#35613,#35614,#35615,#35616,#35617,#35618,
#35619,#35620,#35621,#35622,#35623,#35624,#35625,#35626,#35627,#35628,#35629,
#35630,#35631,#35632,#35633,#35634,#35635,#35636,#35637,#35638,#35639,#35640,
#35641,#35642,#35643,#35644,#35645,#35646,#35647,#35648,#35649,#35650,#35651,
#35652,#35653,#35654,#35655,#35656,#35657,#35658,#35659,#35660,#35661,#35662,
#35663,#35664,#35665,#35666,#35667,#35668,#35669,#35670,#35671)),
 .UNSPECIFIED.,.F.,.F.,.F.,(4,4),(4,1,1,1,1,1,1,1,1,1,1,1,1,1,1,1,1,1,1,
1,1,1,1,1,1,1,1,1,1,1,1,1,1,1,1,1,1,1,1,1,1,1,1,1,1,1,1,1,1,1,1,1,1,1,1,
1,1,1,1,1,1,1,1,1,1,1,1,1,1,1,1,1,1,1,1,1,1,1,1,1,1,1,1,1,1,1,1,1,1,1,1,
1,1,1,1,1,1,1,1,1,1,1,1,1,1,1,1,1,1,1,1,1,1,1,1,1,1,1,1,1,1,1,1,1,1,1,1,
1,1,1,1,1,1,1,1,1,1,1,1,1,1,1,1,1,1,1,1,1,1,1,1,1,1,1,1,1,1,1,1,1,1,1,1,
1,1,1,1,1,1,1,1,1,1,1,1,1,1,1,1,1,1,1,1,1,1,1,1,1,1,1,1,1,1,1,1,1,1,1,1,
1,1,1,1,1,1,1,1,1,1,1,1,1,1,1,1,1,1,1,1,1,1,1,1,1,1,1,1,1,1,1,1,1,1,1,1,
1,1,1,1,1,1,1,1,1,1,1,1,1,1,1,1,1,1,1,1,1,1,1,1,1,1,1,1,1,1,1,1,1,1,1,1,
1,1,1,1,1,1,1,1,1,1,1,1,1,1,1,1,1,1,1,1,1,1,1,1,1,1,1,1,1,1,1,1,1,1,1,1,
1,1,1,1,1,1,1,1,1,1,1,1,1,1,1,1,1,1,1,1,1,1,1,1,1,1,1,1,1,1,1,1,1,1,1,1,
1,1,1,1,1,1,1,1,1,1,1,1,1,1,1,1,1,4),(-4.46121474024446E-5,0.115356621383595),
(11.6153617464843,12.1145577438013,12.6136939684918,13.1128301931823,13.6119664178728,
14.1111026425634,14.6102388672539,15.1093750919444,15.608511316635,16.1076475413255,
16.606783766016,17.1059199907065,17.6050562153971,18.1041924400876,18.6033286647781,
19.1024648894686,19.6016011141592,20.1007373388497,20.5998735635402,21.0990097882307,
21.5981460129213,22.0972822376118,22.5964184623023,23.0955546869928,23.5946909116834,
24.0938271363739,24.5929633610644,25.092099585755,25.5912358104455,26.090372035136,
26.5895082598265,27.0886444845171,27.5877807092076,28.0869169338981,28.5860531585886,
29.0851893832792,29.5843256079697,30.0834618326602,30.5825980573507,31.0817342820413,
31.5808705067318,32.0800067314223,32.5791429561128,33.0782791808034,33.5774154054939,
34.0765516301844,34.575687854875,35.0748240795655,35.573960304256,36.0730965289465,
36.5722327536371,37.0713689783276,37.5705052030181,38.0696414277086,38.5687776523992,
39.0679138770897,39.5670501017802,40.0661863264707,40.5653225511613,41.0644587758518,
41.5635950005423,42.0627312252329,42.5618674499234,43.0610036746139,43.5601398993044,
44.059276123995,44.5584123486855,45.057548573376,45.5566847980665,46.0558210227571,
46.5549572474476,47.0540934721381,47.5532296968286,48.0523659215192,48.5515021462097,
49.0506383709002,49.5497745955907,50.0489108202813,50.5480470449718,51.0471832696623,
51.5463194943529,52.0454557190434,52.5445919437339,53.0437281684244,53.542864393115,
54.0420006178055,54.541136842496,55.0402730671865,55.5394092918771,56.0385455165676,
56.5376817412581,57.0368179659486,57.5359541906392,58.0350904153297,58.5342266400202,
59.0333628647107,59.5324990894013,60.0316353140918,60.5307715387823,61.0299077634728,
61.5290439881634,62.0281802128539,62.5273164375444,63.026452662235,63.5255888869255,
64.024725111616,64.5238613363065,65.0229975609971,65.5221337856876,66.0212700103781,
66.5204062350686,67.0195424597592,67.5186786844497,68.0178149091402,68.5169511338307,
69.0160873585213,69.5152235832118,70.0143598079023,70.5134960325929,71.0126322572834,
71.5117684819739,72.0109047066644,72.510040931355,73.0091771560455,73.508313380736,
74.0074496054265,74.5065858301171,75.0057220548076,75.5048582794981,76.0039945041887,
76.5031307288792,77.0022669535697,77.5014031782602,78.0005394029507,78.4996756276413,
78.9988118523318,79.4979480770223,79.9970843017128,80.4962205264034,80.9953567510939,
81.4944929757844,81.993629200475,82.4927654251655,82.991901649856,83.4910378745465,
83.9901740992371,84.4893103239276,84.9884465486181,85.4875827733086,85.9867189979992,
86.4858552226897,86.9849914473802,87.4841276720708,87.9832638967613,88.4824001214518,
88.9815363461423,89.4806725708329,89.9798087955234,90.4789450202139,90.9780812449044,
91.477217469595,91.9763536942855,92.475489918976,92.9746261436665,93.4737623683571,
93.9728985930476,94.4720348177381,94.9711710424286,95.4703072671192,95.9694434918097,
96.4685797165002,96.9677159411908,97.4668521658813,97.9659883905718,98.4651246152623,
98.9642608399529,99.4633970646434,99.9625332893339,100.461669514024,100.960805738715,
101.459941963405,101.959078188096,102.458214412787,102.957350637477,103.456486862168,
103.955623086858,104.454759311549,104.953895536239,105.45303176093,105.95216798562,
106.451304210311,106.950440435001,107.449576659692,107.948712884382,108.447849109073,
108.946985333763,109.446121558454,109.945257783144,110.444394007835,110.943530232525,
111.442666457216,111.941802681907,112.440938906597,112.940075131288,113.439211355978,
113.938347580669,114.437483805359,114.93662003005,115.43575625474,115.934892479431,
116.434028704121,116.933164928812,117.432301153502,117.931437378193,118.430573602883,
118.929709827574,119.428846052264,119.927982276955,120.427118501645,120.926254726336,
121.425390951027,121.924527175717,122.423663400408,122.922799625098,123.421935849789,
123.921072074479,124.42020829917,124.91934452386,125.418480748551,125.917616973241,
126.416753197932,126.915889422622,127.415025647313,127.914161872003,128.413298096694,
128.912434321384,129.411570546075,129.910706770766,130.409842995456,130.908979220147,
131.408115444837,131.907251669528,132.406387894218,132.905524118909,133.404660343599,
133.90379656829,134.40293279298,134.902069017671,135.401205242361,135.900341467052,
136.399477691742,136.898613916433,137.397750141123,137.896886365814,138.396022590504,
138.895158815195,139.394295039885,139.893431264576,140.392567489267,140.891703713957,
141.390839938648,141.889976163338,142.389112388029,142.888248612719,143.38738483741,
143.8865210621,144.385657286791,144.884793511481,145.383929736172,145.883065960862,
146.382202185553,146.881338410243,147.380474634934,147.879610859624,148.378747084315,
148.877883309006,149.377019533696,149.876155758387,150.375291983077,150.874428207768,
151.373564432458,151.872700657149,152.371836881839,152.87097310653,153.37010933122,
153.869245555911,154.368381780601,154.867518005292,155.366654229982,155.865790454673,
156.364926679363,156.864062904054,157.363199128744,157.862335353435,158.361471578126,
158.860607802816,159.359744027507,159.858880252197,160.358016476888,160.857152701578,
161.356288926269,161.855425150959,162.35456137565,162.85369760034,163.352833825031,
163.851970049721,164.351106274412,164.850242499102,165.349378723793,165.848514948483,
166.347651173174,166.846787397864,167.345923622555,167.845059847246,168.344196071936,
168.843332296627,169.342468521317,169.841604746008,170.340740970698,170.839877195389,
171.339013420079,171.83814964477,172.33728586946,172.836422094151,173.335558318841,
173.834694543532,174.333830768222,174.832966992913,175.332103217603,175.831239442294,
176.330375666984,176.829511891675,177.328648116366,177.827784341056,178.326920565747,
178.826056790437,179.325193015128,179.824329239818,180.323465464509,180.822601689199,
181.32173791389,181.82087413858,182.320010363271,182.819146587961,183.318282812652,
183.817419037342,184.316555262033,184.815691486723,185.314827711414,185.813963936104,
186.313100160795,186.812236385486,187.311372610176,187.810508834867,188.309645059557,
188.808781284248,189.307917508938,189.807053733629,190.306189958319,190.80532618301,
191.3044624077),.UNSPECIFIED.);
#151=B_SPLINE_SURFACE_WITH_KNOTS('',3,3,((#35779,#35780,#35781,#35782,#35783,
#35784,#35785,#35786,#35787,#35788,#35789,#35790,#35791,#35792,#35793,#35794,
#35795,#35796,#35797,#35798,#35799,#35800,#35801,#35802,#35803,#35804,#35805,
#35806,#35807,#35808,#35809,#35810,#35811,#35812,#35813,#35814,#35815,#35816,
#35817,#35818,#35819,#35820,#35821,#35822,#35823,#35824,#35825,#35826,#35827,
#35828,#35829,#35830,#35831,#35832,#35833,#35834,#35835,#35836,#35837,#35838,
#35839,#35840,#35841,#35842,#35843,#35844,#35845,#35846,#35847,#35848,#35849,
#35850,#35851,#35852,#35853,#35854,#35855,#35856,#35857,#35858,#35859,#35860,
#35861,#35862,#35863,#35864,#35865,#35866,#35867,#35868,#35869,#35870,#35871,
#35872,#35873,#35874,#35875,#35876,#35877,#35878,#35879,#35880,#35881,#35882,
#35883,#35884,#35885,#35886,#35887,#35888,#35889,#35890,#35891,#35892,#35893,
#35894,#35895,#35896,#35897,#35898,#35899,#35900,#35901,#35902,#35903,#35904,
#35905,#35906,#35907,#35908,#35909,#35910,#35911,#35912,#35913,#35914,#35915,
#35916,#35917,#35918,#35919,#35920,#35921,#35922,#35923,#35924,#35925,#35926,
#35927,#35928,#35929,#35930,#35931,#35932,#35933,#35934,#35935,#35936,#35937,
#35938,#35939,#35940,#35941,#35942,#35943,#35944,#35945,#35946,#35947,#35948,
#35949,#35950,#35951,#35952,#35953,#35954,#35955,#35956,#35957,#35958,#35959,
#35960,#35961,#35962,#35963,#35964,#35965,#35966,#35967,#35968,#35969,#35970,
#35971,#35972,#35973,#35974,#35975,#35976,#35977,#35978,#35979,#35980,#35981,
#35982,#35983,#35984,#35985,#35986,#35987,#35988,#35989,#35990,#35991,#35992,
#35993,#35994,#35995,#35996,#35997,#35998,#35999,#36000,#36001,#36002,#36003,
#36004,#36005,#36006,#36007,#36008,#36009,#36010,#36011,#36012,#36013,#36014,
#36015,#36016,#36017,#36018,#36019,#36020,#36021,#36022,#36023,#36024,#36025,
#36026,#36027,#36028,#36029,#36030,#36031,#36032,#36033,#36034,#36035,#36036,
#36037,#36038,#36039,#36040,#36041,#36042,#36043,#36044,#36045,#36046,#36047,
#36048,#36049,#36050,#36051,#36052,#36053,#36054,#36055,#36056,#36057,#36058,
#36059,#36060,#36061,#36062,#36063,#36064,#36065,#36066,#36067,#36068,#36069,
#36070,#36071,#36072,#36073,#36074,#36075,#36076,#36077,#36078,#36079,#36080,
#36081,#36082,#36083,#36084,#36085,#36086,#36087,#36088,#36089,#36090,#36091,
#36092,#36093,#36094,#36095,#36096,#36097,#36098,#36099,#36100,#36101,#36102,
#36103,#36104,#36105,#36106,#36107,#36108,#36109,#36110,#36111,#36112,#36113,
#36114,#36115,#36116,#36117,#36118,#36119,#36120,#36121,#36122,#36123,#36124,
#36125,#36126,#36127,#36128,#36129,#36130,#36131,#36132,#36133,#36134,#36135,
#36136,#36137,#36138,#36139,#36140,#36141,#36142,#36143,#36144,#36145),
(#36146,#36147,#36148,#36149,#36150,#36151,#36152,#36153,#36154,#36155,
#36156,#36157,#36158,#36159,#36160,#36161,#36162,#36163,#36164,#36165,#36166,
#36167,#36168,#36169,#36170,#36171,#36172,#36173,#36174,#36175,#36176,#36177,
#36178,#36179,#36180,#36181,#36182,#36183,#36184,#36185,#36186,#36187,#36188,
#36189,#36190,#36191,#36192,#36193,#36194,#36195,#36196,#36197,#36198,#36199,
#36200,#36201,#36202,#36203,#36204,#36205,#36206,#36207,#36208,#36209,#36210,
#36211,#36212,#36213,#36214,#36215,#36216,#36217,#36218,#36219,#36220,#36221,
#36222,#36223,#36224,#36225,#36226,#36227,#36228,#36229,#36230,#36231,#36232,
#36233,#36234,#36235,#36236,#36237,#36238,#36239,#36240,#36241,#36242,#36243,
#36244,#36245,#36246,#36247,#36248,#36249,#36250,#36251,#36252,#36253,#36254,
#36255,#36256,#36257,#36258,#36259,#36260,#36261,#36262,#36263,#36264,#36265,
#36266,#36267,#36268,#36269,#36270,#36271,#36272,#36273,#36274,#36275,#36276,
#36277,#36278,#36279,#36280,#36281,#36282,#36283,#36284,#36285,#36286,#36287,
#36288,#36289,#36290,#36291,#36292,#36293,#36294,#36295,#36296,#36297,#36298,
#36299,#36300,#36301,#36302,#36303,#36304,#36305,#36306,#36307,#36308,#36309,
#36310,#36311,#36312,#36313,#36314,#36315,#36316,#36317,#36318,#36319,#36320,
#36321,#36322,#36323,#36324,#36325,#36326,#36327,#36328,#36329,#36330,#36331,
#36332,#36333,#36334,#36335,#36336,#36337,#36338,#36339,#36340,#36341,#36342,
#36343,#36344,#36345,#36346,#36347,#36348,#36349,#36350,#36351,#36352,#36353,
#36354,#36355,#36356,#36357,#36358,#36359,#36360,#36361,#36362,#36363,#36364,
#36365,#36366,#36367,#36368,#36369,#36370,#36371,#36372,#36373,#36374,#36375,
#36376,#36377,#36378,#36379,#36380,#36381,#36382,#36383,#36384,#36385,#36386,
#36387,#36388,#36389,#36390,#36391,#36392,#36393,#36394,#36395,#36396,#36397,
#36398,#36399,#36400,#36401,#36402,#36403,#36404,#36405,#36406,#36407,#36408,
#36409,#36410,#36411,#36412,#36413,#36414,#36415,#36416,#36417,#36418,#36419,
#36420,#36421,#36422,#36423,#36424,#36425,#36426,#36427,#36428,#36429,#36430,
#36431,#36432,#36433,#36434,#36435,#36436,#36437,#36438,#36439,#36440,#36441,
#36442,#36443,#36444,#36445,#36446,#36447,#36448,#36449,#36450,#36451,#36452,
#36453,#36454,#36455,#36456,#36457,#36458,#36459,#36460,#36461,#36462,#36463,
#36464,#36465,#36466,#36467,#36468,#36469,#36470,#36471,#36472,#36473,#36474,
#36475,#36476,#36477,#36478,#36479,#36480,#36481,#36482,#36483,#36484,#36485,
#36486,#36487,#36488,#36489,#36490,#36491,#36492,#36493,#36494,#36495,#36496,
#36497,#36498,#36499,#36500,#36501,#36502,#36503,#36504,#36505,#36506,#36507,
#36508,#36509,#36510,#36511,#36512),(#36513,#36514,#36515,#36516,#36517,
#36518,#36519,#36520,#36521,#36522,#36523,#36524,#36525,#36526,#36527,#36528,
#36529,#36530,#36531,#36532,#36533,#36534,#36535,#36536,#36537,#36538,#36539,
#36540,#36541,#36542,#36543,#36544,#36545,#36546,#36547,#36548,#36549,#36550,
#36551,#36552,#36553,#36554,#36555,#36556,#36557,#36558,#36559,#36560,#36561,
#36562,#36563,#36564,#36565,#36566,#36567,#36568,#36569,#36570,#36571,#36572,
#36573,#36574,#36575,#36576,#36577,#36578,#36579,#36580,#36581,#36582,#36583,
#36584,#36585,#36586,#36587,#36588,#36589,#36590,#36591,#36592,#36593,#36594,
#36595,#36596,#36597,#36598,#36599,#36600,#36601,#36602,#36603,#36604,#36605,
#36606,#36607,#36608,#36609,#36610,#36611,#36612,#36613,#36614,#36615,#36616,
#36617,#36618,#36619,#36620,#36621,#36622,#36623,#36624,#36625,#36626,#36627,
#36628,#36629,#36630,#36631,#36632,#36633,#36634,#36635,#36636,#36637,#36638,
#36639,#36640,#36641,#36642,#36643,#36644,#36645,#36646,#36647,#36648,#36649,
#36650,#36651,#36652,#36653,#36654,#36655,#36656,#36657,#36658,#36659,#36660,
#36661,#36662,#36663,#36664,#36665,#36666,#36667,#36668,#36669,#36670,#36671,
#36672,#36673,#36674,#36675,#36676,#36677,#36678,#36679,#36680,#36681,#36682,
#36683,#36684,#36685,#36686,#36687,#36688,#36689,#36690,#36691,#36692,#36693,
#36694,#36695,#36696,#36697,#36698,#36699,#36700,#36701,#36702,#36703,#36704,
#36705,#36706,#36707,#36708,#36709,#36710,#36711,#36712,#36713,#36714,#36715,
#36716,#36717,#36718,#36719,#36720,#36721,#36722,#36723,#36724,#36725,#36726,
#36727,#36728,#36729,#36730,#36731,#36732,#36733,#36734,#36735,#36736,#36737,
#36738,#36739,#36740,#36741,#36742,#36743,#36744,#36745,#36746,#36747,#36748,
#36749,#36750,#36751,#36752,#36753,#36754,#36755,#36756,#36757,#36758,#36759,
#36760,#36761,#36762,#36763,#36764,#36765,#36766,#36767,#36768,#36769,#36770,
#36771,#36772,#36773,#36774,#36775,#36776,#36777,#36778,#36779,#36780,#36781,
#36782,#36783,#36784,#36785,#36786,#36787,#36788,#36789,#36790,#36791,#36792,
#36793,#36794,#36795,#36796,#36797,#36798,#36799,#36800,#36801,#36802,#36803,
#36804,#36805,#36806,#36807,#36808,#36809,#36810,#36811,#36812,#36813,#36814,
#36815,#36816,#36817,#36818,#36819,#36820,#36821,#36822,#36823,#36824,#36825,
#36826,#36827,#36828,#36829,#36830,#36831,#36832,#36833,#36834,#36835,#36836,
#36837,#36838,#36839,#36840,#36841,#36842,#36843,#36844,#36845,#36846,#36847,
#36848,#36849,#36850,#36851,#36852,#36853,#36854,#36855,#36856,#36857,#36858,
#36859,#36860,#36861,#36862,#36863,#36864,#36865,#36866,#36867,#36868,#36869,
#36870,#36871,#36872,#36873,#36874,#36875,#36876,#36877,#36878,#36879),
(#36880,#36881,#36882,#36883,#36884,#36885,#36886,#36887,#36888,#36889,
#36890,#36891,#36892,#36893,#36894,#36895,#36896,#36897,#36898,#36899,#36900,
#36901,#36902,#36903,#36904,#36905,#36906,#36907,#36908,#36909,#36910,#36911,
#36912,#36913,#36914,#36915,#36916,#36917,#36918,#36919,#36920,#36921,#36922,
#36923,#36924,#36925,#36926,#36927,#36928,#36929,#36930,#36931,#36932,#36933,
#36934,#36935,#36936,#36937,#36938,#36939,#36940,#36941,#36942,#36943,#36944,
#36945,#36946,#36947,#36948,#36949,#36950,#36951,#36952,#36953,#36954,#36955,
#36956,#36957,#36958,#36959,#36960,#36961,#36962,#36963,#36964,#36965,#36966,
#36967,#36968,#36969,#36970,#36971,#36972,#36973,#36974,#36975,#36976,#36977,
#36978,#36979,#36980,#36981,#36982,#36983,#36984,#36985,#36986,#36987,#36988,
#36989,#36990,#36991,#36992,#36993,#36994,#36995,#36996,#36997,#36998,#36999,
#37000,#37001,#37002,#37003,#37004,#37005,#37006,#37007,#37008,#37009,#37010,
#37011,#37012,#37013,#37014,#37015,#37016,#37017,#37018,#37019,#37020,#37021,
#37022,#37023,#37024,#37025,#37026,#37027,#37028,#37029,#37030,#37031,#37032,
#37033,#37034,#37035,#37036,#37037,#37038,#37039,#37040,#37041,#37042,#37043,
#37044,#37045,#37046,#37047,#37048,#37049,#37050,#37051,#37052,#37053,#37054,
#37055,#37056,#37057,#37058,#37059,#37060,#37061,#37062,#37063,#37064,#37065,
#37066,#37067,#37068,#37069,#37070,#37071,#37072,#37073,#37074,#37075,#37076,
#37077,#37078,#37079,#37080,#37081,#37082,#37083,#37084,#37085,#37086,#37087,
#37088,#37089,#37090,#37091,#37092,#37093,#37094,#37095,#37096,#37097,#37098,
#37099,#37100,#37101,#37102,#37103,#37104,#37105,#37106,#37107,#37108,#37109,
#37110,#37111,#37112,#37113,#37114,#37115,#37116,#37117,#37118,#37119,#37120,
#37121,#37122,#37123,#37124,#37125,#37126,#37127,#37128,#37129,#37130,#37131,
#37132,#37133,#37134,#37135,#37136,#37137,#37138,#37139,#37140,#37141,#37142,
#37143,#37144,#37145,#37146,#37147,#37148,#37149,#37150,#37151,#37152,#37153,
#37154,#37155,#37156,#37157,#37158,#37159,#37160,#37161,#37162,#37163,#37164,
#37165,#37166,#37167,#37168,#37169,#37170,#37171,#37172,#37173,#37174,#37175,
#37176,#37177,#37178,#37179,#37180,#37181,#37182,#37183,#37184,#37185,#37186,
#37187,#37188,#37189,#37190,#37191,#37192,#37193,#37194,#37195,#37196,#37197,
#37198,#37199,#37200,#37201,#37202,#37203,#37204,#37205,#37206,#37207,#37208,
#37209,#37210,#37211,#37212,#37213,#37214,#37215,#37216,#37217,#37218,#37219,
#37220,#37221,#37222,#37223,#37224,#37225,#37226,#37227,#37228,#37229,#37230,
#37231,#37232,#37233,#37234,#37235,#37236,#37237,#37238,#37239,#37240,#37241,
#37242,#37243,#37244,#37245,#37246)),.UNSPECIFIED.,.F.,.F.,.F.,(4,4),(4,
1,1,1,1,1,1,1,1,1,1,1,1,1,1,1,1,1,1,1,1,1,1,1,1,1,1,1,1,1,1,1,1,1,1,1,1,
1,1,1,1,1,1,1,1,1,1,1,1,1,1,1,1,1,1,1,1,1,1,1,1,1,1,1,1,1,1,1,1,1,1,1,1,
1,1,1,1,1,1,1,1,1,1,1,1,1,1,1,1,1,1,1,1,1,1,1,1,1,1,1,1,1,1,1,1,1,1,1,1,
1,1,1,1,1,1,1,1,1,1,1,1,1,1,1,1,1,1,1,1,1,1,1,1,1,1,1,1,1,1,1,1,1,1,1,1,
1,1,1,1,1,1,1,1,1,1,1,1,1,1,1,1,1,1,1,1,1,1,1,1,1,1,1,1,1,1,1,1,1,1,1,1,
1,1,1,1,1,1,1,1,1,1,1,1,1,1,1,1,1,1,1,1,1,1,1,1,1,1,1,1,1,1,1,1,1,1,1,1,
1,1,1,1,1,1,1,1,1,1,1,1,1,1,1,1,1,1,1,1,1,1,1,1,1,1,1,1,1,1,1,1,1,1,1,1,
1,1,1,1,1,1,1,1,1,1,1,1,1,1,1,1,1,1,1,1,1,1,1,1,1,1,1,1,1,1,1,1,1,1,1,1,
1,1,1,1,1,1,1,1,1,1,1,1,1,1,1,1,1,1,1,1,1,1,1,1,1,1,1,1,1,1,1,1,1,1,1,1,
1,1,1,1,1,1,1,1,1,1,1,1,1,1,1,1,1,1,1,1,1,1,1,1,1,1,1,1,1,1,1,1,1,1,1,1,
1,1,1,4),(-5.96503795939263E-5,0.115340908092672),(8.30592286723182,8.80479480237994,
9.30366673752807,9.80253867267619,10.3014106078243,10.8002825429724,11.2991544781206,
11.7980264132687,12.2968983484168,12.7957702835649,13.2946422187131,13.7935141538612,
14.2923860890093,14.7912580241574,15.2901299593056,15.7890018944537,16.2878738296018,
16.7867457647499,17.2856176998981,17.7844896350462,18.2833615701943,18.7822335053424,
19.2811054404905,19.7799773756387,20.2788493107868,20.7777212459349,21.276593181083,
21.7754651162312,22.2743370513793,22.7732089865274,23.2720809216755,23.7709528568237,
24.2698247919718,24.7686967271199,25.267568662268,25.7664405974162,26.2653125325643,
26.7641844677124,27.2630564028605,27.7619283380087,28.2608002731568,28.7596722083049,
29.258544143453,29.7574160786012,30.2562880137493,30.7551599488974,31.2540318840455,
31.7529038191936,32.2517757543418,32.7506476894899,33.249519624638,33.7483915597861,
34.2472634949343,34.7461354300824,35.2450073652305,35.7438793003786,36.2427512355268,
36.7416231706749,37.240495105823,37.7393670409711,38.2382389761193,38.7371109112674,
39.2359828464155,39.7348547815636,40.2337267167118,40.7325986518599,41.231470587008,
41.7303425221561,42.2292144573043,42.7280863924524,43.2269583276005,43.7258302627486,
44.2247021978968,44.7235741330449,45.222446068193,45.7213180033411,46.2201899384892,
46.7190618736374,47.2179338087855,47.7168057439336,48.2156776790817,48.7145496142299,
49.213421549378,49.7122934845261,50.2111654196742,50.7100373548224,51.2089092899705,
51.7077812251186,52.2066531602667,52.7055250954149,53.204397030563,53.7032689657111,
54.2021409008592,54.7010128360074,55.1998847711555,55.6987567063036,56.1976286414517,
56.6965005765999,57.195372511748,57.6942444468961,58.1931163820442,58.6919883171924,
59.1908602523405,59.6897321874886,60.1886041226367,60.6874760577848,61.186347992933,
61.6852199280811,62.1840918632292,62.6829637983773,63.1818357335255,63.6807076686736,
64.1795796038217,64.6784515389698,65.177323474118,65.6761954092661,66.1750673444142,
66.6739392795623,67.1728112147104,67.6716831498586,68.1705550850067,68.6694270201548,
69.168298955303,69.6671708904511,70.1660428255992,70.6649147607473,71.1637866958955,
71.6626586310436,72.1615305661917,72.6604025013398,73.1592744364879,73.6581463716361,
74.1570183067842,74.6558902419323,75.1547621770804,75.6536341122286,76.1525060473767,
76.6513779825248,77.1502499176729,77.6491218528211,78.1479937879692,78.6468657231173,
79.1457376582654,79.6446095934135,80.1434815285617,80.6423534637098,81.1412253988579,
81.640097334006,82.1389692691542,82.6378412043023,83.1367131394504,83.6355850745985,
84.1344570097467,84.6333289448948,85.1322008800429,85.631072815191,86.1299447503392,
86.6288166854873,87.1276886206354,87.6265605557835,88.1254324909317,88.6243044260798,
89.1231763612279,89.622048296376,90.1209202315242,90.6197921666723,91.1186641018204,
91.6175360369685,92.1164079721167,92.6152799072648,93.1141518424129,93.613023777561,
94.1118957127092,94.6107676478573,95.1096395830054,95.6085115181535,96.1073834533017,
96.6062553884498,97.1051273235979,97.603999258746,98.1028711938941,98.6017431290423,
99.1006150641904,99.5994869993385,100.098358934487,100.597230869635,101.096102804783,
101.594974739931,102.093846675079,102.592718610227,103.091590545375,103.590462480524,
104.089334415672,104.58820635082,105.087078285968,105.585950221116,106.084822156264,
106.583694091412,107.08256602656,107.581437961709,108.080309896857,108.579181832005,
109.078053767153,109.576925702301,110.075797637449,110.574669572597,111.073541507745,
111.572413442893,112.071285378042,112.57015731319,113.069029248338,113.567901183486,
114.066773118634,114.565645053782,115.06451698893,115.563388924078,116.062260859227,
116.561132794375,117.060004729523,117.558876664671,118.057748599819,118.556620534967,
119.055492470115,119.554364405263,120.053236340412,120.55210827556,121.050980210708,
121.549852145856,122.048724081004,122.547596016152,123.0464679513,123.545339886448,
124.044211821597,124.543083756745,125.041955691893,125.540827627041,126.039699562189,
126.538571497337,127.037443432485,127.536315367633,128.035187302782,128.53405923793,
129.032931173078,129.531803108226,130.030675043374,130.529546978522,131.02841891367,
131.527290848818,132.026162783967,132.525034719115,133.023906654263,133.522778589411,
134.021650524559,134.520522459707,135.019394394855,135.518266330003,136.017138265152,
136.5160102003,137.014882135448,137.513754070596,138.012626005744,138.511497940892,
139.01036987604,139.509241811188,140.008113746337,140.506985681485,141.005857616633,
141.504729551781,142.003601486929,142.502473422077,143.001345357225,143.500217292373,
143.999089227522,144.49796116267,144.996833097818,145.495705032966,145.994576968114,
146.493448903262,146.99232083841,147.491192773558,147.990064708707,148.488936643855,
148.987808579003,149.486680514151,149.985552449299,150.484424384447,150.983296319595,
151.482168254743,151.981040189892,152.47991212504,152.978784060188,153.477655995336,
153.976527930484,154.475399865632,154.97427180078,155.473143735928,155.972015671077,
156.470887606225,156.969759541373,157.468631476521,157.967503411669,158.466375346817,
158.965247281965,159.464119217113,159.962991152262,160.46186308741,160.960735022558,
161.459606957706,161.958478892854,162.457350828002,162.95622276315,163.455094698298,
163.953966633447,164.452838568595,164.951710503743,165.450582438891,165.949454374039,
166.448326309187,166.947198244335,167.446070179483,167.944942114632,168.44381404978,
168.942685984928,169.441557920076,169.940429855224,170.439301790372,170.93817372552,
171.437045660668,171.935917595817,172.434789530965,172.933661466113,173.432533401261,
173.931405336409,174.430277271557,174.929149206705,175.428021141853,175.926893077002,
176.42576501215,176.924636947298,177.423508882446,177.922380817594,178.421252752742,
178.92012468789,179.418996623038,179.917868558187,180.416740493335,180.915612428483,
181.414484363631,181.913356298779,182.412228233927,182.911100169075,183.409972104223,
183.908844039372,184.40771597452,184.906587909668,185.405459844816,185.904331779964,
186.403203715112,186.90207565026,187.400947585408,187.899819520556,188.398691455705,
188.897563390853,189.396435326001,189.895366911529),.UNSPECIFIED.);
#245=B_SPLINE_CURVE_WITH_KNOTS('',3,(#14172,#14173,#14174,#14175,#14176,
#14177,#14178,#14179,#14180,#14181,#14182,#14183,#14184,#14185,#14186,#14187,
#14188,#14189,#14190,#14191,#14192,#14193,#14194,#14195,#14196,#14197,#14198,
#14199,#14200,#14201,#14202,#14203,#14204,#14205,#14206,#14207,#14208,#14209,
#14210,#14211,#14212,#14213,#14214,#14215,#14216,#14217,#14218,#14219,#14220,
#14221,#14222,#14223,#14224,#14225,#14226,#14227,#14228,#14229,#14230,#14231,
#14232,#14233,#14234,#14235,#14236,#14237,#14238,#14239,#14240,#14241,#14242,
#14243,#14244,#14245,#14246,#14247),.UNSPECIFIED.,.F.,.F.,(4,3,3,3,3,3,
3,3,3,3,3,3,3,3,3,3,3,3,3,3,3,3,3,3,3,4),(-4.0925417488383,-4.00338655469883,
-3.99308979752421,-3.90920016748237,-3.82532702077677,-3.74145069821191,
-3.65757994399786,-3.57368718421055,-3.49395357283368,-3.4100720147821,
-3.32620694997733,-3.24233864749926,-3.15847586347122,-3.07459091498262,
-2.99481734814316,-2.91093267105568,-2.82706451995705,-2.74319321087022,
-2.65932746977074,-2.57543967428308,-2.49568112345263,-2.41211430491665,
-2.32654186004125,-2.24299415390576,-2.1564093396604,-2.06982452541504),
 .UNSPECIFIED.);
#246=B_SPLINE_CURVE_WITH_KNOTS('',3,(#14250,#14251,#14252,#14253,#14254,
#14255),.UNSPECIFIED.,.F.,.F.,(4,1,1,4),(0.,0.498871935148122,0.997743870296246,
1.11885509353771),.UNSPECIFIED.);
#247=B_SPLINE_CURVE_WITH_KNOTS('',3,(#14260,#14261,#14262,#14263,#14264,
#14265,#14266,#14267,#14268,#14269,#14270,#14271,#14272,#14273,#14274,#14275,
#14276,#14277,#14278,#14279,#14280,#14281,#14282,#14283,#14284,#14285,#14286,
#14287,#14288,#14289,#14290,#14291,#14292,#14293,#14294,#14295,#14296,#14297,
#14298,#14299,#14300,#14301,#14302,#14303,#14304,#14305,#14306,#14307,#14308,
#14309,#14310,#14311,#14312,#14313,#14314,#14315,#14316,#14317,#14318,#14319,
#14320,#14321,#14322,#14323,#14324,#14325,#14326,#14327,#14328,#14329,#14330,
#14331,#14332,#14333,#14334,#14335,#14336,#14337,#14338,#14339,#14340,#14341,
#14342,#14343,#14344,#14345,#14346,#14347,#14348,#14349,#14350,#14351,#14352,
#14353,#14354,#14355,#14356,#14357,#14358,#14359,#14360,#14361,#14362,#14363,
#14364,#14365,#14366,#14367,#14368,#14369,#14370,#14371,#14372,#14373,#14374,
#14375,#14376,#14377,#14378,#14379,#14380,#14381,#14382,#14383,#14384,#14385,
#14386,#14387,#14388,#14389,#14390,#14391,#14392,#14393,#14394,#14395,#14396,
#14397,#14398,#14399,#14400,#14401,#14402,#14403,#14404,#14405,#14406,#14407,
#14408,#14409,#14410,#14411,#14412,#14413,#14414,#14415,#14416,#14417,#14418,
#14419,#14420,#14421,#14422,#14423,#14424,#14425,#14426,#14427,#14428,#14429,
#14430,#14431,#14432,#14433,#14434,#14435,#14436,#14437,#14438,#14439,#14440,
#14441,#14442,#14443,#14444,#14445,#14446,#14447,#14448,#14449,#14450,#14451,
#14452,#14453,#14454,#14455,#14456,#14457,#14458,#14459,#14460,#14461,#14462,
#14463,#14464,#14465,#14466,#14467,#14468,#14469,#14470,#14471,#14472,#14473,
#14474,#14475,#14476,#14477,#14478,#14479,#14480,#14481,#14482,#14483,#14484,
#14485,#14486,#14487,#14488),.UNSPECIFIED.,.F.,.F.,(4,3,3,3,3,3,3,3,3,3,
3,3,3,3,3,3,3,3,3,3,3,3,3,3,3,3,3,3,3,3,3,3,3,3,3,3,3,3,3,3,3,3,3,3,3,3,
3,3,3,3,3,3,3,3,3,3,3,3,3,3,3,3,3,3,3,3,3,3,3,3,3,3,3,3,3,3,4),(-10.3757270560179,
-10.2921698941946,-10.2086117681573,-10.1250584922855,-10.0414843439998,
-9.98272449381053,-9.8988388229379,-9.81496964470574,-9.73109726706072,
-9.64723043695178,-9.56334152922015,-9.48358826912,-9.39970259968953,-9.31583342289778,
-9.23196104667645,-9.14809421797911,-9.06420531162583,-8.98445204442947,
-8.90056637659468,-8.81669720141806,-8.73282482682699,-8.64895799976509,
-8.56506909503931,-8.48531581973895,-8.40143014094074,-8.31756095474053,
-8.23368856913816,-8.14982173109376,-8.06593281553891,-7.98617959504842,
-7.90229394774752,-7.81842479317629,-7.73455243910345,-7.65068563247056,
-7.56679674783129,-7.4870433703579,-7.40315765686906,-7.31928843588881,
-7.23541601570045,-7.15154914324569,-7.06766019390088,-6.98790714566737,
-6.90402153903721,-6.82015242517192,-6.73628011147098,-6.6524133449469,
-6.56852449959617,-6.48877092097684,-6.40488520025293,-6.32101597225773,
-6.23714354545871,-6.1532766666274,-6.06938771135321,-5.98963469628632,
-5.9057489595102,-5.82187971461069,-5.73800726976125,-5.65414037229036,
-5.57025139758467,-5.49049847159579,-5.4066132244952,-5.32274447232866,
-5.23887252021098,-5.15500611447788,-5.07111762514282,-4.99136224690526,
-4.90747538257756,-4.82360500594776,-4.73973143373954,-4.65586341356851,
-4.57197333463933,-4.49222602221474,-4.40866870611299,-4.32512134153701,
-4.24158525877463,-4.15803693785589,-4.09254174894968),.UNSPECIFIED.);
#248=B_SPLINE_CURVE_WITH_KNOTS('',3,(#14489,#14490,#14491,#14492,#14493,
#14494,#14495,#14496,#14497,#14498,#14499,#14500,#14501,#14502,#14503,#14504),
 .UNSPECIFIED.,.F.,.F.,(4,1,1,1,1,1,1,1,1,1,1,1,1,4),(1.11885509353771,
1.49661580544437,1.9954877405925,2.49435967574062,2.99323161088875,3.49210354603688,
3.990975481185,4.48984741633313,4.98871935148126,5.48759128662938,5.98646322177751,
6.48533515692564,6.98420709207376,7.4020404007173),.UNSPECIFIED.);
#249=B_SPLINE_CURVE_WITH_KNOTS('',3,(#14509,#14510,#14511,#14512,#14513,
#14514,#14515,#14516,#14517,#14518,#14519,#14520,#14521,#14522,#14523,#14524,
#14525),.UNSPECIFIED.,.F.,.F.,(4,1,1,1,1,1,1,1,1,1,1,1,1,1,4),(-16.6589123270017,
-16.4714954147874,-15.9723591900968,-15.4732229654063,-14.9740867407158,
-14.4749505160253,-13.9758142913347,-13.4766780666442,-12.9775418419537,
-12.4784056172632,-11.9792693925726,-11.4801331678821,-10.9809969431916,
-10.4818607185011,-10.3757270560179),.UNSPECIFIED.);
#250=B_SPLINE_CURVE_WITH_KNOTS('',3,(#14526,#14527,#14528,#14529,#14530,
#14531,#14532,#14533,#14534,#14535,#14536,#14537,#14538,#14539,#14540,#14541,
#14542),.UNSPECIFIED.,.F.,.F.,(4,1,1,1,1,1,1,1,1,1,1,1,1,1,4),(7.4020404007173,
7.48307902722189,7.98195096237001,8.48082289751813,8.97969483266625,9.47856676781438,
9.9774387029625,10.4763106381106,10.9751825732587,11.4740545084069,11.972926443555,
12.4717983787031,12.9706703138512,13.4695422489993,13.6852256829822),
 .UNSPECIFIED.);
#251=B_SPLINE_CURVE_WITH_KNOTS('',3,(#14547,#14548,#14549,#14550,#14551,
#14552,#14553,#14554,#14555,#14556,#14557,#14558,#14559,#14560,#14561,#14562,
#14563,#14564,#14565,#14566,#14567,#14568,#14569,#14570,#14571,#14572,#14573,
#14574,#14575,#14576,#14577,#14578,#14579,#14580,#14581,#14582,#14583,#14584,
#14585,#14586,#14587,#14588,#14589,#14590,#14591,#14592,#14593,#14594,#14595,
#14596,#14597,#14598,#14599,#14600,#14601,#14602,#14603,#14604,#14605,#14606,
#14607,#14608,#14609,#14610,#14611,#14612,#14613,#14614,#14615,#14616,#14617,
#14618,#14619,#14620,#14621,#14622,#14623,#14624,#14625,#14626,#14627,#14628,
#14629,#14630,#14631,#14632,#14633,#14634,#14635,#14636,#14637,#14638,#14639,
#14640,#14641,#14642,#14643,#14644,#14645,#14646,#14647,#14648,#14649,#14650,
#14651,#14652,#14653,#14654,#14655,#14656,#14657,#14658,#14659,#14660,#14661,
#14662,#14663,#14664,#14665,#14666,#14667,#14668,#14669,#14670,#14671,#14672,
#14673,#14674,#14675,#14676,#14677,#14678,#14679,#14680,#14681,#14682,#14683,
#14684,#14685,#14686,#14687,#14688,#14689,#14690,#14691,#14692,#14693,#14694,
#14695,#14696,#14697,#14698,#14699,#14700,#14701,#14702,#14703,#14704,#14705,
#14706,#14707,#14708,#14709,#14710,#14711,#14712,#14713,#14714,#14715,#14716,
#14717,#14718,#14719,#14720,#14721,#14722,#14723,#14724,#14725,#14726,#14727,
#14728,#14729,#14730,#14731,#14732,#14733,#14734,#14735,#14736,#14737,#14738,
#14739,#14740,#14741,#14742,#14743,#14744,#14745,#14746,#14747,#14748,#14749,
#14750,#14751,#14752,#14753,#14754,#14755,#14756,#14757,#14758,#14759,#14760,
#14761,#14762,#14763,#14764,#14765,#14766,#14767,#14768,#14769,#14770,#14771,
#14772,#14773,#14774,#14775),.UNSPECIFIED.,.F.,.F.,(4,3,3,3,3,3,3,3,3,3,
3,3,3,3,3,3,3,3,3,3,3,3,3,3,3,3,3,3,3,3,3,3,3,3,3,3,3,3,3,3,3,3,3,3,3,3,
3,3,3,3,3,3,3,3,3,3,3,3,3,3,3,3,3,3,3,3,3,3,3,3,3,3,3,3,3,3,4),(-22.9420976702851,
-22.8583444588836,-22.7746078996228,-22.6908686933099,-22.6071340014371,
-22.5233784473718,-22.4611301110737,-22.37724444117,-22.2933752639082,-22.2095028872263,
-22.1256360580747,-22.0417471512818,-21.9619938863832,-21.8781082164793,
-21.7942390392172,-21.7103666625351,-21.6264998333833,-21.54261092659,-21.4628576616926,
-21.3789719917889,-21.2951028145268,-21.2112304378449,-21.1273636086934,
-21.0434747019003,-20.9637214370021,-20.8798357670984,-20.7959665898365,
-20.7120942131547,-20.6282273840031,-20.5443384772101,-20.4645852123116,
-20.3806995424079,-20.2968303651459,-20.2129579884638,-20.1290911593122,
-20.045202252519,-19.9654489876211,-19.8815633177171,-19.797694140455,-19.713821763773,
-19.6299549346209,-19.5460660278276,-19.4663127629305,-19.3824270930267,
-19.2985579157645,-19.2146855390827,-19.1308187099311,-19.0469298031378,
-18.96717653824,-18.8832908683363,-18.7994216910748,-18.7155493143931,-18.6316824852416,
-18.5477935784487,-18.4680403135495,-18.3841546436457,-18.300285466383,
-18.2164130897008,-18.1325462605488,-18.0486573537555,-17.9689040888589,
-17.8850184189553,-17.801149241693,-17.717276865011,-17.6334100358592,-17.5495211290661,
-17.4697678641684,-17.3858821942648,-17.3020130170031,-17.2181406403213,
-17.1342738111701,-17.0503849043771,-16.9706316394779,-16.8865508561898,
-16.8024890596186,-16.7184321798819,-16.6589123631975),.UNSPECIFIED.);
#252=B_SPLINE_CURVE_WITH_KNOTS('',3,(#14776,#14777,#14778,#14779,#14780,
#14781,#14782,#14783,#14784,#14785,#14786,#14787,#14788,#14789,#14790,#14791,
#14792,#14793,#14794,#14795,#14796,#14797,#14798,#14799,#14800,#14801,#14802,
#14803,#14804,#14805,#14806,#14807,#14808,#14809,#14810,#14811,#14812,#14813,
#14814,#14815,#14816,#14817,#14818,#14819,#14820,#14821,#14822,#14823,#14824,
#14825,#14826,#14827,#14828,#14829,#14830,#14831,#14832,#14833,#14834,#14835,
#14836,#14837,#14838,#14839,#14840,#14841,#14842,#14843,#14844,#14845,#14846,
#14847,#14848,#14849,#14850,#14851,#14852,#14853,#14854,#14855,#14856,#14857,
#14858,#14859,#14860,#14861,#14862,#14863,#14864,#14865,#14866,#14867,#14868,
#14869,#14870,#14871,#14872,#14873,#14874,#14875,#14876,#14877,#14878,#14879,
#14880,#14881,#14882,#14883,#14884,#14885,#14886,#14887,#14888,#14889,#14890,
#14891,#14892,#14893,#14894,#14895,#14896,#14897,#14898,#14899,#14900,#14901,
#14902,#14903,#14904,#14905,#14906,#14907,#14908,#14909,#14910,#14911,#14912,
#14913,#14914,#14915,#14916,#14917,#14918,#14919,#14920,#14921,#14922,#14923,
#14924,#14925,#14926,#14927,#14928,#14929,#14930,#14931,#14932,#14933,#14934,
#14935,#14936,#14937,#14938,#14939,#14940,#14941,#14942,#14943,#14944,#14945,
#14946,#14947,#14948,#14949,#14950,#14951,#14952,#14953,#14954,#14955,#14956,
#14957,#14958,#14959,#14960,#14961,#14962,#14963,#14964,#14965,#14966,#14967,
#14968,#14969,#14970,#14971,#14972,#14973,#14974,#14975,#14976,#14977,#14978,
#14979,#14980,#14981,#14982,#14983,#14984,#14985,#14986,#14987,#14988,#14989,
#14990,#14991,#14992,#14993,#14994,#14995,#14996,#14997,#14998,#14999,#15000,
#15001,#15002,#15003,#15004,#15005,#15006,#15007),.UNSPECIFIED.,.F.,.F.,
(4,3,3,3,3,3,3,3,3,3,3,3,3,3,3,3,3,3,3,3,3,3,3,3,3,3,3,3,3,3,3,3,3,3,3,
3,3,3,3,3,3,3,3,3,3,3,3,3,3,3,3,3,3,3,3,3,3,3,3,3,3,3,3,3,3,3,3,3,3,3,3,
3,3,3,3,3,3,4),(13.6852257078969,13.7696192421721,13.8540154419322,13.9384321835534,
13.9684141841475,14.0523012934223,14.1361719329257,14.2200457703978,14.3039140722452,
14.3878043962055,14.4672861192956,14.5511732285658,14.6350438680643,14.7189177055317,
14.8027860073745,14.8866763313302,14.9661580544437,15.0500451637151,15.1339158032148,
15.2177896406835,15.3016579425272,15.3855482664841,15.4650299895918,15.5489170988635,
15.632787738364,15.716661575833,15.8005298776769,15.8844202016341,15.96390192474,
16.0477890340111,16.1316596735105,16.2155335109788,16.2994018128224,16.3832921367788,
16.4627738598881,16.5466609691597,16.6305316086596,16.7144054461283,16.7982737479722,
16.8821640719291,16.9616457950362,17.0455329043074,17.1294035438071,17.2132773812757,
17.2971456831196,17.3810360070764,17.4605177301843,17.5444048394559,17.6282754789555,
17.7121493164243,17.7960176182683,17.8799079422252,17.9593896653325,18.0432767746037,
18.1271474141036,18.2110212515721,18.2948895534159,18.3787798773727,18.4582616004806,
18.5421487097518,18.6260193492519,18.7098931867206,18.793761488564,18.8776518125207,
18.9571335356287,19.0410206449002,19.1248912844002,19.2087651218687,19.2926334237124,
19.3765237476693,19.4560054707768,19.5398925800482,19.6237632195474,19.7076370570163,
19.7915053588603,19.8753956828172,19.954877405925,19.9684110150765),
 .UNSPECIFIED.);
#253=B_SPLINE_CURVE_WITH_KNOTS('',3,(#15012,#15013,#15014,#15015,#15016,
#15017,#15018,#15019,#15020,#15021,#15022,#15023,#15024,#15025,#15026,#15027,
#15028,#15029,#15030,#15031,#15032,#15033,#15034,#15035,#15036,#15037,#15038,
#15039,#15040,#15041,#15042,#15043,#15044,#15045,#15046,#15047,#15048,#15049,
#15050,#15051,#15052,#15053,#15054,#15055,#15056,#15057,#15058,#15059,#15060,
#15061,#15062,#15063,#15064,#15065,#15066,#15067,#15068,#15069,#15070,#15071,
#15072,#15073,#15074,#15075,#15076,#15077,#15078,#15079,#15080,#15081,#15082,
#15083,#15084,#15085,#15086,#15087,#15088,#15089,#15090,#15091,#15092,#15093,
#15094,#15095,#15096,#15097,#15098,#15099,#15100,#15101,#15102,#15103,#15104,
#15105,#15106,#15107,#15108,#15109,#15110,#15111,#15112,#15113,#15114,#15115,
#15116,#15117,#15118,#15119,#15120,#15121,#15122,#15123,#15124,#15125,#15126,
#15127,#15128,#15129,#15130,#15131,#15132,#15133,#15134,#15135,#15136,#15137,
#15138,#15139,#15140,#15141,#15142,#15143,#15144,#15145,#15146,#15147,#15148,
#15149,#15150,#15151,#15152,#15153,#15154,#15155,#15156,#15157,#15158,#15159,
#15160,#15161,#15162,#15163,#15164,#15165,#15166,#15167,#15168,#15169,#15170,
#15171,#15172,#15173,#15174,#15175,#15176,#15177,#15178,#15179,#15180,#15181,
#15182,#15183,#15184,#15185,#15186,#15187,#15188,#15189,#15190,#15191,#15192,
#15193,#15194,#15195,#15196,#15197,#15198,#15199,#15200,#15201,#15202,#15203,
#15204,#15205,#15206,#15207,#15208,#15209,#15210,#15211,#15212,#15213,#15214,
#15215,#15216,#15217,#15218,#15219,#15220,#15221,#15222,#15223,#15224,#15225,
#15226,#15227,#15228,#15229,#15230,#15231,#15232,#15233,#15234,#15235,#15236,
#15237,#15238,#15239,#15240,#15241,#15242,#15243),.UNSPECIFIED.,.F.,.F.,
(4,3,3,3,3,3,3,3,3,3,3,3,3,3,3,3,3,3,3,3,3,3,3,3,3,3,3,3,3,3,3,3,3,3,3,
3,3,3,3,3,3,3,3,3,3,3,3,3,3,3,3,3,3,3,3,3,3,3,3,3,3,3,3,3,3,3,3,3,3,3,3,
3,3,3,3,3,3,4),(-29.2252829775567,-29.1407809000066,-29.0562748594698,-28.9717485871814,
-28.9499010320505,-28.8660153621469,-28.7821461848854,-28.6982738082037,
-28.6144069790521,-28.5305180722592,-28.45076480736,-28.3668791374562,-28.2830099601946,
-28.1991375835126,-28.115270754361,-28.0313818475678,-27.9516285826695,
-27.8677429127658,-27.7838737355038,-27.7000013588219,-27.6161345296702,
-27.5322456228771,-27.452492357979,-27.3686066880751,-27.2847375108129,
-27.2008651341309,-27.1169983049791,-27.0331093981858,-26.9533561332884,
-26.8694704633847,-26.7856012861231,-26.7017289094412,-26.6178620802896,
-26.5339731734966,-26.4542199085979,-26.3703342386943,-26.2864650614322,
-26.2025926847503,-26.1187258555989,-26.0348369488059,-25.9550836839074,
-25.8711980140034,-25.7873288367412,-25.7034564600591,-25.6195896309072,
-25.5357007241138,-25.4559474592168,-25.3720617893132,-25.2881926120514,
-25.2043202353694,-25.1204534062176,-25.0365644994246,-24.9568112345263,
-24.8729255646225,-24.7890563873604,-24.7051840106786,-24.6213171815268,
-24.5374282747336,-24.4576750098358,-24.3737893399322,-24.2899201626703,
-24.2060477859883,-24.1221809568366,-24.0382920500434,-23.9585387851453,
-23.8746531152411,-23.7907839379782,-23.706911561296,-23.6230447321438,
-23.5391558253504,-23.4594025604547,-23.3755168905508,-23.2916477132885,
-23.2077753366064,-23.1239085074543,-23.040019600661,-22.9602663357642,
-22.9420976703771),.UNSPECIFIED.);
#254=B_SPLINE_CURVE_WITH_KNOTS('',3,(#15244,#15245,#15246,#15247,#15248,
#15249,#15250,#15251,#15252,#15253,#15254,#15255,#15256,#15257,#15258,#15259,
#15260,#15261,#15262,#15263,#15264,#15265,#15266,#15267,#15268,#15269,#15270,
#15271,#15272,#15273,#15274,#15275,#15276,#15277,#15278,#15279,#15280,#15281,
#15282,#15283,#15284,#15285,#15286,#15287,#15288,#15289,#15290,#15291,#15292,
#15293,#15294,#15295,#15296,#15297,#15298,#15299,#15300,#15301,#15302,#15303,
#15304,#15305,#15306,#15307,#15308,#15309,#15310,#15311,#15312,#15313,#15314,
#15315,#15316,#15317,#15318,#15319,#15320,#15321,#15322,#15323,#15324,#15325,
#15326,#15327,#15328,#15329,#15330,#15331,#15332,#15333,#15334,#15335,#15336,
#15337,#15338,#15339,#15340,#15341,#15342,#15343,#15344,#15345,#15346,#15347,
#15348,#15349,#15350,#15351,#15352,#15353,#15354,#15355,#15356,#15357,#15358,
#15359,#15360,#15361,#15362,#15363,#15364,#15365,#15366,#15367,#15368,#15369,
#15370,#15371,#15372,#15373,#15374,#15375,#15376,#15377,#15378,#15379,#15380,
#15381,#15382,#15383,#15384,#15385,#15386,#15387,#15388,#15389,#15390,#15391,
#15392,#15393,#15394,#15395,#15396,#15397,#15398,#15399,#15400,#15401,#15402,
#15403,#15404,#15405,#15406,#15407,#15408,#15409,#15410,#15411,#15412,#15413,
#15414,#15415,#15416,#15417,#15418,#15419,#15420,#15421,#15422,#15423,#15424,
#15425,#15426,#15427,#15428,#15429,#15430,#15431,#15432,#15433,#15434,#15435,
#15436,#15437,#15438,#15439,#15440,#15441,#15442,#15443,#15444,#15445,#15446,
#15447,#15448,#15449,#15450,#15451,#15452,#15453,#15454,#15455,#15456,#15457,
#15458,#15459,#15460,#15461,#15462,#15463,#15464,#15465,#15466,#15467,#15468,
#15469,#15470,#15471,#15472),.UNSPECIFIED.,.F.,.F.,(4,3,3,3,3,3,3,3,3,3,
3,3,3,3,3,3,3,3,3,3,3,3,3,3,3,3,3,3,3,3,3,3,3,3,3,3,3,3,3,3,3,3,3,3,3,3,
3,3,3,3,3,3,3,3,3,3,3,3,3,3,3,3,3,3,3,3,3,3,3,3,3,3,3,3,3,3,4),(19.9684110152191,
20.0521965060799,20.1359653468292,20.2197369128689,20.3035036871813,20.3872915667496,
20.4537493410731,20.5376364503445,20.6215070898444,20.705380927313,20.7892492291569,
20.8731395531138,20.9526212762212,21.0365083854925,21.1203790249926,21.2042528624611,
21.288121164305,21.3720114882618,21.4514932113693,21.5353803206406,21.6192509601403,
21.7031247976089,21.7869930994529,21.8708834234096,21.9503651465174,22.0342522557888,
22.1181228952888,22.2019967327576,22.2858650346016,22.3697553585586,22.4492370816656,
22.5331241909368,22.6169948304367,22.7008686679053,22.7847369697493,22.8686272937061,
22.9481090168137,23.031996126085,23.1158667655848,23.1997406030536,23.2836089048974,
23.3674992288542,23.4469809519618,23.5308680612332,23.6147387007327,23.6986125382014,
23.7824808400452,23.8663711640021,23.9458528871099,24.0297399963815,24.1136106358812,
24.1974844733501,24.2813527751942,24.3652430991513,24.4447248222581,24.5286119315294,
24.612482571029,24.6963564084977,24.7802247103415,24.8641150342984,24.9435967574062,
25.0274838666776,25.1113545061777,25.1952283436463,25.2790966454902,25.3629869694469,
25.4424686925543,25.5263558018254,25.6102264413247,25.6941002787931,25.777968580637,
25.8618589045937,25.9413406277024,26.0254361266215,26.1095126610158,26.1935839844518,
26.2515963222561),.UNSPECIFIED.);
#255=B_SPLINE_CURVE_WITH_KNOTS('',3,(#15477,#15478,#15479,#15480,#15481,
#15482,#15483,#15484,#15485,#15486,#15487,#15488,#15489,#15490,#15491,#15492,
#15493,#15494,#15495,#15496,#15497,#15498,#15499,#15500,#15501,#15502,#15503,
#15504,#15505,#15506,#15507,#15508,#15509,#15510,#15511,#15512,#15513,#15514,
#15515,#15516,#15517,#15518,#15519,#15520,#15521,#15522,#15523,#15524,#15525,
#15526,#15527,#15528,#15529,#15530,#15531,#15532,#15533,#15534,#15535,#15536,
#15537,#15538,#15539,#15540,#15541,#15542,#15543,#15544,#15545,#15546,#15547,
#15548,#15549,#15550,#15551,#15552,#15553,#15554,#15555,#15556,#15557,#15558,
#15559,#15560,#15561,#15562,#15563,#15564,#15565,#15566,#15567,#15568,#15569,
#15570,#15571,#15572,#15573,#15574,#15575,#15576,#15577,#15578,#15579,#15580,
#15581,#15582,#15583,#15584,#15585,#15586,#15587,#15588,#15589,#15590,#15591,
#15592,#15593,#15594,#15595,#15596,#15597,#15598,#15599,#15600,#15601,#15602,
#15603,#15604,#15605,#15606,#15607,#15608,#15609,#15610,#15611,#15612,#15613,
#15614,#15615,#15616,#15617,#15618,#15619,#15620,#15621,#15622,#15623,#15624,
#15625,#15626,#15627,#15628,#15629,#15630,#15631,#15632,#15633,#15634,#15635,
#15636,#15637,#15638,#15639,#15640,#15641,#15642,#15643,#15644,#15645,#15646,
#15647,#15648,#15649,#15650,#15651,#15652,#15653,#15654,#15655,#15656,#15657,
#15658,#15659,#15660,#15661,#15662,#15663,#15664,#15665,#15666,#15667,#15668,
#15669,#15670,#15671,#15672,#15673,#15674,#15675,#15676,#15677,#15678,#15679,
#15680,#15681,#15682,#15683,#15684,#15685,#15686,#15687,#15688,#15689,#15690,
#15691,#15692,#15693,#15694,#15695,#15696,#15697,#15698,#15699,#15700,#15701,
#15702,#15703,#15704,#15705),.UNSPECIFIED.,.F.,.F.,(4,3,3,3,3,3,3,3,3,3,
3,3,3,3,3,3,3,3,3,3,3,3,3,3,3,3,3,3,3,3,3,3,3,3,3,3,3,3,3,3,3,3,3,3,3,3,
3,3,3,3,3,3,3,3,3,3,3,3,3,3,3,3,3,3,3,3,3,3,3,3,3,3,3,3,3,3,4),(-35.5084682847362,
-35.4386719530274,-35.3547862831221,-35.2709171058588,-35.1870447291753,
-35.103177900022,-35.0192889932272,-34.9395357283368,-34.8556500584337,
-34.7717808811724,-34.687908504491,-34.60404167534,-34.5201527685474,-34.4403995036463,
-34.3565138337424,-34.2726446564803,-34.1887722797983,-34.1049054506465,
-34.0210165438532,-33.9412632789558,-33.8573776090521,-33.7735084317902,
-33.6896360551083,-33.6057692259566,-33.5218803191635,-33.4421270542653,
-33.3582413843614,-33.2743722070994,-33.1904998304174,-33.1066330012656,
-33.0227440944724,-32.9429908295747,-32.8591051596709,-32.775235982409,
-32.6913636057271,-32.6074967765754,-32.5236078697822,-32.4438546048842,
-32.3599689349805,-32.2760997577186,-32.1922273810368,-32.1083605518851,
-32.024471645092,-31.9447183801937,-31.86083271029,-31.7769635330281,-31.6930911563462,
-31.6092243271946,-31.5253354204015,-31.4455821555032,-31.3616964855993,
-31.2778273083373,-31.1939549316552,-31.1100881025034,-31.0261991957101,
-30.9464459308126,-30.8625602609089,-30.778691083647,-30.6948187069651,
-30.6109518778135,-30.5270629710203,-30.4473097061221,-30.3634240362183,
-30.2795548589565,-30.1956824822747,-30.1118156531231,-30.0279267463299,
-29.9481734814316,-29.8642878115278,-29.7804186342659,-29.696546257584,
-29.6126794284323,-29.5287905216391,-29.4490372567411,-29.363612783768,
-29.278209766101,-29.2252829777188),.UNSPECIFIED.);
#256=B_SPLINE_CURVE_WITH_KNOTS('',3,(#15706,#15707,#15708,#15709,#15710,
#15711,#15712,#15713,#15714,#15715,#15716,#15717,#15718,#15719,#15720,#15721,
#15722),.UNSPECIFIED.,.F.,.F.,(4,1,1,1,1,1,1,1,1,1,1,1,1,1,4),(26.2515963581132,
26.4402125628506,26.9390844979987,27.4379564331468,27.9368283682949,28.4357003034431,
28.9345722385912,29.4334441737393,29.9323161088874,30.4311880440356,30.9300599791837,
31.4289319143318,31.9278038494799,32.4266757846281,32.5347816294356),
 .UNSPECIFIED.);
#257=B_SPLINE_CURVE_WITH_KNOTS('',3,(#15727,#15728,#15729,#15730,#15731,
#15732,#15733,#15734,#15735,#15736,#15737,#15738,#15739,#15740,#15741,#15742),
 .UNSPECIFIED.,.F.,.F.,(4,1,1,1,1,1,1,1,1,1,1,1,1,4),(-41.7916535919158,
-41.4283066493137,-40.9291704246232,-40.4300341999326,-39.9308979752421,
-39.4317617505516,-38.9326255258611,-38.4334893011705,-37.93435307648,-37.4352168517895,
-36.9360806270989,-36.4369444024084,-35.9378081777179,-35.5084683183979),
 .UNSPECIFIED.);
#258=B_SPLINE_CURVE_WITH_KNOTS('',3,(#15743,#15744,#15745,#15746,#15747,
#15748,#15749,#15750,#15751,#15752,#15753,#15754,#15755,#15756,#15757,#15758,
#15759,#15760,#15761,#15762,#15763,#15764,#15765,#15766,#15767,#15768,#15769,
#15770,#15771,#15772,#15773,#15774,#15775,#15776,#15777,#15778,#15779,#15780,
#15781,#15782,#15783,#15784,#15785,#15786,#15787,#15788,#15789,#15790,#15791,
#15792,#15793,#15794,#15795,#15796,#15797,#15798,#15799,#15800,#15801,#15802,
#15803,#15804,#15805,#15806,#15807,#15808,#15809,#15810,#15811,#15812,#15813,
#15814,#15815,#15816,#15817,#15818,#15819,#15820,#15821,#15822,#15823,#15824,
#15825,#15826,#15827,#15828,#15829,#15830,#15831,#15832,#15833,#15834,#15835,
#15836,#15837,#15838,#15839,#15840,#15841,#15842,#15843,#15844,#15845,#15846,
#15847,#15848,#15849,#15850,#15851,#15852,#15853,#15854,#15855,#15856,#15857,
#15858,#15859,#15860,#15861,#15862,#15863,#15864,#15865,#15866,#15867,#15868,
#15869,#15870,#15871,#15872,#15873,#15874,#15875,#15876,#15877,#15878,#15879,
#15880,#15881,#15882,#15883,#15884,#15885,#15886,#15887,#15888,#15889,#15890,
#15891,#15892,#15893,#15894,#15895,#15896,#15897,#15898,#15899,#15900,#15901,
#15902,#15903,#15904,#15905,#15906,#15907,#15908,#15909,#15910,#15911,#15912,
#15913,#15914,#15915,#15916,#15917,#15918,#15919,#15920,#15921,#15922,#15923,
#15924,#15925,#15926,#15927,#15928,#15929,#15930,#15931,#15932,#15933,#15934,
#15935,#15936,#15937,#15938,#15939,#15940,#15941,#15942,#15943,#15944,#15945,
#15946,#15947,#15948,#15949,#15950,#15951,#15952,#15953,#15954,#15955,#15956,
#15957,#15958,#15959,#15960,#15961,#15962,#15963,#15964,#15965,#15966,#15967,
#15968,#15969,#15970,#15971),.UNSPECIFIED.,.F.,.F.,(4,3,3,3,3,3,3,3,3,3,
3,3,3,3,3,3,3,3,3,3,3,3,3,3,3,3,3,3,3,3,3,3,3,3,3,3,3,3,3,3,3,3,3,3,3,3,
3,3,3,3,3,3,3,3,3,3,3,3,3,3,3,3,3,3,3,3,3,3,3,3,3,3,3,3,3,3,4),(32.5347816294356,
32.618344792917,32.7019091144161,32.7854688123165,32.8690491961098,32.9255477197762,
33.0094348290475,33.0933054685473,33.177179306016,33.2610476078598,33.3449379318165,
33.4244196549243,33.5083067641954,33.5921774036951,33.6760512411636,33.7599195430073,
33.8438098669641,33.9232915900724,34.0071786993439,34.0910493388438,34.1749231763126,
34.2587914781565,34.3426818021134,34.4221635252206,34.5060506344918,34.5899212739919,
34.6737951114604,34.7576634133044,34.8415537372611,34.9210354603687,35.0049225696402,
35.0887932091399,35.1726670466086,35.2565353484524,35.3404256724092,35.4199073955168,
35.5037945047881,35.587665144288,35.6715389817566,35.7554072836003,35.8392976075571,
35.9187793306649,36.0026664399364,36.0865370794367,36.1704109169056,36.2542792187495,
36.3381695427065,36.4176512658131,36.5015383750845,36.5854090145842,36.6692828520528,
36.7531511538964,36.8370414778532,36.9165232009612,37.0004103102327,37.0842809497323,
37.1681547872009,37.2520230890448,37.3359134130015,37.4153951361093,37.4992822453806,
37.5831528848803,37.667026722349,37.7508950241926,37.8347853481493,37.9142670712574,
37.9981541805289,38.0820248200289,38.1658986574978,38.2497669593422,38.3336572832991,
38.4131390064056,38.4966936713022,38.5802388631689,38.663772774134,38.7473200173164,
38.8179669364678),.UNSPECIFIED.);
#259=B_SPLINE_CURVE_WITH_KNOTS('',3,(#15976,#15977,#15978,#15979,#15980,
#15981,#15982,#15983,#15984,#15985,#15986,#15987,#15988,#15989,#15990,#15991,
#15992),.UNSPECIFIED.,.F.,.F.,(4,1,1,1,1,1,1,1,1,1,1,1,1,1,4),(-48.0748388990954,
-47.9170775702905,-47.4179413456,-46.9188051209095,-46.419668896219,-45.9205326715284,
-45.4213964468379,-44.9222602221474,-44.4231239974569,-43.9239877727663,
-43.4248515480758,-42.9257153233853,-42.4265790986947,-41.9274428740042,
-41.7916535919158),.UNSPECIFIED.);
#260=B_SPLINE_CURVE_WITH_KNOTS('',3,(#15993,#15994,#15995,#15996,#15997,
#15998,#15999,#16000,#16001,#16002,#16003,#16004,#16005,#16006,#16007,#16008,
#16009,#16010,#16011,#16012,#16013,#16014,#16015,#16016,#16017,#16018,#16019,
#16020,#16021,#16022,#16023,#16024,#16025,#16026,#16027,#16028,#16029,#16030,
#16031,#16032,#16033,#16034,#16035,#16036,#16037,#16038,#16039,#16040,#16041,
#16042,#16043,#16044,#16045,#16046,#16047,#16048,#16049,#16050,#16051,#16052,
#16053,#16054,#16055,#16056,#16057,#16058,#16059,#16060,#16061,#16062,#16063,
#16064,#16065,#16066,#16067,#16068,#16069,#16070,#16071,#16072,#16073,#16074,
#16075,#16076,#16077,#16078,#16079,#16080,#16081,#16082,#16083,#16084,#16085,
#16086,#16087,#16088,#16089,#16090,#16091,#16092,#16093,#16094,#16095,#16096,
#16097,#16098,#16099,#16100,#16101,#16102,#16103,#16104,#16105,#16106,#16107,
#16108,#16109,#16110,#16111,#16112,#16113,#16114,#16115,#16116,#16117,#16118,
#16119,#16120,#16121,#16122,#16123,#16124,#16125,#16126,#16127,#16128,#16129,
#16130,#16131,#16132,#16133,#16134,#16135,#16136,#16137,#16138,#16139,#16140,
#16141,#16142,#16143,#16144,#16145,#16146,#16147,#16148,#16149,#16150,#16151,
#16152,#16153,#16154,#16155,#16156,#16157,#16158,#16159,#16160,#16161,#16162,
#16163,#16164,#16165,#16166,#16167,#16168,#16169,#16170,#16171,#16172,#16173,
#16174,#16175,#16176,#16177,#16178,#16179,#16180,#16181,#16182,#16183,#16184,
#16185,#16186,#16187,#16188,#16189,#16190,#16191,#16192,#16193,#16194,#16195,
#16196,#16197,#16198,#16199,#16200,#16201,#16202,#16203,#16204,#16205,#16206,
#16207,#16208,#16209,#16210,#16211,#16212,#16213,#16214,#16215,#16216,#16217,
#16218,#16219,#16220,#16221),.UNSPECIFIED.,.F.,.F.,(4,3,3,3,3,3,3,3,3,3,
3,3,3,3,3,3,3,3,3,3,3,3,3,3,3,3,3,3,3,3,3,3,3,3,3,3,3,3,3,3,3,3,3,3,3,3,
3,3,3,3,3,3,3,3,3,3,3,3,3,3,3,3,3,3,3,3,3,3,3,3,3,3,3,3,3,3,4),(38.8179669366152,
38.9120109415537,38.9958980508245,39.0797686903237,39.1636425277917,39.2475108296349,
39.3314011535911,39.4108828767018,39.4947699859733,39.5786406254735,39.6625144629423,
39.7463827647863,39.8302730887433,39.9097548118499,39.9936419211213,40.0775125606213,
40.16138639809,40.245254699934,40.3291450238909,40.4086267469981,40.4925138562694,
40.5763844957693,40.6602583332379,40.7441266350817,40.8280169590385,40.9074986821462,
40.9913857914176,41.0752564309173,41.159130268386,41.2429985702298,41.3268888941867,
41.4063706172943,41.4902577265657,41.5741283660655,41.6580022035341,41.741870505378,
41.8257608293349,41.9052425524424,41.9891296617137,42.0730003012134,42.1568741386819,
42.2407424405257,42.3246327644825,42.4041144875905,42.488001596862,42.571872236362,
42.6557460738308,42.7396143756748,42.8235046996318,42.9029864227387,42.98687353201,
43.0707441715098,43.1546180089784,43.2384863108222,43.322376634779,43.4018583578868,
43.4857454671581,43.5696161066578,43.6534899441264,43.7373582459703,43.8212485699271,
43.9007302930349,43.9846174023063,44.0684880418061,44.1523618792748,44.2362301811186,
44.3201205050754,44.399602228183,44.4834893374546,44.5673599769545,44.6512338144233,
44.7351021162673,44.8189924402242,44.8984741633312,44.984359198492,45.0702196443385,
45.1011522436613),.UNSPECIFIED.);
#261=B_SPLINE_CURVE_WITH_KNOTS('',3,(#16226,#16227,#16228,#16229,#16230,
#16231,#16232,#16233,#16234,#16235,#16236,#16237,#16238,#16239,#16240,#16241),
 .UNSPECIFIED.,.F.,.F.,(4,1,1,1,1,1,1,1,1,1,1,1,1,4),(-54.358024206275,
-53.9067122665769,-53.4075760418863,-52.9084398171958,-52.4093035925053,
-51.9101673678147,-51.4110311431242,-50.9118949184337,-50.4127586937432,
-49.9136224690526,-49.4144862443621,-48.9153500196716,-48.4162137949811,
-48.0748388990954),.UNSPECIFIED.);
#262=B_SPLINE_CURVE_WITH_KNOTS('',3,(#16242,#16243,#16244,#16245,#16246,
#16247,#16248,#16249,#16250,#16251,#16252,#16253,#16254,#16255,#16256,#16257,
#16258,#16259,#16260,#16261,#16262,#16263,#16264,#16265,#16266,#16267,#16268,
#16269,#16270,#16271,#16272,#16273,#16274,#16275,#16276,#16277,#16278,#16279,
#16280,#16281,#16282,#16283,#16284,#16285,#16286,#16287,#16288,#16289,#16290,
#16291,#16292,#16293,#16294,#16295,#16296,#16297,#16298,#16299,#16300,#16301,
#16302,#16303,#16304,#16305,#16306,#16307,#16308,#16309,#16310,#16311,#16312,
#16313,#16314,#16315,#16316,#16317,#16318,#16319,#16320,#16321,#16322,#16323,
#16324,#16325,#16326,#16327,#16328,#16329,#16330,#16331,#16332,#16333,#16334,
#16335,#16336,#16337,#16338,#16339,#16340,#16341,#16342,#16343,#16344,#16345,
#16346,#16347,#16348,#16349,#16350,#16351,#16352,#16353,#16354,#16355,#16356,
#16357,#16358,#16359,#16360,#16361,#16362,#16363,#16364,#16365,#16366,#16367,
#16368,#16369,#16370,#16371,#16372,#16373,#16374,#16375,#16376,#16377,#16378,
#16379,#16380,#16381,#16382,#16383,#16384,#16385,#16386,#16387,#16388,#16389,
#16390,#16391,#16392,#16393,#16394,#16395,#16396,#16397,#16398,#16399,#16400,
#16401,#16402,#16403,#16404,#16405,#16406,#16407,#16408,#16409,#16410,#16411,
#16412,#16413,#16414,#16415,#16416,#16417,#16418,#16419,#16420,#16421,#16422,
#16423,#16424,#16425,#16426,#16427,#16428,#16429,#16430,#16431,#16432,#16433,
#16434,#16435,#16436,#16437,#16438,#16439,#16440,#16441,#16442,#16443,#16444,
#16445,#16446,#16447,#16448,#16449,#16450,#16451,#16452,#16453,#16454,#16455,
#16456,#16457,#16458,#16459,#16460,#16461,#16462,#16463,#16464,#16465,#16466,
#16467,#16468,#16469,#16470),.UNSPECIFIED.,.F.,.F.,(4,3,3,3,3,3,3,3,3,3,
3,3,3,3,3,3,3,3,3,3,3,3,3,3,3,3,3,3,3,3,3,3,3,3,3,3,3,3,3,3,3,3,3,3,3,3,
3,3,3,3,3,3,3,3,3,3,3,3,3,3,3,3,3,3,3,3,3,3,3,3,3,3,3,3,3,3,4),(45.1011522437948,
45.1853822629713,45.2696128695901,45.3538646416685,45.3973460984793,45.4812332077506,
45.5651038472503,45.6489776847188,45.7328459865627,45.8167363105194,45.8962180336274,
45.9801051428987,46.0639757823986,46.1478496198672,46.231717921711,46.3156082456678,
46.3950899687755,46.4789770780471,46.5628477175468,46.6467215550156,46.7305898568594,
46.8144801808164,46.8939619039237,46.9778490131949,47.0617196526949,47.1455934901634,
47.2294617920072,47.313352115964,47.3928338390718,47.4767209483433,47.5605915878429,
47.6444654253115,47.7283337271555,47.8122240511123,47.8917057742199,47.9755928834914,
48.0594635229913,48.1433373604599,48.2272056623041,48.3110959862609,48.390577709368,
48.4744648186397,48.5583354581401,48.6422092956089,48.7260775974526,48.8099679214096,
48.8894496445162,48.9733367537875,49.0572073932872,49.1410812307558,49.2249495325996,
49.3088398565565,49.3883215796643,49.4722086889355,49.5560793284352,49.6399531659037,
49.7238214677474,49.8077117917041,49.8871935148124,49.9710806240838,50.0549512635837,
50.1388251010524,50.2226934028966,50.3065837268537,50.3860654499606,50.4699525592319,
50.5538231987315,50.6376970362001,50.7215653380443,50.8054556620009,50.8849373851087,
50.9688288180462,51.0527037957669,51.1365819974282,51.220454637499,51.3043493368271,
51.3843375509714),.UNSPECIFIED.);
#263=B_SPLINE_CURVE_WITH_KNOTS('',3,(#16475,#16476,#16477,#16478,#16479,
#16480,#16481,#16482,#16483,#16484,#16485,#16486,#16487,#16488,#16489,#16490,
#16491),.UNSPECIFIED.,.F.,.F.,(4,1,1,1,1,1,1,1,1,1,1,1,1,1,4),(-60.6412095134546,
-60.3954831875537,-59.8963469628632,-59.3972107381726,-58.8980745134821,
-58.3989382887916,-57.8998020641011,-57.4006658394105,-56.90152961472,-56.4023933900295,
-55.903257165339,-55.4041209406484,-54.9049847159579,-54.4058484912674,
-54.358024206275),.UNSPECIFIED.);
#264=B_SPLINE_CURVE_WITH_KNOTS('',3,(#16492,#16493,#16494,#16495,#16496,
#16497,#16498,#16499,#16500,#16501,#16502,#16503,#16504,#16505,#16506,#16507,
#16508,#16509,#16510,#16511,#16512,#16513,#16514,#16515,#16516,#16517,#16518,
#16519,#16520,#16521,#16522,#16523,#16524,#16525,#16526,#16527,#16528,#16529,
#16530,#16531,#16532,#16533,#16534,#16535,#16536,#16537,#16538,#16539,#16540,
#16541,#16542,#16543,#16544,#16545,#16546,#16547,#16548,#16549,#16550,#16551,
#16552,#16553,#16554,#16555,#16556,#16557,#16558,#16559,#16560,#16561,#16562,
#16563,#16564,#16565,#16566,#16567,#16568,#16569,#16570,#16571,#16572,#16573,
#16574,#16575,#16576,#16577,#16578,#16579,#16580,#16581,#16582,#16583,#16584,
#16585,#16586,#16587,#16588,#16589,#16590,#16591,#16592,#16593,#16594,#16595,
#16596,#16597,#16598,#16599,#16600,#16601,#16602,#16603,#16604,#16605,#16606,
#16607,#16608,#16609,#16610,#16611,#16612,#16613,#16614,#16615,#16616,#16617,
#16618,#16619,#16620,#16621,#16622,#16623,#16624,#16625,#16626,#16627,#16628,
#16629,#16630,#16631,#16632,#16633,#16634,#16635,#16636,#16637,#16638,#16639,
#16640,#16641,#16642,#16643,#16644,#16645,#16646,#16647,#16648,#16649,#16650,
#16651,#16652,#16653,#16654,#16655,#16656,#16657,#16658,#16659,#16660,#16661,
#16662,#16663,#16664,#16665,#16666,#16667,#16668,#16669,#16670,#16671,#16672,
#16673,#16674,#16675,#16676,#16677,#16678,#16679,#16680,#16681,#16682,#16683,
#16684,#16685,#16686,#16687,#16688,#16689,#16690,#16691,#16692,#16693,#16694,
#16695,#16696,#16697,#16698,#16699,#16700,#16701,#16702,#16703,#16704,#16705,
#16706,#16707,#16708,#16709,#16710,#16711,#16712,#16713,#16714,#16715,#16716,
#16717,#16718,#16719,#16720),.UNSPECIFIED.,.F.,.F.,(4,3,3,3,3,3,3,3,3,3,
3,3,3,3,3,3,3,3,3,3,3,3,3,3,3,3,3,3,3,3,3,3,3,3,3,3,3,3,3,3,3,3,3,3,3,3,
3,3,3,3,3,3,3,3,3,3,3,3,3,3,3,3,3,3,3,3,3,3,3,3,3,3,3,3,3,3,4),(51.3843375509763,
51.4682203639788,51.5520866930172,51.6359561942946,51.7198201859624,51.8037061623815,
51.8826812554049,51.9665683646764,52.0504390041763,52.134312841645,52.218181143489,
52.3020714674459,52.3815531905531,52.4654402998244,52.5493109393242,52.6331847767927,
52.7170530786366,52.8009434025933,52.8804251257012,52.9643122349725,53.0481828744723,
53.1320567119409,53.2159250137848,53.2998153377415,53.3792970608493,53.4631841701207,
53.5470548096206,53.6309286470893,53.7147969489332,53.79868727289,53.8781689959974,
53.9620561052687,54.0459267447684,54.129800582237,54.2136688840808,54.2975592080375,
54.3770409311455,54.460928040417,54.544798679917,54.6286725173858,54.7125408192299,
54.7964311431868,54.8759128662937,54.959799975565,55.0436706150647,55.1275444525333,
55.2114127543771,55.2953030783338,55.3747848014418,55.4586719107132,55.542542550213,
55.6264163876816,55.7102846895255,55.7941750134823,55.8736567365899,55.9575438458613,
56.0414144853612,56.1252883228298,56.2091566246738,56.2930469486307,56.372528671738,
56.4564157810092,56.5402864205089,56.6241602579774,56.7080285598212,56.7919188837779,
56.8714006068861,56.9552877161577,57.0391583556578,57.1230321931266,57.2069004949706,
57.2907908189276,57.3702725420343,57.4545129399576,57.53873434292,57.6229476551049,
57.667522858154),.UNSPECIFIED.);
#265=B_SPLINE_CURVE_WITH_KNOTS('',3,(#16725,#16726,#16727,#16728,#16729,
#16730,#16731,#16732,#16733,#16734,#16735,#16736,#16737,#16738,#16739,#16740,
#16741,#16742,#16743,#16744,#16745,#16746,#16747,#16748,#16749,#16750,#16751,
#16752,#16753,#16754,#16755,#16756,#16757,#16758,#16759,#16760,#16761,#16762,
#16763,#16764,#16765,#16766,#16767,#16768,#16769,#16770,#16771,#16772,#16773,
#16774,#16775,#16776,#16777,#16778,#16779,#16780,#16781,#16782,#16783,#16784,
#16785,#16786,#16787,#16788,#16789,#16790,#16791,#16792,#16793,#16794,#16795,
#16796,#16797,#16798,#16799,#16800,#16801,#16802,#16803,#16804,#16805,#16806,
#16807,#16808,#16809,#16810,#16811,#16812,#16813,#16814,#16815,#16816,#16817,
#16818,#16819,#16820,#16821,#16822,#16823,#16824,#16825,#16826,#16827,#16828,
#16829,#16830,#16831,#16832,#16833,#16834,#16835,#16836,#16837,#16838,#16839,
#16840,#16841,#16842,#16843,#16844,#16845,#16846,#16847,#16848,#16849,#16850,
#16851,#16852,#16853,#16854,#16855,#16856,#16857,#16858,#16859,#16860,#16861,
#16862,#16863,#16864,#16865,#16866,#16867,#16868,#16869,#16870,#16871,#16872,
#16873,#16874,#16875,#16876,#16877,#16878,#16879,#16880,#16881,#16882,#16883,
#16884,#16885,#16886,#16887,#16888,#16889,#16890,#16891,#16892,#16893,#16894,
#16895,#16896,#16897,#16898,#16899,#16900,#16901,#16902,#16903,#16904,#16905,
#16906,#16907,#16908,#16909,#16910,#16911,#16912,#16913,#16914,#16915,#16916,
#16917,#16918,#16919,#16920,#16921,#16922,#16923,#16924,#16925,#16926,#16927,
#16928,#16929,#16930,#16931,#16932,#16933,#16934,#16935,#16936,#16937,#16938,
#16939,#16940,#16941,#16942,#16943,#16944,#16945,#16946,#16947,#16948,#16949,
#16950,#16951,#16952,#16953),.UNSPECIFIED.,.F.,.F.,(4,3,3,3,3,3,3,3,3,3,
3,3,3,3,3,3,3,3,3,3,3,3,3,3,3,3,3,3,3,3,3,3,3,3,3,3,3,3,3,3,3,3,3,3,3,3,
3,3,3,3,3,3,3,3,3,3,3,3,3,3,3,3,3,3,3,3,3,3,3,3,3,3,3,3,3,3,4),(-66.9243948206342,
-66.8842541085305,-66.8003684386284,-66.7164992613681,-66.6326268846879,
-66.5487600555379,-66.4648711487464,-66.38511788384,-66.3012322139357,-66.2173630366733,
-66.1334906599908,-66.0496238308386,-65.9657349240449,-65.8859816591495,
-65.8020959892458,-65.718226811984,-65.6343544353021,-65.5504876061504,
-65.4665986993573,-65.3868454344589,-65.3029597645552,-65.2190905872933,
-65.1352182106114,-65.0513513814597,-64.9674624746665,-64.8877092097684,
-64.8038235398646,-64.7199543626027,-64.6360819859208,-64.552215156769,
-64.4683262499758,-64.3885729850779,-64.3046873151741,-64.2208181379122,
-64.1369457612303,-64.0530789320785,-63.9691900252854,-63.8894367603874,
-63.8055510904837,-63.7216819132219,-63.6378095365401,-63.5539427073885,
-63.4700538005955,-63.3903005356969,-63.306414865793,-63.2225456885309,
-63.1386733118488,-63.0548064826969,-62.9709175759036,-62.8911643110063,
-62.8072786411026,-62.7234094638407,-62.6395370871588,-62.5556702580072,
-62.4717813512141,-62.3920280863158,-62.308142416412,-62.2242732391502,
-62.1404008624683,-62.0565340333166,-61.9726451265235,-61.8928918616253,
-61.8090061917216,-61.7251370144597,-61.6412646377777,-61.5573978086262,
-61.4735089018331,-61.3937556369348,-61.309869967031,-61.2260007897689,
-61.1421284130868,-61.058261583935,-60.9743726771418,-60.8946194122442,
-60.8097498638457,-60.7248961180713,-60.6412095136835),.UNSPECIFIED.);
#266=B_SPLINE_CURVE_WITH_KNOTS('',3,(#16954,#16955,#16956,#16957,#16958,
#16959,#16960,#16961,#16962,#16963,#16964,#16965,#16966,#16967,#16968,#16969,
#16970,#16971,#16972,#16973,#16974,#16975,#16976,#16977,#16978,#16979,#16980,
#16981,#16982,#16983,#16984,#16985,#16986,#16987,#16988,#16989,#16990,#16991,
#16992,#16993,#16994,#16995,#16996,#16997,#16998,#16999,#17000,#17001,#17002,
#17003,#17004,#17005,#17006,#17007,#17008,#17009,#17010,#17011,#17012,#17013,
#17014,#17015,#17016,#17017,#17018,#17019,#17020,#17021,#17022,#17023,#17024,
#17025,#17026,#17027,#17028,#17029,#17030,#17031,#17032,#17033,#17034,#17035,
#17036,#17037,#17038,#17039,#17040,#17041,#17042,#17043,#17044,#17045,#17046,
#17047,#17048,#17049,#17050,#17051,#17052,#17053,#17054,#17055,#17056,#17057,
#17058,#17059,#17060,#17061,#17062,#17063,#17064,#17065,#17066,#17067,#17068,
#17069,#17070,#17071,#17072,#17073,#17074,#17075,#17076,#17077,#17078,#17079,
#17080,#17081,#17082,#17083,#17084,#17085,#17086,#17087,#17088,#17089,#17090,
#17091,#17092,#17093,#17094,#17095,#17096,#17097,#17098,#17099,#17100,#17101,
#17102,#17103,#17104,#17105,#17106,#17107,#17108,#17109,#17110,#17111,#17112,
#17113,#17114,#17115,#17116,#17117,#17118,#17119,#17120,#17121,#17122,#17123,
#17124,#17125,#17126,#17127,#17128,#17129,#17130,#17131,#17132,#17133,#17134,
#17135,#17136,#17137,#17138,#17139,#17140,#17141,#17142,#17143,#17144,#17145,
#17146,#17147,#17148,#17149,#17150,#17151,#17152,#17153,#17154,#17155,#17156,
#17157,#17158,#17159,#17160,#17161,#17162,#17163,#17164,#17165,#17166,#17167,
#17168,#17169,#17170,#17171,#17172,#17173,#17174,#17175,#17176,#17177,#17178,
#17179,#17180,#17181,#17182,#17183,#17184,#17185),.UNSPECIFIED.,.F.,.F.,
(4,3,3,3,3,3,3,3,3,3,3,3,3,3,3,3,3,3,3,3,3,3,3,3,3,3,3,3,3,3,3,3,3,3,3,
3,3,3,3,3,3,3,3,3,3,3,3,3,3,3,3,3,3,3,3,3,3,3,3,3,3,3,3,3,3,3,3,3,3,3,3,
3,3,3,3,3,3,4),(57.6675228582893,57.7534041072256,57.8393136045471,57.8691444771824,
57.9530315864536,58.0369022259531,58.1207760634215,58.2046443652652,58.2885346892219,
58.3680164123305,58.4519035216018,58.5357741611016,58.6196479985702,58.703516300414,
58.7874066243708,58.8668883474786,58.9507754567501,59.0346460962501,59.1185199337189,
59.2023882355629,59.2862785595198,59.3657602826268,59.4496473918981,59.5335180313978,
59.6173918688663,59.7012601707101,59.7851504946669,59.8646322177749,59.9485193270462,
60.032389966546,60.1162638040146,60.2001321058585,60.2840224298153,60.363504152923,
60.4473912621943,60.5312619016941,60.6151357391627,60.6990040410066,60.7828943649633,
60.8623760880711,60.9462631973426,61.0301338368426,61.1140076743113,61.1978759761554,
61.2817663001124,61.3612480232193,61.4451351324906,61.5290057719904,61.612879609459,
61.6967479113029,61.7806382352596,61.8601199583674,61.9440070676387,62.0278777071385,
62.1117515446071,62.1956198464509,62.2795101704077,62.3589918935155,62.4428790027869,
62.5267496422866,62.6106234797552,62.6944917815991,62.7783821055559,62.8578638286636,
62.9417509379351,63.0256215774348,63.1094954149035,63.1933637167476,63.2772540407045,
63.3567357638118,63.4406228730832,63.524493512583,63.6083673500517,63.6922356518955,
63.7761259758523,63.8556076989599,63.9449408103947,63.9507081653336),
 .UNSPECIFIED.);
#267=B_SPLINE_CURVE_WITH_KNOTS('',3,(#17190,#17191,#17192,#17193,#17194,
#17195,#17196,#17197,#17198,#17199,#17200,#17201,#17202,#17203,#17204,#17205,
#17206,#17207,#17208,#17209,#17210,#17211,#17212,#17213,#17214,#17215,#17216,
#17217,#17218,#17219,#17220,#17221,#17222,#17223,#17224,#17225,#17226,#17227,
#17228,#17229,#17230,#17231,#17232,#17233,#17234,#17235,#17236,#17237,#17238,
#17239,#17240,#17241,#17242,#17243,#17244,#17245,#17246,#17247,#17248,#17249,
#17250,#17251,#17252,#17253,#17254,#17255,#17256,#17257,#17258,#17259,#17260,
#17261,#17262,#17263,#17264,#17265,#17266,#17267,#17268,#17269,#17270,#17271,
#17272,#17273,#17274,#17275,#17276,#17277,#17278,#17279,#17280,#17281,#17282,
#17283,#17284,#17285,#17286,#17287,#17288,#17289,#17290,#17291,#17292,#17293,
#17294,#17295,#17296,#17297,#17298,#17299,#17300,#17301,#17302,#17303,#17304,
#17305,#17306,#17307,#17308,#17309,#17310,#17311,#17312,#17313,#17314,#17315,
#17316,#17317,#17318,#17319,#17320,#17321,#17322,#17323,#17324,#17325,#17326,
#17327,#17328,#17329,#17330,#17331,#17332,#17333,#17334,#17335,#17336,#17337,
#17338,#17339,#17340,#17341,#17342,#17343,#17344,#17345,#17346,#17347,#17348,
#17349,#17350,#17351,#17352,#17353,#17354,#17355,#17356,#17357,#17358,#17359,
#17360,#17361,#17362,#17363,#17364,#17365,#17366,#17367,#17368,#17369,#17370,
#17371,#17372,#17373,#17374,#17375,#17376,#17377,#17378,#17379,#17380,#17381,
#17382,#17383,#17384,#17385,#17386,#17387,#17388,#17389,#17390,#17391,#17392,
#17393,#17394,#17395,#17396,#17397,#17398,#17399,#17400,#17401,#17402,#17403,
#17404,#17405,#17406,#17407,#17408,#17409,#17410,#17411,#17412,#17413,#17414,
#17415,#17416,#17417,#17418),.UNSPECIFIED.,.F.,.F.,(4,3,3,3,3,3,3,3,3,3,
3,3,3,3,3,3,3,3,3,3,3,3,3,3,3,3,3,3,3,3,3,3,3,3,3,3,3,3,3,3,3,3,3,3,3,3,
3,3,3,3,3,3,3,3,3,3,3,3,3,3,3,3,3,3,3,3,3,3,3,3,3,3,3,3,3,3,4),(-73.2075801278138,
-73.1237189665367,-73.0398629051662,-72.9559834080525,-72.8738888048169,
-72.7900031349128,-72.7061339576504,-72.6222615809683,-72.5383947518164,
-72.454505845023,-72.3747525801263,-72.2908669102225,-72.2069977329604,
-72.1231253562785,-72.0392585271269,-71.9553696203339,-71.8756163554358,
-71.791730685532,-71.7078615082704,-71.6239891315887,-71.5401223024372,
-71.4562333956442,-71.3764801307453,-71.2925944608413,-71.208725283579,
-71.1248529068969,-71.0409860777452,-70.9570971709518,-70.8773439060547,
-70.7934582361511,-70.7095890588888,-70.6257166822069,-70.5418498530552,
-70.4579609462621,-70.3782076813642,-70.2943220114605,-70.2104528341989,
-70.1265804575169,-70.0427136283652,-69.958824721572,-69.8790714566737,
-69.79518578677,-69.7113166095082,-69.6274442328262,-69.5435774036746,-69.4596884968814,
-69.3799352319832,-69.2960495620793,-69.2121803848174,-69.1283080081353,
-69.0444411789833,-68.96055227219,-68.8807990072926,-68.7969133373889,-68.7130441601271,
-68.6291717834451,-68.5453049542936,-68.4614160475006,-68.3816627826021,
-68.2977771126984,-68.2139079354367,-68.1300355587546,-68.0461687296027,
-67.9622798228095,-67.8825265579116,-67.798640888008,-67.7147717107465,
-67.6308993340648,-67.547032504913,-67.4631435981197,-67.3833903332211,
-67.299752204125,-67.2161313803661,-67.1325096836612,-67.0488920048269,
-66.9652563514555,-66.9243948207875),.UNSPECIFIED.);
#268=B_SPLINE_CURVE_WITH_KNOTS('',3,(#17419,#17420,#17421,#17422,#17423,
#17424,#17425,#17426,#17427,#17428,#17429,#17430,#17431,#17432,#17433,#17434,
#17435,#17436,#17437,#17438,#17439,#17440,#17441,#17442,#17443,#17444,#17445,
#17446,#17447,#17448,#17449,#17450,#17451,#17452,#17453,#17454,#17455,#17456,
#17457,#17458,#17459,#17460,#17461,#17462,#17463,#17464,#17465,#17466,#17467,
#17468,#17469,#17470,#17471,#17472,#17473,#17474,#17475,#17476,#17477,#17478,
#17479,#17480,#17481,#17482,#17483,#17484,#17485,#17486,#17487,#17488,#17489,
#17490,#17491,#17492,#17493,#17494,#17495,#17496,#17497,#17498,#17499,#17500,
#17501,#17502,#17503,#17504,#17505,#17506,#17507,#17508,#17509,#17510,#17511,
#17512,#17513,#17514,#17515,#17516,#17517,#17518,#17519,#17520,#17521,#17522,
#17523,#17524,#17525,#17526,#17527,#17528,#17529,#17530,#17531,#17532,#17533,
#17534,#17535,#17536,#17537,#17538,#17539,#17540,#17541,#17542,#17543,#17544,
#17545,#17546,#17547,#17548,#17549,#17550,#17551,#17552,#17553,#17554,#17555,
#17556,#17557,#17558,#17559,#17560,#17561,#17562,#17563,#17564,#17565,#17566,
#17567,#17568,#17569,#17570,#17571,#17572,#17573,#17574,#17575,#17576,#17577,
#17578,#17579,#17580,#17581,#17582,#17583,#17584,#17585,#17586,#17587,#17588,
#17589,#17590,#17591,#17592,#17593,#17594,#17595,#17596,#17597,#17598,#17599,
#17600,#17601,#17602,#17603,#17604,#17605,#17606,#17607,#17608,#17609,#17610,
#17611,#17612,#17613,#17614,#17615,#17616,#17617,#17618,#17619,#17620,#17621,
#17622,#17623,#17624,#17625,#17626,#17627,#17628,#17629,#17630,#17631,#17632,
#17633,#17634,#17635,#17636,#17637,#17638,#17639,#17640,#17641,#17642,#17643,
#17644,#17645,#17646,#17647),.UNSPECIFIED.,.F.,.F.,(4,3,3,3,3,3,3,3,3,3,
3,3,3,3,3,3,3,3,3,3,3,3,3,3,3,3,3,3,3,3,3,3,3,3,3,3,3,3,3,3,3,3,3,3,3,3,
3,3,3,3,3,3,3,3,3,3,3,3,3,3,3,3,3,3,3,3,3,3,3,3,3,3,3,3,3,3,4),(63.9507081654737,
64.0342511929075,64.1177942057486,64.2013312260194,64.2848898688643,64.354479634108,
64.4383667433793,64.5222373828791,64.6061112203477,64.6899795221913,64.7738698461479,
64.8533515692561,64.9372386785277,65.0211093180277,65.1049831554964,65.1888514573402,
65.2727417812972,65.3522235044043,65.4361106136757,65.5199812531758,65.6038550906444,
65.6877233924882,65.771613716445,65.8510954395524,65.9349825488237,66.0188531883232,
66.1027270257919,66.1865953276358,66.2704856515926,66.3499673747005,66.4338544839719,
66.5177251234716,66.6015989609404,66.6854672627844,66.7693575867413,66.8488393098486,
66.93272641912,67.0165970586195,67.100470896088,67.1843391979319,67.2682295218888,
67.3477112449967,67.4315983542682,67.5154689937682,67.5993428312371,67.6832111330812,
67.7671014570381,67.8465831801449,67.9304702894162,68.0143409289157,68.0982147663844,
68.1820830682279,68.2659733921847,68.345455115293,68.4293422245644,68.5132128640643,
68.597086701533,68.6809550033769,68.7648453273338,68.8443270504411,68.9282141597127,
69.0120847992117,69.0959586366804,69.1798269385242,69.2637172624809,69.3431989855892,
69.4270860948607,69.5109567343604,69.594830571829,69.6786988736732,69.7625891976302,
69.8420709207374,69.9256471339678,70.0092127771835,70.0927671613274,70.1763321069992,
70.2338934725132),.UNSPECIFIED.);
#269=B_SPLINE_CURVE_WITH_KNOTS('',3,(#17652,#17653,#17654,#17655,#17656,
#17657,#17658,#17659,#17660,#17661,#17662,#17663,#17664,#17665,#17666,#17667,
#17668,#17669,#17670,#17671,#17672,#17673,#17674,#17675,#17676,#17677,#17678,
#17679,#17680,#17681,#17682,#17683,#17684,#17685,#17686,#17687,#17688,#17689,
#17690,#17691,#17692,#17693,#17694,#17695,#17696,#17697,#17698,#17699,#17700,
#17701,#17702,#17703,#17704,#17705,#17706,#17707,#17708,#17709,#17710,#17711,
#17712,#17713,#17714,#17715,#17716,#17717,#17718,#17719,#17720,#17721,#17722,
#17723,#17724,#17725,#17726,#17727,#17728,#17729,#17730,#17731,#17732,#17733,
#17734,#17735,#17736,#17737,#17738,#17739,#17740,#17741,#17742,#17743,#17744,
#17745,#17746,#17747,#17748,#17749,#17750,#17751,#17752,#17753,#17754,#17755,
#17756,#17757,#17758,#17759,#17760,#17761,#17762,#17763,#17764,#17765,#17766,
#17767,#17768,#17769,#17770,#17771,#17772,#17773,#17774,#17775,#17776,#17777,
#17778,#17779,#17780,#17781,#17782,#17783,#17784,#17785,#17786,#17787,#17788,
#17789,#17790,#17791,#17792,#17793,#17794,#17795,#17796,#17797,#17798,#17799,
#17800,#17801,#17802,#17803,#17804,#17805,#17806,#17807,#17808,#17809,#17810,
#17811,#17812,#17813,#17814,#17815,#17816,#17817,#17818,#17819,#17820,#17821,
#17822,#17823,#17824,#17825,#17826,#17827,#17828,#17829,#17830,#17831,#17832,
#17833,#17834,#17835,#17836,#17837,#17838,#17839,#17840,#17841,#17842,#17843,
#17844,#17845,#17846,#17847,#17848,#17849,#17850,#17851,#17852,#17853,#17854,
#17855,#17856,#17857,#17858,#17859,#17860,#17861,#17862,#17863,#17864,#17865,
#17866,#17867,#17868,#17869,#17870,#17871,#17872,#17873,#17874,#17875,#17876,
#17877,#17878,#17879,#17880),.UNSPECIFIED.,.F.,.F.,(4,3,3,3,3,3,3,3,3,3,
3,3,3,3,3,3,3,3,3,3,3,3,3,3,3,3,3,3,3,3,3,3,3,3,3,3,3,3,3,3,3,3,3,3,3,3,
3,3,3,3,3,3,3,3,3,3,3,3,3,3,3,3,3,3,3,3,3,3,3,3,3,3,3,3,3,3,4),(-79.4907654337011,
-79.4027074760698,-79.3626597257937,-79.2787740558902,-79.1949048786287,
-79.1110325019471,-79.0271656727957,-78.9432767660027,-78.8635235011032,
-78.7796378311995,-78.6957686539375,-78.6118962772556,-78.5280294481038,
-78.4441405413106,-78.3643872764127,-78.2805016065089,-78.1966324292469,
-78.1127600525649,-78.0288932234132,-77.9450043166199,-77.8652510517221,
-77.7813653818183,-77.6974962045565,-77.6136238278745,-77.5297569987229,
-77.4458680919298,-77.3661148270316,-77.2822291571279,-77.1983599798659,
-77.114487603184,-77.0306207740324,-76.9467318672392,-76.8669786023411,
-76.7830929324374,-76.6992237551755,-76.6153513784937,-76.531484549342,
-76.4475956425489,-76.3678423776506,-76.2839567077467,-76.2000875304846,
-76.1162151538024,-76.0323483246506,-75.9484594178572,-75.86870615296,-75.7848204830563,
-75.7009513057945,-75.6170789291127,-75.5332120999611,-75.449323193168,
-75.3695699282695,-75.2856842583658,-75.201815081104,-75.1179427044221,
-75.0340758752705,-74.9501869684774,-74.870433703579,-74.786548033675,-74.7026788564129,
-74.6188064797308,-74.5349396505789,-74.4510507437856,-74.3712974788884,
-74.2874118089847,-74.2035426317232,-74.1196702550413,-74.0358034258898,
-73.9519145190967,-73.8721612541979,-73.7882755842942,-73.7044064070323,
-73.6205340303503,-73.5366672011987,-73.4527782944055,-73.3730250295074,
-73.2861666536806,-73.2075801279635),.UNSPECIFIED.);
#270=B_SPLINE_CURVE_WITH_KNOTS('',3,(#17881,#17882,#17883,#17884,#17885,
#17886,#17887,#17888,#17889,#17890,#17891,#17892,#17893,#17894,#17895,#17896,
#17897),.UNSPECIFIED.,.F.,.F.,(4,1,1,1,1,1,1,1,1,1,1,1,1,1,4),(70.2338934725132,
70.3409428558855,70.8398147910336,71.3386867261817,71.8375586613299,72.336430596478,
72.8353025316261,73.3341744667742,73.8330464019223,74.3319183370705,74.8307902722186,
75.3296622073667,75.8285341425149,76.327406077663,76.517078744021),
 .UNSPECIFIED.);
#271=B_SPLINE_CURVE_WITH_KNOTS('',3,(#17902,#17903,#17904,#17905,#17906,
#17907,#17908,#17909,#17910,#17911,#17912,#17913,#17914,#17915,#17916,#17917),
 .UNSPECIFIED.,.F.,.F.,(4,1,1,1,1,1,1,1,1,1,1,1,1,4),(-85.7739507126178,
-85.35229442208,-84.8531581973895,-84.354021972699,-83.8548857480084,-83.3557495233179,
-82.8566132986274,-82.3574770739369,-81.8583408492463,-81.3592046245558,
-80.8600683998653,-80.3609321751748,-79.8617959504842,-79.4907654349934),
 .UNSPECIFIED.);
#272=B_SPLINE_CURVE_WITH_KNOTS('',3,(#17918,#17919,#17920,#17921,#17922,
#17923,#17924,#17925,#17926,#17927,#17928,#17929,#17930,#17931,#17932,#17933,
#17934,#17935,#17936,#17937,#17938,#17939,#17940,#17941,#17942,#17943,#17944,
#17945,#17946,#17947,#17948,#17949,#17950,#17951,#17952,#17953,#17954,#17955,
#17956,#17957,#17958,#17959,#17960,#17961,#17962,#17963,#17964,#17965,#17966,
#17967,#17968,#17969,#17970,#17971,#17972,#17973,#17974,#17975,#17976,#17977,
#17978,#17979,#17980,#17981,#17982,#17983,#17984,#17985,#17986,#17987,#17988,
#17989,#17990,#17991,#17992,#17993,#17994,#17995,#17996,#17997,#17998,#17999,
#18000,#18001,#18002,#18003,#18004,#18005,#18006,#18007,#18008,#18009,#18010,
#18011,#18012,#18013,#18014,#18015,#18016,#18017,#18018,#18019,#18020,#18021,
#18022,#18023,#18024,#18025,#18026,#18027,#18028,#18029,#18030,#18031,#18032,
#18033,#18034,#18035,#18036,#18037,#18038,#18039,#18040,#18041,#18042,#18043,
#18044,#18045,#18046,#18047,#18048,#18049,#18050,#18051,#18052,#18053,#18054,
#18055,#18056,#18057,#18058,#18059,#18060,#18061,#18062,#18063,#18064,#18065,
#18066,#18067,#18068,#18069,#18070,#18071,#18072,#18073,#18074,#18075,#18076,
#18077,#18078,#18079,#18080,#18081,#18082,#18083,#18084,#18085,#18086,#18087,
#18088,#18089,#18090,#18091,#18092,#18093,#18094,#18095,#18096,#18097,#18098,
#18099,#18100,#18101,#18102,#18103,#18104,#18105,#18106,#18107,#18108,#18109,
#18110,#18111,#18112,#18113,#18114,#18115,#18116,#18117,#18118,#18119,#18120,
#18121,#18122,#18123,#18124,#18125,#18126,#18127,#18128,#18129,#18130,#18131,
#18132,#18133,#18134,#18135,#18136,#18137,#18138,#18139,#18140,#18141,#18142,
#18143,#18144,#18145,#18146),.UNSPECIFIED.,.F.,.F.,(4,3,3,3,3,3,3,3,3,3,
3,3,3,3,3,3,3,3,3,3,3,3,3,3,3,3,3,3,3,3,3,3,3,3,3,3,3,3,3,3,3,3,3,3,3,3,
3,3,3,3,3,3,3,3,3,3,3,3,3,3,3,3,3,3,3,3,3,3,3,3,3,3,3,3,3,3,4),(76.5170787796928,
76.6011639019145,76.6852475777892,76.7693531117986,76.8262780128111,76.9101651220824,
76.9940357615821,77.0779095990506,77.1617779008945,77.2456682248513,77.3251499479592,
77.4090370572304,77.4929076967303,77.5767815341989,77.6606498360427,77.7445401599995,
77.8240218831073,77.9079089923787,77.9917796318787,78.0756534693475,78.1595217711914,
78.2434120951483,78.3228938182555,78.4067809275269,78.4906515670271,78.5745254044957,
78.6583937063397,78.7422840302966,78.8217657534036,78.905652862675,78.9895235021748,
79.0733973396434,79.1572656414872,79.241155965444,79.3206376885517,79.4045247978231,
79.4883954373227,79.5722692747913,79.6561375766353,79.740027900592,79.8195096236998,
79.9033967329711,79.9872673724711,80.07114120994,80.1550095117838,80.2388998357408,
80.318381558848,80.4022686681195,80.4861393076195,80.5700131450882,80.653881446932,
80.7377717708888,80.8172534939961,80.9011406032674,80.9850112427667,81.0688850802354,
81.1527533820793,81.236643706036,81.3161254291442,81.4000125384156,81.4838831779163,
81.5677570153852,81.6516253172292,81.735515641186,81.8149973642924,81.8988844735638,
81.9827551130635,82.0666289505322,82.1504972523764,82.2343875763332,82.3138692994405,
82.397662418436,82.4814387563788,82.5652176399422,82.6489915553591,82.7327864637313,
82.8002640868724),.UNSPECIFIED.);
#273=B_SPLINE_CURVE_WITH_KNOTS('',3,(#18151,#18152,#18153,#18154,#18155,
#18156,#18157,#18158,#18159,#18160,#18161,#18162,#18163,#18164,#18165,#18166,
#18167,#18168,#18169,#18170,#18171,#18172,#18173,#18174,#18175,#18176,#18177,
#18178,#18179,#18180,#18181,#18182,#18183,#18184,#18185,#18186,#18187,#18188,
#18189,#18190,#18191,#18192,#18193,#18194,#18195,#18196,#18197,#18198,#18199,
#18200,#18201,#18202,#18203,#18204,#18205,#18206,#18207,#18208,#18209,#18210,
#18211,#18212,#18213,#18214,#18215,#18216,#18217,#18218,#18219,#18220,#18221,
#18222,#18223,#18224,#18225,#18226,#18227,#18228,#18229,#18230,#18231,#18232,
#18233,#18234,#18235,#18236,#18237,#18238,#18239,#18240,#18241,#18242,#18243,
#18244,#18245,#18246,#18247,#18248,#18249,#18250,#18251,#18252,#18253,#18254,
#18255,#18256,#18257,#18258,#18259,#18260,#18261,#18262,#18263,#18264,#18265,
#18266,#18267,#18268,#18269,#18270,#18271,#18272,#18273,#18274,#18275,#18276,
#18277,#18278,#18279,#18280,#18281,#18282,#18283,#18284,#18285,#18286,#18287,
#18288,#18289,#18290,#18291,#18292,#18293,#18294,#18295,#18296,#18297,#18298,
#18299,#18300,#18301,#18302,#18303,#18304,#18305,#18306,#18307,#18308,#18309,
#18310,#18311,#18312,#18313,#18314,#18315,#18316,#18317,#18318,#18319,#18320,
#18321,#18322,#18323,#18324,#18325,#18326,#18327,#18328,#18329,#18330,#18331,
#18332,#18333,#18334,#18335,#18336,#18337,#18338,#18339,#18340,#18341,#18342,
#18343,#18344,#18345,#18346,#18347,#18348,#18349,#18350,#18351,#18352,#18353,
#18354,#18355,#18356,#18357,#18358,#18359,#18360,#18361,#18362,#18363,#18364,
#18365,#18366,#18367,#18368,#18369,#18370,#18371,#18372,#18373,#18374,#18375,
#18376,#18377,#18378,#18379),.UNSPECIFIED.,.F.,.F.,(4,3,3,3,3,3,3,3,3,3,
3,3,3,3,3,3,3,3,3,3,3,3,3,3,3,3,3,3,3,3,3,3,3,3,3,3,3,3,3,3,3,3,3,3,3,3,
3,3,3,3,3,3,3,3,3,3,3,3,3,3,3,3,3,3,3,3,3,3,3,3,3,3,3,3,3,3,4),(-92.0571360463357,
-91.9715779609207,-91.8859914371021,-91.8410653430568,-91.7571796731532,
-91.6733104958916,-91.5894381192099,-91.5055712900585,-91.4216823832656,
-91.3419291183663,-91.2580434484625,-91.1741742712005,-91.0903018945185,
-91.0064350653667,-90.9225461585735,-90.8427928936758,-90.7589072237721,
-90.6750380465103,-90.5911656698284,-90.5072988406768,-90.4234099338837,
-90.3436566689853,-90.2597709990815,-90.1759018218195,-90.0920294451375,
-90.0081626159857,-89.9242737091924,-89.8445204442947,-89.7606347743909,
-89.676765597129,-89.5928932204471,-89.5090263912954,-89.4251374845022,
-89.3453842196042,-89.2614985497005,-89.1776293724386,-89.0937569957567,
-89.009890166605,-88.9260012598119,-88.8462479949137,-88.7623623250099,
-88.678493147748,-88.5946207710661,-88.5107539419144,-88.4268650351213,
-88.3471117702232,-88.2632261003193,-88.1793569230573,-88.0954845463753,
-88.0116177172235,-87.9277288104303,-87.8479755455326,-87.7640898756289,
-87.680220698367,-87.5963483216851,-87.5124814925333,-87.4285925857402,
-87.3488393208421,-87.2649536509384,-87.1810844736765,-87.0972120969946,
-87.013345267843,-86.9294563610499,-86.8497030961516,-86.7658174262477,
-86.6819482489858,-86.5980758723037,-86.514209043152,-86.4303201363587,
-86.350566871461,-86.2666812015572,-86.1828120242953,-86.0989396476133,
-86.0150728184617,-85.9311839116685,-85.8514306467705,-85.773950742173),
 .UNSPECIFIED.);
#274=B_SPLINE_CURVE_WITH_KNOTS('',3,(#18380,#18381,#18382,#18383,#18384,
#18385,#18386,#18387,#18388,#18389,#18390,#18391,#18392,#18393,#18394,#18395,
#18396,#18397),.UNSPECIFIED.,.F.,.F.,(4,2,1,1,1,1,1,1,1,1,1,1,1,1,4),(82.8002640868724,
82.8127412345886,83.3116131697367,83.8104851048849,84.309357040033,84.8082289751811,
85.3071009103292,85.8059728454774,86.3048447806255,86.8037167157736,87.3025886509217,
87.8014605860699,88.300332521218,88.7992044563661,89.083449394052),
 .UNSPECIFIED.);
#275=B_SPLINE_CURVE_WITH_KNOTS('',3,(#18402,#18403,#18404,#18405,#18406,
#18407,#18408,#18409,#18410,#18411,#18412,#18413,#18414,#18415,#18416,#18417,
#18418,#18419),.UNSPECIFIED.,.F.,.F.,(4,2,1,1,1,1,1,1,1,1,1,1,1,1,4),(-98.3403213565322,
-98.3298362640337,-97.8307000393432,-97.3315638146527,-96.8324275899621,
-96.3332913652716,-95.8341551405811,-95.3350189158905,-94.8358826912,-94.3367464665095,
-93.837610241819,-93.3384740171284,-92.8393377924379,-92.3402015677474,
-92.0571360493526),.UNSPECIFIED.);
#276=B_SPLINE_CURVE_WITH_KNOTS('',3,(#18420,#18421,#18422,#18423,#18424,
#18425,#18426,#18427,#18428,#18429,#18430,#18431,#18432,#18433,#18434,#18435,
#18436),.UNSPECIFIED.,.F.,.F.,(4,1,1,1,1,1,1,1,1,1,1,1,1,1,4),(89.083449394052,
89.2980763915142,89.7969483266623,90.2958202618104,90.7946921969586,91.2935641321067,
91.7924360672548,92.2913080024029,92.7901799375511,93.2890518726992,93.7879238078473,
94.2867957429954,94.7856676781436,95.2845396132917,95.3666347012316),
 .UNSPECIFIED.);
#277=B_SPLINE_CURVE_WITH_KNOTS('',3,(#18441,#18442,#18443,#18444,#18445,
#18446,#18447,#18448,#18449,#18450,#18451,#18452,#18453,#18454,#18455,#18456,
#18457,#18458,#18459,#18460,#18461,#18462,#18463,#18464,#18465,#18466,#18467,
#18468,#18469,#18470,#18471,#18472,#18473,#18474,#18475,#18476,#18477,#18478,
#18479,#18480,#18481,#18482,#18483,#18484,#18485,#18486,#18487,#18488,#18489,
#18490,#18491,#18492,#18493,#18494,#18495,#18496,#18497,#18498,#18499,#18500,
#18501,#18502,#18503,#18504,#18505,#18506,#18507,#18508,#18509,#18510,#18511,
#18512,#18513,#18514,#18515,#18516,#18517,#18518,#18519,#18520,#18521,#18522,
#18523,#18524,#18525,#18526,#18527,#18528,#18529,#18530,#18531,#18532,#18533,
#18534,#18535,#18536,#18537,#18538,#18539,#18540,#18541,#18542,#18543,#18544,
#18545,#18546,#18547,#18548,#18549,#18550,#18551,#18552,#18553,#18554,#18555,
#18556,#18557,#18558,#18559,#18560,#18561,#18562,#18563,#18564,#18565,#18566,
#18567,#18568,#18569,#18570,#18571,#18572,#18573,#18574,#18575,#18576,#18577,
#18578,#18579,#18580,#18581,#18582,#18583,#18584,#18585,#18586,#18587,#18588,
#18589,#18590,#18591,#18592,#18593,#18594,#18595,#18596,#18597,#18598,#18599,
#18600,#18601,#18602,#18603,#18604,#18605,#18606,#18607,#18608,#18609,#18610,
#18611,#18612,#18613,#18614,#18615,#18616,#18617,#18618,#18619,#18620,#18621,
#18622,#18623,#18624,#18625,#18626,#18627,#18628,#18629,#18630,#18631,#18632,
#18633,#18634,#18635,#18636,#18637,#18638,#18639,#18640,#18641,#18642,#18643,
#18644,#18645,#18646,#18647,#18648,#18649,#18650,#18651,#18652,#18653,#18654,
#18655,#18656,#18657,#18658,#18659,#18660,#18661,#18662,#18663,#18664,#18665,
#18666,#18667,#18668,#18669),.UNSPECIFIED.,.F.,.F.,(4,3,3,3,3,3,3,3,3,3,
3,3,3,3,3,3,3,3,3,3,3,3,3,3,3,3,3,3,3,3,3,3,3,3,3,3,3,3,3,3,3,3,3,3,3,3,
3,3,3,3,3,3,3,3,3,3,3,3,3,3,3,3,3,3,3,3,3,3,3,3,3,3,3,3,3,3,4),(-104.623506663712,
-104.539365643134,-104.455225239483,-104.371063224086,-104.31947096032,
-104.235585290418,-104.151716113158,-104.067843736478,-103.983976907328,
-103.900088000536,-103.82033473563,-103.736449065725,-103.652579888463,
-103.56870751178,-103.484840682628,-103.400951775834,-103.321198510939,
-103.237312841034,-103.153443663771,-103.069571287088,-102.985704457936,
-102.901815551142,-102.822062286248,-102.738176616346,-102.654307439086,
-102.570435062405,-102.486568233255,-102.402679326464,-102.322926061558,
-102.239040391653,-102.15517121439,-102.071298837707,-101.987432008554,
-101.903543101759,-101.823789836867,-101.739904166964,-101.656034989703,
-101.572162613023,-101.488295783872,-101.40440687708,-101.324653612177,
-101.240767942272,-101.156898765009,-101.073026388326,-100.989159559174,
-100.90527065238,-100.825517387486,-100.741631717583,-100.657762540321,
-100.57389016364,-100.490023334489,-100.406134427696,-100.326381162796,
-100.242495492892,-100.15862631563,-100.074753938948,-99.9908871097962,
-99.9069982030031,-99.8272449381053,-99.7433592682012,-99.6594900909393,
-99.575617714257,-99.4917508851051,-99.4078619783115,-99.3281087134148,
-99.2442230435111,-99.1603538662499,-99.0764814895682,-98.9926146604168,
-98.9087257536239,-98.8289724887242,-98.7451668881793,-98.6613780460848,
-98.5775865485867,-98.4938001160868,-98.4099924549528,-98.3403213565322),
 .UNSPECIFIED.);
#278=B_SPLINE_CURVE_WITH_KNOTS('',3,(#18670,#18671,#18672,#18673,#18674,
#18675,#18676,#18677,#18678,#18679,#18680,#18681,#18682,#18683,#18684,#18685),
 .UNSPECIFIED.,.F.,.F.,(4,1,1,1,1,1,1,1,1,1,1,1,1,4),(95.3666347012316,
95.7834115484398,96.2822834835879,96.781155418736,97.2800273538842,97.7788992890323,
98.2777712241804,98.7766431593285,99.2755150944767,99.7743870296248,100.273258964773,
100.772130899921,101.271002835069,101.649820008411),.UNSPECIFIED.);
#279=B_SPLINE_CURVE_WITH_KNOTS('',3,(#18690,#18691,#18692,#18693,#18694,
#18695,#18696,#18697,#18698,#18699,#18700,#18701,#18702,#18703,#18704,#18705,
#18706),.UNSPECIFIED.,.F.,.F.,(4,1,1,1,1,1,1,1,1,1,1,1,1,1,4),(-110.906691970891,
-110.808241881297,-110.309105656606,-109.809969431916,-109.310833207225,
-108.811696982535,-108.312560757844,-107.813424533154,-107.314288308463,
-106.815152083773,-106.316015859082,-105.816879634392,-105.317743409701,
-104.818607185011,-104.623506698272),.UNSPECIFIED.);
#280=B_SPLINE_CURVE_WITH_KNOTS('',3,(#18707,#18708,#18709,#18710,#18711,
#18712,#18713,#18714,#18715,#18716,#18717,#18718,#18719,#18720,#18721,#18722,
#18723,#18724,#18725,#18726,#18727,#18728,#18729,#18730,#18731,#18732,#18733,
#18734,#18735,#18736,#18737,#18738,#18739,#18740,#18741,#18742,#18743,#18744,
#18745,#18746,#18747,#18748,#18749,#18750,#18751,#18752,#18753,#18754,#18755,
#18756,#18757,#18758,#18759,#18760,#18761,#18762,#18763,#18764,#18765,#18766,
#18767,#18768,#18769,#18770,#18771,#18772,#18773,#18774,#18775,#18776,#18777,
#18778,#18779,#18780,#18781,#18782,#18783,#18784,#18785,#18786,#18787,#18788,
#18789,#18790,#18791,#18792,#18793,#18794,#18795,#18796,#18797,#18798,#18799,
#18800,#18801,#18802,#18803,#18804,#18805,#18806,#18807,#18808,#18809,#18810,
#18811,#18812,#18813,#18814,#18815,#18816,#18817,#18818,#18819,#18820,#18821,
#18822,#18823,#18824,#18825,#18826,#18827,#18828,#18829,#18830,#18831,#18832,
#18833,#18834,#18835,#18836,#18837,#18838,#18839,#18840,#18841,#18842,#18843,
#18844,#18845,#18846,#18847,#18848,#18849,#18850,#18851,#18852,#18853,#18854,
#18855,#18856,#18857,#18858,#18859,#18860,#18861,#18862,#18863,#18864,#18865,
#18866,#18867,#18868,#18869,#18870,#18871,#18872,#18873,#18874,#18875,#18876,
#18877,#18878,#18879,#18880,#18881,#18882,#18883,#18884,#18885,#18886,#18887,
#18888,#18889,#18890,#18891,#18892,#18893,#18894,#18895,#18896,#18897,#18898,
#18899,#18900,#18901,#18902,#18903,#18904,#18905,#18906,#18907,#18908,#18909,
#18910,#18911,#18912,#18913,#18914,#18915,#18916,#18917,#18918,#18919,#18920,
#18921,#18922,#18923,#18924,#18925,#18926,#18927,#18928,#18929,#18930,#18931,
#18932,#18933,#18934,#18935),.UNSPECIFIED.,.F.,.F.,(4,3,3,3,3,3,3,3,3,3,
3,3,3,3,3,3,3,3,3,3,3,3,3,3,3,3,3,3,3,3,3,3,3,3,3,3,3,3,3,3,3,3,3,3,3,3,
3,3,3,3,3,3,3,3,3,3,3,3,3,3,3,3,3,3,3,3,3,3,3,3,3,3,3,3,3,3,4),(101.649820008525,
101.738164112558,101.769874770217,101.853761879489,101.937632518989,102.021506356458,
102.105374658302,102.189264982259,102.268746705365,102.352633814637,102.436504454139,
102.520378291608,102.604246593453,102.688136917411,102.767618640514,102.851505749785,
102.935376389285,103.019250226753,103.103118528596,103.187008852553,103.266490575662,
103.350377684933,103.434248324432,103.5181221619,103.601990463744,103.6858807877,
103.76536251081,103.849249620082,103.933120259582,104.016994097051,104.100862398895,
104.184752722852,104.264234445958,104.348121555229,104.431992194729,104.515866032197,
104.599734334041,104.683624657998,104.763106381106,104.846993490377,104.930864129877,
105.014737967346,105.09860626919,105.182496593147,105.261978316254,105.345865425525,
105.429736065025,105.513609902494,105.597478204337,105.681368528294,105.760850251402,
105.844737360673,105.928608000172,106.01248183764,106.096350139483,106.180240463439,
106.25972218655,106.343609295823,106.427479935324,106.511353772795,106.59522207464,
106.679112398598,106.758594121699,106.84248123097,106.926351870469,107.010225707938,
107.094094009781,107.177984333737,107.257466056847,107.341353166118,107.425223805617,
107.509097643085,107.592965944928,107.676856268884,107.756337991995,107.844671651442,
107.933005310889),.UNSPECIFIED.);
#281=B_SPLINE_CURVE_WITH_KNOTS('',3,(#18940,#18941,#18942,#18943,#18944,
#18945,#18946,#18947,#18948,#18949,#18950,#18951,#18952,#18953,#18954,#18955,
#18956,#18957,#18958,#18959,#18960,#18961,#18962,#18963,#18964,#18965,#18966,
#18967,#18968,#18969,#18970,#18971,#18972,#18973,#18974,#18975,#18976,#18977,
#18978,#18979,#18980,#18981,#18982,#18983,#18984,#18985,#18986,#18987,#18988,
#18989,#18990,#18991,#18992,#18993,#18994,#18995,#18996,#18997,#18998,#18999,
#19000,#19001,#19002,#19003,#19004,#19005,#19006,#19007,#19008,#19009,#19010,
#19011,#19012,#19013,#19014,#19015,#19016,#19017,#19018,#19019,#19020,#19021,
#19022,#19023,#19024,#19025,#19026,#19027,#19028,#19029,#19030,#19031,#19032,
#19033,#19034,#19035,#19036,#19037,#19038,#19039,#19040,#19041,#19042,#19043,
#19044,#19045,#19046,#19047,#19048,#19049,#19050,#19051,#19052,#19053,#19054,
#19055,#19056,#19057,#19058,#19059,#19060,#19061,#19062,#19063,#19064,#19065,
#19066,#19067,#19068,#19069,#19070,#19071,#19072,#19073,#19074,#19075,#19076,
#19077,#19078,#19079,#19080,#19081,#19082,#19083,#19084,#19085,#19086,#19087,
#19088,#19089,#19090,#19091,#19092,#19093,#19094,#19095,#19096,#19097,#19098,
#19099,#19100,#19101,#19102,#19103,#19104,#19105,#19106,#19107,#19108,#19109,
#19110,#19111,#19112,#19113,#19114,#19115,#19116,#19117,#19118,#19119,#19120,
#19121,#19122,#19123,#19124,#19125,#19126,#19127,#19128,#19129,#19130,#19131,
#19132,#19133,#19134,#19135,#19136,#19137,#19138,#19139,#19140,#19141,#19142,
#19143,#19144,#19145,#19146,#19147,#19148,#19149,#19150,#19151,#19152,#19153,
#19154,#19155,#19156,#19157,#19158,#19159,#19160,#19161,#19162,#19163,#19164,
#19165,#19166,#19167,#19168),.UNSPECIFIED.,.F.,.F.,(4,3,3,3,3,3,3,3,3,3,
3,3,3,3,3,3,3,3,3,3,3,3,3,3,3,3,3,3,3,3,3,3,3,3,3,3,3,3,3,3,3,3,3,3,3,3,
3,3,3,3,3,3,3,3,3,3,3,3,3,3,3,3,3,3,3,3,3,3,3,3,3,3,3,3,3,3,4),(-117.189877278071,
-117.106318081834,-117.022757825786,-116.939202312273,-116.855625995822,
-116.797876577583,-116.713990907681,-116.63012173042,-116.54624935374,-116.46238252459,
-116.378493617798,-116.298740352893,-116.214854682988,-116.130985505724,
-116.047113129041,-115.963246299888,-115.879357393093,-115.799604128202,
-115.715718458299,-115.631849281039,-115.547976904358,-115.464110075207,
-115.380221168415,-115.300467903512,-115.216582233607,-115.132713056344,
-115.048840679661,-114.964973850509,-114.881084943714,-114.801331678821,
-114.717446008918,-114.633576831657,-114.549704454976,-114.465837625825,
-114.381948719033,-114.302195454131,-114.218309784227,-114.134440606965,
-114.050568230283,-113.966701401131,-113.882812494337,-113.80305922944,
-113.719173559535,-113.635304382272,-113.551432005589,-113.467565176436,
-113.383676269642,-113.303923004749,-113.220037334847,-113.136168157587,
-113.052295780907,-112.968428951757,-112.884540044965,-112.804786780059,
-112.720901110154,-112.63703193289,-112.553159556207,-112.469292727054,
-112.385403820259,-112.305650555368,-112.221764885466,-112.137895708205,
-112.054023331524,-111.970156502374,-111.886267595581,-111.806514330678,
-111.722628660774,-111.638759483511,-111.554887106828,-111.471020277677,
-111.387131370883,-111.307378105987,-111.223819822338,-111.140271399509,
-111.056734262025,-110.973184693901,-110.906691970891),.UNSPECIFIED.);
#282=B_SPLINE_CURVE_WITH_KNOTS('',3,(#19169,#19170,#19171,#19172,#19173,
#19174,#19175,#19176,#19177,#19178,#19179,#19180,#19181,#19182,#19183,#19184),
 .UNSPECIFIED.,.F.,.F.,(4,1,1,1,1,1,1,1,1,1,1,1,1,4),(107.933005315591,
108.255209927143,108.754081862291,109.252953797439,109.751825732587,110.250697667735,
110.749569602884,111.248441538032,111.74731347318,112.246185408328,112.745057343476,
113.243929278624,113.742801213772,114.21619062277),.UNSPECIFIED.);
#283=B_SPLINE_CURVE_WITH_KNOTS('',3,(#19189,#19190,#19191,#19192,#19193,
#19194,#19195,#19196,#19197,#19198,#19199,#19200,#19201,#19202,#19203,#19204,
#19205),.UNSPECIFIED.,.F.,.F.,(4,1,1,1,1,1,1,1,1,1,1,1,1,1,4),(-123.473062548923,
-123.28664749856,-122.78751127387,-122.288375049179,-121.789238824488,-121.290102599798,
-120.790966375107,-120.291830150417,-119.792693925726,-119.293557701036,
-118.794421476345,-118.295285251655,-117.796149026964,-117.297012802274,
-117.189877278071),.UNSPECIFIED.);
#284=B_SPLINE_CURVE_WITH_KNOTS('',3,(#19206,#19207,#19208,#19209,#19210,
#19211,#19212,#19213,#19214,#19215,#19216,#19217,#19218,#19219,#19220,#19221,
#19222),.UNSPECIFIED.,.F.,.F.,(4,1,1,1,1,1,1,1,1,1,1,1,1,1,4),(114.21619062277,
114.24167314892,114.740545084069,115.239417019217,115.738288954365,116.237160889513,
116.736032824661,117.234904759809,117.733776694957,118.232648630105,118.731520565254,
119.230392500402,119.72926443555,120.228136370698,120.49937592995),
 .UNSPECIFIED.);
#285=B_SPLINE_CURVE_WITH_KNOTS('',3,(#19227,#19228,#19229,#19230,#19231,
#19232,#19233,#19234,#19235,#19236,#19237,#19238,#19239,#19240,#19241,#19242,
#19243,#19244,#19245,#19246,#19247,#19248,#19249,#19250,#19251,#19252,#19253,
#19254,#19255,#19256,#19257,#19258,#19259,#19260,#19261,#19262,#19263,#19264,
#19265,#19266,#19267,#19268,#19269,#19270,#19271,#19272,#19273,#19274,#19275,
#19276,#19277,#19278,#19279,#19280,#19281,#19282,#19283,#19284,#19285,#19286,
#19287,#19288,#19289,#19290,#19291,#19292,#19293,#19294,#19295,#19296,#19297,
#19298,#19299,#19300,#19301,#19302,#19303,#19304,#19305,#19306,#19307,#19308,
#19309,#19310,#19311,#19312,#19313,#19314,#19315,#19316,#19317,#19318,#19319,
#19320,#19321,#19322,#19323,#19324,#19325,#19326,#19327,#19328,#19329,#19330,
#19331,#19332,#19333,#19334,#19335,#19336,#19337,#19338,#19339,#19340,#19341,
#19342,#19343,#19344,#19345,#19346,#19347,#19348,#19349,#19350,#19351,#19352,
#19353,#19354,#19355,#19356,#19357,#19358,#19359,#19360,#19361,#19362,#19363,
#19364,#19365,#19366,#19367,#19368,#19369,#19370,#19371,#19372,#19373,#19374,
#19375,#19376,#19377,#19378,#19379,#19380,#19381,#19382,#19383,#19384,#19385,
#19386,#19387,#19388,#19389,#19390,#19391,#19392,#19393,#19394,#19395,#19396,
#19397,#19398,#19399,#19400,#19401,#19402,#19403,#19404,#19405,#19406,#19407,
#19408,#19409,#19410,#19411,#19412,#19413,#19414,#19415,#19416,#19417,#19418,
#19419,#19420,#19421,#19422,#19423,#19424,#19425,#19426,#19427,#19428,#19429,
#19430,#19431,#19432,#19433,#19434,#19435,#19436,#19437,#19438,#19439,#19440,
#19441,#19442,#19443,#19444,#19445,#19446,#19447,#19448,#19449,#19450,#19451,
#19452,#19453,#19454,#19455),.UNSPECIFIED.,.F.,.F.,(4,3,3,3,3,3,3,3,3,3,
3,3,3,3,3,3,3,3,3,3,3,3,3,3,3,3,3,3,3,3,3,3,3,3,3,3,3,3,3,3,3,3,3,3,3,3,
3,3,3,3,3,3,3,3,3,3,3,3,3,3,3,3,3,3,3,3,3,3,3,3,3,3,3,3,3,3,4),(-129.756247892334,
-129.672501065347,-129.588770880719,-129.505038060992,-129.421309691022,
-129.337560521526,-129.276282194846,-129.192396524943,-129.108527347683,
-129.024654971003,-128.940788141852,-128.85689923506,-128.777145970156,
-128.693260300251,-128.609391122988,-128.525518746304,-128.441651917152,
-128.357763010357,-128.278009745465,-128.194124075562,-128.110254898301,
-128.02638252162,-127.942515692469,-127.858626785677,-127.778873520775,
-127.69498785087,-127.611118673607,-127.527246296924,-127.443379467772,
-127.359490560978,-127.279737296084,-127.195851626181,-127.11198244892,
-127.028110072239,-126.944243243089,-126.860354336296,-126.780601071394,
-126.696715401489,-126.612846224226,-126.528973847544,-126.445107018391,
-126.361218111597,-126.281464846703,-126.1975791768,-126.113709999539,-126.029837622858,
-125.945970793707,-125.862081886915,-125.782328622013,-125.698442952108,
-125.614573774845,-125.530701398162,-125.44683456901,-125.362945662216,
-125.283192397322,-125.199306727419,-125.115437550158,-125.031565173477,
-124.947698344326,-124.863809437534,-124.784056172632,-124.700170502727,
-124.616301325465,-124.532428948782,-124.448562119629,-124.364673212835,
-124.284919947941,-124.201034278038,-124.117165100776,-124.033292724094,
-123.949425894943,-123.86553698815,-123.785783723251,-123.70171321643,-123.617661695445,
-123.533614860638,-123.473062585251),.UNSPECIFIED.);
#286=B_SPLINE_CURVE_WITH_KNOTS('',3,(#19456,#19457,#19458,#19459,#19460,
#19461,#19462,#19463,#19464,#19465,#19466,#19467,#19468,#19469,#19470,#19471,
#19472,#19473,#19474,#19475,#19476,#19477,#19478,#19479,#19480,#19481,#19482,
#19483,#19484,#19485,#19486,#19487,#19488,#19489,#19490,#19491,#19492,#19493,
#19494,#19495,#19496,#19497,#19498,#19499,#19500,#19501,#19502,#19503,#19504,
#19505,#19506,#19507,#19508,#19509,#19510,#19511,#19512,#19513,#19514,#19515,
#19516,#19517,#19518,#19519,#19520,#19521,#19522,#19523,#19524,#19525,#19526,
#19527,#19528,#19529,#19530,#19531,#19532,#19533,#19534,#19535,#19536,#19537,
#19538,#19539,#19540,#19541,#19542,#19543,#19544,#19545,#19546,#19547,#19548,
#19549,#19550,#19551,#19552,#19553,#19554,#19555,#19556,#19557,#19558,#19559,
#19560,#19561,#19562,#19563,#19564,#19565,#19566,#19567,#19568,#19569,#19570,
#19571,#19572,#19573,#19574,#19575,#19576,#19577,#19578,#19579,#19580,#19581,
#19582,#19583,#19584,#19585,#19586,#19587,#19588,#19589,#19590,#19591,#19592,
#19593,#19594,#19595,#19596,#19597,#19598,#19599,#19600,#19601,#19602,#19603,
#19604,#19605,#19606,#19607,#19608,#19609,#19610,#19611,#19612,#19613,#19614,
#19615,#19616,#19617,#19618,#19619,#19620,#19621,#19622,#19623,#19624,#19625,
#19626,#19627,#19628,#19629,#19630,#19631,#19632,#19633,#19634,#19635,#19636,
#19637,#19638,#19639,#19640,#19641,#19642,#19643,#19644,#19645,#19646,#19647,
#19648,#19649,#19650,#19651,#19652,#19653,#19654,#19655,#19656,#19657,#19658,
#19659,#19660,#19661,#19662,#19663,#19664,#19665,#19666,#19667,#19668,#19669,
#19670,#19671,#19672,#19673,#19674,#19675,#19676,#19677,#19678,#19679,#19680,
#19681,#19682,#19683,#19684),.UNSPECIFIED.,.F.,.F.,(4,3,3,3,3,3,3,3,3,3,
3,3,3,3,3,3,3,3,3,3,3,3,3,3,3,3,3,3,3,3,3,3,3,3,3,3,3,3,3,3,3,3,3,3,3,3,
3,3,3,3,3,3,3,3,3,3,3,3,3,3,3,3,3,3,3,3,3,3,3,3,3,3,3,3,3,3,4),(120.499375931658,
120.584690836811,120.670034253282,120.727008305846,120.810895415117,120.894766054617,
120.978639892086,121.06250819393,121.146398517887,121.225880240994,121.309767350265,
121.393637989765,121.477511827234,121.561380129077,121.645270453034,121.724752176142,
121.808639285413,121.892509924912,121.97638376238,122.060252064223,122.144142388179,
122.22362411129,122.307511220563,122.391381860064,122.475255697534,122.559123999379,
122.643014323338,122.722496046439,122.80638315571,122.890253795209,122.974127632677,
123.057995934521,123.141886258477,123.221367981587,123.305255090858,123.389125730358,
123.472999567826,123.556867869669,123.640758193626,123.720239916735,123.804127026007,
123.887997665507,123.971871502975,124.05573980482,124.139630128777,124.219111851883,
124.302998961154,124.386869600654,124.470743438122,124.554611739966,124.638502063923,
124.717983787031,124.801870896302,124.885741535802,124.969615373271,125.053483675115,
125.137373999072,125.216855722179,125.30074283145,125.38461347095,125.468487308419,
125.552355610263,125.636245934219,125.715727657327,125.799614766598,125.883485406097,
125.967359243565,126.051227545408,126.135117869364,126.214599592475,126.298486701747,
126.382357341248,126.466231178718,126.550099480562,126.63398980452,126.713471527624,
126.78256123713),.UNSPECIFIED.);
#287=B_SPLINE_CURVE_WITH_KNOTS('',3,(#19689,#19690,#19691,#19692,#19693,
#19694,#19695,#19696,#19697,#19698,#19699,#19700,#19701,#19702,#19703,#19704,
#19705,#19706,#19707,#19708,#19709,#19710,#19711,#19712,#19713,#19714,#19715,
#19716,#19717,#19718,#19719,#19720,#19721,#19722,#19723,#19724,#19725,#19726,
#19727,#19728,#19729,#19730,#19731,#19732,#19733,#19734,#19735,#19736,#19737,
#19738,#19739,#19740,#19741,#19742,#19743,#19744,#19745,#19746,#19747,#19748,
#19749,#19750,#19751,#19752,#19753,#19754,#19755,#19756,#19757,#19758,#19759,
#19760,#19761,#19762,#19763,#19764,#19765,#19766,#19767,#19768,#19769,#19770,
#19771,#19772,#19773,#19774,#19775,#19776,#19777,#19778,#19779,#19780,#19781,
#19782,#19783,#19784,#19785,#19786,#19787,#19788,#19789,#19790,#19791,#19792,
#19793,#19794,#19795,#19796,#19797,#19798,#19799,#19800,#19801,#19802,#19803,
#19804,#19805,#19806,#19807,#19808,#19809,#19810,#19811,#19812,#19813,#19814,
#19815,#19816,#19817,#19818,#19819,#19820,#19821,#19822,#19823,#19824,#19825,
#19826,#19827,#19828,#19829,#19830,#19831,#19832,#19833,#19834,#19835,#19836,
#19837,#19838,#19839,#19840,#19841,#19842,#19843,#19844,#19845,#19846,#19847,
#19848,#19849,#19850,#19851,#19852,#19853,#19854,#19855,#19856,#19857,#19858,
#19859,#19860,#19861,#19862,#19863,#19864,#19865,#19866,#19867,#19868,#19869,
#19870,#19871,#19872,#19873,#19874,#19875,#19876,#19877,#19878,#19879,#19880,
#19881,#19882,#19883,#19884,#19885,#19886,#19887,#19888,#19889,#19890,#19891,
#19892,#19893,#19894,#19895,#19896,#19897,#19898,#19899,#19900,#19901,#19902,
#19903,#19904,#19905,#19906,#19907,#19908,#19909,#19910,#19911,#19912,#19913,
#19914,#19915,#19916,#19917,#19918,#19919,#19920),.UNSPECIFIED.,.F.,.F.,
(4,3,3,3,3,3,3,3,3,3,3,3,3,3,3,3,3,3,3,3,3,3,3,3,3,3,3,3,3,3,3,3,3,3,3,
3,3,3,3,3,3,3,3,3,3,3,3,3,3,3,3,3,3,3,3,3,3,3,3,3,3,3,3,3,3,3,3,3,3,3,3,
3,3,3,3,3,3,4),(-136.03943319961,-135.954916822178,-135.870396318605,-135.785855626795,
-135.765053115823,-135.681167445922,-135.597298268663,-135.513425891983,
-135.429559062834,-135.345670156044,-135.265916891133,-135.182031221228,
-135.098162043964,-135.01428966728,-134.930422838127,-134.846533931332,
-134.766780666442,-134.682894996539,-134.599025819279,-134.515153442598,
-134.431286613447,-134.347397706655,-134.267644441752,-134.183758771847,
-134.099889594585,-134.016017217902,-133.932150388749,-133.848261481955,
-133.768508217061,-133.684622547158,-133.600753369897,-133.516880993216,
-133.433014164065,-133.349125257273,-133.269371992371,-133.185486322466,
-133.101617145203,-133.017744768521,-132.933877939368,-132.849989032574,
-132.77023576768,-132.686350097777,-132.602480920516,-132.518608543835,
-132.434741714684,-132.350852807892,-132.27109954299,-132.187213873086,
-132.103344695825,-132.019472319143,-131.935605489991,-131.851716583198,
-131.771963318299,-131.688077648394,-131.604208471131,-131.520336094447,
-131.436469265294,-131.3525803585,-131.272827093608,-131.188941423706,-131.105072246446,
-131.021199869766,-130.937333040617,-130.853444133825,-130.773690868918,
-130.689805199013,-130.605936021749,-130.522063645066,-130.438196815913,
-130.354307909119,-130.274554644227,-130.190668974324,-130.106799797063,
-130.022927420382,-129.939060591231,-129.855171684438,-129.775418419537,
-129.75624789243),.UNSPECIFIED.);
#288=B_SPLINE_CURVE_WITH_KNOTS('',3,(#19921,#19922,#19923,#19924,#19925,
#19926,#19927,#19928,#19929,#19930,#19931,#19932,#19933,#19934,#19935,#19936),
 .UNSPECIFIED.,.F.,.F.,(4,1,1,1,1,1,1,1,1,1,1,1,1,4),(126.782561270967,
127.212343462772,127.71121539792,128.210087333068,128.708959268216,129.207831203364,
129.706703138512,130.20557507366,130.704447008809,131.203318943957,131.702190879105,
132.201062814253,132.699934749401,133.065746544309),.UNSPECIFIED.);
#289=B_SPLINE_CURVE_WITH_KNOTS('',3,(#19941,#19942,#19943,#19944,#19945,
#19946,#19947,#19948,#19949,#19950,#19951,#19952,#19953,#19954,#19955,#19956,
#19957,#19958,#19959,#19960,#19961,#19962,#19963,#19964,#19965,#19966,#19967,
#19968,#19969,#19970,#19971,#19972,#19973,#19974,#19975,#19976,#19977,#19978,
#19979,#19980,#19981,#19982,#19983,#19984,#19985,#19986,#19987,#19988,#19989,
#19990,#19991,#19992,#19993,#19994,#19995,#19996,#19997,#19998,#19999,#20000,
#20001,#20002,#20003,#20004,#20005,#20006,#20007,#20008,#20009,#20010,#20011,
#20012,#20013,#20014,#20015,#20016,#20017,#20018,#20019,#20020,#20021,#20022,
#20023,#20024,#20025,#20026,#20027,#20028,#20029,#20030,#20031,#20032,#20033,
#20034,#20035,#20036,#20037,#20038,#20039,#20040,#20041,#20042,#20043,#20044,
#20045,#20046,#20047,#20048,#20049,#20050,#20051,#20052,#20053,#20054,#20055,
#20056,#20057,#20058,#20059,#20060,#20061,#20062,#20063,#20064,#20065,#20066,
#20067,#20068,#20069,#20070,#20071,#20072,#20073,#20074,#20075,#20076,#20077,
#20078,#20079,#20080,#20081,#20082,#20083,#20084,#20085,#20086,#20087,#20088,
#20089,#20090,#20091,#20092,#20093,#20094,#20095,#20096,#20097,#20098,#20099,
#20100,#20101,#20102,#20103,#20104,#20105,#20106,#20107,#20108,#20109,#20110,
#20111,#20112,#20113,#20114,#20115,#20116,#20117,#20118,#20119,#20120,#20121,
#20122,#20123,#20124,#20125,#20126,#20127,#20128,#20129,#20130,#20131,#20132,
#20133,#20134,#20135,#20136,#20137,#20138,#20139,#20140,#20141,#20142,#20143,
#20144,#20145,#20146,#20147,#20148,#20149,#20150,#20151,#20152,#20153,#20154,
#20155,#20156,#20157,#20158,#20159,#20160,#20161,#20162,#20163,#20164,#20165,
#20166,#20167,#20168,#20169),.UNSPECIFIED.,.F.,.F.,(4,3,3,3,3,3,3,3,3,3,
3,3,3,3,3,3,3,3,3,3,3,3,3,3,3,3,3,3,3,3,3,3,3,3,3,3,3,3,3,3,3,3,3,3,3,3,
3,3,3,3,3,3,3,3,3,3,3,3,3,3,3,3,3,3,3,3,3,3,3,3,3,3,3,3,3,3,4),(-142.322618506789,
-142.2538240368,-142.169938366889,-142.08606918962,-142.002196812931,-141.918329983772,
-141.834441076971,-141.754687812109,-141.670802142209,-141.586932964951,
-141.503060588272,-141.419193759124,-141.335304852334,-141.255551587419,
-141.171665917514,-141.08779674025,-141.003924363566,-140.920057534413,
-140.836168627618,-140.756415362728,-140.672529692825,-140.588660515564,
-140.504788138883,-140.420921309732,-140.33703240294,-140.257279138038,
-140.173393468133,-140.089524290871,-140.005651914188,-139.921785085036,
-139.837896178242,-139.758142913347,-139.674257243444,-139.590388066183,
-139.506515689502,-139.422648860351,-139.338759953558,-139.259006688657,
-139.175121018752,-139.09125184149,-139.007379464807,-138.923512635655,
-138.839623728861,-138.759870463966,-138.675984794063,-138.592115616802,
-138.508243240121,-138.42437641097,-138.340487504177,-138.260734239276,
-138.176848569371,-138.092979392109,-138.009107015426,-137.925240186274,
-137.84135127948,-137.761598014585,-137.677712344682,-137.593843167421,
-137.50997079074,-137.426103961589,-137.342215054797,-137.262461789895,
-137.17857611999,-137.094706942727,-137.010834566045,-136.926967736892,
-136.843078830098,-136.763325565204,-136.679439895301,-136.595570718039,
-136.511698341357,-136.427831512206,-136.343942605413,-136.264189340514,
-136.178785436816,-136.09340281952,-136.039433199766),.UNSPECIFIED.);
#290=B_SPLINE_CURVE_WITH_KNOTS('',3,(#20170,#20171,#20172,#20173,#20174,
#20175,#20176,#20177,#20178,#20179,#20180,#20181,#20182,#20183,#20184,#20185,
#20186,#20187,#20188,#20189,#20190,#20191,#20192,#20193,#20194,#20195,#20196,
#20197,#20198,#20199,#20200,#20201,#20202,#20203,#20204,#20205,#20206,#20207,
#20208,#20209,#20210,#20211,#20212,#20213,#20214,#20215,#20216,#20217,#20218,
#20219,#20220,#20221,#20222,#20223,#20224,#20225,#20226,#20227,#20228,#20229,
#20230,#20231,#20232,#20233,#20234,#20235,#20236,#20237,#20238,#20239,#20240,
#20241,#20242,#20243,#20244,#20245,#20246,#20247,#20248,#20249,#20250,#20251,
#20252,#20253,#20254,#20255,#20256,#20257,#20258,#20259,#20260,#20261,#20262,
#20263,#20264,#20265,#20266,#20267,#20268,#20269,#20270,#20271,#20272,#20273,
#20274,#20275,#20276,#20277,#20278,#20279,#20280,#20281,#20282,#20283,#20284,
#20285,#20286,#20287,#20288,#20289,#20290,#20291,#20292,#20293,#20294,#20295,
#20296,#20297,#20298,#20299,#20300,#20301,#20302,#20303,#20304,#20305,#20306,
#20307,#20308,#20309,#20310,#20311,#20312,#20313,#20314,#20315,#20316,#20317,
#20318,#20319,#20320,#20321,#20322,#20323,#20324,#20325,#20326,#20327,#20328,
#20329,#20330,#20331,#20332,#20333,#20334,#20335,#20336,#20337,#20338,#20339,
#20340,#20341,#20342,#20343,#20344,#20345,#20346,#20347,#20348,#20349,#20350,
#20351,#20352,#20353,#20354,#20355,#20356,#20357,#20358,#20359,#20360,#20361,
#20362,#20363,#20364,#20365,#20366,#20367,#20368,#20369,#20370,#20371,#20372,
#20373,#20374,#20375,#20376,#20377,#20378,#20379,#20380,#20381,#20382,#20383,
#20384,#20385,#20386,#20387,#20388,#20389,#20390,#20391,#20392,#20393,#20394,
#20395,#20396,#20397,#20398),.UNSPECIFIED.,.F.,.F.,(4,3,3,3,3,3,3,3,3,3,
3,3,3,3,3,3,3,3,3,3,3,3,3,3,3,3,3,3,3,3,3,3,3,3,3,3,3,3,3,3,3,3,3,3,3,3,
3,3,3,3,3,3,3,3,3,3,3,3,3,3,3,3,3,3,3,3,3,3,3,3,3,3,3,3,3,3,4),(133.06574654591,
133.153625358515,133.198806684549,133.28269379382,133.36656443332,133.450438270789,
133.534306572632,133.618196896589,133.697678619697,133.781565728968,133.865436368467,
133.949310205935,134.033178507778,134.117068831734,134.196550554845,134.280437664118,
134.364308303619,134.448182141089,134.532050442935,134.615940766893,134.695422489994,
134.779309599265,134.863180238764,134.947054076232,135.030922378076,135.114812702032,
135.194294425142,135.278181534413,135.362052173913,135.445926011381,135.529794313224,
135.613684637181,135.69316636029,135.777053469562,135.860924109062,135.944797946531,
136.028666248375,136.112556572332,136.192038295438,136.275925404709,136.359796044209,
136.443669881677,136.527538183521,136.611428507478,136.690910230586,136.774797339857,
136.858667979357,136.942541816826,137.02641011867,137.110300442627,137.189782165734,
137.273669275005,137.357539914505,137.441413751974,137.525282053817,137.609172377774,
137.688654100882,137.772541210153,137.856411849652,137.94028568712,138.024153988963,
138.108044312919,138.18752603603,138.271413145303,138.355283784804,138.439157622274,
138.52302592412,138.606916248078,138.686397971179,138.77028508045,138.854155719949,
138.938029557418,139.021897859261,139.105788183218,139.185269906327,139.27217567586,
139.348931851342),.UNSPECIFIED.);
#291=B_SPLINE_CURVE_WITH_KNOTS('',3,(#20403,#20404,#20405,#20406,#20407,
#20408,#20409,#20410,#20411,#20412,#20413,#20414,#20415,#20416,#20417,#20418,
#20419,#20420,#20421,#20422,#20423,#20424,#20425,#20426,#20427,#20428,#20429,
#20430,#20431,#20432,#20433,#20434,#20435,#20436,#20437,#20438,#20439,#20440,
#20441,#20442,#20443,#20444,#20445,#20446,#20447,#20448,#20449,#20450,#20451,
#20452,#20453,#20454,#20455,#20456,#20457,#20458,#20459,#20460,#20461,#20462,
#20463,#20464,#20465,#20466,#20467,#20468,#20469,#20470,#20471,#20472,#20473,
#20474,#20475,#20476,#20477,#20478,#20479,#20480,#20481,#20482,#20483,#20484,
#20485,#20486,#20487,#20488,#20489,#20490,#20491,#20492,#20493,#20494,#20495,
#20496,#20497,#20498,#20499,#20500,#20501,#20502,#20503,#20504,#20505,#20506,
#20507,#20508,#20509,#20510,#20511,#20512,#20513,#20514,#20515,#20516,#20517,
#20518,#20519,#20520,#20521,#20522,#20523,#20524,#20525,#20526,#20527,#20528,
#20529,#20530,#20531,#20532,#20533,#20534,#20535,#20536,#20537,#20538,#20539,
#20540,#20541,#20542,#20543,#20544,#20545,#20546,#20547,#20548,#20549,#20550,
#20551,#20552,#20553,#20554,#20555,#20556,#20557,#20558,#20559,#20560,#20561,
#20562,#20563,#20564,#20565,#20566,#20567,#20568,#20569,#20570,#20571,#20572,
#20573,#20574,#20575,#20576,#20577,#20578,#20579,#20580,#20581,#20582,#20583,
#20584,#20585,#20586,#20587,#20588,#20589,#20590,#20591,#20592,#20593,#20594,
#20595,#20596,#20597,#20598,#20599,#20600,#20601,#20602,#20603,#20604,#20605,
#20606,#20607,#20608,#20609,#20610,#20611,#20612,#20613,#20614,#20615,#20616,
#20617,#20618,#20619,#20620,#20621,#20622,#20623,#20624,#20625,#20626,#20627,
#20628,#20629,#20630,#20631,#20632,#20633,#20634),.UNSPECIFIED.,.F.,.F.,
(4,3,3,3,3,3,3,3,3,3,3,3,3,3,3,3,3,3,3,3,3,3,3,3,3,3,3,3,3,3,3,3,3,3,3,
3,3,3,3,3,3,3,3,3,3,3,3,3,3,3,3,3,3,3,3,3,3,3,3,3,3,3,3,3,3,3,3,3,3,3,3,
3,3,3,3,3,3,4),(-148.605803813969,-148.522140022128,-148.438471933085,-148.354805244716,
-148.271119566466,-148.243458733086,-148.159573063184,-148.075703885924,
-147.991831509244,-147.907964680095,-147.824075773303,-147.744322508396,
-147.660436838491,-147.576567661227,-147.492695284544,-147.408828455391,
-147.324939548596,-147.245186283705,-147.161300613802,-147.077431436542,
-146.993559059861,-146.90969223071,-146.825803323918,-146.746050059015,
-146.66216438911,-146.578295211848,-146.494422835165,-146.410556006012,
-146.326667099218,-146.246913834324,-146.163028164421,-146.079158987161,
-145.99528661048,-145.911419781329,-145.827530874536,-145.747777609634,
-145.663891939729,-145.580022762467,-145.496150385784,-145.412283556631,
-145.328394649837,-145.248641384943,-145.16475571504,-145.080886537779,
-144.997014161098,-144.913147331947,-144.829258425155,-144.749505160253,
-144.665619490348,-144.581750313085,-144.497877936402,-144.41401110725,
-144.330122200456,-144.250368935562,-144.166483265659,-144.082614088398,
-143.998741711717,-143.914874882566,-143.830985975773,-143.751232710872,
-143.667347040967,-143.583477863704,-143.499605487021,-143.415738657868,
-143.331849751074,-143.252096486181,-143.168210816278,-143.084341639018,
-143.000469262337,-142.916602433186,-142.832713526393,-142.752960261491,
-142.669402437547,-142.582706454893,-142.499167632398,-142.415631931664,
-142.332082149227,-142.322618506932),.UNSPECIFIED.);
#292=B_SPLINE_CURVE_WITH_KNOTS('',3,(#20635,#20636,#20637,#20638,#20639,
#20640,#20641,#20642,#20643,#20644,#20645,#20646,#20647,#20648,#20649,#20650,
#20651,#20652,#20653,#20654,#20655,#20656,#20657,#20658,#20659,#20660,#20661,
#20662,#20663,#20664,#20665,#20666,#20667,#20668,#20669,#20670,#20671,#20672,
#20673,#20674,#20675,#20676,#20677,#20678,#20679,#20680,#20681,#20682,#20683,
#20684,#20685,#20686,#20687,#20688,#20689,#20690,#20691,#20692,#20693,#20694,
#20695,#20696,#20697,#20698,#20699,#20700,#20701,#20702,#20703,#20704,#20705,
#20706,#20707,#20708,#20709,#20710,#20711,#20712,#20713,#20714,#20715,#20716,
#20717,#20718,#20719,#20720,#20721,#20722,#20723,#20724,#20725,#20726,#20727,
#20728,#20729,#20730,#20731,#20732,#20733,#20734,#20735,#20736,#20737,#20738,
#20739,#20740,#20741,#20742,#20743,#20744,#20745,#20746,#20747,#20748,#20749,
#20750,#20751,#20752,#20753,#20754,#20755,#20756,#20757,#20758,#20759,#20760,
#20761,#20762,#20763,#20764,#20765,#20766,#20767,#20768,#20769,#20770,#20771,
#20772,#20773,#20774,#20775,#20776,#20777,#20778,#20779,#20780,#20781,#20782,
#20783,#20784,#20785,#20786,#20787,#20788,#20789,#20790,#20791,#20792,#20793,
#20794,#20795,#20796,#20797,#20798,#20799,#20800,#20801,#20802,#20803,#20804,
#20805,#20806,#20807,#20808,#20809,#20810,#20811,#20812,#20813,#20814,#20815,
#20816,#20817,#20818,#20819,#20820,#20821,#20822,#20823,#20824,#20825,#20826,
#20827,#20828,#20829,#20830,#20831,#20832,#20833,#20834,#20835,#20836,#20837,
#20838,#20839,#20840,#20841,#20842,#20843,#20844,#20845,#20846,#20847,#20848,
#20849,#20850,#20851,#20852,#20853,#20854,#20855,#20856,#20857,#20858,#20859,
#20860,#20861,#20862,#20863),.UNSPECIFIED.,.F.,.F.,(4,3,3,3,3,3,3,3,3,3,
3,3,3,3,3,3,3,3,3,3,3,3,3,3,3,3,3,3,3,3,3,3,3,3,3,3,3,3,3,3,3,3,3,3,3,3,
3,3,3,3,3,3,3,3,3,3,3,3,3,3,3,3,3,3,3,3,3,3,3,3,3,3,3,3,3,3,4),(139.348931851489,
139.432781290692,139.516625387566,139.600492989817,139.684141841475,139.768028950746,
139.851899590246,139.935773427714,140.019641729558,140.103532053515,140.183013776623,
140.266900885895,140.350771525394,140.434645362863,140.518513664707,140.602403988664,
140.681885711771,140.765772821042,140.849643460542,140.93351729801,141.017385599854,
141.101275923811,141.180757646919,141.26464475619,141.34851539569,141.432389233158,
141.516257535002,141.600147858959,141.679629582067,141.763516691338,141.847387330838,
141.931261168306,142.01512947015,142.099019794107,142.178501517215,142.262388626485,
142.346259265984,142.430133103452,142.514001405295,142.597891729251,142.677373452363,
142.761260561636,142.845131201137,142.929005038607,143.012873340453,143.096763664411,
143.176245387512,143.260132496783,143.344003136282,143.42787697375,143.511745275594,
143.59563559955,143.67511732266,143.759004431931,143.84287507143,143.926748908899,
144.010617210742,144.094507534699,144.173989257808,144.257876367079,144.341747006579,
144.425620844049,144.509489145893,144.59337946985,144.672861192956,144.756748302227,
144.840618941727,144.924492779196,145.00836108104,145.092251404997,145.171733128104,
145.255379913839,145.33900944156,145.422639950478,145.506266407228,145.589910997829,
145.632117158518),.UNSPECIFIED.);
#293=B_SPLINE_CURVE_WITH_KNOTS('',3,(#20868,#20869,#20870,#20871,#20872,
#20873,#20874,#20875,#20876,#20877,#20878,#20879,#20880,#20881,#20882,#20883,
#20884),.UNSPECIFIED.,.F.,.F.,(4,1,1,1,1,1,1,1,1,1,1,1,1,1,4),(-154.888989121148,
-154.732229654063,-154.233093429373,-153.733957204682,-153.234820979992,
-152.735684755301,-152.236548530611,-151.73741230592,-151.238276081229,
-150.739139856539,-150.240003631848,-149.740867407158,-149.241731182467,
-148.742594957777,-148.605803832893),.UNSPECIFIED.);
#294=B_SPLINE_CURVE_WITH_KNOTS('',3,(#20885,#20886,#20887,#20888,#20889,
#20890,#20891,#20892,#20893,#20894,#20895,#20896,#20897,#20898,#20899,#20900,
#20901,#20902,#20903,#20904,#20905,#20906,#20907,#20908,#20909,#20910,#20911,
#20912,#20913,#20914,#20915,#20916,#20917,#20918,#20919,#20920,#20921,#20922,
#20923,#20924,#20925,#20926,#20927,#20928,#20929,#20930,#20931,#20932,#20933,
#20934,#20935,#20936,#20937,#20938,#20939,#20940,#20941,#20942,#20943,#20944,
#20945,#20946,#20947,#20948,#20949,#20950,#20951,#20952,#20953,#20954,#20955,
#20956,#20957,#20958,#20959,#20960,#20961,#20962,#20963,#20964,#20965,#20966,
#20967,#20968,#20969,#20970,#20971,#20972,#20973,#20974,#20975,#20976,#20977,
#20978,#20979,#20980,#20981,#20982,#20983,#20984,#20985,#20986,#20987,#20988,
#20989,#20990,#20991,#20992,#20993,#20994,#20995,#20996,#20997,#20998,#20999,
#21000,#21001,#21002,#21003,#21004,#21005,#21006,#21007,#21008,#21009,#21010,
#21011,#21012,#21013,#21014,#21015,#21016,#21017,#21018,#21019,#21020,#21021,
#21022,#21023,#21024,#21025,#21026,#21027,#21028,#21029,#21030,#21031,#21032,
#21033,#21034,#21035,#21036,#21037,#21038,#21039,#21040,#21041,#21042,#21043,
#21044,#21045,#21046,#21047,#21048,#21049,#21050,#21051,#21052,#21053,#21054,
#21055,#21056,#21057,#21058,#21059,#21060,#21061,#21062,#21063,#21064,#21065,
#21066,#21067,#21068,#21069,#21070,#21071,#21072,#21073,#21074,#21075,#21076,
#21077,#21078,#21079,#21080,#21081,#21082,#21083,#21084,#21085,#21086,#21087,
#21088,#21089,#21090,#21091,#21092,#21093,#21094,#21095,#21096,#21097,#21098,
#21099,#21100,#21101,#21102,#21103,#21104,#21105,#21106,#21107,#21108,#21109,
#21110,#21111,#21112,#21113),.UNSPECIFIED.,.F.,.F.,(4,3,3,3,3,3,3,3,3,3,
3,3,3,3,3,3,3,3,3,3,3,3,3,3,3,3,3,3,3,3,3,3,3,3,3,3,3,3,3,3,3,3,3,3,3,3,
3,3,3,3,3,3,3,3,3,3,3,3,3,3,3,3,3,3,3,3,3,3,3,3,3,3,3,3,3,3,4),(145.632117158668,
145.670605063252,145.754492172522,145.83836281202,145.922236649487,146.006104951329,
146.089995275284,146.1694769984,146.253364107671,146.337234747171,146.421108584639,
146.504976886483,146.58886721044,146.668348933548,146.752236042821,146.836106682322,
146.919980519792,147.003848821637,147.087739145595,147.167220868697,147.251107977968,
147.334978617467,147.418852454935,147.502720756779,147.586611080735,147.666092803845,
147.749979913116,147.833850552616,147.917724390084,148.001592691927,148.085483015884,
148.164964738993,148.248851848265,148.332722487765,148.416596325233,148.500464627077,
148.584354951034,148.663836674141,148.747723783412,148.831594422912,148.91546826038,
148.999336562224,149.083226886181,149.162708609289,149.24659571856,149.33046635806,
149.414340195529,149.498208497373,149.58209882133,149.661580544437,149.745467653708,
149.829338293208,149.913212130677,149.99708043252,150.080970756477,150.160452479585,
150.244339588856,150.328210228355,150.412084065823,150.495952367666,150.579842691622,
150.659324414733,150.743211524006,150.827082163507,150.910956000977,150.994824302823,
151.078714626781,151.158196349882,151.242083459153,151.325954098653,151.409827936121,
151.493696237965,151.577586561921,151.65706828503,151.741856065642,151.828579265745,
151.915302465848),.UNSPECIFIED.);
#295=B_SPLINE_CURVE_WITH_KNOTS('',3,(#21118,#21119,#21120,#21121,#21122,
#21123,#21124,#21125,#21126,#21127,#21128,#21129,#21130,#21131,#21132,#21133),
 .UNSPECIFIED.,.F.,.F.,(4,1,1,1,1,1,1,1,1,1,1,1,1,4),(-161.172174428328,
-160.72186435035,-160.222728125659,-159.723591900968,-159.224455676278,
-158.725319451587,-158.226183226897,-157.727047002206,-157.227910777516,
-156.728774552825,-156.229638328135,-155.730502103444,-155.231365878754,
-154.888989121148),.UNSPECIFIED.);
#296=B_SPLINE_CURVE_WITH_KNOTS('',3,(#21134,#21135,#21136,#21137,#21138,
#21139,#21140,#21141,#21142,#21143,#21144,#21145,#21146,#21147,#21148,#21149,
#21150),.UNSPECIFIED.,.F.,.F.,(4,1,1,1,1,1,1,1,1,1,1,1,1,1,4),(151.915302472681,
152.155940220178,152.654812155326,153.153684090474,153.652556025622,154.15142796077,
154.650299895918,155.149171831067,155.648043766215,156.146915701363,156.645787636511,
157.144659571659,157.643531506807,158.142403441955,158.198487773027),
 .UNSPECIFIED.);
#297=B_SPLINE_CURVE_WITH_KNOTS('',3,(#21155,#21156,#21157,#21158,#21159,
#21160,#21161,#21162,#21163,#21164,#21165,#21166,#21167,#21168,#21169,#21170,
#21171),.UNSPECIFIED.,.F.,.F.,(4,1,1,1,1,1,1,1,1,1,1,1,1,1,4),(-167.455359731888,
-167.210635271326,-166.711499046636,-166.212362821945,-165.713226597255,
-165.214090372564,-164.714954147874,-164.215817923183,-163.716681698493,
-163.217545473802,-162.718409249112,-162.219273024421,-161.720136799731,
-161.22100057504,-161.172174428328),.UNSPECIFIED.);
#298=B_SPLINE_CURVE_WITH_KNOTS('',3,(#21172,#21173,#21174,#21175,#21176,
#21177,#21178,#21179,#21180,#21181,#21182,#21183,#21184,#21185,#21186,#21187,
#21188,#21189,#21190,#21191,#21192,#21193,#21194,#21195,#21196,#21197,#21198,
#21199,#21200,#21201,#21202,#21203,#21204,#21205,#21206,#21207,#21208,#21209,
#21210,#21211,#21212,#21213,#21214,#21215,#21216,#21217,#21218,#21219,#21220,
#21221,#21222,#21223,#21224,#21225,#21226,#21227,#21228,#21229,#21230,#21231,
#21232,#21233,#21234,#21235,#21236,#21237,#21238,#21239,#21240,#21241,#21242,
#21243,#21244,#21245,#21246,#21247,#21248,#21249,#21250,#21251,#21252,#21253,
#21254,#21255,#21256,#21257,#21258,#21259,#21260,#21261,#21262,#21263,#21264,
#21265,#21266,#21267,#21268,#21269,#21270,#21271,#21272,#21273,#21274,#21275,
#21276,#21277,#21278,#21279,#21280,#21281,#21282,#21283,#21284,#21285,#21286,
#21287,#21288,#21289,#21290,#21291,#21292,#21293,#21294,#21295,#21296,#21297,
#21298,#21299,#21300,#21301,#21302,#21303,#21304,#21305,#21306,#21307,#21308,
#21309,#21310,#21311,#21312,#21313,#21314,#21315,#21316,#21317,#21318,#21319,
#21320,#21321,#21322,#21323,#21324,#21325,#21326,#21327,#21328,#21329,#21330,
#21331,#21332,#21333,#21334,#21335,#21336,#21337,#21338,#21339,#21340,#21341,
#21342,#21343,#21344,#21345,#21346,#21347,#21348,#21349,#21350,#21351,#21352,
#21353,#21354,#21355,#21356,#21357,#21358,#21359,#21360,#21361,#21362,#21363,
#21364,#21365,#21366,#21367,#21368,#21369,#21370,#21371,#21372,#21373,#21374,
#21375,#21376,#21377,#21378,#21379,#21380,#21381,#21382,#21383,#21384,#21385,
#21386,#21387,#21388,#21389,#21390,#21391,#21392,#21393,#21394,#21395,#21396,
#21397,#21398,#21399,#21400,#21401,#21402,#21403),.UNSPECIFIED.,.F.,.F.,
(4,3,3,3,3,3,3,3,3,3,3,3,3,3,3,3,3,3,3,3,3,3,3,3,3,3,3,3,3,3,3,3,3,3,3,
3,3,3,3,3,3,3,3,3,3,3,3,3,3,3,3,3,3,3,3,3,3,3,3,3,3,3,3,3,3,3,3,3,3,3,3,
3,3,3,3,3,3,4),(158.198487773027,158.282067716573,158.365632542258,158.449200633782,
158.53276711861,158.616352361724,158.641275377103,158.725162486376,158.809033125877,
158.892906963347,158.976775265193,159.060665589151,159.140147312252,159.224034421523,
159.307905061022,159.391778898491,159.475647200334,159.55953752429,159.6390192474,
159.722906356671,159.80677699617,159.890650833639,159.974519135482,160.058409459439,
160.137891182548,160.221778291819,160.305648931319,160.389522768788,160.473391070632,
160.557281394589,160.636763117696,160.720650226967,160.804520866467,160.888394703936,
160.97226300578,161.056153329736,161.135635052844,161.219522162115,161.303392801615,
161.387266639084,161.471134940928,161.555025264885,161.634506987992,161.718394097263,
161.802264736764,161.886138574232,161.970006876076,162.053897200033,162.13337892314,
162.21726603241,162.301136671909,162.385010509377,162.46887881122,162.552769135176,
162.632250858288,162.716137967561,162.800008607062,162.883882444532,162.967750746378,
163.051641070336,163.131122793437,163.215009902708,163.298880542208,163.382754379676,
163.466622681519,163.550513005476,163.629994728585,163.713881837856,163.797752477355,
163.881626314824,163.965494616667,164.049384940624,164.128866663733,164.212606748055,
164.296333176365,164.380048090638,164.463765710071,164.481673080207),
 .UNSPECIFIED.);
#299=B_SPLINE_CURVE_WITH_KNOTS('',3,(#21408,#21409,#21410,#21411,#21412,
#21413,#21414,#21415,#21416,#21417,#21418,#21419,#21420,#21421,#21422,#21423,
#21424,#21425,#21426,#21427,#21428,#21429,#21430,#21431,#21432,#21433,#21434,
#21435,#21436,#21437,#21438,#21439,#21440,#21441,#21442,#21443,#21444,#21445,
#21446,#21447,#21448,#21449,#21450,#21451,#21452,#21453,#21454,#21455,#21456,
#21457,#21458,#21459,#21460,#21461,#21462,#21463,#21464,#21465,#21466,#21467,
#21468,#21469,#21470,#21471,#21472,#21473,#21474,#21475,#21476,#21477,#21478,
#21479,#21480,#21481,#21482,#21483,#21484,#21485,#21486,#21487,#21488,#21489,
#21490,#21491,#21492,#21493,#21494,#21495,#21496,#21497,#21498,#21499,#21500,
#21501,#21502,#21503,#21504,#21505,#21506,#21507,#21508,#21509,#21510,#21511,
#21512,#21513,#21514,#21515,#21516,#21517,#21518,#21519,#21520,#21521,#21522,
#21523,#21524,#21525,#21526,#21527,#21528,#21529,#21530,#21531,#21532,#21533,
#21534,#21535,#21536,#21537,#21538,#21539,#21540,#21541,#21542,#21543,#21544,
#21545,#21546,#21547,#21548,#21549,#21550,#21551,#21552,#21553,#21554,#21555,
#21556,#21557,#21558,#21559,#21560,#21561,#21562,#21563,#21564,#21565,#21566,
#21567,#21568,#21569,#21570,#21571,#21572,#21573,#21574,#21575,#21576,#21577,
#21578,#21579,#21580,#21581,#21582,#21583,#21584,#21585,#21586,#21587,#21588,
#21589,#21590,#21591,#21592,#21593,#21594,#21595,#21596,#21597,#21598,#21599,
#21600,#21601,#21602,#21603,#21604,#21605,#21606,#21607,#21608,#21609,#21610,
#21611,#21612,#21613,#21614,#21615,#21616,#21617,#21618,#21619,#21620,#21621,
#21622,#21623,#21624,#21625,#21626,#21627,#21628,#21629,#21630,#21631,#21632,
#21633,#21634,#21635,#21636),.UNSPECIFIED.,.F.,.F.,(4,3,3,3,3,3,3,3,3,3,
3,3,3,3,3,3,3,3,3,3,3,3,3,3,3,3,3,3,3,3,3,3,3,3,3,3,3,3,3,3,3,3,3,3,3,3,
3,3,3,3,3,3,3,3,3,3,3,3,3,3,3,3,3,3,3,3,3,3,3,3,3,3,3,3,3,3,4),(-173.738545042687,
-173.699406192303,-173.615520474108,-173.531651247652,-173.447778820846,
-173.36391194116,-173.280022983632,-173.200269967613,-173.116384358978,
-173.032515243893,-172.9486429302,-172.864776164356,-172.780887320795,-172.701133742922,
-172.617248030574,-172.533378810287,-172.449506390094,-172.365639517252,
-172.281750566889,-172.201997518232,-172.118111870431,-172.034242715556,
-171.950370361485,-171.866503555021,-171.782614670828,-171.702861293541,
-171.618975614894,-171.535106428785,-171.451234043183,-171.367367205088,
-171.283478289399,-171.203725068851,-171.119839401012,-171.035970225832,
-170.95209785124,-170.868231024179,-170.784342119456,-170.70458884416,-170.620703174694,
-170.536833997881,-170.452961621661,-170.369094792976,-170.285205886656,
-170.20545261947,-170.12156694863,-170.037697770418,-169.953825392773,-169.869958562653,
-169.786069654891,-169.706316394779,-169.622430725601,-169.538561549075,
-169.454689173137,-169.370822344733,-169.286933438686,-169.207180170088,
-169.123294499777,-169.039425322103,-168.955552945005,-168.871686115435,
-168.787797208226,-168.708043945398,-168.62415827567,-168.540289098585,
-168.456416722082,-168.37254989311,-168.288660986495,-168.208907720707,
-168.125022050752,-168.041152873438,-167.957280496704,-167.8734136675,-167.789524760655,
-167.709771496017,-167.624918798546,-167.540081689336,-167.455359735508),
 .UNSPECIFIED.);
#300=B_SPLINE_CURVE_WITH_KNOTS('',3,(#21637,#21638,#21639,#21640,#21641,
#21642,#21643,#21644,#21645,#21646,#21647,#21648,#21649,#21650,#21651,#21652,
#21653,#21654,#21655,#21656,#21657,#21658,#21659,#21660,#21661,#21662,#21663,
#21664,#21665,#21666,#21667,#21668,#21669,#21670,#21671,#21672,#21673,#21674,
#21675,#21676,#21677,#21678,#21679,#21680,#21681,#21682,#21683,#21684,#21685,
#21686,#21687,#21688,#21689,#21690,#21691,#21692,#21693,#21694,#21695,#21696,
#21697,#21698,#21699,#21700,#21701,#21702,#21703,#21704,#21705,#21706,#21707,
#21708,#21709,#21710,#21711,#21712,#21713,#21714,#21715,#21716,#21717,#21718,
#21719,#21720,#21721,#21722,#21723,#21724,#21725,#21726,#21727,#21728,#21729,
#21730,#21731,#21732,#21733,#21734,#21735,#21736,#21737,#21738,#21739,#21740,
#21741,#21742,#21743,#21744,#21745,#21746,#21747,#21748,#21749,#21750,#21751,
#21752,#21753,#21754,#21755,#21756,#21757,#21758,#21759,#21760,#21761,#21762,
#21763,#21764,#21765,#21766,#21767,#21768,#21769,#21770,#21771,#21772,#21773,
#21774,#21775,#21776,#21777,#21778,#21779,#21780,#21781,#21782,#21783,#21784,
#21785,#21786,#21787,#21788,#21789,#21790,#21791,#21792,#21793,#21794,#21795,
#21796,#21797,#21798,#21799,#21800,#21801,#21802,#21803,#21804,#21805,#21806,
#21807,#21808,#21809,#21810,#21811,#21812,#21813,#21814,#21815,#21816,#21817,
#21818,#21819,#21820,#21821,#21822,#21823,#21824,#21825,#21826,#21827,#21828,
#21829,#21830,#21831,#21832,#21833,#21834,#21835,#21836,#21837,#21838,#21839,
#21840,#21841,#21842,#21843,#21844,#21845,#21846,#21847,#21848,#21849,#21850,
#21851,#21852,#21853,#21854,#21855,#21856,#21857,#21858,#21859,#21860,#21861,
#21862,#21863,#21864,#21865),.UNSPECIFIED.,.F.,.F.,(4,3,3,3,3,3,3,3,3,3,
3,3,3,3,3,3,3,3,3,3,3,3,3,3,3,3,3,3,3,3,3,3,3,3,3,3,3,3,3,3,3,3,3,3,3,3,
3,3,3,3,3,3,3,3,3,3,3,3,3,3,3,3,3,3,3,3,3,3,3,3,3,3,3,3,3,3,4),(164.481673080314,
164.569118274427,164.627738598881,164.711625708152,164.795496347652,164.87937018512,
164.963238486964,165.04712881092,165.126610534029,165.2104976433,165.2943682828,
165.378242120268,165.462110422112,165.546000746069,165.625482469177,165.709369578449,
165.793240217948,165.877114055417,165.960982357261,166.044872681218,166.124354404325,
166.208241513596,166.292112153095,166.375985990563,166.459854292407,166.543744616363,
166.623226339473,166.707113448745,166.790984088245,166.874857925714,166.958726227558,
167.042616551515,167.122098274622,167.205985383896,167.289856023399,167.373729860871,
167.457598162718,167.541488486678,167.62097020977,167.704857319034,167.788727958525,
167.872601795986,167.956470097822,168.040360421771,168.119842144918,168.203729254202,
168.287599893714,168.371473731196,168.455342033052,168.539232357021,168.618714080066,
168.702601189323,168.786471828809,168.870345666264,168.954213968094,169.038104292037,
169.117586015214,169.201473124485,169.285343763985,169.369217601454,169.453085903297,
169.536976227254,169.616457950362,169.700345059686,169.784215699238,169.86808953676,
169.951957838656,170.035848162665,170.11532988551,170.199216994602,170.283087633921,
170.36696147121,170.450829772875,170.534720096655,170.614201820658,170.701501165913,
170.764858384118),.UNSPECIFIED.);
#301=B_SPLINE_CURVE_WITH_KNOTS('',3,(#21871,#21872,#21873,#21874,#21875,
#21876,#21877,#21878,#21879,#21880,#21881,#21882,#21883,#21884,#21885,#21886,
#21887,#21888,#21889,#21890,#21891,#21892,#21893,#21894,#21895,#21896,#21897,
#21898,#21899,#21900,#21901,#21902,#21903,#21904,#21905,#21906,#21907,#21908,
#21909,#21910,#21911,#21912,#21913,#21914,#21915,#21916,#21917,#21918,#21919,
#21920,#21921,#21922,#21923,#21924,#21925,#21926,#21927,#21928,#21929,#21930,
#21931,#21932,#21933,#21934,#21935,#21936,#21937,#21938,#21939,#21940,#21941,
#21942,#21943,#21944,#21945,#21946,#21947,#21948,#21949,#21950,#21951,#21952,
#21953,#21954,#21955,#21956,#21957,#21958,#21959,#21960,#21961,#21962,#21963,
#21964,#21965,#21966,#21967,#21968,#21969,#21970,#21971,#21972,#21973,#21974,
#21975,#21976,#21977,#21978,#21979,#21980,#21981,#21982,#21983,#21984,#21985,
#21986,#21987,#21988,#21989,#21990,#21991,#21992,#21993,#21994,#21995,#21996,
#21997,#21998,#21999,#22000,#22001,#22002,#22003,#22004,#22005,#22006,#22007,
#22008,#22009,#22010,#22011,#22012,#22013,#22014,#22015,#22016,#22017,#22018,
#22019,#22020,#22021,#22022,#22023,#22024,#22025,#22026,#22027,#22028,#22029,
#22030,#22031,#22032,#22033,#22034,#22035,#22036,#22037,#22038,#22039,#22040,
#22041,#22042,#22043,#22044,#22045,#22046,#22047,#22048,#22049,#22050,#22051,
#22052,#22053,#22054,#22055,#22056,#22057,#22058,#22059,#22060,#22061,#22062,
#22063,#22064,#22065,#22066,#22067,#22068,#22069,#22070,#22071,#22072,#22073,
#22074,#22075,#22076,#22077,#22078,#22079,#22080,#22081,#22082,#22083,#22084,
#22085,#22086),.UNSPECIFIED.,.F.,.F.,(4,2,2,2,2,2,2,2,2,2,2,2,2,2,2,2,2,
2,2,2,2,2,2,2,2,2,2,2,2,2,2,2,2,2,2,2,2,2,2,2,2,2,2,2,2,2,2,2,2,2,2,2,2,
2,2,2,2,2,2,2,2,2,2,2,2,2,2,2,2,2,2,2,2,2,2,2,2,2,2,2,2,2,2,2,2,2,2,2,2,
2,2,2,2,2,2,2,2,2,2,2,2,2,2,2,2,2,2,4),(-2.50346624102753,-2.43566920503879,
-2.42234310441723,-2.41035223133324,-2.37127141320223,-2.31761164675876,
-2.29859044626815,-2.27703879221759,-2.2248560455562,-2.18904768902528,
-2.17607336568454,-2.1638362674717,-2.1239626082453,-2.08289413542988,-2.05863349320715,
-2.03821977278105,-2.00561269853488,-1.97829323757455,-1.94103356910006,
-1.92891303314842,-1.91578007696407,-1.89955124089702,-1.85806998165083,
-1.82268755444853,-1.80211163604484,-1.77857993497384,-1.75126575489051,
-1.70260310294369,-1.68726144390728,-1.67716363456753,-1.65689027179377,
-1.62317397840196,-1.58021080636604,-1.56120223810918,-1.53963604757273,
-1.52761556617662,-1.4722056871182,-1.44834505614351,-1.43770829427052,
-1.42482247531397,-1.41668210727651,-1.39252640615786,-1.35943129143669,
-1.32853587377931,-1.30821411897408,-1.28328768866377,-1.25290018652973,
-1.2030445926792,-1.1922795136485,-1.17962456865186,-1.16428534746891,-1.12819197914595,
-1.11363628885357,-1.08275460647199,-1.06243842889265,-1.03752117251266,
-1.00714964079731,-0.957239748577986,-0.946483423730389,-0.933818042528201,
-0.918460270652399,-0.882268090172703,-0.842592179484583,-0.823627131129384,
-0.812109376798758,-0.7853416346558,-0.747758021721972,-0.713514886085762,
-0.700886880660439,-0.696882063678745,-0.696137250227313,-0.695202287417338,
-0.694399496298766,-0.69366231154534,-0.692951505311127,-0.692239065910569,
-0.691501346633369,-0.690715330571306,-0.689855991440339,-0.688893893977781,
-0.68779255385779,-0.686505193452603,-0.669950760361063,-0.62627733587133,
-0.592875183501239,-0.576900412250272,-0.556514282642967,-0.533244428834864,
-0.484086277971169,-0.462531063040552,-0.452374125784664,-0.44147482145213,
-0.436499934341845,-0.415921371225028,-0.349296598887226,-0.328915722615678,
-0.325520518491996,-0.3208861435602,-0.293223633430687,-0.255120882169807,
-0.222254699809382,-0.209457603808669,-0.197591336071566,-0.129828723489989,
-0.0994569524648762,-0.079786402304052,-0.060619434171579,-0.000296546468343627),
 .UNSPECIFIED.);
#302=B_SPLINE_CURVE_WITH_KNOTS('',3,(#22089,#22090,#22091,#22092,#22093,
#22094,#22095,#22096,#22097,#22098,#22099,#22100,#22101,#22102,#22103,#22104,
#22105,#22106,#22107,#22108,#22109,#22110,#22111,#22112,#22113,#22114,#22115,
#22116,#22117,#22118,#22119,#22120,#22121,#22122,#22123,#22124,#22125,#22126,
#22127,#22128,#22129,#22130,#22131,#22132,#22133,#22134,#22135,#22136,#22137,
#22138,#22139,#22140,#22141,#22142,#22143,#22144,#22145,#22146,#22147,#22148,
#22149,#22150,#22151,#22152,#22153,#22154,#22155,#22156,#22157,#22158,#22159,
#22160,#22161,#22162,#22163,#22164,#22165,#22166,#22167,#22168,#22169,#22170,
#22171,#22172,#22173,#22174,#22175,#22176,#22177,#22178,#22179,#22180,#22181,
#22182,#22183,#22184,#22185,#22186,#22187,#22188,#22189,#22190,#22191,#22192,
#22193,#22194,#22195,#22196,#22197,#22198,#22199,#22200,#22201,#22202,#22203,
#22204,#22205,#22206,#22207,#22208,#22209,#22210,#22211,#22212,#22213,#22214,
#22215,#22216,#22217,#22218,#22219,#22220,#22221,#22222,#22223,#22224,#22225,
#22226,#22227),.UNSPECIFIED.,.F.,.F.,(4,3,3,3,3,3,3,3,3,3,3,3,3,3,3,3,3,
3,3,3,3,3,3,3,3,3,3,3,3,3,3,3,3,3,3,3,3,3,3,3,3,3,3,3,3,3,4),(11.6154215191107,
11.7037890220323,11.792149404157,11.88052357879,11.9688971865904,12.0572944191562,
12.1145577438013,12.2021423255354,12.2897048061461,12.3772666890726,12.4648219322771,
12.5523990053126,12.6136939684918,12.7016932197362,12.7896766558619,12.8776648682661,
12.9656484882494,13.0536532570389,13.1128301931823,13.2006194523635,13.2883899961423,
13.3761630672174,13.4639307927713,13.551720479078,13.6119664178728,13.6998390788243,
13.787694051925,13.8755522709807,13.9634053514766,14.0512799364259,14.1111026425634,
14.1989543387987,14.2867881460337,14.3746251065054,14.4624569262738,14.5503104433313,
14.6102388672539,14.6980876008522,14.7859183567643,14.873752161574,14.9615807742626,
15.0494310323098,15.1093750919444,15.1972366894229,15.2850783147494,15.3729229087857,
15.4568668615432),.UNSPECIFIED.);
#303=B_SPLINE_CURVE_WITH_KNOTS('',3,(#22232,#22233,#22234,#22235,#22236,
#22237,#22238,#22239,#22240,#22241,#22242,#22243,#22244,#22245,#22246,#22247,
#22248,#22249,#22250,#22251,#22252,#22253,#22254,#22255,#22256,#22257,#22258,
#22259,#22260,#22261,#22262,#22263,#22264,#22265,#22266,#22267,#22268,#22269,
#22270,#22271,#22272,#22273,#22274,#22275,#22276,#22277,#22278,#22279,#22280,
#22281,#22282,#22283,#22284,#22285,#22286,#22287,#22288,#22289,#22290,#22291,
#22292,#22293,#22294,#22295,#22296,#22297,#22298,#22299,#22300,#22301,#22302,
#22303,#22304,#22305,#22306,#22307,#22308,#22309,#22310,#22311,#22312,#22313,
#22314,#22315,#22316,#22317,#22318,#22319,#22320,#22321,#22322,#22323,#22324,
#22325,#22326,#22327,#22328,#22329,#22330,#22331,#22332,#22333,#22334,#22335,
#22336,#22337,#22338,#22339,#22340,#22341,#22342,#22343,#22344,#22345,#22346,
#22347,#22348,#22349,#22350,#22351,#22352,#22353,#22354,#22355,#22356,#22357,
#22358,#22359,#22360,#22361,#22362,#22363,#22364,#22365,#22366,#22367,#22368,
#22369,#22370,#22371,#22372,#22373,#22374,#22375,#22376,#22377,#22378,#22379,
#22380,#22381,#22382,#22383,#22384,#22385,#22386,#22387,#22388,#22389,#22390,
#22391,#22392,#22393,#22394,#22395,#22396,#22397,#22398,#22399,#22400,#22401,
#22402,#22403,#22404,#22405,#22406,#22407,#22408,#22409,#22410,#22411,#22412,
#22413,#22414,#22415,#22416,#22417,#22418,#22419,#22420,#22421,#22422,#22423,
#22424,#22425,#22426,#22427,#22428,#22429,#22430,#22431,#22432,#22433,#22434,
#22435,#22436,#22437,#22438,#22439,#22440,#22441,#22442,#22443,#22444,#22445,
#22446,#22447,#22448,#22449,#22450,#22451,#22452,#22453,#22454,#22455,#22456,
#22457,#22458,#22459,#22460,#22461,#22462,#22463,#22464,#22465),
 .UNSPECIFIED.,.F.,.F.,(4,2,2,2,2,2,2,2,2,2,2,2,2,2,2,2,2,2,2,2,2,2,2,2,
2,2,2,2,2,2,2,2,2,2,2,2,2,2,2,2,2,2,2,2,2,2,2,2,2,2,2,2,2,2,2,2,2,2,2,2,
2,2,2,2,2,2,2,2,2,2,2,2,2,2,2,2,2,2,2,2,2,2,2,2,2,2,2,2,2,2,2,2,2,2,2,2,
2,2,2,2,2,2,2,2,2,2,2,2,2,2,2,2,2,2,2,2,4),(-5.59900260275164,-5.57358240255277,
-5.51165284056021,-5.49263343147153,-5.47121234894638,-5.42398221307496,
-5.39516584557432,-5.3812712053524,-5.37134641644009,-5.35916799738254,
-5.32885752303004,-5.26581391524423,-5.24678968929203,-5.22534966611294,
-5.17847547088572,-5.14948182461449,-5.13554812274009,-5.12561293920981,
-5.11346219280575,-5.076415254475,-5.02096939997193,-5.00201805586705,-4.98089140929248,
-4.92791834000774,-4.9018770271356,-4.88862137263518,-4.87872227782179,
-4.8726118309089,-4.85291041528789,-4.80301215700534,-4.77906957765278,
-4.75715086190172,-4.73580964228653,-4.69625405224592,-4.66104010524081,
-4.64031843680571,-4.63018620019017,-4.61504399459285,-4.56657558685244,
-4.53777400190244,-4.51454876625657,-4.49411681288997,-4.45767782720016,
-4.4526939042528,-4.41037080659345,-4.39272768956872,-4.38168137600639,
-4.36302775406093,-4.31072814770884,-4.28703801625921,-4.26524071621447,
-4.24637696734528,-4.20907327992395,-4.16288904681854,-4.15484808569998,
-4.1420653383365,-4.12966941855086,-4.08642028836228,-4.0402578741606,-4.01869842575924,
-3.9970320789072,-3.94774176684927,-3.90851453659152,-3.89595078434686,
-3.88512761203502,-3.83595040185292,-3.80534008288096,-3.78031764295576,
-3.76000978685046,-3.72934084871589,-3.68216354281777,-3.67049623815089,
-3.66268637483629,-3.65014340250904,-3.63930659521469,-3.59045632130235,
-3.54581366141594,-3.52483920545617,-3.50234972282123,-3.45547769134334,
-3.41692070959218,-3.40437177170927,-3.39353894583252,-3.34421499832587,
-3.31369122375166,-3.28870648845562,-3.26839461624078,-3.23764478219075,
-3.19057679959306,-3.17892170112111,-3.17111705729583,-3.15857951209892,
-3.14773912298333,-3.09835172750094,-3.06787083493495,-3.04290480581821,
-3.02259085270363,-2.99180015628655,-2.94478715371729,-2.93313820362214,
-2.9253361890858,-2.91280137576584,-2.90016922072955,-2.86143600694281,
-2.81910702155092,-2.79527683714919,-2.77477688298191,-2.74069060294262,
-2.69060390246969,-2.67256321414734,-2.66152113907093,-2.64330037384373,
-2.62910108771731,-2.56115342594594,-2.54063289062032,-2.51766972993501,
-2.50346624102753),.UNSPECIFIED.);
#304=B_SPLINE_CURVE_WITH_KNOTS('',3,(#22467,#22468,#22469,#22470,#22471,
#22472,#22473,#22474,#22475,#22476,#22477,#22478,#22479),.UNSPECIFIED.,
 .F.,.F.,(4,3,3,3,4),(15.4568668615432,15.5447259441062,15.608511316635,
15.7018829174837,15.707963267949),.UNSPECIFIED.);
#305=B_SPLINE_CURVE_WITH_KNOTS('',3,(#22480,#22481,#22482,#22483,#22484,
#22485,#22486,#22487,#22488,#22489,#22490,#22491,#22492,#22493,#22494,#22495),
 .UNSPECIFIED.,.F.,.F.,(4,1,1,1,1,1,1,1,1,1,1,1,1,4),(15.7079632826947,
16.1076475413255,16.606783766016,17.1059199907065,17.6050562153971,18.1041924400876,
18.6033286647781,19.1024648894686,19.6016011141592,20.1007373388497,20.5998735635402,
21.0990097882307,21.5981460129213,21.7400919742423),.UNSPECIFIED.);
#306=B_SPLINE_CURVE_WITH_KNOTS('',3,(#22501,#22502,#22503,#22504,#22505,
#22506,#22507,#22508,#22509,#22510,#22511,#22512,#22513,#22514,#22515,#22516,
#22517,#22518,#22519,#22520,#22521,#22522,#22523,#22524,#22525,#22526,#22527,
#22528,#22529,#22530,#22531,#22532,#22533,#22534,#22535,#22536,#22537,#22538,
#22539,#22540,#22541,#22542,#22543,#22544,#22545,#22546,#22547,#22548,#22549,
#22550,#22551,#22552,#22553,#22554,#22555,#22556,#22557,#22558,#22559,#22560,
#22561,#22562,#22563,#22564,#22565,#22566,#22567,#22568,#22569,#22570,#22571,
#22572,#22573,#22574,#22575,#22576,#22577,#22578,#22579,#22580,#22581,#22582,
#22583,#22584,#22585,#22586,#22587,#22588,#22589,#22590,#22591,#22592,#22593,
#22594,#22595,#22596,#22597,#22598,#22599,#22600,#22601,#22602,#22603,#22604,
#22605,#22606,#22607,#22608,#22609,#22610,#22611,#22612,#22613,#22614,#22615,
#22616,#22617,#22618,#22619,#22620,#22621,#22622,#22623,#22624,#22625,#22626,
#22627,#22628,#22629,#22630,#22631,#22632,#22633,#22634,#22635,#22636,#22637,
#22638,#22639,#22640,#22641,#22642,#22643,#22644,#22645,#22646,#22647,#22648,
#22649,#22650,#22651,#22652,#22653,#22654,#22655,#22656,#22657,#22658,#22659,
#22660,#22661,#22662,#22663,#22664,#22665,#22666,#22667,#22668,#22669,#22670,
#22671,#22672,#22673,#22674,#22675,#22676,#22677,#22678,#22679,#22680,#22681,
#22682,#22683,#22684,#22685,#22686,#22687,#22688,#22689,#22690,#22691,#22692,
#22693,#22694,#22695,#22696,#22697,#22698,#22699,#22700,#22701,#22702,#22703,
#22704,#22705,#22706,#22707,#22708,#22709,#22710,#22711,#22712,#22713,#22714,
#22715,#22716,#22717,#22718,#22719,#22720,#22721,#22722,#22723,#22724,#22725,
#22726,#22727,#22728,#22729,#22730,#22731,#22732,#22733,#22734,#22735,#22736,
#22737,#22738,#22739,#22740,#22741,#22742,#22743,#22744,#22745,#22746,#22747,
#22748,#22749,#22750,#22751,#22752,#22753,#22754,#22755,#22756,#22757,#22758,
#22759,#22760,#22761,#22762,#22763,#22764,#22765,#22766,#22767,#22768,#22769,
#22770,#22771,#22772,#22773,#22774,#22775,#22776,#22777,#22778),
 .UNSPECIFIED.,.F.,.F.,(4,2,2,2,2,2,2,2,2,2,2,2,2,2,2,2,2,2,2,2,2,2,2,2,
2,2,2,2,2,2,2,2,2,2,2,2,2,2,2,2,2,2,2,2,2,2,2,2,2,2,2,2,2,2,2,2,2,2,2,2,
2,2,2,2,2,2,2,2,2,2,2,2,2,2,2,2,2,2,2,2,2,2,2,2,2,2,2,2,2,2,2,2,2,2,2,2,
2,2,2,2,2,2,2,2,2,2,2,2,2,2,2,2,2,2,2,2,2,2,2,2,2,2,2,2,2,2,2,2,2,2,2,2,
2,2,2,2,2,2,4),(-2.97196746186506,-2.96554523147083,-2.94375453468809,-2.9200782670592,
-2.86789256842528,-2.84913715582557,-2.83808885593877,-2.82053203157918,
-2.77326033280646,-2.73996878261319,-2.72087423787642,-2.69942052484035,
-2.68752647692188,-2.65638477391494,-2.61017277181855,-2.5975304658713,
-2.58500486364593,-2.54754739868587,-2.49346285010931,-2.47449444696937,
-2.45286562308431,-2.44077643098385,-2.38263843636578,-2.36073911712372,
-2.34937078793702,-2.33504290993638,-2.32544974605833,-2.29349861593572,
-2.24826374765408,-2.22919420733565,-2.20770812064741,-2.19577776633339,
-2.17956666855177,-2.12946516239794,-2.11137058604908,-2.1003284331591,
-2.08216188986844,-2.04059787428,-2.001735654572,-1.98279537104709,-1.96112352505991,
-1.91774281422472,-1.88041246503279,-1.86436234421339,-1.85438123978714,
-1.83595214157335,-1.80776113304496,-1.75924403899271,-1.73753185246712,
-1.71601464646001,-1.67292575493603,-1.62589690251005,-1.61368496978913,
-1.60067733179182,-1.59241774917134,-1.56768350400614,-1.51137060711735,
-1.49012079036956,-1.46807935799086,-1.44388203285615,-1.39176253176631,
-1.37388251137214,-1.36283924323199,-1.34444896643786,-1.29620030516498,
-1.26127745363222,-1.24072833206364,-1.21709824679231,-1.18957319606848,
-1.13316976391415,-1.12246831819291,-1.1097036729239,-1.1016804290902,-1.05554123375904,
-1.01815323081825,-0.999286043247915,-0.977493681817305,-0.953813956574885,
-0.901601889460169,-0.882869052147508,-0.871974343344133,-0.871451452338479,
-0.870924972089645,-0.870388005932971,-0.869834385563424,-0.86959819539595,
-0.86933921966252,-0.869052002827504,-0.868729804214971,-0.868364190597761,
-0.867944499445601,-0.867457130185425,-0.866884610757177,-0.866204378022422,
-0.86538720745753,-0.864395236690978,-0.863179555823405,-0.861677384207923,
-0.860450545261345,-0.841979054709722,-0.782582939308917,-0.759313611014873,
-0.748058574936621,-0.729041866799972,-0.68040905134498,-0.642035253523077,
-0.631210144962236,-0.621402342565702,-0.620068238234284,-0.61818748843547,
-0.615436987028471,-0.611397425798984,-0.589422175342839,-0.52922459688947,
-0.523970921706879,-0.504736997211866,-0.485849232861956,-0.462133899145304,
-0.409648415184581,-0.391148480639574,-0.380262466323677,-0.379222988399134,
-0.377003493705187,-0.375282570559809,-0.37102322061783,-0.359245578098004,
-0.327407181154658,-0.281981642284065,-0.262556297193585,-0.243598695643424,
-0.221503920951076,-0.179876928881037,-0.150266609942873,-0.13950151117311,
-0.129683655183871,-0.101666480253791,-0.0344675474333192,-0.0165223660564507,
-7.86535600802601E-5),.UNSPECIFIED.);
#307=B_SPLINE_CURVE_WITH_KNOTS('',3,(#22779,#22780,#22781,#22782,#22783,
#22784,#22785,#22786,#22787,#22788,#22789,#22790,#22791,#22792,#22793,#22794),
 .UNSPECIFIED.,.F.,.F.,(4,2,2,2,2,2,2,4),(-5.72269097713674,-5.7048997707614,
-5.66921491536667,-5.64074759372965,-5.62693046584006,-5.6170261790475,
-5.60479096905175,-5.59900260275164),.UNSPECIFIED.);
#308=B_SPLINE_CURVE_WITH_KNOTS('',3,(#22796,#22797,#22798,#22799),
 .UNSPECIFIED.,.F.,.F.,(4,4),(21.7400919742423,21.9911485668441),
 .UNSPECIFIED.);
#309=B_SPLINE_CURVE_WITH_KNOTS('',3,(#22800,#22801,#22802,#22803,#22804,
#22805,#22806,#22807,#22808,#22809,#22810,#22811,#22812,#22813,#22814,#22815,
#22816,#22817,#22818,#22819,#22820,#22821,#22822,#22823,#22824,#22825,#22826,
#22827,#22828,#22829,#22830,#22831,#22832,#22833,#22834,#22835,#22836,#22837,
#22838,#22839,#22840,#22841,#22842,#22843,#22844,#22845,#22846,#22847,#22848,
#22849,#22850,#22851,#22852,#22853,#22854,#22855,#22856,#22857,#22858,#22859,
#22860,#22861,#22862,#22863,#22864,#22865,#22866,#22867,#22868,#22869,#22870,
#22871,#22872,#22873,#22874,#22875,#22876,#22877,#22878,#22879,#22880,#22881,
#22882,#22883,#22884,#22885,#22886,#22887,#22888,#22889,#22890,#22891,#22892,
#22893,#22894,#22895,#22896,#22897,#22898,#22899,#22900,#22901,#22902,#22903,
#22904,#22905,#22906,#22907,#22908,#22909,#22910,#22911,#22912,#22913,#22914,
#22915,#22916,#22917,#22918,#22919,#22920,#22921,#22922,#22923,#22924,#22925,
#22926,#22927,#22928,#22929,#22930,#22931,#22932,#22933,#22934,#22935,#22936,
#22937,#22938,#22939,#22940,#22941,#22942,#22943,#22944,#22945,#22946,#22947,
#22948,#22949,#22950,#22951,#22952,#22953,#22954,#22955,#22956,#22957,#22958,
#22959,#22960,#22961,#22962,#22963,#22964,#22965,#22966,#22967,#22968,#22969,
#22970,#22971,#22972,#22973,#22974,#22975,#22976,#22977,#22978,#22979,#22980,
#22981,#22982,#22983,#22984,#22985,#22986,#22987,#22988,#22989,#22990,#22991,
#22992,#22993,#22994,#22995,#22996,#22997,#22998,#22999,#23000,#23001,#23002,
#23003,#23004,#23005,#23006,#23007,#23008,#23009,#23010,#23011,#23012,#23013,
#23014,#23015,#23016,#23017,#23018,#23019),.UNSPECIFIED.,.F.,.F.,(4,3,3,
3,3,3,3,3,3,3,3,3,3,3,3,3,3,3,3,3,3,3,3,3,3,3,3,3,3,3,3,3,3,3,3,3,3,3,3,
3,3,3,3,3,3,3,3,3,3,3,3,3,3,3,3,3,3,3,3,3,3,3,3,3,3,3,3,3,3,3,3,3,3,4),
(21.9911485751286,22.0842384360753,22.0972822376118,22.1851351036133,22.2729700638413,
22.3608081401585,22.448641052211,22.5364956141511,22.5964184623023,22.6842713276911,
22.7721062872985,22.8599443629887,22.9477772744123,23.0356318357261,23.0955546869928,
23.1834075526208,23.27124251247,23.3590805884042,23.4469135000723,23.5347680616292,
23.5946909116834,23.6825437772571,23.7703787370515,23.8582168129308,23.9460497245441,
24.0339042860466,24.0938271363739,24.1816800019336,24.2695149617138,24.3573530375785,
24.4451859491769,24.5330405106645,24.5929633610644,24.6808162266509,24.7686511864583,
24.8564892623505,24.9443221739767,25.032176735492,25.092099585755,25.1799524513211,
25.2677874111078,25.355625486979,25.4434583985842,25.5313129600785,25.5912358104455,
25.6790886760229,25.766923635821,25.8547617117038,25.9425946233205,26.0304491848264,
26.090372035136,26.1782249007086,26.2660598605019,26.3538979363798,26.4417308479916,
26.5295854094927,26.5895082598265,26.6773611254005,26.7651960851951,26.8530341610745,
26.9408670726877,27.0287216341901,27.0886444845171,27.1764973500911,27.2643323098857,
27.352170385765,27.4400032973782,27.5278578588806,27.5877807092076,27.675632926961,
27.7634773101345,27.8513089857246,27.939155693041,28.0232375357607),
 .UNSPECIFIED.);
#310=B_SPLINE_CURVE_WITH_KNOTS('',3,(#23024,#23025,#23026,#23027,#23028,
#23029,#23030,#23031,#23032,#23033,#23034,#23035,#23036,#23037,#23038,#23039,
#23040,#23041,#23042,#23043,#23044,#23045,#23046,#23047,#23048,#23049,#23050,
#23051,#23052,#23053,#23054,#23055,#23056,#23057,#23058,#23059,#23060,#23061,
#23062,#23063,#23064,#23065,#23066,#23067,#23068,#23069,#23070,#23071,#23072,
#23073,#23074,#23075,#23076,#23077,#23078,#23079,#23080,#23081,#23082,#23083,
#23084,#23085,#23086,#23087,#23088,#23089,#23090,#23091,#23092,#23093,#23094,
#23095,#23096,#23097,#23098,#23099,#23100,#23101,#23102,#23103,#23104,#23105,
#23106,#23107,#23108,#23109,#23110,#23111,#23112,#23113,#23114,#23115,#23116,
#23117,#23118,#23119,#23120,#23121,#23122,#23123,#23124,#23125,#23126,#23127,
#23128,#23129,#23130,#23131,#23132,#23133,#23134,#23135,#23136,#23137,#23138,
#23139,#23140,#23141,#23142,#23143,#23144,#23145,#23146,#23147,#23148,#23149,
#23150,#23151,#23152,#23153,#23154,#23155,#23156,#23157,#23158,#23159,#23160,
#23161,#23162,#23163,#23164,#23165,#23166,#23167,#23168,#23169,#23170,#23171,
#23172,#23173,#23174,#23175,#23176,#23177,#23178,#23179,#23180,#23181,#23182,
#23183,#23184,#23185,#23186,#23187,#23188,#23189,#23190,#23191,#23192,#23193,
#23194,#23195,#23196,#23197,#23198,#23199,#23200,#23201,#23202,#23203,#23204,
#23205,#23206,#23207,#23208,#23209,#23210,#23211,#23212,#23213,#23214,#23215,
#23216,#23217,#23218,#23219,#23220,#23221,#23222,#23223,#23224,#23225,#23226,
#23227,#23228,#23229,#23230,#23231,#23232,#23233,#23234,#23235,#23236,#23237,
#23238,#23239,#23240,#23241,#23242,#23243,#23244,#23245,#23246,#23247,#23248,
#23249,#23250,#23251,#23252,#23253,#23254,#23255,#23256,#23257,#23258,#23259,
#23260,#23261,#23262,#23263,#23264,#23265,#23266,#23267,#23268,#23269,#23270,
#23271,#23272,#23273,#23274,#23275,#23276,#23277,#23278,#23279,#23280,#23281,
#23282,#23283,#23284,#23285,#23286,#23287,#23288,#23289,#23290,#23291,#23292,
#23293,#23294,#23295,#23296,#23297,#23298,#23299,#23300,#23301,#23302,#23303,
#23304,#23305,#23306,#23307,#23308,#23309,#23310,#23311,#23312,#23313,#23314,
#23315,#23316,#23317,#23318,#23319,#23320,#23321,#23322,#23323,#23324,#23325),
 .UNSPECIFIED.,.F.,.F.,(4,2,2,2,2,2,2,2,2,2,2,2,2,2,2,2,2,2,2,2,2,2,2,2,
2,2,2,2,2,2,2,2,2,2,2,2,2,2,2,2,2,2,2,2,2,2,2,2,2,2,2,2,2,2,2,2,2,2,2,2,
2,2,2,2,2,2,2,2,2,2,2,2,2,2,2,2,2,2,2,2,2,2,2,2,2,2,2,2,2,2,2,2,2,2,2,2,
2,2,2,2,2,2,2,2,2,2,2,2,2,2,2,2,2,2,2,2,2,2,2,2,2,2,2,2,2,2,2,2,2,2,2,2,
2,2,2,2,2,2,2,2,2,2,2,2,2,2,2,2,2,2,4),(-6.06758662286169,-6.05672118825285,
-6.04398051113079,-6.0334226331625,-6.01645295742768,-5.96666224032135,
-5.94114870105503,-5.92208655058119,-5.91518501487488,-5.8934594205242,
-5.84516952494057,-5.81686818659048,-5.80779422838678,-5.79443767954243,
-5.79349800157478,-5.78139613242103,-5.74401084754885,-5.70741227554712,
-5.68623075021572,-5.6675727357668,-5.64882559886436,-5.58864345832522,
-5.5666613677867,-5.56355015090866,-5.56159369713408,-5.56033134932902,
-5.55949467533685,-5.55892676896793,-5.5576607109228,-5.55654449748931,
-5.55553499768505,-5.55459418941356,-5.55368497778539,-5.55276492868988,
-5.55177336537258,-5.54087185868793,-5.5219755565811,-5.47140328296167,
-5.44725177462835,-5.42865316832329,-5.42216638709216,-5.41919045683931,
-5.3956199805333,-5.3361070297681,-5.31762079130934,-5.31656252102421,-5.3157355291818,
-5.31508399021442,-5.31456676757517,-5.31415332858434,-5.31382081068278,
-5.31355192854873,-5.3128676449826,-5.31223466419711,-5.31164612693527,
-5.31109596225334,-5.31057875703017,-5.31008964022883,-5.30962417776799,
-5.30917827411671,-5.30874807656039,-5.3083298774212,-5.30792000816874,
-5.30751471697572,-5.30711001706769,-5.30670148574894,-5.2956590562236,
-5.27765940673098,-5.22457788682926,-5.20078636996917,-5.17894020571089,
-5.16010343352462,-5.11847597057348,-5.08311004235011,-5.06790088348071,
-5.05531648675626,-5.04273421768311,-5.0031222086333,-4.96535122427611,
-4.95343436929804,-4.93196026441603,-4.91020054069653,-4.86251208498258,
-4.83392024190604,-4.81534636325053,-4.80535799733817,-4.78940550815818,
-4.73389901708083,-4.70980469701429,-4.6878128270867,-4.66905181585447,
-4.60130973741285,-4.58154842692496,-4.56663799035407,-4.55543071779441,
-4.53245022824654,-4.47443858681815,-4.46238716115369,-4.44079230976937,
-4.42180096123763,-4.36313103880956,-4.33923779230291,-4.33115234655257,
-4.31832361029933,-4.30765787948439,-4.2543917421821,-4.22186452681116,
-4.1988154916661,-4.17832496274169,-4.1094394811482,-4.09555848268397,-4.07757565161444,
-4.06653305458312,-4.04825149061814,-3.99675856673836,-3.97257833171424,
-3.95054491909916,-3.92928909844223,-3.87282789977919,-3.84819289792589,
-3.83113291561169,-3.82006763470954,-3.80067290596053,-3.75009256408658,
-3.72621861706015,-3.70433270841676,-3.68551715512471,-3.62268318677427,
-3.59082819880285,-3.5790428179909,-3.56535289758157,-3.50498071401217,
-3.48086804822901,-3.45886723926148,-3.43758778758782,-3.38091392375934,
-3.34779794910163,-3.33504250496864,-3.32262183945877,-3.27979225686106,
-3.23286871133276,-3.21139990690842,-3.19231689299758,-3.14874343295967,
-3.11572311208957,-3.0956648088067,-3.08457342216825,-3.06795378935973,
-3.0218279603193,-2.98441336346076,-2.97196746186506),.UNSPECIFIED.);
#311=B_SPLINE_CURVE_WITH_KNOTS('',3,(#23327,#23328,#23329,#23330,#23331,
#23332,#23333,#23334,#23335,#23336),.UNSPECIFIED.,.F.,.F.,(4,3,3,4),(28.0232375357607,
28.0869169338981,28.1806254081031,28.2743338823082),.UNSPECIFIED.);
#312=B_SPLINE_CURVE_WITH_KNOTS('',3,(#23337,#23338,#23339,#23340,#23341,
#23342,#23343,#23344,#23345,#23346,#23347,#23348,#23349,#23350,#23351,#23352,
#23353,#23354,#23355,#23356,#23357,#23358,#23359,#23360,#23361,#23362,#23363,
#23364,#23365,#23366,#23367,#23368,#23369,#23370,#23371,#23372,#23373,#23374,
#23375,#23376,#23377,#23378,#23379,#23380,#23381,#23382,#23383,#23384,#23385,
#23386,#23387,#23388,#23389,#23390,#23391,#23392,#23393,#23394,#23395,#23396,
#23397,#23398,#23399,#23400,#23401,#23402,#23403,#23404,#23405,#23406,#23407,
#23408,#23409,#23410,#23411,#23412,#23413,#23414,#23415,#23416,#23417,#23418,
#23419,#23420,#23421,#23422,#23423,#23424,#23425,#23426,#23427,#23428,#23429,
#23430,#23431,#23432,#23433,#23434,#23435,#23436,#23437,#23438,#23439,#23440,
#23441,#23442,#23443,#23444,#23445,#23446,#23447,#23448,#23449,#23450,#23451,
#23452,#23453,#23454,#23455,#23456,#23457,#23458,#23459,#23460,#23461,#23462,
#23463,#23464,#23465,#23466,#23467,#23468,#23469,#23470,#23471,#23472,#23473,
#23474,#23475,#23476,#23477,#23478,#23479,#23480,#23481,#23482,#23483,#23484,
#23485,#23486,#23487,#23488,#23489,#23490,#23491,#23492,#23493,#23494,#23495,
#23496,#23497,#23498,#23499,#23500,#23501,#23502,#23503,#23504,#23505,#23506,
#23507,#23508,#23509,#23510,#23511,#23512,#23513,#23514,#23515,#23516,#23517,
#23518,#23519,#23520,#23521,#23522,#23523,#23524,#23525,#23526,#23527,#23528,
#23529,#23530,#23531,#23532,#23533,#23534,#23535,#23536,#23537,#23538,#23539,
#23540,#23541,#23542,#23543,#23544,#23545,#23546,#23547,#23548,#23549,#23550,
#23551,#23552,#23553,#23554,#23555,#23556,#23557,#23558,#23559,#23560,#23561,
#23562,#23563,#23564,#23565,#23566,#23567,#23568,#23569,#23570,#23571,#23572,
#23573,#23574,#23575,#23576,#23577,#23578,#23579,#23580,#23581,#23582,#23583,
#23584,#23585,#23586,#23587,#23588,#23589,#23590,#23591,#23592,#23593,#23594,
#23595,#23596,#23597,#23598,#23599,#23600,#23601,#23602,#23603,#23604,#23605,
#23606,#23607,#23608,#23609,#23610,#23611,#23612,#23613,#23614,#23615,#23616,
#23617,#23618,#23619,#23620),.UNSPECIFIED.,.F.,.F.,(4,2,2,2,2,2,2,2,2,2,
2,2,2,2,2,2,2,2,2,2,2,2,2,2,2,2,2,2,2,2,2,2,2,2,2,2,2,2,2,2,2,2,2,2,2,2,
2,2,2,2,2,2,2,2,2,2,2,2,2,2,2,2,2,2,2,2,2,2,2,2,2,2,2,2,2,2,2,2,2,2,2,2,
2,2,2,2,2,2,2,2,2,2,2,2,2,2,2,2,2,2,2,2,2,2,2,2,2,2,2,2,2,2,2,2,2,2,2,2,
2,2,2,2,2,2,2,2,2,2,2,2,2,2,2,2,2,2,2,2,2,2,2,4),(-6.19174977417099,-6.17790055894357,
-6.16530844262692,-6.14488062628941,-6.11016394335594,-6.05746865424026,
-6.04395990877691,-6.03345737334001,-6.01671312488883,-5.96693939896737,
-5.94108351866951,-5.92183282063829,-5.91339110029996,-5.89094141021784,
-5.84321905355417,-5.81582671700227,-5.80705047866299,-5.79376231777089,
-5.79283345590746,-5.78046847860075,-5.75110684024062,-5.70992911883133,
-5.68781295060037,-5.66839735790778,-5.64985257178812,-5.58453612918225,
-5.56437800196991,-5.56185865109168,-5.56024447158564,-5.55917924296637,
-5.55845613724759,-5.55714597697236,-5.5559893725437,-5.55494108762057,
-5.55396078138865,-5.5530082564484,-5.55203588284284,-5.54147642800634,
-5.52457428735703,-5.47472865740141,-5.44900954047236,-5.42977729035764,
-5.42205833795195,-5.41902630307087,-5.41614286536467,-5.39146794003943,
-5.33472194871901,-5.31650090691653,-5.31550703188536,-5.31472580806067,
-5.31410649336461,-5.31361164388215,-5.31321340678309,-5.31289086926891,
-5.31262817114584,-5.31194633479694,-5.3113140118618,-5.31072444801069,
-5.31017164063459,-5.30965020797847,-5.30915527141661,-5.30868234635121,
-5.30822723719189,-5.30778593130822,-5.30735448554185,-5.30692889644243,
-5.29573799550333,-5.27907634992805,-5.22435293542331,-5.20025642266531,
-5.1781773307116,-5.15915929913742,-5.12126130497449,-5.07456457511193,
-5.06676062206611,-5.05419163944611,-5.04130164166706,-5.0087161772395,
-4.96034832777065,-4.93645306482614,-4.91570524324687,-4.88014968311171,
-4.83865893376585,-4.82238056721064,-4.80919322439788,-4.79686877353386,
-4.76471717714858,-4.73337436413831,-4.70897605865634,-4.68675245002698,
-4.66525730794326,-4.6008837523092,-4.58069467204775,-4.56555050419774,
-4.55423614060313,-4.53600703437018,-4.48510939633242,-4.46150698067304,
-4.43966322989653,-4.41784287826541,-4.36852982104803,-4.32914466389923,
-4.31651089497893,-4.30369093417459,-4.26608021284519,-4.21760521409203,
-4.19524853232157,-4.17384677045649,-4.11742965631162,-4.09260597282443,
-4.08431152843695,-4.07123722613881,-4.06050864990156,-4.00710393798522,
-3.97442997609026,-3.95126494422135,-3.93052607211835,-3.86413107294597,
-3.84928816341928,-3.83055785684892,-3.81940148587177,-3.80130100514156,
-3.74849319904076,-3.72448780047543,-3.70245210051695,-3.68080770527405,
-3.61907787523084,-3.58877090111763,-3.57698016609012,-3.5628675431258,
-3.47781268181903,-3.45594630129282,-3.43680114361935,-3.37783159005303,
-3.35401276423705,-3.3459267790151,-3.3330665613329,-3.32047046038928,-3.27960629669956,
-3.24448573447427,-3.2321624904099,-3.21960145114545),.UNSPECIFIED.);
#313=B_SPLINE_CURVE_WITH_KNOTS('',3,(#23626,#23627,#23628,#23629,#23630,
#23631,#23632,#23633,#23634,#23635,#23636,#23637,#23638,#23639,#23640,#23641,
#23642,#23643,#23644,#23645,#23646,#23647,#23648,#23649,#23650,#23651,#23652,
#23653,#23654,#23655,#23656,#23657,#23658,#23659,#23660,#23661,#23662,#23663,
#23664,#23665,#23666,#23667,#23668,#23669,#23670,#23671,#23672,#23673,#23674,
#23675,#23676,#23677,#23678,#23679,#23680,#23681,#23682,#23683,#23684,#23685,
#23686,#23687,#23688,#23689,#23690,#23691,#23692,#23693,#23694,#23695,#23696,
#23697,#23698,#23699,#23700,#23701,#23702,#23703,#23704,#23705,#23706,#23707,
#23708,#23709,#23710,#23711,#23712,#23713,#23714,#23715,#23716,#23717,#23718,
#23719,#23720,#23721,#23722,#23723,#23724,#23725,#23726,#23727,#23728,#23729,
#23730,#23731,#23732,#23733,#23734,#23735,#23736,#23737,#23738,#23739,#23740,
#23741,#23742,#23743,#23744,#23745,#23746,#23747,#23748,#23749,#23750,#23751,
#23752,#23753,#23754,#23755,#23756,#23757,#23758,#23759,#23760,#23761,#23762,
#23763,#23764,#23765,#23766,#23767,#23768,#23769,#23770,#23771,#23772,#23773,
#23774,#23775,#23776,#23777,#23778,#23779,#23780,#23781,#23782,#23783,#23784,
#23785,#23786,#23787,#23788,#23789,#23790,#23791,#23792,#23793,#23794,#23795,
#23796,#23797,#23798,#23799,#23800,#23801,#23802,#23803,#23804,#23805,#23806,
#23807,#23808,#23809,#23810,#23811,#23812,#23813,#23814,#23815,#23816,#23817,
#23818,#23819,#23820,#23821,#23822,#23823,#23824,#23825,#23826,#23827,#23828,
#23829,#23830,#23831,#23832,#23833,#23834,#23835,#23836,#23837,#23838,#23839,
#23840,#23841,#23842),.UNSPECIFIED.,.F.,.F.,(4,3,3,3,3,3,3,3,3,3,3,3,3,
3,3,3,3,3,3,3,3,3,3,3,3,3,3,3,3,3,3,3,3,3,3,3,3,3,3,3,3,3,3,3,3,3,3,3,3,
3,3,3,3,3,3,3,3,3,3,3,3,3,3,3,3,3,3,3,3,3,3,3,4),(34.5575191894878,34.6518273097851,
34.7461354300824,34.8339898030957,34.9218262952673,35.0096659023973,35.0975003577409,
35.1853564084918,35.2450073652305,35.3328617382438,35.4206982304155,35.5085378375455,
35.5963722928892,35.6842283436401,35.7438793003786,35.8317336733919,35.9195701655634,
36.0074097726934,36.0952442280371,36.183100278788,36.2427512355268,36.3306056085401,
36.4184421007117,36.5062817078417,36.5941161631853,36.6819722139362,36.7416231706749,
36.8294775436881,36.9173140358597,37.0051536429896,37.0929880983332,37.1808441490841,
37.240495105823,37.3283494788363,37.4161859710079,37.504025578138,37.5918600334816,
37.6797160842325,37.7393670409711,37.8272214139844,37.915057906156,38.002897513286,
38.0907319686296,38.1785880193805,38.2382389761193,38.3260933491326,38.4139298413042,
38.5017694484342,38.5896039037779,38.6774599545289,38.7371109112674,38.8249652842806,
38.9128017764521,39.000641383582,39.0884758389256,39.1763318896765,39.2359828464155,
39.3238372194288,39.4116737116004,39.4995133187305,39.5873477740742,39.6752038248252,
39.7348547815636,39.8227091545768,39.9105456467483,39.9983852538783,40.0862197092219,
40.1740757599728,40.2337267167118,40.3226968924185,40.4105362766921,40.5000718481154,
40.5896074195387),.UNSPECIFIED.);
#314=B_SPLINE_CURVE_WITH_KNOTS('',3,(#23843,#23844,#23845,#23846,#23847,
#23848,#23849,#23850,#23851,#23852,#23853,#23854),.UNSPECIFIED.,.F.,.F.,
(4,2,2,2,2,4),(-6.1912980755545,-6.1778196623817,-6.16552121345783,-6.14529911471674,
-6.11138976728743,-6.06758662286169),.UNSPECIFIED.);
#315=B_SPLINE_CURVE_WITH_KNOTS('',3,(#23855,#23856,#23857,#23858,#23859,
#23860,#23861,#23862,#23863,#23864,#23865,#23866,#23867,#23868,#23869,#23870,
#23871,#23872,#23873,#23874,#23875,#23876,#23877,#23878,#23879,#23880,#23881,
#23882,#23883,#23884,#23885,#23886,#23887,#23888,#23889,#23890,#23891,#23892,
#23893,#23894,#23895,#23896,#23897,#23898,#23899,#23900,#23901,#23902,#23903,
#23904,#23905,#23906,#23907,#23908,#23909,#23910,#23911,#23912,#23913,#23914,
#23915,#23916,#23917,#23918,#23919,#23920,#23921,#23922,#23923,#23924,#23925,
#23926,#23927,#23928,#23929,#23930,#23931,#23932,#23933,#23934,#23935,#23936,
#23937,#23938,#23939,#23940,#23941,#23942,#23943,#23944,#23945,#23946,#23947,
#23948,#23949,#23950,#23951,#23952,#23953,#23954,#23955,#23956,#23957,#23958,
#23959,#23960,#23961,#23962,#23963,#23964,#23965,#23966,#23967,#23968,#23969,
#23970,#23971,#23972,#23973,#23974,#23975,#23976,#23977,#23978,#23979,#23980,
#23981,#23982,#23983,#23984,#23985,#23986,#23987,#23988,#23989,#23990,#23991,
#23992,#23993,#23994,#23995,#23996,#23997,#23998,#23999,#24000,#24001,#24002,
#24003,#24004,#24005,#24006,#24007,#24008,#24009,#24010,#24011,#24012,#24013,
#24014,#24015,#24016,#24017,#24018,#24019,#24020,#24021,#24022,#24023,#24024,
#24025,#24026,#24027,#24028,#24029,#24030,#24031,#24032,#24033,#24034,#24035,
#24036,#24037,#24038,#24039,#24040,#24041,#24042,#24043,#24044,#24045,#24046,
#24047,#24048,#24049,#24050,#24051,#24052,#24053,#24054,#24055,#24056,#24057,
#24058,#24059,#24060,#24061,#24062,#24063,#24064,#24065,#24066,#24067,#24068,
#24069,#24070,#24071,#24072,#24073,#24074,#24075,#24076,#24077,#24078,#24079,
#24080,#24081,#24082,#24083,#24084,#24085,#24086,#24087,#24088,#24089,#24090,
#24091,#24092,#24093,#24094,#24095,#24096,#24097,#24098,#24099,#24100,#24101,
#24102),.UNSPECIFIED.,.F.,.F.,(4,2,2,2,2,2,2,2,2,2,2,2,2,2,2,2,2,2,2,2,
2,2,2,2,2,2,2,2,2,2,2,2,2,2,2,2,2,2,2,2,2,2,2,2,2,2,2,2,2,2,2,2,2,2,2,2,
2,2,2,2,2,2,2,2,2,2,2,2,2,2,2,2,2,2,2,2,2,2,2,2,2,2,2,2,2,2,2,2,2,2,2,2,
2,2,2,2,2,2,2,2,2,2,2,2,2,2,2,2,2,2,2,2,2,2,2,2,2,2,2,2,2,2,2,4),(-3.21960145114545,
-3.21022947980482,-3.19112654555098,-3.12190443326165,-3.09587143195948,
-3.08443680155034,-3.06975920450714,-3.05054634619234,-2.98342362393314,
-2.9642023801869,-2.94244696641799,-2.93032115889807,-2.87179626716825,
-2.84993062193197,-2.83849524516932,-2.82382056968935,-2.80461365150436,
-2.73747429472207,-2.71825414929352,-2.6964975555484,-2.68437034145876,
-2.62584826119843,-2.60398569176725,-2.59255083537871,-2.57787477984499,
-2.55866494068083,-2.49153507515123,-2.47231455933765,-2.45055882323833,
-2.43843248183758,-2.37990893501068,-2.35804534744514,-2.3466103957743,
-2.33193504074819,-2.31272656637389,-2.24559355529108,-2.22637337949345,
-2.2046175153028,-2.19249094397454,-2.1339684033277,-2.11210553979271,-2.10067075481821,
-2.08599521481463,-2.06678628118138,-1.999655502551,-1.98043536443547,-1.9586797916078,
-1.94655345954775,-1.88803101997814,-1.86616805217765,-1.85473330934196,
-1.84005800533958,-1.82084947963615,-1.75371837659818,-1.73449841990162,
-1.7127429390072,-1.70061662313771,-1.64209473571131,-1.62023204519314,
-1.6087974018717,-1.59412213994422,-1.57491362269492,-1.50778337306259,
-1.48856353157109,-1.46680823447338,-1.45468203755197,-1.3961604996727,
-1.37429790761334,-1.36286333691478,-1.34818820794881,-1.32897988637461,
-1.2618499381358,-1.24263024288065,-1.22087508652415,-1.20874896039024,
-1.15022786805139,-1.12836545764103,-1.11693097207478,-1.10225593378729,
-1.08304772078849,-1.01591833074346,-0.99669876728702,-0.974943771699952,
-0.962817738757497,-0.904297047533957,-0.882434779930312,-0.870962174567235,
-0.860513830808857,-0.859315401260965,-0.857322528650568,-0.854023333159055,
-0.832319673335272,-0.771005489349052,-0.751900051905642,-0.732659958985613,
-0.710803786802656,-0.671104247453748,-0.639253207951319,-0.626917177408989,
-0.616905504178548,-0.614457072570467,-0.611372041135868,-0.608511309618207,
-0.587273001283989,-0.524787244576754,-0.512229481817021,-0.491917860624872,
-0.471652228619173,-0.455383098515217,-0.40103038495825,-0.38539648417881,
-0.374160267884775,-0.37006891953753,-0.367619896947356,-0.344190706999339,
-0.278024281148239,-0.25785169605832,-0.238760867794644,-0.21606878029411,
-0.17140056146557,-0.149906130813608,-0.136588295513562,-0.126447364794008,
-0.123761332807637),.UNSPECIFIED.);
#316=B_SPLINE_CURVE_WITH_KNOTS('',3,(#24108,#24109,#24110,#24111,#24112,
#24113,#24114,#24115,#24116,#24117,#24118,#24119,#24120,#24121,#24122,#24123,
#24124,#24125,#24126,#24127,#24128,#24129,#24130,#24131,#24132,#24133,#24134,
#24135,#24136,#24137,#24138,#24139,#24140,#24141,#24142,#24143,#24144,#24145,
#24146,#24147,#24148,#24149,#24150,#24151,#24152,#24153,#24154,#24155,#24156,
#24157,#24158,#24159,#24160,#24161,#24162,#24163,#24164,#24165,#24166,#24167,
#24168,#24169,#24170,#24171,#24172,#24173,#24174,#24175,#24176,#24177,#24178,
#24179,#24180,#24181,#24182,#24183,#24184,#24185,#24186,#24187,#24188,#24189,
#24190,#24191,#24192,#24193,#24194,#24195,#24196,#24197,#24198,#24199,#24200,
#24201,#24202,#24203,#24204,#24205,#24206,#24207,#24208,#24209,#24210,#24211,
#24212,#24213,#24214,#24215,#24216,#24217,#24218,#24219,#24220,#24221,#24222,
#24223,#24224,#24225,#24226,#24227,#24228,#24229,#24230,#24231,#24232,#24233,
#24234,#24235,#24236,#24237,#24238,#24239,#24240,#24241,#24242,#24243,#24244,
#24245,#24246,#24247,#24248,#24249,#24250,#24251,#24252,#24253,#24254,#24255,
#24256,#24257,#24258,#24259,#24260,#24261,#24262,#24263,#24264,#24265,#24266,
#24267,#24268,#24269,#24270,#24271,#24272,#24273,#24274,#24275,#24276,#24277,
#24278,#24279,#24280,#24281,#24282,#24283,#24284,#24285,#24286,#24287,#24288,
#24289,#24290,#24291,#24292,#24293,#24294,#24295,#24296,#24297,#24298,#24299,
#24300,#24301,#24302,#24303,#24304,#24305,#24306,#24307,#24308,#24309,#24310,
#24311,#24312,#24313,#24314,#24315,#24316,#24317,#24318,#24319,#24320,#24321,
#24322,#24323,#24324,#24325,#24326,#24327,#24328,#24329,#24330,#24331,#24332,
#24333,#24334,#24335,#24336,#24337,#24338,#24339,#24340,#24341,#24342,#24343,
#24344,#24345,#24346,#24347,#24348,#24349,#24350,#24351),.UNSPECIFIED.,
 .F.,.F.,(4,2,2,2,2,2,2,2,2,2,2,2,2,2,2,2,2,2,2,2,2,2,2,2,2,2,2,2,2,2,2,
2,2,2,2,2,2,2,2,2,2,2,2,2,2,2,2,2,2,2,2,2,2,2,2,2,2,2,2,2,2,2,2,2,2,2,2,
2,2,2,2,2,2,2,2,2,2,2,2,2,2,2,2,2,2,2,2,2,2,2,2,2,2,2,2,2,2,2,2,2,2,2,2,
2,2,2,2,2,2,2,2,2,2,2,2,2,2,2,2,2,2,4),(-2.97193325191145,-2.97164574381583,
-2.92102915801035,-2.90216692995615,-2.89111652013216,-2.87364861696247,
-2.82834372839519,-2.79144189690155,-2.7725982633729,-2.75076459223857,
-2.72699873701708,-2.67412231978996,-2.65595025215559,-2.64490809658809,
-2.62681899905642,-2.59954947584692,-2.55088088755474,-2.52883403008647,
-2.50758810140748,-2.45918934095238,-2.41685203979126,-2.40440363217966,
-2.39167904182718,-2.35884312687339,-2.34683759451771,-2.30118673634944,
-2.28212551253655,-2.26062832232885,-2.21249860315353,-2.17121832592259,
-2.15871404305064,-2.14604947757248,-2.13069328305726,-2.09450777103372,
-2.05469867866883,-2.03575910358966,-2.01408606064914,-1.9906554093374,
-1.94030618555707,-1.91990714178543,-1.9087997095913,-1.89238140091297,
-1.84650605846805,-1.80913980932642,-1.79016332429391,-1.76854676503619,
-1.75647112571681,-1.6980228099185,-1.67521535554473,-1.66396397111819,
-1.64862466304223,-1.60311662207386,-1.59700382718513,-1.5606621987561,
-1.54023539541018,-1.51699241246588,-1.48722028339018,-1.4314293137659,
-1.42085859124806,-1.4078453244037,-1.39958021464946,-1.35284846971754,
-1.3163753382843,-1.29758967640907,-1.27564723889801,-1.25165523263094,
-1.20173448753213,-1.18213389128223,-1.17106146744814,-1.15414593661864,
-1.12986344755896,-1.0722881894719,-1.05322543523818,-1.03173062852031,
-0.983967850883072,-0.942252395241978,-0.929770736403734,-0.917082329125133,
-0.901682142448709,-0.865247592264209,-0.825920341281493,-0.805248539838595,
-0.787460996593727,-0.76508144518638,-0.721751826282113,-0.695141924529433,
-0.68320670260102,-0.671960376617552,-0.670929298408179,-0.669720700601747,
-0.668276479581411,-0.650390392697354,-0.596212681215645,-0.572559135833189,
-0.557121076167727,-0.534388274815794,-0.508039114692328,-0.457135112408879,
-0.441744518263323,-0.43127672360959,-0.428685155619503,-0.426521220034364,
-0.423430915281326,-0.417764335747122,-0.394747082652951,-0.334119006313926,
-0.313491193834681,-0.311501757358665,-0.309706484477112,-0.307017635846705,
-0.281560258528114,-0.24929703766151,-0.211831127423816,-0.196354387224509,
-0.185900936827732,-0.167273217435851,-0.13699596743803,-0.0887764016844955,
-0.0697834210280926,-0.0508249785909599,-0.033290469383095,-7.60621500899032E-5),
 .UNSPECIFIED.);
#317=B_SPLINE_CURVE_WITH_KNOTS('',3,(#24352,#24353,#24354,#24355,#24356,
#24357,#24358,#24359,#24360,#24361,#24362,#24363,#24364),.UNSPECIFIED.,
 .F.,.F.,(4,3,3,3,4),(40.5896074195387,40.677463067737,40.7325986518599,
40.8255995484923,40.8407044966674),.UNSPECIFIED.);
#318=B_SPLINE_CURVE_WITH_KNOTS('',3,(#24366,#24367,#24368,#24369,#24370,
#24371,#24372,#24373,#24374,#24375),.UNSPECIFIED.,.F.,.F.,(4,2,2,2,4),(-0.123761332807637,
-0.100838124130903,-0.0326226656386009,-0.0154724073688336,-4.23457580937261E-5),
 .UNSPECIFIED.);
#319=B_SPLINE_CURVE_WITH_KNOTS('',3,(#24376,#24377,#24378,#24379,#24380,
#24381,#24382,#24383,#24384,#24385,#24386,#24387,#24388,#24389,#24390,#24391),
 .UNSPECIFIED.,.F.,.F.,(4,1,1,1,1,1,1,1,1,1,1,1,1,4),(40.8407044966674,
41.0644587758518,41.5635950005423,42.0627312252329,42.5618674499234,43.0610036746139,
43.5601398993044,44.059276123995,44.5584123486855,45.057548573376,45.5566847980665,
46.0558210227571,46.5549572474476,46.8727891676101),.UNSPECIFIED.);
#320=B_SPLINE_CURVE_WITH_KNOTS('',3,(#24396,#24397,#24398,#24399,#24400,
#24401,#24402,#24403,#24404,#24405,#24406,#24407,#24408,#24409,#24410,#24411,
#24412,#24413,#24414,#24415,#24416,#24417,#24418,#24419,#24420,#24421,#24422,
#24423,#24424,#24425,#24426,#24427,#24428,#24429,#24430,#24431,#24432,#24433,
#24434,#24435,#24436,#24437,#24438,#24439,#24440,#24441,#24442,#24443,#24444,
#24445,#24446,#24447,#24448,#24449,#24450,#24451,#24452,#24453,#24454,#24455,
#24456,#24457,#24458,#24459,#24460,#24461,#24462,#24463,#24464,#24465,#24466,
#24467,#24468,#24469,#24470,#24471,#24472,#24473,#24474,#24475,#24476,#24477,
#24478,#24479,#24480,#24481,#24482,#24483,#24484,#24485,#24486,#24487,#24488,
#24489,#24490,#24491,#24492,#24493,#24494,#24495,#24496,#24497,#24498,#24499,
#24500,#24501,#24502,#24503,#24504,#24505,#24506,#24507,#24508,#24509,#24510,
#24511,#24512,#24513,#24514,#24515,#24516,#24517,#24518,#24519,#24520,#24521,
#24522,#24523,#24524,#24525,#24526,#24527,#24528,#24529,#24530,#24531,#24532,
#24533,#24534,#24535,#24536,#24537,#24538,#24539,#24540,#24541,#24542,#24543,
#24544,#24545,#24546,#24547,#24548,#24549,#24550,#24551,#24552,#24553,#24554,
#24555,#24556,#24557,#24558,#24559,#24560,#24561,#24562,#24563,#24564,#24565,
#24566,#24567,#24568,#24569,#24570,#24571,#24572,#24573,#24574,#24575,#24576,
#24577,#24578,#24579,#24580,#24581,#24582,#24583,#24584,#24585,#24586,#24587,
#24588,#24589,#24590,#24591,#24592,#24593,#24594,#24595,#24596,#24597,#24598,
#24599,#24600,#24601,#24602,#24603,#24604,#24605,#24606,#24607,#24608,#24609,
#24610,#24611,#24612,#24613,#24614,#24615,#24616,#24617,#24618,#24619,#24620,
#24621,#24622,#24623,#24624,#24625,#24626,#24627,#24628,#24629,#24630,#24631),
 .UNSPECIFIED.,.F.,.F.,(4,2,2,2,2,2,2,2,2,2,2,2,2,2,2,2,2,2,2,2,2,2,2,2,
2,2,2,2,2,2,2,2,2,2,2,2,2,2,2,2,2,2,2,2,2,2,2,2,2,2,2,2,2,2,2,2,2,2,2,2,
2,2,2,2,2,2,2,2,2,2,2,2,2,2,2,2,2,2,2,2,2,2,2,2,2,2,2,2,2,2,2,2,2,2,2,2,
2,2,2,2,2,2,2,2,2,2,2,2,2,2,2,2,2,2,2,2,2,4),(-6.06752948703079,-6.01968975532367,
-6.00279863227356,-5.97729076238544,-5.95859254006379,-5.93211083694878,
-5.87908462928733,-5.86132864964779,-5.85029413377576,-5.83937636039134,
-5.82013402624847,-5.76851251713189,-5.74491130681351,-5.7239372297368,
-5.70313148561065,-5.6586090845869,-5.62622511510572,-5.6115827919692,-5.60007748730739,
-5.58937275134007,-5.56524373229554,-5.5199334118267,-5.49518139551221,
-5.47784438500099,-5.45695813998917,-5.39132811303644,-5.37169925714225,
-5.36012517940655,-5.35400373133728,-5.35232377145435,-5.35079672789885,
-5.34878497557384,-5.33107367656639,-5.27763830554734,-5.25380157143114,
-5.23193364477924,-5.21310868128819,-5.17649705092115,-5.12943422451358,
-5.12137438236276,-5.10857205929379,-5.09619280852159,-5.05266151895532,
-5.00666210026908,-4.98511863150322,-4.96609123203312,-4.91902604917745,
-4.88812100560458,-4.86874620249341,-4.85768166922201,-4.84101385605415,
-4.78647590617933,-4.75392004146292,-4.73350912632917,-4.70923085635204,
-4.66820715326864,-4.63003247268438,-4.61714019136484,-4.60650849515677,
-4.58269317571645,-4.53699326847181,-4.50663984395818,-4.48634711077696,
-4.46117139570225,-4.40697730394375,-4.39362156739793,-4.37604107614999,
-4.36499328867072,-4.34626584044617,-4.29465495007958,-4.27076953772001,
-4.24887818118798,-4.23006572420335,-4.19362580542125,-4.13703954012282,
-4.12470293874582,-4.1118506776887,-4.07518075017096,-4.02357217418132,
-4.00201904726829,-3.98299853156462,-3.93568433401717,-3.90491630760021,
-3.8855873371089,-3.87452429095245,-3.85782505255265,-3.80332854344605,
-3.77935842095198,-3.75742632544126,-3.7360950905289,-3.68388020916178,
-3.64540278990727,-3.63309083417994,-3.62020915567856,-3.5571897006089,
-3.53333875106678,-3.51146404787057,-3.4900874894295,-3.43295118585468,
-3.40904269705533,-3.40095407803768,-3.38812210182429,-3.37576849245923,
-3.33182518793383,-3.28720013192981,-3.2654131585503,-3.24654299299434,
-3.20904089299356,-3.16295272135323,-3.15495076570774,-3.14220827216713,
-3.13149424736765,-3.10623092664853,-3.09564974794408,-3.0390892544507,
-3.01782572016804,-2.99580342183124,-2.97193325191145),.UNSPECIFIED.);
#321=B_SPLINE_CURVE_WITH_KNOTS('',3,(#24633,#24634,#24635,#24636,#24637),
 .UNSPECIFIED.,.F.,.F.,(4,1,4),(46.8727891676101,47.0540934721381,47.123889803847),
 .UNSPECIFIED.);
#322=B_SPLINE_CURVE_WITH_KNOTS('',3,(#24638,#24639,#24640,#24641,#24642,
#24643,#24644,#24645,#24646,#24647,#24648,#24649,#24650,#24651,#24652,#24653,
#24654,#24655,#24656,#24657,#24658,#24659,#24660,#24661,#24662,#24663,#24664,
#24665,#24666,#24667,#24668,#24669,#24670,#24671,#24672,#24673,#24674,#24675,
#24676,#24677,#24678,#24679,#24680,#24681,#24682,#24683,#24684,#24685,#24686,
#24687,#24688,#24689,#24690,#24691,#24692,#24693,#24694,#24695,#24696,#24697,
#24698,#24699,#24700,#24701,#24702,#24703,#24704,#24705,#24706,#24707,#24708,
#24709,#24710,#24711,#24712,#24713,#24714,#24715,#24716,#24717,#24718,#24719,
#24720,#24721,#24722,#24723,#24724,#24725,#24726,#24727,#24728,#24729,#24730,
#24731,#24732,#24733,#24734,#24735,#24736,#24737,#24738,#24739,#24740,#24741,
#24742,#24743,#24744,#24745,#24746,#24747,#24748,#24749,#24750,#24751,#24752,
#24753,#24754,#24755,#24756,#24757,#24758,#24759,#24760,#24761,#24762,#24763,
#24764,#24765,#24766,#24767,#24768,#24769,#24770,#24771,#24772,#24773,#24774,
#24775,#24776,#24777,#24778,#24779,#24780,#24781,#24782,#24783,#24784,#24785,
#24786,#24787,#24788,#24789,#24790,#24791,#24792,#24793,#24794,#24795,#24796,
#24797,#24798,#24799,#24800,#24801,#24802,#24803,#24804,#24805,#24806,#24807,
#24808,#24809,#24810,#24811,#24812,#24813,#24814,#24815,#24816,#24817,#24818,
#24819,#24820,#24821,#24822,#24823,#24824,#24825,#24826,#24827,#24828,#24829,
#24830,#24831,#24832,#24833,#24834,#24835,#24836,#24837,#24838,#24839,#24840,
#24841,#24842,#24843,#24844,#24845,#24846,#24847,#24848,#24849,#24850,#24851,
#24852,#24853,#24854,#24855,#24856,#24857,#24858,#24859,#24860,#24861,#24862,
#24863,#24864,#24865,#24866,#24867,#24868,#24869),.UNSPECIFIED.,.F.,.F.,
(4,2,2,2,2,2,2,2,2,2,2,2,2,2,2,2,2,2,2,2,2,2,2,2,2,2,2,2,2,2,2,2,2,2,2,
2,2,2,2,2,2,2,2,2,2,2,2,2,2,2,2,2,2,2,2,2,2,2,2,2,2,2,2,2,2,2,2,2,2,2,2,
2,2,2,2,2,2,2,2,2,2,2,2,2,2,2,2,2,2,2,2,2,2,2,2,2,2,2,2,2,2,2,2,2,2,2,2,
2,2,2,2,2,2,2,2,4),(-6.19118392946141,-6.13037761200805,-6.11093273724125,
-6.0918143257748,-6.06357102546708,-5.991874087076,-5.97971012129886,-5.96703953917199,
-5.92779582267618,-5.8928724473279,-5.86633525347181,-5.86322290707405,
-5.86091746316682,-5.85603361626317,-5.84535111229184,-5.82145515198586,
-5.7674476150873,-5.74952878321101,-5.73564738312852,-5.72397445151794,
-5.70085021757395,-5.65432578088489,-5.63134831756085,-5.61124156573648,
-5.59486940739819,-5.55901387544994,-5.51785286198639,-5.50162610579027,
-5.50035763511655,-5.49926118983562,-5.49829201249427,-5.48748519703164,
-5.47453260639729,-5.43797930406928,-5.40196185482296,-5.38079075388334,
-5.36582059512924,-5.3468344534799,-5.30984233649761,-5.26436766578781,
-5.24687785432739,-5.23570846593294,-5.21624903551618,-5.1661727113296,
-5.14199174210581,-5.11987318286207,-5.10087906665762,-5.06375082924483,
-5.02986046835593,-5.01741715553728,-5.0092649989165,-4.99633703633041,
-4.98380396117748,-4.94170496517013,-4.89685445677497,-4.87453669398018,
-4.85311211493562,-4.79630162960949,-4.77178531149256,-4.76355430223362,
-4.75054537581196,-4.73808164000655,-4.69473053315154,-4.64842648910057,
-4.62672777822736,-4.60475913002213,-4.55819274999848,-4.52892606002085,
-4.5100738298483,-4.49891716120239,-4.48092999692706,-4.42767042470952,
-4.40375960667328,-4.38177014343958,-4.36008996826393,-4.30727939445949,
-4.28111380660068,-4.26340945736504,-4.25224688168972,-4.23306097748823,
-4.18268731754972,-4.1584588601933,-4.13631756339948,-4.11733531626208,
-4.0804063518357,-4.03384296964623,-4.02567586731035,-4.01273252606796,
-4.00021283489043,-3.95786026081262,-3.91064189623736,-3.88895817104347,
-3.86697262073152,-3.82075324475661,-3.77914431751064,-3.76644917332635,
-3.75369557858554,-3.7154780847956,-3.66745014865499,-3.64509673896242,
-3.6236963011979,-3.56723089621119,-3.54244317846208,-3.53415640195549,
-3.5210903814546,-3.51035924399168,-3.45697986918221,-3.42431377682065,
-3.40114743426828,-3.38041190179878,-3.31397990711238,-3.29915428296019,
-3.28043715606588,-3.27035488719525,-3.25408593620953,-3.21935065787348),
 .UNSPECIFIED.);
#323=B_SPLINE_CURVE_WITH_KNOTS('',3,(#24875,#24876,#24877,#24878,#24879,
#24880,#24881,#24882,#24883,#24884,#24885,#24886,#24887,#24888,#24889,#24890,
#24891,#24892,#24893,#24894,#24895,#24896,#24897,#24898,#24899,#24900,#24901,
#24902,#24903,#24904,#24905,#24906,#24907,#24908,#24909,#24910,#24911,#24912,
#24913,#24914,#24915,#24916,#24917,#24918,#24919,#24920,#24921,#24922,#24923,
#24924,#24925,#24926,#24927,#24928,#24929,#24930,#24931,#24932,#24933,#24934,
#24935,#24936,#24937,#24938,#24939,#24940,#24941,#24942,#24943,#24944,#24945,
#24946,#24947,#24948,#24949,#24950,#24951,#24952,#24953,#24954,#24955,#24956,
#24957,#24958,#24959,#24960,#24961,#24962,#24963,#24964,#24965,#24966,#24967,
#24968,#24969,#24970,#24971,#24972,#24973,#24974,#24975,#24976,#24977,#24978,
#24979,#24980,#24981,#24982,#24983,#24984,#24985,#24986,#24987,#24988,#24989,
#24990,#24991,#24992,#24993,#24994,#24995,#24996,#24997,#24998,#24999,#25000,
#25001,#25002,#25003,#25004,#25005,#25006,#25007,#25008,#25009,#25010,#25011,
#25012,#25013,#25014,#25015,#25016,#25017,#25018,#25019,#25020,#25021,#25022,
#25023,#25024,#25025,#25026,#25027,#25028,#25029,#25030,#25031,#25032,#25033,
#25034,#25035,#25036,#25037,#25038,#25039,#25040,#25041,#25042,#25043,#25044,
#25045,#25046,#25047,#25048,#25049,#25050,#25051,#25052,#25053,#25054,#25055,
#25056,#25057,#25058,#25059,#25060,#25061,#25062,#25063,#25064,#25065,#25066,
#25067,#25068,#25069,#25070,#25071,#25072,#25073,#25074,#25075,#25076,#25077,
#25078,#25079,#25080,#25081,#25082,#25083,#25084,#25085,#25086,#25087,#25088,
#25089,#25090,#25091,#25092,#25093,#25094,#25095,#25096,#25097,#25098,#25099,
#25100,#25101,#25102,#25103,#25104,#25105,#25106,#25107,#25108,#25109,#25110,
#25111,#25112,#25113,#25114,#25115,#25116,#25117,#25118,#25119,#25120,#25121,
#25122,#25123,#25124,#25125,#25126,#25127,#25128,#25129,#25130,#25131,#25132,
#25133,#25134,#25135,#25136,#25137,#25138,#25139,#25140,#25141,#25142,#25143,
#25144,#25145,#25146,#25147,#25148,#25149,#25150,#25151,#25152,#25153,#25154,
#25155,#25156,#25157,#25158),.UNSPECIFIED.,.F.,.F.,(4,2,2,2,2,2,2,2,2,2,
2,2,2,2,2,2,2,2,2,2,2,2,2,2,2,2,2,2,2,2,2,2,2,2,2,2,2,2,2,2,2,2,2,2,2,2,
2,2,2,2,2,2,2,2,2,2,2,2,2,2,2,2,2,2,2,2,2,2,2,2,2,2,2,2,2,2,2,2,2,2,2,2,
2,2,2,2,2,2,2,2,2,2,2,2,2,2,2,2,2,2,2,2,2,2,2,2,2,2,2,2,2,2,2,2,2,2,2,2,
2,2,2,2,2,2,2,2,2,2,2,2,2,2,2,2,2,2,2,2,2,2,2,4),(-2.97193608483724,-2.95192887323686,
-2.94012091410521,-2.90939597506129,-2.86047323796893,-2.84964247725588,
-2.8370898122707,-2.7983648378627,-2.75335703660431,-2.73035666552808,-2.70960978611333,
-2.67103173278106,-2.62240165692139,-2.60709516004842,-2.59699068818906,
-2.57663599727033,-2.54265354284125,-2.49989542929081,-2.48091802615095,
-2.45930240684551,-2.44722791131797,-2.38876883161093,-2.36596416851559,
-2.35471288561814,-2.33937239663575,-2.32868938600274,-2.28950399592165,
-2.25190455096406,-2.23141072131705,-2.20837106893445,-2.17581260534265,
-2.12253913486938,-2.11187411227277,-2.09904396385401,-2.09095727041018,
-2.06705795903259,-2.01141884276346,-1.98969977530631,-1.96818876663688,
-1.92161264544932,-1.87858971518575,-1.86617991899995,-1.85341229946849,
-1.84538618615958,-1.79923984675326,-1.76186576808191,-1.74299906076222,
-1.72120576212628,-1.69752412548059,-1.64529768411949,-1.62657703831408,
-1.61552934972242,-1.59794300642241,-1.58457980200152,-1.5303846474279,
-1.50521890933385,-1.48492514159982,-1.45455170860782,-1.40878193496465,
-1.38503664389725,-1.37441247636476,-1.36150561710902,-1.3036436110138,
-1.26798071259805,-1.24759135033079,-1.22422159422923,-1.1972515690798,
-1.1483366310095,-1.13286194451083,-1.12168770151473,-1.1000891057743,-1.06173611117017,
-1.02448714822718,-1.00562548119416,-0.983823363157249,-0.960123367584209,
-0.907756340566979,-0.889155637231191,-0.878265985002877,-0.877800523395954,
-0.877339573478321,-0.87687710719356,-0.876407848295914,-0.875926931138482,
-0.875429662648014,-0.874911343635513,-0.874367124318079,-0.873791878721041,
-0.873180087941176,-0.872960224745066,-0.872699570843726,-0.872388713835824,
-0.872015543849654,-0.871564343823832,-0.871014546561892,-0.870339041284213,
-0.86950188436627,-0.868455248153306,-0.867135439061309,-0.848961851427595,
-0.792155219620062,-0.767687499783322,-0.760127278344985,-0.747378291801462,
-0.727195204507704,-0.6956224038808,-0.653785941992173,-0.639632919810163,
-0.629171961549914,-0.628038955424361,-0.627650531208356,-0.627135655781143,
-0.626434726475891,-0.625451391820586,-0.624026098420751,-0.621891513544238,
-0.618606603424055,-0.59760520556375,-0.534886668924286,-0.515517748846135,
-0.496189359178997,-0.47427068471987,-0.433661336058603,-0.403293736559134,
-0.391100521352264,-0.389622585788981,-0.388725809455814,-0.374088004665795,
-0.346541156696376,-0.288907830836164,-0.270388531947011,-0.260445690242536,
-0.241163694574249,-0.192923662299934,-0.188151847174608,-0.157581533242111,
-0.145362980693881,-0.135452691958635,-0.0774953999897133,-0.040120865432972,
-0.0194272729031921,-4.22450758382579E-5),.UNSPECIFIED.);
#324=B_SPLINE_CURVE_WITH_KNOTS('',3,(#25159,#25160,#25161,#25162,#25163,
#25164,#25165,#25166,#25167,#25168,#25169,#25170),.UNSPECIFIED.,.F.,.F.,
(4,2,2,2,2,4),(-6.19125061960131,-6.11459210477152,-6.10118218427413,-6.09138246653058,
-6.0805744142751,-6.06752948703079),.UNSPECIFIED.);
#325=B_SPLINE_CURVE_WITH_KNOTS('',3,(#25171,#25172,#25173,#25174,#25175,
#25176,#25177,#25178,#25179,#25180,#25181,#25182,#25183,#25184,#25185,#25186,
#25187,#25188,#25189,#25190,#25191,#25192,#25193,#25194,#25195,#25196,#25197,
#25198,#25199,#25200,#25201,#25202,#25203,#25204,#25205,#25206,#25207,#25208,
#25209,#25210,#25211,#25212,#25213,#25214,#25215,#25216,#25217,#25218,#25219,
#25220,#25221,#25222,#25223,#25224,#25225,#25226,#25227,#25228,#25229,#25230,
#25231,#25232,#25233,#25234,#25235,#25236,#25237,#25238,#25239,#25240,#25241,
#25242,#25243,#25244,#25245,#25246,#25247,#25248,#25249,#25250,#25251,#25252,
#25253,#25254,#25255,#25256,#25257,#25258,#25259,#25260,#25261,#25262,#25263,
#25264,#25265,#25266,#25267,#25268,#25269,#25270,#25271,#25272,#25273,#25274,
#25275,#25276,#25277,#25278,#25279,#25280,#25281,#25282,#25283,#25284,#25285,
#25286,#25287,#25288,#25289,#25290,#25291,#25292,#25293,#25294,#25295,#25296,
#25297,#25298,#25299,#25300,#25301,#25302,#25303,#25304,#25305,#25306,#25307,
#25308,#25309,#25310,#25311,#25312,#25313,#25314,#25315,#25316,#25317,#25318,
#25319,#25320,#25321,#25322,#25323,#25324,#25325,#25326,#25327,#25328,#25329,
#25330,#25331,#25332,#25333,#25334,#25335,#25336,#25337,#25338,#25339,#25340,
#25341,#25342,#25343,#25344,#25345,#25346,#25347,#25348,#25349,#25350,#25351,
#25352,#25353,#25354,#25355,#25356,#25357,#25358,#25359,#25360,#25361,#25362,
#25363,#25364,#25365,#25366,#25367,#25368,#25369,#25370,#25371,#25372,#25373,
#25374,#25375,#25376,#25377,#25378,#25379,#25380,#25381,#25382,#25383,#25384,
#25385,#25386,#25387,#25388,#25389,#25390,#25391,#25392,#25393,#25394,#25395,
#25396,#25397,#25398,#25399,#25400,#25401,#25402,#25403,#25404,#25405,#25406,
#25407,#25408),.UNSPECIFIED.,.F.,.F.,(4,2,2,2,2,2,2,2,2,2,2,2,2,2,2,2,2,
2,2,2,2,2,2,2,2,2,2,2,2,2,2,2,2,2,2,2,2,2,2,2,2,2,2,2,2,2,2,2,2,2,2,2,2,
2,2,2,2,2,2,2,2,2,2,2,2,2,2,2,2,2,2,2,2,2,2,2,2,2,2,2,2,2,2,2,2,2,2,2,2,
2,2,2,2,2,2,2,2,2,2,2,2,2,2,2,2,2,2,2,2,2,2,2,2,2,2,2,2,2,4),(-3.21935065787348,
-3.19883993215343,-3.17468046572755,-3.15257215478691,-3.13357248786813,
-3.09564218739132,-3.03911040714761,-3.02834218215764,-3.01534663051692,
-2.93503669739894,-2.91100011453367,-2.89028938197555,-2.85536529536879,
-2.79326096098075,-2.78246612806759,-2.76951952060248,-2.7536920558834,
-2.71502398629461,-2.67793946133549,-2.65894795258787,-2.63682451956624,
-2.61263304134145,-2.5571309527284,-2.54104592183675,-2.53094940153547,
-2.51195313597093,-2.46271554281743,-2.43196737827471,-2.41298554602547,
-2.39084333428992,-2.36661271308228,-2.31420585751401,-2.29625973902099,
-2.28510235990775,-2.26620327200656,-2.23680336056377,-2.19050319584225,
-2.16852192966704,-2.14683423988054,-2.09877524151553,-2.05740984799487,
-2.04483905359599,-2.03195324182503,-2.02384218017162,-1.99990260085111,
-1.94283716841452,-1.92125884073421,-1.89914773078583,-1.87498213319719,
-1.81969249512517,-1.80345275169595,-1.79336832740628,-1.77460794421193,
-1.75972195848574,-1.69345995746482,-1.67271944336393,-1.6495661656083,
-1.61688781155841,-1.56340595922979,-1.5526923073717,-1.53959174384977,
-1.52347634227395,-1.48302696811088,-1.44649984896306,-1.42590469936836,
-1.40231255218522,-1.37503727225636,-1.32617837815377,-1.31066594779575,
-1.30045903902699,-1.27976446586618,-1.24479086077293,-1.20321200726434,
-1.18410449774137,-1.16218302345912,-1.11758202812253,-1.07332603885463,
-1.06091736331595,-1.04784084730578,-1.03954395378982,-1.02674608117364,
-0.968499318443193,-0.944192451583691,-0.923539977830503,-0.889649820455283,
-0.830127757784366,-0.816623310358302,-0.80495799538402,-0.79099201017799,
-0.762046506379547,-0.714844132629646,-0.692907950015024,-0.675121487949285,
-0.670832324905051,-0.666461806578334,-0.64046577079663,-0.59076945943148,
-0.574183141373688,-0.568620726120053,-0.557711346467638,-0.542875572991077,
-0.509730565833909,-0.466117009584465,-0.445164893188363,-0.43147798176649,
-0.397285006004167,-0.34710160658848,-0.329047989813588,-0.326518363962881,
-0.324371516630138,-0.32216218654158,-0.316920419244058,-0.29844487407586,
-0.268191413548545,-0.219692548601389,-0.198837715538191,-0.180423147243701,
-0.129072604151441,-0.123769996527385),.UNSPECIFIED.);
#326=B_SPLINE_CURVE_WITH_KNOTS('',3,(#25413,#25414,#25415,#25416,#25417,
#25418,#25419,#25420,#25421,#25422,#25423,#25424,#25425,#25426,#25427,#25428,
#25429,#25430,#25431,#25432,#25433,#25434,#25435,#25436,#25437,#25438,#25439,
#25440,#25441,#25442,#25443,#25444,#25445,#25446,#25447,#25448,#25449,#25450,
#25451,#25452,#25453,#25454,#25455,#25456,#25457,#25458,#25459,#25460,#25461,
#25462,#25463,#25464,#25465,#25466,#25467,#25468,#25469,#25470,#25471,#25472,
#25473,#25474,#25475,#25476,#25477,#25478,#25479,#25480,#25481,#25482,#25483,
#25484,#25485,#25486,#25487,#25488,#25489,#25490,#25491,#25492,#25493,#25494,
#25495,#25496,#25497,#25498,#25499,#25500,#25501,#25502,#25503,#25504,#25505,
#25506,#25507,#25508,#25509,#25510,#25511,#25512,#25513,#25514,#25515,#25516,
#25517,#25518,#25519,#25520,#25521,#25522,#25523,#25524,#25525,#25526,#25527,
#25528,#25529,#25530,#25531,#25532,#25533,#25534,#25535,#25536,#25537,#25538,
#25539,#25540,#25541,#25542,#25543,#25544,#25545,#25546,#25547,#25548,#25549,
#25550,#25551,#25552,#25553,#25554,#25555,#25556,#25557,#25558,#25559,#25560,
#25561,#25562,#25563,#25564,#25565,#25566,#25567,#25568,#25569,#25570,#25571,
#25572,#25573,#25574,#25575,#25576,#25577,#25578,#25579,#25580,#25581,#25582,
#25583,#25584,#25585,#25586,#25587,#25588,#25589,#25590,#25591,#25592,#25593,
#25594,#25595,#25596,#25597,#25598,#25599,#25600,#25601,#25602,#25603,#25604,
#25605,#25606,#25607,#25608,#25609,#25610,#25611,#25612,#25613,#25614,#25615,
#25616,#25617,#25618,#25619,#25620,#25621,#25622,#25623,#25624,#25625,#25626,
#25627,#25628,#25629,#25630,#25631,#25632,#25633,#25634,#25635,#25636,#25637,
#25638,#25639,#25640,#25641,#25642,#25643,#25644,#25645,#25646,#25647,#25648,
#25649,#25650,#25651,#25652,#25653,#25654,#25655,#25656,#25657,#25658,#25659,
#25660,#25661,#25662,#25663,#25664),.UNSPECIFIED.,.F.,.F.,(4,2,2,2,2,2,
2,2,2,2,2,2,2,2,2,2,2,2,2,2,2,2,2,2,2,2,2,2,2,2,2,2,2,2,2,2,2,2,2,2,2,2,
2,2,2,2,2,2,2,2,2,2,2,2,2,2,2,2,2,2,2,2,2,2,2,2,2,2,2,2,2,2,2,2,2,2,2,2,
2,2,2,2,2,2,2,2,2,2,2,2,2,2,2,2,2,2,2,2,2,2,2,2,2,2,2,2,2,2,2,2,2,2,2,2,
2,2,2,2,2,2,2,2,2,2,2,4),(-6.06751823289617,-6.05216985439356,-6.04103481939818,
-6.02557321717136,-5.97667191387825,-5.94968968410486,-5.93039731693532,
-5.91944651626977,-5.90063830947764,-5.84116683591585,-5.8164919490186,
-5.80194847891225,-5.80106147909734,-5.79959516612697,-5.78736829731487,
-5.75662931646851,-5.71631317697064,-5.69444685649932,-5.67516324903087,
-5.6558514710628,-5.59291939713055,-5.57204497524852,-5.56884284248475,
-5.56676591268161,-5.56538124728371,-5.56442789091796,-5.55347319652719,
-5.54276581966756,-5.51863878038839,-5.47333433612668,-5.4590086239272,
-5.43960189395014,-5.42960245830538,-5.40775855864031,-5.34358675264726,
-5.3245364822329,-5.32305198427973,-5.32188176296775,-5.32095155593872,
-5.32020569217921,-5.3196024497203,-5.30759664293841,-5.29511853294368,
-5.2483675487801,-5.20603207764642,-5.18444778657414,-5.16544951498595,
-5.12818006932293,-5.08231423978833,-5.06590499029098,-5.0547968335007,
-5.03438207189384,-4.98405378648087,-4.96062675124528,-4.93895534777799,
-4.92001489661793,-4.88115097955362,-4.83958434917752,-4.821417591176,-4.81037548631603,
-4.79228128067626,-4.74218267710513,-4.72597268310792,-4.71404289800843,
-4.6925572783407,-4.67348748930582,-4.62019019659991,-4.58342395693775,
-4.57054122681807,-4.55823019031933,-4.52221913441196,-4.49450549413032,
-4.4703950265217,-4.4483953197237,-4.42711520985584,-4.37043780926428,-4.3373277814431,
-4.32457302525111,-4.31215184207256,-4.26933239663672,-4.22249370042298,
-4.20100430556186,-4.17926155933519,-4.12921099743551,-4.09039684130619,
-4.07808218236373,-4.06520371641284,-4.02872858719653,-3.97698848959201,
-3.95543577231078,-3.93641507025487,-3.88910970172197,-3.85833701207767,
-3.83900650592549,-3.82794344240008,-3.81124535387285,-3.77522116985027,
-3.73085601460143,-3.70938320584275,-3.69030354853046,-3.64562300336844,
-3.61333548988716,-3.60368651433719,-3.58930543073169,-3.57795425894659,
-3.55616676277755,-3.4977325755875,-3.485666969139,-3.46405934236577,-3.44507670393331,
-3.3763885214348,-3.3502333740173,-3.33875764952293,-3.32431075568772,-3.26557124610015,
-3.24146005785084,-3.21946002542466,-3.19818023406349,-3.14150432593376,
-3.10839224131371,-3.09563728477073,-3.08321632980159,-3.0405853613927,
-2.99518020863916,-2.97330607703263,-2.97193608483724),.UNSPECIFIED.);
#327=B_SPLINE_CURVE_WITH_KNOTS('',3,(#25666,#25667,#25668,#25669,#25670,
#25671,#25672,#25673,#25674,#25675,#25676,#25677),.UNSPECIFIED.,.F.,.F.,
(4,2,2,2,2,4),(-0.123769996527385,-0.0905127513457727,-0.0777901832579179,
-0.0678980718455824,-0.0543312819426131,-7.62333445612098E-5),
 .UNSPECIFIED.);
#328=B_SPLINE_CURVE_WITH_KNOTS('',3,(#25678,#25679,#25680,#25681,#25682,
#25683,#25684,#25685,#25686,#25687,#25688,#25689,#25690,#25691,#25692,#25693,
#25694,#25695,#25696,#25697,#25698,#25699,#25700,#25701,#25702,#25703,#25704,
#25705,#25706,#25707,#25708,#25709,#25710,#25711,#25712,#25713,#25714,#25715,
#25716,#25717,#25718,#25719,#25720,#25721,#25722,#25723,#25724,#25725,#25726,
#25727,#25728,#25729,#25730,#25731,#25732,#25733,#25734,#25735,#25736,#25737,
#25738,#25739,#25740,#25741,#25742,#25743,#25744,#25745,#25746,#25747,#25748,
#25749,#25750,#25751,#25752,#25753,#25754,#25755,#25756,#25757,#25758,#25759,
#25760,#25761,#25762,#25763,#25764,#25765,#25766,#25767,#25768,#25769,#25770,
#25771,#25772,#25773,#25774,#25775,#25776,#25777,#25778,#25779,#25780,#25781,
#25782,#25783,#25784,#25785,#25786,#25787,#25788,#25789,#25790,#25791,#25792,
#25793,#25794,#25795,#25796,#25797,#25798,#25799,#25800,#25801,#25802,#25803,
#25804,#25805,#25806,#25807,#25808,#25809,#25810,#25811,#25812,#25813,#25814,
#25815,#25816,#25817,#25818,#25819,#25820,#25821,#25822,#25823,#25824,#25825,
#25826,#25827,#25828,#25829,#25830,#25831,#25832,#25833,#25834,#25835,#25836,
#25837,#25838,#25839,#25840,#25841,#25842,#25843,#25844,#25845,#25846,#25847,
#25848,#25849,#25850,#25851,#25852,#25853,#25854,#25855,#25856,#25857,#25858,
#25859,#25860,#25861,#25862,#25863,#25864,#25865,#25866,#25867,#25868,#25869,
#25870,#25871,#25872,#25873,#25874,#25875,#25876,#25877,#25878,#25879,#25880,
#25881,#25882,#25883,#25884,#25885,#25886,#25887,#25888,#25889,#25890,#25891,
#25892,#25893,#25894,#25895,#25896,#25897,#25898,#25899,#25900,#25901,#25902,
#25903,#25904,#25905,#25906,#25907,#25908,#25909,#25910,#25911,#25912,#25913,
#25914,#25915,#25916,#25917,#25918,#25919,#25920,#25921,#25922,#25923,#25924,
#25925,#25926,#25927),.UNSPECIFIED.,.F.,.F.,(4,2,2,2,2,2,2,2,2,2,2,2,2,
2,2,2,2,2,2,2,2,2,2,2,2,2,2,2,2,2,2,2,2,2,2,2,2,2,2,2,2,2,2,2,2,2,2,2,2,
2,2,2,2,2,2,2,2,2,2,2,2,2,2,2,2,2,2,2,2,2,2,2,2,2,2,2,2,2,2,2,2,2,2,2,2,
2,2,2,2,2,2,2,2,2,2,2,2,2,2,2,2,2,2,2,2,2,2,2,2,2,2,2,2,2,2,2,2,2,2,2,2,
2,2,2,4),(-6.19126743548388,-6.16828474090662,-6.14963669721633,-6.12911626038459,
-6.09407045290797,-6.04469600614485,-6.02998196054132,-6.02386121116435,
-6.01159825099855,-5.95368397556366,-5.92710415616773,-5.90421029149716,
-5.90021607519006,-5.87841716429693,-5.82000325402683,-5.79737342519182,
-5.79267308287125,-5.78858396591072,-5.77677067690243,-5.763794382649,-5.72740605585022,
-5.69132633743218,-5.67014275657265,-5.65171719209081,-5.63454244806347,
-5.56796826879926,-5.54857202038289,-5.54709494978456,-5.54617504089132,
-5.54559020305959,-5.54419373615834,-5.54299794275277,-5.54195158343031,
-5.54101409538384,-5.54015203704611,-5.52924140760204,-5.51501686712426,
-5.45662020770856,-5.43203024657978,-5.41175884842804,-5.39118243177943,
-5.38957350127555,-5.35033717751618,-5.31363618012526,-5.2981433826564,
-5.28537722947894,-5.27269374992325,-5.23997200558627,-5.19165610213958,
-5.16761046779675,-5.14690102368562,-5.11310367121344,-5.07006809097023,
-5.05355856087118,-5.04024936256002,-5.0296336672651,-5.00647453346544,
-4.95036148269244,-4.93817769851656,-4.9163708986313,-4.89718777425577,
-4.86434940364664,-4.82343290460124,-4.80724377807857,-4.79410406073478,
-4.78174469382991,-4.74930740421553,-4.71774629642357,-4.69356256449648,
-4.6714423341025,-4.65244808474731,-4.61052461602099,-4.57196623791136,
-4.55331944261558,-4.54216457790801,-4.52398933596185,-4.47227732687522,
-4.44793903421221,-4.42574481020861,-4.40423002831425,-4.37061406694095,
-4.33110700122942,-4.3091582311323,-4.2978727563582,-4.28217170822759,-4.23302884429366,
-4.20615261685623,-4.18274749012401,-4.16209459124178,-4.12452332339496,
-4.08514945436609,-4.06323528165216,-4.05195189836505,-4.03623646868448,
-3.98708296269589,-3.96022269422368,-3.93682514102816,-3.91616993218671,
-3.8799125896541,-3.83959194282026,-3.82349638939828,-3.81040649619156,
-3.79800829724502,-3.76547446920891,-3.71726030650093,-3.69283088232667,
-3.67220171957627,-3.63872775754081,-3.59488424748989,-3.57825732565668,
-3.56488643363806,-3.55269358153526,-3.51528834266287,-3.48796576787696,
-3.46386705117982,-3.44178754238168,-3.42277161251931,-3.38511406908166,
-3.33893450363513,-3.33092372657556,-3.31814148682508,-3.30725003571265,
-3.25782453257591,-3.227198544306,-3.21940568334086),.UNSPECIFIED.);
#329=B_SPLINE_CURVE_WITH_KNOTS('',3,(#25933,#25934,#25935,#25936,#25937,
#25938,#25939,#25940,#25941,#25942,#25943,#25944,#25945,#25946,#25947,#25948,
#25949,#25950,#25951,#25952,#25953,#25954,#25955,#25956,#25957,#25958,#25959,
#25960,#25961,#25962,#25963,#25964,#25965,#25966,#25967,#25968,#25969,#25970,
#25971,#25972,#25973,#25974,#25975,#25976,#25977,#25978,#25979,#25980,#25981,
#25982,#25983,#25984,#25985,#25986,#25987,#25988,#25989,#25990,#25991,#25992,
#25993,#25994,#25995,#25996,#25997,#25998,#25999,#26000,#26001,#26002,#26003,
#26004,#26005,#26006,#26007,#26008,#26009,#26010,#26011,#26012,#26013,#26014,
#26015,#26016,#26017,#26018,#26019,#26020,#26021,#26022,#26023,#26024,#26025,
#26026,#26027,#26028,#26029,#26030,#26031,#26032,#26033,#26034,#26035,#26036,
#26037,#26038,#26039,#26040,#26041,#26042,#26043,#26044,#26045,#26046,#26047,
#26048,#26049,#26050,#26051,#26052,#26053,#26054,#26055,#26056,#26057,#26058,
#26059,#26060,#26061,#26062,#26063,#26064,#26065,#26066,#26067,#26068,#26069,
#26070,#26071,#26072,#26073,#26074,#26075,#26076,#26077,#26078,#26079,#26080,
#26081,#26082,#26083,#26084,#26085,#26086,#26087,#26088,#26089,#26090,#26091,
#26092,#26093,#26094,#26095,#26096,#26097,#26098,#26099,#26100,#26101,#26102,
#26103,#26104,#26105,#26106,#26107,#26108,#26109,#26110,#26111,#26112,#26113,
#26114,#26115,#26116,#26117,#26118,#26119,#26120,#26121,#26122,#26123,#26124,
#26125,#26126,#26127,#26128,#26129,#26130,#26131,#26132,#26133,#26134,#26135,
#26136,#26137,#26138,#26139,#26140,#26141,#26142,#26143,#26144,#26145,#26146,
#26147,#26148,#26149,#26150,#26151,#26152,#26153,#26154,#26155,#26156),
 .UNSPECIFIED.,.F.,.F.,(4,2,2,2,2,2,2,2,2,2,2,2,2,2,2,2,2,2,2,2,2,2,2,2,
2,2,2,2,2,2,2,2,2,2,2,2,2,2,2,2,2,2,2,2,2,2,2,2,2,2,2,2,2,2,2,2,2,2,2,2,
2,2,2,2,2,2,2,2,2,2,2,2,2,2,2,2,2,2,2,2,2,2,2,2,2,2,2,2,2,2,2,2,2,2,2,2,
2,2,2,2,2,2,2,2,2,2,2,2,2,2,2,4),(-2.97194085139843,-2.94720454401188,-2.92566231016735,
-2.90397702385757,-2.86051929887029,-2.82465054145874,-2.80787106414141,
-2.79681155251526,-2.7775973373761,-2.74716968982091,-2.69923207646114,
-2.68023021012824,-2.65865057730204,-2.64661598158126,-2.58979555400551,
-2.56692485617133,-2.5564119937776,-2.54327419413601,-2.5270360980217,-2.48549429734368,
-2.4501651762219,-2.429592601371,-2.40605095797732,-2.36037576064841,-2.32250927335493,
-2.31162328725177,-2.29915169432355,-2.29141098067681,-2.24597551189013,
-2.21611003985732,-2.19281752224885,-2.17217174544167,-2.13554071754574,
-2.0861573261149,-2.07001213803844,-2.06003746159135,-2.04174443590058,
-2.02744768186526,-1.95977683493294,-1.93924675203804,-1.91630760462578,
-1.86901146007682,-1.83078791279796,-1.81994514128857,-1.80741050635883,
-1.79960887728262,-1.78796090745952,-1.74095528196348,-1.71016066593002,
-1.68984610606951,-1.66488083338587,-1.63440217472169,-1.58500446603003,
-1.57416275046488,-1.56162647157065,-1.52366524158169,-1.47187743755666,
-1.45047394030724,-1.42863155009465,-1.40484773404046,-1.35183276020116,
-1.33377485674184,-1.32273254318616,-1.30452844940075,-1.26303606644378,
-1.22415961713766,-1.20521982789832,-1.18354678337682,-1.1399823029505,
-1.10471572555404,-1.08762624998673,-1.07657703856195,-1.05777790033058,
-1.01581243229156,-0.978129648870317,-0.959230991313171,-0.937491640597036,
-0.893420452873878,-0.84855216661018,-0.836259127369291,-0.827241481570068,
-0.814007125752753,-0.788054562102724,-0.734781189971937,-0.713689333105909,
-0.695987873343957,-0.673847854430633,-0.63384205353527,-0.602616315005399,
-0.590379232392695,-0.57848395128835,-0.56335215670829,-0.528407931174318,
-0.48918639969776,-0.468054608601724,-0.446837684251083,-0.383704569944666,
-0.355887136398819,-0.345104699599106,-0.336392856808139,-0.32355232068174,
-0.299200230067635,-0.242460285456655,-0.221530628746799,-0.210680784737342,
-0.184716624213847,-0.148210722704724,-0.110535353186893,-0.0984733264317177,
-0.088502788824408,-0.0744376508116578,-4.22937978884163E-5),
 .UNSPECIFIED.);
#330=B_SPLINE_CURVE_WITH_KNOTS('',3,(#26157,#26158,#26159,#26160,#26161,
#26162,#26163,#26164,#26165,#26166,#26167,#26168),.UNSPECIFIED.,.F.,.F.,
(4,2,2,2,2,4),(-6.19124774226682,-6.17979920712744,-6.16889498083572,-6.14808214462905,
-6.07247948514389,-6.06751823289617),.UNSPECIFIED.);
#331=B_SPLINE_CURVE_WITH_KNOTS('',3,(#26169,#26170,#26171,#26172,#26173,
#26174,#26175,#26176,#26177,#26178,#26179,#26180,#26181,#26182,#26183,#26184,
#26185,#26186,#26187,#26188,#26189,#26190,#26191,#26192,#26193,#26194,#26195,
#26196,#26197,#26198,#26199,#26200,#26201,#26202,#26203,#26204,#26205,#26206,
#26207,#26208,#26209,#26210,#26211,#26212,#26213,#26214,#26215,#26216,#26217,
#26218,#26219,#26220,#26221,#26222,#26223,#26224,#26225,#26226,#26227,#26228,
#26229,#26230,#26231,#26232,#26233,#26234,#26235,#26236,#26237,#26238,#26239,
#26240,#26241,#26242,#26243,#26244,#26245,#26246,#26247,#26248,#26249,#26250,
#26251,#26252,#26253,#26254,#26255,#26256,#26257,#26258,#26259,#26260,#26261,
#26262,#26263,#26264,#26265,#26266,#26267,#26268,#26269,#26270,#26271,#26272,
#26273,#26274,#26275,#26276,#26277,#26278,#26279,#26280,#26281,#26282,#26283,
#26284,#26285,#26286,#26287,#26288,#26289,#26290,#26291,#26292,#26293,#26294,
#26295,#26296,#26297,#26298,#26299,#26300,#26301,#26302,#26303,#26304,#26305,
#26306,#26307,#26308,#26309,#26310,#26311,#26312,#26313,#26314,#26315,#26316,
#26317,#26318,#26319,#26320,#26321,#26322,#26323,#26324,#26325,#26326,#26327,
#26328,#26329,#26330,#26331,#26332,#26333,#26334,#26335,#26336,#26337,#26338,
#26339,#26340,#26341,#26342,#26343,#26344,#26345,#26346,#26347,#26348,#26349,
#26350,#26351,#26352,#26353,#26354,#26355,#26356,#26357,#26358,#26359,#26360,
#26361,#26362,#26363,#26364,#26365,#26366,#26367,#26368,#26369,#26370,#26371,
#26372,#26373,#26374,#26375,#26376,#26377,#26378,#26379,#26380,#26381,#26382,
#26383,#26384,#26385,#26386,#26387,#26388,#26389,#26390,#26391,#26392,#26393,
#26394,#26395,#26396,#26397,#26398,#26399,#26400,#26401,#26402),
 .UNSPECIFIED.,.F.,.F.,(4,2,2,2,2,2,2,2,2,2,2,2,2,2,2,2,2,2,2,2,2,2,2,2,
2,2,2,2,2,2,2,2,2,2,2,2,2,2,2,2,2,2,2,2,2,2,2,2,2,2,2,2,2,2,2,2,2,2,2,2,
2,2,2,2,2,2,2,2,2,2,2,2,2,2,2,2,2,2,2,2,2,2,2,2,2,2,2,2,2,2,2,2,2,2,2,2,
2,2,2,2,2,2,2,2,2,2,2,2,2,2,2,2,2,2,2,2,4),(-3.21940568334086,-3.21537518281795,
-3.19388774193548,-3.17165692436193,-3.12302283788408,-3.09569644682846,
-3.07754890742245,-3.0663938538005,-3.04771748855768,-3.03294881751308,
-2.96636327134014,-2.94563227095093,-2.9224521615715,-2.88981276131488,
-2.83646498215127,-2.82572714784475,-2.81267331782483,-2.77725580497548,
-2.72441739094326,-2.70274064263488,-2.68074610034784,-2.65682487107412,
-2.60349271392291,-2.58556032236083,-2.57440246759245,-2.55548681158526,
-2.52604015184907,-2.47982883707528,-2.45784279271721,-2.43615845527834,
-2.42411163874887,-2.37240571003688,-2.34551192307258,-2.33452652564069,
-2.32188896753746,-2.2822927869588,-2.23329088089453,-2.21145448751781,
-2.18962991914374,-2.17742623062078,-2.12169781414149,-2.09834709892359,
-2.08770600008823,-2.07445341813518,-2.05805153802712,-2.01573901141806,
-1.98093861853728,-1.96023434351834,-1.93616654182965,-1.88785460325268,
-1.8551250464599,-1.84246469577492,-1.82967460853503,-1.79675708291012,
-1.74011555734052,-1.71857923434076,-1.69641361277398,-1.67213458252677,
-1.62079143998806,-1.60228743225512,-1.59113339355084,-1.57282210582547,
-1.52459732453246,-1.48971601185184,-1.46893898393931,-1.44516035009689,
-1.36908148091808,-1.35380556144267,-1.34238444613811,-1.31829372119246,
-1.27994683956392,-1.24705192910284,-1.22786357015394,-1.20606381835904,
-1.19388794222435,-1.1373428992037,-1.11442862701847,-1.10384670406367,
-1.09045852983862,-1.07379911084305,-1.02972730707585,-0.996447331222667,
-0.975828834285558,-0.951338733694337,-0.903134242177257,-0.870665632373246,
-0.858295198757108,-0.848295578259484,-0.834311223982213,-0.805282885672852,
-0.758244952392974,-0.736665546557421,-0.717480796217459,-0.69539793510178,
-0.654411094506414,-0.624539223894218,-0.61224561467836,-0.602218042126419,
-0.588128117322131,-0.558615882604407,-0.512531037488587,-0.490904180488482,
-0.471707812870348,-0.44967731277801,-0.40899133647246,-0.378573842295565,
-0.366300615793601,-0.356265328841865,-0.34214640007698,-0.312499905836464,
-0.266673952521797,-0.245035028836767,-0.225835694027473,-0.203818362017452,
-0.163207496702661,-0.132704799728157,-0.12380451714121),.UNSPECIFIED.);
#332=B_SPLINE_CURVE_WITH_KNOTS('',3,(#26407,#26408,#26409,#26410,#26411,
#26412,#26413,#26414,#26415,#26416,#26417,#26418,#26419,#26420,#26421,#26422,
#26423,#26424,#26425,#26426,#26427,#26428,#26429,#26430,#26431,#26432,#26433,
#26434,#26435,#26436,#26437,#26438,#26439,#26440,#26441,#26442,#26443,#26444,
#26445,#26446,#26447,#26448,#26449,#26450,#26451,#26452,#26453,#26454,#26455,
#26456,#26457,#26458,#26459,#26460,#26461,#26462,#26463,#26464,#26465,#26466,
#26467,#26468,#26469,#26470,#26471,#26472,#26473,#26474,#26475,#26476,#26477,
#26478,#26479,#26480,#26481,#26482,#26483,#26484,#26485,#26486,#26487,#26488,
#26489,#26490,#26491,#26492,#26493,#26494,#26495,#26496,#26497,#26498,#26499,
#26500,#26501,#26502,#26503,#26504,#26505,#26506,#26507,#26508,#26509,#26510,
#26511,#26512,#26513,#26514,#26515,#26516,#26517,#26518,#26519,#26520,#26521,
#26522,#26523,#26524,#26525,#26526,#26527,#26528,#26529,#26530,#26531,#26532,
#26533,#26534,#26535,#26536,#26537,#26538,#26539,#26540,#26541,#26542,#26543,
#26544,#26545,#26546,#26547,#26548,#26549,#26550,#26551,#26552,#26553,#26554,
#26555,#26556,#26557,#26558,#26559,#26560,#26561,#26562,#26563,#26564,#26565,
#26566,#26567,#26568,#26569,#26570,#26571,#26572,#26573,#26574,#26575,#26576,
#26577,#26578,#26579,#26580,#26581,#26582,#26583,#26584,#26585,#26586,#26587,
#26588,#26589,#26590,#26591,#26592,#26593,#26594,#26595,#26596,#26597,#26598,
#26599,#26600,#26601,#26602,#26603,#26604,#26605,#26606,#26607,#26608,#26609,
#26610,#26611,#26612,#26613,#26614,#26615,#26616,#26617,#26618,#26619,#26620,
#26621,#26622,#26623,#26624,#26625,#26626,#26627,#26628,#26629,#26630,#26631,
#26632,#26633,#26634,#26635,#26636,#26637,#26638,#26639,#26640,#26641,#26642,
#26643,#26644,#26645,#26646,#26647,#26648,#26649,#26650,#26651,#26652,#26653,
#26654,#26655,#26656,#26657,#26658),.UNSPECIFIED.,.F.,.F.,(4,2,2,2,2,2,
2,2,2,2,2,2,2,2,2,2,2,2,2,2,2,2,2,2,2,2,2,2,2,2,2,2,2,2,2,2,2,2,2,2,2,2,
2,2,2,2,2,2,2,2,2,2,2,2,2,2,2,2,2,2,2,2,2,2,2,2,2,2,2,2,2,2,2,2,2,2,2,2,
2,2,2,2,2,2,2,2,2,2,2,2,2,2,2,2,2,2,2,2,2,2,2,2,2,2,2,2,2,2,2,2,2,2,2,2,
2,2,2,2,2,2,2,2,2,2,2,4),(-6.06757918107776,-6.0425092840288,-6.01913297277231,
-6.00269541027639,-6.00150315298628,-5.9998313797898,-5.99763976448805,
-5.98465418449314,-5.9406681252557,-5.9088475850095,-5.8836036632628,-5.8810292257421,
-5.87923008645437,-5.87722136327289,-5.8742110451739,-5.86788716148614,
-5.84269595422236,-5.78665680273765,-5.76856503940206,-5.76500447727211,
-5.75283216642732,-5.74047817198498,-5.67918711101816,-5.65423562140544,
-5.6325240517583,-5.61715766711512,-5.58736987975874,-5.53897062659706,
-5.52177496444567,-5.5204609047147,-5.51935035276981,-5.50794793173914,
-5.50029649178016,-5.48077251674079,-5.42946812382137,-5.39793361855681,
-5.37797793281941,-5.35385127240683,-5.29558425720612,-5.28281203245124,
-5.27454271554864,-5.26152521450837,-5.25095638266374,-5.22767217437242,
-5.17427351781813,-5.14749367538006,-5.1272835884852,-5.09937774256489,
-5.06054431887117,-5.03650023810903,-5.02838323144583,-5.01552196856433,
-5.0048737315627,-4.98073387911697,-4.93529157456466,-4.92094640247116,
-4.89725205134467,-4.87671895644528,-4.84207563224789,-4.79977336674278,
-4.78341996674339,-4.770221271667,-4.75973499494835,-4.73705191893717,-4.68034176094925,
-4.66822463102999,-4.64657038874826,-4.62761834863283,-4.58794163748908,
-4.54293239717864,-4.53536231103792,-4.52306537548176,-4.51016510867539,
-4.47384643051742,-4.42200101559401,-4.4004483927239,-4.38142732226523,
-4.32275420088346,-4.28831320715352,-4.27643508322084,-4.26291901857581,
-4.20361235139557,-4.16988039991287,-4.14940084427622,-4.12547595072461,
-4.04538047260695,-4.03244839446304,-4.02183700689893,-3.99820596617183,
-3.94248514280315,-3.91696301581566,-3.89669919714872,-3.86699525065758,
-3.81847538714104,-3.79451216933769,-3.78318289032979,-3.76821010785203,
-3.71108531348086,-3.67794447119182,-3.6574994466546,-3.63340544408877,
-3.59185012370537,-3.55200549463713,-3.53976894458819,-3.52679307883785,
-3.48199018969532,-3.45056451401728,-3.43861234632596,-3.41710658863934,
-3.39538173783905,-3.34707275653335,-3.31877978936851,-3.3003136537619,
-3.28926962034477,-3.27145927913169,-3.21923671067992,-3.1950365723045,
-3.17299358771688,-3.15174471974862,-3.09562857937333,-3.09013019814411,
-3.06039538616283,-3.04817502755174,-3.0351783347152,-2.99976503962884,
-2.97194085139843),.UNSPECIFIED.);
#333=B_SPLINE_CURVE_WITH_KNOTS('',3,(#26660,#26661,#26662,#26663,#26664,
#26665,#26666,#26667,#26668,#26669,#26670,#26671),.UNSPECIFIED.,.F.,.F.,
(4,2,2,2,2,4),(-0.12380451714121,-0.120419049820546,-0.110388596683704,
-0.0962877087444727,-0.0203605578094701,-8.03739326426108E-5),
 .UNSPECIFIED.);
#334=B_SPLINE_CURVE_WITH_KNOTS('',3,(#26672,#26673,#26674,#26675,#26676,
#26677,#26678,#26679,#26680,#26681,#26682,#26683,#26684,#26685,#26686,#26687,
#26688,#26689,#26690,#26691,#26692,#26693,#26694,#26695,#26696,#26697,#26698,
#26699,#26700,#26701,#26702,#26703,#26704,#26705,#26706,#26707,#26708,#26709,
#26710,#26711,#26712,#26713,#26714,#26715,#26716,#26717,#26718,#26719,#26720,
#26721,#26722,#26723,#26724,#26725,#26726,#26727,#26728,#26729,#26730,#26731,
#26732,#26733,#26734,#26735,#26736,#26737,#26738,#26739,#26740,#26741,#26742,
#26743,#26744,#26745,#26746,#26747,#26748,#26749,#26750,#26751,#26752,#26753,
#26754,#26755,#26756,#26757,#26758,#26759,#26760,#26761,#26762,#26763,#26764,
#26765,#26766,#26767,#26768,#26769,#26770,#26771,#26772,#26773,#26774,#26775,
#26776,#26777,#26778,#26779,#26780,#26781,#26782,#26783,#26784,#26785,#26786,
#26787,#26788,#26789,#26790,#26791,#26792,#26793,#26794,#26795,#26796,#26797,
#26798,#26799,#26800,#26801,#26802,#26803,#26804,#26805,#26806,#26807,#26808,
#26809,#26810,#26811,#26812,#26813,#26814,#26815,#26816,#26817,#26818,#26819,
#26820,#26821,#26822,#26823,#26824,#26825,#26826,#26827,#26828,#26829,#26830,
#26831,#26832,#26833,#26834,#26835,#26836,#26837,#26838,#26839,#26840,#26841,
#26842,#26843,#26844,#26845,#26846,#26847,#26848,#26849,#26850,#26851,#26852,
#26853,#26854,#26855,#26856,#26857,#26858,#26859,#26860,#26861,#26862,#26863,
#26864,#26865,#26866,#26867,#26868,#26869,#26870,#26871,#26872,#26873,#26874,
#26875,#26876,#26877,#26878,#26879,#26880,#26881,#26882,#26883,#26884,#26885,
#26886,#26887,#26888,#26889,#26890,#26891,#26892,#26893,#26894,#26895,#26896,
#26897,#26898,#26899,#26900,#26901),.UNSPECIFIED.,.F.,.F.,(4,2,2,2,2,2,
2,2,2,2,2,2,2,2,2,2,2,2,2,2,2,2,2,2,2,2,2,2,2,2,2,2,2,2,2,2,2,2,2,2,2,2,
2,2,2,2,2,2,2,2,2,2,2,2,2,2,2,2,2,2,2,2,2,2,2,2,2,2,2,2,2,2,2,2,2,2,2,2,
2,2,2,2,2,2,2,2,2,2,2,2,2,2,2,2,2,2,2,2,2,2,2,2,2,2,2,2,2,2,2,2,2,2,2,2,
4),(-6.19122556259034,-6.18004740270646,-6.16748591998267,-6.09113194607832,
-6.07706836346535,-6.06704779425147,-6.05473520553522,-6.02501903578712,
-5.98397307877302,-5.96188042653447,-5.94269819912774,-5.92110448534014,
-5.87399109860499,-5.84499751355316,-5.83102063291017,-5.8210229763796,
-5.80864667274274,-5.77935919896759,-5.73815902250305,-5.71603969695784,
-5.69686303505453,-5.67529397400228,-5.6277335336895,-5.59896071793734,
-5.58503255073024,-5.57504767079496,-5.56431860329828,-5.54017043434067,
-5.49464051115725,-5.4718140082508,-5.45273490810619,-5.43180851022003,
-5.37882004361869,-5.35191059712329,-5.33840671596333,-5.32847465982512,
-5.31565405015465,-5.26964061721162,-5.23840972234037,-5.22646140127431,
-5.2048640825141,-5.18277462051979,-5.14845992804416,-5.11124578379915,
-5.09566355949358,-5.08284897101742,-5.0702115402229,-5.01960042980399,
-4.98590509253942,-4.96290430734998,-4.94210216476408,-4.87788392953217,
-4.84684417213855,-4.83501970443291,-4.82098522698032,-4.76229845625624,
-4.73766427614092,-4.71532813422006,-4.69391474227125,-4.63809691043105,
-4.60153542554785,-4.58953062666189,-4.57585291875668,-4.51508742865812,
-4.49090680494819,-4.4687880773086,-4.44979307946989,-4.41265860140473,
-4.37403350522802,-4.35231588542249,-4.34104388667543,-4.32524399167478,
-4.2871529368824,-4.28318436773609,-4.25328416838485,-4.24161278356404,
-4.22025690534415,-4.19783417444567,-4.1500095774358,-4.10985760192419,
-4.09780744778015,-4.0842092232353,-3.99989869582475,-3.97755882727475,
-3.95614885444126,-3.8994693489945,-3.87483294966568,-3.86657717297908,
-3.85354281502676,-3.8410998466868,-3.7973975195042,-3.76451350691437,-3.75223279299253,
-3.73033896190173,-3.71121389745691,-3.67282028174865,-3.63568216311131,
-3.62011333051749,-3.60730609629866,-3.59466237471625,-3.56193199085345,
-3.51362789091799,-3.48954513603817,-3.46884456223314,-3.43518517415531,
-3.3919894801938,-3.37545658835731,-3.36213514293282,-3.34990876266441,
-3.31273786921841,-3.28534066085584,-3.26122171044855,-3.23913259834888,
-3.22012209697371,-3.2192985515723),.UNSPECIFIED.);
#335=B_SPLINE_CURVE_WITH_KNOTS('',3,(#26907,#26908,#26909,#26910,#26911,
#26912,#26913,#26914,#26915,#26916,#26917,#26918,#26919,#26920,#26921,#26922,
#26923,#26924,#26925,#26926,#26927,#26928,#26929,#26930,#26931,#26932,#26933,
#26934,#26935,#26936,#26937,#26938,#26939,#26940,#26941,#26942,#26943,#26944,
#26945,#26946,#26947,#26948,#26949,#26950,#26951,#26952,#26953,#26954,#26955,
#26956,#26957,#26958,#26959,#26960,#26961,#26962,#26963,#26964,#26965,#26966,
#26967,#26968,#26969,#26970,#26971,#26972,#26973,#26974,#26975,#26976,#26977,
#26978,#26979,#26980,#26981,#26982,#26983,#26984,#26985,#26986,#26987,#26988,
#26989,#26990,#26991,#26992,#26993,#26994,#26995,#26996,#26997,#26998,#26999,
#27000,#27001,#27002,#27003,#27004,#27005,#27006,#27007,#27008,#27009,#27010,
#27011,#27012,#27013,#27014,#27015,#27016,#27017,#27018,#27019,#27020,#27021,
#27022,#27023,#27024,#27025,#27026,#27027,#27028,#27029,#27030,#27031,#27032,
#27033,#27034,#27035,#27036,#27037,#27038,#27039,#27040,#27041,#27042,#27043,
#27044,#27045,#27046,#27047,#27048,#27049,#27050,#27051,#27052,#27053,#27054,
#27055,#27056,#27057,#27058,#27059,#27060,#27061,#27062,#27063,#27064,#27065,
#27066,#27067,#27068,#27069,#27070,#27071,#27072,#27073,#27074,#27075,#27076,
#27077,#27078,#27079,#27080,#27081,#27082,#27083,#27084,#27085,#27086,#27087,
#27088,#27089,#27090,#27091,#27092,#27093,#27094,#27095,#27096,#27097,#27098,
#27099,#27100,#27101,#27102,#27103,#27104,#27105,#27106,#27107,#27108,#27109,
#27110,#27111,#27112,#27113,#27114,#27115,#27116,#27117,#27118,#27119,#27120,
#27121,#27122,#27123,#27124,#27125,#27126),.UNSPECIFIED.,.F.,.F.,(4,3,3,
3,3,3,3,3,3,3,3,3,3,3,3,3,3,3,3,3,3,3,3,3,3,3,3,3,3,3,3,3,3,3,3,3,3,3,3,
3,3,3,3,3,3,3,3,3,3,3,3,3,3,3,3,3,3,3,3,3,3,3,3,3,3,3,3,3,3,3,3,3,3,4),
(78.539816339745,78.6328610561734,78.6468657231173,78.7347200961305,78.822556588302,
78.9103961954321,78.9982306507758,79.0860867015266,79.1457376582654,79.2335920312787,
79.3214285234505,79.4092681305805,79.4971025859242,79.5849586366751,79.6446095934135,
79.7324639664267,79.8203004585983,79.9081400657283,79.9959745210719,80.0838305718228,
80.1434815285617,80.231335901575,80.3191723937466,80.4070120008766,80.4948464562203,
80.5827025069712,80.6423534637098,80.730207836723,80.8180443288945,80.9058839360245,
80.9937183913681,81.081574442119,81.1412253988579,81.2290797718712,81.3169162640427,
81.4047558711728,81.4925903265164,81.5804463772674,81.640097334006,81.7279517070193,
81.8157881991909,81.9036278063209,81.9914622616646,82.0793183124155,82.1389692691542,
82.2268236421675,82.3146601343391,82.4024997414692,82.4903341968129,82.5781902475638,
82.6378412043023,82.7256955773155,82.8135320694871,82.901371676617,82.9892061319606,
83.0770621827114,83.1367131394504,83.2245675124637,83.3124040046352,83.4002436117652,
83.4880780671088,83.5759341178598,83.6355850745985,83.7234394476117,83.8112759397833,
83.8991155469133,83.9869500022568,84.0748060530077,84.1344570097467,84.2223107498068,
84.3101568702724,84.3979902799314,84.4858391601252,84.5719056092393),
 .UNSPECIFIED.);
#336=B_SPLINE_CURVE_WITH_KNOTS('',3,(#27127,#27128,#27129,#27130,#27131,
#27132,#27133,#27134,#27135,#27136),.UNSPECIFIED.,.F.,.F.,(4,2,2,2,4),(-6.19130099814293,
-6.14184388955133,-6.1229614278331,-6.1022946734106,-6.06757918107776),
 .UNSPECIFIED.);
#337=B_SPLINE_CURVE_WITH_KNOTS('',3,(#27137,#27138,#27139,#27140,#27141,
#27142,#27143,#27144,#27145,#27146,#27147,#27148,#27149,#27150,#27151,#27152,
#27153,#27154,#27155,#27156,#27157,#27158,#27159,#27160,#27161,#27162,#27163,
#27164,#27165,#27166,#27167,#27168,#27169,#27170,#27171,#27172,#27173,#27174,
#27175,#27176,#27177,#27178,#27179,#27180,#27181,#27182,#27183,#27184,#27185,
#27186,#27187,#27188,#27189,#27190,#27191,#27192,#27193,#27194,#27195,#27196,
#27197,#27198,#27199,#27200,#27201,#27202,#27203,#27204,#27205,#27206,#27207,
#27208,#27209,#27210,#27211,#27212,#27213,#27214,#27215,#27216,#27217,#27218,
#27219,#27220,#27221,#27222,#27223,#27224,#27225,#27226,#27227,#27228,#27229,
#27230,#27231,#27232,#27233,#27234,#27235,#27236,#27237,#27238,#27239,#27240,
#27241,#27242,#27243,#27244,#27245,#27246,#27247,#27248,#27249,#27250,#27251,
#27252,#27253,#27254,#27255,#27256,#27257,#27258,#27259,#27260,#27261,#27262,
#27263,#27264,#27265,#27266,#27267,#27268,#27269,#27270,#27271,#27272,#27273,
#27274,#27275,#27276,#27277,#27278,#27279,#27280,#27281,#27282,#27283,#27284,
#27285,#27286,#27287,#27288,#27289,#27290,#27291,#27292,#27293,#27294,#27295,
#27296,#27297,#27298,#27299,#27300,#27301,#27302,#27303,#27304,#27305,#27306,
#27307,#27308,#27309,#27310,#27311,#27312,#27313,#27314,#27315,#27316,#27317,
#27318,#27319,#27320,#27321,#27322,#27323,#27324,#27325,#27326,#27327,#27328,
#27329,#27330,#27331,#27332,#27333,#27334,#27335,#27336,#27337,#27338,#27339,
#27340,#27341,#27342,#27343,#27344,#27345,#27346,#27347,#27348,#27349,#27350,
#27351,#27352,#27353,#27354,#27355,#27356,#27357,#27358,#27359,#27360,#27361,
#27362,#27363,#27364,#27365,#27366,#27367,#27368,#27369,#27370,#27371,#27372,
#27373,#27374,#27375,#27376,#27377,#27378,#27379,#27380,#27381,#27382,#27383,
#27384,#27385,#27386,#27387,#27388,#27389,#27390,#27391,#27392,#27393,#27394,
#27395,#27396,#27397,#27398,#27399,#27400),.UNSPECIFIED.,.F.,.F.,(4,2,2,
2,2,2,2,2,2,2,2,2,2,2,2,2,2,2,2,2,2,2,2,2,2,2,2,2,2,2,2,2,2,2,2,2,2,2,2,
2,2,2,2,2,2,2,2,2,2,2,2,2,2,2,2,2,2,2,2,2,2,2,2,2,2,2,2,2,2,2,2,2,2,2,2,
2,2,2,2,2,2,2,2,2,2,2,2,2,2,2,2,2,2,2,2,2,2,2,2,2,2,2,2,2,2,2,2,2,2,2,2,
2,2,2,2,2,2,2,2,2,2,2,2,2,2,2,2,2,2,2,2,4),(-3.2192985515723,-3.18265944603559,
-3.14434517439237,-3.12271054243446,-3.11144339833662,-3.09560717917629,
-3.05018396632192,-3.04432698129421,-3.00837583280461,-2.98760755445556,
-2.96379769075988,-2.94941525188386,-2.90398453440576,-2.87976174903752,
-2.86901240027736,-2.8559810403335,-2.84772830370259,-2.82310650443899,
-2.76641397725233,-2.7450029092827,-2.7226646827579,-2.67325738302474,-2.63693130363473,
-2.62394592375348,-2.61146205320639,-2.60374130907329,-2.55828575630219,
-2.51923748099461,-2.50015962391689,-2.47818937511186,-2.45431887249412,
-2.4013812793087,-2.3831247563813,-2.37197059794452,-2.35341023317234,-2.32496180164914,
-2.27674090889921,-2.25486002931815,-2.2330793914816,-2.22092455711493,
-2.16324613987547,-2.14124574970439,-2.13069226849502,-2.11723575208084,
-2.10044553346399,-2.05544567550507,-2.02292895824591,-2.00235332073483,
-1.97760819146157,-1.94780682686908,-1.89809023372047,-1.88554351573609,
-1.87263054675197,-1.86449315278697,-1.84042789113114,-1.78934925871981,
-1.76624873104276,-1.74524285504112,-1.70438660485658,-1.65165088707617,
-1.63929599995273,-1.62615086713831,-1.60995173647188,-1.56896776463117,
-1.53333986424049,-1.51272195368063,-1.48920601434088,-1.46209356739356,
-1.41311463885229,-1.39746117381454,-1.3862224074529,-1.36354736859436,
-1.32111552123002,-1.28642196505976,-1.26572381443998,-1.24162980472358,
-1.19332593809121,-1.16059263856094,-1.14795916129151,-1.1351409264376,
-1.07657216580981,-1.04094837950543,-1.02019812166103,-0.996319517697121,
-0.9479470278713,-0.915387861894753,-0.90247232835115,-0.889927778921748,
-0.882147513265054,-0.859751541562816,-0.800584697187891,-0.77886312606304,
-0.766150728356179,-0.745790583365495,-0.713879139954891,-0.677791452497193,
-0.661005985749173,-0.658752994464158,-0.648140347314674,-0.647282893276361,
-0.646370680460327,-0.645371486243262,-0.644248344657781,-0.642956161481402,
-0.642648982649548,-0.642184574832556,-0.641472454273843,-0.640359738802267,
-0.63857978180825,-0.618825466318749,-0.552693910308086,-0.53523534812288,
-0.516484097181045,-0.495003566717608,-0.457359302300728,-0.453922556818062,
-0.422039456846717,-0.409704011905179,-0.3971574922677,-0.391530599966084,
-0.38488729847581,-0.354243021828057,-0.306479274633751,-0.291400620184979,
-0.283460049227869,-0.260608212341912,-0.234157658944324,-0.184731030556678,
-0.168621869564749,-0.158352893080881,-0.145998352350197,-0.123752409919132),
 .UNSPECIFIED.);
#338=B_SPLINE_CURVE_WITH_KNOTS('',3,(#27406,#27407,#27408,#27409,#27410,
#27411,#27412,#27413,#27414,#27415,#27416,#27417,#27418,#27419,#27420,#27421),
 .UNSPECIFIED.,.F.,.F.,(4,1,1,1,1,1,1,1,1,1,1,1,1,4),(84.8230016469245,
85.1322008800429,85.631072815191,86.1299447503392,86.6288166854873,87.1276886206354,
87.6265605557835,88.1254324909317,88.6243044260798,89.1231763612279,89.622048296376,
90.1209202315242,90.6197921666723,90.8551096506934),.UNSPECIFIED.);
#339=B_SPLINE_CURVE_WITH_KNOTS('',3,(#27422,#27423,#27424,#27425,#27426,
#27427,#27428,#27429,#27430,#27431),.UNSPECIFIED.,.F.,.F.,(4,3,3,4),(84.5719056092393,
84.6333289448948,84.7281652959096,84.8230016469245),.UNSPECIFIED.);
#340=B_SPLINE_CURVE_WITH_KNOTS('',3,(#27433,#27434,#27435,#27436,#27437,
#27438,#27439,#27440,#27441,#27442,#27443,#27444),.UNSPECIFIED.,.F.,.F.,
(4,2,2,2,2,4),(-0.123752409919132,-0.0930689444384096,-0.0582089112007299,
-0.0377177607519244,-0.0205407051112054,-4.23346110096705E-5),
 .UNSPECIFIED.);
#341=B_SPLINE_CURVE_WITH_KNOTS('',3,(#27445,#27446,#27447,#27448,#27449,
#27450,#27451,#27452,#27453,#27454,#27455,#27456,#27457,#27458,#27459,#27460),
 .UNSPECIFIED.,.F.,.F.,(4,1,1,1,1,1,1,1,1,1,1,1,1,4),(84.8230016469245,
84.9884465486181,85.4875827733086,85.9867189979992,86.4858552226897,86.9849914473802,
87.4841276720708,87.9832638967613,88.4824001214518,88.9815363461423,89.4806725708329,
89.9798087955234,90.4789450202139,90.855079291793),.UNSPECIFIED.);
#342=B_SPLINE_CURVE_WITH_KNOTS('',3,(#27466,#27467,#27468,#27469,#27470,
#27471,#27472,#27473,#27474,#27475,#27476,#27477,#27478,#27479,#27480,#27481,
#27482,#27483,#27484,#27485,#27486,#27487,#27488,#27489,#27490,#27491,#27492,
#27493,#27494,#27495,#27496,#27497,#27498,#27499,#27500,#27501,#27502,#27503,
#27504,#27505,#27506,#27507,#27508,#27509,#27510,#27511,#27512,#27513,#27514,
#27515,#27516,#27517,#27518,#27519,#27520,#27521,#27522,#27523,#27524,#27525,
#27526,#27527,#27528,#27529,#27530,#27531,#27532,#27533,#27534,#27535,#27536,
#27537,#27538,#27539,#27540,#27541,#27542,#27543,#27544,#27545,#27546,#27547,
#27548,#27549,#27550,#27551,#27552,#27553,#27554,#27555,#27556,#27557,#27558,
#27559,#27560,#27561,#27562,#27563,#27564,#27565,#27566,#27567,#27568,#27569,
#27570,#27571,#27572,#27573,#27574,#27575,#27576,#27577,#27578,#27579,#27580,
#27581,#27582,#27583,#27584,#27585,#27586,#27587,#27588,#27589,#27590,#27591,
#27592,#27593,#27594,#27595,#27596,#27597,#27598,#27599,#27600,#27601,#27602,
#27603,#27604,#27605,#27606,#27607,#27608,#27609,#27610,#27611,#27612,#27613,
#27614,#27615,#27616,#27617,#27618,#27619,#27620,#27621,#27622,#27623,#27624,
#27625,#27626,#27627,#27628,#27629,#27630,#27631,#27632,#27633,#27634,#27635,
#27636,#27637,#27638,#27639,#27640,#27641,#27642,#27643,#27644,#27645,#27646,
#27647,#27648,#27649,#27650,#27651,#27652,#27653,#27654,#27655,#27656,#27657,
#27658,#27659,#27660,#27661,#27662,#27663,#27664,#27665,#27666,#27667,#27668,
#27669,#27670,#27671,#27672,#27673,#27674,#27675,#27676,#27677,#27678,#27679,
#27680,#27681,#27682,#27683,#27684,#27685,#27686,#27687,#27688,#27689,#27690,
#27691,#27692,#27693,#27694,#27695,#27696,#27697,#27698,#27699,#27700,#27701,
#27702,#27703),.UNSPECIFIED.,.F.,.F.,(4,2,2,2,2,2,2,2,2,2,2,2,2,2,2,2,2,
2,2,2,2,2,2,2,2,2,2,2,2,2,2,2,2,2,2,2,2,2,2,2,2,2,2,2,2,2,2,2,2,2,2,2,2,
2,2,2,2,2,2,2,2,2,2,2,2,2,2,2,2,2,2,2,2,2,2,2,2,2,2,2,2,2,2,2,2,2,2,2,2,
2,2,2,2,2,2,2,2,2,2,2,2,2,2,2,2,2,2,2,2,2,2,2,2,2,2,2,2,2,4),(-2.97188390835979,
-2.95930360230679,-2.94813049352868,-2.92654700709351,-2.88824968232717,
-2.85094146776425,-2.83207769380161,-2.81028046180207,-2.78659016540223,
-2.7342946618611,-2.71563441099786,-2.70458798215227,-2.68695057534491,
-2.67352131896951,-2.6192975620724,-2.59420744323309,-2.57409993213815,
-2.54382795260748,-2.4984174132146,-2.47427087862044,-2.46361108093319,
-2.45077211713454,-2.44267676202592,-2.41873573334499,-2.36029330763336,
-2.34127912176928,-2.31971823122944,-2.3077041938349,-2.25312819013689,
-2.22918423253904,-2.2183268607472,-2.20581457084965,-2.19803439701932,
-2.15146502875884,-2.11374129623816,-2.09485613369102,-2.07309568903009,
-2.01988048900073,-2.01717711750618,-1.98453337403748,-1.97213593235675,
-1.95935497884516,-1.95131585634724,-1.90513800086238,-1.86782883109767,
-1.84896506190972,-1.82716795845727,-1.80347787548065,-1.7511836837004,
-1.73252247172757,-1.72147605415282,-1.70383956240128,-1.69041146482386,
-1.63618833630999,-1.61109701791401,-1.59098968567115,-1.56072033362341,
-1.51531892825007,-1.49117296105698,-1.48050940005662,-1.46767744606798,
-1.45958888267165,-1.43568024937039,-1.37840311223537,-1.35705864281533,
-1.33514458589156,-1.31121114205248,-1.2596315246863,-1.24096875896605,
-1.22992235088225,-1.2122873106871,-1.19886105801143,-1.1446388947538,-1.11954563582482,
-1.09943857432114,-1.0691734044744,-1.02378657882265,-0.999641897630113,
-0.98897218144264,-0.976151597421332,-0.968074049488683,-0.944217906727671,
-0.885986113094425,-0.866909016037012,-0.847924122848715,-0.838828430897599,
-0.811976487158419,-0.762174904402619,-0.747083888625468,-0.736041390284051,
-0.72384034197845,-0.712532820093758,-0.668463932200259,-0.63535328159074,
-0.615290171385401,-0.596320400449478,-0.547225528508128,-0.511291014668111,
-0.49846522688991,-0.488471446920141,-0.475344302630777,-0.430194801231896,
-0.393107848696171,-0.374254213376987,-0.355334441256989,-0.291948221686628,
-0.265012553372072,-0.252374515124856,-0.242470545133809,-0.229222440880817,
-0.186963697760637,-0.167084065608167,-0.139497337172782,-0.120655190704037,
-0.101368977746664,-0.0546587056616307,-0.0192581144472614,-0.0087590194227128,
-7.99011461200493E-5),.UNSPECIFIED.);
#343=B_SPLINE_CURVE_WITH_KNOTS('',3,(#27704,#27705,#27706,#27707),
 .UNSPECIFIED.,.F.,.F.,(4,4),(90.8551096506934,91.1061869363603),
 .UNSPECIFIED.);
#344=B_SPLINE_CURVE_WITH_KNOTS('',3,(#27709,#27710,#27711,#27712,#27713),
 .UNSPECIFIED.,.F.,.F.,(4,1,4),(90.855079291793,90.9780812449044,91.106186943595),
 .UNSPECIFIED.);
#345=B_SPLINE_CURVE_WITH_KNOTS('',3,(#27714,#27715,#27716,#27717,#27718,
#27719,#27720,#27721,#27722,#27723,#27724,#27725,#27726,#27727,#27728,#27729,
#27730,#27731,#27732,#27733,#27734,#27735,#27736,#27737,#27738,#27739,#27740,
#27741,#27742,#27743,#27744,#27745,#27746,#27747,#27748,#27749,#27750,#27751,
#27752,#27753,#27754,#27755,#27756,#27757,#27758,#27759,#27760,#27761,#27762,
#27763,#27764,#27765,#27766,#27767,#27768,#27769,#27770,#27771,#27772,#27773,
#27774,#27775,#27776,#27777,#27778,#27779,#27780,#27781,#27782,#27783,#27784,
#27785,#27786,#27787,#27788,#27789,#27790,#27791,#27792,#27793,#27794,#27795,
#27796,#27797,#27798,#27799,#27800,#27801,#27802,#27803,#27804,#27805,#27806,
#27807,#27808,#27809,#27810,#27811,#27812,#27813,#27814,#27815,#27816,#27817,
#27818,#27819,#27820,#27821,#27822,#27823,#27824,#27825,#27826,#27827,#27828,
#27829,#27830,#27831,#27832,#27833,#27834,#27835,#27836,#27837,#27838,#27839,
#27840,#27841,#27842,#27843,#27844,#27845,#27846,#27847,#27848,#27849,#27850,
#27851,#27852,#27853,#27854,#27855,#27856,#27857,#27858,#27859,#27860,#27861,
#27862,#27863,#27864,#27865,#27866,#27867,#27868,#27869,#27870,#27871,#27872,
#27873,#27874,#27875,#27876,#27877,#27878,#27879,#27880,#27881,#27882,#27883,
#27884,#27885,#27886,#27887,#27888,#27889,#27890,#27891,#27892,#27893,#27894,
#27895,#27896,#27897,#27898,#27899,#27900,#27901,#27902,#27903,#27904,#27905,
#27906,#27907,#27908,#27909,#27910,#27911,#27912,#27913,#27914,#27915,#27916,
#27917,#27918,#27919,#27920,#27921,#27922,#27923,#27924,#27925,#27926,#27927,
#27928,#27929,#27930,#27931,#27932,#27933),.UNSPECIFIED.,.F.,.F.,(4,3,3,
3,3,3,3,3,3,3,3,3,3,3,3,3,3,3,3,3,3,3,3,3,3,3,3,3,3,3,3,3,3,3,3,3,3,3,3,
3,3,3,3,3,3,3,3,3,3,3,3,3,3,3,3,3,3,3,3,3,3,3,3,3,3,3,3,3,3,3,3,3,3,4),
(91.1061869541041,91.1937659933166,91.2813481576857,91.3689282889393,91.4565282400459,
91.477217469595,91.5650703351689,91.6529052949637,91.7407433708428,91.8285762824558,
91.9164308439581,91.9763536942855,92.0642065598592,92.1520415196537,92.2398795955327,
92.3277125071459,92.4155670686481,92.475489918976,92.5633427845498,92.6511777443445,
92.7390158202237,92.8268487318367,92.914703293339,92.9746261436665,93.0624790092402,
93.1503139690347,93.2381520449139,93.3259849565268,93.4138395180291,93.4737623683571,
93.561615233931,93.6494501937261,93.7372882696053,93.8251211812183,93.9129757427206,
93.9728985930476,94.0607514586212,94.1485864184154,94.2364244942945,94.3242574059074,
94.4121119674096,94.4720348177381,94.559887683312,94.6477226431064,94.7355607189857,
94.8233936305985,94.9112481921007,94.9711710424286,95.0590239080024,95.1468588677968,
95.2346969436761,95.3225298552889,95.4103844167912,95.4703072671192,95.5581601326931,
95.6459950924875,95.7338331683666,95.8216660799797,95.9095206414821,95.9694434918097,
96.0572963573838,96.1451313171785,96.2329693930575,96.3208023046708,96.4086568661731,
96.4685797165002,96.5564325820741,96.6442675418685,96.7321056177478,96.8199385293601,
96.9077930908624,96.9677159411908,97.0552213902458,97.1382969843455),
 .UNSPECIFIED.);
#346=B_SPLINE_CURVE_WITH_KNOTS('',3,(#27938,#27939,#27940,#27941,#27942,
#27943,#27944,#27945,#27946,#27947,#27948,#27949,#27950,#27951,#27952,#27953,
#27954,#27955,#27956,#27957,#27958,#27959,#27960,#27961,#27962,#27963,#27964,
#27965,#27966,#27967,#27968,#27969,#27970,#27971,#27972,#27973,#27974,#27975,
#27976,#27977,#27978,#27979,#27980,#27981,#27982,#27983,#27984,#27985,#27986,
#27987,#27988,#27989,#27990,#27991,#27992,#27993,#27994,#27995,#27996,#27997,
#27998,#27999,#28000,#28001,#28002,#28003,#28004,#28005,#28006,#28007,#28008,
#28009,#28010,#28011,#28012,#28013,#28014,#28015,#28016,#28017,#28018,#28019,
#28020,#28021,#28022,#28023,#28024,#28025,#28026,#28027,#28028,#28029,#28030,
#28031,#28032,#28033,#28034,#28035,#28036,#28037,#28038,#28039,#28040,#28041,
#28042,#28043,#28044,#28045,#28046,#28047,#28048,#28049,#28050,#28051,#28052,
#28053,#28054,#28055,#28056,#28057,#28058,#28059,#28060,#28061,#28062,#28063,
#28064,#28065,#28066,#28067,#28068,#28069,#28070,#28071,#28072,#28073,#28074,
#28075,#28076,#28077,#28078,#28079,#28080,#28081,#28082,#28083,#28084,#28085,
#28086,#28087,#28088,#28089,#28090,#28091,#28092,#28093,#28094,#28095,#28096,
#28097,#28098,#28099,#28100,#28101,#28102,#28103,#28104,#28105,#28106,#28107,
#28108,#28109,#28110,#28111,#28112,#28113,#28114,#28115,#28116,#28117,#28118,
#28119,#28120,#28121,#28122,#28123,#28124,#28125,#28126,#28127,#28128,#28129,
#28130,#28131,#28132,#28133,#28134,#28135,#28136,#28137,#28138,#28139,#28140,
#28141,#28142,#28143,#28144,#28145,#28146,#28147,#28148,#28149,#28150,#28151,
#28152,#28153,#28154,#28155,#28156,#28157,#28158,#28159,#28160,#28161,#28162,
#28163,#28164,#28165,#28166,#28167,#28168,#28169,#28170,#28171,#28172,#28173,
#28174,#28175,#28176,#28177,#28178,#28179,#28180,#28181,#28182,#28183),
 .UNSPECIFIED.,.F.,.F.,(4,2,2,2,2,2,2,2,2,2,2,2,2,2,2,2,2,2,2,2,2,2,2,2,
2,2,2,2,2,2,2,2,2,2,2,2,2,2,2,2,2,2,2,2,2,2,2,2,2,2,2,2,2,2,2,2,2,2,2,2,
2,2,2,2,2,2,2,2,2,2,2,2,2,2,2,2,2,2,2,2,2,2,2,2,2,2,2,2,2,2,2,2,2,2,2,2,
2,2,2,2,2,2,2,2,2,2,2,2,2,2,2,2,2,2,2,2,2,2,2,2,2,2,4),(-6.06739611659123,
-6.04890634739659,-6.02918138480762,-6.00796119668724,-5.95506196377217,
-5.9281994073552,-5.91055613045296,-5.9062807363049,-5.89454214084383,-5.83796854963403,
-5.7995941317827,-5.78303501833826,-5.76172088759372,-5.69878898354961,
-5.67791540045163,-5.66287162905995,-5.65669994687286,-5.65259798077859,
-5.64823381999523,-5.59912663531025,-5.56848191341442,-5.56008297219719,
-5.55308141228642,-5.53547225595711,-5.51362860225442,-5.46757029749411,
-5.4381626263111,-5.42413864141611,-5.41845996335461,-5.40876425159925,
-5.39237654472097,-5.34264650304186,-5.31670432465222,-5.31405387462264,
-5.31187344235433,-5.30994754658458,-5.30810623452789,-5.28727060032299,
-5.26449143353979,-5.21870031346397,-5.18004364153831,-5.16749269679253,
-5.15666144336242,-5.10735244277498,-5.07681993232706,-5.0518315502198,
-5.03152038230495,-5.0007795558325,-4.95370065078756,-4.94204442086742,
-4.93423933264814,-4.92170138772236,-4.90907275024535,-4.85809638847423,
-4.82553299757179,-4.80253449665306,-4.78202716917478,-4.71367657308658,
-4.69961499356507,-4.68149683208091,-4.67045502268247,-4.65231329247252,
-4.5994060437416,-4.57563740288442,-4.55380253563748,-4.5323942329941,-4.49375889420732,
-4.45812472260172,-4.44286722896336,-4.4302566283844,-4.41770105224706,
-4.37747286092775,-4.32824441071514,-4.30678999234457,-4.28769718524396,
-4.25442037305272,-4.21417271423322,-4.19813566772727,-4.18510505632296,
-4.17454317604071,-4.15131022502166,-4.09555575100564,-4.08341969925314,
-4.0617487929656,-4.04280887834227,-4.00394192561131,-3.96241396068146,
-3.94422729829558,-3.93318544923321,-3.91511182561434,-3.86212235509494,
-3.83834316473064,-3.81650324081526,-3.79766396173923,-3.76082805603957,
-3.7064259906953,-3.69346046251259,-3.68121660739566,-3.64990939718142,
-3.64578850930668,-3.6060966288402,-3.57940795269051,-3.56120830499061,
-3.53549996849126,-3.46001428467461,-3.44729891042931,-3.43484245441477,
-3.39266217414502,-3.34436394152978,-3.32307172655708,-3.30108915425806,
-3.2633031222042,-3.22875502504213,-3.2082301723572,-3.19811308120898,-3.18288470572753,
-3.1343316752737,-3.09558651517567,-3.07503671030317,-3.05215162362301,
-3.02031166947022,-2.97478411742481,-2.97188390835979),.UNSPECIFIED.);
#347=B_SPLINE_CURVE_WITH_KNOTS('',3,(#28185,#28186,#28187,#28188,#28189,
#28190,#28191,#28192,#28193,#28194),.UNSPECIFIED.,.F.,.F.,(4,3,3,4),(97.1382969843455,
97.2257767656916,97.3132734200704,97.3893722574151),.UNSPECIFIED.);
#348=B_SPLINE_CURVE_WITH_KNOTS('',3,(#28195,#28196,#28197,#28198,#28199,
#28200,#28201,#28202,#28203,#28204,#28205,#28206,#28207,#28208,#28209,#28210),
 .UNSPECIFIED.,.F.,.F.,(4,1,1,1,1,1,1,1,1,1,1,1,1,4),(97.3893722612837,
97.4668521658813,97.9659883905718,98.4651246152623,98.9642608399529,99.4633970646434,
99.9625332893339,100.461669514024,100.960805738715,101.459941963405,101.959078188096,
102.458214412787,102.957350637477,103.421463986725),.UNSPECIFIED.);
#349=B_SPLINE_CURVE_WITH_KNOTS('',3,(#28216,#28217,#28218,#28219,#28220,
#28221,#28222,#28223,#28224,#28225,#28226,#28227,#28228,#28229,#28230,#28231,
#28232,#28233,#28234,#28235,#28236,#28237,#28238,#28239,#28240,#28241,#28242,
#28243,#28244,#28245,#28246,#28247,#28248,#28249,#28250,#28251,#28252,#28253,
#28254,#28255,#28256,#28257,#28258,#28259,#28260,#28261,#28262,#28263,#28264,
#28265,#28266,#28267,#28268,#28269,#28270,#28271,#28272,#28273,#28274,#28275,
#28276,#28277,#28278,#28279,#28280,#28281,#28282,#28283,#28284,#28285,#28286,
#28287,#28288,#28289,#28290,#28291,#28292,#28293,#28294,#28295,#28296,#28297,
#28298,#28299,#28300,#28301,#28302,#28303,#28304,#28305,#28306,#28307,#28308,
#28309,#28310,#28311,#28312,#28313,#28314,#28315,#28316,#28317,#28318,#28319,
#28320,#28321,#28322,#28323,#28324,#28325,#28326,#28327,#28328,#28329,#28330,
#28331,#28332,#28333,#28334,#28335,#28336,#28337,#28338,#28339,#28340,#28341,
#28342,#28343,#28344,#28345,#28346,#28347,#28348,#28349,#28350,#28351,#28352,
#28353,#28354,#28355,#28356,#28357,#28358,#28359,#28360,#28361,#28362,#28363,
#28364,#28365,#28366,#28367,#28368,#28369,#28370,#28371,#28372,#28373,#28374,
#28375,#28376,#28377,#28378,#28379,#28380,#28381,#28382,#28383,#28384,#28385,
#28386,#28387,#28388,#28389,#28390,#28391,#28392,#28393,#28394,#28395,#28396,
#28397,#28398,#28399,#28400,#28401,#28402,#28403,#28404,#28405,#28406,#28407,
#28408,#28409,#28410,#28411,#28412,#28413,#28414,#28415,#28416,#28417,#28418,
#28419,#28420,#28421,#28422,#28423,#28424,#28425,#28426,#28427,#28428,#28429,
#28430,#28431,#28432,#28433,#28434,#28435,#28436,#28437,#28438,#28439,#28440,
#28441,#28442,#28443,#28444,#28445,#28446,#28447,#28448,#28449,#28450,#28451),
 .UNSPECIFIED.,.F.,.F.,(4,2,2,2,2,2,2,2,2,2,2,2,2,2,2,2,2,2,2,2,2,2,2,2,
2,2,2,2,2,2,2,2,2,2,2,2,2,2,2,2,2,2,2,2,2,2,2,2,2,2,2,2,2,2,2,2,2,2,2,2,
2,2,2,2,2,2,2,2,2,2,2,2,2,2,2,2,2,2,2,2,2,2,2,2,2,2,2,2,2,2,2,2,2,2,2,2,
2,2,2,2,2,2,2,2,2,2,2,2,2,2,2,2,2,2,2,2,2,4),(-2.97195104590692,-2.96785731741696,
-2.92217885664269,-2.90936567333568,-2.89699615966277,-2.88935476710183,
-2.84416880408123,-2.82633349817458,-2.7976174272583,-2.77738972113305,
-2.75124194836679,-2.69474988104159,-2.67275371403184,-2.66228603455495,
-2.64904430325233,-2.6326094660691,-2.58975433302553,-2.55560533913252,
-2.53510160348009,-2.51128689789865,-2.46322801939443,-2.42809306775177,
-2.41733468308247,-2.40466748949289,-2.38930635285144,-2.35309235177817,
-2.31337370536685,-2.29442627164094,-2.27276611417383,-2.22958865696618,
-2.18956041580427,-2.17461787750089,-2.16328164650938,-2.13921313100205,
-2.08610587199597,-2.06144679348156,-2.04116654530749,-2.01585568527845,
-1.95838610543814,-1.93557379016381,-1.92506922811594,-1.91191309731386,
-1.89564032229228,-1.85386995916075,-1.8219345708956,-1.80296702805452,
-1.78133735396513,-1.76924711468633,-1.71115127327577,-1.68923066226832,
-1.67785911475009,-1.66354145407655,-1.61685984184392,-1.57530039887851,
-1.55647003830275,-1.5346128076183,-1.510797731504,-1.4575362420338,-1.43968161753604,
-1.42863823220506,-1.41022095978168,-1.3820622104627,-1.33347822731307,
-1.3117702180792,-1.29024962363137,-1.24226814993072,-1.20093905597605,
-1.18843740533266,-1.17577030489421,-1.16040936699153,-1.124196657836,-1.08447356358303,
-1.06552644824461,-1.0438656239945,-1.00068136685562,-0.960750293559231,
-0.945763688633204,-0.934437899479715,-0.91052378709959,-0.862241766807108,
-0.832374395201497,-0.81286113588637,-0.79127147505588,-0.763678287012345,
-0.707459976144883,-0.695686116009359,-0.684387070609555,-0.683232880624469,
-0.681867153745732,-0.664640140195931,-0.615990580307078,-0.586381523641675,
-0.570730661414335,-0.548681768559753,-0.523265479697681,-0.469984555741397,
-0.454593127443027,-0.444132045810674,-0.441361870022094,-0.438892899662171,
-0.435173421070681,-0.417129760065319,-0.361528325738389,-0.336380334968567,
-0.328730230085166,-0.325211210846139,-0.323035602891817,-0.320473782055981,
-0.295654411923943,-0.26462716457408,-0.217428748493838,-0.205073931066454,
-0.192832984744859,-0.119422015026088,-0.0949473551364795,-0.075450854731309,
-0.0563330778625723,-7.60666707596163E-5),.UNSPECIFIED.);
#350=B_SPLINE_CURVE_WITH_KNOTS('',3,(#28452,#28453,#28454,#28455,#28456,
#28457,#28458,#28459,#28460,#28461,#28462,#28463,#28464,#28465),
 .UNSPECIFIED.,.F.,.F.,(4,2,2,2,2,2,4),(-6.19108034638175,-6.17183981108263,
-6.16031491317487,-6.15046655821583,-6.13776449339168,-6.09803741160187,
-6.06739611659123),.UNSPECIFIED.);
#351=B_SPLINE_CURVE_WITH_KNOTS('',3,(#28467,#28468,#28469,#28470,#28471),
 .UNSPECIFIED.,.F.,.F.,(4,1,4),(103.421463986725,103.456486862168,103.672557546372),
 .UNSPECIFIED.);
#352=B_SPLINE_CURVE_WITH_KNOTS('',3,(#28472,#28473,#28474,#28475,#28476,
#28477,#28478,#28479,#28480,#28481,#28482,#28483,#28484,#28485,#28486,#28487,
#28488,#28489,#28490,#28491,#28492,#28493,#28494,#28495,#28496,#28497,#28498,
#28499,#28500,#28501,#28502,#28503,#28504,#28505,#28506,#28507,#28508,#28509,
#28510,#28511,#28512,#28513,#28514,#28515,#28516,#28517,#28518,#28519,#28520,
#28521,#28522,#28523,#28524,#28525,#28526,#28527,#28528,#28529,#28530,#28531,
#28532,#28533,#28534,#28535,#28536,#28537,#28538,#28539,#28540,#28541,#28542,
#28543,#28544,#28545,#28546,#28547,#28548,#28549,#28550,#28551,#28552,#28553,
#28554,#28555,#28556,#28557,#28558,#28559,#28560,#28561,#28562,#28563,#28564,
#28565,#28566,#28567,#28568,#28569,#28570,#28571,#28572,#28573,#28574,#28575,
#28576,#28577,#28578,#28579,#28580,#28581,#28582,#28583,#28584,#28585,#28586,
#28587,#28588,#28589,#28590,#28591,#28592,#28593,#28594,#28595,#28596,#28597,
#28598,#28599,#28600,#28601,#28602,#28603,#28604,#28605,#28606,#28607,#28608,
#28609,#28610,#28611,#28612,#28613,#28614,#28615,#28616,#28617,#28618,#28619,
#28620,#28621,#28622,#28623,#28624,#28625,#28626,#28627,#28628,#28629,#28630,
#28631,#28632,#28633,#28634,#28635,#28636,#28637,#28638,#28639,#28640,#28641,
#28642,#28643,#28644,#28645,#28646,#28647,#28648,#28649,#28650,#28651,#28652,
#28653,#28654,#28655,#28656,#28657,#28658,#28659,#28660,#28661,#28662,#28663,
#28664,#28665,#28666,#28667,#28668,#28669,#28670,#28671,#28672,#28673,#28674,
#28675,#28676,#28677,#28678,#28679,#28680,#28681,#28682,#28683,#28684,#28685,
#28686,#28687,#28688,#28689,#28690,#28691,#28692,#28693,#28694,#28695,#28696,
#28697,#28698,#28699,#28700,#28701,#28702,#28703,#28704,#28705,#28706,#28707,
#28708,#28709,#28710,#28711,#28712,#28713,#28714,#28715,#28716,#28717),
 .UNSPECIFIED.,.F.,.F.,(4,2,2,2,2,2,2,2,2,2,2,2,2,2,2,2,2,2,2,2,2,2,2,2,
2,2,2,2,2,2,2,2,2,2,2,2,2,2,2,2,2,2,2,2,2,2,2,2,2,2,2,2,2,2,2,2,2,2,2,2,
2,2,2,2,2,2,2,2,2,2,2,2,2,2,2,2,2,2,2,2,2,2,2,2,2,2,2,2,2,2,2,2,2,2,2,2,
2,2,2,2,2,2,2,2,2,2,2,2,2,2,2,2,2,2,2,2,2,2,2,2,2,2,4),(-6.19125288673404,
-6.17508219709553,-6.15753828259376,-6.11890984406139,-6.06250600267116,
-6.0524853606948,-6.04017426316179,-6.01332573894149,-5.97047335452146,
-5.94807557503419,-5.92894927198427,-5.90931059639689,-5.84407907151587,
-5.82109036638719,-5.81587510621001,-5.80596728296801,-5.79507843430614,
-5.75653171497579,-5.72958245957422,-5.70558689319716,-5.68651984516126,
-5.66705175205571,-5.6641559080366,-5.60425624187656,-5.58082308107648,
-5.57594514987642,-5.57302517221989,-5.57101555516809,-5.56957655694856,
-5.5595755231996,-5.54659016163239,-5.51026850910374,-5.47416556457379,
-5.45297783343695,-5.43347707129468,-5.41558498912886,-5.35044439733363,
-5.33122320336565,-5.3295909586851,-5.32865538683616,-5.32811778636156,
-5.32780797684332,-5.32654555762053,-5.32551152573869,-5.32465588809124,
-5.31465419817859,-5.30229036980523,-5.25735975327803,-5.2122888585239,
-5.19060495819653,-5.16861900165768,-5.12240154924134,-5.08040741364554,
-5.06785874457934,-5.05494799488295,-5.0223860941896,-4.97401732211412,
-4.95013675861123,-4.92938711638593,-4.89494423688343,-4.85265005010578,
-4.83000771555363,-4.8187711618381,-4.80310566556307,-4.75411942988798,
-4.72702283520463,-4.70351428385425,-4.68289430727978,-4.64723106888212,
-4.60628148935744,-4.59008741573791,-4.57694516150772,-4.56458820386378,
-4.51955815990319,-4.47542462339307,-4.45354349280265,-4.43441048738455,
-4.38606085447809,-4.35572649014296,-4.33650430271747,-4.32534082603624,
-4.30766550428407,-4.25402043504048,-4.23006041690325,-4.20804738425489,
-4.18899481938808,-4.14921542231969,-4.10398524131171,-4.08813957479584,
-4.07682472514551,-4.05953706342537,-4.00896908886919,-3.98471358475004,
-3.96255920837257,-3.94358332940043,-3.90675480382874,-3.85213066297697,
-3.83908227614756,-3.8283418059308,-3.80411735082831,-3.7586690931932,-3.74428449282565,
-3.72047259794651,-3.69970478302615,-3.66376438673982,-3.62269242749822,
-3.60647926546033,-3.59332682923647,-3.58097747450412,-3.54856941972768,
-3.54559334511914,-3.49329007397899,-3.47103271320139,-3.44956483935213,
-3.39195886652383,-3.36802134121612,-3.35991063287445,-3.34702523428542,
-3.33445369996295,-3.29310435540861,-3.24485406110885,-3.22320627505701,
-3.21940741207938),.UNSPECIFIED.);
#353=B_SPLINE_CURVE_WITH_KNOTS('',3,(#28722,#28723,#28724,#28725,#28726,
#28727,#28728,#28729,#28730,#28731,#28732,#28733,#28734,#28735,#28736,#28737,
#28738,#28739,#28740,#28741,#28742,#28743,#28744,#28745,#28746,#28747,#28748,
#28749,#28750,#28751,#28752,#28753,#28754,#28755,#28756,#28757,#28758,#28759,
#28760,#28761,#28762,#28763,#28764,#28765,#28766,#28767,#28768,#28769,#28770,
#28771,#28772,#28773,#28774,#28775,#28776,#28777,#28778,#28779,#28780,#28781,
#28782,#28783,#28784,#28785,#28786,#28787,#28788,#28789,#28790,#28791,#28792,
#28793,#28794,#28795,#28796,#28797,#28798,#28799,#28800,#28801,#28802,#28803,
#28804,#28805,#28806,#28807,#28808,#28809,#28810,#28811,#28812,#28813,#28814,
#28815,#28816,#28817,#28818,#28819,#28820,#28821,#28822,#28823,#28824,#28825,
#28826,#28827,#28828,#28829,#28830,#28831,#28832,#28833,#28834,#28835,#28836,
#28837,#28838,#28839,#28840,#28841,#28842,#28843,#28844,#28845,#28846,#28847,
#28848,#28849,#28850,#28851,#28852,#28853,#28854,#28855,#28856,#28857,#28858,
#28859,#28860,#28861,#28862,#28863,#28864,#28865,#28866,#28867,#28868,#28869,
#28870,#28871,#28872,#28873,#28874,#28875,#28876,#28877,#28878,#28879,#28880,
#28881,#28882,#28883,#28884,#28885,#28886,#28887,#28888,#28889,#28890,#28891,
#28892,#28893,#28894,#28895,#28896,#28897,#28898,#28899,#28900,#28901,#28902,
#28903,#28904,#28905,#28906,#28907,#28908,#28909,#28910,#28911,#28912,#28913,
#28914,#28915,#28916,#28917,#28918,#28919,#28920,#28921,#28922,#28923,#28924,
#28925,#28926,#28927,#28928,#28929,#28930,#28931,#28932,#28933,#28934,#28935,
#28936,#28937,#28938,#28939,#28940,#28941,#28942,#28943,#28944,#28945,#28946,
#28947,#28948,#28949,#28950,#28951,#28952,#28953,#28954,#28955,#28956,#28957,
#28958,#28959,#28960,#28961),.UNSPECIFIED.,.F.,.F.,(4,2,2,2,2,2,2,2,2,2,
2,2,2,2,2,2,2,2,2,2,2,2,2,2,2,2,2,2,2,2,2,2,2,2,2,2,2,2,2,2,2,2,2,2,2,2,
2,2,2,2,2,2,2,2,2,2,2,2,2,2,2,2,2,2,2,2,2,2,2,2,2,2,2,2,2,2,2,2,2,2,2,2,
2,2,2,2,2,2,2,2,2,2,2,2,2,2,2,2,2,2,2,2,2,2,2,2,2,2,2,2,2,2,2,2,2,2,2,2,
2,4),(-6.06743986436456,-6.05146266686438,-6.0170766699814,-5.99084287541892,
-5.97507687341059,-5.95074837268195,-5.8929187530285,-5.87463693518481,
-5.86344954632942,-5.85855813820818,-5.8461204240607,-5.7970592585569,-5.76703887105114,
-5.7427810693363,-5.72341768441375,-5.69487220762185,-5.645197661881,-5.62784180292691,
-5.61429260539229,-5.60778130290437,-5.59112163908842,-5.54146782770256,
-5.51568819018526,-5.5071799204263,-5.4895290323691,-5.4678741999934,-5.41239384283465,
-5.38824717806325,-5.37545860914837,-5.36723691164706,-5.35660471760888,
-5.33278319787387,-5.32061964495729,-5.27250869023555,-5.24885362716181,
-5.2283114013168,-5.19350239543318,-5.15138697292266,-5.13506185151351,
-5.12187822882361,-5.1113858862278,-5.08865910725165,-5.03202786703808,
-5.01990971238666,-4.99825483855614,-4.9793041181001,-4.93913632900284,
-4.90324785383206,-4.88794451549379,-4.87530890994602,-4.86277733620302,
-4.82205159650951,-4.77315900980552,-4.75172577616791,-4.72991981159943,
-4.67916751260443,-4.64148640859403,-4.62910999337595,-4.6163049389692,
-4.57927154320596,-4.54353448850621,-4.51643130035729,-4.49622539640922,
-4.46868052514976,-4.44871989026378,-4.40643226541081,-4.38883545317932,
-4.37778823478465,-4.35908074563864,-4.30684418683341,-4.28316228806938,
-4.26136893995054,-4.24250292108282,-4.2051415728905,-4.15898680497175,
-4.15095776999203,-4.13818734348755,-4.12578054895554,-4.08271636562276,
-4.03613866044279,-4.01463791746702,-3.99290855769124,-3.94279694223018,
-3.91563756117052,-3.89758991726223,-3.8865478433578,-3.86833414291467,
-3.81551251706288,-3.79175467510695,-3.76992485541263,-3.75107950282549,
-3.71414646890209,-3.66884927313065,-3.6513996393683,-3.64034890417972,
-3.62146488716467,-3.58915375469089,-3.54546932724234,-3.52376446640606,
-3.50224119236757,-3.4495260603246,-3.4234128377245,-3.40576488281478,-3.39471862304028,
-3.37607046366351,-3.32376422005898,-3.30007316990067,-3.27827539637536,
-3.25941182166347,-3.22211370384445,-3.17592639552706,-3.16788422257047,
-3.1551002096396,-3.14270532815845,-3.09565991500632,-3.05150376830842,
-3.03241680025527,-3.01095404856947,-2.99904967789612,-2.97195104590692),
 .UNSPECIFIED.);
#354=B_SPLINE_CURVE_WITH_KNOTS('',3,(#28962,#28963,#28964,#28965,#28966,
#28967,#28968,#28969,#28970,#28971,#28972,#28973,#28974,#28975,#28976,#28977,
#28978,#28979,#28980,#28981,#28982,#28983,#28984,#28985,#28986,#28987,#28988,
#28989,#28990,#28991,#28992,#28993,#28994,#28995,#28996,#28997,#28998,#28999,
#29000,#29001,#29002,#29003,#29004,#29005,#29006,#29007,#29008,#29009,#29010,
#29011,#29012,#29013,#29014,#29015,#29016,#29017,#29018,#29019,#29020,#29021,
#29022,#29023,#29024,#29025,#29026,#29027,#29028,#29029,#29030,#29031,#29032,
#29033,#29034,#29035,#29036,#29037,#29038,#29039,#29040,#29041,#29042,#29043,
#29044,#29045,#29046,#29047,#29048,#29049,#29050,#29051,#29052,#29053,#29054,
#29055,#29056,#29057,#29058,#29059,#29060,#29061,#29062,#29063,#29064,#29065,
#29066,#29067,#29068,#29069,#29070,#29071,#29072,#29073,#29074,#29075,#29076,
#29077,#29078,#29079,#29080,#29081,#29082,#29083,#29084,#29085,#29086,#29087,
#29088,#29089,#29090,#29091,#29092,#29093,#29094,#29095,#29096,#29097,#29098,
#29099,#29100,#29101,#29102,#29103,#29104,#29105,#29106,#29107,#29108,#29109,
#29110,#29111,#29112,#29113,#29114,#29115,#29116,#29117,#29118,#29119,#29120,
#29121,#29122,#29123,#29124,#29125,#29126,#29127,#29128,#29129,#29130,#29131,
#29132,#29133,#29134,#29135,#29136,#29137,#29138,#29139,#29140,#29141,#29142,
#29143,#29144,#29145,#29146,#29147,#29148,#29149,#29150,#29151,#29152,#29153,
#29154,#29155,#29156,#29157,#29158,#29159,#29160,#29161,#29162,#29163,#29164,
#29165,#29166,#29167,#29168,#29169,#29170,#29171,#29172,#29173,#29174,#29175,
#29176,#29177,#29178,#29179,#29180,#29181,#29182,#29183,#29184,#29185,#29186,
#29187,#29188,#29189,#29190,#29191,#29192,#29193,#29194,#29195,#29196,#29197,
#29198,#29199,#29200,#29201,#29202,#29203,#29204,#29205,#29206,#29207,#29208,
#29209,#29210,#29211,#29212,#29213,#29214,#29215,#29216,#29217,#29218,#29219,
#29220,#29221,#29222,#29223),.UNSPECIFIED.,.F.,.F.,(4,2,2,2,2,2,2,2,2,2,
2,2,2,2,2,2,2,2,2,2,2,2,2,2,2,2,2,2,2,2,2,2,2,2,2,2,2,2,2,2,2,2,2,2,2,2,
2,2,2,2,2,2,2,2,2,2,2,2,2,2,2,2,2,2,2,2,2,2,2,2,2,2,2,2,2,2,2,2,2,2,2,2,
2,2,2,2,2,2,2,2,2,2,2,2,2,2,2,2,2,2,2,2,2,2,2,2,2,2,2,2,2,2,2,2,2,2,2,2,
2,2,2,2,2,2,2,2,2,2,2,2,4),(-3.21940741207938,-3.20117837848131,-3.15588003122262,
-3.12595304682234,-3.10687043466454,-3.09570977334897,-3.07791981249033,
-3.05153371237635,-2.99960101454642,-2.97780527749097,-2.95593992425781,
-2.87092302223556,-2.85679505762079,-2.84501212794811,-2.81485048994345,
-2.74936479065764,-2.72860014541299,-2.70550726384004,-2.69191442073332,
-2.65171987798415,-2.62060564968142,-2.60829625257774,-2.59509036618975,
-2.5787768250194,-2.53704972617425,-2.50491961757408,-2.48580264052286,
-2.46389527817565,-2.41044503118838,-2.40854592004315,-2.37584543693753,
-2.3631076293498,-2.35039614146276,-2.30864030969151,-2.26265562533825,
-2.24065874607255,-2.2189837041233,-2.17598350112437,-2.12814508283956,
-2.11720340539568,-2.10450034971466,-2.0627800231029,-2.01672470947108,
-1.99473110567979,-1.97305313935917,-1.92407146269707,-1.88370548692773,
-1.8710864861823,-1.85825247345477,-1.8501917539699,-1.80389052367407,-1.76648864922323,
-1.74748059586703,-1.7253862397806,-1.70125630104755,-1.67382182127231,
-1.63675971082746,-1.62451665716257,-1.61121877010471,-1.59473104313657,
-1.55184116828966,-1.5175512474389,-1.49687579507737,-1.47267773194202,
-1.42440291811256,-1.39168762928195,-1.37914506198586,-1.36622702846646,
-1.35808477458443,-1.3339964509513,-1.27604631115371,-1.25680965980543,
-1.23507815074704,-1.2229784031365,-1.16522997130604,-1.14282866581271,
-1.13232056012668,-1.11874642667915,-1.1017303985035,-1.05507827256674,
-1.02385015226429,-1.00334194709201,-0.978077252158774,-0.935609070481279,
-0.89939383293148,-0.887021411230156,-0.873898687661494,-0.873067260651591,
-0.872019630484148,-0.870687618612639,-0.851714784252702,-0.788620684246302,
-0.766248788602609,-0.758609375565332,-0.739412613818327,-0.713963257522252,
-0.66398644077587,-0.646760463165984,-0.636086158627321,-0.635068227654396,
-0.634063832159682,-0.633021295070353,-0.631896801722091,-0.630646112338921,
-0.629987326553337,-0.629053869885849,-0.627689839121058,-0.625630802015863,
-0.622430342610499,-0.600961522933363,-0.539016431020233,-0.519877953041265,
-0.500527453506894,-0.47854250127256,-0.438115582836877,-0.407363034767613,
-0.395060571615654,-0.393906197711282,-0.380303664839752,-0.367834103227159,
-0.332033843084473,-0.292312088127189,-0.274470994541147,-0.265337195509639,
-0.245997058404553,-0.219525231519165,-0.170112023501597,-0.154024091758782,
-0.143763021626771,-0.128863813576066,-0.123785925501408),.UNSPECIFIED.);
#355=B_SPLINE_CURVE_WITH_KNOTS('',3,(#29229,#29230,#29231,#29232,#29233,
#29234,#29235,#29236,#29237,#29238,#29239,#29240,#29241,#29242,#29243,#29244,
#29245,#29246,#29247,#29248,#29249,#29250,#29251,#29252,#29253,#29254,#29255,
#29256,#29257,#29258,#29259,#29260,#29261,#29262,#29263,#29264,#29265,#29266,
#29267,#29268,#29269,#29270,#29271,#29272,#29273,#29274,#29275,#29276,#29277,
#29278,#29279,#29280,#29281,#29282,#29283,#29284,#29285,#29286,#29287,#29288,
#29289,#29290,#29291,#29292,#29293,#29294,#29295,#29296,#29297,#29298,#29299,
#29300,#29301,#29302,#29303,#29304,#29305,#29306,#29307,#29308,#29309,#29310,
#29311,#29312,#29313,#29314,#29315,#29316,#29317,#29318,#29319,#29320,#29321,
#29322,#29323,#29324,#29325,#29326,#29327,#29328,#29329,#29330,#29331,#29332,
#29333,#29334,#29335,#29336,#29337,#29338,#29339,#29340,#29341,#29342,#29343,
#29344,#29345,#29346,#29347,#29348,#29349,#29350,#29351,#29352,#29353,#29354,
#29355,#29356,#29357,#29358,#29359,#29360,#29361,#29362,#29363,#29364,#29365,
#29366,#29367,#29368,#29369,#29370,#29371,#29372,#29373,#29374,#29375,#29376,
#29377,#29378,#29379,#29380,#29381,#29382,#29383,#29384,#29385,#29386,#29387,
#29388,#29389,#29390,#29391,#29392,#29393,#29394,#29395,#29396,#29397,#29398,
#29399,#29400,#29401,#29402,#29403,#29404,#29405,#29406,#29407,#29408,#29409,
#29410,#29411,#29412,#29413,#29414,#29415,#29416,#29417,#29418,#29419,#29420,
#29421,#29422,#29423,#29424,#29425,#29426,#29427,#29428,#29429,#29430,#29431,
#29432,#29433,#29434,#29435,#29436,#29437,#29438,#29439,#29440,#29441,#29442,
#29443,#29444,#29445,#29446,#29447,#29448,#29449,#29450,#29451,#29452,#29453,
#29454,#29455,#29456,#29457,#29458,#29459,#29460,#29461,#29462,#29463,#29464,
#29465,#29466,#29467,#29468,#29469,#29470,#29471,#29472,#29473,#29474,#29475,
#29476,#29477,#29478,#29479,#29480,#29481,#29482),.UNSPECIFIED.,.F.,.F.,
(4,2,2,2,2,2,2,2,2,2,2,2,2,2,2,2,2,2,2,2,2,2,2,2,2,2,2,2,2,2,2,2,2,2,2,
2,2,2,2,2,2,2,2,2,2,2,2,2,2,2,2,2,2,2,2,2,2,2,2,2,2,2,2,2,2,2,2,2,2,2,2,
2,2,2,2,2,2,2,2,2,2,2,2,2,2,2,2,2,2,2,2,2,2,2,2,2,2,2,2,2,2,2,2,2,2,2,2,
2,2,2,2,2,2,2,2,2,2,2,2,2,2,2,2,2,2,2,4),(-2.97204421563466,-2.96411068123968,
-2.91744367631199,-2.87468121859989,-2.86225627162148,-2.8495052821607,
-2.81643080078128,-2.75973433747324,-2.73844941655722,-2.71645538238226,
-2.69235672589235,-2.63682392554474,-2.6208865987792,-2.61089675711181,
-2.59229885871006,-2.56364055208758,-2.51609147438116,-2.49432403669667,
-2.47285582380535,-2.42766606843871,-2.38273041990521,-2.37044184460446,
-2.3575310111409,-2.34936596508652,-2.3250909908574,-2.26749621386711,-2.24843365123487,
-2.22693735535935,-2.17901952237725,-2.13748589935439,-2.12499437112371,
-2.11231580970935,-2.09693398244242,-2.06060476202399,-2.02122610212621,
-2.00224796063232,-1.98063278146582,-1.9685589308996,-1.91009425903436,
-1.88753569297473,-1.87635206914754,-1.86133426404452,-1.8413472171381,
-1.77340321453001,-1.75288179754832,-1.7299184410829,-1.69747867221596,
-1.64588080607389,-1.63339633250518,-1.62071037317785,-1.61276318198242,
-1.5657548315989,-1.52882260262654,-1.5099769082946,-1.4881460057099,-1.464386274588,
-1.41155957705095,-1.3933451321187,-1.38230270391219,-1.36425463894452,
-1.3370948705326,-1.28698789859071,-1.26525771895218,-1.24375639243774,
-1.18798419266902,-1.17421962352946,-1.15156001482275,-1.14107712158639,
-1.12787039252154,-1.11150211520354,-1.06909793887235,-1.034548961541,-1.01402136076166,
-0.990304325809183,-0.942210960313155,-0.928498812103099,-0.905803140557983,
-0.895315086773724,-0.882120503240361,-0.881753868598437,-0.881287986439464,
-0.880692398365737,-0.879925715301487,-0.861676218366873,-0.804152975018271,
-0.779682918535555,-0.778017706347123,-0.776026791239908,-0.77270629154702,
-0.759036201349059,-0.738529908225396,-0.705360058728234,-0.662588316996233,
-0.650164056121249,-0.639214429830502,-0.638006790607304,-0.636602107646557,
-0.635744690185578,-0.634405220189693,-0.632261065419,-0.612125061447222,
-0.546670820709636,-0.528919190454727,-0.510033755830493,-0.4884871100927,
-0.449947882730136,-0.417237674486417,-0.404645601880206,-0.403780615437516,
-0.391218892841825,-0.390362601025878,-0.386943243723255,-0.37254514149451,
-0.32491051586424,-0.294989975079325,-0.281226405983203,-0.276231233184317,
-0.252655688206253,-0.224716300277075,-0.168762783551146,-0.158197035656233,
-0.151256244051262,-0.130480181326522,-0.053707851031223,-0.0332280819668891,
-0.0177128010838843,-7.60539288497946E-5),.UNSPECIFIED.);
#356=B_SPLINE_CURVE_WITH_KNOTS('',3,(#29483,#29484,#29485,#29486,#29487,
#29488,#29489,#29490,#29491,#29492,#29493,#29494),.UNSPECIFIED.,.F.,.F.,
(4,2,2,2,2,4),(-6.19114003241633,-6.12736564474044,-6.11393757622783,-6.10413348852557,
-6.09157219568023,-6.06743986436456),.UNSPECIFIED.);
#357=B_SPLINE_CURVE_WITH_KNOTS('',3,(#29496,#29497,#29498,#29499,#29500,
#29501,#29502,#29503,#29504,#29505),.UNSPECIFIED.,.F.,.F.,(4,2,2,2,4),(-0.123785925501408,
-0.0778141641564192,-0.0430456999861967,-0.022634408400357,-7.62206233211306E-5),
 .UNSPECIFIED.);
#358=B_SPLINE_CURVE_WITH_KNOTS('',3,(#29506,#29507,#29508,#29509,#29510,
#29511,#29512,#29513,#29514,#29515,#29516,#29517,#29518,#29519,#29520,#29521,
#29522,#29523,#29524,#29525,#29526,#29527,#29528,#29529,#29530,#29531,#29532,
#29533,#29534,#29535,#29536,#29537,#29538,#29539,#29540,#29541,#29542,#29543,
#29544,#29545,#29546,#29547,#29548,#29549,#29550,#29551,#29552,#29553,#29554,
#29555,#29556,#29557,#29558,#29559,#29560,#29561,#29562,#29563,#29564,#29565,
#29566,#29567,#29568,#29569,#29570,#29571,#29572,#29573,#29574,#29575,#29576,
#29577,#29578,#29579,#29580,#29581,#29582,#29583,#29584,#29585,#29586,#29587,
#29588,#29589,#29590,#29591,#29592,#29593,#29594,#29595,#29596,#29597,#29598,
#29599,#29600,#29601,#29602,#29603,#29604,#29605,#29606,#29607,#29608,#29609,
#29610,#29611,#29612,#29613,#29614,#29615,#29616,#29617,#29618,#29619,#29620,
#29621,#29622,#29623,#29624,#29625,#29626,#29627,#29628,#29629,#29630,#29631,
#29632,#29633,#29634,#29635,#29636,#29637,#29638,#29639,#29640,#29641,#29642,
#29643,#29644,#29645,#29646,#29647,#29648,#29649,#29650,#29651,#29652,#29653,
#29654,#29655,#29656,#29657,#29658,#29659,#29660,#29661,#29662,#29663,#29664,
#29665,#29666,#29667,#29668,#29669,#29670,#29671,#29672,#29673,#29674,#29675,
#29676,#29677,#29678,#29679,#29680,#29681,#29682,#29683,#29684,#29685,#29686,
#29687,#29688,#29689,#29690,#29691,#29692,#29693,#29694,#29695,#29696,#29697,
#29698,#29699,#29700,#29701,#29702,#29703,#29704,#29705,#29706,#29707,#29708,
#29709,#29710,#29711,#29712,#29713,#29714,#29715,#29716,#29717,#29718,#29719,
#29720,#29721,#29722,#29723,#29724,#29725),.UNSPECIFIED.,.F.,.F.,(4,3,3,
3,3,3,3,3,3,3,3,3,3,3,3,3,3,3,3,3,3,3,3,3,3,3,3,3,3,3,3,3,3,3,3,3,3,3,3,
3,3,3,3,3,3,3,3,3,3,3,3,3,3,3,3,3,3,3,3,3,3,3,3,3,3,3,3,3,3,3,3,3,3,4),
(116.23892818295,116.329038697768,116.419178925844,116.434028704121,116.521881569694,
116.609716529488,116.697554605367,116.78538751698,116.873242078482,116.933164928812,
117.021017794386,117.108852754181,117.19669083006,117.284523741674,117.372378303176,
117.432301153502,117.520154019075,117.607988978869,117.695827054748,117.783659966361,
117.871514527863,117.931437378193,118.019290243767,118.107125203562,118.194963279442,
118.282796191055,118.370650752558,118.430573602883,118.518426468456,118.60626142825,
118.694099504129,118.781932415742,118.869786977244,118.929709827574,119.017562693148,
119.105397652943,119.193235728823,119.281068640436,119.368923201939,119.428846052264,
119.516698917837,119.604533877631,119.69237195351,119.780204865123,119.868059426624,
119.927982276955,120.015835142529,120.103670102324,120.191508178203,120.279341089816,
120.367195651319,120.427118501645,120.514971367219,120.602806327013,120.690644402893,
120.778477314506,120.866331876008,120.926254726336,121.01410759191,121.101942551705,
121.189780627584,121.277613539197,121.365468100699,121.425390951027,121.513243816601,
121.601078776396,121.688916852275,121.776749763889,121.864604325391,121.924527175717,
122.012384664524,122.100222139734,122.188062354191,122.271017224399),
 .UNSPECIFIED.);
#359=B_SPLINE_CURVE_WITH_KNOTS('',3,(#29730,#29731,#29732,#29733,#29734,
#29735,#29736,#29737,#29738,#29739,#29740,#29741,#29742,#29743,#29744,#29745,
#29746,#29747,#29748,#29749,#29750,#29751,#29752,#29753,#29754,#29755,#29756,
#29757,#29758,#29759,#29760,#29761,#29762,#29763,#29764,#29765,#29766,#29767,
#29768,#29769,#29770,#29771,#29772,#29773,#29774,#29775,#29776,#29777,#29778,
#29779,#29780,#29781,#29782,#29783,#29784,#29785,#29786,#29787,#29788,#29789,
#29790,#29791,#29792,#29793,#29794,#29795,#29796,#29797,#29798,#29799,#29800,
#29801,#29802,#29803,#29804,#29805,#29806,#29807,#29808,#29809,#29810,#29811,
#29812,#29813,#29814,#29815,#29816,#29817,#29818,#29819,#29820,#29821,#29822,
#29823,#29824,#29825,#29826,#29827,#29828,#29829,#29830,#29831,#29832,#29833,
#29834,#29835,#29836,#29837,#29838,#29839,#29840,#29841,#29842,#29843,#29844,
#29845,#29846,#29847,#29848,#29849,#29850,#29851,#29852,#29853,#29854,#29855,
#29856,#29857,#29858,#29859,#29860,#29861,#29862,#29863,#29864,#29865,#29866,
#29867,#29868,#29869,#29870,#29871,#29872,#29873,#29874,#29875,#29876,#29877,
#29878,#29879,#29880,#29881,#29882,#29883,#29884,#29885,#29886,#29887,#29888,
#29889,#29890,#29891,#29892,#29893,#29894,#29895,#29896,#29897,#29898,#29899,
#29900,#29901,#29902,#29903,#29904,#29905,#29906,#29907,#29908,#29909,#29910,
#29911,#29912,#29913,#29914,#29915,#29916,#29917,#29918,#29919,#29920,#29921,
#29922,#29923,#29924,#29925,#29926,#29927,#29928,#29929,#29930,#29931,#29932,
#29933,#29934,#29935,#29936,#29937,#29938,#29939,#29940,#29941,#29942,#29943,
#29944,#29945,#29946,#29947,#29948,#29949,#29950,#29951,#29952,#29953,#29954,
#29955,#29956,#29957,#29958,#29959,#29960,#29961,#29962,#29963,#29964,#29965,
#29966,#29967,#29968,#29969,#29970,#29971,#29972,#29973,#29974,#29975,#29976,
#29977,#29978,#29979,#29980,#29981,#29982,#29983),.UNSPECIFIED.,.F.,.F.,
(4,2,2,2,2,2,2,2,2,2,2,2,2,2,2,2,2,2,2,2,2,2,2,2,2,2,2,2,2,2,2,2,2,2,2,
2,2,2,2,2,2,2,2,2,2,2,2,2,2,2,2,2,2,2,2,2,2,2,2,2,2,2,2,2,2,2,2,2,2,2,2,
2,2,2,2,2,2,2,2,2,2,2,2,2,2,2,2,2,2,2,2,2,2,2,2,2,2,2,2,2,2,2,2,2,2,2,2,
2,2,2,2,2,2,2,2,2,2,2,2,2,2,2,2,2,2,2,4),(-6.0676600479345,-6.06300156311093,
-6.05219138912275,-6.03403505117364,-5.9811424083886,-5.957374965299,-5.93848494184618,
-5.91894324672321,-5.88560449324608,-5.82977515111898,-5.82184467149748,
-5.81203068738065,-5.79950396495754,-5.76678865704346,-5.72458186220645,
-5.7039088418214,-5.68440742435925,-5.66955669263987,-5.62614474751871,
-5.59296482766278,-5.58292490633869,-5.57907136200978,-5.57653037666039,
-5.56664577247056,-5.55435211806181,-5.5296487941202,-5.48562302875605,
-5.46313071623149,-5.44422334845029,-5.42529021711367,-5.35898025850103,
-5.33868196785035,-5.33552159899471,-5.33357451185097,-5.33238166820454,
-5.33164915145285,-5.33119719676992,-5.33006187810181,-5.32022200351016,
-5.30754064128436,-5.2614552314717,-5.23030194993611,-5.21840552167871,
-5.19694943654444,-5.17785616100705,-5.14458295702549,-5.10432752555258,
-5.0882887724177,-5.07525703006934,-5.06469485173655,-5.04146253920956,
-4.98570215921476,-4.97356560109165,-4.95189370903324,-4.93295280603225,
-4.89408631268292,-4.85254758091093,-4.83436404014637,-4.82332165350525,
-4.80524318050571,-4.75225588562127,-4.72005109932547,-4.69965991241476,
-4.67526091300608,-4.61757937635378,-4.6048651217391,-4.58779211111111,
-4.57672729765341,-4.5573502049262,-4.50587958383057,-4.49075616524917,
-4.47927430982784,-4.45818069596309,-4.43590059997698,-4.38819747804384,
-4.34928134021141,-4.33690061662485,-4.32409950450634,-4.28702911913072,
-4.23648030027445,-4.21474189745155,-4.19324787879561,-4.14028149562153,
-4.10501446609073,-4.09203235253466,-4.07980032813057,-4.03211776649508,
-4.00116189355644,-3.97598938722291,-3.95569585114088,-3.92533453810172,
-3.87773444205573,-3.85396001940228,-3.8426434721844,-3.82761558442093,
-3.77926386810471,-3.74005958307201,-3.7192825551871,-3.6963588180046,-3.66530566220567,
-3.62834344211144,-3.61285045469689,-3.6001118404878,-3.58939525630702,
-3.56144954088596,-3.52357197159221,-3.49970923078575,-3.47782862160092,
-3.4590099697934,-3.39306302753264,-3.37841972958564,-3.35987348003764,
-3.34882833151189,-3.33108964336148,-3.27768677201668,-3.25385386610659,
-3.23198759311768,-3.21316118267848,-3.17165229713062,-3.13615376728696,
-3.12092036008069,-3.10832266253643,-3.09575311703086,-3.0562811115272,
-3.00733901118612,-2.98565146539759,-2.97204421563466),.UNSPECIFIED.);
#360=B_SPLINE_CURVE_WITH_KNOTS('',3,(#29985,#29986,#29987,#29988,#29989,
#29990,#29991,#29992,#29993,#29994,#29995,#29996,#29997),.UNSPECIFIED.,
 .F.,.F.,(4,3,3,3,4),(122.271017224399,122.358872260288,122.423663400408,
122.517081472137,122.522113490002),.UNSPECIFIED.);
#361=B_SPLINE_CURVE_WITH_KNOTS('',3,(#29998,#29999,#30000,#30001,#30002,
#30003,#30004,#30005,#30006,#30007,#30008,#30009,#30010,#30011,#30012,#30013),
 .UNSPECIFIED.,.F.,.F.,(4,1,1,1,1,1,1,1,1,1,1,1,1,4),(122.522113505659,
122.922799625098,123.421935849789,123.921072074479,124.42020829917,124.91934452386,
125.418480748551,125.917616973241,126.416753197932,126.915889422622,127.415025647313,
127.914161872003,128.413298096694,128.55424228146),.UNSPECIFIED.);
#362=B_SPLINE_CURVE_WITH_KNOTS('',3,(#30019,#30020,#30021,#30022,#30023,
#30024,#30025,#30026,#30027,#30028,#30029,#30030,#30031,#30032,#30033,#30034),
 .UNSPECIFIED.,.F.,.F.,(4,1,1,1,1,1,1,1,1,1,1,1,1,4),(128.805298812316,
129.032931173078,129.531803108226,130.030675043374,130.529546978522,131.02841891367,
131.527290848818,132.026162783967,132.525034719115,133.023906654263,133.522778589411,
134.021650524559,134.520522459707,134.837383691965),.UNSPECIFIED.);
#363=B_SPLINE_CURVE_WITH_KNOTS('',3,(#30035,#30036,#30037,#30038,#30039,
#30040,#30041,#30042,#30043,#30044,#30045,#30046),.UNSPECIFIED.,.F.,.F.,
(4,2,2,2,2,4),(-6.19136935571345,-6.17837183141341,-6.16428959311484,-6.1316433424487,
-6.07729914642043,-6.0676600479345),.UNSPECIFIED.);
#364=B_SPLINE_CURVE_WITH_KNOTS('',3,(#30048,#30049,#30050,#30051),
 .UNSPECIFIED.,.F.,.F.,(4,4),(128.55424228146,128.805298790277),
 .UNSPECIFIED.);
#365=B_SPLINE_CURVE_WITH_KNOTS('',3,(#30052,#30053,#30054,#30055,#30056,
#30057,#30058,#30059,#30060,#30061,#30062,#30063,#30064,#30065,#30066,#30067,
#30068,#30069,#30070,#30071,#30072,#30073,#30074,#30075,#30076,#30077,#30078,
#30079,#30080,#30081,#30082,#30083,#30084,#30085,#30086,#30087,#30088,#30089,
#30090,#30091,#30092,#30093,#30094,#30095,#30096,#30097,#30098,#30099,#30100,
#30101,#30102,#30103,#30104,#30105,#30106,#30107,#30108,#30109,#30110,#30111,
#30112,#30113,#30114,#30115,#30116,#30117,#30118,#30119,#30120,#30121,#30122,
#30123,#30124,#30125,#30126,#30127,#30128,#30129,#30130,#30131,#30132,#30133,
#30134,#30135,#30136,#30137,#30138,#30139,#30140,#30141,#30142,#30143,#30144,
#30145,#30146,#30147,#30148,#30149,#30150,#30151,#30152,#30153,#30154,#30155,
#30156,#30157,#30158,#30159,#30160,#30161,#30162,#30163,#30164,#30165,#30166,
#30167,#30168,#30169,#30170,#30171,#30172,#30173,#30174,#30175,#30176,#30177,
#30178,#30179,#30180,#30181,#30182,#30183,#30184,#30185,#30186,#30187,#30188,
#30189,#30190,#30191,#30192,#30193,#30194,#30195,#30196,#30197,#30198,#30199,
#30200,#30201,#30202,#30203,#30204,#30205,#30206,#30207,#30208,#30209,#30210,
#30211,#30212,#30213,#30214,#30215,#30216,#30217,#30218,#30219,#30220,#30221,
#30222,#30223,#30224,#30225,#30226,#30227,#30228,#30229,#30230,#30231,#30232,
#30233,#30234,#30235,#30236,#30237,#30238,#30239,#30240,#30241,#30242,#30243,
#30244,#30245,#30246,#30247,#30248,#30249,#30250,#30251,#30252,#30253,#30254,
#30255,#30256,#30257,#30258,#30259,#30260,#30261,#30262,#30263,#30264,#30265,
#30266,#30267,#30268,#30269,#30270,#30271),.UNSPECIFIED.,.F.,.F.,(4,3,3,
3,3,3,3,3,3,3,3,3,3,3,3,3,3,3,3,3,3,3,3,3,3,3,3,3,3,3,3,3,3,3,3,3,3,3,3,
3,3,3,3,3,3,3,3,3,3,3,3,3,3,3,3,3,3,3,3,3,3,3,3,3,3,3,3,3,3,3,3,3,3,4),
(128.805298797182,128.89834684814,128.912434321384,129.000287186958,129.088122146753,
129.175960222633,129.263793134246,129.351647695749,129.411570546075,129.499423411649,
129.587258371443,129.675096447323,129.762929358936,129.850783920438,129.910706770766,
129.99855963634,130.086394596135,130.174232672014,130.262065583628,130.34992014513,
130.409842995456,130.497695861029,130.585530820823,130.673368896702,130.761201808315,
130.849056369816,130.908979220147,130.996832085721,131.084667045516,131.172505121396,
131.260338033009,131.348192594512,131.408115444837,131.49596831041,131.583803270204,
131.671641346083,131.759474257696,131.847328819197,131.907251669528,131.995104535102,
132.082939494897,132.170777570777,132.25861048239,132.346465043893,132.406387894218,
132.494240759791,132.582075719585,132.669913795464,132.757746707077,132.845601268579,
132.905524118909,132.993376984483,133.081211944278,133.169050020158,133.256882931771,
133.344737493274,133.404660343599,133.492513209172,133.580348168967,133.668186244845,
133.756019156458,133.84387371796,133.90379656829,133.991649433864,134.079484393659,
134.167322469539,134.255155381152,134.343009942655,134.40293279298,134.490785003982,
134.578629290641,134.666460879314,134.754307286045,134.837387641181),
 .UNSPECIFIED.);
#366=B_SPLINE_CURVE_WITH_KNOTS('',3,(#30277,#30278,#30279,#30280,#30281,
#30282,#30283,#30284,#30285,#30286,#30287,#30288,#30289,#30290,#30291,#30292,
#30293,#30294,#30295,#30296,#30297,#30298,#30299,#30300,#30301,#30302,#30303,
#30304,#30305,#30306,#30307,#30308,#30309,#30310,#30311,#30312,#30313,#30314,
#30315,#30316,#30317,#30318,#30319,#30320,#30321,#30322,#30323,#30324,#30325,
#30326,#30327,#30328,#30329,#30330,#30331,#30332,#30333,#30334,#30335,#30336,
#30337,#30338,#30339,#30340,#30341,#30342,#30343,#30344,#30345,#30346,#30347,
#30348,#30349,#30350,#30351,#30352,#30353,#30354,#30355,#30356,#30357,#30358,
#30359,#30360,#30361,#30362,#30363,#30364,#30365,#30366,#30367,#30368,#30369,
#30370,#30371,#30372,#30373,#30374,#30375,#30376,#30377,#30378,#30379,#30380,
#30381,#30382,#30383,#30384,#30385,#30386,#30387,#30388,#30389,#30390,#30391,
#30392,#30393,#30394,#30395,#30396,#30397,#30398,#30399,#30400,#30401,#30402,
#30403,#30404,#30405,#30406,#30407,#30408,#30409,#30410,#30411,#30412,#30413,
#30414,#30415,#30416,#30417,#30418,#30419,#30420,#30421,#30422,#30423,#30424,
#30425,#30426,#30427,#30428,#30429,#30430,#30431,#30432,#30433,#30434,#30435,
#30436,#30437,#30438,#30439,#30440,#30441,#30442,#30443,#30444,#30445,#30446,
#30447,#30448,#30449,#30450,#30451,#30452,#30453,#30454,#30455,#30456,#30457,
#30458,#30459,#30460,#30461,#30462,#30463,#30464,#30465,#30466,#30467,#30468,
#30469,#30470,#30471,#30472,#30473,#30474,#30475,#30476,#30477,#30478,#30479,
#30480,#30481,#30482,#30483,#30484,#30485,#30486,#30487,#30488,#30489,#30490,
#30491,#30492,#30493,#30494,#30495,#30496),.UNSPECIFIED.,.F.,.F.,(4,3,3,
3,3,3,3,3,3,3,3,3,3,3,3,3,3,3,3,3,3,3,3,3,3,3,3,3,3,3,3,3,3,3,3,3,3,3,3,
3,3,3,3,3,3,3,3,3,3,3,3,3,3,3,3,3,3,3,3,3,3,3,3,3,3,3,3,3,3,3,3,3,3,4),
(135.088484109301,135.17598699825,135.263487430307,135.350979186156,135.438494599681,
135.518266330003,135.606120703016,135.693957195188,135.781796802318,135.869631257661,
135.957487308412,136.017138265152,136.104992638165,136.192829130337,136.280668737468,
136.368503192812,136.456359243563,136.5160102003,136.603864573313,136.691701065484,
136.779540672614,136.867375127957,136.955231178708,137.014882135448,137.102736508461,
137.190573000633,137.278412607763,137.366247063106,137.454103113857,137.513754070596,
137.601608443609,137.689444935781,137.777284542911,137.865118998254,137.952975049005,
138.012626005744,138.100480378757,138.188316870929,138.276156478059,138.363990933403,
138.451846984154,138.511497940892,138.599352313905,138.687188806077,138.775028413206,
138.86286286855,138.9507189193,139.01036987604,139.098224249053,139.186060741225,
139.273900348355,139.361734803699,139.44959085445,139.509241811188,139.597096184202,
139.684932676373,139.772772283503,139.860606738847,139.948462789598,140.008113746337,
140.095968119351,140.183804611522,140.271644218652,140.359478673996,140.447334724747,
140.506985681485,140.594840054498,140.682676546669,140.770516153799,140.858350609142,
140.946206659893,141.005857616633,141.093483641527,141.120602214731),
 .UNSPECIFIED.);
#367=B_SPLINE_CURVE_WITH_KNOTS('',3,(#30497,#30498,#30499,#30500,#30501),
 .UNSPECIFIED.,.F.,.F.,(4,1,4),(134.837383691965,135.019394394855,135.088484104361),
 .UNSPECIFIED.);
#368=B_SPLINE_CURVE_WITH_KNOTS('',3,(#30503,#30504,#30505,#30506,#30507,
#30508,#30509,#30510,#30511,#30512),.UNSPECIFIED.,.F.,.F.,(4,3,3,4),(134.837387641181,
134.902069017671,134.995276561016,135.088484104361),.UNSPECIFIED.);
#369=B_SPLINE_CURVE_WITH_KNOTS('',3,(#30513,#30514,#30515,#30516,#30517,
#30518,#30519,#30520,#30521,#30522,#30523,#30524,#30525,#30526,#30527,#30528,
#30529,#30530,#30531,#30532,#30533,#30534,#30535,#30536,#30537,#30538,#30539,
#30540,#30541,#30542,#30543,#30544,#30545,#30546,#30547,#30548,#30549,#30550,
#30551,#30552,#30553,#30554,#30555,#30556,#30557,#30558,#30559,#30560,#30561,
#30562,#30563,#30564,#30565,#30566,#30567,#30568,#30569,#30570,#30571,#30572,
#30573,#30574,#30575,#30576,#30577,#30578,#30579,#30580,#30581,#30582,#30583,
#30584,#30585,#30586,#30587,#30588,#30589,#30590,#30591,#30592,#30593,#30594,
#30595,#30596,#30597,#30598,#30599,#30600,#30601,#30602,#30603,#30604,#30605,
#30606,#30607,#30608,#30609,#30610,#30611,#30612,#30613,#30614,#30615,#30616,
#30617,#30618,#30619,#30620,#30621,#30622,#30623,#30624,#30625,#30626,#30627,
#30628,#30629,#30630,#30631,#30632,#30633,#30634,#30635,#30636,#30637,#30638,
#30639,#30640,#30641,#30642,#30643,#30644,#30645,#30646,#30647,#30648,#30649,
#30650,#30651,#30652,#30653,#30654,#30655,#30656,#30657,#30658,#30659,#30660,
#30661,#30662,#30663,#30664,#30665,#30666,#30667,#30668,#30669,#30670,#30671,
#30672,#30673,#30674,#30675,#30676,#30677,#30678,#30679,#30680,#30681,#30682,
#30683,#30684,#30685,#30686,#30687,#30688,#30689,#30690,#30691,#30692,#30693,
#30694,#30695,#30696,#30697,#30698,#30699,#30700,#30701,#30702,#30703,#30704,
#30705,#30706,#30707,#30708,#30709,#30710,#30711,#30712,#30713,#30714,#30715,
#30716,#30717,#30718,#30719,#30720,#30721,#30722,#30723,#30724,#30725,#30726,
#30727,#30728,#30729,#30730,#30731,#30732,#30733,#30734,#30735,#30736,#30737,
#30738,#30739,#30740,#30741,#30742,#30743,#30744,#30745,#30746,#30747,#30748,
#30749,#30750,#30751,#30752,#30753,#30754,#30755,#30756,#30757,#30758),
 .UNSPECIFIED.,.F.,.F.,(4,2,2,2,2,2,2,2,2,2,2,2,2,2,2,2,2,2,2,2,2,2,2,2,
2,2,2,2,2,2,2,2,2,2,2,2,2,2,2,2,2,2,2,2,2,2,2,2,2,2,2,2,2,2,2,2,2,2,2,2,
2,2,2,2,2,2,2,2,2,2,2,2,2,2,2,2,2,2,2,2,2,2,2,2,2,2,2,2,2,2,2,2,2,2,2,2,
2,2,2,2,2,2,2,2,2,2,2,2,2,2,2,2,2,2,2,2,2,2,2,2,2,2,4),(-6.19116494302175,
-6.17703734950308,-6.1642332800254,-6.14380755584216,-6.10914123558922,
-6.05622377563799,-6.04286629535891,-6.03234035590157,-6.01553011095014,
-5.96572983886545,-5.93993559338612,-5.92069483504914,-5.91137080832514,
-5.89411263056373,-5.83723919301332,-5.81279712282643,-5.80555977645213,
-5.79247970631615,-5.79143790586598,-5.77887172285572,-5.75072147711475,
-5.70913847348934,-5.68695422494636,-5.66748676667828,-5.64903922621219,
-5.58356864396798,-5.56338254532162,-5.56088440472294,-5.55928667875535,
-5.55823444449872,-5.55752193230004,-5.55702784204972,-5.54582465351428,
-5.53510838929563,-5.48047347045303,-5.45195674899915,-5.43226314035227,
-5.41650800972621,-5.39213794921603,-5.33402503226821,-5.3156560429689,
-5.31464792868625,-5.31385702723433,-5.31323124398406,-5.30004351817591,
-5.28772132550516,-5.25555507480882,-5.22422777874082,-5.19983214911048,
-5.17761075762797,-5.15866866544375,-5.12229318038202,-5.08286654308721,
-5.06093895062442,-5.04965501464434,-5.03394581732045,-4.98479788555917,
-4.95793185388434,-4.93453184105898,-4.91387810287515,-4.87763843878035,
-4.87327177306261,-4.82703692882799,-4.81119233634939,-4.79987746975932,
-4.78258871437243,-4.73202313732268,-4.7077680272941,-4.6856139534971,-4.66406961199734,
-4.60683893170405,-4.58289912767763,-4.57478799775961,-4.56190224715054,
-4.54933147062396,-4.51660691591032,-4.46832616088545,-4.44416483231003,
-4.42348211844725,-4.38905651192622,-4.34631926662311,-4.32985397789693,
-4.31656819753484,-4.30594248383866,-4.28270749976801,-4.22672921524457,
-4.21454257038949,-4.19273345571192,-4.17355271186985,-4.11536233632143,
-4.09122701256364,-4.07433804594037,-4.06313680873221,-4.04340516322852,
-3.99241158015077,-3.96879773026077,-3.94694950494545,-3.92779502187308,
-3.88016358396155,-3.84944531309101,-3.83009312768414,-3.81892651988141,
-3.80135407367478,-3.74869432044514,-3.72433193807619,-3.70212643137315,
-3.68062105142192,-3.6261521734276,-3.59139947631689,-3.57841366511148,
-3.56593028739867,-3.52291716201066,-3.47629038964963,-3.45459983301622,
-3.43533310475785,-3.40079251087165,-3.36147349575419,-3.33957378120327,
-3.32829141674859,-3.31257031538694,-3.26341318653884,-3.23655984982501,
-3.21935699787793),.UNSPECIFIED.);
#370=B_SPLINE_CURVE_WITH_KNOTS('',3,(#30764,#30765,#30766,#30767,#30768,
#30769,#30770,#30771,#30772,#30773,#30774,#30775,#30776,#30777,#30778,#30779),
 .UNSPECIFIED.,.F.,.F.,(4,1,1,1,1,1,1,1,1,1,1,1,1,4),(141.371669425729,
141.504729551781,142.003601486929,142.502473422077,143.001345357225,143.500217292373,
143.999089227522,144.49796116267,144.996833097818,145.495705032966,145.994576968114,
146.493448903262,146.99232083841,147.403749232517),.UNSPECIFIED.);
#371=B_SPLINE_CURVE_WITH_KNOTS('',3,(#30780,#30781,#30782,#30783,#30784,
#30785,#30786,#30787,#30788,#30789),.UNSPECIFIED.,.F.,.F.,(4,3,3,4),(141.120602214731,
141.208209304607,141.295822961552,141.371669411541),.UNSPECIFIED.);
#372=B_SPLINE_CURVE_WITH_KNOTS('',3,(#30790,#30791,#30792,#30793,#30794,
#30795,#30796,#30797,#30798,#30799,#30800,#30801,#30802,#30803,#30804,#30805,
#30806,#30807,#30808,#30809,#30810,#30811,#30812,#30813,#30814,#30815,#30816,
#30817,#30818,#30819,#30820,#30821,#30822,#30823,#30824,#30825,#30826,#30827,
#30828,#30829,#30830,#30831,#30832,#30833,#30834,#30835,#30836,#30837,#30838,
#30839,#30840,#30841,#30842,#30843,#30844,#30845,#30846,#30847,#30848,#30849,
#30850,#30851,#30852,#30853,#30854,#30855,#30856,#30857,#30858,#30859,#30860,
#30861,#30862,#30863,#30864,#30865,#30866,#30867,#30868,#30869,#30870,#30871,
#30872,#30873,#30874,#30875,#30876,#30877,#30878,#30879,#30880,#30881,#30882,
#30883,#30884,#30885,#30886,#30887,#30888,#30889,#30890,#30891,#30892,#30893,
#30894,#30895,#30896,#30897,#30898,#30899,#30900,#30901,#30902,#30903,#30904,
#30905,#30906,#30907,#30908,#30909,#30910,#30911,#30912,#30913,#30914,#30915,
#30916,#30917,#30918,#30919,#30920,#30921,#30922,#30923,#30924,#30925,#30926,
#30927,#30928,#30929,#30930,#30931,#30932,#30933,#30934,#30935,#30936,#30937,
#30938,#30939,#30940,#30941,#30942,#30943,#30944,#30945,#30946,#30947,#30948,
#30949,#30950,#30951,#30952,#30953,#30954,#30955,#30956,#30957,#30958,#30959,
#30960,#30961,#30962,#30963,#30964,#30965,#30966,#30967,#30968,#30969,#30970,
#30971,#30972,#30973,#30974,#30975,#30976,#30977,#30978,#30979,#30980,#30981,
#30982,#30983,#30984,#30985,#30986,#30987,#30988,#30989,#30990,#30991,#30992,
#30993,#30994,#30995,#30996,#30997,#30998,#30999,#31000,#31001,#31002,#31003,
#31004,#31005,#31006,#31007,#31008,#31009,#31010,#31011,#31012,#31013,#31014,
#31015,#31016,#31017,#31018,#31019,#31020,#31021,#31022,#31023,#31024,#31025,
#31026,#31027,#31028,#31029,#31030,#31031,#31032,#31033,#31034,#31035,#31036,
#31037),.UNSPECIFIED.,.F.,.F.,(4,2,2,2,2,2,2,2,2,2,2,2,2,2,2,2,2,2,2,2,
2,2,2,2,2,2,2,2,2,2,2,2,2,2,2,2,2,2,2,2,2,2,2,2,2,2,2,2,2,2,2,2,2,2,2,2,
2,2,2,2,2,2,2,2,2,2,2,2,2,2,2,2,2,2,2,2,2,2,2,2,2,2,2,2,2,2,2,2,2,2,2,2,
2,2,2,2,2,2,2,2,2,2,2,2,2,2,2,2,2,2,2,2,2,2,2,2,2,2,2,2,2,2,2,4),(-3.21935699787793,
-3.21316574382707,-3.19250989034801,-3.12355310177051,-3.09563748505854,
-3.08510027142359,-3.07160316901746,-3.05473506422643,-3.00917199984596,
-2.97710495108727,-2.95655385603739,-2.93164162185956,-2.86234423940217,
-2.84524819467226,-2.83407987182315,-2.81466375467055,-2.7837549282786,
-2.73647812724851,-2.71731400536239,-2.6954801539321,-2.6518927399594,-2.61669784915749,
-2.59945486001201,-2.58829144305401,-2.56907356360656,-2.53875182401622,
-2.49038352427511,-2.47125139413836,-2.44936880460065,-2.42568237233774,
-2.37415174452258,-2.35468710802651,-2.34351742839056,-2.32603112372484,
-2.2805418421437,-2.24355865422078,-2.22457294543408,-2.20243767323222,
-2.17822174496133,-2.11590501654389,-2.10292696087652,-2.09043678634569,
-2.08270985379705,-2.03723873670129,-1.99764336815913,-1.97865723782612,
-1.95652242097001,-1.93230757697079,-1.87143333557131,-1.85784458764912,
-1.8457888581465,-1.80665611724896,-1.75274959080811,-1.73359806255764,
-1.71174459709267,-1.66793522467079,-1.63617314630175,-1.61685525028106,
-1.60568933672935,-1.58808956392394,-1.56219243683647,-1.50845526340811,
-1.48687994314329,-1.46476418569153,-1.44058927319633,-1.38896356972876,
-1.37044976025338,-1.35929571259066,-1.3409940267418,-1.3132533887721,-1.27213519698725,
-1.24773067096726,-1.2270967831308,-1.19353998525343,-1.13523365967798,
-1.12094698710776,-1.10922956394915,-1.08033236632137,-1.01293362655361,
-0.992227825167441,-0.968978051344675,-0.936899162881563,-0.885268327354135,
-0.872704649199791,-0.862767793654905,-0.86162103217559,-0.861281487285616,
-0.860726587094819,-0.859815351734257,-0.858312056532366,-0.855830139949326,
-0.836649112705669,-0.771835850106395,-0.752167074879882,-0.732844513280138,
-0.711249010258384,-0.672985890047654,-0.666222628819701,-0.637110847403014,
-0.626420749717713,-0.616414869848926,-0.613899412979933,-0.610412801638719,
-0.603823332220953,-0.577022026661718,-0.523311490345541,-0.510886707762487,
-0.490772954721622,-0.470351614673873,-0.412358250096588,-0.390247685735212,
-0.378734878019143,-0.368321278159657,-0.353343782086913,-0.317910129570223,
-0.278198157293771,-0.257791049881306,-0.238679495714611,-0.216170129610846,
-0.172642003635443,-0.157979298938959,-0.140305586474041,-0.129627005635082,
-0.123748402156024),.UNSPECIFIED.);
#373=B_SPLINE_CURVE_WITH_KNOTS('',3,(#31043,#31044,#31045,#31046,#31047,
#31048,#31049,#31050,#31051,#31052,#31053,#31054,#31055,#31056,#31057,#31058,
#31059,#31060,#31061,#31062,#31063,#31064,#31065,#31066,#31067,#31068,#31069,
#31070,#31071,#31072,#31073,#31074,#31075,#31076,#31077,#31078,#31079,#31080,
#31081,#31082,#31083,#31084,#31085,#31086,#31087,#31088,#31089,#31090,#31091,
#31092,#31093,#31094,#31095,#31096,#31097,#31098,#31099,#31100,#31101,#31102,
#31103,#31104,#31105,#31106,#31107,#31108,#31109,#31110,#31111,#31112,#31113,
#31114,#31115,#31116,#31117,#31118,#31119,#31120,#31121,#31122,#31123,#31124,
#31125,#31126,#31127,#31128,#31129,#31130,#31131,#31132,#31133,#31134,#31135,
#31136,#31137,#31138,#31139,#31140,#31141,#31142,#31143,#31144,#31145,#31146,
#31147,#31148,#31149,#31150,#31151,#31152,#31153,#31154,#31155,#31156,#31157,
#31158,#31159,#31160,#31161,#31162,#31163,#31164,#31165,#31166,#31167,#31168,
#31169,#31170,#31171,#31172,#31173,#31174,#31175,#31176,#31177,#31178,#31179,
#31180,#31181,#31182,#31183,#31184,#31185,#31186,#31187,#31188,#31189,#31190,
#31191,#31192,#31193,#31194,#31195,#31196,#31197,#31198,#31199,#31200,#31201,
#31202,#31203,#31204,#31205,#31206,#31207,#31208,#31209,#31210,#31211,#31212,
#31213,#31214,#31215,#31216,#31217,#31218,#31219,#31220,#31221,#31222,#31223,
#31224,#31225,#31226,#31227,#31228,#31229,#31230,#31231,#31232,#31233,#31234,
#31235,#31236,#31237,#31238,#31239,#31240,#31241,#31242,#31243,#31244,#31245,
#31246,#31247,#31248,#31249,#31250,#31251,#31252,#31253,#31254,#31255,#31256,
#31257,#31258,#31259,#31260,#31261,#31262,#31263,#31264,#31265,#31266,#31267,
#31268,#31269,#31270,#31271,#31272,#31273,#31274,#31275,#31276,#31277,#31278,
#31279,#31280,#31281,#31282,#31283,#31284,#31285,#31286,#31287,#31288,#31289,
#31290,#31291,#31292,#31293,#31294,#31295,#31296,#31297,#31298),
 .UNSPECIFIED.,.F.,.F.,(4,2,2,2,2,2,2,2,2,2,2,2,2,2,2,2,2,2,2,2,2,2,2,2,
2,2,2,2,2,2,2,2,2,2,2,2,2,2,2,2,2,2,2,2,2,2,2,2,2,2,2,2,2,2,2,2,2,2,2,2,
2,2,2,2,2,2,2,2,2,2,2,2,2,2,2,2,2,2,2,2,2,2,2,2,2,2,2,2,2,2,2,2,2,2,2,2,
2,2,2,2,2,2,2,2,2,2,2,2,2,2,2,2,2,2,2,2,2,2,2,2,2,2,2,2,2,2,2,4),(-2.97188626525704,
-2.96975074164106,-2.9263303559528,-2.88990303366061,-2.87340634195713,
-2.86233267829574,-2.84269920478538,-2.81100941469992,-2.76533127746046,
-2.7462707140118,-2.7247728406981,-2.6765192930133,-2.635386131538,-2.62287443420638,
-2.61021777327762,-2.59487609980264,-2.55877206357895,-2.53991360842078,
-2.51140177136903,-2.49117954246924,-2.46488356337848,-2.4312244043192,
-2.38954215043325,-2.37705869051714,-2.36437210188408,-2.35642422903556,
-2.31047195879666,-2.27275279109622,-2.25386565246452,-2.23210769488765,
-2.18782021780113,-2.14331501979756,-2.13099759075805,-2.11812258910905,
-2.10999229723689,-2.06358956611743,-2.0266939900833,-2.00785075623836,
-1.98601646118949,-1.96224927075858,-1.90936226198506,-1.89119909313463,
-1.88015696730535,-1.86205912518019,-1.82066704256834,-1.80127060929152,
-1.7734238141848,-1.75321472726857,-1.72638425432589,-1.69136378590274,
-1.65258557915946,-1.63995611764576,-1.62741821724914,-1.61961341288586,
-1.60795796824994,-1.56088506667449,-1.5301409185966,-1.50982903714417,
-1.48484084014843,-1.45430943591898,-1.4049907147059,-1.39415840059693,
-1.38160812315362,-1.34299207442822,-1.29674465774136,-1.27409066376061,
-1.2531973919192,-1.21119472270484,-1.16091106314901,-1.14832539592815,
-1.13574428661718,-1.09577025043834,-1.04753389025392,-1.02580548884736,
-1.0043031330915,-0.992354621862678,-0.954467592238873,-0.915158450992807,
-0.902562234097002,-0.889991637216024,-0.889367716728599,-0.888687303470545,
-0.887941651527501,-0.887710854495311,-0.887415376257045,-0.887035506880723,
-0.869489228676335,-0.818248354178469,-0.790352965228216,-0.77074926593518,
-0.747423812408836,-0.71682537905745,-0.667618776287439,-0.656794343839576,
-0.64596645841836,-0.644924376966577,-0.643727768686432,-0.642324942176007,
-0.641667930139639,-0.640624694724322,-0.638933502496702,-0.619148211900778,
-0.552477596556398,-0.535420404979643,-0.516704037292846,-0.495277012953636,
-0.457382904592064,-0.447636955771573,-0.437768710568182,-0.419477416066318,
-0.408204860698465,-0.393885593098416,-0.383789411424907,-0.349783964485769,
-0.307044322047352,-0.286357470563327,-0.283096889067452,-0.259892285100198,
-0.232620374462148,-0.183926660325592,-0.168550369124722,-0.157585914554883,
-0.137157497631893,-0.0798175246746923,-0.0524557511181905,-0.0336832247805891,
-0.0185010444887893,-4.22433275936514E-5),.UNSPECIFIED.);
#374=B_SPLINE_CURVE_WITH_KNOTS('',3,(#31299,#31300,#31301,#31302,#31303),
 .UNSPECIFIED.,.F.,.F.,(4,1,4),(147.403749232517,147.491192773558,147.65485471872),
 .UNSPECIFIED.);
#375=B_SPLINE_CURVE_WITH_KNOTS('',3,(#31305,#31306,#31307,#31308,#31309,
#31310,#31311,#31312,#31313,#31314,#31315,#31316),.UNSPECIFIED.,.F.,.F.,
(4,2,2,2,2,4),(-0.123748402156024,-0.114490652887485,-0.060891536213952,
-0.0277646115254283,-0.0134254131229336,-4.23462887881731E-5),
 .UNSPECIFIED.);
#376=B_SPLINE_CURVE_WITH_KNOTS('',3,(#31317,#31318,#31319,#31320,#31321,
#31322,#31323,#31324,#31325,#31326,#31327,#31328,#31329,#31330,#31331,#31332),
 .UNSPECIFIED.,.F.,.F.,(4,1,1,1,1,1,1,1,1,1,1,1,1,4),(147.65485471872,147.879610859624,
148.378747084315,148.877883309006,149.377019533696,149.876155758387,150.375291983077,
150.874428207768,151.373564432458,151.872700657149,152.371836881839,152.87097310653,
153.37010933122,153.686939606376),.UNSPECIFIED.);
#377=B_SPLINE_CURVE_WITH_KNOTS('',3,(#31337,#31338,#31339,#31340,#31341,
#31342,#31343,#31344,#31345,#31346,#31347,#31348,#31349,#31350,#31351,#31352,
#31353,#31354,#31355,#31356,#31357,#31358,#31359,#31360,#31361,#31362,#31363,
#31364,#31365,#31366,#31367,#31368,#31369,#31370,#31371,#31372,#31373,#31374,
#31375,#31376,#31377,#31378,#31379,#31380,#31381,#31382,#31383,#31384,#31385,
#31386,#31387,#31388,#31389,#31390,#31391,#31392,#31393,#31394,#31395,#31396,
#31397,#31398,#31399,#31400,#31401,#31402,#31403,#31404,#31405,#31406,#31407,
#31408,#31409,#31410,#31411,#31412,#31413,#31414,#31415,#31416,#31417,#31418,
#31419,#31420,#31421,#31422,#31423,#31424,#31425,#31426,#31427,#31428,#31429,
#31430,#31431,#31432,#31433,#31434,#31435,#31436,#31437,#31438,#31439,#31440,
#31441,#31442,#31443,#31444,#31445,#31446,#31447,#31448,#31449,#31450,#31451,
#31452,#31453,#31454,#31455,#31456,#31457,#31458,#31459,#31460,#31461,#31462,
#31463,#31464,#31465,#31466,#31467,#31468,#31469,#31470,#31471,#31472,#31473,
#31474,#31475,#31476,#31477,#31478,#31479,#31480,#31481,#31482,#31483,#31484,
#31485,#31486,#31487,#31488,#31489,#31490,#31491,#31492,#31493,#31494,#31495,
#31496,#31497,#31498,#31499,#31500,#31501,#31502,#31503,#31504,#31505,#31506,
#31507,#31508,#31509,#31510,#31511,#31512,#31513,#31514,#31515,#31516,#31517,
#31518,#31519,#31520,#31521,#31522,#31523,#31524,#31525,#31526,#31527,#31528,
#31529,#31530,#31531,#31532,#31533,#31534,#31535,#31536,#31537,#31538,#31539,
#31540,#31541,#31542,#31543,#31544,#31545,#31546,#31547,#31548,#31549,#31550,
#31551,#31552,#31553,#31554,#31555,#31556,#31557,#31558,#31559,#31560,#31561,
#31562,#31563,#31564,#31565,#31566,#31567,#31568,#31569,#31570,#31571,#31572,
#31573,#31574,#31575,#31576,#31577,#31578),.UNSPECIFIED.,.F.,.F.,(4,2,2,
2,2,2,2,2,2,2,2,2,2,2,2,2,2,2,2,2,2,2,2,2,2,2,2,2,2,2,2,2,2,2,2,2,2,2,2,
2,2,2,2,2,2,2,2,2,2,2,2,2,2,2,2,2,2,2,2,2,2,2,2,2,2,2,2,2,2,2,2,2,2,2,2,
2,2,2,2,2,2,2,2,2,2,2,2,2,2,2,2,2,2,2,2,2,2,2,2,2,2,2,2,2,2,2,2,2,2,2,2,
2,2,2,2,2,2,2,2,2,4),(-6.06742144176788,-6.06407799162494,-6.05160770778557,
-6.00076330556691,-5.96719222778308,-5.94807689102041,-5.92856945746908,
-5.8995703315435,-5.85057997654442,-5.82899710278286,-5.81902806230131,
-5.80696228986996,-5.78027118837979,-5.73710895416591,-5.71475719531442,
-5.69583550374847,-5.67549401984022,-5.60968635942604,-5.58652077754147,
-5.58175358782967,-5.57180900202197,-5.55887911052905,-5.49637904783472,
-5.47238928580918,-5.45348687153915,-5.43324397326591,-5.39950525275359,
-5.35704058862313,-5.34277395591618,-5.33828548945826,-5.33648887758617,
-5.32666830212619,-5.31416580357581,-5.2728557190283,-5.22483935773843,
-5.2033237088039,-5.18160982529904,-5.13311289189205,-5.10490957464148,
-5.08647600539771,-5.07543234408859,-5.0575923385754,-5.0075628445441,-4.97321891374844,
-4.95270352679775,-4.92893719400904,-4.88640619473629,-4.84749304142301,
-4.83493609505112,-4.82410817003078,-4.77484054846688,-4.7442803950602,
-4.71927959715428,-4.69896904205886,-4.6682523192502,-4.62113809750946,
-4.60947772126166,-4.60167077129116,-4.58913075191011,-4.57829168340389,
-4.52891485914777,-4.49842542666809,-4.4734554650417,-4.45314155836037,
-4.42235805441496,-4.37533382143012,-4.36368350125133,-4.355880850752,-4.34334529813755,
-4.33071340349779,-4.29197294521198,-4.25693850532766,-4.23010269341009,
-4.20989366375154,-4.18205297665057,-4.16264237328303,-4.12124487055019,
-4.10314752183386,-4.09210538235301,-4.07394167222515,-4.02105879477338,
-3.99729280885844,-3.9754589213058,-3.95661537453561,-3.9197173040692,-3.87331234729695,
-3.86518189673572,-3.85230683702556,-3.8399894035144,-3.79548819927903,
-3.75120170888419,-3.72944395152908,-3.71055657791946,-3.67147810328407,
-3.63454558328402,-3.61333364709922,-3.60218240890063,-3.58653869013744,
-3.53749442901179,-3.51071528190879,-3.48743555124862,-3.46701994167282,
-3.43088401605884,-3.39020056885571,-3.37409474727358,-3.3610273876202,
-3.3488603697357,-3.31192271235755,-3.28450178674414,-3.26047044114872,
-3.23850887037474,-3.21973274028817,-3.18374031448609,-3.14406523957616,
-3.12212052596242,-3.11092497889359,-3.09559144875588,-3.05049171530733,
-3.01297771107997,-2.99143257034414,-2.97188626525704),.UNSPECIFIED.);
#378=B_SPLINE_CURVE_WITH_KNOTS('',3,(#31580,#31581,#31582,#31583,#31584),
 .UNSPECIFIED.,.F.,.F.,(4,1,4),(153.686939606376,153.869245555911,153.9380400259),
 .UNSPECIFIED.);
#379=B_SPLINE_CURVE_WITH_KNOTS('',3,(#31585,#31586,#31587,#31588,#31589,
#31590,#31591,#31592,#31593,#31594,#31595,#31596,#31597,#31598,#31599,#31600,
#31601,#31602,#31603,#31604,#31605,#31606,#31607,#31608,#31609,#31610,#31611,
#31612,#31613,#31614,#31615,#31616,#31617,#31618,#31619,#31620,#31621,#31622,
#31623,#31624,#31625,#31626,#31627,#31628,#31629,#31630,#31631,#31632,#31633,
#31634,#31635,#31636,#31637,#31638,#31639,#31640,#31641,#31642,#31643,#31644,
#31645,#31646,#31647,#31648,#31649,#31650,#31651,#31652,#31653,#31654,#31655,
#31656,#31657,#31658,#31659,#31660,#31661,#31662,#31663,#31664,#31665,#31666,
#31667,#31668,#31669,#31670,#31671,#31672,#31673,#31674,#31675,#31676,#31677,
#31678,#31679,#31680,#31681,#31682,#31683,#31684,#31685,#31686,#31687,#31688,
#31689,#31690,#31691,#31692,#31693,#31694,#31695,#31696,#31697,#31698,#31699,
#31700,#31701,#31702,#31703,#31704,#31705,#31706,#31707,#31708,#31709,#31710,
#31711,#31712,#31713,#31714,#31715,#31716,#31717,#31718,#31719,#31720,#31721,
#31722,#31723,#31724,#31725,#31726,#31727,#31728,#31729,#31730,#31731,#31732,
#31733,#31734,#31735,#31736,#31737,#31738,#31739,#31740,#31741,#31742,#31743,
#31744,#31745,#31746,#31747,#31748,#31749,#31750,#31751,#31752,#31753,#31754,
#31755,#31756,#31757,#31758,#31759,#31760,#31761,#31762,#31763,#31764,#31765,
#31766,#31767,#31768,#31769,#31770,#31771,#31772,#31773,#31774,#31775,#31776,
#31777,#31778,#31779,#31780,#31781,#31782,#31783,#31784,#31785,#31786,#31787,
#31788,#31789,#31790,#31791,#31792,#31793,#31794,#31795,#31796,#31797,#31798,
#31799,#31800,#31801,#31802,#31803,#31804,#31805,#31806,#31807,#31808,#31809,
#31810,#31811,#31812),.UNSPECIFIED.,.F.,.F.,(4,2,2,2,2,2,2,2,2,2,2,2,2,
2,2,2,2,2,2,2,2,2,2,2,2,2,2,2,2,2,2,2,2,2,2,2,2,2,2,2,2,2,2,2,2,2,2,2,2,
2,2,2,2,2,2,2,2,2,2,2,2,2,2,2,2,2,2,2,2,2,2,2,2,2,2,2,2,2,2,2,2,2,2,2,2,
2,2,2,2,2,2,2,2,2,2,2,2,2,2,2,2,2,2,2,2,2,2,2,2,2,2,2,2,4),(-6.19115773559391,
-6.13978402677965,-6.11845966752513,-6.0990275018796,-6.07606680140882,
-5.99291711066576,-5.98007377883281,-5.96801237580815,-5.91817766023449,
-5.88788156212622,-5.86342350784108,-5.86107494362402,-5.85703378075258,
-5.83803868019293,-5.80089496545136,-5.76722987174831,-5.74916122623811,
-5.73519303373494,-5.72354786405738,-5.70060780934709,-5.65388679229046,
-5.63087959595418,-5.61074360855692,-5.59432516089233,-5.55844565038033,
-5.51730921859077,-5.50108613413929,-5.48927295805451,-5.48042478322879,
-5.45976688528121,-5.40954548881871,-5.37821958006577,-5.36485326481983,
-5.3621062805176,-5.33949053368747,-5.30630023981983,-5.26967850719128,
-5.25419972746558,-5.24144121841607,-5.22875057949216,-5.18232796356464,
-5.13985381781297,-5.11811868250635,-5.09888515542233,-5.0406312342978,
-5.01670475292962,-5.00859637825522,-4.9957134100255,-4.98313981773564,
-4.94183385068555,-4.89354733171623,-4.87189944529077,-4.84987193614447,
-4.80456775304053,-4.7746441834212,-4.75556279944509,-4.74440222291625,
-4.72661143052049,-4.67310928877592,-4.64916731580293,-4.62716283816976,
-4.60810515271709,-4.56814577675448,-4.53182291078504,-4.51639688490346,
-4.50366698173267,-4.49094816097923,-4.45235122521209,-4.40442178382397,
-4.38211951728747,-4.36068373226232,-4.32663673283387,-4.28716620084722,
-4.26522711649107,-4.2539424061385,-4.23823778546967,-4.18909294237154,
-4.16222147721896,-4.13881880088144,-4.11816565297058,-4.08057407705395,
-4.02470911137608,-4.01192803929309,-4.00103621165331,-3.95160490125583,
-3.92098364477319,-3.90916136641944,-3.88767507509096,-3.86544363208039,
-3.81681490595078,-3.78948868881414,-3.77134135945358,-3.76018651101403,
-3.74151061919928,-3.68907599710731,-3.6652714035854,-3.64333247501297,
-3.6242358333334,-3.56534626076997,-3.54132426486435,-3.53319589924436,
-3.52029236352149,-3.50773736955315,-3.47501829531416,-3.42674253917791,
-3.40256175490641,-3.38188306686002,-3.34753095942292,-3.30470944677134,
-3.28823161662024,-3.27493919060774,-3.2626926804812,-3.22565993154105,
-3.21930413045193),.UNSPECIFIED.);
#380=B_SPLINE_CURVE_WITH_KNOTS('',3,(#31818,#31819,#31820,#31821,#31822,
#31823,#31824,#31825,#31826,#31827,#31828,#31829,#31830,#31831,#31832,#31833,
#31834,#31835,#31836,#31837,#31838,#31839,#31840,#31841,#31842,#31843,#31844,
#31845,#31846,#31847,#31848,#31849,#31850,#31851,#31852,#31853,#31854,#31855,
#31856,#31857,#31858,#31859,#31860,#31861,#31862,#31863,#31864,#31865,#31866,
#31867,#31868,#31869,#31870,#31871,#31872,#31873,#31874,#31875,#31876,#31877,
#31878,#31879,#31880,#31881,#31882,#31883,#31884,#31885,#31886,#31887,#31888,
#31889,#31890,#31891,#31892,#31893,#31894,#31895,#31896,#31897,#31898,#31899,
#31900,#31901,#31902,#31903,#31904,#31905,#31906,#31907,#31908,#31909,#31910,
#31911,#31912,#31913,#31914,#31915,#31916,#31917,#31918,#31919,#31920,#31921,
#31922,#31923,#31924,#31925,#31926,#31927,#31928,#31929,#31930,#31931,#31932,
#31933,#31934,#31935,#31936,#31937,#31938,#31939,#31940,#31941,#31942,#31943,
#31944,#31945,#31946,#31947,#31948,#31949,#31950,#31951,#31952,#31953,#31954,
#31955,#31956,#31957,#31958,#31959,#31960,#31961,#31962,#31963,#31964,#31965,
#31966,#31967,#31968,#31969,#31970,#31971,#31972,#31973,#31974,#31975,#31976,
#31977,#31978,#31979,#31980,#31981,#31982,#31983,#31984,#31985,#31986,#31987,
#31988,#31989,#31990,#31991,#31992,#31993,#31994,#31995,#31996,#31997,#31998,
#31999,#32000,#32001,#32002,#32003,#32004,#32005,#32006,#32007,#32008,#32009,
#32010,#32011,#32012,#32013,#32014,#32015,#32016,#32017,#32018,#32019,#32020,
#32021,#32022,#32023,#32024,#32025,#32026,#32027,#32028,#32029,#32030,#32031,
#32032,#32033,#32034,#32035,#32036,#32037),.UNSPECIFIED.,.F.,.F.,(4,3,3,
3,3,3,3,3,3,3,3,3,3,3,3,3,3,3,3,3,3,3,3,3,3,3,3,3,3,3,3,3,3,3,3,3,3,3,3,
3,3,3,3,3,3,3,3,3,3,3,3,3,3,3,3,3,3,3,3,3,3,3,3,3,3,3,3,3,3,3,3,3,3,4),
(160.22122533308,160.310313635352,160.399431796454,160.46186308741,160.549717460423,
160.637553952595,160.725393559725,160.813228015068,160.901084065819,160.960735022558,
161.048589395571,161.136425887743,161.224265494873,161.312099950217,161.399956000968,
161.459606957706,161.547461330719,161.635297822891,161.723137430021,161.810971885365,
161.898827936115,161.958478892854,162.046333265867,162.134169758039,162.222009365169,
162.309843820512,162.397699871263,162.457350828002,162.545205201015,162.633041693186,
162.720881300316,162.80871575566,162.89657180641,162.95622276315,163.044077136164,
163.131913628335,163.219753235466,163.307587690809,163.395443741561,163.455094698298,
163.542949071311,163.630785563483,163.718625170613,163.806459625957,163.894315676708,
163.953966633447,164.041821006461,164.129657498632,164.217497105763,164.305331561106,
164.393187611858,164.452838568595,164.540692941608,164.628529433779,164.716369040909,
164.804203496252,164.892059547003,164.951710503743,165.039564876756,165.127401368928,
165.215240976058,165.303075431401,165.390931482152,165.450582438891,165.538436811904,
165.626273304076,165.714112911206,165.801947366549,165.8898034173,165.949454374039,
166.037310852933,166.125147748629,166.212980689828,166.253319805291),
 .UNSPECIFIED.);
#381=B_SPLINE_CURVE_WITH_KNOTS('',3,(#32038,#32039,#32040,#32041,#32042,
#32043,#32044,#32045,#32046,#32047,#32048,#32049),.UNSPECIFIED.,.F.,.F.,
(4,2,2,2,2,4),(-6.19113417191044,-6.17867666764163,-6.16455856974076,-6.10126357361464,
-6.07390768735744,-6.06742144176788),.UNSPECIFIED.);
#382=B_SPLINE_CURVE_WITH_KNOTS('',3,(#32050,#32051,#32052,#32053,#32054,
#32055,#32056,#32057,#32058,#32059,#32060,#32061,#32062,#32063,#32064,#32065,
#32066,#32067,#32068,#32069,#32070,#32071,#32072,#32073,#32074,#32075,#32076,
#32077,#32078,#32079,#32080,#32081,#32082,#32083,#32084,#32085,#32086,#32087,
#32088,#32089,#32090,#32091,#32092,#32093,#32094,#32095,#32096,#32097,#32098,
#32099,#32100,#32101,#32102,#32103,#32104,#32105,#32106,#32107,#32108,#32109,
#32110,#32111,#32112,#32113,#32114,#32115,#32116,#32117,#32118,#32119,#32120,
#32121,#32122,#32123,#32124,#32125,#32126,#32127,#32128,#32129,#32130,#32131,
#32132,#32133,#32134,#32135,#32136,#32137,#32138,#32139,#32140,#32141,#32142,
#32143,#32144,#32145,#32146,#32147,#32148,#32149,#32150,#32151,#32152,#32153,
#32154,#32155,#32156,#32157,#32158,#32159,#32160,#32161,#32162,#32163,#32164,
#32165,#32166,#32167,#32168,#32169,#32170,#32171,#32172,#32173,#32174,#32175,
#32176,#32177,#32178,#32179,#32180,#32181,#32182,#32183,#32184,#32185,#32186,
#32187,#32188,#32189,#32190,#32191,#32192,#32193,#32194,#32195,#32196,#32197,
#32198,#32199,#32200,#32201,#32202,#32203,#32204,#32205,#32206,#32207,#32208,
#32209,#32210,#32211,#32212,#32213,#32214,#32215,#32216,#32217,#32218,#32219,
#32220,#32221,#32222,#32223,#32224,#32225,#32226,#32227,#32228,#32229,#32230,
#32231,#32232,#32233,#32234,#32235,#32236,#32237,#32238,#32239,#32240,#32241,
#32242,#32243,#32244,#32245,#32246,#32247,#32248,#32249,#32250,#32251,#32252,
#32253,#32254,#32255,#32256,#32257,#32258,#32259,#32260,#32261,#32262,#32263,
#32264,#32265,#32266,#32267,#32268,#32269,#32270,#32271,#32272,#32273,#32274,
#32275,#32276,#32277,#32278,#32279,#32280,#32281,#32282,#32283,#32284,#32285,
#32286,#32287,#32288,#32289,#32290,#32291),.UNSPECIFIED.,.F.,.F.,(4,2,2,
2,2,2,2,2,2,2,2,2,2,2,2,2,2,2,2,2,2,2,2,2,2,2,2,2,2,2,2,2,2,2,2,2,2,2,2,
2,2,2,2,2,2,2,2,2,2,2,2,2,2,2,2,2,2,2,2,2,2,2,2,2,2,2,2,2,2,2,2,2,2,2,2,
2,2,2,2,2,2,2,2,2,2,2,2,2,2,2,2,2,2,2,2,2,2,2,2,2,2,2,2,2,2,2,2,2,2,2,2,
2,2,2,2,2,2,2,2,2,4),(-3.21930413045193,-3.19821895702288,-3.1740881861233,
-3.1519934702773,-3.1329861388801,-3.09559741316757,-3.04683547256862,-3.03143132293309,
-3.02120633601416,-3.00026928727761,-2.96446516427597,-2.93768636476454,
-2.91244968626192,-2.89213357025697,-2.86111608945007,-2.81330751301519,
-2.79133621896855,-2.77988541746673,-2.76526543280403,-2.74617026192556,
-2.69184569051622,-2.66658055460417,-2.64626772712302,-2.61531223093145,
-2.56773633213867,-2.54556295825083,-2.53408142612529,-2.51955946629205,
-2.46641694638413,-2.43300380847211,-2.41376926903898,-2.39203579458847,
-2.37993361341199,-2.32203045081919,-2.29996395133401,-2.28941826765291,
-2.27594253337349,-2.2591154343958,-2.21384971782128,-2.18154667171162,
-2.16098281960491,-2.13616004489249,-2.12154549557563,-2.06937050746921,
-2.05046942519298,-2.03931198757433,-2.02136752202807,-2.00758778652186,
-1.93815840565377,-1.91751807187727,-1.89407566259905,-1.86609039132995,
-1.81731372016487,-1.801893056179,-1.79167104624693,-1.77077235955525,-1.73510062345755,
-1.69357588818809,-1.67461739439505,-1.65242889811755,-1.62810177210808,
-1.57594166010619,-1.55801231759893,-1.5468545775697,-1.52793599538702,
-1.49848062143119,-1.45228775512562,-1.43030118330118,-1.40861791109259,
-1.3572671430483,-1.31987151883562,-1.30702725153194,-1.29441828303544,
-1.28657514925565,-1.27486898677441,-1.22755557403127,-1.19682110045702,
-1.17633679789597,-1.15083804491047,-1.1193016169689,-1.0753713497353,-1.06194408206572,
-1.04978857394223,-1.0103349893949,-0.959570909841802,-0.93779757711804,
-0.91590899529176,-0.871692638480005,-0.826795365771362,-0.814428911222402,
-0.80524774805795,-0.791748796936568,-0.764859027120126,-0.71174609356172,
-0.690751040529247,-0.670654640740498,-0.666798279841583,-0.64132396660455,
-0.591359115583464,-0.574164225752605,-0.568787224730732,-0.557576671645744,
-0.542983964486431,-0.511066242008585,-0.465564162968799,-0.444623014070843,
-0.430780768429424,-0.39612072132774,-0.346037043878999,-0.328319812056502,
-0.325871641634217,-0.32377308942613,-0.321547822994558,-0.316047485152077,
-0.295953959524207,-0.261702867484532,-0.218977449536296,-0.198162881597824,
-0.179620600092242,-0.128417530992846,-0.123769554268864),.UNSPECIFIED.);
#383=B_SPLINE_CURVE_WITH_KNOTS('',3,(#32297,#32298,#32299,#32300,#32301,
#32302,#32303,#32304,#32305,#32306,#32307,#32308,#32309,#32310,#32311,#32312),
 .UNSPECIFIED.,.F.,.F.,(4,1,1,1,1,1,1,1,1,1,1,1,1,4),(166.504410682989,
166.947198244335,167.446070179483,167.944942114632,168.44381404978,168.942685984928,
169.441557920076,169.940429855224,170.439301790372,170.93817372552,171.437045660668,
171.935917595817,172.434789530965,172.536539600894),.UNSPECIFIED.);
#384=B_SPLINE_CURVE_WITH_KNOTS('',3,(#32313,#32314,#32315,#32316,#32317,
#32318,#32319,#32320,#32321,#32322,#32323,#32324,#32325),.UNSPECIFIED.,
 .F.,.F.,(4,3,3,3,4),(166.253319805291,166.341154624617,166.429008307032,
166.448326309187,166.504410640259),.UNSPECIFIED.);
#385=B_SPLINE_CURVE_WITH_KNOTS('',3,(#32327,#32328,#32329,#32330,#32331,
#32332,#32333,#32334,#32335,#32336,#32337,#32338),.UNSPECIFIED.,.F.,.F.,
(4,2,2,2,2,4),(-0.123769554268864,-0.0900669150748557,-0.0773253769985558,
-0.0674267057802843,-0.0538731003174174,-7.62332589639553E-5),
 .UNSPECIFIED.);
#386=B_SPLINE_CURVE_WITH_KNOTS('',3,(#32339,#32340,#32341,#32342,#32343,
#32344,#32345,#32346,#32347,#32348,#32349,#32350,#32351,#32352,#32353,#32354,
#32355,#32356,#32357,#32358,#32359,#32360,#32361,#32362,#32363,#32364,#32365,
#32366,#32367,#32368,#32369,#32370,#32371,#32372,#32373,#32374,#32375,#32376,
#32377,#32378,#32379,#32380,#32381,#32382,#32383,#32384,#32385,#32386,#32387,
#32388,#32389,#32390,#32391,#32392,#32393,#32394,#32395,#32396,#32397,#32398,
#32399,#32400,#32401,#32402,#32403,#32404,#32405,#32406,#32407,#32408,#32409,
#32410,#32411,#32412,#32413,#32414,#32415,#32416,#32417,#32418,#32419,#32420,
#32421,#32422,#32423,#32424,#32425,#32426,#32427,#32428,#32429,#32430,#32431,
#32432,#32433,#32434,#32435,#32436,#32437,#32438,#32439,#32440,#32441,#32442,
#32443,#32444,#32445,#32446,#32447,#32448,#32449,#32450,#32451,#32452,#32453,
#32454,#32455,#32456,#32457,#32458,#32459,#32460,#32461,#32462,#32463,#32464,
#32465,#32466,#32467,#32468,#32469,#32470,#32471,#32472,#32473,#32474,#32475,
#32476,#32477,#32478,#32479,#32480,#32481,#32482,#32483,#32484,#32485,#32486,
#32487,#32488,#32489,#32490,#32491,#32492,#32493,#32494,#32495,#32496,#32497,
#32498,#32499,#32500,#32501,#32502,#32503,#32504,#32505,#32506,#32507,#32508,
#32509,#32510,#32511,#32512,#32513,#32514,#32515,#32516,#32517,#32518,#32519,
#32520,#32521,#32522,#32523,#32524,#32525,#32526,#32527,#32528,#32529,#32530,
#32531,#32532,#32533,#32534,#32535,#32536,#32537,#32538,#32539,#32540,#32541,
#32542,#32543,#32544,#32545,#32546,#32547,#32548,#32549,#32550,#32551,#32552,
#32553,#32554,#32555,#32556,#32557,#32558,#32559,#32560,#32561,#32562,#32563,
#32564,#32565,#32566,#32567,#32568,#32569,#32570,#32571,#32572,#32573,#32574,
#32575,#32576,#32577,#32578,#32579,#32580,#32581,#32582,#32583,#32584,#32585,
#32586,#32587,#32588,#32589,#32590,#32591,#32592,#32593,#32594,#32595,#32596,
#32597,#32598),.UNSPECIFIED.,.F.,.F.,(4,2,2,2,2,2,2,2,2,2,2,2,2,2,2,2,2,
2,2,2,2,2,2,2,2,2,2,2,2,2,2,2,2,2,2,2,2,2,2,2,2,2,2,2,2,2,2,2,2,2,2,2,2,
2,2,2,2,2,2,2,2,2,2,2,2,2,2,2,2,2,2,2,2,2,2,2,2,2,2,2,2,2,2,2,2,2,2,2,2,
2,2,2,2,2,2,2,2,2,2,2,2,2,2,2,2,2,2,2,2,2,2,2,2,2,2,2,2,2,2,2,2,2,2,2,2,
2,2,2,2,4),(-6.1913800756723,-6.17067857718631,-6.15416759396204,-6.13512852001715,
-6.10714964374355,-6.04949551586851,-6.03016362183847,-6.01891967319071,
-6.00326796720119,-5.9541618387972,-5.92723006119227,-5.9041552920683,-5.90175032429661,
-5.88091883462017,-5.82232469085236,-5.79816404507313,-5.79259327439422,
-5.78840635509426,-5.77651128602982,-5.76362237081052,-5.72658443180081,
-5.69074538006163,-5.66960789853106,-5.65123335961385,-5.62847837269773,
-5.56646749327657,-5.54762456604348,-5.54638106722991,-5.54560174635282,
-5.54414922599148,-5.54291199349935,-5.54183560207732,-5.5408773061103,
-5.54000233814295,-5.53918073069057,-5.53838420729294,-5.53758236675965,
-5.53673646997048,-5.53578598822348,-5.53424078005765,-5.52991557134065,
-5.52547020566476,-5.50737944103455,-5.45424216161364,-5.4303460820723,
-5.41043944490215,-5.39131931290488,-5.39024351151347,-5.38856761065132,
-5.34888773452981,-5.31293204660583,-5.29195093702676,-5.2817224014293,
-5.26633671237753,-5.21759302961125,-5.19016622191713,-5.16650270514723,
-5.14592661328751,-5.10977215236485,-5.06892497233756,-5.05274646572066,
-5.03961231014794,-5.02891469557269,-5.00815101840954,-4.94965303077316,
-4.93753247773549,-4.91578209106171,-4.89386788213271,-4.84622927994932,
-4.8056498008151,-4.79298812978226,-4.78019886188033,-4.74232040976024,
-4.69119755090187,-4.66953995633978,-4.64752228027722,-4.60197564536534,
-4.5721788437998,-4.55314101734022,-4.54198091638866,-4.52415253447887,
-4.47069445505799,-4.44675754364414,-4.42475514701808,-4.40569524574346,
-4.36567533494732,-4.32940011302846,-4.31398225156481,-4.30125663949336,
-4.29032934966841,-4.26252823900804,-4.21151367579109,-4.1994718185711,
-4.17779162477969,-4.15580010543284,-4.10968485517058,-4.06805641973549,
-4.05533418150158,-4.04260688149864,-4.01564954458518,-4.00940163958921,
-3.96100578953942,-3.93719704781849,-3.91642765587057,-3.88046774871173,
-3.83941443783963,-3.82320390186537,-3.81005273822562,-3.79770180725745,
-3.76135166735944,-3.71256196703528,-3.68957869611001,-3.66876907117997,
-3.60481092107409,-3.57358766112734,-3.56175491713929,-3.54773833002112,
-3.48902368787403,-3.46438518463211,-3.44204691870484,-3.42063479565248,
-3.36393472581923,-3.33931306298977,-3.33106022321823,-3.31802873891789,
-3.30558273082634,-3.27667549062873,-3.23535869043582,-3.22158689325656,
-3.21942130955984),.UNSPECIFIED.);
#387=B_SPLINE_CURVE_WITH_KNOTS('',3,(#32604,#32605,#32606,#32607,#32608,
#32609,#32610,#32611,#32612,#32613,#32614,#32615,#32616,#32617,#32618,#32619,
#32620,#32621,#32622,#32623,#32624,#32625,#32626,#32627,#32628,#32629,#32630,
#32631,#32632,#32633,#32634,#32635,#32636,#32637,#32638,#32639,#32640,#32641,
#32642,#32643,#32644,#32645,#32646,#32647,#32648,#32649,#32650,#32651,#32652,
#32653,#32654,#32655,#32656,#32657,#32658,#32659,#32660,#32661,#32662,#32663,
#32664,#32665,#32666,#32667,#32668,#32669,#32670,#32671,#32672,#32673,#32674,
#32675,#32676,#32677,#32678,#32679,#32680,#32681,#32682,#32683,#32684,#32685,
#32686,#32687,#32688,#32689,#32690,#32691,#32692,#32693,#32694,#32695,#32696,
#32697,#32698,#32699,#32700,#32701,#32702,#32703,#32704,#32705,#32706,#32707,
#32708,#32709,#32710,#32711,#32712,#32713,#32714,#32715,#32716,#32717,#32718,
#32719,#32720,#32721,#32722,#32723,#32724,#32725,#32726,#32727,#32728,#32729,
#32730,#32731,#32732,#32733,#32734,#32735,#32736,#32737,#32738,#32739,#32740,
#32741,#32742,#32743,#32744,#32745,#32746,#32747,#32748,#32749,#32750,#32751,
#32752,#32753,#32754,#32755,#32756,#32757,#32758,#32759,#32760,#32761,#32762,
#32763,#32764,#32765,#32766,#32767,#32768,#32769,#32770,#32771,#32772,#32773,
#32774,#32775,#32776,#32777,#32778,#32779,#32780,#32781,#32782,#32783,#32784,
#32785,#32786,#32787,#32788,#32789,#32790,#32791,#32792,#32793,#32794,#32795,
#32796,#32797,#32798,#32799,#32800,#32801,#32802,#32803,#32804,#32805,#32806,
#32807,#32808,#32809,#32810,#32811,#32812,#32813,#32814,#32815,#32816,#32817,
#32818,#32819,#32820,#32821,#32822,#32823),.UNSPECIFIED.,.F.,.F.,(4,2,2,
2,2,2,2,2,2,2,2,2,2,2,2,2,2,2,2,2,2,2,2,2,2,2,2,2,2,2,2,2,2,2,2,2,2,2,2,
2,2,2,2,2,2,2,2,2,2,2,2,2,2,2,2,2,2,2,2,2,2,2,2,2,2,2,2,2,2,2,2,2,2,2,2,
2,2,2,2,2,2,2,2,2,2,2,2,2,2,2,2,2,2,2,2,2,2,2,2,2,2,2,2,2,2,2,2,2,2,4),
(-2.97195484317244,-2.91662865217212,-2.89779221698913,-2.87594479156734,
-2.85215060598283,-2.79905544977423,-2.78106326611344,-2.77002065265098,
-2.7517486240445,-2.73748038139496,-2.66972738674698,-2.6491998397412,-2.62625341290914,
-2.59390865768494,-2.54197864914045,-2.52956362206813,-2.51680173438993,
-2.50878119052095,-2.46264847549782,-2.42524660827217,-2.40637878873055,
-2.38458711743793,-2.36090899197926,-2.30871011669473,-2.28996549946835,
-2.27891731577259,-2.26135111404435,-2.23544820546775,-2.18200971160627,
-2.16056977046165,-2.1387703544922,-2.11507608882696,-2.06275361780042,
-2.04411467823821,-2.03306830190307,-2.01541151946985,-1.9728240407116,
-1.93950174847006,-1.91725144382443,-1.89613997842978,-1.84770133637917,
-1.80460126619897,-1.79219587904024,-1.77942312916082,-1.77139207655314,
-1.72523337505143,-1.68788293721545,-1.66901702230384,-1.64722202762939,
-1.62353698445096,-1.57128523117997,-1.55258587518402,-1.54153849804936,
-1.52393379733011,-1.48166566028458,-1.46176028522242,-1.43418643718348,
-1.41397977858964,-1.38690224658569,-1.35123440070221,-1.31401172667698,
-1.30122886059127,-1.28883238235635,-1.24607249403879,-1.20074254928594,
-1.17886479364796,-1.15749005008917,-1.10922404672469,-1.06745082707563,
-1.05497192320139,-1.04228006357283,-1.00206336059066,-0.954507144778013,
-0.932740322302675,-0.911271940373778,-0.899361565372025,-0.843774282387121,
-0.819627100938718,-0.807903970736283,-0.794527822711242,-0.777573886003473,
-0.73102092646425,-0.699886005324059,-0.681165044986464,-0.657655465997681,
-0.629931284744476,-0.574054015278958,-0.563335241104719,-0.552329466851587,
-0.538041984434196,-0.507398355324752,-0.459860792167081,-0.439130301418296,
-0.428613625985288,-0.400430174505115,-0.360037447653399,-0.329402162777094,
-0.317179450594455,-0.314098720290468,-0.301074285541704,-0.282409168565291,
-0.221416972947329,-0.198456539095972,-0.181117596885108,-0.151828055013685,
-0.106403764995796,-0.082256284976266,-0.0705396952843348,-0.060451715834582,
-4.22977414189134E-5),.UNSPECIFIED.);
#388=B_SPLINE_CURVE_WITH_KNOTS('',3,(#32824,#32825,#32826,#32827),
 .UNSPECIFIED.,.F.,.F.,(4,4),(172.536539600894,172.787595947439),
 .UNSPECIFIED.);
#389=B_SPLINE_CURVE_WITH_KNOTS('',3,(#32828,#32829,#32830,#32831,#32832,
#32833,#32834,#32835,#32836,#32837,#32838,#32839,#32840,#32841,#32842,#32843,
#32844,#32845,#32846,#32847,#32848,#32849,#32850,#32851,#32852,#32853,#32854,
#32855,#32856,#32857,#32858,#32859,#32860,#32861,#32862,#32863,#32864,#32865,
#32866,#32867,#32868,#32869,#32870,#32871,#32872,#32873,#32874,#32875,#32876,
#32877,#32878,#32879,#32880,#32881,#32882,#32883,#32884,#32885,#32886,#32887,
#32888,#32889,#32890,#32891,#32892,#32893,#32894,#32895,#32896,#32897,#32898,
#32899,#32900,#32901,#32902,#32903,#32904,#32905,#32906,#32907,#32908,#32909,
#32910,#32911,#32912,#32913,#32914,#32915,#32916,#32917,#32918,#32919,#32920,
#32921,#32922,#32923,#32924,#32925,#32926,#32927,#32928,#32929,#32930,#32931,
#32932,#32933,#32934,#32935,#32936,#32937,#32938,#32939,#32940,#32941,#32942,
#32943,#32944,#32945,#32946,#32947,#32948,#32949,#32950,#32951,#32952,#32953,
#32954,#32955,#32956,#32957,#32958,#32959,#32960,#32961,#32962,#32963,#32964,
#32965,#32966,#32967,#32968,#32969,#32970,#32971,#32972,#32973,#32974,#32975,
#32976,#32977,#32978,#32979,#32980,#32981,#32982,#32983,#32984,#32985,#32986,
#32987,#32988,#32989,#32990,#32991,#32992,#32993,#32994,#32995,#32996,#32997,
#32998,#32999,#33000,#33001,#33002,#33003,#33004,#33005,#33006,#33007,#33008,
#33009,#33010,#33011,#33012,#33013,#33014,#33015,#33016,#33017,#33018,#33019,
#33020,#33021,#33022,#33023,#33024,#33025,#33026,#33027,#33028,#33029,#33030,
#33031,#33032,#33033,#33034,#33035,#33036,#33037,#33038,#33039,#33040,#33041,
#33042,#33043,#33044,#33045,#33046,#33047,#33048,#33049,#33050,#33051,#33052,
#33053,#33054,#33055,#33056,#33057,#33058,#33059,#33060,#33061,#33062,#33063,
#33064,#33065),.UNSPECIFIED.,.F.,.F.,(4,2,2,2,2,2,2,2,2,2,2,2,2,2,2,2,2,
2,2,2,2,2,2,2,2,2,2,2,2,2,2,2,2,2,2,2,2,2,2,2,2,2,2,2,2,2,2,2,2,2,2,2,2,
2,2,2,2,2,2,2,2,2,2,2,2,2,2,2,2,2,2,2,2,2,2,2,2,2,2,2,2,2,2,2,2,2,2,2,2,
2,2,2,2,2,2,2,2,2,2,2,2,2,2,2,2,2,2,2,2,2,2,2,2,2,2,2,2,2,4),(-3.21942130955984,
-3.19833034902414,-3.17762650184267,-3.11014558210518,-3.09569482555007,
-3.07724916805604,-3.06609500473019,-3.04772563408401,-3.03337871304127,
-2.96560766923414,-2.94491326891506,-2.92162994646329,-2.89501200012371,
-2.83721000537578,-2.82493793371155,-2.81168045364214,-2.79526946799109,
-2.7528974110563,-2.71852469058027,-2.69777890558541,-2.6738800190411,-2.62551292942305,
-2.59292091621499,-2.58003781907883,-2.5674635852813,-2.55965443733128,
-2.51294691049226,-2.47503133312629,-2.45602321221816,-2.43392820613057,
-2.40979720657546,-2.38235965182285,-2.34530555043866,-2.33306108011966,
-2.31976479713902,-2.30328023260175,-2.26041272529873,-2.22610225845176,
-2.20542538814414,-2.18123232240695,-2.13295540228018,-2.10023758091653,
-2.08769067776905,-2.07477717223001,-2.06663937837715,-2.04257261261481,
-1.99812205184573,-1.97287079271416,-1.95240375822785,-1.92206771980915,
-1.8767425879191,-1.8525526563831,-1.84175021003303,-1.82881587347761,-1.82065782583839,
-1.77411730159096,-1.73715011494937,-1.7181649032282,-1.69602695193314,
-1.67180607480177,-1.62033308541774,-1.6018051179295,-1.59065081345178,
-1.57236217177524,-1.55812441006771,-1.4900405960124,-1.46935626724098,
-1.44604437067114,-1.41528159096145,-1.361537654392,-1.34932643446531,-1.33598224872465,
-1.31940661575981,-1.27591647674414,-1.24524050748075,-1.22626532657779,
-1.20410813625716,-1.17984700049751,-1.129196340505,-1.11023378431642,-1.09907506196553,
-1.08118283430355,-1.03344588593146,-1.00061233862785,-0.981429639534398,
-0.959621818298641,-0.91488093336989,-0.870203057459326,-0.857821549539762,
-0.847825809514792,-0.83385618869784,-0.80489481561337,-0.757722448334184,
-0.736150077867063,-0.716967031380558,-0.694876289140778,-0.653843929106904,
-0.624085478754477,-0.611777995185696,-0.601755623568807,-0.587685246213096,
-0.558263117562371,-0.512003339023885,-0.490384880343963,-0.471190597845841,
-0.449150973801902,-0.408412683162301,-0.378046386433222,-0.365784706658776,
-0.355744957157113,-0.341609329660175,-0.311885359069004,-0.26620747556139,
-0.24456176447186,-0.225360727470203,-0.203350675080102,-0.162781426989361,
-0.132226410056128,-0.123804338336763),.UNSPECIFIED.);
#390=B_SPLINE_CURVE_WITH_KNOTS('',3,(#33070,#33071,#33072,#33073,#33074,
#33075,#33076,#33077,#33078,#33079,#33080,#33081,#33082,#33083,#33084,#33085,
#33086,#33087,#33088,#33089,#33090,#33091,#33092,#33093,#33094,#33095,#33096,
#33097,#33098,#33099,#33100,#33101,#33102,#33103,#33104,#33105,#33106,#33107,
#33108,#33109,#33110,#33111,#33112,#33113,#33114,#33115,#33116,#33117,#33118,
#33119,#33120,#33121,#33122,#33123,#33124,#33125,#33126,#33127,#33128,#33129,
#33130,#33131,#33132,#33133,#33134,#33135,#33136,#33137,#33138,#33139,#33140,
#33141,#33142,#33143,#33144,#33145,#33146,#33147,#33148,#33149,#33150,#33151,
#33152,#33153,#33154,#33155,#33156,#33157,#33158,#33159,#33160,#33161,#33162,
#33163,#33164,#33165,#33166,#33167,#33168,#33169,#33170,#33171,#33172,#33173,
#33174,#33175,#33176,#33177,#33178,#33179,#33180,#33181,#33182,#33183,#33184,
#33185,#33186,#33187,#33188,#33189,#33190,#33191,#33192,#33193,#33194,#33195,
#33196,#33197,#33198,#33199,#33200,#33201,#33202,#33203,#33204,#33205,#33206,
#33207,#33208,#33209,#33210,#33211,#33212,#33213,#33214,#33215,#33216,#33217,
#33218,#33219,#33220,#33221,#33222,#33223,#33224,#33225,#33226,#33227,#33228,
#33229,#33230,#33231,#33232,#33233,#33234,#33235,#33236,#33237,#33238,#33239,
#33240,#33241,#33242,#33243,#33244,#33245,#33246,#33247,#33248,#33249,#33250,
#33251,#33252,#33253,#33254,#33255,#33256,#33257,#33258,#33259,#33260,#33261,
#33262,#33263,#33264,#33265,#33266,#33267,#33268,#33269,#33270,#33271,#33272,
#33273,#33274,#33275,#33276,#33277,#33278,#33279,#33280,#33281,#33282,#33283,
#33284,#33285,#33286,#33287,#33288,#33289,#33290,#33291,#33292,#33293,#33294,
#33295,#33296,#33297,#33298,#33299,#33300,#33301,#33302,#33303,#33304,#33305,
#33306,#33307,#33308,#33309,#33310,#33311,#33312,#33313,#33314,#33315),
 .UNSPECIFIED.,.F.,.F.,(4,2,2,2,2,2,2,2,2,2,2,2,2,2,2,2,2,2,2,2,2,2,2,2,
2,2,2,2,2,2,2,2,2,2,2,2,2,2,2,2,2,2,2,2,2,2,2,2,2,2,2,2,2,2,2,2,2,2,2,2,
2,2,2,2,2,2,2,2,2,2,2,2,2,2,2,2,2,2,2,2,2,2,2,2,2,2,2,2,2,2,2,2,2,2,2,2,
2,2,2,2,2,2,2,2,2,2,2,2,2,2,2,2,2,2,2,2,2,2,2,2,2,2,4),(-6.06755362652627,
-6.05425213686216,-5.9830849064687,-5.97100646247755,-5.95853702788697,
-5.91659712697962,-5.88305907004699,-5.85702045100482,-5.84855013099762,
-5.82969106017962,-5.7924834923253,-5.75408554743836,-5.73834870448597,
-5.73452601656187,-5.72349912521049,-5.7097978339891,-5.65078453704456,
-5.62619702201709,-5.6066925109695,-5.58652066833823,-5.55160551748355,
-5.50960878495049,-5.49330134107481,-5.49187061051971,-5.49063994836124,
-5.48955783087141,-5.4798368380119,-5.46771796605209,-5.43677943629094,
-5.39653843997406,-5.37468534001023,-5.35780925693728,-5.35364812642821,
-5.35148633634693,-5.34972684243515,-5.32507578582433,-5.2850888196536,
-5.24601825658349,-5.23345793716701,-5.22263263999495,-5.17340527152829,
-5.13194098576691,-5.1103917655996,-5.09136874074132,-5.03288512778012,
-5.00899166129382,-5.00090619171659,-4.98807745525644,-4.97572097278534,
-4.91136805628013,-4.88751284202727,-4.86563608459446,-4.84426115498006,
-4.78778877308601,-4.76349354303907,-4.75532434027678,-4.74240946153522,
-4.73178958167123,-4.70808231781952,-4.66228049337883,-4.63189861927627,
-4.61160464059256,-4.5864433476347,-4.53224368943837,-4.5188754785911,-4.50128533226249,
-4.49023781017001,-4.47152197139837,-4.41929397560244,-4.39561291713768,
-4.37381979560172,-4.35495310812868,-4.31758174580036,-4.27143105421713,
-4.26340383082188,-4.25063520083035,-4.23822640838169,-4.19519250236425,
-4.14862933391866,-4.12711898315795,-4.10539947610897,-4.05523825915691,
-4.02808240191872,-4.01003595941011,-3.99899371405451,-3.98077824729366,
-3.92795755726902,-3.9041995660234,-3.8823695079746,-3.86352379150114,-3.82572158929199,
-3.77969221120906,-3.76315172386917,-3.7520543681746,-3.73246730981183,
-3.70172711863458,-3.65794559996691,-3.63623187939583,-3.61471603975411,
-3.56193593522228,-3.53583988310811,-3.51819846644601,-3.5071518829171,
-3.48849548200209,-3.4369094832764,-3.41297573958261,-3.39106111371404,
-3.36971608113663,-3.30554325202029,-3.29119801646875,-3.27286929933081,
-3.26182644329393,-3.24388854271475,-3.19073131063413,-3.16692998891198,
-3.14507904537909,-3.12624470346781,-3.09565257879225,-3.03654123665552,
-3.02289998470606,-3.01108952204565,-2.97861413531433,-2.97195484317244),
 .UNSPECIFIED.);
#391=B_SPLINE_CURVE_WITH_KNOTS('',3,(#33317,#33318,#33319,#33320,#33321,
#33322,#33323,#33324,#33325,#33326,#33327,#33328),.UNSPECIFIED.,.F.,.F.,
(4,2,2,2,2,4),(-0.123804338336763,-0.119935359050831,-0.109906915523079,
-0.0958135679357499,-0.0198720624599457,-8.03630370901633E-5),
 .UNSPECIFIED.);
#392=B_SPLINE_CURVE_WITH_KNOTS('',3,(#33329,#33330,#33331,#33332,#33333,
#33334,#33335,#33336,#33337,#33338,#33339,#33340,#33341,#33342,#33343,#33344),
 .UNSPECIFIED.,.F.,.F.,(4,1,1,1,1,1,1,1,1,1,1,1,1,4),(179.070781254618,
179.325193015128,179.824329239818,180.323465464509,180.822601689199,181.32173791389,
181.82087413858,182.320010363271,182.819146587961,183.318282812652,183.817419037342,
184.316555262033,184.815691486723,185.102873615134),.UNSPECIFIED.);
#393=B_SPLINE_CURVE_WITH_KNOTS('',3,(#33347,#33348,#33349,#33350,#33351),
 .UNSPECIFIED.,.F.,.F.,(4,1,4),(185.102873615134,185.314827711414,185.353966561798),
 .UNSPECIFIED.);
#394=B_SPLINE_CURVE_WITH_KNOTS('',3,(#33353,#33354,#33355,#33356,#33357,
#33358,#33359,#33360,#33361,#33362,#33363,#33364,#33365,#33366,#33367,#33368,
#33369,#33370,#33371,#33372,#33373,#33374,#33375,#33376,#33377,#33378,#33379,
#33380,#33381,#33382,#33383,#33384,#33385,#33386,#33387,#33388,#33389,#33390,
#33391,#33392,#33393,#33394,#33395,#33396,#33397,#33398,#33399,#33400,#33401,
#33402,#33403,#33404,#33405,#33406,#33407,#33408,#33409,#33410,#33411,#33412,
#33413,#33414,#33415,#33416,#33417,#33418,#33419,#33420,#33421,#33422,#33423,
#33424,#33425,#33426,#33427,#33428,#33429,#33430,#33431,#33432,#33433,#33434,
#33435,#33436,#33437,#33438,#33439,#33440,#33441,#33442,#33443,#33444,#33445,
#33446,#33447,#33448,#33449,#33450,#33451,#33452,#33453,#33454,#33455,#33456,
#33457,#33458,#33459,#33460,#33461,#33462,#33463,#33464,#33465,#33466,#33467,
#33468,#33469,#33470,#33471,#33472,#33473,#33474,#33475,#33476,#33477,#33478,
#33479,#33480,#33481,#33482,#33483,#33484,#33485,#33486,#33487,#33488,#33489,
#33490,#33491,#33492,#33493,#33494,#33495,#33496,#33497,#33498,#33499,#33500,
#33501,#33502,#33503,#33504,#33505,#33506,#33507,#33508,#33509,#33510,#33511,
#33512,#33513,#33514,#33515,#33516,#33517,#33518,#33519,#33520,#33521,#33522,
#33523,#33524,#33525,#33526,#33527,#33528,#33529,#33530,#33531,#33532,#33533,
#33534,#33535,#33536,#33537,#33538,#33539,#33540,#33541,#33542,#33543,#33544,
#33545,#33546,#33547,#33548,#33549,#33550,#33551,#33552,#33553,#33554,#33555,
#33556,#33557,#33558,#33559,#33560,#33561,#33562,#33563),.UNSPECIFIED.,
 .F.,.F.,(4,3,3,3,3,3,3,3,3,3,3,3,3,3,3,3,3,3,3,3,3,3,3,3,3,3,3,3,3,3,3,
3,3,3,3,3,3,3,3,3,3,3,3,3,3,3,3,3,3,3,3,3,3,3,3,3,3,3,3,3,3,3,3,3,3,3,3,
3,3,3,4),(185.353966567087,185.441561764946,185.529139524043,185.616720093993,
185.704298367222,185.791896369604,185.813963936104,185.901816358879,185.989650873403,
186.077488504696,186.165320973144,186.25317509779,186.313100160795,186.400954277281,
186.488790493292,186.576629820951,186.664463978937,186.75231976687,186.812236385486,
186.900086650938,186.987919001855,187.07575448145,187.163584809882,187.251436832492,
187.311372610176,187.399229623174,187.487068740212,187.57491094705,187.662747965263,
187.750606557437,187.810508834867,187.898357394128,187.986188047343,188.074021858677,
188.161850539207,188.249700960886,188.309645059557,188.397496885361,188.485330768919,
188.573167724538,188.660999493881,188.748852889323,188.808781284248,188.896654168151,
188.984509272561,189.072367483231,189.160220476904,189.248094852537,189.307917508938,
189.395705498216,189.483475293582,189.571248411567,189.659016630357,189.746807507752,
189.807053733629,189.895056832682,189.983042532751,190.071030596453,190.159012711986,
190.247013862932,190.306189958319,190.393765197248,190.481322162753,190.568884375155,
190.656443223482,190.74402903841,190.80532618301,190.893910047384,190.982472415762,
191.071025137546,191.135001724242),.UNSPECIFIED.);
#395=B_SPLINE_CURVE_WITH_KNOTS('',3,(#33567,#33568,#33569,#33570,#33571,
#33572,#33573,#33574,#33575,#33576,#33577,#33578,#33579,#33580,#33581,#33582,
#33583,#33584,#33585,#33586,#33587,#33588,#33589,#33590,#33591,#33592,#33593,
#33594,#33595,#33596,#33597,#33598,#33599,#33600,#33601,#33602,#33603,#33604,
#33605,#33606,#33607,#33608,#33609,#33610,#33611,#33612,#33613,#33614,#33615,
#33616,#33617,#33618,#33619,#33620,#33621,#33622,#33623,#33624,#33625,#33626,
#33627,#33628,#33629,#33630,#33631,#33632,#33633,#33634,#33635,#33636,#33637,
#33638,#33639,#33640,#33641,#33642,#33643,#33644,#33645,#33646,#33647,#33648,
#33649,#33650,#33651,#33652,#33653,#33654,#33655,#33656,#33657,#33658,#33659,
#33660,#33661,#33662,#33663,#33664,#33665,#33666,#33667,#33668,#33669,#33670,
#33671,#33672,#33673,#33674,#33675,#33676,#33677,#33678,#33679,#33680,#33681,
#33682,#33683,#33684,#33685,#33686,#33687,#33688,#33689,#33690,#33691,#33692,
#33693,#33694,#33695,#33696,#33697,#33698,#33699,#33700,#33701,#33702,#33703,
#33704,#33705,#33706,#33707,#33708,#33709,#33710,#33711,#33712,#33713,#33714,
#33715,#33716,#33717,#33718,#33719,#33720,#33721,#33722,#33723,#33724,#33725,
#33726,#33727,#33728,#33729,#33730,#33731,#33732),.UNSPECIFIED.,.F.,.F.,
(4,3,3,3,3,3,3,3,3,3,3,3,3,3,3,3,3,3,3,3,3,3,3,3,3,3,3,3,3,3,3,3,3,3,3,
3,3,3,3,3,3,3,3,3,3,3,3,3,3,3,3,3,3,3,3,4),(185.353966561798,185.405459844816,
185.493311626503,185.581145518636,185.668982538294,185.756814419245,185.844667939728,
185.904331779964,185.99219028366,186.080030916271,186.167874637635,186.25571318292,
186.343573248018,186.403203715112,186.491053804869,186.578886013568,186.666721379097,
186.754551626175,186.842403559431,186.90207565026,186.989928966623,187.077764365727,
187.165602836015,187.253436132681,187.341291001396,187.400947585408,187.488821955081,
187.576678569885,187.664538289577,187.752392804605,187.840268647382,187.899819520556,
187.987609134066,188.075380579373,188.163155346114,188.250925226068,188.338717707918,
188.398691455705,188.486695776435,188.574682721781,188.662672030794,188.750655404904,
188.838657766452,188.897563390853,188.985140605913,189.072699573761,189.160263784227,
189.247824641547,189.335412399295,189.396435326001,189.484832149658,189.57321009574,
189.661583933721,189.749947134336,189.838318291413,189.895307261149),
 .UNSPECIFIED.);
#396=B_SPLINE_CURVE_WITH_KNOTS('',3,(#33733,#33734,#33735,#33736,#33737,
#33738,#33739,#33740,#33741,#33742),.UNSPECIFIED.,.F.,.F.,(4,2,2,2,4),(-6.1912792335152,
-6.12088779730415,-6.10166850366315,-6.08259528877872,-6.06755362652627),
 .UNSPECIFIED.);
#397=B_SPLINE_CURVE_WITH_KNOTS('',3,(#33745,#33746,#33747,#33748,#33749,
#33750,#33751,#33752,#33753,#33754,#33755,#33756,#33757,#33758,#33759),
 .UNSPECIFIED.,.F.,.F.,(4,1,1,1,1,1,1,1,1,1,1,1,4),(170.764858387386,171.113073755807,
171.611945690955,172.110817626103,172.609689561251,173.108561496399,173.607433431547,
174.106305366695,174.605177301843,175.104049236992,175.60292117214,176.101793107288,
176.22808870207),.UNSPECIFIED.);
#398=B_SPLINE_CURVE_WITH_KNOTS('',3,(#33762,#33763,#33764,#33765,#33766,
#33767,#33768,#33769,#33770,#33771,#33772,#33773,#33774,#33775,#33776,#33777,
#33778,#33779,#33780,#33781,#33782,#33783,#33784,#33785,#33786,#33787,#33788,
#33789,#33790,#33791,#33792,#33793,#33794,#33795,#33796,#33797,#33798,#33799,
#33800,#33801,#33802,#33803,#33804,#33805,#33806,#33807,#33808,#33809,#33810,
#33811,#33812,#33813,#33814,#33815,#33816,#33817,#33818,#33819,#33820,#33821,
#33822,#33823,#33824,#33825,#33826,#33827,#33828,#33829,#33830,#33831,#33832,
#33833,#33834,#33835,#33836,#33837,#33838,#33839,#33840,#33841,#33842,#33843,
#33844,#33845,#33846,#33847,#33848,#33849,#33850,#33851,#33852,#33853,#33854,
#33855,#33856,#33857,#33858,#33859,#33860,#33861,#33862,#33863,#33864,#33865,
#33866,#33867,#33868,#33869,#33870,#33871,#33872,#33873,#33874,#33875,#33876,
#33877,#33878,#33879,#33880,#33881,#33882,#33883,#33884,#33885,#33886,#33887,
#33888,#33889,#33890,#33891,#33892,#33893,#33894,#33895,#33896,#33897,#33898,
#33899,#33900,#33901,#33902,#33903,#33904,#33905,#33906,#33907,#33908,#33909,
#33910,#33911,#33912,#33913,#33914,#33915,#33916,#33917,#33918,#33919,#33920,
#33921,#33922,#33923,#33924,#33925,#33926,#33927,#33928,#33929,#33930),
 .UNSPECIFIED.,.F.,.F.,(4,3,3,3,3,3,3,3,3,3,3,3,3,3,3,3,3,3,3,3,3,3,3,3,
3,3,3,3,3,3,3,3,3,3,3,3,3,3,3,3,3,3,3,3,3,3,3,3,3,3,3,3,3,3,3,3,4),(-178.297882100285,
-178.208849797516,-178.191632214518,-178.107807278713,-178.02399957922,
-177.940189246353,-177.856384647973,-177.77255768974,-177.692495989827,
-177.608591418453,-177.524703139297,-177.440811534382,-177.356925446745,
-177.273017416127,-177.193359765137,-177.109475211766,-177.025607135838,
-176.941735826047,-176.857870042694,-176.773982136324,-176.694223540446,
-176.61034181593,-176.526476649979,-176.442608348443,-176.358745621261,
-176.274860821962,-176.195087315756,-176.111197803111,-176.027324727734,
-175.943448404497,-175.859577610181,-175.77568474517,-175.695951091065,
-175.612067842047,-175.528201118133,-175.444331221577,-175.36046688224,
-175.276580457569,-175.196814866375,-175.112928026889,-175.029057665353,
-174.945184093002,-174.861316064346,-174.777425963151,-174.697678641684,
-174.613793388471,-174.529924632591,-174.446052680509,-174.362186276864,
-174.278297793008,-174.198542416994,-174.114899946371,-174.031274766378,
-173.94764864838,-173.864026576569,-173.78038640654,-173.738545042839),
 .UNSPECIFIED.);
#399=B_SPLINE_CURVE_WITH_KNOTS('',3,(#33933,#33934,#33935,#33936,#33937,
#33938,#33939,#33940,#33941,#33942,#33943,#33944,#33945,#33946,#33947,#33948,
#33949,#33950,#33951,#33952,#33953,#33954,#33955,#33956,#33957,#33958,#33959,
#33960,#33961,#33962,#33963,#33964,#33965,#33966,#33967,#33968,#33969,#33970,
#33971,#33972,#33973,#33974,#33975,#33976,#33977,#33978,#33979,#33980,#33981,
#33982,#33983,#33984,#33985,#33986,#33987,#33988,#33989,#33990,#33991,#33992,
#33993,#33994,#33995,#33996,#33997,#33998,#33999,#34000,#34001,#34002,#34003,
#34004,#34005,#34006,#34007,#34008,#34009,#34010,#34011,#34012,#34013,#34014,
#34015,#34016,#34017,#34018,#34019,#34020,#34021,#34022,#34023,#34024,#34025,
#34026,#34027,#34028,#34029,#34030,#34031,#34032,#34033,#34034,#34035,#34036,
#34037,#34038,#34039,#34040,#34041,#34042,#34043,#34044,#34045,#34046,#34047,
#34048,#34049,#34050,#34051,#34052,#34053,#34054,#34055,#34056,#34057,#34058,
#34059,#34060,#34061,#34062,#34063,#34064,#34065,#34066,#34067,#34068,#34069,
#34070,#34071,#34072,#34073,#34074,#34075,#34076,#34077,#34078,#34079,#34080,
#34081,#34082,#34083,#34084,#34085,#34086,#34087,#34088,#34089,#34090,#34091,
#34092,#34093,#34094,#34095,#34096,#34097,#34098,#34099,#34100,#34101,#34102,
#34103,#34104,#34105,#34106,#34107,#34108,#34109,#34110,#34111,#34112,#34113,
#34114,#34115,#34116,#34117,#34118,#34119,#34120,#34121,#34122,#34123,#34124,
#34125,#34126,#34127,#34128,#34129,#34130,#34131,#34132,#34133,#34134,#34135,
#34136,#34137,#34138,#34139,#34140,#34141,#34142,#34143,#34144,#34145,#34146,
#34147,#34148,#34149,#34150,#34151,#34152,#34153,#34154,#34155,#34156,#34157,
#34158,#34159,#34160,#34161,#34162,#34163,#34164,#34165,#34166,#34167,#34168,
#34169,#34170,#34171,#34172,#34173,#34174,#34175,#34176,#34177,#34178,#34179,
#34180,#34181,#34182,#34183,#34184,#34185,#34186,#34187,#34188,#34189,#34190,
#34191,#34192,#34193,#34194,#34195,#34196,#34197,#34198,#34199,#34200,#34201,
#34202,#34203),.UNSPECIFIED.,.F.,.F.,(4,3,3,3,3,3,3,3,3,3,3,3,3,3,3,3,3,
3,3,3,3,3,3,3,3,3,3,3,3,3,3,3,3,3,3,3,3,3,3,3,3,3,3,3,3,3,3,3,3,3,3,3,3,
3,3,3,3,3,3,3,3,3,3,3,3,3,3,3,3,3,3,3,3,3,3,3,3,3,3,3,3,3,3,3,3,3,3,3,3,
3,4),(-2.84993027792945,-2.80581822492884,-2.77529095167904,-2.7639218300317,
-2.75777942373964,-2.71263817698004,-2.68370913192962,-2.63875182487813,
-2.59363222502916,-2.58642105701857,-2.57995978207043,-2.53462721743547,
-2.48902111530139,-2.44364758188306,-2.42724183695243,-2.39465624397139,
-2.38706665961561,-2.38082233194916,-2.33559763534729,-2.289576912667,-2.24355101834038,
-2.20505405572223,-2.18494067399242,-2.17696362392625,-2.16655709310407,
-2.12098494540008,-2.07475303934683,-2.02830225529523,-1.99659238554031,
-1.98209758802444,-1.97566444826943,-1.96991855489481,-1.92303849932432,
-1.90146277627555,-1.85485020732147,-1.80793499832861,-1.78593728731861,
-1.77037557248463,-1.76173309083023,-1.71460089183786,-1.66723806593038,
-1.63195331024862,-1.584641738859,-1.56888373105132,-1.55568481852088,-1.54982255046505,
-1.50191942593017,-1.45410564653405,-1.40615784942979,-1.35821005232553,
-1.34135883462771,-1.33595821079862,-1.28868021166659,-1.24070939844527,
-1.19246502715133,-1.14453907183535,-1.12692320891387,-1.11915523664791,
-1.08026432333022,-1.03220098375255,-0.983614733943928,-0.937169494271226,
-0.918719630218846,-0.904783582288534,-0.898697963027374,-0.848265869140248,
-0.797833775253121,-0.748864203381356,-0.699782475575903,-0.686312324754147,
-0.677639075649963,-0.628355660399474,-0.578788413932711,-0.529454269015081,
-0.511071810597535,-0.474708847474015,-0.461193855367628,-0.452940585084499,
-0.403785746204721,-0.353813383121523,-0.303841691601361,-0.262004898605367,
-0.241086502107369,-0.233148200519642,-0.225480555224177,-0.220168105609372,
-0.17099079510222,-0.120761505811504,-0.070321660673032,-0.0202259151736165,
0.),.UNSPECIFIED.);
#400=B_SPLINE_CURVE_WITH_KNOTS('',3,(#34206,#34207,#34208,#34209,#34210,
#34211,#34212,#34213,#34214,#34215,#34216,#34217,#34218,#34219),
 .UNSPECIFIED.,.F.,.F.,(4,2,2,2,2,2,4),(-1.02378211072902,-0.827714664332123,
-0.640554828731562,-0.390437320911094,-0.289794336115012,-0.139985920865823,
0.),.UNSPECIFIED.);
#401=B_SPLINE_CURVE_WITH_KNOTS('',3,(#35673,#35674,#35675,#35676,#35677,
#35678,#35679,#35680,#35681,#35682,#35683,#35684,#35685,#35686,#35687,#35688,
#35689,#35690,#35691,#35692,#35693,#35694,#35695,#35696,#35697,#35698,#35699,
#35700,#35701,#35702,#35703,#35704,#35705,#35706,#35707,#35708,#35709,#35710,
#35711,#35712,#35713,#35714,#35715,#35716,#35717,#35718,#35719,#35720,#35721,
#35722,#35723,#35724,#35725,#35726,#35727,#35728,#35729,#35730,#35731,#35732,
#35733,#35734,#35735,#35736,#35737,#35738,#35739,#35740,#35741,#35742,#35743,
#35744,#35745,#35746,#35747,#35748,#35749,#35750,#35751,#35752,#35753,#35754,
#35755,#35756,#35757,#35758,#35759,#35760,#35761,#35762,#35763,#35764,#35765,
#35766,#35767,#35768,#35769,#35770,#35771,#35772,#35773,#35774,#35775,#35776,
#35777,#35778),.UNSPECIFIED.,.F.,.F.,(4,3,3,3,3,3,3,3,3,3,3,3,3,3,3,3,3,
3,3,3,3,3,3,3,3,3,3,3,3,3,3,3,3,3,3,4),(-1.12653966532773,-1.08328443004837,
-1.03353709077206,-0.983959868704988,-0.972855476239986,-0.963909412895039,
-0.915025462469927,-0.866807833003593,-0.822978744363957,-0.816869072976604,
-0.795216619847291,-0.747460895965115,-0.69953853011811,-0.652271227547244,
-0.618804187172226,-0.607057707248577,-0.599647258206796,-0.553127126757695,
-0.518403066047171,-0.471676364421963,-0.425384243431735,-0.403792903604889,
-0.397276085507847,-0.390955965366398,-0.345490498978405,-0.299377878107159,
-0.253265257235913,-0.221607100081425,-0.205353593604308,-0.19501215756986,
-0.189043536422963,-0.168481916872947,-0.124214947369948,-0.0802229003350188,
-0.0371763150134234,-7.68796522159327E-15),.UNSPECIFIED.);
#402=B_SPLINE_CURVE_WITH_KNOTS('',3,(#37248,#37249,#37250,#37251,#37252,
#37253,#37254,#37255,#37256,#37257,#37258,#37259,#37260,#37261,#37262,#37263,
#37264,#37265,#37266,#37267,#37268,#37269,#37270,#37271,#37272,#37273,#37274,
#37275,#37276,#37277,#37278,#37279,#37280,#37281,#37282,#37283,#37284,#37285,
#37286,#37287,#37288,#37289,#37290,#37291,#37292,#37293,#37294,#37295,#37296,
#37297,#37298,#37299,#37300,#37301,#37302,#37303,#37304,#37305,#37306,#37307,
#37308,#37309,#37310,#37311,#37312,#37313,#37314,#37315,#37316,#37317,#37318,
#37319,#37320,#37321,#37322,#37323,#37324,#37325,#37326,#37327,#37328,#37329,
#37330,#37331,#37332,#37333,#37334,#37335,#37336,#37337,#37338,#37339,#37340,
#37341,#37342,#37343,#37344,#37345,#37346,#37347,#37348,#37349,#37350,#37351,
#37352,#37353,#37354,#37355,#37356,#37357,#37358,#37359),.UNSPECIFIED.,
 .F.,.F.,(4,3,3,3,3,3,3,3,3,3,3,3,3,3,3,3,3,3,3,3,3,3,3,3,3,3,3,3,3,3,3,
3,3,3,3,3,3,4),(-1.13094109509782,-1.09392182272659,-1.05040682482303,-1.00628645113637,
-0.999731233283575,-0.992626582922596,-0.947774596581187,-0.902652843289582,
-0.870560015591072,-0.859702426029801,-0.838467187892562,-0.793476327210687,
-0.747788564637451,-0.70352361360926,-0.670324900338118,-0.659878430803487,
-0.653412422619991,-0.638475761066728,-0.591272337150695,-0.570728760524689,
-0.52391018670982,-0.482335832098637,-0.461548654793045,-0.449191859151303,
-0.441818134511173,-0.440761477487453,-0.392779311016725,-0.341972967637929,
-0.291166624259132,-0.25477079622674,-0.238847621462569,-0.228959626544373,
-0.221325717796781,-0.172774573159914,-0.123227258018104,-0.0734982443681584,
-0.0241644143980285,0.),.UNSPECIFIED.);
#403=B_SPLINE_CURVE_WITH_KNOTS('',3,(#37360,#37361,#37362,#37363),
 .UNSPECIFIED.,.F.,.F.,(4,4),(-0.000448380443499476,0.),.UNSPECIFIED.);
#408=ELLIPSE('',#4562,4.28989109945289,3.72791464996848);
#409=ELLIPSE('',#4563,4.42862181409974,3.8415820723178);
#418=SHAPE_REPRESENTATION_RELATIONSHIP('SRR','None',#37787,#436);
#436=ADVANCED_BREP_SHAPE_REPRESENTATION('',(#472),#37691);
#454=STYLED_ITEM('',(#37883),#472);
#472=MANIFOLD_SOLID_BREP('Body1',#4152);
#504=FACE_BOUND('',#992,.T.);
#505=FACE_BOUND('',#995,.T.);
#556=PLANE('',#4564);
#557=PLANE('',#4565);
#558=PLANE('',#4566);
#559=PLANE('',#4567);
#560=PLANE('',#4568);
#561=PLANE('',#4569);
#562=PLANE('',#4570);
#563=PLANE('',#4571);
#564=PLANE('',#4575);
#565=PLANE('',#4576);
#689=FACE_OUTER_BOUND('',#923,.T.);
#690=FACE_OUTER_BOUND('',#924,.T.);
#691=FACE_OUTER_BOUND('',#925,.T.);
#692=FACE_OUTER_BOUND('',#926,.T.);
#693=FACE_OUTER_BOUND('',#927,.T.);
#694=FACE_OUTER_BOUND('',#928,.T.);
#695=FACE_OUTER_BOUND('',#929,.T.);
#696=FACE_OUTER_BOUND('',#930,.T.);
#697=FACE_OUTER_BOUND('',#931,.T.);
#698=FACE_OUTER_BOUND('',#932,.T.);
#699=FACE_OUTER_BOUND('',#933,.T.);
#700=FACE_OUTER_BOUND('',#934,.T.);
#701=FACE_OUTER_BOUND('',#935,.T.);
#702=FACE_OUTER_BOUND('',#936,.T.);
#703=FACE_OUTER_BOUND('',#937,.T.);
#704=FACE_OUTER_BOUND('',#938,.T.);
#705=FACE_OUTER_BOUND('',#939,.T.);
#706=FACE_OUTER_BOUND('',#940,.T.);
#707=FACE_OUTER_BOUND('',#941,.T.);
#708=FACE_OUTER_BOUND('',#942,.T.);
#709=FACE_OUTER_BOUND('',#943,.T.);
#710=FACE_OUTER_BOUND('',#944,.T.);
#711=FACE_OUTER_BOUND('',#945,.T.);
#712=FACE_OUTER_BOUND('',#946,.T.);
#713=FACE_OUTER_BOUND('',#947,.T.);
#714=FACE_OUTER_BOUND('',#948,.T.);
#715=FACE_OUTER_BOUND('',#949,.T.);
#716=FACE_OUTER_BOUND('',#950,.T.);
#717=FACE_OUTER_BOUND('',#951,.T.);
#718=FACE_OUTER_BOUND('',#952,.T.);
#719=FACE_OUTER_BOUND('',#953,.T.);
#720=FACE_OUTER_BOUND('',#954,.T.);
#721=FACE_OUTER_BOUND('',#955,.T.);
#722=FACE_OUTER_BOUND('',#956,.T.);
#723=FACE_OUTER_BOUND('',#957,.T.);
#724=FACE_OUTER_BOUND('',#958,.T.);
#725=FACE_OUTER_BOUND('',#959,.T.);
#726=FACE_OUTER_BOUND('',#960,.T.);
#727=FACE_OUTER_BOUND('',#961,.T.);
#728=FACE_OUTER_BOUND('',#962,.T.);
#729=FACE_OUTER_BOUND('',#963,.T.);
#730=FACE_OUTER_BOUND('',#964,.T.);
#731=FACE_OUTER_BOUND('',#965,.T.);
#732=FACE_OUTER_BOUND('',#966,.T.);
#733=FACE_OUTER_BOUND('',#967,.T.);
#734=FACE_OUTER_BOUND('',#968,.T.);
#735=FACE_OUTER_BOUND('',#969,.T.);
#736=FACE_OUTER_BOUND('',#970,.T.);
#737=FACE_OUTER_BOUND('',#971,.T.);
#738=FACE_OUTER_BOUND('',#972,.T.);
#739=FACE_OUTER_BOUND('',#973,.T.);
#740=FACE_OUTER_BOUND('',#974,.T.);
#741=FACE_OUTER_BOUND('',#975,.T.);
#742=FACE_OUTER_BOUND('',#976,.T.);
#743=FACE_OUTER_BOUND('',#977,.T.);
#744=FACE_OUTER_BOUND('',#978,.T.);
#745=FACE_OUTER_BOUND('',#979,.T.);
#746=FACE_OUTER_BOUND('',#980,.T.);
#747=FACE_OUTER_BOUND('',#981,.T.);
#748=FACE_OUTER_BOUND('',#982,.T.);
#749=FACE_OUTER_BOUND('',#983,.T.);
#750=FACE_OUTER_BOUND('',#984,.T.);
#751=FACE_OUTER_BOUND('',#985,.T.);
#752=FACE_OUTER_BOUND('',#986,.T.);
#753=FACE_OUTER_BOUND('',#987,.T.);
#754=FACE_OUTER_BOUND('',#988,.T.);
#755=FACE_OUTER_BOUND('',#989,.T.);
#756=FACE_OUTER_BOUND('',#990,.T.);
#757=FACE_OUTER_BOUND('',#991,.T.);
#758=FACE_OUTER_BOUND('',#993,.T.);
#759=FACE_OUTER_BOUND('',#994,.T.);
#760=FACE_OUTER_BOUND('',#996,.T.);
#923=EDGE_LOOP('',(#3139,#3140,#3141,#3142));
#924=EDGE_LOOP('',(#3143,#3144,#3145,#3146));
#925=EDGE_LOOP('',(#3147,#3148,#3149,#3150));
#926=EDGE_LOOP('',(#3151,#3152,#3153,#3154));
#927=EDGE_LOOP('',(#3155,#3156,#3157,#3158));
#928=EDGE_LOOP('',(#3159,#3160,#3161,#3162));
#929=EDGE_LOOP('',(#3163,#3164,#3165,#3166));
#930=EDGE_LOOP('',(#3167,#3168,#3169,#3170));
#931=EDGE_LOOP('',(#3171,#3172,#3173,#3174));
#932=EDGE_LOOP('',(#3175,#3176,#3177,#3178));
#933=EDGE_LOOP('',(#3179,#3180,#3181,#3182));
#934=EDGE_LOOP('',(#3183,#3184,#3185,#3186));
#935=EDGE_LOOP('',(#3187,#3188,#3189,#3190));
#936=EDGE_LOOP('',(#3191,#3192,#3193,#3194));
#937=EDGE_LOOP('',(#3195,#3196,#3197,#3198));
#938=EDGE_LOOP('',(#3199,#3200,#3201,#3202));
#939=EDGE_LOOP('',(#3203,#3204,#3205,#3206));
#940=EDGE_LOOP('',(#3207,#3208,#3209,#3210));
#941=EDGE_LOOP('',(#3211,#3212,#3213,#3214));
#942=EDGE_LOOP('',(#3215,#3216,#3217,#3218));
#943=EDGE_LOOP('',(#3219,#3220,#3221,#3222));
#944=EDGE_LOOP('',(#3223,#3224,#3225,#3226));
#945=EDGE_LOOP('',(#3227,#3228,#3229,#3230));
#946=EDGE_LOOP('',(#3231,#3232,#3233,#3234));
#947=EDGE_LOOP('',(#3235,#3236,#3237,#3238));
#948=EDGE_LOOP('',(#3239,#3240,#3241,#3242));
#949=EDGE_LOOP('',(#3243,#3244,#3245,#3246));
#950=EDGE_LOOP('',(#3247,#3248,#3249,#3250));
#951=EDGE_LOOP('',(#3251,#3252,#3253,#3254));
#952=EDGE_LOOP('',(#3255,#3256,#3257,#3258,#3259));
#953=EDGE_LOOP('',(#3260,#3261,#3262,#3263,#3264,#3265));
#954=EDGE_LOOP('',(#3266,#3267,#3268,#3269,#3270));
#955=EDGE_LOOP('',(#3271,#3272,#3273,#3274,#3275));
#956=EDGE_LOOP('',(#3276,#3277,#3278,#3279,#3280,#3281));
#957=EDGE_LOOP('',(#3282,#3283,#3284,#3285,#3286));
#958=EDGE_LOOP('',(#3287,#3288,#3289,#3290,#3291));
#959=EDGE_LOOP('',(#3292,#3293,#3294,#3295,#3296));
#960=EDGE_LOOP('',(#3297,#3298,#3299,#3300,#3301));
#961=EDGE_LOOP('',(#3302,#3303,#3304,#3305,#3306));
#962=EDGE_LOOP('',(#3307,#3308,#3309,#3310,#3311));
#963=EDGE_LOOP('',(#3312,#3313,#3314,#3315,#3316,#3317));
#964=EDGE_LOOP('',(#3318,#3319,#3320,#3321,#3322,#3323));
#965=EDGE_LOOP('',(#3324,#3325,#3326,#3327,#3328));
#966=EDGE_LOOP('',(#3329,#3330,#3331,#3332,#3333,#3334));
#967=EDGE_LOOP('',(#3335,#3336,#3337,#3338));
#968=EDGE_LOOP('',(#3339,#3340,#3341,#3342,#3343,#3344));
#969=EDGE_LOOP('',(#3345,#3346,#3347,#3348,#3349));
#970=EDGE_LOOP('',(#3350,#3351,#3352,#3353,#3354,#3355));
#971=EDGE_LOOP('',(#3356,#3357,#3358,#3359,#3360,#3361));
#972=EDGE_LOOP('',(#3362,#3363,#3364,#3365,#3366));
#973=EDGE_LOOP('',(#3367,#3368,#3369,#3370,#3371,#3372));
#974=EDGE_LOOP('',(#3373,#3374,#3375,#3376,#3377));
#975=EDGE_LOOP('',(#3378,#3379,#3380,#3381,#3382));
#976=EDGE_LOOP('',(#3383,#3384,#3385,#3386,#3387,#3388));
#977=EDGE_LOOP('',(#3389,#3390,#3391,#3392,#3393));
#978=EDGE_LOOP('',(#3394,#3395,#3396,#3397,#3398));
#979=EDGE_LOOP('',(#3399,#3400,#3401,#3402,#3403,#3404));
#980=EDGE_LOOP('',(#3405,#3406,#3407,#3408));
#981=EDGE_LOOP('',(#3409,#3410,#3411,#3412));
#982=EDGE_LOOP('',(#3413,#3414,#3415,#3416,#3417,#3418,#3419,#3420,#3421,
#3422,#3423,#3424,#3425,#3426,#3427,#3428,#3429,#3430,#3431,#3432,#3433,
#3434,#3435,#3436,#3437,#3438,#3439,#3440,#3441,#3442,#3443,#3444,#3445,
#3446,#3447,#3448,#3449,#3450,#3451,#3452,#3453,#3454,#3455,#3456,#3457,
#3458,#3459,#3460,#3461,#3462,#3463,#3464,#3465,#3466,#3467,#3468,#3469,
#3470,#3471,#3472,#3473,#3474,#3475,#3476,#3477,#3478,#3479,#3480,#3481,
#3482,#3483,#3484,#3485,#3486,#3487,#3488,#3489,#3490,#3491,#3492,#3493));
#983=EDGE_LOOP('',(#3494,#3495,#3496,#3497,#3498,#3499,#3500,#3501,#3502,
#3503,#3504,#3505,#3506,#3507,#3508,#3509,#3510,#3511,#3512,#3513,#3514,
#3515,#3516,#3517,#3518,#3519,#3520,#3521,#3522,#3523,#3524,#3525,#3526,
#3527,#3528,#3529,#3530,#3531,#3532,#3533,#3534,#3535,#3536,#3537,#3538,
#3539,#3540,#3541,#3542,#3543,#3544,#3545,#3546,#3547,#3548,#3549,#3550,
#3551,#3552,#3553,#3554,#3555,#3556,#3557,#3558,#3559,#3560,#3561,#3562,
#3563,#3564,#3565,#3566,#3567,#3568,#3569,#3570,#3571,#3572,#3573));
#984=EDGE_LOOP('',(#3574,#3575,#3576,#3577));
#985=EDGE_LOOP('',(#3578,#3579,#3580,#3581));
#986=EDGE_LOOP('',(#3582,#3583,#3584,#3585));
#987=EDGE_LOOP('',(#3586,#3587,#3588,#3589));
#988=EDGE_LOOP('',(#3590,#3591,#3592,#3593));
#989=EDGE_LOOP('',(#3594,#3595,#3596,#3597));
#990=EDGE_LOOP('',(#3598,#3599,#3600,#3601,#3602,#3603));
#991=EDGE_LOOP('',(#3604));
#992=EDGE_LOOP('',(#3605,#3606,#3607,#3608,#3609));
#993=EDGE_LOOP('',(#3610,#3611,#3612,#3613));
#994=EDGE_LOOP('',(#3614));
#995=EDGE_LOOP('',(#3615,#3616,#3617,#3618,#3619,#3620));
#996=EDGE_LOOP('',(#3621,#3622,#3623,#3624));
#1175=LINE('',#14170,#1424);
#1176=LINE('',#14259,#1425);
#1177=LINE('',#14508,#1426);
#1178=LINE('',#14546,#1427);
#1179=LINE('',#15011,#1428);
#1180=LINE('',#15476,#1429);
#1181=LINE('',#15726,#1430);
#1182=LINE('',#15975,#1431);
#1183=LINE('',#16225,#1432);
#1184=LINE('',#16474,#1433);
#1185=LINE('',#16724,#1434);
#1186=LINE('',#17189,#1435);
#1187=LINE('',#17651,#1436);
#1188=LINE('',#17901,#1437);
#1189=LINE('',#18150,#1438);
#1190=LINE('',#18401,#1439);
#1191=LINE('',#18440,#1440);
#1192=LINE('',#18689,#1441);
#1193=LINE('',#18939,#1442);
#1194=LINE('',#19188,#1443);
#1195=LINE('',#19226,#1444);
#1196=LINE('',#19688,#1445);
#1197=LINE('',#19940,#1446);
#1198=LINE('',#20402,#1447);
#1199=LINE('',#20867,#1448);
#1200=LINE('',#21117,#1449);
#1201=LINE('',#21154,#1450);
#1202=LINE('',#21407,#1451);
#1203=LINE('',#21869,#1452);
#1204=LINE('',#22231,#1453);
#1205=LINE('',#22499,#1454);
#1206=LINE('',#23023,#1455);
#1207=LINE('',#23624,#1456);
#1208=LINE('',#24106,#1457);
#1209=LINE('',#24395,#1458);
#1210=LINE('',#24873,#1459);
#1211=LINE('',#25412,#1460);
#1212=LINE('',#25931,#1461);
#1213=LINE('',#26406,#1462);
#1214=LINE('',#26905,#1463);
#1215=LINE('',#27404,#1464);
#1216=LINE('',#27464,#1465);
#1217=LINE('',#27937,#1466);
#1218=LINE('',#28214,#1467);
#1219=LINE('',#28721,#1468);
#1220=LINE('',#29227,#1469);
#1221=LINE('',#29729,#1470);
#1222=LINE('',#30017,#1471);
#1223=LINE('',#30275,#1472);
#1224=LINE('',#30762,#1473);
#1225=LINE('',#31041,#1474);
#1226=LINE('',#31336,#1475);
#1227=LINE('',#31816,#1476);
#1228=LINE('',#32295,#1477);
#1229=LINE('',#32602,#1478);
#1230=LINE('',#33069,#1479);
#1231=LINE('',#37368,#1480);
#1232=LINE('',#37370,#1481);
#1233=LINE('',#37372,#1482);
#1234=LINE('',#37373,#1483);
#1235=LINE('',#37376,#1484);
#1236=LINE('',#37378,#1485);
#1237=LINE('',#37379,#1486);
#1238=LINE('',#37382,#1487);
#1239=LINE('',#37384,#1488);
#1240=LINE('',#37385,#1489);
#1241=LINE('',#37388,#1490);
#1242=LINE('',#37390,#1491);
#1243=LINE('',#37391,#1492);
#1244=LINE('',#37394,#1493);
#1245=LINE('',#37396,#1494);
#1246=LINE('',#37397,#1495);
#1247=LINE('',#37399,#1496);
#1248=LINE('',#37400,#1497);
#1249=LINE('',#37407,#1498);
#1424=VECTOR('',#5098,5.91675);
#1425=VECTOR('',#5103,5.91675);
#1426=VECTOR('',#5106,5.91675);
#1427=VECTOR('',#5109,5.91675);
#1428=VECTOR('',#5112,5.91675);
#1429=VECTOR('',#5115,5.91675);
#1430=VECTOR('',#5118,5.91675);
#1431=VECTOR('',#5121,5.91675);
#1432=VECTOR('',#5124,5.91675);
#1433=VECTOR('',#5127,5.91675);
#1434=VECTOR('',#5130,5.91675);
#1435=VECTOR('',#5133,5.91675);
#1436=VECTOR('',#5136,5.91675);
#1437=VECTOR('',#5139,5.91675);
#1438=VECTOR('',#5142,5.91675);
#1439=VECTOR('',#5145,5.91675);
#1440=VECTOR('',#5148,5.91675);
#1441=VECTOR('',#5151,5.91675);
#1442=VECTOR('',#5154,5.91675);
#1443=VECTOR('',#5157,5.91675);
#1444=VECTOR('',#5160,5.91675);
#1445=VECTOR('',#5163,5.91675);
#1446=VECTOR('',#5166,5.91675);
#1447=VECTOR('',#5169,5.91675);
#1448=VECTOR('',#5172,5.91675);
#1449=VECTOR('',#5175,5.91675);
#1450=VECTOR('',#5178,5.91675);
#1451=VECTOR('',#5181,5.91675);
#1452=VECTOR('',#5184,4.91825);
#1453=VECTOR('',#5189,4.91825);
#1454=VECTOR('',#5192,4.91825);
#1455=VECTOR('',#5195,4.91825);
#1456=VECTOR('',#5198,4.91825);
#1457=VECTOR('',#5201,4.91825);
#1458=VECTOR('',#5204,4.91825);
#1459=VECTOR('',#5207,4.91825);
#1460=VECTOR('',#5210,4.91825);
#1461=VECTOR('',#5213,4.91825);
#1462=VECTOR('',#5216,4.91825);
#1463=VECTOR('',#5219,4.91825);
#1464=VECTOR('',#5222,4.91825);
#1465=VECTOR('',#5225,4.91825);
#1466=VECTOR('',#5228,4.91825);
#1467=VECTOR('',#5231,4.91825);
#1468=VECTOR('',#5234,4.91825);
#1469=VECTOR('',#5237,4.91825);
#1470=VECTOR('',#5240,4.91825);
#1471=VECTOR('',#5243,4.91825);
#1472=VECTOR('',#5246,4.91825);
#1473=VECTOR('',#5249,4.91825);
#1474=VECTOR('',#5252,4.91825);
#1475=VECTOR('',#5255,4.91825);
#1476=VECTOR('',#5258,4.91825);
#1477=VECTOR('',#5261,4.91825);
#1478=VECTOR('',#5264,4.91825);
#1479=VECTOR('',#5267,4.91825);
#1480=VECTOR('',#5286,10.);
#1481=VECTOR('',#5287,10.);
#1482=VECTOR('',#5288,10.);
#1483=VECTOR('',#5289,10.);
#1484=VECTOR('',#5292,10.);
#1485=VECTOR('',#5293,10.);
#1486=VECTOR('',#5294,10.);
#1487=VECTOR('',#5297,9.99999999999999);
#1488=VECTOR('',#5298,10.);
#1489=VECTOR('',#5299,10.);
#1490=VECTOR('',#5302,10.);
#1491=VECTOR('',#5303,10.);
#1492=VECTOR('',#5304,10.);
#1493=VECTOR('',#5307,10.);
#1494=VECTOR('',#5308,10.);
#1495=VECTOR('',#5309,10.);
#1496=VECTOR('',#5312,10.);
#1497=VECTOR('',#5313,10.);
#1498=VECTOR('',#5322,9.);
#1596=CIRCLE('',#4499,5.91675);
#1597=CIRCLE('',#4528,4.91825);
#1598=CIRCLE('',#4557,4.91825);
#1599=CIRCLE('',#4559,5.91675);
#1600=CIRCLE('',#4561,5.);
#1601=CIRCLE('',#4572,9.);
#1602=CIRCLE('',#4574,9.);
#1816=VERTEX_POINT('',#14168);
#1817=VERTEX_POINT('',#14169);
#1818=VERTEX_POINT('',#14171);
#1819=VERTEX_POINT('',#14248);
#1820=VERTEX_POINT('',#14257);
#1821=VERTEX_POINT('',#14258);
#1822=VERTEX_POINT('',#14506);
#1823=VERTEX_POINT('',#14507);
#1824=VERTEX_POINT('',#14544);
#1825=VERTEX_POINT('',#14545);
#1826=VERTEX_POINT('',#15009);
#1827=VERTEX_POINT('',#15010);
#1828=VERTEX_POINT('',#15474);
#1829=VERTEX_POINT('',#15475);
#1830=VERTEX_POINT('',#15724);
#1831=VERTEX_POINT('',#15725);
#1832=VERTEX_POINT('',#15973);
#1833=VERTEX_POINT('',#15974);
#1834=VERTEX_POINT('',#16223);
#1835=VERTEX_POINT('',#16224);
#1836=VERTEX_POINT('',#16472);
#1837=VERTEX_POINT('',#16473);
#1838=VERTEX_POINT('',#16722);
#1839=VERTEX_POINT('',#16723);
#1840=VERTEX_POINT('',#17187);
#1841=VERTEX_POINT('',#17188);
#1842=VERTEX_POINT('',#17649);
#1843=VERTEX_POINT('',#17650);
#1844=VERTEX_POINT('',#17899);
#1845=VERTEX_POINT('',#17900);
#1846=VERTEX_POINT('',#18148);
#1847=VERTEX_POINT('',#18149);
#1848=VERTEX_POINT('',#18399);
#1849=VERTEX_POINT('',#18400);
#1850=VERTEX_POINT('',#18438);
#1851=VERTEX_POINT('',#18439);
#1852=VERTEX_POINT('',#18687);
#1853=VERTEX_POINT('',#18688);
#1854=VERTEX_POINT('',#18937);
#1855=VERTEX_POINT('',#18938);
#1856=VERTEX_POINT('',#19186);
#1857=VERTEX_POINT('',#19187);
#1858=VERTEX_POINT('',#19224);
#1859=VERTEX_POINT('',#19225);
#1860=VERTEX_POINT('',#19686);
#1861=VERTEX_POINT('',#19687);
#1862=VERTEX_POINT('',#19938);
#1863=VERTEX_POINT('',#19939);
#1864=VERTEX_POINT('',#20400);
#1865=VERTEX_POINT('',#20401);
#1866=VERTEX_POINT('',#20865);
#1867=VERTEX_POINT('',#20866);
#1868=VERTEX_POINT('',#21115);
#1869=VERTEX_POINT('',#21116);
#1870=VERTEX_POINT('',#21152);
#1871=VERTEX_POINT('',#21153);
#1872=VERTEX_POINT('',#21405);
#1873=VERTEX_POINT('',#21406);
#1874=VERTEX_POINT('',#21867);
#1875=VERTEX_POINT('',#21868);
#1876=VERTEX_POINT('',#21870);
#1877=VERTEX_POINT('',#22087);
#1878=VERTEX_POINT('',#22229);
#1879=VERTEX_POINT('',#22230);
#1880=VERTEX_POINT('',#22466);
#1881=VERTEX_POINT('',#22497);
#1882=VERTEX_POINT('',#22498);
#1883=VERTEX_POINT('',#22500);
#1884=VERTEX_POINT('',#22795);
#1885=VERTEX_POINT('',#23021);
#1886=VERTEX_POINT('',#23022);
#1887=VERTEX_POINT('',#23326);
#1888=VERTEX_POINT('',#23622);
#1889=VERTEX_POINT('',#23623);
#1890=VERTEX_POINT('',#23625);
#1891=VERTEX_POINT('',#24104);
#1892=VERTEX_POINT('',#24105);
#1893=VERTEX_POINT('',#24107);
#1894=VERTEX_POINT('',#24365);
#1895=VERTEX_POINT('',#24393);
#1896=VERTEX_POINT('',#24394);
#1897=VERTEX_POINT('',#24632);
#1898=VERTEX_POINT('',#24871);
#1899=VERTEX_POINT('',#24872);
#1900=VERTEX_POINT('',#24874);
#1901=VERTEX_POINT('',#25410);
#1902=VERTEX_POINT('',#25411);
#1903=VERTEX_POINT('',#25665);
#1904=VERTEX_POINT('',#25929);
#1905=VERTEX_POINT('',#25930);
#1906=VERTEX_POINT('',#25932);
#1907=VERTEX_POINT('',#26404);
#1908=VERTEX_POINT('',#26405);
#1909=VERTEX_POINT('',#26659);
#1910=VERTEX_POINT('',#26903);
#1911=VERTEX_POINT('',#26904);
#1912=VERTEX_POINT('',#26906);
#1913=VERTEX_POINT('',#27402);
#1914=VERTEX_POINT('',#27403);
#1915=VERTEX_POINT('',#27405);
#1916=VERTEX_POINT('',#27432);
#1917=VERTEX_POINT('',#27462);
#1918=VERTEX_POINT('',#27463);
#1919=VERTEX_POINT('',#27465);
#1920=VERTEX_POINT('',#27708);
#1921=VERTEX_POINT('',#27935);
#1922=VERTEX_POINT('',#27936);
#1923=VERTEX_POINT('',#28184);
#1924=VERTEX_POINT('',#28212);
#1925=VERTEX_POINT('',#28213);
#1926=VERTEX_POINT('',#28215);
#1927=VERTEX_POINT('',#28466);
#1928=VERTEX_POINT('',#28719);
#1929=VERTEX_POINT('',#28720);
#1930=VERTEX_POINT('',#29225);
#1931=VERTEX_POINT('',#29226);
#1932=VERTEX_POINT('',#29228);
#1933=VERTEX_POINT('',#29495);
#1934=VERTEX_POINT('',#29727);
#1935=VERTEX_POINT('',#29728);
#1936=VERTEX_POINT('',#29984);
#1937=VERTEX_POINT('',#30015);
#1938=VERTEX_POINT('',#30016);
#1939=VERTEX_POINT('',#30018);
#1940=VERTEX_POINT('',#30047);
#1941=VERTEX_POINT('',#30273);
#1942=VERTEX_POINT('',#30274);
#1943=VERTEX_POINT('',#30276);
#1944=VERTEX_POINT('',#30502);
#1945=VERTEX_POINT('',#30760);
#1946=VERTEX_POINT('',#30761);
#1947=VERTEX_POINT('',#30763);
#1948=VERTEX_POINT('',#31039);
#1949=VERTEX_POINT('',#31040);
#1950=VERTEX_POINT('',#31042);
#1951=VERTEX_POINT('',#31304);
#1952=VERTEX_POINT('',#31334);
#1953=VERTEX_POINT('',#31335);
#1954=VERTEX_POINT('',#31579);
#1955=VERTEX_POINT('',#31814);
#1956=VERTEX_POINT('',#31815);
#1957=VERTEX_POINT('',#31817);
#1958=VERTEX_POINT('',#32293);
#1959=VERTEX_POINT('',#32294);
#1960=VERTEX_POINT('',#32296);
#1961=VERTEX_POINT('',#32326);
#1962=VERTEX_POINT('',#32600);
#1963=VERTEX_POINT('',#32601);
#1964=VERTEX_POINT('',#32603);
#1965=VERTEX_POINT('',#33067);
#1966=VERTEX_POINT('',#33068);
#1967=VERTEX_POINT('',#33316);
#1968=VERTEX_POINT('',#33346);
#1969=VERTEX_POINT('',#33352);
#1970=VERTEX_POINT('',#33564);
#1971=VERTEX_POINT('',#33566);
#1972=VERTEX_POINT('',#33744);
#1973=VERTEX_POINT('',#33760);
#1974=VERTEX_POINT('',#33932);
#1975=VERTEX_POINT('',#34204);
#1976=VERTEX_POINT('',#37247);
#1977=VERTEX_POINT('',#37366);
#1978=VERTEX_POINT('',#37367);
#1979=VERTEX_POINT('',#37369);
#1980=VERTEX_POINT('',#37371);
#1981=VERTEX_POINT('',#37375);
#1982=VERTEX_POINT('',#37377);
#1983=VERTEX_POINT('',#37381);
#1984=VERTEX_POINT('',#37383);
#1985=VERTEX_POINT('',#37387);
#1986=VERTEX_POINT('',#37389);
#1987=VERTEX_POINT('',#37393);
#1988=VERTEX_POINT('',#37395);
#1989=VERTEX_POINT('',#37403);
#1990=VERTEX_POINT('',#37406);
#2303=EDGE_CURVE('',#1816,#1817,#1175,.T.);
#2304=EDGE_CURVE('',#1816,#1818,#245,.T.);
#2305=EDGE_CURVE('',#1818,#1819,#1596,.F.);
#2306=EDGE_CURVE('',#1819,#1817,#246,.T.);
#2307=EDGE_CURVE('',#1820,#1821,#1176,.T.);
#2308=EDGE_CURVE('',#1820,#1816,#247,.T.);
#2309=EDGE_CURVE('',#1817,#1821,#248,.T.);
#2310=EDGE_CURVE('',#1822,#1823,#1177,.T.);
#2311=EDGE_CURVE('',#1822,#1820,#249,.T.);
#2312=EDGE_CURVE('',#1821,#1823,#250,.T.);
#2313=EDGE_CURVE('',#1824,#1825,#1178,.T.);
#2314=EDGE_CURVE('',#1824,#1822,#251,.T.);
#2315=EDGE_CURVE('',#1823,#1825,#252,.T.);
#2316=EDGE_CURVE('',#1826,#1827,#1179,.T.);
#2317=EDGE_CURVE('',#1826,#1824,#253,.T.);
#2318=EDGE_CURVE('',#1825,#1827,#254,.T.);
#2319=EDGE_CURVE('',#1828,#1829,#1180,.T.);
#2320=EDGE_CURVE('',#1828,#1826,#255,.T.);
#2321=EDGE_CURVE('',#1827,#1829,#256,.T.);
#2322=EDGE_CURVE('',#1830,#1831,#1181,.T.);
#2323=EDGE_CURVE('',#1830,#1828,#257,.T.);
#2324=EDGE_CURVE('',#1829,#1831,#258,.T.);
#2325=EDGE_CURVE('',#1832,#1833,#1182,.T.);
#2326=EDGE_CURVE('',#1832,#1830,#259,.T.);
#2327=EDGE_CURVE('',#1831,#1833,#260,.T.);
#2328=EDGE_CURVE('',#1834,#1835,#1183,.T.);
#2329=EDGE_CURVE('',#1834,#1832,#261,.T.);
#2330=EDGE_CURVE('',#1833,#1835,#262,.T.);
#2331=EDGE_CURVE('',#1836,#1837,#1184,.T.);
#2332=EDGE_CURVE('',#1836,#1834,#263,.T.);
#2333=EDGE_CURVE('',#1835,#1837,#264,.T.);
#2334=EDGE_CURVE('',#1838,#1839,#1185,.T.);
#2335=EDGE_CURVE('',#1838,#1836,#265,.T.);
#2336=EDGE_CURVE('',#1837,#1839,#266,.T.);
#2337=EDGE_CURVE('',#1840,#1841,#1186,.T.);
#2338=EDGE_CURVE('',#1840,#1838,#267,.T.);
#2339=EDGE_CURVE('',#1839,#1841,#268,.T.);
#2340=EDGE_CURVE('',#1842,#1843,#1187,.T.);
#2341=EDGE_CURVE('',#1842,#1840,#269,.T.);
#2342=EDGE_CURVE('',#1841,#1843,#270,.T.);
#2343=EDGE_CURVE('',#1844,#1845,#1188,.T.);
#2344=EDGE_CURVE('',#1844,#1842,#271,.T.);
#2345=EDGE_CURVE('',#1843,#1845,#272,.T.);
#2346=EDGE_CURVE('',#1846,#1847,#1189,.T.);
#2347=EDGE_CURVE('',#1846,#1844,#273,.T.);
#2348=EDGE_CURVE('',#1845,#1847,#274,.T.);
#2349=EDGE_CURVE('',#1848,#1849,#1190,.T.);
#2350=EDGE_CURVE('',#1848,#1846,#275,.T.);
#2351=EDGE_CURVE('',#1847,#1849,#276,.T.);
#2352=EDGE_CURVE('',#1850,#1851,#1191,.T.);
#2353=EDGE_CURVE('',#1850,#1848,#277,.T.);
#2354=EDGE_CURVE('',#1849,#1851,#278,.T.);
#2355=EDGE_CURVE('',#1852,#1853,#1192,.T.);
#2356=EDGE_CURVE('',#1852,#1850,#279,.T.);
#2357=EDGE_CURVE('',#1851,#1853,#280,.T.);
#2358=EDGE_CURVE('',#1854,#1855,#1193,.T.);
#2359=EDGE_CURVE('',#1854,#1852,#281,.T.);
#2360=EDGE_CURVE('',#1853,#1855,#282,.T.);
#2361=EDGE_CURVE('',#1856,#1857,#1194,.T.);
#2362=EDGE_CURVE('',#1856,#1854,#283,.T.);
#2363=EDGE_CURVE('',#1855,#1857,#284,.T.);
#2364=EDGE_CURVE('',#1858,#1859,#1195,.T.);
#2365=EDGE_CURVE('',#1858,#1856,#285,.T.);
#2366=EDGE_CURVE('',#1857,#1859,#286,.T.);
#2367=EDGE_CURVE('',#1860,#1861,#1196,.T.);
#2368=EDGE_CURVE('',#1860,#1858,#287,.T.);
#2369=EDGE_CURVE('',#1859,#1861,#288,.T.);
#2370=EDGE_CURVE('',#1862,#1863,#1197,.T.);
#2371=EDGE_CURVE('',#1862,#1860,#289,.T.);
#2372=EDGE_CURVE('',#1861,#1863,#290,.T.);
#2373=EDGE_CURVE('',#1864,#1865,#1198,.T.);
#2374=EDGE_CURVE('',#1864,#1862,#291,.T.);
#2375=EDGE_CURVE('',#1863,#1865,#292,.T.);
#2376=EDGE_CURVE('',#1866,#1867,#1199,.T.);
#2377=EDGE_CURVE('',#1866,#1864,#293,.T.);
#2378=EDGE_CURVE('',#1865,#1867,#294,.T.);
#2379=EDGE_CURVE('',#1868,#1869,#1200,.T.);
#2380=EDGE_CURVE('',#1868,#1866,#295,.T.);
#2381=EDGE_CURVE('',#1867,#1869,#296,.T.);
#2382=EDGE_CURVE('',#1870,#1871,#1201,.T.);
#2383=EDGE_CURVE('',#1870,#1868,#297,.T.);
#2384=EDGE_CURVE('',#1869,#1871,#298,.T.);
#2385=EDGE_CURVE('',#1872,#1873,#1202,.T.);
#2386=EDGE_CURVE('',#1872,#1870,#299,.T.);
#2387=EDGE_CURVE('',#1871,#1873,#300,.T.);
#2388=EDGE_CURVE('',#1874,#1875,#1203,.T.);
#2389=EDGE_CURVE('',#1876,#1874,#301,.F.);
#2390=EDGE_CURVE('',#1877,#1876,#1597,.T.);
#2391=EDGE_CURVE('',#1877,#1875,#302,.T.);
#2392=EDGE_CURVE('',#1878,#1879,#1204,.T.);
#2393=EDGE_CURVE('',#1874,#1878,#303,.F.);
#2394=EDGE_CURVE('',#1875,#1880,#304,.T.);
#2395=EDGE_CURVE('',#1880,#1879,#305,.T.);
#2396=EDGE_CURVE('',#1881,#1882,#1205,.T.);
#2397=EDGE_CURVE('',#1883,#1881,#306,.F.);
#2398=EDGE_CURVE('',#1878,#1883,#307,.F.);
#2399=EDGE_CURVE('',#1879,#1884,#308,.T.);
#2400=EDGE_CURVE('',#1884,#1882,#309,.T.);
#2401=EDGE_CURVE('',#1885,#1886,#1206,.T.);
#2402=EDGE_CURVE('',#1881,#1885,#310,.F.);
#2403=EDGE_CURVE('',#1882,#1887,#311,.T.);
#2404=EDGE_CURVE('',#1887,#1886,#312,.T.);
#2405=EDGE_CURVE('',#1888,#1889,#1207,.T.);
#2406=EDGE_CURVE('',#1890,#1888,#313,.T.);
#2407=EDGE_CURVE('',#1885,#1890,#314,.F.);
#2408=EDGE_CURVE('',#1886,#1889,#315,.T.);
#2409=EDGE_CURVE('',#1891,#1892,#1208,.T.);
#2410=EDGE_CURVE('',#1893,#1891,#316,.F.);
#2411=EDGE_CURVE('',#1888,#1893,#317,.T.);
#2412=EDGE_CURVE('',#1889,#1894,#318,.T.);
#2413=EDGE_CURVE('',#1894,#1892,#319,.T.);
#2414=EDGE_CURVE('',#1895,#1896,#1209,.T.);
#2415=EDGE_CURVE('',#1891,#1895,#320,.F.);
#2416=EDGE_CURVE('',#1892,#1897,#321,.T.);
#2417=EDGE_CURVE('',#1897,#1896,#322,.T.);
#2418=EDGE_CURVE('',#1898,#1899,#1210,.T.);
#2419=EDGE_CURVE('',#1900,#1898,#323,.F.);
#2420=EDGE_CURVE('',#1895,#1900,#324,.F.);
#2421=EDGE_CURVE('',#1896,#1899,#325,.T.);
#2422=EDGE_CURVE('',#1901,#1902,#1211,.T.);
#2423=EDGE_CURVE('',#1898,#1901,#326,.F.);
#2424=EDGE_CURVE('',#1899,#1903,#327,.T.);
#2425=EDGE_CURVE('',#1903,#1902,#328,.T.);
#2426=EDGE_CURVE('',#1904,#1905,#1212,.T.);
#2427=EDGE_CURVE('',#1906,#1904,#329,.F.);
#2428=EDGE_CURVE('',#1901,#1906,#330,.F.);
#2429=EDGE_CURVE('',#1902,#1905,#331,.T.);
#2430=EDGE_CURVE('',#1907,#1908,#1213,.T.);
#2431=EDGE_CURVE('',#1904,#1907,#332,.F.);
#2432=EDGE_CURVE('',#1905,#1909,#333,.T.);
#2433=EDGE_CURVE('',#1909,#1908,#334,.T.);
#2434=EDGE_CURVE('',#1910,#1911,#1214,.T.);
#2435=EDGE_CURVE('',#1912,#1910,#335,.T.);
#2436=EDGE_CURVE('',#1907,#1912,#336,.F.);
#2437=EDGE_CURVE('',#1908,#1911,#337,.T.);
#2438=EDGE_CURVE('',#1913,#1914,#1215,.T.);
#2439=EDGE_CURVE('',#1915,#1913,#338,.T.);
#2440=EDGE_CURVE('',#1910,#1915,#339,.T.);
#2441=EDGE_CURVE('',#1911,#1916,#340,.T.);
#2442=EDGE_CURVE('',#1916,#1914,#341,.T.);
#2443=EDGE_CURVE('',#1917,#1918,#1216,.T.);
#2444=EDGE_CURVE('',#1919,#1917,#342,.F.);
#2445=EDGE_CURVE('',#1913,#1919,#343,.T.);
#2446=EDGE_CURVE('',#1914,#1920,#344,.T.);
#2447=EDGE_CURVE('',#1920,#1918,#345,.T.);
#2448=EDGE_CURVE('',#1921,#1922,#1217,.T.);
#2449=EDGE_CURVE('',#1917,#1921,#346,.F.);
#2450=EDGE_CURVE('',#1918,#1923,#347,.T.);
#2451=EDGE_CURVE('',#1923,#1922,#348,.T.);
#2452=EDGE_CURVE('',#1924,#1925,#1218,.T.);
#2453=EDGE_CURVE('',#1926,#1924,#349,.F.);
#2454=EDGE_CURVE('',#1921,#1926,#350,.F.);
#2455=EDGE_CURVE('',#1922,#1927,#351,.T.);
#2456=EDGE_CURVE('',#1927,#1925,#352,.T.);
#2457=EDGE_CURVE('',#1928,#1929,#1219,.T.);
#2458=EDGE_CURVE('',#1924,#1928,#353,.F.);
#2459=EDGE_CURVE('',#1925,#1929,#354,.T.);
#2460=EDGE_CURVE('',#1930,#1931,#1220,.T.);
#2461=EDGE_CURVE('',#1932,#1930,#355,.F.);
#2462=EDGE_CURVE('',#1928,#1932,#356,.F.);
#2463=EDGE_CURVE('',#1929,#1933,#357,.T.);
#2464=EDGE_CURVE('',#1933,#1931,#358,.T.);
#2465=EDGE_CURVE('',#1934,#1935,#1221,.T.);
#2466=EDGE_CURVE('',#1930,#1934,#359,.F.);
#2467=EDGE_CURVE('',#1931,#1936,#360,.T.);
#2468=EDGE_CURVE('',#1936,#1935,#361,.T.);
#2469=EDGE_CURVE('',#1937,#1938,#1222,.T.);
#2470=EDGE_CURVE('',#1939,#1937,#362,.T.);
#2471=EDGE_CURVE('',#1934,#1939,#363,.F.);
#2472=EDGE_CURVE('',#1935,#1940,#364,.T.);
#2473=EDGE_CURVE('',#1940,#1938,#365,.T.);
#2474=EDGE_CURVE('',#1941,#1942,#1223,.T.);
#2475=EDGE_CURVE('',#1943,#1941,#366,.T.);
#2476=EDGE_CURVE('',#1937,#1943,#367,.T.);
#2477=EDGE_CURVE('',#1938,#1944,#368,.T.);
#2478=EDGE_CURVE('',#1944,#1942,#369,.T.);
#2479=EDGE_CURVE('',#1945,#1946,#1224,.T.);
#2480=EDGE_CURVE('',#1947,#1945,#370,.T.);
#2481=EDGE_CURVE('',#1941,#1947,#371,.T.);
#2482=EDGE_CURVE('',#1942,#1946,#372,.T.);
#2483=EDGE_CURVE('',#1948,#1949,#1225,.T.);
#2484=EDGE_CURVE('',#1950,#1948,#373,.F.);
#2485=EDGE_CURVE('',#1945,#1950,#374,.T.);
#2486=EDGE_CURVE('',#1946,#1951,#375,.T.);
#2487=EDGE_CURVE('',#1951,#1949,#376,.T.);
#2488=EDGE_CURVE('',#1952,#1953,#1226,.T.);
#2489=EDGE_CURVE('',#1948,#1952,#377,.F.);
#2490=EDGE_CURVE('',#1949,#1954,#378,.T.);
#2491=EDGE_CURVE('',#1954,#1953,#379,.T.);
#2492=EDGE_CURVE('',#1955,#1956,#1227,.T.);
#2493=EDGE_CURVE('',#1957,#1955,#380,.T.);
#2494=EDGE_CURVE('',#1952,#1957,#381,.F.);
#2495=EDGE_CURVE('',#1953,#1956,#382,.T.);
#2496=EDGE_CURVE('',#1958,#1959,#1228,.T.);
#2497=EDGE_CURVE('',#1960,#1958,#383,.T.);
#2498=EDGE_CURVE('',#1955,#1960,#384,.T.);
#2499=EDGE_CURVE('',#1956,#1961,#385,.T.);
#2500=EDGE_CURVE('',#1961,#1959,#386,.T.);
#2501=EDGE_CURVE('',#1962,#1963,#1229,.T.);
#2502=EDGE_CURVE('',#1964,#1962,#387,.F.);
#2503=EDGE_CURVE('',#1958,#1964,#388,.T.);
#2504=EDGE_CURVE('',#1959,#1963,#389,.T.);
#2505=EDGE_CURVE('',#1965,#1966,#1230,.T.);
#2506=EDGE_CURVE('',#1962,#1965,#390,.F.);
#2507=EDGE_CURVE('',#1963,#1967,#391,.T.);
#2508=EDGE_CURVE('',#1967,#1966,#392,.T.);
#2509=EDGE_CURVE('',#1966,#1968,#393,.T.);
#2510=EDGE_CURVE('',#1968,#1969,#394,.T.);
#2511=EDGE_CURVE('',#1970,#1969,#1598,.T.);
#2512=EDGE_CURVE('',#1971,#1970,#395,.T.);
#2513=EDGE_CURVE('',#1965,#1971,#396,.F.);
#2514=EDGE_CURVE('',#1873,#1972,#397,.T.);
#2515=EDGE_CURVE('',#1972,#1973,#1599,.T.);
#2516=EDGE_CURVE('',#1973,#1872,#398,.T.);
#2517=EDGE_CURVE('',#1974,#1972,#399,.T.);
#2518=EDGE_CURVE('',#1975,#1974,#1600,.T.);
#2519=EDGE_CURVE('',#1973,#1975,#400,.T.);
#2520=EDGE_CURVE('',#1969,#1975,#408,.T.);
#2521=EDGE_CURVE('',#1818,#1877,#401,.T.);
#2522=EDGE_CURVE('',#1976,#1819,#402,.T.);
#2523=EDGE_CURVE('',#1976,#1876,#403,.T.);
#2524=EDGE_CURVE('',#1974,#1970,#409,.T.);
#2525=EDGE_CURVE('',#1977,#1978,#1231,.T.);
#2526=EDGE_CURVE('',#1977,#1979,#1232,.T.);
#2527=EDGE_CURVE('',#1979,#1980,#1233,.T.);
#2528=EDGE_CURVE('',#1978,#1980,#1234,.T.);
#2529=EDGE_CURVE('',#1981,#1977,#1235,.T.);
#2530=EDGE_CURVE('',#1981,#1982,#1236,.T.);
#2531=EDGE_CURVE('',#1982,#1979,#1237,.T.);
#2532=EDGE_CURVE('',#1983,#1981,#1238,.T.);
#2533=EDGE_CURVE('',#1983,#1984,#1239,.T.);
#2534=EDGE_CURVE('',#1984,#1982,#1240,.T.);
#2535=EDGE_CURVE('',#1985,#1983,#1241,.T.);
#2536=EDGE_CURVE('',#1985,#1986,#1242,.T.);
#2537=EDGE_CURVE('',#1986,#1984,#1243,.T.);
#2538=EDGE_CURVE('',#1987,#1985,#1244,.T.);
#2539=EDGE_CURVE('',#1987,#1988,#1245,.T.);
#2540=EDGE_CURVE('',#1988,#1986,#1246,.T.);
#2541=EDGE_CURVE('',#1978,#1987,#1247,.T.);
#2542=EDGE_CURVE('',#1980,#1988,#1248,.T.);
#2543=EDGE_CURVE('',#1989,#1989,#1601,.T.);
#2544=EDGE_CURVE('',#1989,#1990,#1249,.T.);
#2545=EDGE_CURVE('',#1990,#1990,#1602,.T.);
#3139=ORIENTED_EDGE('',*,*,#2303,.F.);
#3140=ORIENTED_EDGE('',*,*,#2304,.T.);
#3141=ORIENTED_EDGE('',*,*,#2305,.T.);
#3142=ORIENTED_EDGE('',*,*,#2306,.T.);
#3143=ORIENTED_EDGE('',*,*,#2307,.F.);
#3144=ORIENTED_EDGE('',*,*,#2308,.T.);
#3145=ORIENTED_EDGE('',*,*,#2303,.T.);
#3146=ORIENTED_EDGE('',*,*,#2309,.T.);
#3147=ORIENTED_EDGE('',*,*,#2310,.F.);
#3148=ORIENTED_EDGE('',*,*,#2311,.T.);
#3149=ORIENTED_EDGE('',*,*,#2307,.T.);
#3150=ORIENTED_EDGE('',*,*,#2312,.T.);
#3151=ORIENTED_EDGE('',*,*,#2313,.F.);
#3152=ORIENTED_EDGE('',*,*,#2314,.T.);
#3153=ORIENTED_EDGE('',*,*,#2310,.T.);
#3154=ORIENTED_EDGE('',*,*,#2315,.T.);
#3155=ORIENTED_EDGE('',*,*,#2316,.F.);
#3156=ORIENTED_EDGE('',*,*,#2317,.T.);
#3157=ORIENTED_EDGE('',*,*,#2313,.T.);
#3158=ORIENTED_EDGE('',*,*,#2318,.T.);
#3159=ORIENTED_EDGE('',*,*,#2319,.F.);
#3160=ORIENTED_EDGE('',*,*,#2320,.T.);
#3161=ORIENTED_EDGE('',*,*,#2316,.T.);
#3162=ORIENTED_EDGE('',*,*,#2321,.T.);
#3163=ORIENTED_EDGE('',*,*,#2322,.F.);
#3164=ORIENTED_EDGE('',*,*,#2323,.T.);
#3165=ORIENTED_EDGE('',*,*,#2319,.T.);
#3166=ORIENTED_EDGE('',*,*,#2324,.T.);
#3167=ORIENTED_EDGE('',*,*,#2325,.F.);
#3168=ORIENTED_EDGE('',*,*,#2326,.T.);
#3169=ORIENTED_EDGE('',*,*,#2322,.T.);
#3170=ORIENTED_EDGE('',*,*,#2327,.T.);
#3171=ORIENTED_EDGE('',*,*,#2328,.F.);
#3172=ORIENTED_EDGE('',*,*,#2329,.T.);
#3173=ORIENTED_EDGE('',*,*,#2325,.T.);
#3174=ORIENTED_EDGE('',*,*,#2330,.T.);
#3175=ORIENTED_EDGE('',*,*,#2331,.F.);
#3176=ORIENTED_EDGE('',*,*,#2332,.T.);
#3177=ORIENTED_EDGE('',*,*,#2328,.T.);
#3178=ORIENTED_EDGE('',*,*,#2333,.T.);
#3179=ORIENTED_EDGE('',*,*,#2334,.F.);
#3180=ORIENTED_EDGE('',*,*,#2335,.T.);
#3181=ORIENTED_EDGE('',*,*,#2331,.T.);
#3182=ORIENTED_EDGE('',*,*,#2336,.T.);
#3183=ORIENTED_EDGE('',*,*,#2337,.F.);
#3184=ORIENTED_EDGE('',*,*,#2338,.T.);
#3185=ORIENTED_EDGE('',*,*,#2334,.T.);
#3186=ORIENTED_EDGE('',*,*,#2339,.T.);
#3187=ORIENTED_EDGE('',*,*,#2340,.F.);
#3188=ORIENTED_EDGE('',*,*,#2341,.T.);
#3189=ORIENTED_EDGE('',*,*,#2337,.T.);
#3190=ORIENTED_EDGE('',*,*,#2342,.T.);
#3191=ORIENTED_EDGE('',*,*,#2343,.F.);
#3192=ORIENTED_EDGE('',*,*,#2344,.T.);
#3193=ORIENTED_EDGE('',*,*,#2340,.T.);
#3194=ORIENTED_EDGE('',*,*,#2345,.T.);
#3195=ORIENTED_EDGE('',*,*,#2346,.F.);
#3196=ORIENTED_EDGE('',*,*,#2347,.T.);
#3197=ORIENTED_EDGE('',*,*,#2343,.T.);
#3198=ORIENTED_EDGE('',*,*,#2348,.T.);
#3199=ORIENTED_EDGE('',*,*,#2349,.F.);
#3200=ORIENTED_EDGE('',*,*,#2350,.T.);
#3201=ORIENTED_EDGE('',*,*,#2346,.T.);
#3202=ORIENTED_EDGE('',*,*,#2351,.T.);
#3203=ORIENTED_EDGE('',*,*,#2352,.F.);
#3204=ORIENTED_EDGE('',*,*,#2353,.T.);
#3205=ORIENTED_EDGE('',*,*,#2349,.T.);
#3206=ORIENTED_EDGE('',*,*,#2354,.T.);
#3207=ORIENTED_EDGE('',*,*,#2355,.F.);
#3208=ORIENTED_EDGE('',*,*,#2356,.T.);
#3209=ORIENTED_EDGE('',*,*,#2352,.T.);
#3210=ORIENTED_EDGE('',*,*,#2357,.T.);
#3211=ORIENTED_EDGE('',*,*,#2358,.F.);
#3212=ORIENTED_EDGE('',*,*,#2359,.T.);
#3213=ORIENTED_EDGE('',*,*,#2355,.T.);
#3214=ORIENTED_EDGE('',*,*,#2360,.T.);
#3215=ORIENTED_EDGE('',*,*,#2361,.F.);
#3216=ORIENTED_EDGE('',*,*,#2362,.T.);
#3217=ORIENTED_EDGE('',*,*,#2358,.T.);
#3218=ORIENTED_EDGE('',*,*,#2363,.T.);
#3219=ORIENTED_EDGE('',*,*,#2364,.F.);
#3220=ORIENTED_EDGE('',*,*,#2365,.T.);
#3221=ORIENTED_EDGE('',*,*,#2361,.T.);
#3222=ORIENTED_EDGE('',*,*,#2366,.T.);
#3223=ORIENTED_EDGE('',*,*,#2367,.F.);
#3224=ORIENTED_EDGE('',*,*,#2368,.T.);
#3225=ORIENTED_EDGE('',*,*,#2364,.T.);
#3226=ORIENTED_EDGE('',*,*,#2369,.T.);
#3227=ORIENTED_EDGE('',*,*,#2370,.F.);
#3228=ORIENTED_EDGE('',*,*,#2371,.T.);
#3229=ORIENTED_EDGE('',*,*,#2367,.T.);
#3230=ORIENTED_EDGE('',*,*,#2372,.T.);
#3231=ORIENTED_EDGE('',*,*,#2373,.F.);
#3232=ORIENTED_EDGE('',*,*,#2374,.T.);
#3233=ORIENTED_EDGE('',*,*,#2370,.T.);
#3234=ORIENTED_EDGE('',*,*,#2375,.T.);
#3235=ORIENTED_EDGE('',*,*,#2376,.F.);
#3236=ORIENTED_EDGE('',*,*,#2377,.T.);
#3237=ORIENTED_EDGE('',*,*,#2373,.T.);
#3238=ORIENTED_EDGE('',*,*,#2378,.T.);
#3239=ORIENTED_EDGE('',*,*,#2379,.F.);
#3240=ORIENTED_EDGE('',*,*,#2380,.T.);
#3241=ORIENTED_EDGE('',*,*,#2376,.T.);
#3242=ORIENTED_EDGE('',*,*,#2381,.T.);
#3243=ORIENTED_EDGE('',*,*,#2382,.F.);
#3244=ORIENTED_EDGE('',*,*,#2383,.T.);
#3245=ORIENTED_EDGE('',*,*,#2379,.T.);
#3246=ORIENTED_EDGE('',*,*,#2384,.T.);
#3247=ORIENTED_EDGE('',*,*,#2385,.F.);
#3248=ORIENTED_EDGE('',*,*,#2386,.T.);
#3249=ORIENTED_EDGE('',*,*,#2382,.T.);
#3250=ORIENTED_EDGE('',*,*,#2387,.T.);
#3251=ORIENTED_EDGE('',*,*,#2388,.F.);
#3252=ORIENTED_EDGE('',*,*,#2389,.F.);
#3253=ORIENTED_EDGE('',*,*,#2390,.F.);
#3254=ORIENTED_EDGE('',*,*,#2391,.T.);
#3255=ORIENTED_EDGE('',*,*,#2392,.F.);
#3256=ORIENTED_EDGE('',*,*,#2393,.F.);
#3257=ORIENTED_EDGE('',*,*,#2388,.T.);
#3258=ORIENTED_EDGE('',*,*,#2394,.T.);
#3259=ORIENTED_EDGE('',*,*,#2395,.T.);
#3260=ORIENTED_EDGE('',*,*,#2396,.F.);
#3261=ORIENTED_EDGE('',*,*,#2397,.F.);
#3262=ORIENTED_EDGE('',*,*,#2398,.F.);
#3263=ORIENTED_EDGE('',*,*,#2392,.T.);
#3264=ORIENTED_EDGE('',*,*,#2399,.T.);
#3265=ORIENTED_EDGE('',*,*,#2400,.T.);
#3266=ORIENTED_EDGE('',*,*,#2401,.F.);
#3267=ORIENTED_EDGE('',*,*,#2402,.F.);
#3268=ORIENTED_EDGE('',*,*,#2396,.T.);
#3269=ORIENTED_EDGE('',*,*,#2403,.T.);
#3270=ORIENTED_EDGE('',*,*,#2404,.T.);
#3271=ORIENTED_EDGE('',*,*,#2405,.F.);
#3272=ORIENTED_EDGE('',*,*,#2406,.F.);
#3273=ORIENTED_EDGE('',*,*,#2407,.F.);
#3274=ORIENTED_EDGE('',*,*,#2401,.T.);
#3275=ORIENTED_EDGE('',*,*,#2408,.T.);
#3276=ORIENTED_EDGE('',*,*,#2409,.F.);
#3277=ORIENTED_EDGE('',*,*,#2410,.F.);
#3278=ORIENTED_EDGE('',*,*,#2411,.F.);
#3279=ORIENTED_EDGE('',*,*,#2405,.T.);
#3280=ORIENTED_EDGE('',*,*,#2412,.T.);
#3281=ORIENTED_EDGE('',*,*,#2413,.T.);
#3282=ORIENTED_EDGE('',*,*,#2414,.F.);
#3283=ORIENTED_EDGE('',*,*,#2415,.F.);
#3284=ORIENTED_EDGE('',*,*,#2409,.T.);
#3285=ORIENTED_EDGE('',*,*,#2416,.T.);
#3286=ORIENTED_EDGE('',*,*,#2417,.T.);
#3287=ORIENTED_EDGE('',*,*,#2418,.F.);
#3288=ORIENTED_EDGE('',*,*,#2419,.F.);
#3289=ORIENTED_EDGE('',*,*,#2420,.F.);
#3290=ORIENTED_EDGE('',*,*,#2414,.T.);
#3291=ORIENTED_EDGE('',*,*,#2421,.T.);
#3292=ORIENTED_EDGE('',*,*,#2422,.F.);
#3293=ORIENTED_EDGE('',*,*,#2423,.F.);
#3294=ORIENTED_EDGE('',*,*,#2418,.T.);
#3295=ORIENTED_EDGE('',*,*,#2424,.T.);
#3296=ORIENTED_EDGE('',*,*,#2425,.T.);
#3297=ORIENTED_EDGE('',*,*,#2426,.F.);
#3298=ORIENTED_EDGE('',*,*,#2427,.F.);
#3299=ORIENTED_EDGE('',*,*,#2428,.F.);
#3300=ORIENTED_EDGE('',*,*,#2422,.T.);
#3301=ORIENTED_EDGE('',*,*,#2429,.T.);
#3302=ORIENTED_EDGE('',*,*,#2430,.F.);
#3303=ORIENTED_EDGE('',*,*,#2431,.F.);
#3304=ORIENTED_EDGE('',*,*,#2426,.T.);
#3305=ORIENTED_EDGE('',*,*,#2432,.T.);
#3306=ORIENTED_EDGE('',*,*,#2433,.T.);
#3307=ORIENTED_EDGE('',*,*,#2434,.F.);
#3308=ORIENTED_EDGE('',*,*,#2435,.F.);
#3309=ORIENTED_EDGE('',*,*,#2436,.F.);
#3310=ORIENTED_EDGE('',*,*,#2430,.T.);
#3311=ORIENTED_EDGE('',*,*,#2437,.T.);
#3312=ORIENTED_EDGE('',*,*,#2438,.F.);
#3313=ORIENTED_EDGE('',*,*,#2439,.F.);
#3314=ORIENTED_EDGE('',*,*,#2440,.F.);
#3315=ORIENTED_EDGE('',*,*,#2434,.T.);
#3316=ORIENTED_EDGE('',*,*,#2441,.T.);
#3317=ORIENTED_EDGE('',*,*,#2442,.T.);
#3318=ORIENTED_EDGE('',*,*,#2443,.F.);
#3319=ORIENTED_EDGE('',*,*,#2444,.F.);
#3320=ORIENTED_EDGE('',*,*,#2445,.F.);
#3321=ORIENTED_EDGE('',*,*,#2438,.T.);
#3322=ORIENTED_EDGE('',*,*,#2446,.T.);
#3323=ORIENTED_EDGE('',*,*,#2447,.T.);
#3324=ORIENTED_EDGE('',*,*,#2448,.F.);
#3325=ORIENTED_EDGE('',*,*,#2449,.F.);
#3326=ORIENTED_EDGE('',*,*,#2443,.T.);
#3327=ORIENTED_EDGE('',*,*,#2450,.T.);
#3328=ORIENTED_EDGE('',*,*,#2451,.T.);
#3329=ORIENTED_EDGE('',*,*,#2452,.F.);
#3330=ORIENTED_EDGE('',*,*,#2453,.F.);
#3331=ORIENTED_EDGE('',*,*,#2454,.F.);
#3332=ORIENTED_EDGE('',*,*,#2448,.T.);
#3333=ORIENTED_EDGE('',*,*,#2455,.T.);
#3334=ORIENTED_EDGE('',*,*,#2456,.T.);
#3335=ORIENTED_EDGE('',*,*,#2457,.F.);
#3336=ORIENTED_EDGE('',*,*,#2458,.F.);
#3337=ORIENTED_EDGE('',*,*,#2452,.T.);
#3338=ORIENTED_EDGE('',*,*,#2459,.T.);
#3339=ORIENTED_EDGE('',*,*,#2460,.F.);
#3340=ORIENTED_EDGE('',*,*,#2461,.F.);
#3341=ORIENTED_EDGE('',*,*,#2462,.F.);
#3342=ORIENTED_EDGE('',*,*,#2457,.T.);
#3343=ORIENTED_EDGE('',*,*,#2463,.T.);
#3344=ORIENTED_EDGE('',*,*,#2464,.T.);
#3345=ORIENTED_EDGE('',*,*,#2465,.F.);
#3346=ORIENTED_EDGE('',*,*,#2466,.F.);
#3347=ORIENTED_EDGE('',*,*,#2460,.T.);
#3348=ORIENTED_EDGE('',*,*,#2467,.T.);
#3349=ORIENTED_EDGE('',*,*,#2468,.T.);
#3350=ORIENTED_EDGE('',*,*,#2469,.F.);
#3351=ORIENTED_EDGE('',*,*,#2470,.F.);
#3352=ORIENTED_EDGE('',*,*,#2471,.F.);
#3353=ORIENTED_EDGE('',*,*,#2465,.T.);
#3354=ORIENTED_EDGE('',*,*,#2472,.T.);
#3355=ORIENTED_EDGE('',*,*,#2473,.T.);
#3356=ORIENTED_EDGE('',*,*,#2474,.F.);
#3357=ORIENTED_EDGE('',*,*,#2475,.F.);
#3358=ORIENTED_EDGE('',*,*,#2476,.F.);
#3359=ORIENTED_EDGE('',*,*,#2469,.T.);
#3360=ORIENTED_EDGE('',*,*,#2477,.T.);
#3361=ORIENTED_EDGE('',*,*,#2478,.T.);
#3362=ORIENTED_EDGE('',*,*,#2479,.F.);
#3363=ORIENTED_EDGE('',*,*,#2480,.F.);
#3364=ORIENTED_EDGE('',*,*,#2481,.F.);
#3365=ORIENTED_EDGE('',*,*,#2474,.T.);
#3366=ORIENTED_EDGE('',*,*,#2482,.T.);
#3367=ORIENTED_EDGE('',*,*,#2483,.F.);
#3368=ORIENTED_EDGE('',*,*,#2484,.F.);
#3369=ORIENTED_EDGE('',*,*,#2485,.F.);
#3370=ORIENTED_EDGE('',*,*,#2479,.T.);
#3371=ORIENTED_EDGE('',*,*,#2486,.T.);
#3372=ORIENTED_EDGE('',*,*,#2487,.T.);
#3373=ORIENTED_EDGE('',*,*,#2488,.F.);
#3374=ORIENTED_EDGE('',*,*,#2489,.F.);
#3375=ORIENTED_EDGE('',*,*,#2483,.T.);
#3376=ORIENTED_EDGE('',*,*,#2490,.T.);
#3377=ORIENTED_EDGE('',*,*,#2491,.T.);
#3378=ORIENTED_EDGE('',*,*,#2492,.F.);
#3379=ORIENTED_EDGE('',*,*,#2493,.F.);
#3380=ORIENTED_EDGE('',*,*,#2494,.F.);
#3381=ORIENTED_EDGE('',*,*,#2488,.T.);
#3382=ORIENTED_EDGE('',*,*,#2495,.T.);
#3383=ORIENTED_EDGE('',*,*,#2496,.F.);
#3384=ORIENTED_EDGE('',*,*,#2497,.F.);
#3385=ORIENTED_EDGE('',*,*,#2498,.F.);
#3386=ORIENTED_EDGE('',*,*,#2492,.T.);
#3387=ORIENTED_EDGE('',*,*,#2499,.T.);
#3388=ORIENTED_EDGE('',*,*,#2500,.T.);
#3389=ORIENTED_EDGE('',*,*,#2501,.F.);
#3390=ORIENTED_EDGE('',*,*,#2502,.F.);
#3391=ORIENTED_EDGE('',*,*,#2503,.F.);
#3392=ORIENTED_EDGE('',*,*,#2496,.T.);
#3393=ORIENTED_EDGE('',*,*,#2504,.T.);
#3394=ORIENTED_EDGE('',*,*,#2505,.F.);
#3395=ORIENTED_EDGE('',*,*,#2506,.F.);
#3396=ORIENTED_EDGE('',*,*,#2501,.T.);
#3397=ORIENTED_EDGE('',*,*,#2507,.T.);
#3398=ORIENTED_EDGE('',*,*,#2508,.T.);
#3399=ORIENTED_EDGE('',*,*,#2505,.T.);
#3400=ORIENTED_EDGE('',*,*,#2509,.T.);
#3401=ORIENTED_EDGE('',*,*,#2510,.T.);
#3402=ORIENTED_EDGE('',*,*,#2511,.F.);
#3403=ORIENTED_EDGE('',*,*,#2512,.F.);
#3404=ORIENTED_EDGE('',*,*,#2513,.F.);
#3405=ORIENTED_EDGE('',*,*,#2385,.T.);
#3406=ORIENTED_EDGE('',*,*,#2514,.T.);
#3407=ORIENTED_EDGE('',*,*,#2515,.T.);
#3408=ORIENTED_EDGE('',*,*,#2516,.T.);
#3409=ORIENTED_EDGE('',*,*,#2517,.F.);
#3410=ORIENTED_EDGE('',*,*,#2518,.F.);
#3411=ORIENTED_EDGE('',*,*,#2519,.F.);
#3412=ORIENTED_EDGE('',*,*,#2515,.F.);
#3413=ORIENTED_EDGE('',*,*,#2519,.T.);
#3414=ORIENTED_EDGE('',*,*,#2520,.F.);
#3415=ORIENTED_EDGE('',*,*,#2510,.F.);
#3416=ORIENTED_EDGE('',*,*,#2509,.F.);
#3417=ORIENTED_EDGE('',*,*,#2508,.F.);
#3418=ORIENTED_EDGE('',*,*,#2507,.F.);
#3419=ORIENTED_EDGE('',*,*,#2504,.F.);
#3420=ORIENTED_EDGE('',*,*,#2500,.F.);
#3421=ORIENTED_EDGE('',*,*,#2499,.F.);
#3422=ORIENTED_EDGE('',*,*,#2495,.F.);
#3423=ORIENTED_EDGE('',*,*,#2491,.F.);
#3424=ORIENTED_EDGE('',*,*,#2490,.F.);
#3425=ORIENTED_EDGE('',*,*,#2487,.F.);
#3426=ORIENTED_EDGE('',*,*,#2486,.F.);
#3427=ORIENTED_EDGE('',*,*,#2482,.F.);
#3428=ORIENTED_EDGE('',*,*,#2478,.F.);
#3429=ORIENTED_EDGE('',*,*,#2477,.F.);
#3430=ORIENTED_EDGE('',*,*,#2473,.F.);
#3431=ORIENTED_EDGE('',*,*,#2472,.F.);
#3432=ORIENTED_EDGE('',*,*,#2468,.F.);
#3433=ORIENTED_EDGE('',*,*,#2467,.F.);
#3434=ORIENTED_EDGE('',*,*,#2464,.F.);
#3435=ORIENTED_EDGE('',*,*,#2463,.F.);
#3436=ORIENTED_EDGE('',*,*,#2459,.F.);
#3437=ORIENTED_EDGE('',*,*,#2456,.F.);
#3438=ORIENTED_EDGE('',*,*,#2455,.F.);
#3439=ORIENTED_EDGE('',*,*,#2451,.F.);
#3440=ORIENTED_EDGE('',*,*,#2450,.F.);
#3441=ORIENTED_EDGE('',*,*,#2447,.F.);
#3442=ORIENTED_EDGE('',*,*,#2446,.F.);
#3443=ORIENTED_EDGE('',*,*,#2442,.F.);
#3444=ORIENTED_EDGE('',*,*,#2441,.F.);
#3445=ORIENTED_EDGE('',*,*,#2437,.F.);
#3446=ORIENTED_EDGE('',*,*,#2433,.F.);
#3447=ORIENTED_EDGE('',*,*,#2432,.F.);
#3448=ORIENTED_EDGE('',*,*,#2429,.F.);
#3449=ORIENTED_EDGE('',*,*,#2425,.F.);
#3450=ORIENTED_EDGE('',*,*,#2424,.F.);
#3451=ORIENTED_EDGE('',*,*,#2421,.F.);
#3452=ORIENTED_EDGE('',*,*,#2417,.F.);
#3453=ORIENTED_EDGE('',*,*,#2416,.F.);
#3454=ORIENTED_EDGE('',*,*,#2413,.F.);
#3455=ORIENTED_EDGE('',*,*,#2412,.F.);
#3456=ORIENTED_EDGE('',*,*,#2408,.F.);
#3457=ORIENTED_EDGE('',*,*,#2404,.F.);
#3458=ORIENTED_EDGE('',*,*,#2403,.F.);
#3459=ORIENTED_EDGE('',*,*,#2400,.F.);
#3460=ORIENTED_EDGE('',*,*,#2399,.F.);
#3461=ORIENTED_EDGE('',*,*,#2395,.F.);
#3462=ORIENTED_EDGE('',*,*,#2394,.F.);
#3463=ORIENTED_EDGE('',*,*,#2391,.F.);
#3464=ORIENTED_EDGE('',*,*,#2521,.F.);
#3465=ORIENTED_EDGE('',*,*,#2304,.F.);
#3466=ORIENTED_EDGE('',*,*,#2308,.F.);
#3467=ORIENTED_EDGE('',*,*,#2311,.F.);
#3468=ORIENTED_EDGE('',*,*,#2314,.F.);
#3469=ORIENTED_EDGE('',*,*,#2317,.F.);
#3470=ORIENTED_EDGE('',*,*,#2320,.F.);
#3471=ORIENTED_EDGE('',*,*,#2323,.F.);
#3472=ORIENTED_EDGE('',*,*,#2326,.F.);
#3473=ORIENTED_EDGE('',*,*,#2329,.F.);
#3474=ORIENTED_EDGE('',*,*,#2332,.F.);
#3475=ORIENTED_EDGE('',*,*,#2335,.F.);
#3476=ORIENTED_EDGE('',*,*,#2338,.F.);
#3477=ORIENTED_EDGE('',*,*,#2341,.F.);
#3478=ORIENTED_EDGE('',*,*,#2344,.F.);
#3479=ORIENTED_EDGE('',*,*,#2347,.F.);
#3480=ORIENTED_EDGE('',*,*,#2350,.F.);
#3481=ORIENTED_EDGE('',*,*,#2353,.F.);
#3482=ORIENTED_EDGE('',*,*,#2356,.F.);
#3483=ORIENTED_EDGE('',*,*,#2359,.F.);
#3484=ORIENTED_EDGE('',*,*,#2362,.F.);
#3485=ORIENTED_EDGE('',*,*,#2365,.F.);
#3486=ORIENTED_EDGE('',*,*,#2368,.F.);
#3487=ORIENTED_EDGE('',*,*,#2371,.F.);
#3488=ORIENTED_EDGE('',*,*,#2374,.F.);
#3489=ORIENTED_EDGE('',*,*,#2377,.F.);
#3490=ORIENTED_EDGE('',*,*,#2380,.F.);
#3491=ORIENTED_EDGE('',*,*,#2383,.F.);
#3492=ORIENTED_EDGE('',*,*,#2386,.F.);
#3493=ORIENTED_EDGE('',*,*,#2516,.F.);
#3494=ORIENTED_EDGE('',*,*,#2517,.T.);
#3495=ORIENTED_EDGE('',*,*,#2514,.F.);
#3496=ORIENTED_EDGE('',*,*,#2387,.F.);
#3497=ORIENTED_EDGE('',*,*,#2384,.F.);
#3498=ORIENTED_EDGE('',*,*,#2381,.F.);
#3499=ORIENTED_EDGE('',*,*,#2378,.F.);
#3500=ORIENTED_EDGE('',*,*,#2375,.F.);
#3501=ORIENTED_EDGE('',*,*,#2372,.F.);
#3502=ORIENTED_EDGE('',*,*,#2369,.F.);
#3503=ORIENTED_EDGE('',*,*,#2366,.F.);
#3504=ORIENTED_EDGE('',*,*,#2363,.F.);
#3505=ORIENTED_EDGE('',*,*,#2360,.F.);
#3506=ORIENTED_EDGE('',*,*,#2357,.F.);
#3507=ORIENTED_EDGE('',*,*,#2354,.F.);
#3508=ORIENTED_EDGE('',*,*,#2351,.F.);
#3509=ORIENTED_EDGE('',*,*,#2348,.F.);
#3510=ORIENTED_EDGE('',*,*,#2345,.F.);
#3511=ORIENTED_EDGE('',*,*,#2342,.F.);
#3512=ORIENTED_EDGE('',*,*,#2339,.F.);
#3513=ORIENTED_EDGE('',*,*,#2336,.F.);
#3514=ORIENTED_EDGE('',*,*,#2333,.F.);
#3515=ORIENTED_EDGE('',*,*,#2330,.F.);
#3516=ORIENTED_EDGE('',*,*,#2327,.F.);
#3517=ORIENTED_EDGE('',*,*,#2324,.F.);
#3518=ORIENTED_EDGE('',*,*,#2321,.F.);
#3519=ORIENTED_EDGE('',*,*,#2318,.F.);
#3520=ORIENTED_EDGE('',*,*,#2315,.F.);
#3521=ORIENTED_EDGE('',*,*,#2312,.F.);
#3522=ORIENTED_EDGE('',*,*,#2309,.F.);
#3523=ORIENTED_EDGE('',*,*,#2306,.F.);
#3524=ORIENTED_EDGE('',*,*,#2522,.F.);
#3525=ORIENTED_EDGE('',*,*,#2523,.T.);
#3526=ORIENTED_EDGE('',*,*,#2389,.T.);
#3527=ORIENTED_EDGE('',*,*,#2393,.T.);
#3528=ORIENTED_EDGE('',*,*,#2398,.T.);
#3529=ORIENTED_EDGE('',*,*,#2397,.T.);
#3530=ORIENTED_EDGE('',*,*,#2402,.T.);
#3531=ORIENTED_EDGE('',*,*,#2407,.T.);
#3532=ORIENTED_EDGE('',*,*,#2406,.T.);
#3533=ORIENTED_EDGE('',*,*,#2411,.T.);
#3534=ORIENTED_EDGE('',*,*,#2410,.T.);
#3535=ORIENTED_EDGE('',*,*,#2415,.T.);
#3536=ORIENTED_EDGE('',*,*,#2420,.T.);
#3537=ORIENTED_EDGE('',*,*,#2419,.T.);
#3538=ORIENTED_EDGE('',*,*,#2423,.T.);
#3539=ORIENTED_EDGE('',*,*,#2428,.T.);
#3540=ORIENTED_EDGE('',*,*,#2427,.T.);
#3541=ORIENTED_EDGE('',*,*,#2431,.T.);
#3542=ORIENTED_EDGE('',*,*,#2436,.T.);
#3543=ORIENTED_EDGE('',*,*,#2435,.T.);
#3544=ORIENTED_EDGE('',*,*,#2440,.T.);
#3545=ORIENTED_EDGE('',*,*,#2439,.T.);
#3546=ORIENTED_EDGE('',*,*,#2445,.T.);
#3547=ORIENTED_EDGE('',*,*,#2444,.T.);
#3548=ORIENTED_EDGE('',*,*,#2449,.T.);
#3549=ORIENTED_EDGE('',*,*,#2454,.T.);
#3550=ORIENTED_EDGE('',*,*,#2453,.T.);
#3551=ORIENTED_EDGE('',*,*,#2458,.T.);
#3552=ORIENTED_EDGE('',*,*,#2462,.T.);
#3553=ORIENTED_EDGE('',*,*,#2461,.T.);
#3554=ORIENTED_EDGE('',*,*,#2466,.T.);
#3555=ORIENTED_EDGE('',*,*,#2471,.T.);
#3556=ORIENTED_EDGE('',*,*,#2470,.T.);
#3557=ORIENTED_EDGE('',*,*,#2476,.T.);
#3558=ORIENTED_EDGE('',*,*,#2475,.T.);
#3559=ORIENTED_EDGE('',*,*,#2481,.T.);
#3560=ORIENTED_EDGE('',*,*,#2480,.T.);
#3561=ORIENTED_EDGE('',*,*,#2485,.T.);
#3562=ORIENTED_EDGE('',*,*,#2484,.T.);
#3563=ORIENTED_EDGE('',*,*,#2489,.T.);
#3564=ORIENTED_EDGE('',*,*,#2494,.T.);
#3565=ORIENTED_EDGE('',*,*,#2493,.T.);
#3566=ORIENTED_EDGE('',*,*,#2498,.T.);
#3567=ORIENTED_EDGE('',*,*,#2497,.T.);
#3568=ORIENTED_EDGE('',*,*,#2503,.T.);
#3569=ORIENTED_EDGE('',*,*,#2502,.T.);
#3570=ORIENTED_EDGE('',*,*,#2506,.T.);
#3571=ORIENTED_EDGE('',*,*,#2513,.T.);
#3572=ORIENTED_EDGE('',*,*,#2512,.T.);
#3573=ORIENTED_EDGE('',*,*,#2524,.F.);
#3574=ORIENTED_EDGE('',*,*,#2525,.F.);
#3575=ORIENTED_EDGE('',*,*,#2526,.T.);
#3576=ORIENTED_EDGE('',*,*,#2527,.T.);
#3577=ORIENTED_EDGE('',*,*,#2528,.F.);
#3578=ORIENTED_EDGE('',*,*,#2529,.F.);
#3579=ORIENTED_EDGE('',*,*,#2530,.T.);
#3580=ORIENTED_EDGE('',*,*,#2531,.T.);
#3581=ORIENTED_EDGE('',*,*,#2526,.F.);
#3582=ORIENTED_EDGE('',*,*,#2532,.F.);
#3583=ORIENTED_EDGE('',*,*,#2533,.T.);
#3584=ORIENTED_EDGE('',*,*,#2534,.T.);
#3585=ORIENTED_EDGE('',*,*,#2530,.F.);
#3586=ORIENTED_EDGE('',*,*,#2535,.F.);
#3587=ORIENTED_EDGE('',*,*,#2536,.T.);
#3588=ORIENTED_EDGE('',*,*,#2537,.T.);
#3589=ORIENTED_EDGE('',*,*,#2533,.F.);
#3590=ORIENTED_EDGE('',*,*,#2538,.F.);
#3591=ORIENTED_EDGE('',*,*,#2539,.T.);
#3592=ORIENTED_EDGE('',*,*,#2540,.T.);
#3593=ORIENTED_EDGE('',*,*,#2536,.F.);
#3594=ORIENTED_EDGE('',*,*,#2541,.F.);
#3595=ORIENTED_EDGE('',*,*,#2528,.T.);
#3596=ORIENTED_EDGE('',*,*,#2542,.T.);
#3597=ORIENTED_EDGE('',*,*,#2539,.F.);
#3598=ORIENTED_EDGE('',*,*,#2542,.F.);
#3599=ORIENTED_EDGE('',*,*,#2527,.F.);
#3600=ORIENTED_EDGE('',*,*,#2531,.F.);
#3601=ORIENTED_EDGE('',*,*,#2534,.F.);
#3602=ORIENTED_EDGE('',*,*,#2537,.F.);
#3603=ORIENTED_EDGE('',*,*,#2540,.F.);
#3604=ORIENTED_EDGE('',*,*,#2543,.T.);
#3605=ORIENTED_EDGE('',*,*,#2521,.T.);
#3606=ORIENTED_EDGE('',*,*,#2390,.T.);
#3607=ORIENTED_EDGE('',*,*,#2523,.F.);
#3608=ORIENTED_EDGE('',*,*,#2522,.T.);
#3609=ORIENTED_EDGE('',*,*,#2305,.F.);
#3610=ORIENTED_EDGE('',*,*,#2543,.F.);
#3611=ORIENTED_EDGE('',*,*,#2544,.T.);
#3612=ORIENTED_EDGE('',*,*,#2545,.T.);
#3613=ORIENTED_EDGE('',*,*,#2544,.F.);
#3614=ORIENTED_EDGE('',*,*,#2545,.F.);
#3615=ORIENTED_EDGE('',*,*,#2525,.T.);
#3616=ORIENTED_EDGE('',*,*,#2541,.T.);
#3617=ORIENTED_EDGE('',*,*,#2538,.T.);
#3618=ORIENTED_EDGE('',*,*,#2535,.T.);
#3619=ORIENTED_EDGE('',*,*,#2532,.T.);
#3620=ORIENTED_EDGE('',*,*,#2529,.T.);
#3621=ORIENTED_EDGE('',*,*,#2518,.T.);
#3622=ORIENTED_EDGE('',*,*,#2524,.T.);
#3623=ORIENTED_EDGE('',*,*,#2511,.T.);
#3624=ORIENTED_EDGE('',*,*,#2520,.T.);
#3856=CYLINDRICAL_SURFACE('',#4498,5.91675);
#3857=CYLINDRICAL_SURFACE('',#4500,5.91675);
#3858=CYLINDRICAL_SURFACE('',#4501,5.91675);
#3859=CYLINDRICAL_SURFACE('',#4502,5.91675);
#3860=CYLINDRICAL_SURFACE('',#4503,5.91675);
#3861=CYLINDRICAL_SURFACE('',#4504,5.91675);
#3862=CYLINDRICAL_SURFACE('',#4505,5.91675);
#3863=CYLINDRICAL_SURFACE('',#4506,5.91675);
#3864=CYLINDRICAL_SURFACE('',#4507,5.91675);
#3865=CYLINDRICAL_SURFACE('',#4508,5.91675);
#3866=CYLINDRICAL_SURFACE('',#4509,5.91675);
#3867=CYLINDRICAL_SURFACE('',#4510,5.91675);
#3868=CYLINDRICAL_SURFACE('',#4511,5.91675);
#3869=CYLINDRICAL_SURFACE('',#4512,5.91675);
#3870=CYLINDRICAL_SURFACE('',#4513,5.91675);
#3871=CYLINDRICAL_SURFACE('',#4514,5.91675);
#3872=CYLINDRICAL_SURFACE('',#4515,5.91675);
#3873=CYLINDRICAL_SURFACE('',#4516,5.91675);
#3874=CYLINDRICAL_SURFACE('',#4517,5.91675);
#3875=CYLINDRICAL_SURFACE('',#4518,5.91675);
#3876=CYLINDRICAL_SURFACE('',#4519,5.91675);
#3877=CYLINDRICAL_SURFACE('',#4520,5.91675);
#3878=CYLINDRICAL_SURFACE('',#4521,5.91675);
#3879=CYLINDRICAL_SURFACE('',#4522,5.91675);
#3880=CYLINDRICAL_SURFACE('',#4523,5.91675);
#3881=CYLINDRICAL_SURFACE('',#4524,5.91675);
#3882=CYLINDRICAL_SURFACE('',#4525,5.91675);
#3883=CYLINDRICAL_SURFACE('',#4526,5.91675);
#3884=CYLINDRICAL_SURFACE('',#4527,4.91825);
#3885=CYLINDRICAL_SURFACE('',#4529,4.91825);
#3886=CYLINDRICAL_SURFACE('',#4530,4.91825);
#3887=CYLINDRICAL_SURFACE('',#4531,4.91825);
#3888=CYLINDRICAL_SURFACE('',#4532,4.91825);
#3889=CYLINDRICAL_SURFACE('',#4533,4.91825);
#3890=CYLINDRICAL_SURFACE('',#4534,4.91825);
#3891=CYLINDRICAL_SURFACE('',#4535,4.91825);
#3892=CYLINDRICAL_SURFACE('',#4536,4.91825);
#3893=CYLINDRICAL_SURFACE('',#4537,4.91825);
#3894=CYLINDRICAL_SURFACE('',#4538,4.91825);
#3895=CYLINDRICAL_SURFACE('',#4539,4.91825);
#3896=CYLINDRICAL_SURFACE('',#4540,4.91825);
#3897=CYLINDRICAL_SURFACE('',#4541,4.91825);
#3898=CYLINDRICAL_SURFACE('',#4542,4.91825);
#3899=CYLINDRICAL_SURFACE('',#4543,4.91825);
#3900=CYLINDRICAL_SURFACE('',#4544,4.91825);
#3901=CYLINDRICAL_SURFACE('',#4545,4.91825);
#3902=CYLINDRICAL_SURFACE('',#4546,4.91825);
#3903=CYLINDRICAL_SURFACE('',#4547,4.91825);
#3904=CYLINDRICAL_SURFACE('',#4548,4.91825);
#3905=CYLINDRICAL_SURFACE('',#4549,4.91825);
#3906=CYLINDRICAL_SURFACE('',#4550,4.91825);
#3907=CYLINDRICAL_SURFACE('',#4551,4.91825);
#3908=CYLINDRICAL_SURFACE('',#4552,4.91825);
#3909=CYLINDRICAL_SURFACE('',#4553,4.91825);
#3910=CYLINDRICAL_SURFACE('',#4554,4.91825);
#3911=CYLINDRICAL_SURFACE('',#4555,4.91825);
#3912=CYLINDRICAL_SURFACE('',#4556,4.91825);
#3913=CYLINDRICAL_SURFACE('',#4558,5.91675);
#3914=CYLINDRICAL_SURFACE('',#4573,9.);
#4019=ADVANCED_FACE('',(#689),#3856,.T.);
#4020=ADVANCED_FACE('',(#690),#3857,.T.);
#4021=ADVANCED_FACE('',(#691),#3858,.T.);
#4022=ADVANCED_FACE('',(#692),#3859,.T.);
#4023=ADVANCED_FACE('',(#693),#3860,.T.);
#4024=ADVANCED_FACE('',(#694),#3861,.T.);
#4025=ADVANCED_FACE('',(#695),#3862,.T.);
#4026=ADVANCED_FACE('',(#696),#3863,.T.);
#4027=ADVANCED_FACE('',(#697),#3864,.T.);
#4028=ADVANCED_FACE('',(#698),#3865,.T.);
#4029=ADVANCED_FACE('',(#699),#3866,.T.);
#4030=ADVANCED_FACE('',(#700),#3867,.T.);
#4031=ADVANCED_FACE('',(#701),#3868,.T.);
#4032=ADVANCED_FACE('',(#702),#3869,.T.);
#4033=ADVANCED_FACE('',(#703),#3870,.T.);
#4034=ADVANCED_FACE('',(#704),#3871,.T.);
#4035=ADVANCED_FACE('',(#705),#3872,.T.);
#4036=ADVANCED_FACE('',(#706),#3873,.T.);
#4037=ADVANCED_FACE('',(#707),#3874,.T.);
#4038=ADVANCED_FACE('',(#708),#3875,.T.);
#4039=ADVANCED_FACE('',(#709),#3876,.T.);
#4040=ADVANCED_FACE('',(#710),#3877,.T.);
#4041=ADVANCED_FACE('',(#711),#3878,.T.);
#4042=ADVANCED_FACE('',(#712),#3879,.T.);
#4043=ADVANCED_FACE('',(#713),#3880,.T.);
#4044=ADVANCED_FACE('',(#714),#3881,.T.);
#4045=ADVANCED_FACE('',(#715),#3882,.T.);
#4046=ADVANCED_FACE('',(#716),#3883,.T.);
#4047=ADVANCED_FACE('',(#717),#3884,.T.);
#4048=ADVANCED_FACE('',(#718),#3885,.T.);
#4049=ADVANCED_FACE('',(#719),#3886,.T.);
#4050=ADVANCED_FACE('',(#720),#3887,.T.);
#4051=ADVANCED_FACE('',(#721),#3888,.T.);
#4052=ADVANCED_FACE('',(#722),#3889,.T.);
#4053=ADVANCED_FACE('',(#723),#3890,.T.);
#4054=ADVANCED_FACE('',(#724),#3891,.T.);
#4055=ADVANCED_FACE('',(#725),#3892,.T.);
#4056=ADVANCED_FACE('',(#726),#3893,.T.);
#4057=ADVANCED_FACE('',(#727),#3894,.T.);
#4058=ADVANCED_FACE('',(#728),#3895,.T.);
#4059=ADVANCED_FACE('',(#729),#3896,.T.);
#4060=ADVANCED_FACE('',(#730),#3897,.T.);
#4061=ADVANCED_FACE('',(#731),#3898,.T.);
#4062=ADVANCED_FACE('',(#732),#3899,.T.);
#4063=ADVANCED_FACE('',(#733),#3900,.T.);
#4064=ADVANCED_FACE('',(#734),#3901,.T.);
#4065=ADVANCED_FACE('',(#735),#3902,.T.);
#4066=ADVANCED_FACE('',(#736),#3903,.T.);
#4067=ADVANCED_FACE('',(#737),#3904,.T.);
#4068=ADVANCED_FACE('',(#738),#3905,.T.);
#4069=ADVANCED_FACE('',(#739),#3906,.T.);
#4070=ADVANCED_FACE('',(#740),#3907,.T.);
#4071=ADVANCED_FACE('',(#741),#3908,.T.);
#4072=ADVANCED_FACE('',(#742),#3909,.T.);
#4073=ADVANCED_FACE('',(#743),#3910,.T.);
#4074=ADVANCED_FACE('',(#744),#3911,.T.);
#4075=ADVANCED_FACE('',(#745),#3912,.T.);
#4076=ADVANCED_FACE('',(#746),#3913,.T.);
#4077=ADVANCED_FACE('',(#747),#147,.T.);
#4078=ADVANCED_FACE('',(#748),#150,.F.);
#4079=ADVANCED_FACE('',(#749),#151,.F.);
#4080=ADVANCED_FACE('',(#750),#556,.F.);
#4081=ADVANCED_FACE('',(#751),#557,.F.);
#4082=ADVANCED_FACE('',(#752),#558,.F.);
#4083=ADVANCED_FACE('',(#753),#559,.F.);
#4084=ADVANCED_FACE('',(#754),#560,.F.);
#4085=ADVANCED_FACE('',(#755),#561,.F.);
#4086=ADVANCED_FACE('',(#756),#562,.F.);
#4087=ADVANCED_FACE('',(#757,#504),#563,.T.);
#4088=ADVANCED_FACE('',(#758),#3914,.T.);
#4089=ADVANCED_FACE('',(#759,#505),#564,.F.);
#4090=ADVANCED_FACE('',(#760),#565,.T.);
#4152=CLOSED_SHELL('',(#4019,#4020,#4021,#4022,#4023,#4024,#4025,#4026,
#4027,#4028,#4029,#4030,#4031,#4032,#4033,#4034,#4035,#4036,#4037,#4038,
#4039,#4040,#4041,#4042,#4043,#4044,#4045,#4046,#4047,#4048,#4049,#4050,
#4051,#4052,#4053,#4054,#4055,#4056,#4057,#4058,#4059,#4060,#4061,#4062,
#4063,#4064,#4065,#4066,#4067,#4068,#4069,#4070,#4071,#4072,#4073,#4074,
#4075,#4076,#4077,#4078,#4079,#4080,#4081,#4082,#4083,#4084,#4085,#4086,
#4087,#4088,#4089,#4090));
#4497=AXIS2_PLACEMENT_3D('',#14166,#5094,#5095);
#4498=AXIS2_PLACEMENT_3D('',#14167,#5096,#5097);
#4499=AXIS2_PLACEMENT_3D('',#14249,#5099,#5100);
#4500=AXIS2_PLACEMENT_3D('',#14256,#5101,#5102);
#4501=AXIS2_PLACEMENT_3D('',#14505,#5104,#5105);
#4502=AXIS2_PLACEMENT_3D('',#14543,#5107,#5108);
#4503=AXIS2_PLACEMENT_3D('',#15008,#5110,#5111);
#4504=AXIS2_PLACEMENT_3D('',#15473,#5113,#5114);
#4505=AXIS2_PLACEMENT_3D('',#15723,#5116,#5117);
#4506=AXIS2_PLACEMENT_3D('',#15972,#5119,#5120);
#4507=AXIS2_PLACEMENT_3D('',#16222,#5122,#5123);
#4508=AXIS2_PLACEMENT_3D('',#16471,#5125,#5126);
#4509=AXIS2_PLACEMENT_3D('',#16721,#5128,#5129);
#4510=AXIS2_PLACEMENT_3D('',#17186,#5131,#5132);
#4511=AXIS2_PLACEMENT_3D('',#17648,#5134,#5135);
#4512=AXIS2_PLACEMENT_3D('',#17898,#5137,#5138);
#4513=AXIS2_PLACEMENT_3D('',#18147,#5140,#5141);
#4514=AXIS2_PLACEMENT_3D('',#18398,#5143,#5144);
#4515=AXIS2_PLACEMENT_3D('',#18437,#5146,#5147);
#4516=AXIS2_PLACEMENT_3D('',#18686,#5149,#5150);
#4517=AXIS2_PLACEMENT_3D('',#18936,#5152,#5153);
#4518=AXIS2_PLACEMENT_3D('',#19185,#5155,#5156);
#4519=AXIS2_PLACEMENT_3D('',#19223,#5158,#5159);
#4520=AXIS2_PLACEMENT_3D('',#19685,#5161,#5162);
#4521=AXIS2_PLACEMENT_3D('',#19937,#5164,#5165);
#4522=AXIS2_PLACEMENT_3D('',#20399,#5167,#5168);
#4523=AXIS2_PLACEMENT_3D('',#20864,#5170,#5171);
#4524=AXIS2_PLACEMENT_3D('',#21114,#5173,#5174);
#4525=AXIS2_PLACEMENT_3D('',#21151,#5176,#5177);
#4526=AXIS2_PLACEMENT_3D('',#21404,#5179,#5180);
#4527=AXIS2_PLACEMENT_3D('',#21866,#5182,#5183);
#4528=AXIS2_PLACEMENT_3D('',#22088,#5185,#5186);
#4529=AXIS2_PLACEMENT_3D('',#22228,#5187,#5188);
#4530=AXIS2_PLACEMENT_3D('',#22496,#5190,#5191);
#4531=AXIS2_PLACEMENT_3D('',#23020,#5193,#5194);
#4532=AXIS2_PLACEMENT_3D('',#23621,#5196,#5197);
#4533=AXIS2_PLACEMENT_3D('',#24103,#5199,#5200);
#4534=AXIS2_PLACEMENT_3D('',#24392,#5202,#5203);
#4535=AXIS2_PLACEMENT_3D('',#24870,#5205,#5206);
#4536=AXIS2_PLACEMENT_3D('',#25409,#5208,#5209);
#4537=AXIS2_PLACEMENT_3D('',#25928,#5211,#5212);
#4538=AXIS2_PLACEMENT_3D('',#26403,#5214,#5215);
#4539=AXIS2_PLACEMENT_3D('',#26902,#5217,#5218);
#4540=AXIS2_PLACEMENT_3D('',#27401,#5220,#5221);
#4541=AXIS2_PLACEMENT_3D('',#27461,#5223,#5224);
#4542=AXIS2_PLACEMENT_3D('',#27934,#5226,#5227);
#4543=AXIS2_PLACEMENT_3D('',#28211,#5229,#5230);
#4544=AXIS2_PLACEMENT_3D('',#28718,#5232,#5233);
#4545=AXIS2_PLACEMENT_3D('',#29224,#5235,#5236);
#4546=AXIS2_PLACEMENT_3D('',#29726,#5238,#5239);
#4547=AXIS2_PLACEMENT_3D('',#30014,#5241,#5242);
#4548=AXIS2_PLACEMENT_3D('',#30272,#5244,#5245);
#4549=AXIS2_PLACEMENT_3D('',#30759,#5247,#5248);
#4550=AXIS2_PLACEMENT_3D('',#31038,#5250,#5251);
#4551=AXIS2_PLACEMENT_3D('',#31333,#5253,#5254);
#4552=AXIS2_PLACEMENT_3D('',#31813,#5256,#5257);
#4553=AXIS2_PLACEMENT_3D('',#32292,#5259,#5260);
#4554=AXIS2_PLACEMENT_3D('',#32599,#5262,#5263);
#4555=AXIS2_PLACEMENT_3D('',#33066,#5265,#5266);
#4556=AXIS2_PLACEMENT_3D('',#33345,#5268,#5269);
#4557=AXIS2_PLACEMENT_3D('',#33565,#5270,#5271);
#4558=AXIS2_PLACEMENT_3D('',#33743,#5272,#5273);
#4559=AXIS2_PLACEMENT_3D('',#33761,#5274,#5275);
#4560=AXIS2_PLACEMENT_3D('',#33931,#5276,#5277);
#4561=AXIS2_PLACEMENT_3D('',#34205,#5278,#5279);
#4562=AXIS2_PLACEMENT_3D('',#35672,#5280,#5281);
#4563=AXIS2_PLACEMENT_3D('',#37364,#5282,#5283);
#4564=AXIS2_PLACEMENT_3D('',#37365,#5284,#5285);
#4565=AXIS2_PLACEMENT_3D('',#37374,#5290,#5291);
#4566=AXIS2_PLACEMENT_3D('',#37380,#5295,#5296);
#4567=AXIS2_PLACEMENT_3D('',#37386,#5300,#5301);
#4568=AXIS2_PLACEMENT_3D('',#37392,#5305,#5306);
#4569=AXIS2_PLACEMENT_3D('',#37398,#5310,#5311);
#4570=AXIS2_PLACEMENT_3D('',#37401,#5314,#5315);
#4571=AXIS2_PLACEMENT_3D('',#37402,#5316,#5317);
#4572=AXIS2_PLACEMENT_3D('',#37404,#5318,#5319);
#4573=AXIS2_PLACEMENT_3D('',#37405,#5320,#5321);
#4574=AXIS2_PLACEMENT_3D('',#37408,#5323,#5324);
#4575=AXIS2_PLACEMENT_3D('',#37409,#5325,#5326);
#4576=AXIS2_PLACEMENT_3D('',#37410,#5327,#5328);
#5094=DIRECTION('axis',(0.,0.,1.));
#5095=DIRECTION('refdir',(1.,0.,0.));
#5096=DIRECTION('center_axis',(0.,0.,1.));
#5097=DIRECTION('ref_axis',(1.,0.,0.));
#5098=DIRECTION('',(0.,0.,-1.));
#5099=DIRECTION('center_axis',(0.,0.,-1.));
#5100=DIRECTION('ref_axis',(1.,0.,0.));
#5101=DIRECTION('center_axis',(0.,0.,1.));
#5102=DIRECTION('ref_axis',(1.,0.,0.));
#5103=DIRECTION('',(0.,0.,-1.));
#5104=DIRECTION('center_axis',(0.,0.,1.));
#5105=DIRECTION('ref_axis',(1.,0.,0.));
#5106=DIRECTION('',(0.,0.,-1.));
#5107=DIRECTION('center_axis',(0.,0.,1.));
#5108=DIRECTION('ref_axis',(1.,0.,0.));
#5109=DIRECTION('',(0.,0.,-1.));
#5110=DIRECTION('center_axis',(0.,0.,1.));
#5111=DIRECTION('ref_axis',(1.,0.,0.));
#5112=DIRECTION('',(0.,0.,-1.));
#5113=DIRECTION('center_axis',(0.,0.,1.));
#5114=DIRECTION('ref_axis',(1.,0.,0.));
#5115=DIRECTION('',(0.,0.,-1.));
#5116=DIRECTION('center_axis',(0.,0.,1.));
#5117=DIRECTION('ref_axis',(1.,0.,0.));
#5118=DIRECTION('',(0.,0.,-1.));
#5119=DIRECTION('center_axis',(0.,0.,1.));
#5120=DIRECTION('ref_axis',(1.,0.,0.));
#5121=DIRECTION('',(0.,0.,-1.));
#5122=DIRECTION('center_axis',(0.,0.,1.));
#5123=DIRECTION('ref_axis',(1.,0.,0.));
#5124=DIRECTION('',(0.,0.,-1.));
#5125=DIRECTION('center_axis',(0.,0.,1.));
#5126=DIRECTION('ref_axis',(1.,0.,0.));
#5127=DIRECTION('',(0.,0.,-1.));
#5128=DIRECTION('center_axis',(0.,0.,1.));
#5129=DIRECTION('ref_axis',(1.,0.,0.));
#5130=DIRECTION('',(0.,0.,-1.));
#5131=DIRECTION('center_axis',(0.,0.,1.));
#5132=DIRECTION('ref_axis',(1.,0.,0.));
#5133=DIRECTION('',(0.,0.,-1.));
#5134=DIRECTION('center_axis',(0.,0.,1.));
#5135=DIRECTION('ref_axis',(1.,0.,0.));
#5136=DIRECTION('',(0.,0.,-1.));
#5137=DIRECTION('center_axis',(0.,0.,1.));
#5138=DIRECTION('ref_axis',(1.,0.,0.));
#5139=DIRECTION('',(0.,0.,-1.));
#5140=DIRECTION('center_axis',(0.,0.,1.));
#5141=DIRECTION('ref_axis',(1.,0.,0.));
#5142=DIRECTION('',(0.,0.,-1.));
#5143=DIRECTION('center_axis',(0.,0.,1.));
#5144=DIRECTION('ref_axis',(1.,0.,0.));
#5145=DIRECTION('',(0.,0.,-1.));
#5146=DIRECTION('center_axis',(0.,0.,1.));
#5147=DIRECTION('ref_axis',(1.,0.,0.));
#5148=DIRECTION('',(0.,0.,-1.));
#5149=DIRECTION('center_axis',(0.,0.,1.));
#5150=DIRECTION('ref_axis',(1.,0.,0.));
#5151=DIRECTION('',(0.,0.,-1.));
#5152=DIRECTION('center_axis',(0.,0.,1.));
#5153=DIRECTION('ref_axis',(1.,0.,0.));
#5154=DIRECTION('',(0.,0.,-1.));
#5155=DIRECTION('center_axis',(0.,0.,1.));
#5156=DIRECTION('ref_axis',(1.,0.,0.));
#5157=DIRECTION('',(0.,0.,-1.));
#5158=DIRECTION('center_axis',(0.,0.,1.));
#5159=DIRECTION('ref_axis',(1.,0.,0.));
#5160=DIRECTION('',(0.,0.,-1.));
#5161=DIRECTION('center_axis',(0.,0.,1.));
#5162=DIRECTION('ref_axis',(1.,0.,0.));
#5163=DIRECTION('',(0.,0.,-1.));
#5164=DIRECTION('center_axis',(0.,0.,1.));
#5165=DIRECTION('ref_axis',(1.,0.,0.));
#5166=DIRECTION('',(0.,0.,-1.));
#5167=DIRECTION('center_axis',(0.,0.,1.));
#5168=DIRECTION('ref_axis',(1.,0.,0.));
#5169=DIRECTION('',(0.,0.,-1.));
#5170=DIRECTION('center_axis',(0.,0.,1.));
#5171=DIRECTION('ref_axis',(1.,0.,0.));
#5172=DIRECTION('',(0.,0.,-1.));
#5173=DIRECTION('center_axis',(0.,0.,1.));
#5174=DIRECTION('ref_axis',(1.,0.,0.));
#5175=DIRECTION('',(0.,0.,-1.));
#5176=DIRECTION('center_axis',(0.,0.,1.));
#5177=DIRECTION('ref_axis',(1.,0.,0.));
#5178=DIRECTION('',(0.,0.,-1.));
#5179=DIRECTION('center_axis',(0.,0.,1.));
#5180=DIRECTION('ref_axis',(1.,0.,0.));
#5181=DIRECTION('',(0.,0.,-1.));
#5182=DIRECTION('center_axis',(0.,0.,1.));
#5183=DIRECTION('ref_axis',(0.968644250912352,-0.248451836729877,0.));
#5184=DIRECTION('',(0.,0.,-1.));
#5185=DIRECTION('center_axis',(0.,0.,-1.));
#5186=DIRECTION('ref_axis',(1.,-9.58699708308227E-14,0.));
#5187=DIRECTION('center_axis',(0.,0.,1.));
#5188=DIRECTION('ref_axis',(0.968644250912352,-0.248451836729877,0.));
#5189=DIRECTION('',(0.,0.,-1.));
#5190=DIRECTION('center_axis',(0.,0.,1.));
#5191=DIRECTION('ref_axis',(0.968644250912352,-0.248451836729877,0.));
#5192=DIRECTION('',(0.,0.,-1.));
#5193=DIRECTION('center_axis',(0.,0.,1.));
#5194=DIRECTION('ref_axis',(0.968644250912352,-0.248451836729877,0.));
#5195=DIRECTION('',(0.,0.,-1.));
#5196=DIRECTION('center_axis',(0.,0.,1.));
#5197=DIRECTION('ref_axis',(0.968644250912352,-0.248451836729877,0.));
#5198=DIRECTION('',(0.,0.,-1.));
#5199=DIRECTION('center_axis',(0.,0.,1.));
#5200=DIRECTION('ref_axis',(0.968644250912352,-0.248451836729877,0.));
#5201=DIRECTION('',(0.,0.,-1.));
#5202=DIRECTION('center_axis',(0.,0.,1.));
#5203=DIRECTION('ref_axis',(0.968644250912352,-0.248451836729877,0.));
#5204=DIRECTION('',(0.,0.,-1.));
#5205=DIRECTION('center_axis',(0.,0.,1.));
#5206=DIRECTION('ref_axis',(0.968644250912352,-0.248451836729877,0.));
#5207=DIRECTION('',(0.,0.,-1.));
#5208=DIRECTION('center_axis',(0.,0.,1.));
#5209=DIRECTION('ref_axis',(0.968644250912352,-0.248451836729877,0.));
#5210=DIRECTION('',(0.,0.,-1.));
#5211=DIRECTION('center_axis',(0.,0.,1.));
#5212=DIRECTION('ref_axis',(0.968644250912352,-0.248451836729877,0.));
#5213=DIRECTION('',(0.,0.,-1.));
#5214=DIRECTION('center_axis',(0.,0.,1.));
#5215=DIRECTION('ref_axis',(0.968644250912352,-0.248451836729877,0.));
#5216=DIRECTION('',(0.,0.,-1.));
#5217=DIRECTION('center_axis',(0.,0.,1.));
#5218=DIRECTION('ref_axis',(0.968644250912352,-0.248451836729877,0.));
#5219=DIRECTION('',(0.,0.,-1.));
#5220=DIRECTION('center_axis',(0.,0.,1.));
#5221=DIRECTION('ref_axis',(0.968644250912352,-0.248451836729877,0.));
#5222=DIRECTION('',(0.,0.,-1.));
#5223=DIRECTION('center_axis',(0.,0.,1.));
#5224=DIRECTION('ref_axis',(0.968644250912352,-0.248451836729877,0.));
#5225=DIRECTION('',(0.,0.,-1.));
#5226=DIRECTION('center_axis',(0.,0.,1.));
#5227=DIRECTION('ref_axis',(0.968644250912352,-0.248451836729877,0.));
#5228=DIRECTION('',(0.,0.,-1.));
#5229=DIRECTION('center_axis',(0.,0.,1.));
#5230=DIRECTION('ref_axis',(0.968644250912352,-0.248451836729877,0.));
#5231=DIRECTION('',(0.,0.,-1.));
#5232=DIRECTION('center_axis',(0.,0.,1.));
#5233=DIRECTION('ref_axis',(0.968644250912352,-0.248451836729877,0.));
#5234=DIRECTION('',(0.,0.,-1.));
#5235=DIRECTION('center_axis',(0.,0.,1.));
#5236=DIRECTION('ref_axis',(0.968644250912352,-0.248451836729877,0.));
#5237=DIRECTION('',(0.,0.,-1.));
#5238=DIRECTION('center_axis',(0.,0.,1.));
#5239=DIRECTION('ref_axis',(0.968644250912352,-0.248451836729877,0.));
#5240=DIRECTION('',(0.,0.,-1.));
#5241=DIRECTION('center_axis',(0.,0.,1.));
#5242=DIRECTION('ref_axis',(0.968644250912352,-0.248451836729877,0.));
#5243=DIRECTION('',(0.,0.,-1.));
#5244=DIRECTION('center_axis',(0.,0.,1.));
#5245=DIRECTION('ref_axis',(0.968644250912352,-0.248451836729877,0.));
#5246=DIRECTION('',(0.,0.,-1.));
#5247=DIRECTION('center_axis',(0.,0.,1.));
#5248=DIRECTION('ref_axis',(0.968644250912352,-0.248451836729877,0.));
#5249=DIRECTION('',(0.,0.,-1.));
#5250=DIRECTION('center_axis',(0.,0.,1.));
#5251=DIRECTION('ref_axis',(0.968644250912352,-0.248451836729877,0.));
#5252=DIRECTION('',(0.,0.,-1.));
#5253=DIRECTION('center_axis',(0.,0.,1.));
#5254=DIRECTION('ref_axis',(0.968644250912352,-0.248451836729877,0.));
#5255=DIRECTION('',(0.,0.,-1.));
#5256=DIRECTION('center_axis',(0.,0.,1.));
#5257=DIRECTION('ref_axis',(0.968644250912352,-0.248451836729877,0.));
#5258=DIRECTION('',(0.,0.,-1.));
#5259=DIRECTION('center_axis',(0.,0.,1.));
#5260=DIRECTION('ref_axis',(0.968644250912352,-0.248451836729877,0.));
#5261=DIRECTION('',(0.,0.,-1.));
#5262=DIRECTION('center_axis',(0.,0.,1.));
#5263=DIRECTION('ref_axis',(0.968644250912352,-0.248451836729877,0.));
#5264=DIRECTION('',(0.,0.,-1.));
#5265=DIRECTION('center_axis',(0.,0.,1.));
#5266=DIRECTION('ref_axis',(0.968644250912352,-0.248451836729877,0.));
#5267=DIRECTION('',(0.,0.,-1.));
#5268=DIRECTION('center_axis',(0.,0.,1.));
#5269=DIRECTION('ref_axis',(0.929914003289978,-0.367777033656544,0.));
#5270=DIRECTION('center_axis',(0.,0.,1.));
#5271=DIRECTION('ref_axis',(1.,-9.58699708308227E-14,0.));
#5272=DIRECTION('center_axis',(0.,0.,1.));
#5273=DIRECTION('ref_axis',(1.,0.,0.));
#5274=DIRECTION('center_axis',(0.,0.,-1.));
#5275=DIRECTION('ref_axis',(1.,0.,0.));
#5276=DIRECTION('center_axis',(0.,0.,-1.));
#5277=DIRECTION('ref_axis',(-0.244277982423325,-0.969705247641359,0.));
#5278=DIRECTION('center_axis',(0.,0.,1.));
#5279=DIRECTION('ref_axis',(1.,0.,0.));
#5280=DIRECTION('center_axis',(-2.18604941971849E-13,1.11567293784461E-13,
1.));
#5281=DIRECTION('ref_axis',(-0.547317217186752,-0.836925243836598,-2.62727639485539E-14));
#5282=DIRECTION('center_axis',(-1.76900854822811E-13,-9.65744760848165E-13,
1.));
#5283=DIRECTION('ref_axis',(0.90668614223658,-0.421805926317007,-2.46963309817708E-13));
#5284=DIRECTION('center_axis',(-1.92296268638356E-16,-1.,0.));
#5285=DIRECTION('ref_axis',(1.,-1.92296268638356E-16,0.));
#5286=DIRECTION('',(1.,-1.92296268638356E-16,0.));
#5287=DIRECTION('',(0.,0.,1.));
#5288=DIRECTION('',(1.,-1.92296268638356E-16,0.));
#5289=DIRECTION('',(0.,0.,1.));
#5290=DIRECTION('center_axis',(-0.866025403784439,-0.5,0.));
#5291=DIRECTION('ref_axis',(0.5,-0.866025403784439,0.));
#5292=DIRECTION('',(0.5,-0.866025403784439,0.));
#5293=DIRECTION('',(0.,0.,1.));
#5294=DIRECTION('',(0.5,-0.866025403784439,0.));
#5295=DIRECTION('center_axis',(-0.866025403784439,0.5,0.));
#5296=DIRECTION('ref_axis',(-0.5,-0.866025403784439,0.));
#5297=DIRECTION('',(-0.5,-0.866025403784439,0.));
#5298=DIRECTION('',(0.,0.,1.));
#5299=DIRECTION('',(-0.5,-0.866025403784439,0.));
#5300=DIRECTION('center_axis',(1.92296268638356E-16,1.,0.));
#5301=DIRECTION('ref_axis',(-1.,1.92296268638356E-16,0.));
#5302=DIRECTION('',(-1.,1.92296268638356E-16,0.));
#5303=DIRECTION('',(0.,0.,1.));
#5304=DIRECTION('',(-1.,1.92296268638356E-16,0.));
#5305=DIRECTION('center_axis',(0.866025403784439,0.5,0.));
#5306=DIRECTION('ref_axis',(-0.5,0.866025403784439,0.));
#5307=DIRECTION('',(-0.5,0.866025403784439,0.));
#5308=DIRECTION('',(0.,0.,1.));
#5309=DIRECTION('',(-0.5,0.866025403784439,0.));
#5310=DIRECTION('center_axis',(0.866025403784439,-0.5,0.));
#5311=DIRECTION('ref_axis',(0.5,0.866025403784439,0.));
#5312=DIRECTION('',(0.5,0.866025403784439,0.));
#5313=DIRECTION('',(0.5,0.866025403784439,0.));
#5314=DIRECTION('center_axis',(0.,0.,1.));
#5315=DIRECTION('ref_axis',(1.,0.,0.));
#5316=DIRECTION('center_axis',(0.,0.,1.));
#5317=DIRECTION('ref_axis',(1.,0.,0.));
#5318=DIRECTION('center_axis',(0.,0.,1.));
#5319=DIRECTION('ref_axis',(1.,0.,0.));
#5320=DIRECTION('center_axis',(0.,0.,1.));
#5321=DIRECTION('ref_axis',(1.,0.,0.));
#5322=DIRECTION('',(0.,0.,-1.));
#5323=DIRECTION('center_axis',(0.,0.,1.));
#5324=DIRECTION('ref_axis',(1.,0.,0.));
#5325=DIRECTION('center_axis',(0.,0.,1.));
#5326=DIRECTION('ref_axis',(1.,0.,0.));
#5327=DIRECTION('center_axis',(0.,0.,1.));
#5328=DIRECTION('ref_axis',(1.,0.,0.));
#14166=CARTESIAN_POINT('',(0.,0.,0.));
#14167=CARTESIAN_POINT('Origin',(0.,0.,0.));
#14168=CARTESIAN_POINT('',(-5.91674999809507,0.000150139963024017,0.56337519223592));
#14169=CARTESIAN_POINT('',(-5.91671935081961,9.79311290895061E-5,0.311624807795122));
#14170=CARTESIAN_POINT('',(-5.91675,-7.2459289488551E-16,0.));
#14171=CARTESIAN_POINT('',(2.58392005625187,5.32271431746993,5.66418127782893E-6));
#14172=CARTESIAN_POINT('Ctrl Pts',(-5.91674999809505,0.000150140621988509,
0.563375192204898));
#14173=CARTESIAN_POINT('Ctrl Pts',(-5.91674553653358,0.175971603634398,
0.555097989792623));
#14174=CARTESIAN_POINT('Ctrl Pts',(-5.90889970267472,0.35175539283155,0.546820787380347));
#14175=CARTESIAN_POINT('Ctrl Pts',(-5.8932485072967,0.526832605051395,0.538543584968072));
#14176=CARTESIAN_POINT('Ctrl Pts',(-5.89144091145379,0.547052711781432,
0.53758763008348));
#14177=CARTESIAN_POINT('Ctrl Pts',(-5.8895292606626,0.567263397909551,0.536631675198887));
#14178=CARTESIAN_POINT('Ctrl Pts',(-5.88751365503158,0.587463636590923,
0.535675720314295));
#14179=CARTESIAN_POINT('Ctrl Pts',(-5.87109213436944,0.752038805355124,
0.527887374892031));
#14180=CARTESIAN_POINT('Ctrl Pts',(-5.84776274299796,0.915954366421261,
0.520099029469766));
#14181=CARTESIAN_POINT('Ctrl Pts',(-5.81760272669442,1.07862369566856,0.512310684047502));
#14182=CARTESIAN_POINT('Ctrl Pts',(-5.78744863648316,1.24126106228533,0.504523868944495));
#14183=CARTESIAN_POINT('Ctrl Pts',(-5.75046665751305,1.4026523717289,0.496737053841489));
#14184=CARTESIAN_POINT('Ctrl Pts',(-5.70678536019788,1.56222002775893,0.488950238738483));
#14185=CARTESIAN_POINT('Ctrl Pts',(-5.66310240888906,1.72179372582311,0.481163128787486));
#14186=CARTESIAN_POINT('Ctrl Pts',(-5.61271971217538,1.87954332311285,0.473376018836489));
#14187=CARTESIAN_POINT('Ctrl Pts',(-5.55581624327961,2.03490452685388,0.465588908885492));
#14188=CARTESIAN_POINT('Ctrl Pts',(-5.49891655207064,2.1902554165318,0.457802315902319));
#14189=CARTESIAN_POINT('Ctrl Pts',(-5.43549706495836,2.34321792997301,0.450015722919146));
#14190=CARTESIAN_POINT('Ctrl Pts',(-5.36578566692213,2.49324582405207,0.442229129935973));
#14191=CARTESIAN_POINT('Ctrl Pts',(-5.29605597837102,2.64331308167145,0.43444049394694));
#14192=CARTESIAN_POINT('Ctrl Pts',(-5.22003121311526,2.79044389061004,0.426651857957906));
#14193=CARTESIAN_POINT('Ctrl Pts',(-5.13798656155565,2.93411394730564,0.418863221968873));
#14194=CARTESIAN_POINT('Ctrl Pts',(-5.06000943480969,3.07066127863795,0.411460722913175));
#14195=CARTESIAN_POINT('Ctrl Pts',(-4.97659498598521,3.20408246256618,0.404058223857477));
#14196=CARTESIAN_POINT('Ctrl Pts',(-4.88801705550324,3.33394958384338,0.396655724801779));
#14197=CARTESIAN_POINT('Ctrl Pts',(-4.79483107421496,3.47057272538046,0.388868128786187));
#14198=CARTESIAN_POINT('Ctrl Pts',(-4.69589676366777,3.60331097514271,0.381080532770595));
#14199=CARTESIAN_POINT('Ctrl Pts',(-4.59156266393042,3.73168633002564,0.373292936755003));
#14200=CARTESIAN_POINT('Ctrl Pts',(-4.48724907892953,3.86003644305015,0.365506871978769));
#14201=CARTESIAN_POINT('Ctrl Pts',(-4.37753802466603,3.98402512499211,0.357720807202535));
#14202=CARTESIAN_POINT('Ctrl Pts',(-4.26281878373472,4.10320686531138,0.349934742426301));
#14203=CARTESIAN_POINT('Ctrl Pts',(-4.14809511398164,4.22239320673053,0.342148377063235));
#14204=CARTESIAN_POINT('Ctrl Pts',(-4.02836308946995,4.33677200218623,0.33436201170017));
#14205=CARTESIAN_POINT('Ctrl Pts',(-3.90404987928167,4.44593354680216,0.326575646337105));
#14206=CARTESIAN_POINT('Ctrl Pts',(-3.77974484877771,4.55508790869813,0.318789793309057));
#14207=CARTESIAN_POINT('Ctrl Pts',(-3.65085947608667,4.65902549591907,0.311003940281009));
#14208=CARTESIAN_POINT('Ctrl Pts',(-3.51785523433146,4.75737586414892,0.303218087252961));
#14209=CARTESIAN_POINT('Ctrl Pts',(-3.38481584030573,4.85575222582609,0.295430176467895));
#14210=CARTESIAN_POINT('Ctrl Pts',(-3.24765565797162,4.94853822608719,0.287642265682829));
#14211=CARTESIAN_POINT('Ctrl Pts',(-3.1068671924737,5.03540532736249,0.279854354897763));
#14212=CARTESIAN_POINT('Ctrl Pts',(-2.9729790723165,5.11801488526997,0.272448146361596));
#14213=CARTESIAN_POINT('Ctrl Pts',(-2.8358100372979,5.19527170903417,0.265041937825429));
#14214=CARTESIAN_POINT('Ctrl Pts',(-2.69580607650546,5.26693081028945,0.257635729289262));
#14215=CARTESIAN_POINT('Ctrl Pts',(-2.54858704760487,5.34228284489603,0.24984784370118));
#14216=CARTESIAN_POINT('Ctrl Pts',(-2.39818035191975,5.41147200648169,0.242059958113099));
#14217=CARTESIAN_POINT('Ctrl Pts',(-2.24512084427557,5.4742454235355,0.234272072525018));
#14218=CARTESIAN_POINT('Ctrl Pts',(-2.09209149064525,5.53700647369674,0.226485721216078));
#14219=CARTESIAN_POINT('Ctrl Pts',(-1.93641066333322,5.59335418010095,0.218699369907139));
#14220=CARTESIAN_POINT('Ctrl Pts',(-1.77863343642197,5.64308370142972,0.210913018598199));
#14221=CARTESIAN_POINT('Ctrl Pts',(-1.62085026853532,5.69281509528388,0.203126374100423));
#14222=CARTESIAN_POINT('Ctrl Pts',(-1.46097084667463,5.73592770555686,0.195339729602648));
#14223=CARTESIAN_POINT('Ctrl Pts',(-1.29956637043957,5.77226626303071,0.187553085104872));
#14224=CARTESIAN_POINT('Ctrl Pts',(-1.1381726094073,5.80860240808688,0.179766957541179));
#14225=CARTESIAN_POINT('Ctrl Pts',(-0.975254308416725,5.83816533018435,
0.171980829977485));
#14226=CARTESIAN_POINT('Ctrl Pts',(-0.811393994756377,5.86085065052619,
0.164194702413792));
#14227=CARTESIAN_POINT('Ctrl Pts',(-0.647490590330721,5.88354193648468,
0.156406527312241));
#14228=CARTESIAN_POINT('Ctrl Pts',(-0.482644994721619,5.89935196088901,
0.148618352210691));
#14229=CARTESIAN_POINT('Ctrl Pts',(-0.317446922897937,5.90822799269313,
0.14083017710914));
#14230=CARTESIAN_POINT('Ctrl Pts',(-0.160380466066584,5.91666711580639,
0.133425362665008));
#14231=CARTESIAN_POINT('Ctrl Pts',(-0.00299566183749642,5.91883844420629,
0.126020548220876));
#14232=CARTESIAN_POINT('Ctrl Pts',(0.154198948809147,5.91474033637033,0.118615733776744));
#14233=CARTESIAN_POINT('Ctrl Pts',(0.318899201834896,5.91044655432059,0.110857358298474));
#14234=CARTESIAN_POINT('Ctrl Pts',(0.483453641539656,5.89926825531666,0.103098982820203));
#14235=CARTESIAN_POINT('Ctrl Pts',(0.647275897512335,5.88123834536568,0.0953406073419322));
#14236=CARTESIAN_POINT('Ctrl Pts',(0.815029932118198,5.86277571267942,0.087396028745211));
#14237=CARTESIAN_POINT('Ctrl Pts',(0.982015844042426,5.83712845066767,0.0794514501484898));
#14238=CARTESIAN_POINT('Ctrl Pts',(1.14760928393256,5.80438829627479,0.0715068715517686));
#14239=CARTESIAN_POINT('Ctrl Pts',(1.30928459978979,5.77242281016499,0.0637502704760876));
#14240=CARTESIAN_POINT('Ctrl Pts',(1.46963226790649,5.73369638273858,0.0559936694004065));
#14241=CARTESIAN_POINT('Ctrl Pts',(1.62808103688705,5.68834621835106,0.0482370683247255));
#14242=CARTESIAN_POINT('Ctrl Pts',(1.79228970118404,5.64134749461445,0.0401985009674842));
#14243=CARTESIAN_POINT('Ctrl Pts',(1.95445845105966,5.58723448296605,0.0321599336102429));
#14244=CARTESIAN_POINT('Ctrl Pts',(2.11396789947378,5.52621663369202,0.0241213662530017));
#14245=CARTESIAN_POINT('Ctrl Pts',(2.2734773478879,5.465198784418,0.0160827988957604));
#14246=CARTESIAN_POINT('Ctrl Pts',(2.43032713552487,5.39727624296388,0.00804423153851909));
#14247=CARTESIAN_POINT('Ctrl Pts',(2.58392005625187,5.32271431746993,5.66418127782893E-6));
#14248=CARTESIAN_POINT('',(-2.58391981634392,5.32271443393361,2.77555756156289E-16));
#14249=CARTESIAN_POINT('Origin',(0.,0.,0.));
#14250=CARTESIAN_POINT('Ctrl Pts',(-2.58391981634392,5.32271443393361,-4.44089209850063E-15));
#14251=CARTESIAN_POINT('Ctrl Pts',(-3.46903743297636,4.89303274091792,0.0463154617617043));
#14252=CARTESIAN_POINT('Ctrl Pts',(-5.01988689220886,3.58402595494104,0.138946385285122));
#14253=CARTESIAN_POINT('Ctrl Pts',(-5.84431863508223,1.46158823788899,0.24282132121683));
#14254=CARTESIAN_POINT('Ctrl Pts',(-5.91696259478107,0.238957375009801,
0.300380795386831));
#14255=CARTESIAN_POINT('Ctrl Pts',(-5.91671935081961,9.79311290895061E-5,
0.311624807795122));
#14256=CARTESIAN_POINT('Origin',(0.,0.,0.));
#14257=CARTESIAN_POINT('',(-5.91674999805022,-0.000151897061178456,2.3133751922049));
#14258=CARTESIAN_POINT('',(-5.91696061209103,-0.000135486519901937,2.06162480779511));
#14259=CARTESIAN_POINT('',(-5.91675,-7.2459289488551E-16,0.));
#14260=CARTESIAN_POINT('Ctrl Pts',(-5.91674999805022,-0.000151897061178456,
2.3133751922049));
#14261=CARTESIAN_POINT('Ctrl Pts',(-5.91675422850432,0.164634301711275,
2.30561771325954));
#14262=CARTESIAN_POINT('Ctrl Pts',(-5.90986997597158,0.329443911336745,
2.29786023431418));
#14263=CARTESIAN_POINT('Ctrl Pts',(-5.8961174422526,0.493689851692964,2.29010275536882));
#14264=CARTESIAN_POINT('Ctrl Pts',(-5.88236474983525,0.657937687377254,
2.28234518690546));
#14265=CARTESIAN_POINT('Ctrl Pts',(-5.86174364025453,0.821621517221492,
2.2745876184421));
#14266=CARTESIAN_POINT('Ctrl Pts',(-5.83432629786468,0.984158123750763,
2.26683004997874));
#14267=CARTESIAN_POINT('Ctrl Pts',(-5.80691054692563,1.14668529577654,2.2590729318066));
#14268=CARTESIAN_POINT('Ctrl Pts',(-5.77269940695638,1.30806505797604,2.25131581363446));
#14269=CARTESIAN_POINT('Ctrl Pts',(-5.7318164437995,1.46772300421083,2.24355869546232));
#14270=CARTESIAN_POINT('Ctrl Pts',(-5.69092326768429,1.62742083453978,2.23579963948728));
#14271=CARTESIAN_POINT('Ctrl Pts',(-5.64335501802441,1.78539567494315,2.22804058351223));
#14272=CARTESIAN_POINT('Ctrl Pts',(-5.58928574077949,1.94108615739205,2.22028152753719));
#14273=CARTESIAN_POINT('Ctrl Pts',(-5.55127036526057,2.05055002405717,2.21482624051296));
#14274=CARTESIAN_POINT('Ctrl Pts',(-5.5100423893398,2.15888493851147,2.20937095348874));
#14275=CARTESIAN_POINT('Ctrl Pts',(-5.46567681880059,2.2659010293757,2.20391566646451));
#14276=CARTESIAN_POINT('Ctrl Pts',(-5.40234044819479,2.41867739874011,2.19612768861303));
#14277=CARTESIAN_POINT('Ctrl Pts',(-5.332583141542,2.5688238602527,2.18833971076156));
#14278=CARTESIAN_POINT('Ctrl Pts',(-5.25664854959036,2.71580127928932,2.18055173291008));
#14279=CARTESIAN_POINT('Ctrl Pts',(-5.18072888702907,2.86274980130808,2.17276528624167));
#14280=CARTESIAN_POINT('Ctrl Pts',(-5.09863450905242,3.00653024031549,2.16497883957326));
#14281=CARTESIAN_POINT('Ctrl Pts',(-5.01065558369874,3.14662695342944,2.15719239290485));
#14282=CARTESIAN_POINT('Ctrl Pts',(-4.92267330215496,3.28672901090513,2.14940564920172));
#14283=CARTESIAN_POINT('Ctrl Pts',(-4.82880619062974,3.42314678858581,2.14161890549859));
#14284=CARTESIAN_POINT('Ctrl Pts',(-4.72938881488245,3.5553919615374,2.13383216179546));
#14285=CARTESIAN_POINT('Ctrl Pts',(-4.62997801485764,3.68762838745105,2.12604593312772));
#14286=CARTESIAN_POINT('Ctrl Pts',(-4.52501787737567,3.81569250555002,2.11825970445997));
#14287=CARTESIAN_POINT('Ctrl Pts',(-4.4148845648174,3.93912742137609,2.11047347579222));
#14288=CARTESIAN_POINT('Ctrl Pts',(-4.30472226008525,4.06259483097229,2.10268519742951));
#14289=CARTESIAN_POINT('Ctrl Pts',(-4.18938427050191,4.18143036333759,2.0948969190668));
#14290=CARTESIAN_POINT('Ctrl Pts',(-4.0692856919947,4.29521181310389,2.08710864070409));
#14291=CARTESIAN_POINT('Ctrl Pts',(-3.95510786529101,4.4033839398267,2.07970431745339));
#14292=CARTESIAN_POINT('Ctrl Pts',(-3.83662771957441,4.50698812224134,2.07229999420269));
#14293=CARTESIAN_POINT('Ctrl Pts',(-3.71423151376274,4.60569373978251,2.06489567095199));
#14294=CARTESIAN_POINT('Ctrl Pts',(-3.58549335751221,4.70951378166657,2.0571076932344));
#14295=CARTESIAN_POINT('Ctrl Pts',(-3.45237649393933,4.8079512819552,2.04931971551681));
#14296=CARTESIAN_POINT('Ctrl Pts',(-3.31535291362396,4.90064951007773,2.04153173779923));
#14297=CARTESIAN_POINT('Ctrl Pts',(-3.17835627331423,4.99332951293726,2.03374529126455));
#14298=CARTESIAN_POINT('Ctrl Pts',(-3.0374547133458,5.0802723161561,2.02595884472987));
#14299=CARTESIAN_POINT('Ctrl Pts',(-2.89314982158033,5.16116408113419,2.01817239819518));
#14300=CARTESIAN_POINT('Ctrl Pts',(-2.74883942489208,5.24205893195998,2.01038565462423));
#14301=CARTESIAN_POINT('Ctrl Pts',(-2.60112571341439,5.31690212294558,2.00259891105328));
#14302=CARTESIAN_POINT('Ctrl Pts',(-2.45053617983699,5.38542505228788,1.99481216748233));
#14303=CARTESIAN_POINT('Ctrl Pts',(-2.29995660661947,5.45394344935613,1.98702593894563));
#14304=CARTESIAN_POINT('Ctrl Pts',(-2.14650188287439,5.5161422890811,1.97923971040894));
#14305=CARTESIAN_POINT('Ctrl Pts',(-1.99072097823127,5.57180047644654,1.97145348187224));
#14306=CARTESIAN_POINT('Ctrl Pts',(-1.83489906479755,5.62747331563954,1.9636652036375));
#14307=CARTESIAN_POINT('Ctrl Pts',(-1.67675004730577,5.67660195251726,1.95587692540276));
#14308=CARTESIAN_POINT('Ctrl Pts',(-1.516840474363,5.71901438517462,1.94808864716802));
#14309=CARTESIAN_POINT('Ctrl Pts',(-1.36481428338547,5.75933592733331,1.9406843232585));
#14310=CARTESIAN_POINT('Ctrl Pts',(-1.21119719741052,5.79358745044747,1.93327999934899));
#14311=CARTESIAN_POINT('Ctrl Pts',(-1.05648660776257,5.82166356036815,1.92587567543947));
#14312=CARTESIAN_POINT('Ctrl Pts',(-0.893759717818616,5.85119442867854,
1.91808769787003));
#14313=CARTESIAN_POINT('Ctrl Pts',(-0.729764785624142,5.87390350126465,
1.91029972030059));
#14314=CARTESIAN_POINT('Ctrl Pts',(-0.565086972430272,5.88970349644951,
1.90251174273114));
#14315=CARTESIAN_POINT('Ctrl Pts',(-0.400441536339083,5.90550038521672,
1.89472529634641));
#14316=CARTESIAN_POINT('Ctrl Pts',(-0.235113805031662,5.91439087646084,
1.88693884996168));
#14317=CARTESIAN_POINT('Ctrl Pts',(-0.0696943950806309,5.91633951475018,
1.87915240357695));
#14318=CARTESIAN_POINT('Ctrl Pts',(0.0957313252371021,5.91828822737554,
1.87136566015735));
#14319=CARTESIAN_POINT('Ctrl Pts',(0.261248411726427,5.91329454942756,1.86357891673775));
#14320=CARTESIAN_POINT('Ctrl Pts',(0.426265156846195,5.90137514301191,1.85579217331816));
#14321=CARTESIAN_POINT('Ctrl Pts',(0.591270987344642,5.8894565249757,1.84800594493329));
#14322=CARTESIAN_POINT('Ctrl Pts',(0.755776223961052,5.87061311830516,1.84021971654843));
#14323=CARTESIAN_POINT('Ctrl Pts',(0.919193042425616,5.84491357620079,1.83243348816357));
#14324=CARTESIAN_POINT('Ctrl Pts',(1.0826528798253,5.81920726877726,1.82464521007993));
#14325=CARTESIAN_POINT('Ctrl Pts',(1.24502341035624,5.78664126718395,1.81685693199629));
#14326=CARTESIAN_POINT('Ctrl Pts',(1.40572487473833,5.74733574267607,1.80906865391264));
#14327=CARTESIAN_POINT('Ctrl Pts',(1.55850393618787,5.70996793668136,1.80166432925075));
#14328=CARTESIAN_POINT('Ctrl Pts',(1.70977427758417,5.66650916541479,1.79426000458885));
#14329=CARTESIAN_POINT('Ctrl Pts',(1.85904874226642,5.617104978223,1.78685567992696));
#14330=CARTESIAN_POINT('Ctrl Pts',(2.01605784001132,5.56514092079152,1.77906770133967));
#14331=CARTESIAN_POINT('Ctrl Pts',(2.17091490275741,5.50658037955851,1.77127972275238));
#14332=CARTESIAN_POINT('Ctrl Pts',(2.32306438204911,5.44162681919247,1.76349174416509));
#14333=CARTESIAN_POINT('Ctrl Pts',(2.47518394753153,5.37668602921794,1.75570529675692));
#14334=CARTESIAN_POINT('Ctrl Pts',(2.62459669801067,5.30535485341998,1.74791884934875));
#14335=CARTESIAN_POINT('Ctrl Pts',(2.77076710281248,5.22788487100397,1.74013240194059));
#14336=CARTESIAN_POINT('Ctrl Pts',(2.91694308365394,5.1504119332996,1.7323456574987));
#14337=CARTESIAN_POINT('Ctrl Pts',(3.0598761871294,5.06679986652189,1.72455891305681));
#14338=CARTESIAN_POINT('Ctrl Pts',(3.19905487166316,4.97734653109347,1.71677216861491));
#14339=CARTESIAN_POINT('Ctrl Pts',(3.33822435052314,4.88789911236291,1.70898593921043));
#14340=CARTESIAN_POINT('Ctrl Pts',(3.47363963860669,4.79261137102534,1.70119970980595));
#14341=CARTESIAN_POINT('Ctrl Pts',(3.60481749027507,4.69182495669936,1.69341348040147));
#14342=CARTESIAN_POINT('Ctrl Pts',(3.73602987383304,4.59101201087215,1.68562520131245));
#14343=CARTESIAN_POINT('Ctrl Pts',(3.86300233725031,4.4846976929188,1.67783692222343));
#14344=CARTESIAN_POINT('Ctrl Pts',(3.98528337592958,4.37326502467428,1.67004864313442));
#14345=CARTESIAN_POINT('Ctrl Pts',(4.101536000905,4.26732594915319,1.66264432356109));
#14346=CARTESIAN_POINT('Ctrl Pts',(4.21354843483753,4.15676120981883,1.65524000398776));
#14347=CARTESIAN_POINT('Ctrl Pts',(4.32096262643276,4.04193178362417,1.64783568441444));
#14348=CARTESIAN_POINT('Ctrl Pts',(4.43394250280458,3.92115245099925,1.64004770875137));
#14349=CARTESIAN_POINT('Ctrl Pts',(4.54187538315362,3.79561154167765,1.6322597330883));
#14350=CARTESIAN_POINT('Ctrl Pts',(4.64437089005308,3.66575361939773,1.62447175742523));
#14351=CARTESIAN_POINT('Ctrl Pts',(4.74684624534447,3.53592122844142,1.61668531295351));
#14352=CARTESIAN_POINT('Ctrl Pts',(4.84388616237861,3.40177376874398,1.60889886848179));
#14353=CARTESIAN_POINT('Ctrl Pts',(4.93514087011828,3.26378846658115,1.60111242401007));
#14354=CARTESIAN_POINT('Ctrl Pts',(5.02639905910903,3.12579790045449,1.59332568249539));
#14355=CARTESIAN_POINT('Ctrl Pts',(5.11187141762193,2.98396946324121,1.58553894098072));
#14356=CARTESIAN_POINT('Ctrl Pts',(5.19125139026312,2.83880953316548,1.57775219946604));
#14357=CARTESIAN_POINT('Ctrl Pts',(5.27062611259703,2.69365920417944,1.56996597297782));
#14358=CARTESIAN_POINT('Ctrl Pts',(5.34390910221005,2.54517810372957,1.56217974648959));
#14359=CARTESIAN_POINT('Ctrl Pts',(5.41083960789498,2.3938975124543,1.55439352000136));
#14360=CARTESIAN_POINT('Ctrl Pts',(5.47778773309103,2.24257709643796,1.54660524378256));
#14361=CARTESIAN_POINT('Ctrl Pts',(5.53837990159402,2.08845600860906,1.53881696756376));
#14362=CARTESIAN_POINT('Ctrl Pts',(5.59240303424354,1.93208666086271,1.53102869134495));
#14363=CARTESIAN_POINT('Ctrl Pts',(5.64376296481145,1.78342592148457,1.52362435719727));
#14364=CARTESIAN_POINT('Ctrl Pts',(5.6891858457379,1.63273349867491,1.5162200230496));
#14365=CARTESIAN_POINT('Ctrl Pts',(5.72853009638974,1.48049771943661,1.50881568890192));
#14366=CARTESIAN_POINT('Ctrl Pts',(5.76991292733899,1.3203740060027,1.50102770709394));
#14367=CARTESIAN_POINT('Ctrl Pts',(5.80458529230649,1.15848547592686,1.49323972528595));
#14368=CARTESIAN_POINT('Ctrl Pts',(5.83241723947752,0.995409316384714,1.48545174347797));
#14369=CARTESIAN_POINT('Ctrl Pts',(5.86024371469618,0.83236521873785,1.47766529284081));
#14370=CARTESIAN_POINT('Ctrl Pts',(5.88123240180981,0.66813427231966,1.46987884220365));
#14371=CARTESIAN_POINT('Ctrl Pts',(5.89530463575843,0.503302904924223,1.46209239156649));
#14372=CARTESIAN_POINT('Ctrl Pts',(5.90937740649521,0.338465250003518,1.45430564391363));
#14373=CARTESIAN_POINT('Ctrl Pts',(5.91653316501837,0.173027446319633,1.44651889626076));
#14374=CARTESIAN_POINT('Ctrl Pts',(5.91674514353126,0.00758083104048666,
1.43873214860789));
#14375=CARTESIAN_POINT('Ctrl Pts',(5.91695710802284,-0.157854840787371,
1.43094591600874));
#14376=CARTESIAN_POINT('Ctrl Pts',(5.91022621132736,-0.323299003468176,
1.42315968340959));
#14377=CARTESIAN_POINT('Ctrl Pts',(5.89657782152837,-0.488160380571532,
1.41537345081044));
#14378=CARTESIAN_POINT('Ctrl Pts',(5.88292583896394,-0.653065155340592,
1.40758516858435));
#14379=CARTESIAN_POINT('Ctrl Pts',(5.86235274910231,-0.817386519151318,
1.39979688635826));
#14380=CARTESIAN_POINT('Ctrl Pts',(5.83493589075115,-0.980537461458797,
1.39200860413217));
#14381=CARTESIAN_POINT('Ctrl Pts',(5.80887074100773,-1.13564472019569,1.38460430055124));
#14382=CARTESIAN_POINT('Ctrl Pts',(5.77662043409478,-1.28969392584956,1.37719999697032));
#14383=CARTESIAN_POINT('Ctrl Pts',(5.73829440721614,-1.44218856555304,1.3697956933894));
#14384=CARTESIAN_POINT('Ctrl Pts',(5.69798244315146,-1.60258500986096,1.36200772150222));
#14385=CARTESIAN_POINT('Ctrl Pts',(5.65093397087917,-1.76131888155211,1.35421974961504));
#14386=CARTESIAN_POINT('Ctrl Pts',(5.59731117314015,-1.91782121000381,1.34643177772786));
#14387=CARTESIAN_POINT('Ctrl Pts',(5.54369891818946,-2.07429276850332,1.33864533703529));
#14388=CARTESIAN_POINT('Ctrl Pts',(5.48351502036226,-2.22853335707382,1.33085889634273));
#14389=CARTESIAN_POINT('Ctrl Pts',(5.41697111517321,-2.37999044113188,1.32307245565016));
#14390=CARTESIAN_POINT('Ctrl Pts',(5.35042467115252,-2.53145330369116,1.31528571788363));
#14391=CARTESIAN_POINT('Ctrl Pts',(5.27751785913328,-2.6801321550939,1.3074989801171));
#14392=CARTESIAN_POINT('Ctrl Pts',(5.19851023020338,-2.82549499185024,1.29971224235056));
#14393=CARTESIAN_POINT('Ctrl Pts',(5.11950782670809,-2.97084821454768,1.29192601958606));
#14394=CARTESIAN_POINT('Ctrl Pts',(5.03440556647351,-3.1128855807527,1.28413979682155));
#14395=CARTESIAN_POINT('Ctrl Pts',(4.94350874662523,-3.25110009605054,1.27635357405704));
#14396=CARTESIAN_POINT('Ctrl Pts',(4.85258799721329,-3.38935099780336,1.2685653014858));
#14397=CARTESIAN_POINT('Ctrl Pts',(4.75586981402496,-3.52377676939567,1.26077702891456));
#14398=CARTESIAN_POINT('Ctrl Pts',(4.65370308235257,-3.65389903853434,1.25298875634332));
#14399=CARTESIAN_POINT('Ctrl Pts',(4.55657261843156,-3.77760698299929,1.24558440352118));
#14400=CARTESIAN_POINT('Ctrl Pts',(4.45451799830206,-3.89742527725001,1.23818005069903));
#14401=CARTESIAN_POINT('Ctrl Pts',(4.34787297933363,-4.01297036097708,1.23077569787689));
#14402=CARTESIAN_POINT('Ctrl Pts',(4.23570253591715,-4.13450199369306,1.2229877153972));
#14403=CARTESIAN_POINT('Ctrl Pts',(4.11841326941338,-4.25134933402431,1.21519973291751));
#14404=CARTESIAN_POINT('Ctrl Pts',(3.99641992455798,-4.36309045850485,1.20741175043782));
#14405=CARTESIAN_POINT('Ctrl Pts',(3.8744505647518,-4.47480961361996,1.19962529914939));
#14406=CARTESIAN_POINT('Ctrl Pts',(3.7477792074702,-4.58142434031684,1.19183884786096));
#14407=CARTESIAN_POINT('Ctrl Pts',(3.61685614939428,-4.68255081735253,1.18405239657253));
#14408=CARTESIAN_POINT('Ctrl Pts',(3.4859280978638,-4.78368115138998,1.17626564830593));
#14409=CARTESIAN_POINT('Ctrl Pts',(3.35074827151816,-4.8793226184451,1.16847890003933));
#14410=CARTESIAN_POINT('Ctrl Pts',(3.21179920916008,-4.96913235912857,1.16069215177272));
#14411=CARTESIAN_POINT('Ctrl Pts',(3.0728593379622,-5.05893615910471,1.15290591858157));
#14412=CARTESIAN_POINT('Ctrl Pts',(2.93015099814565,-5.14290883128224,1.14511968539041));
#14413=CARTESIAN_POINT('Ctrl Pts',(2.78418492235192,-5.22075137127293,1.13733345219926));
#14414=CARTESIAN_POINT('Ctrl Pts',(2.63818042362199,-5.29861440190799,1.12954516942268));
#14415=CARTESIAN_POINT('Ctrl Pts',(2.48891675659648,-5.37034392375692,1.12175688664611));
#14416=CARTESIAN_POINT('Ctrl Pts',(2.3369292236997,-5.43568692677552,1.11396860386953));
#14417=CARTESIAN_POINT('Ctrl Pts',(2.19243506518412,-5.49780835250106,1.10656430336781));
#14418=CARTESIAN_POINT('Ctrl Pts',(2.04547939960954,-5.55415772801522,1.09916000286609));
#14419=CARTESIAN_POINT('Ctrl Pts',(1.89653885159617,-5.60455805098728,1.09175570236437));
#14420=CARTESIAN_POINT('Ctrl Pts',(1.73988035291167,-5.65757006843538,1.08396771839439));
#14421=CARTESIAN_POINT('Ctrl Pts',(1.58096976410852,-5.70401907735309,1.0761797344244));
#14422=CARTESIAN_POINT('Ctrl Pts',(1.42037319087769,-5.74373315546047,1.06839175045442));
#14423=CARTESIAN_POINT('Ctrl Pts',(1.25980819081974,-5.78343942580814,1.06060529759659));
#14424=CARTESIAN_POINT('Ctrl Pts',(1.09755817771552,-5.81641333061659,1.05281884473876));
#14425=CARTESIAN_POINT('Ctrl Pts',(0.934202233413419,-5.84253341878208,
1.04503239188092));
#14426=CARTESIAN_POINT('Ctrl Pts',(0.770840056423254,-5.86865450353426,
1.03724564193851));
#14427=CARTESIAN_POINT('Ctrl Pts',(0.606372178706276,-5.88792119401931,
1.0294588919961));
#14428=CARTESIAN_POINT('Ctrl Pts',(0.441386383453259,-5.90026343674603,
1.02167214205369));
#14429=CARTESIAN_POINT('Ctrl Pts',(0.276411500469021,-5.91260486314871,
1.01388590713203));
#14430=CARTESIAN_POINT('Ctrl Pts',(0.110919087192631,-5.91802273456761,
1.00609967221037));
#14431=CARTESIAN_POINT('Ctrl Pts',(-0.0544993110831236,-5.91649899751462,
0.998313437288713));
#14432=CARTESIAN_POINT('Ctrl Pts',(-0.219961254320349,-5.91497485935104,
0.990525152708109));
#14433=CARTESIAN_POINT('Ctrl Pts',(-0.385348823857749,-5.90650546233805,
0.982736868127505));
#14434=CARTESIAN_POINT('Ctrl Pts',(-0.550070918233379,-5.89112489660624,
0.974948583546901));
#14435=CARTESIAN_POINT('Ctrl Pts',(-0.706671580567881,-5.87650265185025,
0.967544291315217));
#14436=CARTESIAN_POINT('Ctrl Pts',(-0.862670545487099,-5.85563433930647,
0.960139999083533));
#14437=CARTESIAN_POINT('Ctrl Pts',(-1.01756461492942,-5.82859269609256,
0.952735706851849));
#14438=CARTESIAN_POINT('Ctrl Pts',(-1.18048437152111,-5.80014991615843,
0.944947768343532));
#14439=CARTESIAN_POINT('Ctrl Pts',(-1.34223998014971,-5.76486691519121,
0.937159829835215));
#14440=CARTESIAN_POINT('Ctrl Pts',(-1.50225211465874,-5.72286371902244,
0.929371891326898));
#14441=CARTESIAN_POINT('Ctrl Pts',(-1.66223278487941,-5.6808687822315,0.921585484214583));
#14442=CARTESIAN_POINT('Ctrl Pts',(-1.82047035613447,-5.63215636798189,
0.913799077102268));
#14443=CARTESIAN_POINT('Ctrl Pts',(-1.97639826796814,-5.5768970269203,0.906012669989952));
#14444=CARTESIAN_POINT('Ctrl Pts',(-2.13233212911768,-5.52163557747882,
0.898225965792947));
#14445=CARTESIAN_POINT('Ctrl Pts',(-2.28595585199728,-5.45982680439626,
0.890439261595941));
#14446=CARTESIAN_POINT('Ctrl Pts',(-2.43671983863289,-5.39169055032954,
0.882652557398935));
#14447=CARTESIAN_POINT('Ctrl Pts',(-2.5874738553676,-5.32355880205838,0.874866368130401));
#14448=CARTESIAN_POINT('Ctrl Pts',(-2.73536822312365,-5.24910054186575,
0.867080178861867));
#14449=CARTESIAN_POINT('Ctrl Pts',(-2.87987493147773,-5.16858306903799,
0.859293989593333));
#14450=CARTESIAN_POINT('Ctrl Pts',(-3.02441969116596,-5.08804439444529,
0.851505750074724));
#14451=CARTESIAN_POINT('Ctrl Pts',(-3.16557472869233,-5.00144347299672,
0.843717510556114));
#14452=CARTESIAN_POINT('Ctrl Pts',(-3.30283738272883,-4.90909317346381,
0.835929271037505));
#14453=CARTESIAN_POINT('Ctrl Pts',(-3.43333722814679,-4.82129289087463,
0.828524751138114));
#14454=CARTESIAN_POINT('Ctrl Pts',(-3.56031878657049,-4.72829627227522,
0.821120231238722));
#14455=CARTESIAN_POINT('Ctrl Pts',(-3.68337502978592,-4.63040807623362,
0.813715711339331));
#14456=CARTESIAN_POINT('Ctrl Pts',(-3.812805829406,-4.52744907833173,0.805927622687028));
#14457=CARTESIAN_POINT('Ctrl Pts',(-3.93794013521075,-4.41904143915328,
0.798139534034725));
#14458=CARTESIAN_POINT('Ctrl Pts',(-4.05832674032956,-4.30556786396708,
0.790351445382422));
#14459=CARTESIAN_POINT('Ctrl Pts',(-4.17868968384183,-4.19211659165325,
0.782564887454315));
#14460=CARTESIAN_POINT('Ctrl Pts',(-4.29430655619166,-4.0736015890688,0.774778329526209));
#14461=CARTESIAN_POINT('Ctrl Pts',(-4.40476154371107,-3.95044381121211,
0.766991771598102));
#14462=CARTESIAN_POINT('Ctrl Pts',(-4.51522073971969,-3.82728134087217,
0.759204916991269));
#14463=CARTESIAN_POINT('Ctrl Pts',(-4.62051744106989,-3.69947597651694,
0.751418062384436));
#14464=CARTESIAN_POINT('Ctrl Pts',(-4.72027432182029,-3.56748383167521,
0.743631207777603));
#14465=CARTESIAN_POINT('Ctrl Pts',(-4.82002459913294,-3.43550042409455,
0.735844868624032));
#14466=CARTESIAN_POINT('Ctrl Pts',(-4.91423559709953,-3.29933104564105,
0.728058529470462));
#14467=CARTESIAN_POINT('Ctrl Pts',(-5.00257165952262,-3.15946314329525,
0.720272190316891));
#14468=CARTESIAN_POINT('Ctrl Pts',(-5.09093095587724,-3.0195584532415,0.712483803219754));
#14469=CARTESIAN_POINT('Ctrl Pts',(-5.17341205663834,-2.87595356478015,
0.704695416122617));
#14470=CARTESIAN_POINT('Ctrl Pts',(-5.24972337465897,-2.72916380088467,
0.69690702902548));
#14471=CARTESIAN_POINT('Ctrl Pts',(-5.32226619017904,-2.58962299568426,
0.689503257959258));
#14472=CARTESIAN_POINT('Ctrl Pts',(-5.3892337649721,-2.44720451728423,0.682099486893036));
#14473=CARTESIAN_POINT('Ctrl Pts',(-5.45041467059078,-2.30237062201307,
0.674695715826813));
#14474=CARTESIAN_POINT('Ctrl Pts',(-5.51451855214798,-2.15061714968302,
0.66693822255818));
#14475=CARTESIAN_POINT('Ctrl Pts',(-5.57229381698287,-1.99615353593203,
0.659180729289547));
#14476=CARTESIAN_POINT('Ctrl Pts',(-5.62352825526249,-1.83952725578189,
0.651423236020914));
#14477=CARTESIAN_POINT('Ctrl Pts',(-5.67475659161283,-1.68291962953947,
0.64366666665575));
#14478=CARTESIAN_POINT('Ctrl Pts',(-5.71944555125269,-1.52415015800134,
0.635910097290585));
#14479=CARTESIAN_POINT('Ctrl Pts',(-5.75743223964334,-1.36378318233344,
0.628153527925421));
#14480=CARTESIAN_POINT('Ctrl Pts',(-5.79541379850369,-1.20343786181091,
0.620398005968157));
#14481=CARTESIAN_POINT('Ctrl Pts',(-5.82669481876659,-1.04149578374859,
0.612642484010893));
#14482=CARTESIAN_POINT('Ctrl Pts',(-5.85116309175147,-0.878533457658481,
0.604886962053629));
#14483=CARTESIAN_POINT('Ctrl Pts',(-5.87563494937356,-0.715547257353048,
0.597130303901236));
#14484=CARTESIAN_POINT('Ctrl Pts',(-5.89329201504539,-0.551540831112721,
0.589373645748843));
#14485=CARTESIAN_POINT('Ctrl Pts',(-5.90407361576536,-0.38709856900187,
0.58161698759645));
#14486=CARTESIAN_POINT('Ctrl Pts',(-5.9125255268044,-0.258189012200728,
0.57553638914294));
#14487=CARTESIAN_POINT('Ctrl Pts',(-5.91675327563298,-0.129011823564914,
0.56945579068943));
#14488=CARTESIAN_POINT('Ctrl Pts',(-5.91674999809507,0.000150139963021254,
0.56337519223592));
#14489=CARTESIAN_POINT('Ctrl Pts',(-5.91671935081961,9.79311290895061E-5,
0.311624807795122));
#14490=CARTESIAN_POINT('Ctrl Pts',(-5.9159606431657,-0.744933876419475,
0.34669625714854));
#14491=CARTESIAN_POINT('Ctrl Pts',(-5.58832513159245,-2.47438543481707,
0.428083168263666));
#14492=CARTESIAN_POINT('Ctrl Pts',(-3.94583161690989,-4.74057417199595,
0.5557855411405));
#14493=CARTESIAN_POINT('Ctrl Pts',(-1.19688167165833,-6.05056333833174,
0.694731926425626));
#14494=CARTESIAN_POINT('Ctrl Pts',(1.84380127964053,-5.8858030207415,0.833678311710752));
#14495=CARTESIAN_POINT('Ctrl Pts',(4.43505585547799,-4.28630058757937,0.972624696995877));
#14496=CARTESIAN_POINT('Ctrl Pts',(5.94524311070241,-1.64202041018131,1.111571082281));
#14497=CARTESIAN_POINT('Ctrl Pts',(6.00625314087822,1.40252303398188,1.25051746756613));
#14498=CARTESIAN_POINT('Ctrl Pts',(4.6032120253118,4.10518839802672,1.38946385285126));
#14499=CARTESIAN_POINT('Ctrl Pts',(2.07811839533017,5.80719982717728,1.52841023813638));
#14500=CARTESIAN_POINT('Ctrl Pts',(-0.953525845772481,6.09367921958054,
1.66735662342151));
#14501=CARTESIAN_POINT('Ctrl Pts',(-3.75274390497941,4.89479875289577,1.80630300870662));
#14502=CARTESIAN_POINT('Ctrl Pts',(-5.53517423299281,2.63231165564186,1.93772573683117));
#14503=CARTESIAN_POINT('Ctrl Pts',(-5.91614959567988,0.823835166170361,
2.022833003194));
#14504=CARTESIAN_POINT('Ctrl Pts',(-5.91696061209103,-0.000135486519901937,
2.06162480779511));
#14505=CARTESIAN_POINT('Origin',(0.,0.,0.));
#14506=CARTESIAN_POINT('',(-5.9167499990742,0.000104668362501446,4.0633751922049));
#14507=CARTESIAN_POINT('',(-5.91671854102846,6.05288050462508E-5,3.81162480733001));
#14508=CARTESIAN_POINT('',(-5.91675,-7.2459289488551E-16,0.));
#14509=CARTESIAN_POINT('Ctrl Pts',(-5.91636571888598,0.000104875761786346,
4.0633751821236));
#14510=CARTESIAN_POINT('Ctrl Pts',(-5.91659904124727,0.369799356614414,
4.04597532412481));
#14511=CARTESIAN_POINT('Ctrl Pts',(-5.79166172450625,1.72392321031336,3.98223546762185));
#14512=CARTESIAN_POINT('Ctrl Pts',(-4.77062984080853,3.9098068260098,3.87215561261471));
#14513=CARTESIAN_POINT('Ctrl Pts',(-2.31709881191985,5.71634075178491,3.73313561710221));
#14514=CARTESIAN_POINT('Ctrl Pts',(0.701821240062036,6.12804580937004,3.59411562158967));
#14515=CARTESIAN_POINT('Ctrl Pts',(3.54949178673034,5.04446295958584,3.45509562607715));
#14516=CARTESIAN_POINT('Ctrl Pts',(5.5310604289586,2.7299943270923,3.31607563056466));
#14517=CARTESIAN_POINT('Ctrl Pts',(6.16300995416518,-0.250612848028229,
3.17705563505213));
#14518=CARTESIAN_POINT('Ctrl Pts',(5.29114006546501,-3.17006865891296,3.03803563953961));
#14519=CARTESIAN_POINT('Ctrl Pts',(3.12819337966652,-5.31600457811581,2.89901564402709));
#14520=CARTESIAN_POINT('Ctrl Pts',(0.201944675889461,-6.16479657747871,
2.75999564851458));
#14521=CARTESIAN_POINT('Ctrl Pts',(-2.7735800028256,-5.50933321411907,2.62097565300206));
#14522=CARTESIAN_POINT('Ctrl Pts',(-5.07233091594555,-3.50955233214131,
2.48195565748954));
#14523=CARTESIAN_POINT('Ctrl Pts',(-5.85491408923019,-1.40302289339775,
2.37942217055716));
#14524=CARTESIAN_POINT('Ctrl Pts',(-5.91702306393301,-0.209464058491032,
2.32322868212894));
#14525=CARTESIAN_POINT('Ctrl Pts',(-5.91680640865236,-0.000151898509373194,
2.3133751922049));
#14526=CARTESIAN_POINT('Ctrl Pts',(-5.91696061209103,-0.000135486519901937,
2.06162480779511));
#14527=CARTESIAN_POINT('Ctrl Pts',(-5.91711790844504,-0.159944311218166,
2.0691484649557));
#14528=CARTESIAN_POINT('Ctrl Pts',(-5.8717187617454,-1.30344349398301,2.12298758387799));
#14529=CARTESIAN_POINT('Ctrl Pts',(-5.15946265009878,-3.37965766280873,
2.22314216456201));
#14530=CARTESIAN_POINT('Ctrl Pts',(-2.91369452509655,-5.43622339098344,
2.36208854984714));
#14531=CARTESIAN_POINT('Ctrl Pts',(0.0422993022801887,-6.16768606948156,
2.50103493513227));
#14532=CARTESIAN_POINT('Ctrl Pts',(2.987982492874,-5.39574844063278,2.63998132041738));
#14533=CARTESIAN_POINT('Ctrl Pts',(5.20533196103198,-3.30857368275367,2.77892770570252));
#14534=CARTESIAN_POINT('Ctrl Pts',(6.15385913663824,-0.414919702877659,
2.91787409098763));
#14535=CARTESIAN_POINT('Ctrl Pts',(5.60235639658781,2.57987275594974,3.05682047627278));
#14536=CARTESIAN_POINT('Ctrl Pts',(3.68525493156209,4.94581001697408,3.19576686155787));
#14537=CARTESIAN_POINT('Ctrl Pts',(0.869856557091352,6.10618458632405,3.33471324684302));
#14538=CARTESIAN_POINT('Ctrl Pts',(-2.15757313440082,5.77815011947596,3.47365963212813));
#14539=CARTESIAN_POINT('Ctrl Pts',(-4.65908499542979,4.04166644322682,3.61260601741327));
#14540=CARTESIAN_POINT('Ctrl Pts',(-5.76648150081493,1.83499894741018,3.72526107365585));
#14541=CARTESIAN_POINT('Ctrl Pts',(-5.9164332113239,0.425530598565133,3.7916006681367));
#14542=CARTESIAN_POINT('Ctrl Pts',(-5.91628064325804,6.06618882952148E-5,
3.81162480085584));
#14543=CARTESIAN_POINT('Origin',(0.,0.,0.));
#14544=CARTESIAN_POINT('',(-5.91674999987984,-3.77088797724088E-5,5.81337519217928));
#14545=CARTESIAN_POINT('',(-5.91674999993288,2.81822667955784E-5,5.56162480783485));
#14546=CARTESIAN_POINT('',(-5.91675,-7.2459289488551E-16,0.));
#14547=CARTESIAN_POINT('Ctrl Pts',(-5.91674999987984,-3.7708879784822E-5,
5.81337519217929));
#14548=CARTESIAN_POINT('Ctrl Pts',(-5.91675105226619,0.165088037798311,
5.8055995119159));
#14549=CARTESIAN_POINT('Ctrl Pts',(-5.90983522173606,0.330244822975408,
5.79782383165252));
#14550=CARTESIAN_POINT('Ctrl Pts',(-5.8960207664832,0.494843089977935,5.79004815138914));
#14551=CARTESIAN_POINT('Ctrl Pts',(-5.88220905787429,0.659408630909986,
5.78227401711688));
#14552=CARTESIAN_POINT('Ctrl Pts',(-5.8615014880818,0.823415554973462,5.77449988284463));
#14553=CARTESIAN_POINT('Ctrl Pts',(-5.83396828371955,0.986278169207031,
5.76672574857237));
#14554=CARTESIAN_POINT('Ctrl Pts',(-5.80643420898685,1.14914593179905,5.75895136854678));
#14555=CARTESIAN_POINT('Ctrl Pts',(-5.77207411781776,1.3108689944891,5.7511769885212));
#14556=CARTESIAN_POINT('Ctrl Pts',(-5.73100970695798,1.47086991309681,5.74340260849561));
#14557=CARTESIAN_POINT('Ctrl Pts',(-5.68994750990974,1.63086220594139,5.73562864759237));
#14558=CARTESIAN_POINT('Ctrl Pts',(-5.64218179703028,1.78913222916042,5.72785468668913));
#14559=CARTESIAN_POINT('Ctrl Pts',(-5.5878847206219,1.94511565505508,5.72008072578589));
#14560=CARTESIAN_POINT('Ctrl Pts',(-5.53357411629539,2.10113794365016,5.71230482802871));
#14561=CARTESIAN_POINT('Ctrl Pts',(-5.47272900192084,2.25487219245781,5.70452893027153));
#14562=CARTESIAN_POINT('Ctrl Pts',(-5.40557074228287,2.40577129267839,5.69675303251435));
#14563=CARTESIAN_POINT('Ctrl Pts',(-5.35565775468702,2.51792168129976,5.69097387310204));
#14564=CARTESIAN_POINT('Ctrl Pts',(-5.30225861598434,2.62850636722495,5.68519471368974));
#14565=CARTESIAN_POINT('Ctrl Pts',(-5.24548115676519,2.73730853148149,5.67941555427743));
#14566=CARTESIAN_POINT('Ctrl Pts',(-5.16896802428216,2.88392999927327,5.67162757651591));
#14567=CARTESIAN_POINT('Ctrl Pts',(-5.08628982356809,3.02736763814977,5.6638395987544));
#14568=CARTESIAN_POINT('Ctrl Pts',(-4.99773662714317,3.16710580312872,5.65605162099288));
#14569=CARTESIAN_POINT('Ctrl Pts',(-4.90920084103584,3.30681649438646,5.64826517441456));
#14570=CARTESIAN_POINT('Ctrl Pts',(-4.81479253487457,3.44282889327005,5.64047872783624));
#14571=CARTESIAN_POINT('Ctrl Pts',(-4.71484605482713,3.57465484232828,5.63269228125791));
#14572=CARTESIAN_POINT('Ctrl Pts',(-4.61489576204672,3.70648582024938,5.6249055376442));
#14573=CARTESIAN_POINT('Ctrl Pts',(-4.5094070625286,3.83412977175722,5.61711879403049));
#14574=CARTESIAN_POINT('Ctrl Pts',(-4.39875612857577,3.9571296521364,5.60933205041678));
#14575=CARTESIAN_POINT('Ctrl Pts',(-4.28811251335451,4.08012139699356,5.60154582183791));
#14576=CARTESIAN_POINT('Ctrl Pts',(-4.17230756079509,4.19846944790559,5.59375959325904));
#14577=CARTESIAN_POINT('Ctrl Pts',(-4.05175611777413,4.31175172343908,5.58597336468017));
#14578=CARTESIAN_POINT('Ctrl Pts',(-3.93117294001901,4.42506382012453,5.57818508640461));
#14579=CARTESIAN_POINT('Ctrl Pts',(-3.80584100672858,4.53330725632599,5.57039680812905));
#14580=CARTESIAN_POINT('Ctrl Pts',(-3.67621090030028,4.63609792595167,5.56260852985349));
#14581=CARTESIAN_POINT('Ctrl Pts',(-3.55297143262765,4.73382111507355,5.5552042061573));
#14582=CARTESIAN_POINT('Ctrl Pts',(-3.42584758127257,4.82661605532041,5.54779988246111));
#14583=CARTESIAN_POINT('Ctrl Pts',(-3.29525315733809,4.91418733785693,5.54039555876493));
#14584=CARTESIAN_POINT('Ctrl Pts',(-3.1578920003824,5.00629611496172,5.53260758100339));
#14585=CARTESIAN_POINT('Ctrl Pts',(-3.01664193089225,5.09265848517566,5.52481960324185));
#14586=CARTESIAN_POINT('Ctrl Pts',(-2.8720044538864,5.17296056232374,5.51703162548031));
#14587=CARTESIAN_POINT('Ctrl Pts',(-2.72739541384842,5.25324685139507,5.50924517890196));
#14588=CARTESIAN_POINT('Ctrl Pts',(-2.57940057435582,5.32747506978982,5.50145873232361));
#14589=CARTESIAN_POINT('Ctrl Pts',(-2.42854715514535,5.39537665763341,5.49367228574526));
#14590=CARTESIAN_POINT('Ctrl Pts',(-2.27768798121713,5.46328083576944,5.48588554213153));
#14591=CARTESIAN_POINT('Ctrl Pts',(-2.12397029912205,5.52485776565383,5.4780987985178));
#14592=CARTESIAN_POINT('Ctrl Pts',(-1.96794315914089,5.57988622508475,5.47031205490407));
#14593=CARTESIAN_POINT('Ctrl Pts',(-1.81192633918796,5.6349110447947,5.46252582632519));
#14594=CARTESIAN_POINT('Ctrl Pts',(-1.653600668451,5.68338815462775,5.45473959774631));
#14595=CARTESIAN_POINT('Ctrl Pts',(-1.49353241756466,5.72514554227082,5.44695336916743));
#14596=CARTESIAN_POINT('Ctrl Pts',(-1.33342202928609,5.76691392239624,5.43916509089183));
#14597=CARTESIAN_POINT('Ctrl Pts',(-1.17156845313732,5.80195896300279,5.43137681261624));
#14598=CARTESIAN_POINT('Ctrl Pts',(-1.00855115785462,5.83015909941488,5.42358853434064));
#14599=CARTESIAN_POINT('Ctrl Pts',(-0.853570457419871,5.8569689964011,5.41618421064456));
#14600=CARTESIAN_POINT('Ctrl Pts',(-0.697538273997836,5.87759258131212,
5.40877988694848));
#14601=CARTESIAN_POINT('Ctrl Pts',(-0.540959334783866,5.89196856412271,
5.4013755632524));
#14602=CARTESIAN_POINT('Ctrl Pts',(-0.37626727828091,5.90708943660538,5.39358758549088));
#14603=CARTESIAN_POINT('Ctrl Pts',(-0.210911387984493,5.91530348944729,
5.38579960772936));
#14604=CARTESIAN_POINT('Ctrl Pts',(-0.0454822305267683,5.91657518579848,
5.37801162996784));
#14605=CARTESIAN_POINT('Ctrl Pts',(0.119914402140894,5.91784663212327,5.37022518338949));
#14606=CARTESIAN_POINT('Ctrl Pts',(0.285383953883248,5.91217844293329,5.36243873681113));
#14607=CARTESIAN_POINT('Ctrl Pts',(0.450334976858607,5.89958718650024,5.35465229023278));
#14608=CARTESIAN_POINT('Ctrl Pts',(0.615292292343057,5.88699544973917,5.34686554661908));
#14609=CARTESIAN_POINT('Ctrl Pts',(0.779730720565956,5.86748013764543,5.33907880300537));
#14610=CARTESIAN_POINT('Ctrl Pts',(0.943062305544855,5.84110983036276,5.33129205939166));
#14611=CARTESIAN_POINT('Ctrl Pts',(1.10638308736111,5.81474126727867,5.3235058308128));
#14612=CARTESIAN_POINT('Ctrl Pts',(1.26859685696312,5.78151866738902,5.31571960223394));
#14613=CARTESIAN_POINT('Ctrl Pts',(1.42912409412647,5.74156205976102,5.30793337365508));
#14614=CARTESIAN_POINT('Ctrl Pts',(1.5896935895086,5.70159493369953,5.3001450953795));
#14615=CARTESIAN_POINT('Ctrl Pts',(1.74857535453158,5.65489033300201,5.29235681710392));
#14616=CARTESIAN_POINT('Ctrl Pts',(1.90520242872164,5.60161889707727,5.28456853882834));
#14617=CARTESIAN_POINT('Ctrl Pts',(2.05410793977932,5.5509736913734,5.27716421513219));
#14618=CARTESIAN_POINT('Ctrl Pts',(2.20097546360534,5.49439361569545,5.26975989143604));
#14619=CARTESIAN_POINT('Ctrl Pts',(2.34533251403175,5.43206645404173,5.26235556773989));
#14620=CARTESIAN_POINT('Ctrl Pts',(2.49716940617415,5.36650981864635,5.25456758997836));
#14621=CARTESIAN_POINT('Ctrl Pts',(2.64628307307795,5.2945712652669,5.24677961221684));
#14622=CARTESIAN_POINT('Ctrl Pts',(2.79213798906654,5.21650227762928,5.23899163445532));
#14623=CARTESIAN_POINT('Ctrl Pts',(2.93796422872813,5.13844863902397,5.23120518787699));
#14624=CARTESIAN_POINT('Ctrl Pts',(3.08053271429802,5.05426712178518,5.22341874129867));
#14625=CARTESIAN_POINT('Ctrl Pts',(3.21933208742007,4.96425537955165,5.21563229472034));
#14626=CARTESIAN_POINT('Ctrl Pts',(3.35813675542532,4.87424020357306,5.20784555110663));
#14627=CARTESIAN_POINT('Ctrl Pts',(3.49317175301991,4.7783945280985,5.20005880749292));
#14628=CARTESIAN_POINT('Ctrl Pts',(3.62395368407104,4.67706000156166,5.19227206387922));
#14629=CARTESIAN_POINT('Ctrl Pts',(3.75472696487569,4.57573217754575,5.18448583530035));
#14630=CARTESIAN_POINT('Ctrl Pts',(3.88124748952844,4.4689164248052,5.17669960672149));
#14631=CARTESIAN_POINT('Ctrl Pts',(4.00306389537987,4.35699552581893,5.16891337814262));
#14632=CARTESIAN_POINT('Ctrl Pts',(4.12491236896257,4.24504516405803,5.16112509986705));
#14633=CARTESIAN_POINT('Ctrl Pts',(4.24205401248351,4.12798718553333,5.15333682159148));
#14634=CARTESIAN_POINT('Ctrl Pts',(4.35407271622536,4.00624279647675,5.14554854331591));
#14635=CARTESIAN_POINT('Ctrl Pts',(4.4605690063147,3.89050028794358,5.13814421961973));
#14636=CARTESIAN_POINT('Ctrl Pts',(4.56243512271358,3.77052250313101,5.13073989592355));
#14637=CARTESIAN_POINT('Ctrl Pts',(4.65934611035522,3.64670047939473,5.12333557222737));
#14638=CARTESIAN_POINT('Ctrl Pts',(4.76127852816528,3.51646263366925,5.11554759446585));
#14639=CARTESIAN_POINT('Ctrl Pts',(4.85776514854029,3.38192500618747,5.10775961670433));
#14640=CARTESIAN_POINT('Ctrl Pts',(4.94845615893317,3.24356473738639,5.0999716389428));
#14641=CARTESIAN_POINT('Ctrl Pts',(5.03912933869608,3.10523167140004,5.09218519236446));
#14642=CARTESIAN_POINT('Ctrl Pts',(5.12400900697827,2.96307773077667,5.08439874578612));
#14643=CARTESIAN_POINT('Ctrl Pts',(5.20278867008055,2.81760902486159,5.07661229920778));
#14644=CARTESIAN_POINT('Ctrl Pts',(5.2815713384494,2.67213476964327,5.06882555559405));
#14645=CARTESIAN_POINT('Ctrl Pts',(5.35425338035422,2.52334577520074,5.06103881198032));
#14646=CARTESIAN_POINT('Ctrl Pts',(5.42057391169674,2.37177339354601,5.05325206836659));
#14647=CARTESIAN_POINT('Ctrl Pts',(5.48689005643205,2.22021103727085,5.04546583978773));
#14648=CARTESIAN_POINT('Ctrl Pts',(5.54684540462062,2.06586595501828,5.03767961120886));
#14649=CARTESIAN_POINT('Ctrl Pts',(5.60022688696906,1.90929028096014,5.02989338262999));
#14650=CARTESIAN_POINT('Ctrl Pts',(5.65362242180102,1.75267338891812,5.02210510435441));
#14651=CARTESIAN_POINT('Ctrl Pts',(5.70044052775977,1.59382503375644,5.01431682607883));
#14652=CARTESIAN_POINT('Ctrl Pts',(5.74051747969277,1.43331421113507,5.00652854780326));
#14653=CARTESIAN_POINT('Ctrl Pts',(5.77861867669246,1.28071641668446,4.99912422410712));
#14654=CARTESIAN_POINT('Ctrl Pts',(5.81062730972007,1.12661637797558,4.991719900411));
#14655=CARTESIAN_POINT('Ctrl Pts',(5.8364452462182,0.971512969752345,4.98431557671486));
#14656=CARTESIAN_POINT('Ctrl Pts',(5.86360093572451,0.808372898686376,4.97652759895332));
#14657=CARTESIAN_POINT('Ctrl Pts',(5.88391706992344,0.644064360225406,4.96873962119177));
#14658=CARTESIAN_POINT('Ctrl Pts',(5.89731490621227,0.479173725768137,4.96095164343023));
#14659=CARTESIAN_POINT('Ctrl Pts',(5.91071010837164,0.314315510223223,4.95316519685188));
#14660=CARTESIAN_POINT('Ctrl Pts',(5.91718970075061,0.148875745338547,4.94537875027353));
#14661=CARTESIAN_POINT('Ctrl Pts',(5.9167268410067,-0.0165544982084554,
4.93759230369518));
#14662=CARTESIAN_POINT('Ctrl Pts',(5.91626396360573,-0.181991052546074,
4.92980556008146));
#14663=CARTESIAN_POINT('Ctrl Pts',(5.90885810107439,-0.347417765270474,
4.92201881646774));
#14664=CARTESIAN_POINT('Ctrl Pts',(5.8945345389731,-0.512243234560655,4.91423207285402));
#14665=CARTESIAN_POINT('Ctrl Pts',(5.88021192426822,-0.677057801879899,
4.90644584427509));
#14666=CARTESIAN_POINT('Ctrl Pts',(5.85897255340783,-0.841270886979092,
4.89865961569617));
#14667=CARTESIAN_POINT('Ctrl Pts',(5.83089364091742,-1.00429572876161,4.89087338711725));
#14668=CARTESIAN_POINT('Ctrl Pts',(5.80280733675431,-1.1673634862472,4.88308510884167));
#14669=CARTESIAN_POINT('Ctrl Pts',(5.76787794556166,-1.3292420599192,4.87529683056608));
#14670=CARTESIAN_POINT('Ctrl Pts',(5.72623407688394,-1.48935350378381,4.8675085522905));
#14671=CARTESIAN_POINT('Ctrl Pts',(5.68664321061859,-1.64157160846214,4.86010422859445));
#14672=CARTESIAN_POINT('Ctrl Pts',(5.64098402017967,-1.79219236681351,4.85269990489839));
#14673=CARTESIAN_POINT('Ctrl Pts',(5.58940914057945,-1.94073079578464,4.84529558120233));
#14674=CARTESIAN_POINT('Ctrl Pts',(5.53516191532728,-2.0969657240571,4.8375076034408));
#14675=CARTESIAN_POINT('Ctrl Pts',(5.47435027831378,-2.25095269078999,4.82971962567928));
#14676=CARTESIAN_POINT('Ctrl Pts',(5.40718577065045,-2.40213917252422,4.82193164791775));
#14677=CARTESIAN_POINT('Ctrl Pts',(5.34003446810493,-2.55329592970046,4.81414520133939));
#14678=CARTESIAN_POINT('Ctrl Pts',(5.26653291674423,-2.70165300863541,4.80635875476103));
#14679=CARTESIAN_POINT('Ctrl Pts',(5.18694047531005,-2.84667860287921,4.79857230818268));
#14680=CARTESIAN_POINT('Ctrl Pts',(5.10734499760404,-2.99170972952181,4.79078556456897));
#14681=CARTESIAN_POINT('Ctrl Pts',(5.02165831515141,-3.13340883513923,4.78299882095527));
#14682=CARTESIAN_POINT('Ctrl Pts',(4.93018571331,-3.27126877446259,4.77521207734156));
#14683=CARTESIAN_POINT('Ctrl Pts',(4.8387191616968,-3.40911959538244,4.76742584876269));
#14684=CARTESIAN_POINT('Ctrl Pts',(4.74146763330826,-3.54313149193686,4.75963962018381));
#14685=CARTESIAN_POINT('Ctrl Pts',(4.63877978558092,-3.67282625009486,4.75185339160494));
#14686=CARTESIAN_POINT('Ctrl Pts',(4.53606490564644,-3.80255514993217,4.74406511332935));
#14687=CARTESIAN_POINT('Ctrl Pts',(4.42791104371039,-3.92796438855324,4.73627683505376));
#14688=CARTESIAN_POINT('Ctrl Pts',(4.31470776234669,-4.04860809267151,4.72848855677818));
#14689=CARTESIAN_POINT('Ctrl Pts',(4.20708529316667,-4.16330417896707,4.72108423308206));
#14690=CARTESIAN_POINT('Ctrl Pts',(4.0948994550037,-4.27369309251353,4.71367990938594));
#14691=CARTESIAN_POINT('Ctrl Pts',(3.97851640638261,-4.37942208135325,4.70627558568982));
#14692=CARTESIAN_POINT('Ctrl Pts',(3.85610298529545,-4.49062940394276,4.6984876079283));
#14693=CARTESIAN_POINT('Ctrl Pts',(3.72900206037776,-4.59672085508215,4.69069963016678));
#14694=CARTESIAN_POINT('Ctrl Pts',(3.59766383887997,-4.69731257900892,4.68291165240526));
#14695=CARTESIAN_POINT('Ctrl Pts',(3.46635143960298,-4.79788452574001,4.67512520582697));
#14696=CARTESIAN_POINT('Ctrl Pts',(3.33080365953879,-4.89295870857519,4.66733875924867));
#14697=CARTESIAN_POINT('Ctrl Pts',(3.1915027730872,-4.98219234994763,4.65955231267038));
#14698=CARTESIAN_POINT('Ctrl Pts',(3.05219657262047,-5.07142939538256,4.65176556905668));
#14699=CARTESIAN_POINT('Ctrl Pts',(2.90913724621,-5.15482527783159,4.64397882544298));
#14700=CARTESIAN_POINT('Ctrl Pts',(2.76283558715538,-5.23208085572536,4.63619208182928));
#14701=CARTESIAN_POINT('Ctrl Pts',(2.61654360486111,-5.30933132374055,4.62840585325042));
#14702=CARTESIAN_POINT('Ctrl Pts',(2.46701000173054,-5.3804421508112,4.62061962467157));
#14703=CARTESIAN_POINT('Ctrl Pts',(2.31476980315181,-5.44516035768613,4.61283339609271));
#14704=CARTESIAN_POINT('Ctrl Pts',(2.1624895278877,-5.50989560139653,4.60504511781715));
#14705=CARTESIAN_POINT('Ctrl Pts',(2.00750152695864,-5.56823473535495,4.59725683954159));
#14706=CARTESIAN_POINT('Ctrl Pts',(1.85036125985648,-5.61997275531851,4.58946856126603));
#14707=CARTESIAN_POINT('Ctrl Pts',(1.70096785579821,-5.66916014098438,4.58206423756979));
#14708=CARTESIAN_POINT('Ctrl Pts',(1.54962953328846,-5.71238150906856,4.57465991387354));
#14709=CARTESIAN_POINT('Ctrl Pts',(1.39683662901192,-5.74950241276153,4.5672555901773));
#14710=CARTESIAN_POINT('Ctrl Pts',(1.23612678035569,-5.78854673123119,4.55946761241577));
#14711=CARTESIAN_POINT('Ctrl Pts',(1.07375012094943,-5.82085557831578,4.55167963465424));
#14712=CARTESIAN_POINT('Ctrl Pts',(0.910285670327234,-5.8463074295573,4.54389165689271));
#14713=CARTESIAN_POINT('Ctrl Pts',(0.746853358215883,-5.87175427674691,
4.5361052103143));
#14714=CARTESIAN_POINT('Ctrl Pts',(0.582333997172172,-5.89034676890564,
4.5283187637359));
#14715=CARTESIAN_POINT('Ctrl Pts',(0.41731509878028,-5.90201479757803,4.52053231715749));
#14716=CARTESIAN_POINT('Ctrl Pts',(0.252289905290521,-5.91368327135933,
4.51274557354375));
#14717=CARTESIAN_POINT('Ctrl Pts',(0.0867654547850066,-5.91842672659838,
4.50495882993001));
#14718=CARTESIAN_POINT('Ctrl Pts',(-0.0786665887883952,-5.91622701815172,
4.49717208631627));
#14719=CARTESIAN_POINT('Ctrl Pts',(-0.244087690269642,-5.91402745519931,
4.48938585773737));
#14720=CARTESIAN_POINT('Ctrl Pts',(-0.409416077502845,-5.90488565192815,
4.48159962915847));
#14721=CARTESIAN_POINT('Ctrl Pts',(-0.574060907248223,-5.88883559265067,
4.47381340057958));
#14722=CARTESIAN_POINT('Ctrl Pts',(-0.738749079153502,-5.87278130825275,
4.46602512230398));
#14723=CARTESIAN_POINT('Ctrl Pts',(-0.902753015560587,-5.84981516303304,
4.45823684402838));
#14724=CARTESIAN_POINT('Ctrl Pts',(-1.06548689623019,-5.82002304432394,
4.45044856575278));
#14725=CARTESIAN_POINT('Ctrl Pts',(-1.22019815411625,-5.79169964822715,
4.44304424205678));
#14726=CARTESIAN_POINT('Ctrl Pts',(-1.37376130562372,-5.75720714155376,
4.43563991836078));
#14727=CARTESIAN_POINT('Ctrl Pts',(-1.52568148163822,-5.71666218864524,
4.42823559466477));
#14728=CARTESIAN_POINT('Ctrl Pts',(-1.68547338173633,-5.67401640429582,
4.42044761690326));
#14729=CARTESIAN_POINT('Ctrl Pts',(-1.84350468551456,-5.62465905280796,
4.41265963914175));
#14730=CARTESIAN_POINT('Ctrl Pts',(-1.99920884614788,-5.56876059388299,
4.40487166138024));
#14731=CARTESIAN_POINT('Ctrl Pts',(-2.1548823940093,-5.51287312507393,4.39708521480188));
#14732=CARTESIAN_POINT('Ctrl Pts',(-2.30822941107405,-5.45044722275815,
4.38929876822352));
#14733=CARTESIAN_POINT('Ctrl Pts',(-2.45870050568853,-5.38170255456644,
4.38151232164515));
#14734=CARTESIAN_POINT('Ctrl Pts',(-2.60917734043562,-5.31295526392082,
4.37372557803143));
#14735=CARTESIAN_POINT('Ctrl Pts',(-2.75677774091444,-5.23788885424812,
4.3659388344177));
#14736=CARTESIAN_POINT('Ctrl Pts',(-2.9009735428508,-5.15677060437825,4.35815209080398));
#14737=CARTESIAN_POINT('Ctrl Pts',(-3.04515980731366,-5.07565771987373,
4.35036586222509));
#14738=CARTESIAN_POINT('Ctrl Pts',(-3.18594164539739,-4.98849395298694,
4.34257963364619));
#14739=CARTESIAN_POINT('Ctrl Pts',(-3.32281656607375,-4.89559195917366,
4.3347934050673));
#14740=CARTESIAN_POINT('Ctrl Pts',(-3.45972751858079,-4.80266550924459,
4.32700512679174));
#14741=CARTESIAN_POINT('Ctrl Pts',(-3.59272923288249,-4.70399799191563,
4.31921684851617));
#14742=CARTESIAN_POINT('Ctrl Pts',(-3.72134847240647,-4.5999452289585,4.31142857024061));
#14743=CARTESIAN_POINT('Ctrl Pts',(-3.84362690793325,-4.50102216648567,
4.3040242465445));
#14744=CARTESIAN_POINT('Ctrl Pts',(-3.96194435858801,-4.39723220845113,
4.29661992284838));
#14745=CARTESIAN_POINT('Ctrl Pts',(-4.07592217450273,-4.28891466339643,
4.28921559915227));
#14746=CARTESIAN_POINT('Ctrl Pts',(-4.19580573606494,-4.1749846588897,4.28142762139076));
#14747=CARTESIAN_POINT('Ctrl Pts',(-4.31093089259036,-4.05600466286206,
4.27363964362924));
#14748=CARTESIAN_POINT('Ctrl Pts',(-4.42088181152369,-3.93239552576276,
4.26585166586773));
#14749=CARTESIAN_POINT('Ctrl Pts',(-4.53081111316369,-3.80881069127959,
4.25806521928942));
#14750=CARTESIAN_POINT('Ctrl Pts',(-4.63556799477428,-3.68059877031486,
4.25027877271111));
#14751=CARTESIAN_POINT('Ctrl Pts',(-4.73477524020605,-3.5482156060803,4.24249232613279));
#14752=CARTESIAN_POINT('Ctrl Pts',(-4.83398627017057,-3.41582739172646,
4.2347055825191));
#14753=CARTESIAN_POINT('Ctrl Pts',(-4.92764704553999,-3.27926786902791,
4.2269188389054));
#14754=CARTESIAN_POINT('Ctrl Pts',(-5.01542177765188,-3.13902452280247,
4.2191320952917));
#14755=CARTESIAN_POINT('Ctrl Pts',(-5.10319070412162,-2.99879045262564,
4.21134586671287));
#14756=CARTESIAN_POINT('Ctrl Pts',(-5.18507419696735,-2.85487331747097,
4.20355963813403));
#14757=CARTESIAN_POINT('Ctrl Pts',(-5.26078072885105,-2.70778815372426,
4.19577340955519));
#14758=CARTESIAN_POINT('Ctrl Pts',(-5.33650719020755,-2.56066427033609,
4.18798513127963));
#14759=CARTESIAN_POINT('Ctrl Pts',(-5.40605329330799,-2.41037097532072,
4.18019685300407));
#14760=CARTESIAN_POINT('Ctrl Pts',(-5.46917385842482,-2.25744720177959,
4.1724085747285));
#14761=CARTESIAN_POINT('Ctrl Pts',(-5.52918264078712,-2.11206242223167,
4.16500425103225));
#14762=CARTESIAN_POINT('Ctrl Pts',(-5.58338406900463,-1.96430052017851,
4.157599927336));
#14763=CARTESIAN_POINT('Ctrl Pts',(-5.6316081057873,-1.81464065460103,4.15019560363975));
#14764=CARTESIAN_POINT('Ctrl Pts',(-5.68244884304267,-1.65686004536271,
4.1423895114768));
#14765=CARTESIAN_POINT('Ctrl Pts',(-5.7266635347264,-1.49691390443455,4.13458341931385));
#14766=CARTESIAN_POINT('Ctrl Pts',(-5.7640878260625,-1.33537339195374,4.12677732715091));
#14767=CARTESIAN_POINT('Ctrl Pts',(-5.80150366642566,-1.17386935777223,
4.11897299772204));
#14768=CARTESIAN_POINT('Ctrl Pts',(-5.83213209537172,-1.01077197874193,
4.11116866829317));
#14769=CARTESIAN_POINT('Ctrl Pts',(-5.85585942190165,-0.846664628661034,
4.1033643388643));
#14770=CARTESIAN_POINT('Ctrl Pts',(-5.87958536060331,-0.68256687733616,
4.09556046591623));
#14771=CARTESIAN_POINT('Ctrl Pts',(-5.89641095468099,-0.517459585638993,
4.08775659296816));
#14772=CARTESIAN_POINT('Ctrl Pts',(-5.90627404008611,-0.351933979469085,
4.07995272002008));
#14773=CARTESIAN_POINT('Ctrl Pts',(-5.91325798996735,-0.234726990979063,
4.07442687741502));
#14774=CARTESIAN_POINT('Ctrl Pts',(-5.91675207616837,-0.117310438061947,
4.06890103480996));
#14775=CARTESIAN_POINT('Ctrl Pts',(-5.9167499990742,0.000104668362501446,
4.0633751922049));
#14776=CARTESIAN_POINT('Ctrl Pts',(-5.91674999969049,6.05192443194444E-5,
3.81162480779512));
#14777=CARTESIAN_POINT('Ctrl Pts',(-5.91675170265655,-0.166432379585355,
3.81945993587964));
#14778=CARTESIAN_POINT('Ctrl Pts',(-5.90972158488872,-0.332919670560517,
3.82729506396416));
#14779=CARTESIAN_POINT('Ctrl Pts',(-5.89568710169516,-0.498802727944986,
3.83513019204868));
#14780=CARTESIAN_POINT('Ctrl Pts',(-5.88165217523655,-0.66469102457914,
3.84296556759785));
#14781=CARTESIAN_POINT('Ctrl Pts',(-5.86061247156367,-0.829974739898137,
3.85080094314702));
#14782=CARTESIAN_POINT('Ctrl Pts',(-5.83264735018096,-0.994060084163459,
3.85863631869618));
#14783=CARTESIAN_POINT('Ctrl Pts',(-5.80467542214537,-1.15818536646322,
3.8664736013596));
#14784=CARTESIAN_POINT('Ctrl Pts',(-5.76977476205297,-1.32111138849058,
3.87431088402302));
#14785=CARTESIAN_POINT('Ctrl Pts',(-5.72807605569632,-1.48225344076459,
3.88214816668644));
#14786=CARTESIAN_POINT('Ctrl Pts',(-5.7132660711512,-1.53948570315986,3.8849317071188));
#14787=CARTESIAN_POINT('Ctrl Pts',(-5.69759902536455,-1.59649303911082,
3.88771524755117));
#14788=CARTESIAN_POINT('Ctrl Pts',(-5.68108230430109,-1.65324965273157,
3.89049878798353));
#14789=CARTESIAN_POINT('Ctrl Pts',(-5.63486991162358,-1.81204987134696,
3.89828689937681));
#14790=CARTESIAN_POINT('Ctrl Pts',(-5.58198681330044,-1.96893960167442,
3.9060750107701));
#14791=CARTESIAN_POINT('Ctrl Pts',(-5.52261612359663,-2.12335623810292,
3.91386312216338));
#14792=CARTESIAN_POINT('Ctrl Pts',(-5.46325709029263,-2.27774255751705,
3.92164970449678));
#14793=CARTESIAN_POINT('Ctrl Pts',(-5.39741312166799,-2.4296564537871,3.92943628683017));
#14794=CARTESIAN_POINT('Ctrl Pts',(-5.32531614323966,-2.57855357459392,
3.93722286916356));
#14795=CARTESIAN_POINT('Ctrl Pts',(-5.25321641576972,-2.72745637281455,
3.9450097483976));
#14796=CARTESIAN_POINT('Ctrl Pts',(-5.17486333709895,-2.87334187610095,
3.95279662763163));
#14797=CARTESIAN_POINT('Ctrl Pts',(-5.09053595632954,-3.01568802096903,
3.96058350686566));
#14798=CARTESIAN_POINT('Ctrl Pts',(-5.00621414111842,-3.15802477107398,
3.96836987217018));
#14799=CARTESIAN_POINT('Ctrl Pts',(-4.915918975838,-3.29682235535044,3.97615623747469));
#14800=CARTESIAN_POINT('Ctrl Pts',(-4.81997429984372,-3.43158539327613,
3.9839426027792));
#14801=CARTESIAN_POINT('Ctrl Pts',(-4.72400443072594,-3.56638381723883,
3.99173101262512));
#14802=CARTESIAN_POINT('Ctrl Pts',(-4.62238227051841,-3.69714531637354,
3.99951942247104));
#14803=CARTESIAN_POINT('Ctrl Pts',(-4.5154741581875,-3.82340472475003,4.00730783231695));
#14804=CARTESIAN_POINT('Ctrl Pts',(-4.41418427659883,-3.94302895386678,
4.01468694596752));
#14805=CARTESIAN_POINT('Ctrl Pts',(-4.30814989558855,-4.05861191050198,
4.02206605961808));
#14806=CARTESIAN_POINT('Ctrl Pts',(-4.19771511701581,-4.16978636849383,
4.02944517326865));
#14807=CARTESIAN_POINT('Ctrl Pts',(-4.08115933567149,-4.28712282702836,
4.0372332846615));
#14808=CARTESIAN_POINT('Ctrl Pts',(-3.95965990039923,-4.39959014137331,
4.04502139605436));
#14809=CARTESIAN_POINT('Ctrl Pts',(-3.83364677837878,-4.50678188302096,
4.05280950744722));
#14810=CARTESIAN_POINT('Ctrl Pts',(-3.70765839683829,-4.61395257943862,
4.06059608978016));
#14811=CARTESIAN_POINT('Ctrl Pts',(-3.57715833998378,-4.71584956291699,
4.0683826721131));
#14812=CARTESIAN_POINT('Ctrl Pts',(-3.44261070425107,-4.81210578660486,
4.07616925444604));
#14813=CARTESIAN_POINT('Ctrl Pts',(-3.30805793824688,-4.90836568052116,
4.08395613367964));
#14814=CARTESIAN_POINT('Ctrl Pts',(-3.16945754210906,-4.99898419515117,
4.09174301291324));
#14815=CARTESIAN_POINT('Ctrl Pts',(-3.02730432880461,-5.08363640156344,
4.09952989214684));
#14816=CARTESIAN_POINT('Ctrl Pts',(-2.88516049752988,-5.16828302097913,
4.10731625745092));
#14817=CARTESIAN_POINT('Ctrl Pts',(-2.73946459294543,-5.246963956779,4.115102622755));
#14818=CARTESIAN_POINT('Ctrl Pts',(-2.59073799329216,-5.31939914018609,
4.12288898805908));
#14819=CARTESIAN_POINT('Ctrl Pts',(-2.441972341054,-5.3918533436014,4.13067739790457));
#14820=CARTESIAN_POINT('Ctrl Pts',(-2.29017469018288,-5.4580583757989,4.13846580775006));
#14821=CARTESIAN_POINT('Ctrl Pts',(-2.13588928307182,-5.51778103343717,
4.14625421759555));
#14822=CARTESIAN_POINT('Ctrl Pts',(-1.98971187630749,-5.57436514843614,
4.15363333124829));
#14823=CARTESIAN_POINT('Ctrl Pts',(-1.84130170356482,-5.62513059398553,
4.16101244490103));
#14824=CARTESIAN_POINT('Ctrl Pts',(-1.691136622487,-5.66991953087372,4.16839155855377));
#14825=CARTESIAN_POINT('Ctrl Pts',(-1.53264843084162,-5.71719095750752,
4.17617966994674));
#14826=CARTESIAN_POINT('Ctrl Pts',(-1.37214867412026,-5.75782145911191,
4.18396778133971));
#14827=CARTESIAN_POINT('Ctrl Pts',(-1.21020936604839,-5.791659852998,4.19175589273268));
#14828=CARTESIAN_POINT('Ctrl Pts',(-1.04830185193705,-5.82549160330525,
4.19954247506573));
#14829=CARTESIAN_POINT('Ctrl Pts',(-0.884955662987656,-5.85253384133118,
4.20732905739877));
#14830=CARTESIAN_POINT('Ctrl Pts',(-0.720753941031261,-5.87268629495803,
4.21511563973182));
#14831=CARTESIAN_POINT('Ctrl Pts',(-0.556545958099245,-5.89283951699352,
4.22290251896554));
#14832=CARTESIAN_POINT('Ctrl Pts',(-0.391482693540322,-5.90610238611409,
4.23068939819926));
#14833=CARTESIAN_POINT('Ctrl Pts',(-0.22615411137466,-5.9124263107804,4.23847627743298));
#14834=CARTESIAN_POINT('Ctrl Pts',(-0.0608364408003028,-5.91874981807133,
4.24626264273715));
#14835=CARTESIAN_POINT('Ctrl Pts',(0.104746193014632,-5.91813528527265,
4.25404900804133));
#14836=CARTESIAN_POINT('Ctrl Pts',(0.270001961156384,-5.91058622333451,
4.2618353733455));
#14837=CARTESIAN_POINT('Ctrl Pts',(0.435301122107437,-5.90303517916598,
4.2696237831911));
#14838=CARTESIAN_POINT('Ctrl Pts',(0.600272926388305,-5.8885459800386,4.2774121930367));
#14839=CARTESIAN_POINT('Ctrl Pts',(0.764327889628312,-5.8671742295279,4.28520060288231));
#14840=CARTESIAN_POINT('Ctrl Pts',(0.919761443197456,-5.84692560636975,
4.2925797165345));
#14841=CARTESIAN_POINT('Ctrl Pts',(1.07437178288583,-5.82049924276928,4.2999588301867));
#14842=CARTESIAN_POINT('Ctrl Pts',(1.22766377514444,-5.78798516045939,4.30733794383889));
#14843=CARTESIAN_POINT('Ctrl Pts',(1.3894521914279,-5.75366893945971,4.31512605523189));
#14844=CARTESIAN_POINT('Ctrl Pts',(1.54982975620371,-5.71255876693495,4.32291416662489));
#14845=CARTESIAN_POINT('Ctrl Pts',(1.70822184003281,-5.66479555745262,4.33070227801789));
#14846=CARTESIAN_POINT('Ctrl Pts',(1.86658282633796,-5.61704172544368,4.338488860351));
#14847=CARTESIAN_POINT('Ctrl Pts',(2.02295880375937,-5.56263755494402,4.34627544268412));
#14848=CARTESIAN_POINT('Ctrl Pts',(2.17678972842697,-5.50177399033392,4.35406202501724));
#14849=CARTESIAN_POINT('Ctrl Pts',(2.33062651863303,-5.44090810500983,4.36184890425099));
#14850=CARTESIAN_POINT('Ctrl Pts',(2.48191776334469,-5.37358244661775,4.36963578348473));
#14851=CARTESIAN_POINT('Ctrl Pts',(2.63012215378309,-5.30003660540938,4.37742266271847));
#14852=CARTESIAN_POINT('Ctrl Pts',(2.77831676281692,-5.22649561818426,4.38520902802267));
#14853=CARTESIAN_POINT('Ctrl Pts',(2.92342463908043,-5.14673541182737,4.39299539332686));
#14854=CARTESIAN_POINT('Ctrl Pts',(3.06492776385741,-5.06104222120662,4.40078175863105));
#14855=CARTESIAN_POINT('Ctrl Pts',(3.20646804448182,-4.97532652929395,4.40857016847668));
#14856=CARTESIAN_POINT('Ctrl Pts',(3.34440140774417,-4.88367490411294,4.4163585783223));
#14857=CARTESIAN_POINT('Ctrl Pts',(3.47823681667403,-4.78641820254283,4.42414698816793));
#14858=CARTESIAN_POINT('Ctrl Pts',(3.60503891270324,-4.69427253114999,4.43152610181996));
#14859=CARTESIAN_POINT('Ctrl Pts',(3.72816247695504,-4.59709589940894,4.43890521547199));
#14860=CARTESIAN_POINT('Ctrl Pts',(3.84721579092943,-4.49520424680829,4.44628432912403));
#14861=CARTESIAN_POINT('Ctrl Pts',(3.97286780208609,-4.38766510621703,4.45407244051697));
#14862=CARTESIAN_POINT('Ctrl Pts',(4.09403044633948,-4.27483504282268,4.46186055190991));
#14863=CARTESIAN_POINT('Ctrl Pts',(4.21026654696066,-4.15711271991077,4.46964866330286));
#14864=CARTESIAN_POINT('Ctrl Pts',(4.32647982664957,-4.03941350972498,4.47743524563588));
#14865=CARTESIAN_POINT('Ctrl Pts',(4.43776826827729,-3.91682418375546,4.4852218279689));
#14866=CARTESIAN_POINT('Ctrl Pts',(4.54373143906263,-3.78978035935776,4.49300841030193));
#14867=CARTESIAN_POINT('Ctrl Pts',(4.64969865020016,-3.66273169080723,4.50079528953561));
#14868=CARTESIAN_POINT('Ctrl Pts',(4.75033997650185,-3.53122842680167,4.50858216876929));
#14869=CARTESIAN_POINT('Ctrl Pts',(4.84529471079806,-3.39573993821852,4.51636904800297));
#14870=CARTESIAN_POINT('Ctrl Pts',(4.94024317813675,-3.26026039179723,4.52415541330713));
#14871=CARTESIAN_POINT('Ctrl Pts',(5.02950562122506,-3.1207964089004,4.53194177861128));
#14872=CARTESIAN_POINT('Ctrl Pts',(5.11276410085828,-2.97784717732035,4.53972814391544));
#14873=CARTESIAN_POINT('Ctrl Pts',(5.19604444247748,-2.83486041017504,4.547516553761));
#14874=CARTESIAN_POINT('Ctrl Pts',(5.27331750782913,-2.6883868409896,4.55530496360657));
#14875=CARTESIAN_POINT('Ctrl Pts',(5.34431039973913,-2.53895193214448,4.56309337345213));
#14876=CARTESIAN_POINT('Ctrl Pts',(5.4115724761193,-2.39737012047034,4.57047248710447));
#14877=CARTESIAN_POINT('Ctrl Pts',(5.47319736093624,-2.25313044699605,4.57785160075682));
#14878=CARTESIAN_POINT('Ctrl Pts',(5.52899223382608,-2.10669775734226,4.58523071440916));
#14879=CARTESIAN_POINT('Ctrl Pts',(5.58787961592861,-1.95214883015016,4.59301882580214));
#14880=CARTESIAN_POINT('Ctrl Pts',(5.6402934184301,-1.79510169430975,4.60080693719513));
#14881=CARTESIAN_POINT('Ctrl Pts',(5.68604048103982,-1.63611558591575,4.60859504858811));
#14882=CARTESIAN_POINT('Ctrl Pts',(5.73177856201124,-1.47716069167274,4.61638163092118));
#14883=CARTESIAN_POINT('Ctrl Pts',(5.77085242642958,-1.31626789133242,4.62416821325426));
#14884=CARTESIAN_POINT('Ctrl Pts',(5.80311885983356,-1.15401129160161,4.63195479558733));
#14885=CARTESIAN_POINT('Ctrl Pts',(5.83538652354945,-0.991748505062883,
4.63974167482105));
#14886=CARTESIAN_POINT('Ctrl Pts',(5.86084617066828,-0.828122127688309,
4.64752855405476));
#14887=CARTESIAN_POINT('Ctrl Pts',(5.87940561957024,-0.663716899789279,
4.65531543328848));
#14888=CARTESIAN_POINT('Ctrl Pts',(5.89796384355929,-0.499322522540363,
4.66310179859267));
#14889=CARTESIAN_POINT('Ctrl Pts',(5.90962274494601,-0.334149715183336,
4.67088816389685));
#14890=CARTESIAN_POINT('Ctrl Pts',(5.91434196310038,-0.168788939240627,
4.67867452920103));
#14891=CARTESIAN_POINT('Ctrl Pts',(5.9190624204256,-0.00338474291599597,
4.68646293904664));
#14892=CARTESIAN_POINT('Ctrl Pts',(5.91683954228149,0.162207201066173,4.69425134889224));
#14893=CARTESIAN_POINT('Ctrl Pts',(5.90768509116275,0.327394908563692,4.70203975873784));
#14894=CARTESIAN_POINT('Ctrl Pts',(5.89901172438219,0.483901678459688,4.70941887238999));
#14895=CARTESIAN_POINT('Ctrl Pts',(5.88411659620163,0.64004534623984,4.71679798604213));
#14896=CARTESIAN_POINT('Ctrl Pts',(5.86305278519524,0.795325468292249,4.72417709969428));
#14897=CARTESIAN_POINT('Ctrl Pts',(5.84082148287208,0.959212209256606,4.73196521108723));
#14898=CARTESIAN_POINT('Ctrl Pts',(5.81171035141862,1.12219549549672,4.73975332248018));
#14899=CARTESIAN_POINT('Ctrl Pts',(5.77581733064287,1.28369183433777,4.74754143387314));
#14900=CARTESIAN_POINT('Ctrl Pts',(5.73993135683605,1.44515646618796,4.75532801620618));
#14901=CARTESIAN_POINT('Ctrl Pts',(5.69726621973851,1.6051344214137,4.76311459853923));
#14902=CARTESIAN_POINT('Ctrl Pts',(5.64797083235644,1.76305304496234,4.77090118087228));
#14903=CARTESIAN_POINT('Ctrl Pts',(5.59867356535214,1.92097768991315,4.77868806010599));
#14904=CARTESIAN_POINT('Ctrl Pts',(5.54274563362964,2.07684253988684,4.7864749393397));
#14905=CARTESIAN_POINT('Ctrl Pts',(5.48038585078946,2.23009001813082,4.79426181857341));
#14906=CARTESIAN_POINT('Ctrl Pts',(5.41803018365886,2.38332738212992,4.80204818387759));
#14907=CARTESIAN_POINT('Ctrl Pts',(5.3492436354497,2.53394742414701,4.80983454918178));
#14908=CARTESIAN_POINT('Ctrl Pts',(5.27427326218566,2.68141233649236,4.81762091448596));
#14909=CARTESIAN_POINT('Ctrl Pts',(5.19928320322401,2.82891597012916,4.82540932433156));
#14910=CARTESIAN_POINT('Ctrl Pts',(5.11810621779466,2.97326253273323,4.83319773417716));
#14911=CARTESIAN_POINT('Ctrl Pts',(5.03103586090187,3.11393781710865,4.84098614402276));
#14912=CARTESIAN_POINT('Ctrl Pts',(4.94854122181793,3.24722033973423,4.84836525767497));
#14913=CARTESIAN_POINT('Ctrl Pts',(4.86075683288408,3.37720730404721,4.85574437132718));
#14914=CARTESIAN_POINT('Ctrl Pts',(4.76796873347935,3.50348465375023,4.8631234849794));
#14915=CARTESIAN_POINT('Ctrl Pts',(4.67003772331103,3.63676110296223,4.87091159637238));
#14916=CARTESIAN_POINT('Ctrl Pts',(4.56649762274021,3.76595265509376,4.87869970776537));
#14917=CARTESIAN_POINT('Ctrl Pts',(4.45771359841966,3.89059378976583,4.88648781915836));
#14918=CARTESIAN_POINT('Ctrl Pts',(4.34895093194651,4.01521045332322,4.8942744014914));
#14919=CARTESIAN_POINT('Ctrl Pts',(4.23494660596614,4.13527824142421,4.90206098382444));
#14920=CARTESIAN_POINT('Ctrl Pts',(4.11610536275955,4.25036553782873,4.90984756615748));
#14921=CARTESIAN_POINT('Ctrl Pts',(3.99725958816233,4.3654572224867,4.9176344453912));
#14922=CARTESIAN_POINT('Ctrl Pts',(3.87357675407428,4.47556781033418,4.92542132462493));
#14923=CARTESIAN_POINT('Ctrl Pts',(3.74549820763692,4.58030279993459,4.93320820385865));
#14924=CARTESIAN_POINT('Ctrl Pts',(3.61742811430956,4.68503087708625,4.94099456916284));
#14925=CARTESIAN_POINT('Ctrl Pts',(3.48496313664534,4.78438386377635,4.94878093446704));
#14926=CARTESIAN_POINT('Ctrl Pts',(3.34857752634194,4.87800769911013,4.95656729977124));
#14927=CARTESIAN_POINT('Ctrl Pts',(3.21215610394682,4.97165611816187,4.96435570961684));
#14928=CARTESIAN_POINT('Ctrl Pts',(3.07181225430668,5.05957219727864,4.97214411946245));
#14929=CARTESIAN_POINT('Ctrl Pts',(2.92804976962699,5.14144484645001,4.97993252930806));
#14930=CARTESIAN_POINT('Ctrl Pts',(2.79184228512156,5.21901492753392,4.98731164296022));
#14931=CARTESIAN_POINT('Ctrl Pts',(2.65256646183692,5.29116030077305,4.99469075661238));
#14932=CARTESIAN_POINT('Ctrl Pts',(2.51067157661488,5.35765422520697,5.00206987026453));
#14933=CARTESIAN_POINT('Ctrl Pts',(2.360911968037,5.42783366881729,5.00985798165748));
#14934=CARTESIAN_POINT('Ctrl Pts',(2.20818124795279,5.4917424844114,5.01764609305043));
#14935=CARTESIAN_POINT('Ctrl Pts',(2.05302279890085,5.54914659652215,5.02543420444338));
#14936=CARTESIAN_POINT('Ctrl Pts',(1.89789481250508,5.60653943833637,5.03322078677644));
#14937=CARTESIAN_POINT('Ctrl Pts',(1.74034034767591,5.65743001402864,5.04100736910951));
#14938=CARTESIAN_POINT('Ctrl Pts',(1.5809213182788,5.70163295450625,5.04879395144258));
#14939=CARTESIAN_POINT('Ctrl Pts',(1.42149621026995,5.74583758043203,5.05658083067628));
#14940=CARTESIAN_POINT('Ctrl Pts',(1.26020670227525,5.78335397171438,5.06436770990998));
#14941=CARTESIAN_POINT('Ctrl Pts',(1.09762909469295,5.8140468636728,5.07215458914368));
#14942=CARTESIAN_POINT('Ctrl Pts',(0.935062217138572,5.84473772991813,5.07994095444787));
#14943=CARTESIAN_POINT('Ctrl Pts',(0.771207724150727,5.86860593888792,5.08772731975205));
#14944=CARTESIAN_POINT('Ctrl Pts',(0.606651462188195,5.88556748036457,5.09551368505623));
#14945=CARTESIAN_POINT('Ctrl Pts',(0.442051991092846,5.90253347559757,5.10330209490183));
#14946=CARTESIAN_POINT('Ctrl Pts',(0.276750700666946,5.912589144771,5.11109050474743));
#14947=CARTESIAN_POINT('Ctrl Pts',(0.111338818777101,5.91570234460232,5.11887891459302));
#14948=CARTESIAN_POINT('Ctrl Pts',(-0.0453803447093223,5.91865193968433,
5.12625802824523));
#14949=CARTESIAN_POINT('Ctrl Pts',(-0.202198514988835,5.91536997350762,
5.13363714189745));
#14950=CARTESIAN_POINT('Ctrl Pts',(-0.358612690940003,5.90587228954341,
5.14101625554966));
#14951=CARTESIAN_POINT('Ctrl Pts',(-0.523696342332037,5.89584818310266,
5.14880436694261));
#14952=CARTESIAN_POINT('Ctrl Pts',(-0.688388904989159,5.87889621054729,
5.15659247833555));
#14953=CARTESIAN_POINT('Ctrl Pts',(-0.852101232342855,5.85507079823462,
5.1643805897285));
#14954=CARTESIAN_POINT('Ctrl Pts',(-1.01578141763601,5.83125006362617,5.17216717206159));
#14955=CARTESIAN_POINT('Ctrl Pts',(-1.17848143562264,5.80055862786281,5.17995375439468));
#14956=CARTESIAN_POINT('Ctrl Pts',(-1.3396191698002,5.76310255352131,5.18774033672778));
#14957=CARTESIAN_POINT('Ctrl Pts',(-1.50076304812304,5.72564505098818,5.19552721596149));
#14958=CARTESIAN_POINT('Ctrl Pts',(-1.66034421132565,5.68142246224671,5.2033140951952));
#14959=CARTESIAN_POINT('Ctrl Pts',(-1.81779188148033,5.63059173072637,5.21110097442891));
#14960=CARTESIAN_POINT('Ctrl Pts',(-1.97522916017909,5.57976435400516,5.21888733973306));
#14961=CARTESIAN_POINT('Ctrl Pts',(-2.13053292354879,5.52232980556348,5.2266737050372));
#14962=CARTESIAN_POINT('Ctrl Pts',(-2.28314853299054,5.45849460371659,5.23446007034135));
#14963=CARTESIAN_POINT('Ctrl Pts',(-2.43580421619259,5.39464264004182,5.24224848018693));
#14964=CARTESIAN_POINT('Ctrl Pts',(-2.58577003929812,5.3243867861991,5.25003689003252));
#14965=CARTESIAN_POINT('Ctrl Pts',(-2.73251145314194,5.2479816806986,5.2578252998781));
#14966=CARTESIAN_POINT('Ctrl Pts',(-2.87154131825056,5.1755918131548,5.26520441353032));
#14967=CARTESIAN_POINT('Ctrl Pts',(-3.0076767248299,5.09768250108378,5.27258352718255));
#14968=CARTESIAN_POINT('Ctrl Pts',(-3.1404835561888,5.0145083104735,5.27996264083478));
#14969=CARTESIAN_POINT('Ctrl Pts',(-3.28065139275001,4.92672407350102,5.28775075222776));
#14970=CARTESIAN_POINT('Ctrl Pts',(-3.41716126991424,4.83304342979636,5.29553886362074));
#14971=CARTESIAN_POINT('Ctrl Pts',(-3.54952188412015,4.73379604088011,5.30332697501372));
#14972=CARTESIAN_POINT('Ctrl Pts',(-3.6818565116268,4.63456813745856,5.31111355734679));
#14973=CARTESIAN_POINT('Ctrl Pts',(-3.81004324612876,4.52977586112265,5.31890013967987));
#14974=CARTESIAN_POINT('Ctrl Pts',(-3.93362166191435,4.41979085290449,5.32668672201294));
#14975=CARTESIAN_POINT('Ctrl Pts',(-4.05720478971704,4.30980165098279,5.33447360124664));
#14976=CARTESIAN_POINT('Ctrl Pts',(-4.17617900589712,4.194619530459,5.34226048048034));
#14977=CARTESIAN_POINT('Ctrl Pts',(-4.29011818459847,4.07465538722939,5.35004735971404));
#14978=CARTESIAN_POINT('Ctrl Pts',(-4.40404984337992,3.95469916156387,5.35783372501822));
#14979=CARTESIAN_POINT('Ctrl Pts',(-4.5129469097056,3.82996177656109,5.36562009032239));
#14980=CARTESIAN_POINT('Ctrl Pts',(-4.616421148406,3.70088993933213,5.37340645562657));
#14981=CARTESIAN_POINT('Ctrl Pts',(-4.71992255734045,3.57178421045952,5.38119486547217));
#14982=CARTESIAN_POINT('Ctrl Pts',(-4.81799809184262,3.43834200337669,5.38898327531777));
#14983=CARTESIAN_POINT('Ctrl Pts',(-4.91030018013144,3.30104266914275,5.39677168516337));
#14984=CARTESIAN_POINT('Ctrl Pts',(-4.99775161287817,3.17095868386651,5.40415079881555));
#14985=CARTESIAN_POINT('Ctrl Pts',(-5.08002065862202,3.03741275939119,5.41152991246773));
#14986=CARTESIAN_POINT('Ctrl Pts',(-5.15684790293272,2.90083613265528,5.4189090261199));
#14987=CARTESIAN_POINT('Ctrl Pts',(-5.23793340519082,2.75668955451155,5.42669713751287));
#14988=CARTESIAN_POINT('Ctrl Pts',(-5.31298572089407,2.60911530379078,5.43448524890584));
#14989=CARTESIAN_POINT('Ctrl Pts',(-5.38173114686707,2.45863792074817,5.44227336029881));
#14990=CARTESIAN_POINT('Ctrl Pts',(-5.45046307587361,2.30819008131754,5.45005994263181));
#14991=CARTESIAN_POINT('Ctrl Pts',(-5.51289045312819,2.15484053729931,5.45784652496482));
#14992=CARTESIAN_POINT('Ctrl Pts',(-5.56878677447868,1.99913591906386,5.46563310729783));
#14993=CARTESIAN_POINT('Ctrl Pts',(-5.62468522714398,1.84342536384454,5.47341998653156));
#14994=CARTESIAN_POINT('Ctrl Pts',(-5.67405201392717,1.68535985411224,5.48120686576529));
#14995=CARTESIAN_POINT('Ctrl Pts',(-5.71670953107353,1.52550408056912,5.48899374499902));
#14996=CARTESIAN_POINT('Ctrl Pts',(-5.75936423284837,1.36565885741484,5.49678011030321));
#14997=CARTESIAN_POINT('Ctrl Pts',(-5.79531046883721,1.20402391567871,5.5045664756074));
#14998=CARTESIAN_POINT('Ctrl Pts',(-5.82442104131012,1.04117726446746,5.5123528409116));
#14999=CARTESIAN_POINT('Ctrl Pts',(-5.85353925762824,0.878287853032396,
5.52014125075721));
#15000=CARTESIAN_POINT('Ctrl Pts',(-5.87581816565748,0.714186410759292,
5.52792966060282));
#15001=CARTESIAN_POINT('Ctrl Pts',(-5.89118189313341,0.549460157351797,
5.53571807044843));
#15002=CARTESIAN_POINT('Ctrl Pts',(-5.90573822663585,0.393390591228442,
5.54309718410063));
#15003=CARTESIAN_POINT('Ctrl Pts',(-5.91408747402153,0.236760453962896,
5.55047629775283));
#15004=CARTESIAN_POINT('Ctrl Pts',(-5.91620815651611,0.0800725375658166,
5.55785541140503));
#15005=CARTESIAN_POINT('Ctrl Pts',(-5.91656925195911,0.0533927810586914,
5.5591118768684));
#15006=CARTESIAN_POINT('Ctrl Pts',(-5.91674987283727,0.0267105792375199,
5.56036834233176));
#15007=CARTESIAN_POINT('Ctrl Pts',(-5.91674999993288,2.81831104758398E-5,
5.56162480779512));
#15008=CARTESIAN_POINT('Origin',(0.,0.,0.));
#15009=CARTESIAN_POINT('',(-5.91674999981411,-4.69009224444681E-5,7.56337519225006));
#15010=CARTESIAN_POINT('',(-5.91674999911038,-0.000102602491467883,7.31162480779513));
#15011=CARTESIAN_POINT('',(-5.91675,-7.2459289488551E-16,0.));
#15012=CARTESIAN_POINT('Ctrl Pts',(-5.91674999981412,-4.68999629195391E-5,
7.5633751922049));
#15013=CARTESIAN_POINT('Ctrl Pts',(-5.91675132125532,0.166661914366294,
7.55552998692111));
#15014=CARTESIAN_POINT('Ctrl Pts',(-5.90970258340904,0.333362748204337,
7.54768478163732));
#15015=CARTESIAN_POINT('Ctrl Pts',(-5.89563183882621,0.499455487024331,
7.53983957635354));
#15016=CARTESIAN_POINT('Ctrl Pts',(-5.88156043435222,0.665556015277763,
7.53199400314455));
#15017=CARTESIAN_POINT('Ctrl Pts',(-5.86046639555703,0.831048083761738,
7.52414842993556));
#15018=CARTESIAN_POINT('Ctrl Pts',(-5.83242967323381,0.995336460339776,
7.51630285672658));
#15019=CARTESIAN_POINT('Ctrl Pts',(-5.80438623858568,1.15966416950993,7.50845540519401));
#15020=CARTESIAN_POINT('Ctrl Pts',(-5.76939685314964,1.32278730643484,7.50060795366145));
#15021=CARTESIAN_POINT('Ctrl Pts',(-5.7275927811386,1.48411977142985,7.49276050212888));
#15022=CARTESIAN_POINT('Ctrl Pts',(-5.71678765814867,1.52581946819813,7.49073216673264));
#15023=CARTESIAN_POINT('Ctrl Pts',(-5.70552752957678,1.56739959843692,7.48870383133641));
#15024=CARTESIAN_POINT('Ctrl Pts',(-5.69381521029775,1.60885018366597,7.48667549594017));
#15025=CARTESIAN_POINT('Ctrl Pts',(-5.64884469790125,1.76800346599001,7.47888751817866));
#15026=CARTESIAN_POINT('Ctrl Pts',(-5.59718899536415,1.92529850569285,7.47109954041715));
#15027=CARTESIAN_POINT('Ctrl Pts',(-5.53902680273251,2.08017130090548,7.46331156265564));
#15028=CARTESIAN_POINT('Ctrl Pts',(-5.4808760452867,2.23501364679852,7.45552511607734));
#15029=CARTESIAN_POINT('Ctrl Pts',(-5.41622146246665,2.38743439946199,7.44773866949905));
#15030=CARTESIAN_POINT('Ctrl Pts',(-5.34529070695169,2.53688742767114,7.43995222292075));
#15031=CARTESIAN_POINT('Ctrl Pts',(-5.27435724558821,2.68634615717662,7.43216547930705));
#15032=CARTESIAN_POINT('Ctrl Pts',(-5.19714726587681,2.83283664531632,7.42437873569336));
#15033=CARTESIAN_POINT('Ctrl Pts',(-5.1139357172095,2.97583468000979,7.41659199207966));
#15034=CARTESIAN_POINT('Ctrl Pts',(-5.03072967236351,3.11882325645324,7.40880576350079));
#15035=CARTESIAN_POINT('Ctrl Pts',(-4.94152301376513,3.25831956555739,7.40101953492192));
#15036=CARTESIAN_POINT('Ctrl Pts',(-4.8466356883766,3.39382572720732,7.39323330634305));
#15037=CARTESIAN_POINT('Ctrl Pts',(-4.75172338424075,3.52936756036721,7.38544502806749));
#15038=CARTESIAN_POINT('Ctrl Pts',(-4.651127606973,3.66091688411636,7.37765674979194));
#15039=CARTESIAN_POINT('Ctrl Pts',(-4.54521103882801,3.78800569891546,7.36986847151638));
#15040=CARTESIAN_POINT('Ctrl Pts',(-4.4445160549568,3.90882915817717,7.36246414782013));
#15041=CARTESIAN_POINT('Ctrl Pts',(-4.33901243121526,4.02562110951189,7.35505982412388));
#15042=CARTESIAN_POINT('Ctrl Pts',(-4.2290449596083,4.13800788932448,7.34765550042763));
#15043=CARTESIAN_POINT('Ctrl Pts',(-4.11337953782229,4.25621797545483,7.3398675226661));
#15044=CARTESIAN_POINT('Ctrl Pts',(-3.99273402351709,4.36959654925919,7.33207954490457));
#15045=CARTESIAN_POINT('Ctrl Pts',(-3.86753528394729,4.47773395702812,7.32429156714304));
#15046=CARTESIAN_POINT('Ctrl Pts',(-3.74236115952358,4.58585010405514,7.31650512056474));
#15047=CARTESIAN_POINT('Ctrl Pts',(-3.6126358377128,4.68872693236575,7.30871867398644));
#15048=CARTESIAN_POINT('Ctrl Pts',(-3.47882061190941,4.78599391063698,7.30093222740814));
#15049=CARTESIAN_POINT('Ctrl Pts',(-3.34500028135622,4.88326459942459,7.29314548379442));
#15050=CARTESIAN_POINT('Ctrl Pts',(-3.20708999075695,4.97492481887361,7.2853587401807));
#15051=CARTESIAN_POINT('Ctrl Pts',(-3.06558206786894,5.06064592198075,7.27757199656698));
#15052=CARTESIAN_POINT('Ctrl Pts',(-2.92408350467152,5.14636135527814,7.26978576798811));
#15053=CARTESIAN_POINT('Ctrl Pts',(-2.77898805876728,5.22613829285959,7.26199953940923));
#15054=CARTESIAN_POINT('Ctrl Pts',(-2.63081496136454,5.29969274595806,7.25421331083036));
#15055=CARTESIAN_POINT('Ctrl Pts',(-2.48260285792614,5.3732665620021,7.24642503255478));
#15056=CARTESIAN_POINT('Ctrl Pts',(-2.33131176962279,5.44061447646983,7.2386367542792));
#15057=CARTESIAN_POINT('Ctrl Pts',(-2.17748414623837,5.50149919161864,7.23084847600361));
#15058=CARTESIAN_POINT('Ctrl Pts',(-2.03124007577153,5.55938234925103,7.22344415230745));
#15059=CARTESIAN_POINT('Ctrl Pts',(-1.88270378816617,5.61142411885008,7.21603982861129));
#15060=CARTESIAN_POINT('Ctrl Pts',(-1.73235687009803,5.65746146580992,7.20863550491513));
#15061=CARTESIAN_POINT('Ctrl Pts',(-1.57421974610455,5.7058842318903,7.20084752715361));
#15062=CARTESIAN_POINT('Ctrl Pts',(-1.41402280613875,5.7476811402137,7.1930595493921));
#15063=CARTESIAN_POINT('Ctrl Pts',(-1.25233692593782,5.78269684372548,7.18527157163058));
#15064=CARTESIAN_POINT('Ctrl Pts',(-1.09068283456665,5.81770566284985,7.17748512505223));
#15065=CARTESIAN_POINT('Ctrl Pts',(-0.927540699178164,5.84593586978058,
7.16969867847388));
#15066=CARTESIAN_POINT('Ctrl Pts',(-0.76349289492658,5.86728294544388,7.16191223189554));
#15067=CARTESIAN_POINT('Ctrl Pts',(-0.59943883262148,5.88863083544994,7.15412548828183));
#15068=CARTESIAN_POINT('Ctrl Pts',(-0.434479348676863,5.90309502361526,
7.14633874466812));
#15069=CARTESIAN_POINT('Ctrl Pts',(-0.269204017649051,5.91062262028135,
7.13855200105441));
#15070=CARTESIAN_POINT('Ctrl Pts',(-0.103939618347989,5.91814971905324,
7.13076577247554));
#15071=CARTESIAN_POINT('Ctrl Pts',(0.0616402669794469,5.91874113003358,
7.12297954389666));
#15072=CARTESIAN_POINT('Ctrl Pts',(0.226943819083687,5.91239605113525,7.11519331531779));
#15073=CARTESIAN_POINT('Ctrl Pts',(0.392290886754298,5.90604930191769,7.10740503704221));
#15074=CARTESIAN_POINT('Ctrl Pts',(0.557361156241647,5.89276242438704,7.09961675876663));
#15075=CARTESIAN_POINT('Ctrl Pts',(0.721564771939402,5.8725867249787,7.09182848049105));
#15076=CARTESIAN_POINT('Ctrl Pts',(0.87767330834284,5.85340566801983,7.08442415679491));
#15077=CARTESIAN_POINT('Ctrl Pts',(1.03299832143993,5.82799868423886,7.07701983309876));
#15078=CARTESIAN_POINT('Ctrl Pts',(1.1870389405482,5.796453149653,7.06961550940262));
#15079=CARTESIAN_POINT('Ctrl Pts',(1.34906115421956,5.76327308731208,7.06182753164108));
#15080=CARTESIAN_POINT('Ctrl Pts',(1.50972029718412,5.72328957943936,7.05403955387955));
#15081=CARTESIAN_POINT('Ctrl Pts',(1.66844078306887,5.67663949145025,7.04625157611801));
#15082=CARTESIAN_POINT('Ctrl Pts',(1.8271300631457,5.62999857526827,7.03846512953965));
#15083=CARTESIAN_POINT('Ctrl Pts',(1.98388114026828,5.57669378426923,7.0306786829613));
#15084=CARTESIAN_POINT('Ctrl Pts',(2.13813266131111,5.5169121150454,7.02289223638294));
#15085=CARTESIAN_POINT('Ctrl Pts',(2.29239006670133,5.45712816528581,7.01510549276922));
#15086=CARTESIAN_POINT('Ctrl Pts',(2.44414742583559,5.390866954678,7.0073187491555));
#15087=CARTESIAN_POINT('Ctrl Pts',(2.59286177785379,5.31836425637102,6.99953200554178));
#15088=CARTESIAN_POINT('Ctrl Pts',(2.74156629353028,5.24586635357508,6.99174577696289));
#15089=CARTESIAN_POINT('Ctrl Pts',(2.88722791765946,5.16712792935809,6.98395954838401));
#15090=CARTESIAN_POINT('Ctrl Pts',(3.02932665116721,5.082431564028,6.97617331980512));
#15091=CARTESIAN_POINT('Ctrl Pts',(3.17146279165612,4.99771290268396,6.96838504152952));
#15092=CARTESIAN_POINT('Ctrl Pts',(3.3100338916907,4.90703332825587,6.96059676325393));
#15093=CARTESIAN_POINT('Ctrl Pts',(3.44454661891554,4.81072023221238,6.95280848497833));
#15094=CARTESIAN_POINT('Ctrl Pts',(3.57242799890372,4.7191552785676,6.94540416128225));
#15095=CARTESIAN_POINT('Ctrl Pts',(3.69664130054661,4.62249903090095,6.93799983758617));
#15096=CARTESIAN_POINT('Ctrl Pts',(3.8167885852575,4.52106795546673,6.93059551389009));
#15097=CARTESIAN_POINT('Ctrl Pts',(3.94316128583654,4.414381242104,6.92280753612858));
#15098=CARTESIAN_POINT('Ctrl Pts',(4.06508062823147,4.30237358580423,6.91501955836706));
#15099=CARTESIAN_POINT('Ctrl Pts',(4.18210676270983,4.1854406682925,6.90723158060554));
#15100=CARTESIAN_POINT('Ctrl Pts',(4.29910988884662,4.06853074079507,6.89944513402724));
#15101=CARTESIAN_POINT('Ctrl Pts',(4.41122150072586,3.94669770995357,6.89165868744893));
#15102=CARTESIAN_POINT('Ctrl Pts',(4.5180382415108,3.82037445949294,6.88387224087063));
#15103=CARTESIAN_POINT('Ctrl Pts',(4.62485905711387,3.69404639008477,6.87608549725692));
#15104=CARTESIAN_POINT('Ctrl Pts',(4.72638438810034,3.56322799974676,6.86829875364321));
#15105=CARTESIAN_POINT('Ctrl Pts',(4.82225037371936,3.42838619406617,6.8605120100295));
#15106=CARTESIAN_POINT('Ctrl Pts',(4.91811001852061,3.29355330716227,6.85272578145063));
#15107=CARTESIAN_POINT('Ctrl Pts',(5.00831088194913,3.15469779798549,6.84493955287175));
#15108=CARTESIAN_POINT('Ctrl Pts',(5.09253166867592,3.01231667758104,6.83715332429288));
#15109=CARTESIAN_POINT('Ctrl Pts',(5.17677462622219,2.86989807585825,6.82936504601731));
#15110=CARTESIAN_POINT('Ctrl Pts',(5.25503419693593,2.72395228258291,6.82157676774175));
#15111=CARTESIAN_POINT('Ctrl Pts',(5.32703394840831,2.57500288834894,6.81378848946618));
#15112=CARTESIAN_POINT('Ctrl Pts',(5.39548418183408,2.43339655505688,6.80638416576998));
#15113=CARTESIAN_POINT('Ctrl Pts',(5.45827681976575,2.28907587344672,6.79897984207378));
#15114=CARTESIAN_POINT('Ctrl Pts',(5.51521395563209,2.14250917993389,6.79157551837758));
#15115=CARTESIAN_POINT('Ctrl Pts',(5.57510128175738,1.98834815233828,6.78378754061606));
#15116=CARTESIAN_POINT('Ctrl Pts',(5.62853161412413,1.83164703331563,6.77599956285455));
#15117=CARTESIAN_POINT('Ctrl Pts',(5.67530816618571,1.67296377167165,6.76821158509303));
#15118=CARTESIAN_POINT('Ctrl Pts',(5.72207552157626,1.51431170851687,6.76042513851469));
#15119=CARTESIAN_POINT('Ctrl Pts',(5.76219161658887,1.35367858664164,6.75263869193635));
#15120=CARTESIAN_POINT('Ctrl Pts',(5.79550951268791,1.19163755011494,6.74485224535801));
#15121=CARTESIAN_POINT('Ctrl Pts',(5.82882867978955,1.02959033208814,6.73706550174429));
#15122=CARTESIAN_POINT('Ctrl Pts',(5.85534906081321,0.866135404132536,6.72927875813057));
#15123=CARTESIAN_POINT('Ctrl Pts',(5.87497467979639,0.701856875902259,6.72149201451685));
#15124=CARTESIAN_POINT('Ctrl Pts',(5.89459900069162,0.537589213468304,6.713705785938));
#15125=CARTESIAN_POINT('Ctrl Pts',(5.90732943434829,0.372498377106149,6.70591955735915));
#15126=CARTESIAN_POINT('Ctrl Pts',(5.91312178758799,0.207174534275467,6.6981333287803));
#15127=CARTESIAN_POINT('Ctrl Pts',(5.91891566564388,0.041807170536806,6.69034505050474));
#15128=CARTESIAN_POINT('Ctrl Pts',(5.91776780055012,-0.123793002738391,
6.68255677222917));
#15129=CARTESIAN_POINT('Ctrl Pts',(5.90968611136997,-0.289033955757698,
6.67476849395361));
#15130=CARTESIAN_POINT('Ctrl Pts',(5.90200284164276,-0.446128689757979,
6.66736417025743));
#15131=CARTESIAN_POINT('Ctrl Pts',(5.8880529538693,-0.602898505570204,6.65995984656125));
#15132=CARTESIAN_POINT('Ctrl Pts',(5.86788686414186,-0.75883747412171,6.65255552286507));
#15133=CARTESIAN_POINT('Ctrl Pts',(5.84667587110872,-0.922856399964292,
6.64476754510352));
#15134=CARTESIAN_POINT('Ctrl Pts',(5.81857980235061,-1.08601476487503,6.63697956734197));
#15135=CARTESIAN_POINT('Ctrl Pts',(5.78369295186044,-1.24772849654879,6.62919158958042));
#15136=CARTESIAN_POINT('Ctrl Pts',(5.74881296042417,-1.40941043391649,6.62140514300207));
#15137=CARTESIAN_POINT('Ctrl Pts',(5.70714491857074,-1.56964799259304,6.61361869642372));
#15138=CARTESIAN_POINT('Ctrl Pts',(5.65883416014089,-1.72786761950172,6.60583224984536));
#15139=CARTESIAN_POINT('Ctrl Pts',(5.61052155876456,-1.88609328213233,6.59804550623163));
#15140=CARTESIAN_POINT('Ctrl Pts',(5.55556582327765,-2.04230055219289,6.5902587626179));
#15141=CARTESIAN_POINT('Ctrl Pts',(5.49416228134141,-2.19593064298156,6.58247201900417));
#15142=CARTESIAN_POINT('Ctrl Pts',(5.43276280078999,-2.3495505722893,6.57468579042527));
#15143=CARTESIAN_POINT('Ctrl Pts',(5.36491648594019,-2.50059336673357,6.56689956184636));
#15144=CARTESIAN_POINT('Ctrl Pts',(5.29086702922229,-2.6485197076081,6.55911333326745));
#15145=CARTESIAN_POINT('Ctrl Pts',(5.21679807925105,-2.79648498956021,6.55132505499186));
#15146=CARTESIAN_POINT('Ctrl Pts',(5.13652286581074,-2.94133189180655,6.54353677671626));
#15147=CARTESIAN_POINT('Ctrl Pts',(5.05033172712747,-3.08254440494694,6.53574849844067));
#15148=CARTESIAN_POINT('Ctrl Pts',(4.96838972814401,-3.21679527789017,6.52834417474462));
#15149=CARTESIAN_POINT('Ctrl Pts',(4.88110118910696,-3.34776124854887,6.52093985104858));
#15150=CARTESIAN_POINT('Ctrl Pts',(4.78875254687753,-3.47502224557973,6.51353552735253));
#15151=CARTESIAN_POINT('Ctrl Pts',(4.6916188718097,-3.60887725455423,6.50574754959102));
#15152=CARTESIAN_POINT('Ctrl Pts',(4.58885204778303,-3.7386810333868,6.49795957182951));
#15153=CARTESIAN_POINT('Ctrl Pts',(4.48081444090749,-3.86396590417862,6.490171594068));
#15154=CARTESIAN_POINT('Ctrl Pts',(4.37279807515156,-3.9892261428909,6.48238514748967));
#15155=CARTESIAN_POINT('Ctrl Pts',(4.25951320278849,-4.1099690044439,6.47459870091135));
#15156=CARTESIAN_POINT('Ctrl Pts',(4.14136196751739,-4.22576047789039,6.46681225433302));
#15157=CARTESIAN_POINT('Ctrl Pts',(4.023206225043,-4.3415563685206,6.45902551071931));
#15158=CARTESIAN_POINT('Ctrl Pts',(3.90018397363803,-4.45240026660171,6.4512387671056));
#15159=CARTESIAN_POINT('Ctrl Pts',(3.77273418321245,-4.55789505641807,6.44345202349189));
#15160=CARTESIAN_POINT('Ctrl Pts',(3.64529282263673,-4.66338286854356,6.435665794913));
#15161=CARTESIAN_POINT('Ctrl Pts',(3.5134247553285,-4.76352207673162,6.42787956633411));
#15162=CARTESIAN_POINT('Ctrl Pts',(3.37760209659498,-4.85795580873038,6.42009333775521));
#15163=CARTESIAN_POINT('Ctrl Pts',(3.24174368303502,-4.95241440006946,6.41230505947965));
#15164=CARTESIAN_POINT('Ctrl Pts',(3.1019288592739,-5.04116432987048,6.40451678120409));
#15165=CARTESIAN_POINT('Ctrl Pts',(2.95865953805417,-5.1238915191855,6.39672850292853));
#15166=CARTESIAN_POINT('Ctrl Pts',(2.82245325567606,-5.20254033815288,6.38932417923236));
#15167=CARTESIAN_POINT('Ctrl Pts',(2.68312510603525,-5.27574581087367,6.3819198555362));
#15168=CARTESIAN_POINT('Ctrl Pts',(2.54112765407703,-5.34327622420786,6.37451553184003));
#15169=CARTESIAN_POINT('Ctrl Pts',(2.39177262268947,-5.41430571708996,6.3667275540785));
#15170=CARTESIAN_POINT('Ctrl Pts',(2.23941089857263,-5.47908184034542,6.35893957631697));
#15171=CARTESIAN_POINT('Ctrl Pts',(2.08458449997768,-5.53736742730269,6.35115159855545));
#15172=CARTESIAN_POINT('Ctrl Pts',(1.92978854157962,-5.59564155481403,6.34336515197709));
#15173=CARTESIAN_POINT('Ctrl Pts',(1.77252917445244,-5.64742757969805,6.33557870539874));
#15174=CARTESIAN_POINT('Ctrl Pts',(1.61336722615573,-5.69253693497605,6.32779225882038));
#15175=CARTESIAN_POINT('Ctrl Pts',(1.45419920619022,-5.73764801107407,6.32000551520668));
#15176=CARTESIAN_POINT('Ctrl Pts',(1.29312876617486,-5.77608181697151,6.31221877159298));
#15177=CARTESIAN_POINT('Ctrl Pts',(1.13073140640612,-5.80769980707223,6.30443202797927));
#15178=CARTESIAN_POINT('Ctrl Pts',(0.968344788007374,-5.83931570587953,
6.29664579940038));
#15179=CARTESIAN_POINT('Ctrl Pts',(0.804631739196146,-5.86411663007676,
6.2888595708215));
#15180=CARTESIAN_POINT('Ctrl Pts',(0.640177598575581,-5.88201523330074,
6.28107334224261));
#15181=CARTESIAN_POINT('Ctrl Pts',(0.475680165993559,-5.8999185482677,6.27328506396704));
#15182=CARTESIAN_POINT('Ctrl Pts',(0.310441569445996,-5.91091587494821,
6.26549678569146));
#15183=CARTESIAN_POINT('Ctrl Pts',(0.145052825819117,-5.91497170240246,
6.25770850741588));
#15184=CARTESIAN_POINT('Ctrl Pts',(-0.0121824128534097,-5.91882758148951,
6.25030418371976));
#15185=CARTESIAN_POINT('Ctrl Pts',(-0.169553087598295,-5.91640988658437,
6.24289986002364));
#15186=CARTESIAN_POINT('Ctrl Pts',(-0.32655093453622,-5.90773180244783,
6.23549553632751));
#15187=CARTESIAN_POINT('Ctrl Pts',(-0.49168360441094,-5.89860406451503,
6.22770755856601));
#15188=CARTESIAN_POINT('Ctrl Pts',(-0.656462855812958,-5.88254668530447,
6.2199195808045));
#15189=CARTESIAN_POINT('Ctrl Pts',(-0.820299274759474,-5.85961087977086,
6.21213160304299));
#15190=CARTESIAN_POINT('Ctrl Pts',(-0.984103482061949,-5.83667958361319,
6.20434515646465));
#15191=CARTESIAN_POINT('Ctrl Pts',(-1.14696491050467,-5.80687260375928,
6.19655870988631));
#15192=CARTESIAN_POINT('Ctrl Pts',(-1.30830089468569,-5.77029282891819,
6.18877226330797));
#15193=CARTESIAN_POINT('Ctrl Pts',(-1.46964303347078,-5.73371165864114,
6.18098551969425));
#15194=CARTESIAN_POINT('Ctrl Pts',(-1.62945929904668,-5.69035724317976,
6.17319877608053));
#15195=CARTESIAN_POINT('Ctrl Pts',(-1.78717808700344,-5.64038341319406,
6.16541203246681));
#15196=CARTESIAN_POINT('Ctrl Pts',(-1.94488644304213,-5.59041288860342,
6.15762580388793));
#15197=CARTESIAN_POINT('Ctrl Pts',(-2.10049729447075,-5.53382392227884,
6.14983957530906));
#15198=CARTESIAN_POINT('Ctrl Pts',(-2.2534549062819,-5.47082000689604,6.14205334673018));
#15199=CARTESIAN_POINT('Ctrl Pts',(-2.40645278363498,-5.40779950595881,
6.1342650684546));
#15200=CARTESIAN_POINT('Ctrl Pts',(-2.55679572930045,-5.33836080153691,
6.12647679017901));
#15201=CARTESIAN_POINT('Ctrl Pts',(-2.70394783468263,-5.26275561562715,
6.11868851190343));
#15202=CARTESIAN_POINT('Ctrl Pts',(-2.84384548372208,-5.19087769219211,
6.11128418820728));
#15203=CARTESIAN_POINT('Ctrl Pts',(-2.98085909025334,-5.11342676486538,
6.10387986451114));
#15204=CARTESIAN_POINT('Ctrl Pts',(-3.11454871155952,-5.03065769913069,
6.09647554081499));
#15205=CARTESIAN_POINT('Ctrl Pts',(-3.25516544313584,-4.94359996506336,
6.08868756305342));
#15206=CARTESIAN_POINT('Ctrl Pts',(-3.39215488172444,-4.85062720111968,
6.08089958529185));
#15207=CARTESIAN_POINT('Ctrl Pts',(-3.52502403892494,-4.75206650705788,
6.07311160753028));
#15208=CARTESIAN_POINT('Ctrl Pts',(-3.65786707291078,-4.65352519087295,
6.06532516095187));
#15209=CARTESIAN_POINT('Ctrl Pts',(-3.78659118537121,-4.54939832693168,
6.05753871437345));
#15210=CARTESIAN_POINT('Ctrl Pts',(-3.91073404767302,-4.44005515403481,
6.04975226779503));
#15211=CARTESIAN_POINT('Ctrl Pts',(-4.03488164574422,-4.33070780994321,
6.04196552418129));
#15212=CARTESIAN_POINT('Ctrl Pts',(-4.15444740154787,-4.2161439669478,6.03417878056755));
#15213=CARTESIAN_POINT('Ctrl Pts',(-4.26900308220881,-4.09677229616093,
6.02639203695381));
#15214=CARTESIAN_POINT('Ctrl Pts',(-4.38355118586876,-3.97740852091676,
6.01860580837488));
#15215=CARTESIAN_POINT('Ctrl Pts',(-4.49308965633097,-3.85323778490719,
6.01081957979596));
#15216=CARTESIAN_POINT('Ctrl Pts',(-4.59722796558208,-3.7247047661486,6.00303335121704));
#15217=CARTESIAN_POINT('Ctrl Pts',(-4.70139368886861,-3.59613791153502,
5.99524507294144));
#15218=CARTESIAN_POINT('Ctrl Pts',(-4.80015620752505,-3.4632067267366,5.98745679466584));
#15219=CARTESIAN_POINT('Ctrl Pts',(-4.89316548685527,-3.32638874468219,
5.97966851639024));
#15220=CARTESIAN_POINT('Ctrl Pts',(-4.98158949875062,-3.19631575669867,
5.97226419269431));
#15221=CARTESIAN_POINT('Ctrl Pts',(-5.06481371698075,-3.06273018855232,
5.96485986899839));
#15222=CARTESIAN_POINT('Ctrl Pts',(-5.14257386922539,-2.92606639741141,
5.95745554530246));
#15223=CARTESIAN_POINT('Ctrl Pts',(-5.22436315360635,-2.78232138977514,
5.94966756754093));
#15224=CARTESIAN_POINT('Ctrl Pts',(-5.30013635645,-2.63511927412894,5.9418795897794));
#15225=CARTESIAN_POINT('Ctrl Pts',(-5.36961720770652,-2.48498322030593,
5.93409161201786));
#15226=CARTESIAN_POINT('Ctrl Pts',(-5.43908439843228,-2.33487668451767,
5.9263051654395));
#15227=CARTESIAN_POINT('Ctrl Pts',(-5.50226157188416,-2.18183765133573,
5.91851871886113));
#15228=CARTESIAN_POINT('Ctrl Pts',(-5.55891954775881,-2.02641161269004,
5.91073227228276));
#15229=CARTESIAN_POINT('Ctrl Pts',(-5.61557968500736,-1.87097964489175,
5.90294552866902));
#15230=CARTESIAN_POINT('Ctrl Pts',(-5.66572001388714,-1.71316078827903,
5.89515878505529));
#15231=CARTESIAN_POINT('Ctrl Pts',(-5.70916016500507,-1.55351883568219,
5.88737204144156));
#15232=CARTESIAN_POINT('Ctrl Pts',(-5.75259744288209,-1.39388744220579,
5.87958581286264));
#15233=CARTESIAN_POINT('Ctrl Pts',(-5.78933534604039,-1.23243350244636,
5.87179958428373));
#15234=CARTESIAN_POINT('Ctrl Pts',(-5.81924384514638,-1.06973437507913,
5.86401335570481));
#15235=CARTESIAN_POINT('Ctrl Pts',(-5.84916021755721,-0.906992417751686,
5.85622507742922));
#15236=CARTESIAN_POINT('Ctrl Pts',(-5.87224353376436,-0.743004931960494,
5.84843679915363));
#15237=CARTESIAN_POINT('Ctrl Pts',(-5.88841504399207,-0.578358740046192,
5.84064852087803));
#15238=CARTESIAN_POINT('Ctrl Pts',(-5.90378931442035,-0.421829446007969,
5.83324419718201));
#15239=CARTESIAN_POINT('Ctrl Pts',(-5.91291682763475,-0.264705090734196,
5.82583987348598));
#15240=CARTESIAN_POINT('Ctrl Pts',(-5.91577346608668,-0.107493536758192,
5.81843554978995));
#15241=CARTESIAN_POINT('Ctrl Pts',(-5.91642423954695,-0.0716790265576193,
5.81674876392827));
#15242=CARTESIAN_POINT('Ctrl Pts',(-5.91674977158135,-0.0358585978170884,
5.81506197806659));
#15243=CARTESIAN_POINT('Ctrl Pts',(-5.91674999987983,-3.77094237526255E-5,
5.8133751922049));
#15244=CARTESIAN_POINT('Ctrl Pts',(-5.91674999993288,2.81822668001089E-5,
5.56162480783485));
#15245=CARTESIAN_POINT('Ctrl Pts',(-5.91675078674804,-0.165160396169148,
5.56940348493561));
#15246=CARTESIAN_POINT('Ctrl Pts',(-5.90982942903261,-0.330379709080826,
5.57718216203637));
#15247=CARTESIAN_POINT('Ctrl Pts',(-5.89600425644402,-0.495039766578426,
5.58496083913712));
#15248=CARTESIAN_POINT('Ctrl Pts',(-5.88218183123642,-0.659667102320903,
5.59273797043515));
#15249=CARTESIAN_POINT('Ctrl Pts',(-5.86145835535694,-0.823735084627806,
5.60051510173317));
#15250=CARTESIAN_POINT('Ctrl Pts',(-5.83390412672512,-0.986657591406252,
5.60829223303119));
#15251=CARTESIAN_POINT('Ctrl Pts',(-5.80634900165882,-1.14958539861808,
5.61606961734623));
#15252=CARTESIAN_POINT('Ctrl Pts',(-5.77196272892421,-1.31136733851814,
5.62384700166127));
#15253=CARTESIAN_POINT('Ctrl Pts',(-5.73086707782368,-1.47142553288187,
5.6316243859763));
#15254=CARTESIAN_POINT('Ctrl Pts',(-5.68977377739136,-1.63147457192868,
5.63940132542553));
#15255=CARTESIAN_POINT('Ctrl Pts',(-5.64197194692404,-1.78979975185782,
5.64717826487476));
#15256=CARTESIAN_POINT('Ctrl Pts',(-5.58763381326402,-1.9458363064165,5.65495520432399));
#15257=CARTESIAN_POINT('Ctrl Pts',(-5.53328198897035,-2.10191217478963,
5.66273410319327));
#15258=CARTESIAN_POINT('Ctrl Pts',(-5.47239067544521,-2.2556979618502,5.67051300206256));
#15259=CARTESIAN_POINT('Ctrl Pts',(-5.40518132146314,-2.40664609874531,
5.67829190093184));
#15260=CARTESIAN_POINT('Ctrl Pts',(-5.35187308520774,-2.52637316748137,
5.68446186618461));
#15261=CARTESIAN_POINT('Ctrl Pts',(-5.29459106575013,-2.64431532354144,
5.69063183143738));
#15262=CARTESIAN_POINT('Ctrl Pts',(-5.23346695418843,-2.76020908663051,
5.69680179669016));
#15263=CARTESIAN_POINT('Ctrl Pts',(-5.15631232362956,-2.90649735564182,
5.70458990808312));
#15264=CARTESIAN_POINT('Ctrl Pts',(-5.0730064015835,-3.04957472254615,5.71237801947609));
#15265=CARTESIAN_POINT('Ctrl Pts',(-4.9838415312255,-3.18892680288086,5.72016613086906));
#15266=CARTESIAN_POINT('Ctrl Pts',(-4.89469416683538,-3.32825152386391,
5.72795271320213));
#15267=CARTESIAN_POINT('Ctrl Pts',(-4.79969032143716,-3.46385214864654,
5.73573929553519));
#15268=CARTESIAN_POINT('Ctrl Pts',(-4.69916649070406,-3.5952419744913,5.74352587786826));
#15269=CARTESIAN_POINT('Ctrl Pts',(-4.59863882701976,-3.72663681020075,
5.75131275710197));
#15270=CARTESIAN_POINT('Ctrl Pts',(-4.49259094785246,-3.85382026953491,
5.75909963633568));
#15271=CARTESIAN_POINT('Ctrl Pts',(-4.38140103783249,-3.97633694600701,
5.76688651556939));
#15272=CARTESIAN_POINT('Ctrl Pts',(-4.27021846628216,-4.09884553644945,
5.77467288087358));
#15273=CARTESIAN_POINT('Ctrl Pts',(-4.15389475785512,-4.21668772384252,
5.78245924617778));
#15274=CARTESIAN_POINT('Ctrl Pts',(-4.03284661808541,-4.32944323412342,
5.79024561148197));
#15275=CARTESIAN_POINT('Ctrl Pts',(-3.91176669353232,-4.4422283517116,5.79803402132757));
#15276=CARTESIAN_POINT('Ctrl Pts',(-3.78596009141773,-4.54992390391047,
5.80582243117318));
#15277=CARTESIAN_POINT('Ctrl Pts',(-3.6558790851148,-4.65214774889192,5.81361084101878));
#15278=CARTESIAN_POINT('Ctrl Pts',(-3.53263409049762,-4.74899953058208,
5.82098995467095));
#15279=CARTESIAN_POINT('Ctrl Pts',(-3.40555259771247,-4.84093975041548,
5.82836906832312));
#15280=CARTESIAN_POINT('Ctrl Pts',(-3.2750454318935,-4.92767774733023,5.83574818197529));
#15281=CARTESIAN_POINT('Ctrl Pts',(-3.13730472306474,-5.0192233195787,5.84353629336825));
#15282=CARTESIAN_POINT('Ctrl Pts',(-2.99569863356498,-5.10500633062844,
5.85132440476121));
#15283=CARTESIAN_POINT('Ctrl Pts',(-2.85072997627565,-5.18471495502534,
5.85911251615417));
#15284=CARTESIAN_POINT('Ctrl Pts',(-2.70578978105447,-5.26440793002367,
5.86689909848725));
#15285=CARTESIAN_POINT('Ctrl Pts',(-2.55748861512491,-5.33802874410464,
5.87468568082034));
#15286=CARTESIAN_POINT('Ctrl Pts',(-2.40635481877118,-5.40531100388097,
5.88247226315342));
#15287=CARTESIAN_POINT('Ctrl Pts',(-2.25521525972003,-5.47259582911463,
5.89025914238712));
#15288=CARTESIAN_POINT('Ctrl Pts',(-2.10124314441283,-5.53354148287171,
5.89804602162083));
#15289=CARTESIAN_POINT('Ctrl Pts',(-1.94498844792873,-5.5879289991842,5.90583290085453));
#15290=CARTESIAN_POINT('Ctrl Pts',(-1.78874406416405,-5.64231292595214,
5.91361926615872));
#15291=CARTESIAN_POINT('Ctrl Pts',(-1.63021770252737,-5.6901394765073,5.92140563146291));
#15292=CARTESIAN_POINT('Ctrl Pts',(-1.46997635559212,-5.73123896522385,
5.92919199676709));
#15293=CARTESIAN_POINT('Ctrl Pts',(-1.30969293253327,-5.7723492458315,5.93698040661269));
#15294=CARTESIAN_POINT('Ctrl Pts',(-1.14769393357346,-5.80672885366815,
5.94476881645828));
#15295=CARTESIAN_POINT('Ctrl Pts',(-0.984559340411803,-5.83425860480215,
5.95255722630388));
#15296=CARTESIAN_POINT('Ctrl Pts',(-0.829997789670841,-5.86034161358844,
5.95993633995606));
#15297=CARTESIAN_POINT('Ctrl Pts',(-0.674417186707035,-5.88027615178174,
5.96731545360823));
#15298=CARTESIAN_POINT('Ctrl Pts',(-0.518317348950165,-5.89400353650024,
5.97469456726041));
#15299=CARTESIAN_POINT('Ctrl Pts',(-0.353565458387484,-5.90849178080178,
5.98248267865336));
#15300=CARTESIAN_POINT('Ctrl Pts',(-0.188176301311359,-5.91607045415487,
5.99027079004632));
#15301=CARTESIAN_POINT('Ctrl Pts',(-0.0227405974838046,-5.91670629892393,
5.99805890143928));
#15302=CARTESIAN_POINT('Ctrl Pts',(0.14266262592742,-5.91734201885594,6.00584548377234));
#15303=CARTESIAN_POINT('Ctrl Pts',(0.308112058526976,-5.91103762877306,
6.01363206610539));
#15304=CARTESIAN_POINT('Ctrl Pts',(0.473016300660618,-5.89781197918426,
6.02141864843845));
#15305=CARTESIAN_POINT('Ctrl Pts',(0.637926830556203,-5.8845858253044,6.02920552767216));
#15306=CARTESIAN_POINT('Ctrl Pts',(0.802291809580338,-5.86443790545047,
6.03699240690586));
#15307=CARTESIAN_POINT('Ctrl Pts',(0.965523531021385,-5.83743906807977,
6.04477928613957));
#15308=CARTESIAN_POINT('Ctrl Pts',(1.12874447926359,-5.81044201261666,6.05256565144376));
#15309=CARTESIAN_POINT('Ctrl Pts',(1.290832004347,-5.77659499673414,6.06035201674796));
#15310=CARTESIAN_POINT('Ctrl Pts',(1.45120703356333,-5.73602028485224,6.06813838205215));
#15311=CARTESIAN_POINT('Ctrl Pts',(1.61162417400521,-5.69543491887504,6.07592679189774));
#15312=CARTESIAN_POINT('Ctrl Pts',(1.77032760960406,-5.6481184034913,6.08371520174333));
#15313=CARTESIAN_POINT('Ctrl Pts',(1.92675102339513,-5.59424356426727,6.09150361158892));
#15314=CARTESIAN_POINT('Ctrl Pts',(2.07495408038808,-5.54319995337493,6.09888272524113));
#15315=CARTESIAN_POINT('Ctrl Pts',(2.2211103452496,-5.48626967958779,6.10626183889333));
#15316=CARTESIAN_POINT('Ctrl Pts',(2.36475284092546,-5.42364034241163,6.11364095254553));
#15317=CARTESIAN_POINT('Ctrl Pts',(2.51635692372114,-5.3575396862373,6.1214290639385));
#15318=CARTESIAN_POINT('Ctrl Pts',(2.66521482238985,-5.28506668731938,6.12921717533147));
#15319=CARTESIAN_POINT('Ctrl Pts',(2.81079190079884,-5.20647476253402,6.13700528672444));
#15320=CARTESIAN_POINT('Ctrl Pts',(2.95634039768654,-5.12789826790288,6.14479186905751));
#15321=CARTESIAN_POINT('Ctrl Pts',(3.09860907855198,-5.04320539614401,6.15257845139059));
#15322=CARTESIAN_POINT('Ctrl Pts',(3.23708764060745,-4.95269564676919,6.16036503372366));
#15323=CARTESIAN_POINT('Ctrl Pts',(3.37557148281972,-4.86218244627774,6.16815191295739));
#15324=CARTESIAN_POINT('Ctrl Pts',(3.51026464742944,-4.7658520958598,6.17593879219112));
#15325=CARTESIAN_POINT('Ctrl Pts',(3.64068495215819,-4.66404798877852,6.18372567142485));
#15326=CARTESIAN_POINT('Ctrl Pts',(3.77109664922213,-4.56225060070952,6.19151203672905));
#15327=CARTESIAN_POINT('Ctrl Pts',(3.89723579891847,-4.45498037564351,6.19929840203324));
#15328=CARTESIAN_POINT('Ctrl Pts',(4.01865239989385,-4.3426217255625,6.20708476733744));
#15329=CARTESIAN_POINT('Ctrl Pts',(4.14010088240309,-4.23023357238159,6.21487317718305));
#15330=CARTESIAN_POINT('Ctrl Pts',(4.25682410233023,-4.11275454008674,6.22266158702866));
#15331=CARTESIAN_POINT('Ctrl Pts',(4.36840744966687,-3.99060733675904,6.23044999687427));
#15332=CARTESIAN_POINT('Ctrl Pts',(4.47412687352927,-3.87487920823059,6.2378291105264));
#15333=CARTESIAN_POINT('Ctrl Pts',(4.5752325753855,-3.75496112417559,6.24520822417853));
#15334=CARTESIAN_POINT('Ctrl Pts',(4.67140424624382,-3.63124123829239,6.25258733783066));
#15335=CARTESIAN_POINT('Ctrl Pts',(4.77290636706753,-3.50066400392456,6.26037544922361));
#15336=CARTESIAN_POINT('Ctrl Pts',(4.8689482474425,-3.36580494126235,6.26816356061656));
#15337=CARTESIAN_POINT('Ctrl Pts',(4.95918165474667,-3.22714237022851,6.27595167200951));
#15338=CARTESIAN_POINT('Ctrl Pts',(5.04939734629465,-3.08850702317273,6.28373825434258));
#15339=CARTESIAN_POINT('Ctrl Pts',(5.13380666602261,-2.94606992538918,6.29152483667566));
#15340=CARTESIAN_POINT('Ctrl Pts',(5.21210479653212,-2.80033822108454,6.29931141900873));
#15341=CARTESIAN_POINT('Ctrl Pts',(5.29040591253172,-2.65460096006279,6.30709829824243));
#15342=CARTESIAN_POINT('Ctrl Pts',(5.36259521834144,-2.50556912074392,6.31488517747614));
#15343=CARTESIAN_POINT('Ctrl Pts',(5.42841359014247,-2.35377493759632,6.32267205670985));
#15344=CARTESIAN_POINT('Ctrl Pts',(5.4942276179692,-2.2019907727766,6.33045842201405));
#15345=CARTESIAN_POINT('Ctrl Pts',(5.55367142621311,-2.0474449221907,6.33824478731825));
#15346=CARTESIAN_POINT('Ctrl Pts',(5.60653377466187,-1.89069024329097,6.34603115262245));
#15347=CARTESIAN_POINT('Ctrl Pts',(5.65941000368975,-1.73389440379613,6.35381956246805));
#15348=CARTESIAN_POINT('Ctrl Pts',(5.70570121569159,-1.57488887939405,6.36160797231364));
#15349=CARTESIAN_POINT('Ctrl Pts',(5.74524557060721,-1.41424322374839,6.36939638215924));
#15350=CARTESIAN_POINT('Ctrl Pts',(5.78271179221209,-1.26203981198143,6.37677549581142));
#15351=CARTESIAN_POINT('Ctrl Pts',(5.81412197673077,-1.10836447192937,6.3841546094636));
#15352=CARTESIAN_POINT('Ctrl Pts',(5.83938055994312,-0.953711297331862,
6.39153372311579));
#15353=CARTESIAN_POINT('Ctrl Pts',(5.86603913561472,-0.790486253266605,
6.39932183450875));
#15354=CARTESIAN_POINT('Ctrl Pts',(5.88585437186082,-0.626113609616027,
6.40710994590171));
#15355=CARTESIAN_POINT('Ctrl Pts',(5.89874932278544,-0.46117999678903,6.41489805729467));
#15356=CARTESIAN_POINT('Ctrl Pts',(5.91164174201125,-0.296278765801521,
6.42268463962773));
#15357=CARTESIAN_POINT('Ctrl Pts',(5.9176165619907,-0.130817103752322,6.4304712219608));
#15358=CARTESIAN_POINT('Ctrl Pts',(5.91664875128057,0.0346138190619499,
6.43825780429386));
#15359=CARTESIAN_POINT('Ctrl Pts',(5.91568090366804,0.200051049720641,6.44604468352758));
#15360=CARTESIAN_POINT('Ctrl Pts',(5.90776989358004,0.365457219265649,6.45383156276131));
#15361=CARTESIAN_POINT('Ctrl Pts',(5.89294281821464,0.530240986488662,6.46161844199503));
#15362=CARTESIAN_POINT('Ctrl Pts',(5.87811672142768,0.695013878077948,6.46940480729921));
#15363=CARTESIAN_POINT('Ctrl Pts',(5.85637550155739,0.859164131292016,6.47719117260338));
#15364=CARTESIAN_POINT('Ctrl Pts',(5.82779817025247,1.02210520461546,6.48497753790756));
#15365=CARTESIAN_POINT('Ctrl Pts',(5.79921333512064,1.18508906295607,6.49276594775315));
#15366=CARTESIAN_POINT('Ctrl Pts',(5.76378885504401,1.34686279169558,6.50055435759875));
#15367=CARTESIAN_POINT('Ctrl Pts',(5.72165510912876,1.50684882276914,6.50834276744434));
#15368=CARTESIAN_POINT('Ctrl Pts',(5.68173557409338,1.65842727452749,6.51572188109654));
#15369=CARTESIAN_POINT('Ctrl Pts',(5.63579387225719,1.80840083841147,6.52310099474873));
#15370=CARTESIAN_POINT('Ctrl Pts',(5.58398247836574,1.95628991813698,6.53048010840092));
#15371=CARTESIAN_POINT('Ctrl Pts',(5.52929936518024,2.11237595786933,6.53826821979388));
#15372=CARTESIAN_POINT('Ctrl Pts',(5.46805790732545,2.2661956360904,6.54605633118685));
#15373=CARTESIAN_POINT('Ctrl Pts',(5.40047120152811,2.41719700561737,6.55384444257982));
#15374=CARTESIAN_POINT('Ctrl Pts',(5.33289776520245,2.56816872865729,6.56163102491285));
#15375=CARTESIAN_POINT('Ctrl Pts',(5.25898169709123,2.71632295558537,6.56941760724589));
#15376=CARTESIAN_POINT('Ctrl Pts',(5.17898385322954,2.86112859034467,6.57720418957892));
#15377=CARTESIAN_POINT('Ctrl Pts',(5.0989829590676,3.00593974651109,6.58499106881264));
#15378=CARTESIAN_POINT('Ctrl Pts',(5.01289997617998,3.14740177343452,6.59277794804635));
#15379=CARTESIAN_POINT('Ctrl Pts',(4.92104161772181,3.28500836515677,6.60056482728006));
#15380=CARTESIAN_POINT('Ctrl Pts',(4.82918932186224,3.42260587492343,6.60835119258425));
#15381=CARTESIAN_POINT('Ctrl Pts',(4.73156259073039,3.55634819298406,6.61613755788843));
#15382=CARTESIAN_POINT('Ctrl Pts',(4.62851142840317,3.68575806580427,6.62392392319261));
#15383=CARTESIAN_POINT('Ctrl Pts',(4.52543320693327,3.81520191902929,6.63171233303821));
#15384=CARTESIAN_POINT('Ctrl Pts',(4.41692790578704,3.94031080249557,6.6395007428838));
#15385=CARTESIAN_POINT('Ctrl Pts',(4.30338634276314,4.06063991846356,6.6472891527294));
#15386=CARTESIAN_POINT('Ctrl Pts',(4.19581161128232,4.17464550368573,6.65466826638161));
#15387=CARTESIAN_POINT('Ctrl Pts',(4.08371651262214,4.28436058326985,6.66204738003382));
#15388=CARTESIAN_POINT('Ctrl Pts',(3.96746439411179,4.38943696206645,6.66942649368603));
#15389=CARTESIAN_POINT('Ctrl Pts',(3.84476883861533,4.50033734677521,6.67721460507902));
#15390=CARTESIAN_POINT('Ctrl Pts',(3.71739855822804,4.60610984434629,6.68500271647201));
#15391=CARTESIAN_POINT('Ctrl Pts',(3.58580474904591,4.70637173034811,6.69279082786499));
#15392=CARTESIAN_POINT('Ctrl Pts',(3.45423677601469,4.80661393167605,6.70057741019805));
#15393=CARTESIAN_POINT('Ctrl Pts',(3.31844718272779,4.90134748664351,6.7083639925311));
#15394=CARTESIAN_POINT('Ctrl Pts',(3.17891912790614,4.99023083040579,6.71615057486415));
#15395=CARTESIAN_POINT('Ctrl Pts',(3.03938575291036,5.07911756327047,6.72393745409788));
#15396=CARTESIAN_POINT('Ctrl Pts',(2.8961138985044,5.16215346357446,6.73172433333161));
#15397=CARTESIAN_POINT('Ctrl Pts',(2.74961513113557,5.23904067488795,6.73951121256533));
#15398=CARTESIAN_POINT('Ctrl Pts',(2.60312603260058,5.31592281168999,6.74729757786954));
#15399=CARTESIAN_POINT('Ctrl Pts',(2.45341073030344,5.38665692319201,6.75508394317375));
#15400=CARTESIAN_POINT('Ctrl Pts',(2.30100490573404,5.45099137646427,6.76287030847796));
#15401=CARTESIAN_POINT('Ctrl Pts',(2.14855906248999,5.51534272265753,6.77065871832358));
#15402=CARTESIAN_POINT('Ctrl Pts',(1.99342157910068,5.5732909266572,6.7784471281692));
#15403=CARTESIAN_POINT('Ctrl Pts',(1.83614844851996,5.62463238243156,6.78623553801482));
#15404=CARTESIAN_POINT('Ctrl Pts',(1.68714032902148,5.67327574413616,6.79361465166693));
#15405=CARTESIAN_POINT('Ctrl Pts',(1.53621550111517,5.71598881183929,6.80099376531905));
#15406=CARTESIAN_POINT('Ctrl Pts',(1.38385961722288,5.75263966560741,6.80837287897116));
#15407=CARTESIAN_POINT('Ctrl Pts',(1.22305919442603,5.79132194443522,6.81616099036413));
#15408=CARTESIAN_POINT('Ctrl Pts',(1.06060715103004,5.82326475527976,6.82394910175709));
#15409=CARTESIAN_POINT('Ctrl Pts',(0.897082801490368,5.84834788720457,6.83173721315005));
#15410=CARTESIAN_POINT('Ctrl Pts',(0.733590557106401,5.87342609449364,6.83952379548309));
#15411=CARTESIAN_POINT('Ctrl Pts',(0.56902674228538,5.89164726167009,6.84731037781613));
#15412=CARTESIAN_POINT('Ctrl Pts',(0.403979046395523,5.90294261301712,6.85509696014918));
#15413=CARTESIAN_POINT('Ctrl Pts',(0.238925057273242,5.91423839505341,6.86288383938289));
#15414=CARTESIAN_POINT('Ctrl Pts',(0.0733874686636907,5.9186078070816,6.87067071861661));
#15415=CARTESIAN_POINT('Ctrl Pts',(-0.0920419962389234,5.91603404599977,
6.87845759785033));
#15416=CARTESIAN_POINT('Ctrl Pts',(-0.257460542892226,5.91346045478468,
6.88624396315451));
#15417=CARTESIAN_POINT('Ctrl Pts',(-0.422770660606182,5.90394461256802,
6.89403032845869));
#15418=CARTESIAN_POINT('Ctrl Pts',(-0.587381565169692,5.88752184364515,
6.90181669376286));
#15419=CARTESIAN_POINT('Ctrl Pts',(-0.752035693214231,5.87109476243664,
6.90960510360846));
#15420=CARTESIAN_POINT('Ctrl Pts',(-0.915989922886949,5.84775716034388,
6.91739351345406));
#15421=CARTESIAN_POINT('Ctrl Pts',(-1.07865861177825,5.81759625289833,6.92518192329966));
#15422=CARTESIAN_POINT('Ctrl Pts',(-1.23277874243144,5.78902036021849,6.93256103695187));
#15423=CARTESIAN_POINT('Ctrl Pts',(-1.38574471671469,5.75431992011536,6.93994015060408));
#15424=CARTESIAN_POINT('Ctrl Pts',(-1.53706695700239,5.71361144392856,6.94731926425629));
#15425=CARTESIAN_POINT('Ctrl Pts',(-1.69677644504388,5.67064664325959,6.95510737564926));
#15426=CARTESIAN_POINT('Ctrl Pts',(-1.85471185969222,5.62097356837911,6.96289548704222));
#15427=CARTESIAN_POINT('Ctrl Pts',(-2.01030697854925,5.5647638237841,6.97068359843519));
#15428=CARTESIAN_POINT('Ctrl Pts',(-2.16587154901762,5.50856511499237,6.97847018076828));
#15429=CARTESIAN_POINT('Ctrl Pts',(-2.31909644015226,5.44583240567079,6.98625676310137));
#15430=CARTESIAN_POINT('Ctrl Pts',(-2.46943268377581,5.3767864736104,6.99404334543446));
#15431=CARTESIAN_POINT('Ctrl Pts',(-2.61977465968635,5.30773790884424,7.00183022466817));
#15432=CARTESIAN_POINT('Ctrl Pts',(-2.76722747568402,5.23237576942095,7.00961710390188));
#15433=CARTESIAN_POINT('Ctrl Pts',(-2.91126348692853,5.15096840139568,7.01740398313559));
#15434=CARTESIAN_POINT('Ctrl Pts',(-3.05528999187953,5.06956640620965,7.02519034843977));
#15435=CARTESIAN_POINT('Ctrl Pts',(-3.195899865215,4.98212013818004,7.03297671374395));
#15436=CARTESIAN_POINT('Ctrl Pts',(-3.33259122622223,4.88894326837678,7.04076307904814));
#15437=CARTESIAN_POINT('Ctrl Pts',(-3.46931847960501,4.79574193221969,7.04855148889372));
#15438=CARTESIAN_POINT('Ctrl Pts',(-3.60212489936952,4.69680716599325,7.05633989873932));
#15439=CARTESIAN_POINT('Ctrl Pts',(-3.73053794653349,4.59249574762717,7.06412830858491));
#15440=CARTESIAN_POINT('Ctrl Pts',(-3.85220263653191,4.49366609862274,7.07150742223707));
#15441=CARTESIAN_POINT('Ctrl Pts',(-3.96992363601487,4.39001053383125,7.07888653588924));
#15442=CARTESIAN_POINT('Ctrl Pts',(-4.08332677882751,4.28186559571995,7.08626564954141));
#15443=CARTESIAN_POINT('Ctrl Pts',(-4.20301545014583,4.16772657248557,7.09405376093436));
#15444=CARTESIAN_POINT('Ctrl Pts',(-4.31793679218021,4.0485456398114,7.1018418723273));
#15445=CARTESIAN_POINT('Ctrl Pts',(-4.42767569376072,3.92474438828576,7.10962998372025));
#15446=CARTESIAN_POINT('Ctrl Pts',(-4.53739305002053,3.80096744297813,7.11741656605326));
#15447=CARTESIAN_POINT('Ctrl Pts',(-4.64192978418409,3.67257222775606,7.12520314838627));
#15448=CARTESIAN_POINT('Ctrl Pts',(-4.74090946264455,3.54001525837211,7.13298973071929));
#15449=CARTESIAN_POINT('Ctrl Pts',(-4.83989291517847,3.40745323461996,7.14077660995298));
#15450=CARTESIAN_POINT('Ctrl Pts',(-4.93331869368738,3.27072939282946,7.14856348918667));
#15451=CARTESIAN_POINT('Ctrl Pts',(-5.02085184740838,3.13033181769535,7.15635036842036));
#15452=CARTESIAN_POINT('Ctrl Pts',(-5.10837922399208,2.98994350871965,7.16413673372455));
#15453=CARTESIAN_POINT('Ctrl Pts',(-5.19001458509246,2.84588222283844,7.17192309902873));
#15454=CARTESIAN_POINT('Ctrl Pts',(-5.26546728910059,2.6986635192094,7.17970946433292));
#15455=CARTESIAN_POINT('Ctrl Pts',(-5.34093980545652,2.55140615893846,7.18749787417851));
#15456=CARTESIAN_POINT('Ctrl Pts',(-5.41022627318604,2.40099000791569,7.19528628402409));
#15457=CARTESIAN_POINT('Ctrl Pts',(-5.47308244016529,2.24795444029774,7.20307469386968));
#15458=CARTESIAN_POINT('Ctrl Pts',(-5.53263539244729,2.10296119152379,7.21045380752197));
#15459=CARTESIAN_POINT('Ctrl Pts',(-5.58641641177452,1.95561699655019,7.21783292117426));
#15460=CARTESIAN_POINT('Ctrl Pts',(-5.63425794808955,1.80639639528254,7.22521203482654));
#15461=CARTESIAN_POINT('Ctrl Pts',(-5.68487660239283,1.64851379760097,7.23301949319431));
#15462=CARTESIAN_POINT('Ctrl Pts',(-5.72886366753598,1.48847477281738,7.24082695156208));
#15463=CARTESIAN_POINT('Ctrl Pts',(-5.76605560025257,1.32685092504622,7.24863440992985));
#15464=CARTESIAN_POINT('Ctrl Pts',(-5.80323914575064,1.16526352535476,7.25644010762387));
#15465=CARTESIAN_POINT('Ctrl Pts',(-5.83363054628982,1.00209232399418,7.2642458053179));
#15466=CARTESIAN_POINT('Ctrl Pts',(-5.85711694061192,0.837921062211063,
7.27205150301192));
#15467=CARTESIAN_POINT('Ctrl Pts',(-5.88060187927665,0.673759975557509,
7.27985671691856));
#15468=CARTESIAN_POINT('Ctrl Pts',(-5.89718261864945,0.508599264814231,
7.2876619308252));
#15469=CARTESIAN_POINT('Ctrl Pts',(-5.90679783623067,0.34303044238191,7.29546714473184));
#15470=CARTESIAN_POINT('Ctrl Pts',(-5.91343269372531,0.22878180129641,7.30085303241961));
#15471=CARTESIAN_POINT('Ctrl Pts',(-5.91675198364477,0.1143390029343,7.30623892010737));
#15472=CARTESIAN_POINT('Ctrl Pts',(-5.91674999911038,-0.000102602491467883,
7.31162480779513));
#15473=CARTESIAN_POINT('Origin',(0.,0.,0.));
#15474=CARTESIAN_POINT('',(-5.91674999870471,0.000123805739447762,9.3133751922049));
#15475=CARTESIAN_POINT('',(-5.91674999804438,0.000152124367665733,9.06162480779513));
#15476=CARTESIAN_POINT('',(-5.91675,-7.2459289488551E-16,0.));
#15477=CARTESIAN_POINT('Ctrl Pts',(-5.91674999870471,0.000123805739447762,
9.3133751922049));
#15478=CARTESIAN_POINT('Ctrl Pts',(-5.91674711889009,0.137751860954763,
9.30689527400423));
#15479=CARTESIAN_POINT('Ctrl Pts',(-5.91194070528015,0.275360352934919,
9.30041535580356));
#15480=CARTESIAN_POINT('Ctrl Pts',(-5.90234404326611,0.412632230225794,
9.29393543760289));
#15481=CARTESIAN_POINT('Ctrl Pts',(-5.89081016459092,0.577614301686852,
9.28614745984122));
#15482=CARTESIAN_POINT('Ctrl Pts',(-5.87235253261579,0.74214198003531,9.27835948207955));
#15483=CARTESIAN_POINT('Ctrl Pts',(-5.84703094864028,0.905626660463758,
9.27057150431788));
#15484=CARTESIAN_POINT('Ctrl Pts',(-5.82171434310529,1.06907919840233,9.26278505773942));
#15485=CARTESIAN_POINT('Ctrl Pts',(-5.78953652712413,1.23148883198974,9.25499861116095));
#15486=CARTESIAN_POINT('Ctrl Pts',(-5.75060887188758,1.39227445752188,9.24721216458248));
#15487=CARTESIAN_POINT('Ctrl Pts',(-5.71167973164869,1.55306621666338,9.23942542096862));
#15488=CARTESIAN_POINT('Ctrl Pts',(-5.66600030825776,1.71223353228523,9.23163867735477));
#15489=CARTESIAN_POINT('Ctrl Pts',(-5.61373274820993,1.86920710307216,9.22385193374091));
#15490=CARTESIAN_POINT('Ctrl Pts',(-5.56146864527017,2.02617029123174,9.21606570516189));
#15491=CARTESIAN_POINT('Ctrl Pts',(-5.50261737875396,2.18093972174852,9.20827947658287));
#15492=CARTESIAN_POINT('Ctrl Pts',(-5.43739052057007,2.33296268493835,9.20049324800385));
#15493=CARTESIAN_POINT('Ctrl Pts',(-5.37214649165009,2.48502566762711,9.19270496972813));
#15494=CARTESIAN_POINT('Ctrl Pts',(-5.30052364164677,2.63434044365937,9.1849166914524));
#15495=CARTESIAN_POINT('Ctrl Pts',(-5.22278147765959,2.78037483068667,9.17712841317668));
#15496=CARTESIAN_POINT('Ctrl Pts',(-5.14887192710607,2.9192098637882,9.16972408948125));
#15497=CARTESIAN_POINT('Ctrl Pts',(-5.06943200497215,3.05507992408495,9.16231976578582));
#15498=CARTESIAN_POINT('Ctrl Pts',(-4.98472296263196,3.18754883073337,9.15491544209038));
#15499=CARTESIAN_POINT('Ctrl Pts',(-4.89562473231721,3.32688159649295,9.14712746432892));
#15500=CARTESIAN_POINT('Ctrl Pts',(-4.80066497501037,3.46250123228239,9.13933948656745));
#15501=CARTESIAN_POINT('Ctrl Pts',(-4.70017794192323,3.59391957015712,9.13155150880598));
#15502=CARTESIAN_POINT('Ctrl Pts',(-4.59971066544827,3.72531207005997,9.1237650622277));
#15503=CARTESIAN_POINT('Ctrl Pts',(-4.49371847547923,3.85250466649364,9.11597861564943));
#15504=CARTESIAN_POINT('Ctrl Pts',(-4.38257731087115,3.97504046227676,9.10819216907115));
#15505=CARTESIAN_POINT('Ctrl Pts',(-4.27143190647816,4.09758093252428,9.10040542545749));
#15506=CARTESIAN_POINT('Ctrl Pts',(-4.15513734614906,4.2154640073063,9.09261868184383));
#15507=CARTESIAN_POINT('Ctrl Pts',(-4.03410849985289,4.32826745637497,9.08483193823017));
#15508=CARTESIAN_POINT('Ctrl Pts',(-3.91308765870954,4.44106344433932,9.07704570965135));
#15509=CARTESIAN_POINT('Ctrl Pts',(-3.78733339209091,4.54878026112686,9.06925948107253));
#15510=CARTESIAN_POINT('Ctrl Pts',(-3.65729602342713,4.65103390221187,9.06147325249371));
#15511=CARTESIAN_POINT('Ctrl Pts',(-3.52722442289306,4.75331446120066,9.05368497421818));
#15512=CARTESIAN_POINT('Ctrl Pts',(-3.3928677174589,4.85012877154615,9.04589669594264));
#15513=CARTESIAN_POINT('Ctrl Pts',(-3.25470849171235,4.94113379665796,9.03810841766711));
#15514=CARTESIAN_POINT('Ctrl Pts',(-3.1233603820424,5.02765236213423,9.03070409397069));
#15515=CARTESIAN_POINT('Ctrl Pts',(-2.98857586191077,5.108920484133,9.02329977027427));
#15516=CARTESIAN_POINT('Ctrl Pts',(-2.85079309458859,5.184680249962,9.01589544657785));
#15517=CARTESIAN_POINT('Ctrl Pts',(-2.70587113117589,5.26436549816109,9.00810746881631));
#15518=CARTESIAN_POINT('Ctrl Pts',(-2.5575801224491,5.33798491034792,9.00031949105477));
#15519=CARTESIAN_POINT('Ctrl Pts',(-2.40644720979684,5.40526987198243,8.99253151329323));
#15520=CARTESIAN_POINT('Ctrl Pts',(-2.25534401117084,5.47254160481666,8.98474506671488));
#15521=CARTESIAN_POINT('Ctrl Pts',(-2.10140031522255,5.53348124216589,8.97695862013653));
#15522=CARTESIAN_POINT('Ctrl Pts',(-1.94516489664656,5.58786757961872,8.96917217355819));
#15523=CARTESIAN_POINT('Ctrl Pts',(-1.78892351804169,5.64225599178768,8.96138542994446));
#15524=CARTESIAN_POINT('Ctrl Pts',(-1.63039054234946,5.69009049503393,8.95359868633074));
#15525=CARTESIAN_POINT('Ctrl Pts',(-1.47013233171216,5.73119895743941,8.94581194271702));
#15526=CARTESIAN_POINT('Ctrl Pts',(-1.30988472095649,5.77230470082766,8.93802571413813));
#15527=CARTESIAN_POINT('Ctrl Pts',(-1.14791241319261,5.80668521434587,8.93023948555924));
#15528=CARTESIAN_POINT('Ctrl Pts',(-0.98479460116806,5.83421889853391,8.92245325698035));
#15529=CARTESIAN_POINT('Ctrl Pts',(-0.821633848965534,5.86175983086539,
8.91466497870476));
#15530=CARTESIAN_POINT('Ctrl Pts',(-0.657327304919354,5.88245027713472,
8.90687670042917));
#15531=CARTESIAN_POINT('Ctrl Pts',(-0.492462876943627,5.89622004994152,
8.89908842215358));
#15532=CARTESIAN_POINT('Ctrl Pts',(-0.335726105669414,5.90931098627883,
8.8916840984575));
#15533=CARTESIAN_POINT('Ctrl Pts',(-0.178485394289553,5.91614715499982,
8.88427977476142));
#15534=CARTESIAN_POINT('Ctrl Pts',(-0.0212489029355745,5.91671184414317,
8.87687545106534));
#15535=CARTESIAN_POINT('Ctrl Pts',(0.144134776685753,5.91730579258074,8.86908747330382));
#15536=CARTESIAN_POINT('Ctrl Pts',(0.309572948295051,5.91096130722683,8.86129949554229));
#15537=CARTESIAN_POINT('Ctrl Pts',(0.474474206673456,5.89769487085434,8.85351151778077));
#15538=CARTESIAN_POINT('Ctrl Pts',(0.639343044050709,5.88443104277698,8.84572507120244));
#15539=CARTESIAN_POINT('Ctrl Pts',(0.803674860498382,5.86424800471654,8.83793862462411));
#15540=CARTESIAN_POINT('Ctrl Pts',(0.966881950513395,5.83721422052261,8.83015217804578));
#15541=CARTESIAN_POINT('Ctrl Pts',(1.13009526651102,5.81017940505075,8.82236543443207));
#15542=CARTESIAN_POINT('Ctrl Pts',(1.29218345433104,5.77629336881456,8.81457869081835));
#15543=CARTESIAN_POINT('Ctrl Pts',(1.45256685615463,5.73567607967021,8.80679194720464));
#15544=CARTESIAN_POINT('Ctrl Pts',(1.612939649816,5.69506147705569,8.79900571862576));
#15545=CARTESIAN_POINT('Ctrl Pts',(1.77160757335952,5.64771659105516,8.79121949004688));
#15546=CARTESIAN_POINT('Ctrl Pts',(1.92800389197832,5.59381189842995,8.78343326146801));
#15547=CARTESIAN_POINT('Ctrl Pts',(2.08444138136616,5.53989301558805,8.77564498319243));
#15548=CARTESIAN_POINT('Ctrl Pts',(2.23860576796796,5.47941097786755,8.76785670491686));
#15549=CARTESIAN_POINT('Ctrl Pts',(2.38994727436551,5.41258557329608,8.76006842664128));
#15550=CARTESIAN_POINT('Ctrl Pts',(2.53382779100609,5.34905459647865,8.75266410294513));
#15551=CARTESIAN_POINT('Ctrl Pts',(2.67515681233243,5.27979073685871,8.74525977924897));
#15552=CARTESIAN_POINT('Ctrl Pts',(2.81348017613379,5.20502256104642,8.73785545555282));
#15553=CARTESIAN_POINT('Ctrl Pts',(2.95897074696685,5.1263802819684,8.73006747779129));
#15554=CARTESIAN_POINT('Ctrl Pts',(3.10118796001897,5.04161999980981,8.72227950002975));
#15555=CARTESIAN_POINT('Ctrl Pts',(3.2396204534312,4.95103927273964,8.71449152226821));
#15556=CARTESIAN_POINT('Ctrl Pts',(3.37802572982839,4.86047635461699,8.70670507568987));
#15557=CARTESIAN_POINT('Ctrl Pts',(3.51264750407078,4.76409544975376,8.69891862911154));
#15558=CARTESIAN_POINT('Ctrl Pts',(3.64300254427932,4.66223798458148,8.6911321825332));
#15559=CARTESIAN_POINT('Ctrl Pts',(3.77336255723879,4.56037663377653,8.68334543891948));
#15560=CARTESIAN_POINT('Ctrl Pts',(3.89945525624355,4.45303849824056,8.67555869530575));
#15561=CARTESIAN_POINT('Ctrl Pts',(4.02082912853708,4.34060637257143,8.66777195169203));
#15562=CARTESIAN_POINT('Ctrl Pts',(4.14219497285695,4.22818168344632,8.65998572311315));
#15563=CARTESIAN_POINT('Ctrl Pts',(4.25884238068587,4.11066389569112,8.65219949453426));
#15564=CARTESIAN_POINT('Ctrl Pts',(4.37035536258719,3.9884739647145,8.64441326595538));
#15565=CARTESIAN_POINT('Ctrl Pts',(4.48189769988042,3.86625186767748,8.63662498767979));
#15566=CARTESIAN_POINT('Ctrl Pts',(4.58830269342953,3.73935540464159,8.62883670940421));
#15567=CARTESIAN_POINT('Ctrl Pts',(4.68919284601521,3.60824070917944,8.62104843112862));
#15568=CARTESIAN_POINT('Ctrl Pts',(4.78510921174593,3.48358984127697,8.61364410743252));
#15569=CARTESIAN_POINT('Ctrl Pts',(4.87604123022314,3.35512684063529,8.60623978373641));
#15570=CARTESIAN_POINT('Ctrl Pts',(4.96169955605135,3.22326978051479,8.5988354600403));
#15571=CARTESIAN_POINT('Ctrl Pts',(5.05179625684668,3.08458056404265,8.59104748227878));
#15572=CARTESIAN_POINT('Ctrl Pts',(5.13609047328364,2.94208661260913,8.58325950451725));
#15573=CARTESIAN_POINT('Ctrl Pts',(5.2142756628893,2.79629395341411,8.57547152675572));
#15574=CARTESIAN_POINT('Ctrl Pts',(5.29244548061638,2.65052995830582,8.56768508017739));
#15575=CARTESIAN_POINT('Ctrl Pts',(5.36450851710577,2.50146883093088,8.55989863359906));
#15576=CARTESIAN_POINT('Ctrl Pts',(5.4302039262082,2.34964164976131,8.55211218702073));
#15577=CARTESIAN_POINT('Ctrl Pts',(5.49590184144239,2.19780867672704,8.54432544340701));
#15578=CARTESIAN_POINT('Ctrl Pts',(5.55523151269775,2.04320973044566,8.5365386997933));
#15579=CARTESIAN_POINT('Ctrl Pts',(5.60797974468834,1.88639702758071,8.52875195617958));
#15580=CARTESIAN_POINT('Ctrl Pts',(5.66072448777801,1.72959469670288,8.5209657276007));
#15581=CARTESIAN_POINT('Ctrl Pts',(5.70688856094828,1.57057920519222,8.51317949902182));
#15582=CARTESIAN_POINT('Ctrl Pts',(5.74630822459167,1.40991927091238,8.50539327044294));
#15583=CARTESIAN_POINT('Ctrl Pts',(5.7857382653199,1.24921704348203,8.49760499216736));
#15584=CARTESIAN_POINT('Ctrl Pts',(5.81842027071806,1.08686981835545,8.48981671389178));
#15585=CARTESIAN_POINT('Ctrl Pts',(5.84424113584269,0.92345877472909,8.4820284356162));
#15586=CARTESIAN_POINT('Ctrl Pts',(5.8687890573129,0.768103737361335,8.47462411192006));
#15587=CARTESIAN_POINT('Ctrl Pts',(5.88713599670188,0.611787505531511,8.46721978822393));
#15588=CARTESIAN_POINT('Ctrl Pts',(5.89922802781789,0.455015646223092,8.45981546452779));
#15589=CARTESIAN_POINT('Ctrl Pts',(5.91194660594708,0.290120673497471,8.45202748676627));
#15590=CARTESIAN_POINT('Ctrl Pts',(5.91774942167743,0.124662617031762,8.44423950900474));
#15591=CARTESIAN_POINT('Ctrl Pts',(5.91660955052299,-0.0407675012736267,
8.43645153124322));
#15592=CARTESIAN_POINT('Ctrl Pts',(5.915469903477,-0.206165094599524,8.4286650846649));
#15593=CARTESIAN_POINT('Ctrl Pts',(5.9073902953071,-0.371534441378662,8.42087863808657));
#15594=CARTESIAN_POINT('Ctrl Pts',(5.89239591395816,-0.536284398122123,
8.41309219150824));
#15595=CARTESIAN_POINT('Ctrl Pts',(5.87740096060738,-0.701040639705004,
8.40530544789454));
#15596=CARTESIAN_POINT('Ctrl Pts',(5.85549073126761,-0.865177125389408,
8.39751870428083));
#15597=CARTESIAN_POINT('Ctrl Pts',(5.82674236932942,-1.02810696134276,8.38973196066712));
#15598=CARTESIAN_POINT('Ctrl Pts',(5.79799590888029,-1.19102602070637,8.38194573208824));
#15599=CARTESIAN_POINT('Ctrl Pts',(5.76241227657733,-1.35273827535683,8.37415950350937));
#15600=CARTESIAN_POINT('Ctrl Pts',(5.72011993630161,-1.51266601628543,8.3663732749305));
#15601=CARTESIAN_POINT('Ctrl Pts',(5.67781646271926,-1.67263585761727,8.35858499665492));
#15602=CARTESIAN_POINT('Ctrl Pts',(5.62880083209673,-1.83081993689766,8.35079671837935));
#15603=CARTESIAN_POINT('Ctrl Pts',(5.57325193019818,-1.98665384127237,8.34300844010378));
#15604=CARTESIAN_POINT('Ctrl Pts',(5.52044153538815,-2.13480528501913,8.33560411640761));
#15605=CARTESIAN_POINT('Ctrl Pts',(5.46172660855925,-2.28083244648607,8.32819979271144));
#15606=CARTESIAN_POINT('Ctrl Pts',(5.39730180110787,-2.42426562700082,8.32079546901528));
#15607=CARTESIAN_POINT('Ctrl Pts',(5.3295388306719,-2.57513077903245,8.31300749125375));
#15608=CARTESIAN_POINT('Ctrl Pts',(5.25543431630152,-2.72317996704022,8.30521951349223));
#15609=CARTESIAN_POINT('Ctrl Pts',(5.17524752126884,-2.86788138808089,8.2974315357307));
#15610=CARTESIAN_POINT('Ctrl Pts',(5.09507649164752,-3.01255435958162,8.28964508915237));
#15611=CARTESIAN_POINT('Ctrl Pts',(5.00882572218651,-3.15388059808576,8.28185864257405));
#15612=CARTESIAN_POINT('Ctrl Pts',(4.91680028888243,-3.29135313841368,8.27407219599572));
#15613=CARTESIAN_POINT('Ctrl Pts',(4.82477134501554,-3.42883092300911,8.26628545238201));
#15614=CARTESIAN_POINT('Ctrl Pts',(4.72696747096683,-3.56245444752342,8.25849870876829));
#15615=CARTESIAN_POINT('Ctrl Pts',(4.623737325253,-3.691745347334,8.25071196515458));
#15616=CARTESIAN_POINT('Ctrl Pts',(4.52051400744109,-3.82102769551873,8.24292573657571));
#15617=CARTESIAN_POINT('Ctrl Pts',(4.41186533567916,-3.94597774280306,8.23513950799683));
#15618=CARTESIAN_POINT('Ctrl Pts',(4.29818063121219,-4.06614975424816,8.22735327941796));
#15619=CARTESIAN_POINT('Ctrl Pts',(4.18446599965516,-4.18635340054358,8.21956500114239));
#15620=CARTESIAN_POINT('Ctrl Pts',(4.06571290465907,-4.30177626401508,8.21177672286681));
#15621=CARTESIAN_POINT('Ctrl Pts',(3.94234857326351,-4.41200841900684,8.20398844459124));
#15622=CARTESIAN_POINT('Ctrl Pts',(3.82506598398084,-4.51680623546958,8.19658412089507));
#15623=CARTESIAN_POINT('Ctrl Pts',(3.70361606165273,-4.61691263329247,8.18917979719891));
#15624=CARTESIAN_POINT('Ctrl Pts',(3.57839453890219,-4.71200839201873,8.18177547350275));
#15625=CARTESIAN_POINT('Ctrl Pts',(3.44668467930316,-4.81203152506474,8.17398749574121));
#15626=CARTESIAN_POINT('Ctrl Pts',(3.31075487724238,-4.90654676209905,8.16619951797967));
#15627=CARTESIAN_POINT('Ctrl Pts',(3.17108732161921,-4.99521128293548,8.15841154021814));
#15628=CARTESIAN_POINT('Ctrl Pts',(3.03144722583491,-5.08385837156695,8.1506250936398));
#15629=CARTESIAN_POINT('Ctrl Pts',(2.8880711123933,-5.16665686803163,8.14283864706146));
#15630=CARTESIAN_POINT('Ctrl Pts',(2.74146950457276,-5.24330768866348,8.13505220048312));
#15631=CARTESIAN_POINT('Ctrl Pts',(2.59486230423139,-5.31996143335133,8.12726545686939));
#15632=CARTESIAN_POINT('Ctrl Pts',(2.44502964463216,-5.39046688136825,8.11947871325567));
#15633=CARTESIAN_POINT('Ctrl Pts',(2.29250662419488,-5.45457092176118,8.11169196964195));
#15634=CARTESIAN_POINT('Ctrl Pts',(2.13999369201428,-5.51867072215144,8.10390574106306));
#15635=CARTESIAN_POINT('Ctrl Pts',(1.98479104975206,-5.57636983849608,8.09611951248417));
#15636=CARTESIAN_POINT('Ctrl Pts',(1.82745387879159,-5.62746327250472,8.08833328390528));
#15637=CARTESIAN_POINT('Ctrl Pts',(1.67007528938611,-5.67857015667632,8.08054500562969));
#15638=CARTESIAN_POINT('Ctrl Pts',(1.5105613519986,-5.72306778315643,8.0727567273541));
#15639=CARTESIAN_POINT('Ctrl Pts',(1.349483388428,-5.76080073833984,8.06496844907851));
#15640=CARTESIAN_POINT('Ctrl Pts',(1.19634641252904,-5.7966734953603,8.05756412538242));
#15641=CARTESIAN_POINT('Ctrl Pts',(1.04179616223938,-5.82643243777275,8.05015980168633));
#15642=CARTESIAN_POINT('Ctrl Pts',(0.886332889760116,-5.84998671545752,
8.04275547799024));
#15643=CARTESIAN_POINT('Ctrl Pts',(0.722814308118198,-5.87476145496474,
8.03496750022871));
#15644=CARTESIAN_POINT('Ctrl Pts',(0.558227082250128,-5.89268033330261,
8.02717952246719));
#15645=CARTESIAN_POINT('Ctrl Pts',(0.393158669071448,-5.90367316366971,
8.01939154470566));
#15646=CARTESIAN_POINT('Ctrl Pts',(0.228122709757993,-5.91466383275213,
8.01160509812734));
#15647=CARTESIAN_POINT('Ctrl Pts',(0.062606070547979,-5.91873114967639,
8.00381865154901));
#15648=CARTESIAN_POINT('Ctrl Pts',(-0.102799849404808,-5.9158568908876,
7.99603220497068));
#15649=CARTESIAN_POINT('Ctrl Pts',(-0.268212079220525,-5.91298252245233,
7.98824546135697));
#15650=CARTESIAN_POINT('Ctrl Pts',(-0.433513261767925,-5.90316605002174,
7.98045871774326));
#15651=CARTESIAN_POINT('Ctrl Pts',(-0.598112426644313,-5.8864413772324,
7.97267197412955));
#15652=CARTESIAN_POINT('Ctrl Pts',(-0.762700704517325,-5.86971781065504,
7.96488574555067));
#15653=CARTESIAN_POINT('Ctrl Pts',(-0.926586739710877,-5.84608699051395,
7.9570995169718));
#15654=CARTESIAN_POINT('Ctrl Pts',(-1.08918495901314,-5.8156346762464,7.94931328839293));
#15655=CARTESIAN_POINT('Ctrl Pts',(-1.25182598171256,-5.7851743455165,7.94152501011735));
#15656=CARTESIAN_POINT('Ctrl Pts',(-1.41317819644302,-5.74788898934669,
7.93373673184177));
#15657=CARTESIAN_POINT('Ctrl Pts',(-1.57266559333533,-5.70391562823638,
7.92594845356619));
#15658=CARTESIAN_POINT('Ctrl Pts',(-1.72429041595515,-5.6621101112597,7.91854412987003));
#15659=CARTESIAN_POINT('Ctrl Pts',(-1.87422960504385,-5.61426019909701,
7.91113980617387));
#15660=CARTESIAN_POINT('Ctrl Pts',(-2.02200045401077,-5.56052558005808,
7.90373548247772));
#15661=CARTESIAN_POINT('Ctrl Pts',(-2.17742803021923,-5.50400670875095,
7.89594750471619));
#15662=CARTESIAN_POINT('Ctrl Pts',(-2.33051219542683,-5.44095689128444,
7.88815952695465));
#15663=CARTESIAN_POINT('Ctrl Pts',(-2.48070356847719,-5.3715957003338,7.88037154919312));
#15664=CARTESIAN_POINT('Ctrl Pts',(-2.63086541261569,-5.30224814638808,
7.87258510261481));
#15665=CARTESIAN_POINT('Ctrl Pts',(-2.77813530948668,-5.2265918287544,7.86479865603649));
#15666=CARTESIAN_POINT('Ctrl Pts',(-2.92198528977122,-5.14489383066945,
7.85701220945817));
#15667=CARTESIAN_POINT('Ctrl Pts',(-3.06584075760832,-5.06319271598999,
7.84922546584446));
#15668=CARTESIAN_POINT('Ctrl Pts',(-3.20627576799496,-4.97544961403753,
7.84143872223075));
#15669=CARTESIAN_POINT('Ctrl Pts',(-3.34278767963744,-4.88197717030346,
7.83365197861705));
#15670=CARTESIAN_POINT('Ctrl Pts',(-3.47929056203824,-4.78851090907225,
7.82586575003817));
#15671=CARTESIAN_POINT('Ctrl Pts',(-3.61187060133811,-4.68931624504618,
7.8180795214593));
#15672=CARTESIAN_POINT('Ctrl Pts',(-3.74005471663466,-4.58474876946151,
7.81029329288043));
#15673=CARTESIAN_POINT('Ctrl Pts',(-3.86827257593912,-4.4801537668645,7.80250501460485));
#15674=CARTESIAN_POINT('Ctrl Pts',(-3.99209194987532,-4.37018332710374,
7.79471673632928));
#15675=CARTESIAN_POINT('Ctrl Pts',(-4.11107269111636,-4.25523347078128,
7.7869284580537));
#15676=CARTESIAN_POINT('Ctrl Pts',(-4.22418779699555,-4.14595053109636,
7.77952413435753));
#15677=CARTESIAN_POINT('Ctrl Pts',(-4.33292966830714,-4.03216749219219,
7.77211981066136));
#15678=CARTESIAN_POINT('Ctrl Pts',(-4.43695092800242,-3.91425561569482,
7.7647154869652));
#15679=CARTESIAN_POINT('Ctrl Pts',(-4.54636203568433,-3.79023415071524,
7.75692750920367));
#15680=CARTESIAN_POINT('Ctrl Pts',(-4.65058948652761,-3.66160025311989,
7.74913953144214));
#15681=CARTESIAN_POINT('Ctrl Pts',(-4.74925602814725,-3.5288096777252,7.74135155368061));
#15682=CARTESIAN_POINT('Ctrl Pts',(-4.84790317107891,-3.39604521009608,
7.73356510710228));
#15683=CARTESIAN_POINT('Ctrl Pts',(-4.94099139582116,-3.25912595163801,
7.72577866052395));
#15684=CARTESIAN_POINT('Ctrl Pts',(-5.02818499125749,-3.11853912211999,
7.71799221394562));
#15685=CARTESIAN_POINT('Ctrl Pts',(-5.11538191293291,-2.97794692953138,
7.7102054703319));
#15686=CARTESIAN_POINT('Ctrl Pts',(-5.19668358356026,-2.8336871553884,7.70241872671819));
#15687=CARTESIAN_POINT('Ctrl Pts',(-5.27179833909937,-2.68627489925532,
7.69463198310447));
#15688=CARTESIAN_POINT('Ctrl Pts',(-5.3469081263593,-2.53887239334023,7.6868457545256));
#15689=CARTESIAN_POINT('Ctrl Pts',(-5.41583167244711,-2.38831810749391,
7.67905952594672));
#15690=CARTESIAN_POINT('Ctrl Pts',(-5.47832382396314,-2.23515069789441,
7.67127329736785));
#15691=CARTESIAN_POINT('Ctrl Pts',(-5.54083242631362,-2.08194296752444,
7.66348501909227));
#15692=CARTESIAN_POINT('Ctrl Pts',(-5.59690612843184,-1.92612103417125,
7.65569674081668));
#15693=CARTESIAN_POINT('Ctrl Pts',(-5.64634804469368,-1.76824328662202,
7.6479084625411));
#15694=CARTESIAN_POINT('Ctrl Pts',(-5.69335252234669,-1.61814875919138,
7.64050413884496));
#15695=CARTESIAN_POINT('Ctrl Pts',(-5.73436326555133,-1.46619648556496,
7.63309981514882));
#15696=CARTESIAN_POINT('Ctrl Pts',(-5.76925298933626,-1.31287871013838,
7.62569549145268));
#15697=CARTESIAN_POINT('Ctrl Pts',(-5.80662370099699,-1.14865859726936,
7.61776465062411));
#15698=CARTESIAN_POINT('Ctrl Pts',(-5.83698281989535,-0.982822746918895,
7.60983380979554));
#15699=CARTESIAN_POINT('Ctrl Pts',(-5.86021483926551,-0.815973406522722,
7.60190296896697));
#15700=CARTESIAN_POINT('Ctrl Pts',(-5.88344102365571,-0.649165972193497,
7.59397412005725));
#15701=CARTESIAN_POINT('Ctrl Pts',(-5.89954364132265,-0.481345846958705,
7.58604527114753));
#15702=CARTESIAN_POINT('Ctrl Pts',(-5.90845873389386,-0.313122902984345,
7.57811642223781));
#15703=CARTESIAN_POINT('Ctrl Pts',(-5.91398368173311,-0.208870144709672,
7.57320267890856));
#15704=CARTESIAN_POINT('Ctrl Pts',(-5.9167491721295,-0.104462820545378,
7.56828893557931));
#15705=CARTESIAN_POINT('Ctrl Pts',(-5.91674999981411,-4.6900922432644E-5,
7.56337519225006));
#15706=CARTESIAN_POINT('Ctrl Pts',(-5.9163616306653,-0.000102807950176053,
7.3116248177821));
#15707=CARTESIAN_POINT('Ctrl Pts',(-5.91659180076628,-0.372163743325732,
7.32913601855862));
#15708=CARTESIAN_POINT('Ctrl Pts',(-5.79067067213347,-1.72813661589886,
7.39296268109683));
#15709=CARTESIAN_POINT('Ctrl Pts',(-4.76676170732884,-3.91409292922659,
7.50310480539682));
#15710=CARTESIAN_POINT('Ctrl Pts',(-2.31316218083295,-5.71764124077766,
7.64205119068191));
#15711=CARTESIAN_POINT('Ctrl Pts',(0.704280682558441,-6.12748964529958,
7.78099757596707));
#15712=CARTESIAN_POINT('Ctrl Pts',(3.55005206806716,-5.04373581257866,7.91994396125215));
#15713=CARTESIAN_POINT('Ctrl Pts',(5.53048282990672,-2.73054945041935,8.05889034653732));
#15714=CARTESIAN_POINT('Ctrl Pts',(6.16283436094425,0.24822020997984,8.19783673182242));
#15715=CARTESIAN_POINT('Ctrl Pts',(5.29296822665717,3.16648511518309,8.33678311710757));
#15716=CARTESIAN_POINT('Ctrl Pts',(3.13291807858667,5.31290550884743,8.47572950239266));
#15717=CARTESIAN_POINT('Ctrl Pts',(0.209205530063851,6.16428208952746,8.61467588767782));
#15718=CARTESIAN_POINT('Ctrl Pts',(-2.76550177582862,5.51308811474716,8.75362227296292));
#15719=CARTESIAN_POINT('Ctrl Pts',(-5.06610600222509,3.51805494660003,8.89256865824806));
#15720=CARTESIAN_POINT('Ctrl Pts',(-5.85356588340937,1.41028719109854,8.99523616985879));
#15721=CARTESIAN_POINT('Ctrl Pts',(-5.91701383422643,0.213355077629451,
9.05158821970782));
#15722=CARTESIAN_POINT('Ctrl Pts',(-5.91679358169284,0.000152125488236412,
9.06162480779513));
#15723=CARTESIAN_POINT('Origin',(0.,0.,0.));
#15724=CARTESIAN_POINT('',(-5.91662392833365,-0.000151321579282548,11.0633751922049));
#15725=CARTESIAN_POINT('',(-5.91674999820671,-0.000145674166851941,10.811624807754));
#15726=CARTESIAN_POINT('',(-5.91675,-7.2459289488551E-16,0.));
#15727=CARTESIAN_POINT('Ctrl Pts',(-5.91662392833365,-0.000151321579282548,
11.0633751922049));
#15728=CARTESIAN_POINT('Ctrl Pts',(-5.91592640289124,0.716489165398392,
11.029641922721));
#15729=CARTESIAN_POINT('Ctrl Pts',(-5.60646173926398,2.4181775648746,10.9495686547327));
#15730=CARTESIAN_POINT('Ctrl Pts',(-4.01268187007679,4.6844298163471,10.8231553882407));
#15731=CARTESIAN_POINT('Ctrl Pts',(-1.28083654461856,6.03365198206632,10.6841353927279));
#15732=CARTESIAN_POINT('Ctrl Pts',(1.76354224681853,5.91061902328436,10.5451153972156));
#15733=CARTESIAN_POINT('Ctrl Pts',(4.37760385757118,4.34535187998648,10.406095401703));
#15734=CARTESIAN_POINT('Ctrl Pts',(5.92349817403787,1.71978716034709,10.2670754061905));
#15735=CARTESIAN_POINT('Ctrl Pts',(6.02401569919722,-1.32541817949976,10.128055410678));
#15736=CARTESIAN_POINT('Ctrl Pts',(4.65462942321255,-4.04721180904692,9.98903541516539));
#15737=CARTESIAN_POINT('Ctrl Pts',(2.14947959285796,-5.78145621574806,9.85001541965299));
#15738=CARTESIAN_POINT('Ctrl Pts',(-0.880158947650844,-6.10498310575821,
9.71099542414042));
#15739=CARTESIAN_POINT('Ctrl Pts',(-3.69503228047053,-4.9388495564256,9.57197542862794));
#15740=CARTESIAN_POINT('Ctrl Pts',(-5.51911104469368,-2.67812797647235,
9.43943535444122));
#15741=CARTESIAN_POINT('Ctrl Pts',(-5.9162401127627,-0.846510755967147,
9.35323527875873));
#15742=CARTESIAN_POINT('Ctrl Pts',(-5.91702658122213,0.000123612389871874,
9.31337520158039));
#15743=CARTESIAN_POINT('Ctrl Pts',(-5.91674999804438,0.000152124367665733,
9.06162480779513));
#15744=CARTESIAN_POINT('Ctrl Pts',(-5.9167542351693,-0.164647303984843,
9.06938284393673));
#15745=CARTESIAN_POINT('Ctrl Pts',(-5.90986888391126,-0.329469705868361,
9.07714088007834));
#15746=CARTESIAN_POINT('Ctrl Pts',(-5.89611425490407,-0.493727916586623,
9.08489891621994));
#15747=CARTESIAN_POINT('Ctrl Pts',(-5.88235943528536,-0.657988403593735,
9.09265705987234));
#15748=CARTESIAN_POINT('Ctrl Pts',(-5.86173517019319,-0.821684360345096,
9.10041520352474));
#15749=CARTESIAN_POINT('Ctrl Pts',(-5.83431375174233,-0.984232497294403,
9.10817334717714));
#15750=CARTESIAN_POINT('Ctrl Pts',(-5.80689385051353,-1.146771640485,9.11593106157288));
#15751=CARTESIAN_POINT('Ctrl Pts',(-5.77267760299697,-1.30816277131651,
9.12368877596861));
#15752=CARTESIAN_POINT('Ctrl Pts',(-5.73178868066648,-1.4678314217524,9.13144649036434));
#15753=CARTESIAN_POINT('Ctrl Pts',(-5.69088963594573,-1.62753959948071,
9.13920612524631));
#15754=CARTESIAN_POINT('Ctrl Pts',(-5.64331469579614,-1.78552413041893,
9.14696576012827));
#15755=CARTESIAN_POINT('Ctrl Pts',(-5.5892380063774,-1.941223601383,9.15472539501024));
#15756=CARTESIAN_POINT('Ctrl Pts',(-5.55268333914261,-2.04647306119465,
9.15997073961293));
#15757=CARTESIAN_POINT('Ctrl Pts',(-5.51315876414372,-2.1506786540877,9.16521608421562));
#15758=CARTESIAN_POINT('Ctrl Pts',(-5.47073076945238,-2.25367154010229,
9.17046142881831));
#15759=CARTESIAN_POINT('Ctrl Pts',(-5.40773510875417,-2.40659191611593,
9.17824954021127));
#15760=CARTESIAN_POINT('Ctrl Pts',(-5.33831243462539,-2.55689661293207,
9.18603765160423));
#15761=CARTESIAN_POINT('Ctrl Pts',(-5.26270520986413,-2.70404593832444,
9.1938257629972));
#15762=CARTESIAN_POINT('Ctrl Pts',(-5.18711282926339,-2.85116637351204,
9.20161234533026));
#15763=CARTESIAN_POINT('Ctrl Pts',(-5.1053384667167,-2.99513238933499,9.20939892766332));
#15764=CARTESIAN_POINT('Ctrl Pts',(-5.01767115424125,-3.13542768221423,
9.21718550999638));
#15765=CARTESIAN_POINT('Ctrl Pts',(-4.93000049903071,-3.27572832452172,
9.22497238923009));
#15766=CARTESIAN_POINT('Ctrl Pts',(-4.83643661024355,-3.4123576907616,9.2327592684638));
#15767=CARTESIAN_POINT('Ctrl Pts',(-4.73731297790831,-3.54482669701094,
9.24054614769751));
#15768=CARTESIAN_POINT('Ctrl Pts',(-4.6381958876755,-3.67728696038244,9.2483325130017));
#15769=CARTESIAN_POINT('Ctrl Pts',(-4.53351997974197,-3.8055871574595,9.25611887830588));
#15770=CARTESIAN_POINT('Ctrl Pts',(-4.42366041050591,-3.92926954216973,
9.26390524361006));
#15771=CARTESIAN_POINT('Ctrl Pts',(-4.313771994378,-4.05298440336243,9.27169365345564));
#15772=CARTESIAN_POINT('Ctrl Pts',(-4.19869740802239,-4.17207878893119,
9.27948206330123));
#15773=CARTESIAN_POINT('Ctrl Pts',(-4.07885081761466,-4.28612955592155,
9.28727047314682));
#15774=CARTESIAN_POINT('Ctrl Pts',(-3.96530240028921,-4.3941867317031,9.29464958679902));
#15775=CARTESIAN_POINT('Ctrl Pts',(-3.84747082336385,-4.49771657914358,
9.30202870045123));
#15776=CARTESIAN_POINT('Ctrl Pts',(-3.7257376286415,-4.5963909412739,9.30940781410344));
#15777=CARTESIAN_POINT('Ctrl Pts',(-3.59725720058452,-4.7005344685482,9.31719592549638));
#15778=CARTESIAN_POINT('Ctrl Pts',(-3.46438449849465,-4.79930619834674,
9.32498403688933));
#15779=CARTESIAN_POINT('Ctrl Pts',(-3.32759064228207,-4.89234821735911,
9.33277214828227));
#15780=CARTESIAN_POINT('Ctrl Pts',(-3.19082364315839,-4.98537196919307,
9.34055873061532));
#15781=CARTESIAN_POINT('Ctrl Pts',(-3.05013729003561,-5.07266807521593,
9.34834531294836));
#15782=CARTESIAN_POINT('Ctrl Pts',(-2.90603240636465,-5.15392144057886,
9.3561318952814));
#15783=CARTESIAN_POINT('Ctrl Pts',(-2.76192202800644,-5.2351779041146,9.36391877451511));
#15784=CARTESIAN_POINT('Ctrl Pts',(-2.61439313465634,-5.31039100557254,
9.37170565374881));
#15785=CARTESIAN_POINT('Ctrl Pts',(-2.46397256651647,-5.37929082258565,
9.37949253298251));
#15786=CARTESIAN_POINT('Ctrl Pts',(-2.31356192604721,-5.44818609225064,
9.38727889828668));
#15787=CARTESIAN_POINT('Ctrl Pts',(-2.1602602832813,-5.51076877833009,9.39506526359085));
#15788=CARTESIAN_POINT('Ctrl Pts',(-2.00461607347838,-5.56681641159937,
9.40285162889502));
#15789=CARTESIAN_POINT('Ctrl Pts',(-1.84893099466638,-5.62287876183909,
9.41064003874062));
#15790=CARTESIAN_POINT('Ctrl Pts',(-1.69090241986903,-5.67240252024348,
9.41842844858621));
#15791=CARTESIAN_POINT('Ctrl Pts',(-1.53109648437006,-5.71521426702881,
9.4262168584318));
#15792=CARTESIAN_POINT('Ctrl Pts',(-1.37968866380985,-5.75577617266081,
9.43359597208405));
#15793=CARTESIAN_POINT('Ctrl Pts',(-1.22668573656425,-5.79031331334059,
9.44097508573631));
#15794=CARTESIAN_POINT('Ctrl Pts',(-1.07257974506573,-5.81872006999604,
9.44835419938856));
#15795=CARTESIAN_POINT('Ctrl Pts',(-0.90993221249251,-5.84870131104637,
9.45614231078154));
#15796=CARTESIAN_POINT('Ctrl Pts',(-0.745997781172773,-5.87186403532856,
9.46393042217451));
#15797=CARTESIAN_POINT('Ctrl Pts',(-0.581361390602742,-5.88811935137328,
9.47171853356749));
#15798=CARTESIAN_POINT('Ctrl Pts',(-0.416757323518033,-5.90437147597006,
9.47950511590056));
#15799=CARTESIAN_POINT('Ctrl Pts',(-0.251451889955782,-5.91371886687374,
9.48729169823363));
#15800=CARTESIAN_POINT('Ctrl Pts',(-0.0860356269073524,-5.9161244437049,
9.4950782805667));
#15801=CARTESIAN_POINT('Ctrl Pts',(0.0793869434263262,-5.91853011226017,
9.50286515980042));
#15802=CARTESIAN_POINT('Ctrl Pts',(0.24492003227762,-5.9139934285044,9.51065203903415));
#15803=CARTESIAN_POINT('Ctrl Pts',(0.40997186886024,-5.90252942637673,9.51843891826787));
#15804=CARTESIAN_POINT('Ctrl Pts',(0.575012812117128,-5.89106618086658,
9.52622528357206));
#15805=CARTESIAN_POINT('Ctrl Pts',(0.739572247889583,-5.87267655416949,
9.53401164887625));
#15806=CARTESIAN_POINT('Ctrl Pts',(0.903062145535117,-5.84742758174922,
9.54179801418045));
#15807=CARTESIAN_POINT('Ctrl Pts',(1.0665949723077,-5.82217197946154,9.54958642402605));
#15808=CARTESIAN_POINT('Ctrl Pts',(1.22905738348968,-5.79005347931028,9.55737483387165));
#15809=CARTESIAN_POINT('Ctrl Pts',(1.38986927262554,-5.75119065650856,9.56516324371726));
#15810=CARTESIAN_POINT('Ctrl Pts',(1.54223018198633,-5.71437015117021,9.57254235736941));
#15811=CARTESIAN_POINT('Ctrl Pts',(1.69310933092947,-5.67149600691549,9.57992147102155));
#15812=CARTESIAN_POINT('Ctrl Pts',(1.84202411387482,-5.6227108876772,9.5873005846737));
#15813=CARTESIAN_POINT('Ctrl Pts',(1.99919270786961,-5.57122178466877,9.59508869606666));
#15814=CARTESIAN_POINT('Ctrl Pts',(2.15422913816093,-5.51312948870221,9.60287680745961));
#15815=CARTESIAN_POINT('Ctrl Pts',(2.30657722721143,-5.44863579783138,9.61066491885257));
#15816=CARTESIAN_POINT('Ctrl Pts',(2.45889540537103,-5.38415476917223,9.61845150118565));
#15817=CARTESIAN_POINT('Ctrl Pts',(2.60852600135886,-5.31327497779059,9.62623808351872));
#15818=CARTESIAN_POINT('Ctrl Pts',(2.75493271060179,-5.23624639628009,9.6340246658518));
#15819=CARTESIAN_POINT('Ctrl Pts',(2.90134500229945,-5.15921487768719,9.6418115450855));
#15820=CARTESIAN_POINT('Ctrl Pts',(3.04453287667135,-5.07603424510427,9.6495984243192));
#15821=CARTESIAN_POINT('Ctrl Pts',(3.18398387904865,-4.98700082418865,9.65738530355291));
#15822=CARTESIAN_POINT('Ctrl Pts',(3.32342567774074,-4.89797327942714,9.6651716688571));
#15823=CARTESIAN_POINT('Ctrl Pts',(3.45913082870976,-4.80309389140064,9.67295803416129));
#15824=CARTESIAN_POINT('Ctrl Pts',(3.59061504095564,-4.70270286007559,9.68074439946549));
#15825=CARTESIAN_POINT('Ctrl Pts',(3.72213377828536,-4.60228546810454,9.68853280931108));
#15826=CARTESIAN_POINT('Ctrl Pts',(3.84942910690183,-4.49635373342895,9.69632121915667));
#15827=CARTESIAN_POINT('Ctrl Pts',(3.97204835264803,-4.38528932303515,9.70410962900226));
#15828=CARTESIAN_POINT('Ctrl Pts',(4.08822371684238,-4.2800615649617,9.71148874265444));
#15829=CARTESIAN_POINT('Ctrl Pts',(4.20020163905907,-4.17022689480854,9.71886785630663));
#15830=CARTESIAN_POINT('Ctrl Pts',(4.30762658777829,-4.05614148455963,9.72624696995881));
#15831=CARTESIAN_POINT('Ctrl Pts',(4.42100571519722,-3.9357327301737,9.73403508135178));
#15832=CARTESIAN_POINT('Ctrl Pts',(4.52935334063389,-3.81054566362723,9.74182319274476));
#15833=CARTESIAN_POINT('Ctrl Pts',(4.63227761920229,-3.68102358334439,9.74961130413774));
#15834=CARTESIAN_POINT('Ctrl Pts',(4.73518169038258,-3.55152693246442,9.75739788647079));
#15835=CARTESIAN_POINT('Ctrl Pts',(4.83266434057913,-3.41769721606165,9.76518446880384));
#15836=CARTESIAN_POINT('Ctrl Pts',(4.92437422420804,-3.28001052779644,9.77297105113689));
#15837=CARTESIAN_POINT('Ctrl Pts',(5.01608760471454,-3.14231858956823,9.78075793037061));
#15838=CARTESIAN_POINT('Ctrl Pts',(5.1020275977916,-3.00076964893625,9.78854480960432));
#15839=CARTESIAN_POINT('Ctrl Pts',(5.18188597794096,-2.8558690926089,9.79633168883804));
#15840=CARTESIAN_POINT('Ctrl Pts',(5.26173908748337,-2.71097809963459,9.80411805414223));
#15841=CARTESIAN_POINT('Ctrl Pts',(5.33551123318978,-2.56273621355105,9.81190441944641));
#15842=CARTESIAN_POINT('Ctrl Pts',(5.40293991173904,-2.41167387360674,9.81969078475059));
#15843=CARTESIAN_POINT('Ctrl Pts',(5.47038629568999,-2.26057186775961,9.82747919459619));
#15844=CARTESIAN_POINT('Ctrl Pts',(5.53148575203806,-2.10664821937205,9.83526760444178));
#15845=CARTESIAN_POINT('Ctrl Pts',(5.58602338021825,-1.95045465421657,9.84305601428737));
#15846=CARTESIAN_POINT('Ctrl Pts',(5.63769494920871,-1.80246936686354,9.85043512793956));
#15847=CARTESIAN_POINT('Ctrl Pts',(5.68347653938985,-1.65244684911322,9.85781424159176));
#15848=CARTESIAN_POINT('Ctrl Pts',(5.72322635565564,-1.5008699625313,9.86519335524395));
#15849=CARTESIAN_POINT('Ctrl Pts',(5.76517936133073,-1.34089171406683,9.87298146663691));
#15850=CARTESIAN_POINT('Ctrl Pts',(5.80042797722494,-1.17912476859988,9.88076957802986));
#15851=CARTESIAN_POINT('Ctrl Pts',(5.82884020499789,-1.01614586900707,9.88855768942282));
#15852=CARTESIAN_POINT('Ctrl Pts',(5.85724685452527,-0.853198967479796,
9.89634427175589));
#15853=CARTESIAN_POINT('Ctrl Pts',(5.87881973918856,-0.689040901186373,
9.90413085408895));
#15854=CARTESIAN_POINT('Ctrl Pts',(5.89347811440653,-0.524257834954607,
9.91191743642202));
#15855=CARTESIAN_POINT('Ctrl Pts',(5.90813704854507,-0.359468485581343,
9.91970431565573));
#15856=CARTESIAN_POINT('Ctrl Pts',(5.91588091343333,-0.194054406492899,
9.92749119488943));
#15857=CARTESIAN_POINT('Ctrl Pts',(5.91668084404873,-0.0286068552416584,
9.93527807412314));
#15858=CARTESIAN_POINT('Ctrl Pts',(5.91748072186918,0.136829776566631,9.94306443942731));
#15859=CARTESIAN_POINT('Ctrl Pts',(5.9113375811097,0.302299556566704,9.95085080473149));
#15860=CARTESIAN_POINT('Ctrl Pts',(5.89827469245367,0.467211103100703,9.95863717003566));
#15861=CARTESIAN_POINT('Ctrl Pts',(5.88520837374833,0.632165952058229,9.96642557988126));
#15862=CARTESIAN_POINT('Ctrl Pts',(5.86521869974376,0.796561955757151,9.97421398972685));
#15863=CARTESIAN_POINT('Ctrl Pts',(5.8383809264139,0.959811815194203,9.98200239957245));
#15864=CARTESIAN_POINT('Ctrl Pts',(5.81295353064259,1.11448257474256,9.98938151322465));
#15865=CARTESIAN_POINT('Ctrl Pts',(5.78137932716879,1.26812429924061,9.99676062687685));
#15866=CARTESIAN_POINT('Ctrl Pts',(5.74376482047373,1.42024513714652,10.0041397405291));
#15867=CARTESIAN_POINT('Ctrl Pts',(5.70406547690208,1.58079748620148,10.011927851922));
#15868=CARTESIAN_POINT('Ctrl Pts',(5.65762307990393,1.73971291443102,10.019715963315));
#15869=CARTESIAN_POINT('Ctrl Pts',(5.60459765285382,1.89642181808939,10.027504074708));
#15870=CARTESIAN_POINT('Ctrl Pts',(5.55158263642175,2.05309995468695,10.0352906570411));
#15871=CARTESIAN_POINT('Ctrl Pts',(5.49198727113722,2.20757212861727,10.0430772393742));
#15872=CARTESIAN_POINT('Ctrl Pts',(5.42602109526431,2.35928498410995,10.0508638217073));
#15873=CARTESIAN_POINT('Ctrl Pts',(5.36005240411601,2.51100362437956,10.058650700941));
#15874=CARTESIAN_POINT('Ctrl Pts',(5.28771254008613,2.659962441092,10.0664375801748));
#15875=CARTESIAN_POINT('Ctrl Pts',(5.20925903460248,2.80562842744945,10.0742244594085));
#15876=CARTESIAN_POINT('Ctrl Pts',(5.13081070700497,2.95128479993576,10.0820108247127));
#15877=CARTESIAN_POINT('Ctrl Pts',(5.04624969704373,3.09364849568054,10.0897971900169));
#15878=CARTESIAN_POINT('Ctrl Pts',(4.95587937707644,3.2322113424664,10.0975835553211));
#15879=CARTESIAN_POINT('Ctrl Pts',(4.86548532769812,3.37081057304227,10.1053719651667));
#15880=CARTESIAN_POINT('Ctrl Pts',(4.76927909327423,3.5056066915216,10.1131603750123));
#15881=CARTESIAN_POINT('Ctrl Pts',(4.66760774234685,3.63611998235533,10.1209487848579));
#15882=CARTESIAN_POINT('Ctrl Pts',(4.57127942006711,3.75977454410303,10.12832789851));
#15883=CARTESIAN_POINT('Ctrl Pts',(4.47004577228953,3.87958463711967,10.1357070121621));
#15884=CARTESIAN_POINT('Ctrl Pts',(4.36423564215233,3.99516931083869,10.1430861258142));
#15885=CARTESIAN_POINT('Ctrl Pts',(4.25256083690262,4.11716042748022,10.1508742372072));
#15886=CARTESIAN_POINT('Ctrl Pts',(4.13574796316561,4.23448801203535,10.1586623486001));
#15887=CARTESIAN_POINT('Ctrl Pts',(4.0142100596376,4.34672844327826,10.1664504599931));
#15888=CARTESIAN_POINT('Ctrl Pts',(3.89269601795853,4.45894683806887,10.1742370423262));
#15889=CARTESIAN_POINT('Ctrl Pts',(3.76645903207633,4.56607985574839,10.1820236246592));
#15890=CARTESIAN_POINT('Ctrl Pts',(3.63594784723766,4.66774183247829,10.1898102069922));
#15891=CARTESIAN_POINT('Ctrl Pts',(3.50543168603635,4.76940768555691,10.197597086226));
#15892=CARTESIAN_POINT('Ctrl Pts',(3.3706412494076,4.86560188079502,10.2053839654597));
#15893=CARTESIAN_POINT('Ctrl Pts',(3.23205769082457,4.95597958487338,10.2131708446934));
#15894=CARTESIAN_POINT('Ctrl Pts',(3.09348327867668,5.04635132407528,10.2209572099975));
#15895=CARTESIAN_POINT('Ctrl Pts',(2.95111651327928,5.13090716587141,10.2287435753017));
#15896=CARTESIAN_POINT('Ctrl Pts',(2.80546692033342,5.20934601667185,10.2365299406058));
#15897=CARTESIAN_POINT('Ctrl Pts',(2.65977908276168,5.28780546392192,10.2443183504514));
#15898=CARTESIAN_POINT('Ctrl Pts',(2.51080697576852,5.36014455734318,10.252106760297));
#15899=CARTESIAN_POINT('Ctrl Pts',(2.35908488099827,5.42610809759125,10.2598951701426));
#15900=CARTESIAN_POINT('Ctrl Pts',(2.21533607950236,5.48860512458951,10.2672742837948));
#15901=CARTESIAN_POINT('Ctrl Pts',(2.06911912912654,5.54537935514081,10.2746533974471));
#15902=CARTESIAN_POINT('Ctrl Pts',(1.92090505472162,5.59625359801045,10.2820325110993));
#15903=CARTESIAN_POINT('Ctrl Pts',(1.76447600702374,5.64994761726201,10.2898206224923));
#15904=CARTESIAN_POINT('Ctrl Pts',(1.60576630230671,5.69708824938458,10.2976087338852));
#15905=CARTESIAN_POINT('Ctrl Pts',(1.44534131461086,5.7375011151876,10.3053968452782));
#15906=CARTESIAN_POINT('Ctrl Pts',(1.28494782356525,5.77790604662879,10.3131834276113));
#15907=CARTESIAN_POINT('Ctrl Pts',(1.1228400311459,5.81158576929197,10.3209700099443));
#15908=CARTESIAN_POINT('Ctrl Pts',(0.959596505977468,5.8384163185076,10.3287565922774));
#15909=CARTESIAN_POINT('Ctrl Pts',(0.796346756369521,5.86524789076614,10.3365434715111));
#15910=CARTESIAN_POINT('Ctrl Pts',(0.631961502003953,5.88522971128476,10.3443303507448));
#15911=CARTESIAN_POINT('Ctrl Pts',(0.467028235148636,5.89828917484332,10.3521172299785));
#15912=CARTESIAN_POINT('Ctrl Pts',(0.302105853793364,5.91134777648486,10.3599035952827));
#15913=CARTESIAN_POINT('Ctrl Pts',(0.136635850892719,5.91748491033067,10.3676899605869));
#15914=CARTESIAN_POINT('Ctrl Pts',(-0.0287902936134475,5.91667995428971,
10.375476325891));
#15915=CARTESIAN_POINT('Ctrl Pts',(-0.194259875665475,5.91587478688363,
10.3832647357366));
#15916=CARTESIAN_POINT('Ctrl Pts',(-0.359685256566639,5.90812388676744,
10.3910531455822));
#15917=CARTESIAN_POINT('Ctrl Pts',(-0.524475175043601,5.89345877675097,
10.3988415554278));
#15918=CARTESIAN_POINT('Ctrl Pts',(-0.680605060512899,5.87956434699198,
10.40622066908));
#15919=CARTESIAN_POINT('Ctrl Pts',(-0.836164296225479,5.85946374958126,
10.4135997827322));
#15920=CARTESIAN_POINT('Ctrl Pts',(-0.990654489972888,5.83322674374969,
10.4209788963844));
#15921=CARTESIAN_POINT('Ctrl Pts',(-1.15370751974506,5.80553551501071,10.4287670077774));
#15922=CARTESIAN_POINT('Ctrl Pts',(-1.31562787500577,5.77099846070048,10.4365551191703));
#15923=CARTESIAN_POINT('Ctrl Pts',(-1.4758356587507,5.72973294934938,10.4443432305633));
#15924=CARTESIAN_POINT('Ctrl Pts',(-1.63601198849001,5.68847553976209,10.4521298128963));
#15925=CARTESIAN_POINT('Ctrl Pts',(-1.79447610836175,5.64049238860399,10.4599163952294));
#15926=CARTESIAN_POINT('Ctrl Pts',(-1.95066065498055,5.5859514473016,10.4677029775624));
#15927=CARTESIAN_POINT('Ctrl Pts',(-2.10685115688151,5.5314084263652,10.4754898567961));
#15928=CARTESIAN_POINT('Ctrl Pts',(-2.26076160864956,5.47030721655194,10.4832767360299));
#15929=CARTESIAN_POINT('Ctrl Pts',(-2.41184138301624,5.40286513857882,10.4910636152636));
#15930=CARTESIAN_POINT('Ctrl Pts',(-2.56291118620474,5.33542751174403,10.4988499805677));
#15931=CARTESIAN_POINT('Ctrl Pts',(-2.71115039410231,5.2616499845865,10.5066363458719));
#15932=CARTESIAN_POINT('Ctrl Pts',(-2.85602974833675,5.18179743323835,10.514422711176));
#15933=CARTESIAN_POINT('Ctrl Pts',(-3.00094714494784,5.10192391423162,10.5222111210216));
#15934=CARTESIAN_POINT('Ctrl Pts',(-3.14250264405843,5.01597233617464,10.5299995308672));
#15935=CARTESIAN_POINT('Ctrl Pts',(-3.28019212727181,4.92425326020951,10.5377879407128));
#15936=CARTESIAN_POINT('Ctrl Pts',(-3.41064575843563,4.83735420134605,10.545167054365));
#15937=CARTESIAN_POINT('Ctrl Pts',(-3.5376290395649,4.74527838396932,10.5525461680173));
#15938=CARTESIAN_POINT('Ctrl Pts',(-3.66073769636084,4.64832551366002,10.5599252816695));
#15939=CARTESIAN_POINT('Ctrl Pts',(-3.79066982340934,4.54599889430925,10.5677133930625));
#15940=CARTESIAN_POINT('Ctrl Pts',(-3.91633203875168,4.4382027106867,10.5755015044555));
#15941=CARTESIAN_POINT('Ctrl Pts',(-4.03727127483512,4.32531746995422,10.5832896158485));
#15942=CARTESIAN_POINT('Ctrl Pts',(-4.15818676660779,4.21245439227093,10.5910761981816));
#15943=CARTESIAN_POINT('Ctrl Pts',(-4.27438089586976,4.09450446896867,10.5988627805146));
#15944=CARTESIAN_POINT('Ctrl Pts',(-4.38543580176644,3.97188662867977,10.6066493628477));
#15945=CARTESIAN_POINT('Ctrl Pts',(-4.49649494216205,3.84926411299981,10.6144362420815));
#15946=CARTESIAN_POINT('Ctrl Pts',(-4.60241424966546,3.72197355835321,10.6222231213152));
#15947=CARTESIAN_POINT('Ctrl Pts',(-4.70281417979792,3.59046923852463,10.6300100005489));
#15948=CARTESIAN_POINT('Ctrl Pts',(-4.80320748359333,3.45897359790473,10.6377963658532));
#15949=CARTESIAN_POINT('Ctrl Pts',(-4.89808194516815,3.32326500269818,10.6455827311574));
#15950=CARTESIAN_POINT('Ctrl Pts',(-4.98709953674678,3.18382926255163,10.6533690964616));
#15951=CARTESIAN_POINT('Ctrl Pts',(-5.07614050253693,3.04435690941179,10.6611575063072));
#15952=CARTESIAN_POINT('Ctrl Pts',(-5.15932135160683,2.90115572419639,10.6689459161529));
#15953=CARTESIAN_POINT('Ctrl Pts',(-5.23634798948701,2.75473960575139,10.6767343259985));
#15954=CARTESIAN_POINT('Ctrl Pts',(-5.3093267266648,2.6160179411344,10.6841134396506));
#15955=CARTESIAN_POINT('Ctrl Pts',(-5.37678132643697,2.47441078453376,10.6914925533026));
#15956=CARTESIAN_POINT('Ctrl Pts',(-5.43850017603216,2.33037473334186,10.6988716669547));
#15957=CARTESIAN_POINT('Ctrl Pts',(-5.50338173111395,2.17895773431376,10.7066289140845));
#15958=CARTESIAN_POINT('Ctrl Pts',(-5.56194908421775,2.02479825938375,10.7143861612142));
#15959=CARTESIAN_POINT('Ctrl Pts',(-5.6139872295826,1.86844265327665,10.7221434083439));
#15960=CARTESIAN_POINT('Ctrl Pts',(-5.66601947511043,1.71210477402332,10.7298997759939));
#15961=CARTESIAN_POINT('Ctrl Pts',(-5.71152388362962,1.55357156700543,10.7376561436439));
#15962=CARTESIAN_POINT('Ctrl Pts',(-5.75033467496015,1.39340650509854,10.7454125112939));
#15963=CARTESIAN_POINT('Ctrl Pts',(-5.78914022576506,1.23326306988571,10.7531678316207));
#15964=CARTESIAN_POINT('Ctrl Pts',(-5.82125388798296,1.07148853527656,10.7609231519475));
#15965=CARTESIAN_POINT('Ctrl Pts',(-5.84656050553762,0.908658801524338,
10.7686784722742));
#15966=CARTESIAN_POINT('Ctrl Pts',(-5.8718711620906,0.745803079746681,10.7764350303692));
#15967=CARTESIAN_POINT('Ctrl Pts',(-5.89037255084516,0.581892142820665,
10.7841915884641));
#15968=CARTESIAN_POINT('Ctrl Pts',(-5.90200100937398,0.417510057182556,
10.791948146559));
#15969=CARTESIAN_POINT('Ctrl Pts',(-5.91183394626391,0.278509804491384,
10.798507033624));
#15970=CARTESIAN_POINT('Ctrl Pts',(-5.91675342831919,0.139172905666653,
10.805065920689));
#15971=CARTESIAN_POINT('Ctrl Pts',(-5.91674999820671,-0.000145674166803196,
10.811624807754));
#15972=CARTESIAN_POINT('Origin',(0.,0.,0.));
#15973=CARTESIAN_POINT('',(-5.91650109564654,0.000137871390016447,12.8133751922049));
#15974=CARTESIAN_POINT('',(-5.91674999943461,8.17956336808546E-5,12.5616248077579));
#15975=CARTESIAN_POINT('',(-5.91675,-7.2459289488551E-16,0.));
#15976=CARTESIAN_POINT('Ctrl Pts',(-5.91650109564654,0.000137871390016447,
12.8133751922049));
#15977=CARTESIAN_POINT('Ctrl Pts',(-5.91676819625198,0.31131399389983,12.7987285699419));
#15978=CARTESIAN_POINT('Ctrl Pts',(-5.81632669523957,1.60683994088276,12.7377419491744));
#15979=CARTESIAN_POINT('Ctrl Pts',(-4.8844629651232,3.76663245314218,12.6304153299036));
#15980=CARTESIAN_POINT('Ctrl Pts',(-2.48557677379138,5.64512237212916,12.4913953343907));
#15981=CARTESIAN_POINT('Ctrl Pts',(0.519808293086261,6.14616122739744,12.3523753388782));
#15982=CARTESIAN_POINT('Ctrl Pts',(3.39835634226172,5.14749188107496,12.2133553433657));
#15983=CARTESIAN_POINT('Ctrl Pts',(5.44768063861793,2.89279694315932,12.0743353478532));
#15984=CARTESIAN_POINT('Ctrl Pts',(6.16773109540022,-0.0677615640123341,
11.9353153523407));
#15985=CARTESIAN_POINT('Ctrl Pts',(5.38281014535615,-3.01178575495921,11.7962953568282));
#15986=CARTESIAN_POINT('Ctrl Pts',(3.28444422959756,-5.22091223804679,11.6572753613157));
#15987=CARTESIAN_POINT('Ctrl Pts',(0.384649947977164,-6.15609802652996,
11.5182553658031));
#15988=CARTESIAN_POINT('Ctrl Pts',(-2.60900172858952,-5.58915096190302,
11.3792353702907));
#15989=CARTESIAN_POINT('Ctrl Pts',(-4.96603793973493,-3.65841026619979,
11.2402153747781));
#15990=CARTESIAN_POINT('Ctrl Pts',(-5.83342026961988,-1.52009487709728,
11.1349286487496));
#15991=CARTESIAN_POINT('Ctrl Pts',(-5.91688460612658,-0.267972750171078,
11.0759819212251));
#15992=CARTESIAN_POINT('Ctrl Pts',(-5.91662392833365,-0.000151321579282548,
11.0633751922049));
#15993=CARTESIAN_POINT('Ctrl Pts',(-5.91674999820668,-0.000145675039010474,
10.8116248077951));
#15994=CARTESIAN_POINT('Ctrl Pts',(-5.9167454320706,-0.185604253661456,
10.8203558892767));
#15995=CARTESIAN_POINT('Ctrl Pts',(-5.90801584367932,-0.371021786546643,
10.8290869707582));
#15996=CARTESIAN_POINT('Ctrl Pts',(-5.89060459663212,-0.555615018368427,
10.8378180522397));
#15997=CARTESIAN_POINT('Ctrl Pts',(-5.87507379076582,-0.720271900203724,
10.8456061636326));
#15998=CARTESIAN_POINT('Ctrl Pts',(-5.85263204077725,-0.88430658380832,
10.8533942750255));
#15999=CARTESIAN_POINT('Ctrl Pts',(-5.82335341479904,-1.04713206848436,
10.8611823864184));
#16000=CARTESIAN_POINT('Ctrl Pts',(-5.79408053716864,-1.20992558521501,
10.8689689687514));
#16001=CARTESIAN_POINT('Ctrl Pts',(-5.75797351835347,-1.37151006242046,
10.8767555510844));
#16002=CARTESIAN_POINT('Ctrl Pts',(-5.71515779917155,-1.53130724972769,
10.8845421334174));
#16003=CARTESIAN_POINT('Ctrl Pts',(-5.67234044743583,-1.69111053006599,
10.892329012651));
#16004=CARTESIAN_POINT('Ctrl Pts',(-5.6228139623546,-1.84912607448866,10.9001158918847));
#16005=CARTESIAN_POINT('Ctrl Pts',(-5.5667542586208,-2.00478866383146,10.9079027711184));
#16006=CARTESIAN_POINT('Ctrl Pts',(-5.51069825479507,-2.1604409795333,10.9156891364225));
#16007=CARTESIAN_POINT('Ctrl Pts',(-5.44811000357761,-2.31374035031104,
10.9234755017267));
#16008=CARTESIAN_POINT('Ctrl Pts',(-5.3792144279962,-2.4641393426788,10.9312618670308));
#16009=CARTESIAN_POINT('Ctrl Pts',(-5.31030076183565,-2.61457782676791,
10.9390502768764));
#16010=CARTESIAN_POINT('Ctrl Pts',(-5.23507659332383,-2.76211411915151,
10.946838686722));
#16011=CARTESIAN_POINT('Ctrl Pts',(-5.15381426804612,-2.90622247135079,
10.9546270965675));
#16012=CARTESIAN_POINT('Ctrl Pts',(-5.07682243713573,-3.04275764736727,
10.96200621022));
#16013=CARTESIAN_POINT('Ctrl Pts',(-4.9944108880427,-3.17621567975814,10.9693853238725));
#16014=CARTESIAN_POINT('Ctrl Pts',(-4.90684854034149,-3.30617119409273,
10.976764437525));
#16015=CARTESIAN_POINT('Ctrl Pts',(-4.81443292650969,-3.44332967537331,
10.984552548918));
#16016=CARTESIAN_POINT('Ctrl Pts',(-4.71624633646594,-3.57663535081104,
10.992340660311));
#16017=CARTESIAN_POINT('Ctrl Pts',(-4.61263465296196,-3.70560819850055,
11.000128771704));
#16018=CARTESIAN_POINT('Ctrl Pts',(-4.50904331180559,-3.83455572462002,
11.0079153540371));
#16019=CARTESIAN_POINT('Ctrl Pts',(-4.40002920241936,-3.95917187139405,
11.0157019363702));
#16020=CARTESIAN_POINT('Ctrl Pts',(-4.28597913261866,-4.07900887928151,
11.0234885187033));
#16021=CARTESIAN_POINT('Ctrl Pts',(-4.17192471411444,-4.19885045652714,
11.031275397937));
#16022=CARTESIAN_POINT('Ctrl Pts',(-4.05283416837771,-4.31391229607584,
11.0390622771707));
#16023=CARTESIAN_POINT('Ctrl Pts',(-3.92913239089576,-4.42378222987002,
11.0468491564044));
#16024=CARTESIAN_POINT('Ctrl Pts',(-3.80543877765967,-4.53364491231204,
11.0546355217086));
#16025=CARTESIAN_POINT('Ctrl Pts',(-3.67713478070579,-4.638316162603,11.0624218870128));
#16026=CARTESIAN_POINT('Ctrl Pts',(-3.54467982156324,-4.73742287801104,
11.070208252317));
#16027=CARTESIAN_POINT('Ctrl Pts',(-3.41219008243807,-4.83655561683007,
11.0779966621626));
#16028=CARTESIAN_POINT('Ctrl Pts',(-3.27554745800553,-4.9301207080088,11.0857850720082));
#16029=CARTESIAN_POINT('Ctrl Pts',(-3.13524263775297,-5.01778677953894,
11.0935734818538));
#16030=CARTESIAN_POINT('Ctrl Pts',(-3.00231111063719,-5.10084582728774,
11.1009525955059));
#16031=CARTESIAN_POINT('Ctrl Pts',(-2.86609261929444,-5.17860978068094,
11.108331709158));
#16032=CARTESIAN_POINT('Ctrl Pts',(-2.72702682226942,-5.25083376932875,
11.1157108228101));
#16033=CARTESIAN_POINT('Ctrl Pts',(-2.5802531080747,-5.32706087401279,11.123498934203));
#16034=CARTESIAN_POINT('Ctrl Pts',(-2.43025508611663,-5.39714370341423,
11.131287045596));
#16035=CARTESIAN_POINT('Ctrl Pts',(-2.27756614334164,-5.46082622184628,
11.139075156989));
#16036=CARTESIAN_POINT('Ctrl Pts',(-2.12490717837867,-5.52449623732604,
11.146861739322));
#16037=CARTESIAN_POINT('Ctrl Pts',(-1.96955864146968,-5.58176832618418,
11.1546483216551));
#16038=CARTESIAN_POINT('Ctrl Pts',(-1.81207442134101,-5.63243436304602,
11.1624349039882));
#16039=CARTESIAN_POINT('Ctrl Pts',(-1.65458419637423,-5.68310233179252,
11.1702217832219));
#16040=CARTESIAN_POINT('Ctrl Pts',(-1.494958428193,-5.72716364290202,11.1780086624556));
#16041=CARTESIAN_POINT('Ctrl Pts',(-1.33376742295693,-5.76445964717933,
11.1857955416893));
#16042=CARTESIAN_POINT('Ctrl Pts',(-1.17258705623392,-5.80175318994194,
11.1935819069935));
#16043=CARTESIAN_POINT('Ctrl Pts',(-1.00984197053972,-5.83228224748056,
11.2013682722977));
#16044=CARTESIAN_POINT('Ctrl Pts',(-0.846114099909923,-5.85593899323017,
11.2091546376019));
#16045=CARTESIAN_POINT('Ctrl Pts',(-0.68234323766618,-5.87960195076082,
11.2169430474475));
#16046=CARTESIAN_POINT('Ctrl Pts',(-0.517589391005335,-5.89638894303135,
11.2247314572931));
#16047=CARTESIAN_POINT('Ctrl Pts',(-0.352441985621134,-5.90624374787152,
11.2325198671388));
#16048=CARTESIAN_POINT('Ctrl Pts',(-0.195973399883253,-5.9155806634136,
11.2398989807909));
#16049=CARTESIAN_POINT('Ctrl Pts',(-0.0391518156922628,-5.91869523613666,
11.2472780944431));
#16050=CARTESIAN_POINT('Ctrl Pts',(0.11751953811834,-5.91558278791367,11.2546572080952));
#16051=CARTESIAN_POINT('Ctrl Pts',(0.282874621815559,-5.91229782787536,
11.2624453194882));
#16052=CARTESIAN_POINT('Ctrl Pts',(0.448121405794196,-5.90207481692401,
11.2702334308812));
#16053=CARTESIAN_POINT('Ctrl Pts',(0.612669014299875,-5.88494411540304,
11.2780215422741));
#16054=CARTESIAN_POINT('Ctrl Pts',(0.777184316751264,-5.86781677719666,
11.2858081246072));
#16055=CARTESIAN_POINT('Ctrl Pts',(0.941000400011421,-5.84378448751827,
11.2935947069402));
#16056=CARTESIAN_POINT('Ctrl Pts',(1.1035313072279,-5.81292948662444,11.3013812892733));
#16057=CARTESIAN_POINT('Ctrl Pts',(1.26606841171148,-5.78207330923634,11.309168168507));
#16058=CARTESIAN_POINT('Ctrl Pts',(1.42731992744971,-5.74439395578933,11.3169550477407));
#16059=CARTESIAN_POINT('Ctrl Pts',(1.58670915221621,-5.70002496738157,11.3247419269744));
#16060=CARTESIAN_POINT('Ctrl Pts',(1.7460878573861,-5.65565890730139,11.3325282922786));
#16061=CARTESIAN_POINT('Ctrl Pts',(1.90360420972952,-5.60460418160287,11.3403146575828));
#16062=CARTESIAN_POINT('Ctrl Pts',(2.05869561165523,-5.54704452308177,11.3481010228869));
#16063=CARTESIAN_POINT('Ctrl Pts',(2.21382773743365,-5.48946975056321,11.3558894327325));
#16064=CARTESIAN_POINT('Ctrl Pts',(2.36653334001421,-5.42538674158669,11.3636778425781));
#16065=CARTESIAN_POINT('Ctrl Pts',(2.51626793257187,-5.35502812821842,11.3714662524237));
#16066=CARTESIAN_POINT('Ctrl Pts',(2.65813367898902,-5.2883669978018,11.3788453660759));
#16067=CARTESIAN_POINT('Ctrl Pts',(2.7973324131779,-5.21607299921343,11.3862244797281));
#16068=CARTESIAN_POINT('Ctrl Pts',(2.93342000023192,-5.13838278690284,11.3936035933803));
#16069=CARTESIAN_POINT('Ctrl Pts',(3.07705043298201,-5.05638648543129,11.4013917047733));
#16070=CARTESIAN_POINT('Ctrl Pts',(3.21726635705876,-4.96834953748601,11.4091798161662));
#16071=CARTESIAN_POINT('Ctrl Pts',(3.35356343643352,-4.87458129897494,11.4169679275592));
#16072=CARTESIAN_POINT('Ctrl Pts',(3.48983375625269,-4.78083147022292,11.4247545098922));
#16073=CARTESIAN_POINT('Ctrl Pts',(3.62218650346077,-4.68135277708563,11.4325410922253));
#16074=CARTESIAN_POINT('Ctrl Pts',(3.75014648260913,-4.57649777903086,11.4403276745584));
#16075=CARTESIAN_POINT('Ctrl Pts',(3.87811134084303,-4.47163878287834,11.4481145537921));
#16076=CARTESIAN_POINT('Ctrl Pts',(4.00168284621691,-4.36140327106968,11.4559014330258));
#16077=CARTESIAN_POINT('Ctrl Pts',(4.12041847411225,-4.24618442377324,11.4636883122595));
#16078=CARTESIAN_POINT('Ctrl Pts',(4.23914626552484,-4.13097318085406,11.4714746775637));
#16079=CARTESIAN_POINT('Ctrl Pts',(4.35303858891042,-4.01077948324227,11.4792610428679));
#16080=CARTESIAN_POINT('Ctrl Pts',(4.46168931873055,-3.88603383742676,11.487047408172));
#16081=CARTESIAN_POINT('Ctrl Pts',(4.57036857802595,-3.76125543593788,11.4948358180176));
#16082=CARTESIAN_POINT('Ctrl Pts',(4.67380328208609,-3.63192293772112,11.5026242278632));
#16083=CARTESIAN_POINT('Ctrl Pts',(4.77162660398512,-3.49850112400174,11.5104126377088));
#16084=CARTESIAN_POINT('Ctrl Pts',(4.864309118701,-3.37209088794138,11.517791751361));
#16085=CARTESIAN_POINT('Ctrl Pts',(4.95195470633137,-3.24201029445954,11.5251708650132));
#16086=CARTESIAN_POINT('Ctrl Pts',(5.0342865857107,-3.10867964503152,11.5325499786654));
#16087=CARTESIAN_POINT('Ctrl Pts',(5.12118182516919,-2.96795895704839,11.5403380900584));
#16088=CARTESIAN_POINT('Ctrl Pts',(5.20218864833156,-2.82356746086751,11.5481262014514));
#16089=CARTESIAN_POINT('Ctrl Pts',(5.27701219299427,-2.676018101114,11.5559143128443));
#16090=CARTESIAN_POINT('Ctrl Pts',(5.35182104735834,-2.52849771010514,11.5637008951774));
#16091=CARTESIAN_POINT('Ctrl Pts',(5.4204489010451,-2.377820977395,11.5714874775105));
#16092=CARTESIAN_POINT('Ctrl Pts',(5.482647150966,-2.22452484375976,11.5792740598435));
#16093=CARTESIAN_POINT('Ctrl Pts',(5.54484777249233,-2.07122286497706,11.5870609390773));
#16094=CARTESIAN_POINT('Ctrl Pts',(5.60061817590153,-1.9153015800039,11.594847818311));
#16095=CARTESIAN_POINT('Ctrl Pts',(5.6497578814823,-1.75731796870364,11.6026346975447));
#16096=CARTESIAN_POINT('Ctrl Pts',(5.69889434387092,-1.59934478423033,11.6104210628489));
#16097=CARTESIAN_POINT('Ctrl Pts',(5.74140088938333,-1.43930985098022,11.6182074281531));
#16098=CARTESIAN_POINT('Ctrl Pts',(5.77712685939935,-1.27778551130722,11.6259937934573));
#16099=CARTESIAN_POINT('Ctrl Pts',(5.8128622103296,-1.11621875862271,11.6337822033029));
#16100=CARTESIAN_POINT('Ctrl Pts',(5.84181335712389,-0.953162129814492,
11.6415706131485));
#16101=CARTESIAN_POINT('Ctrl Pts',(5.86388054841331,-0.789199262822796,
11.6493590229941));
#16102=CARTESIAN_POINT('Ctrl Pts',(5.88478806557499,-0.633852965663927,
11.6567381366462));
#16103=CARTESIAN_POINT('Ctrl Pts',(5.89951651366658,-0.477693487410386,
11.6641172502984));
#16104=CARTESIAN_POINT('Ctrl Pts',(5.90802393187583,-0.321222326251578,
11.6714963639506));
#16105=CARTESIAN_POINT('Ctrl Pts',(5.91700288569104,-0.156078531165855,
11.6792844753436));
#16106=CARTESIAN_POINT('Ctrl Pts',(5.91905484265651,0.00947145838644853,
11.6870725867365));
#16107=CARTESIAN_POINT('Ctrl Pts',(5.91416628833766,0.174836141545134,11.6948606981295));
#16108=CARTESIAN_POINT('Ctrl Pts',(5.90927869380122,0.340168358230971,11.7026472804625));
#16109=CARTESIAN_POINT('Ctrl Pts',(5.89745331630517,0.505315021923757,11.7104338627956));
#16110=CARTESIAN_POINT('Ctrl Pts',(5.87872874320458,0.669685692187242,11.7182204451286));
#16111=CARTESIAN_POINT('Ctrl Pts',(5.86000345614018,0.834062629867812,11.7260073243623));
#16112=CARTESIAN_POINT('Ctrl Pts',(5.83437847931976,0.997663197003097,11.733794203596));
#16113=CARTESIAN_POINT('Ctrl Pts',(5.80194424574037,1.15990238029765,11.7415810828297));
#16114=CARTESIAN_POINT('Ctrl Pts',(5.76951215280164,1.32213085589998,11.7493674481339));
#16115=CARTESIAN_POINT('Ctrl Pts',(5.73027176519635,1.48299781413655,11.7571538134381));
#16116=CARTESIAN_POINT('Ctrl Pts',(5.68436461491616,1.64192858772515,11.7649401787423));
#16117=CARTESIAN_POINT('Ctrl Pts',(5.63844541035054,1.80090109330747,11.7727285885878));
#16118=CARTESIAN_POINT('Ctrl Pts',(5.58585603199734,1.95793609062769,11.7805169984334));
#16119=CARTESIAN_POINT('Ctrl Pts',(5.52678811887441,2.1124733493156,11.788305408279));
#16120=CARTESIAN_POINT('Ctrl Pts',(5.47082434028861,2.25888937235113,11.7956845219312));
#16121=CARTESIAN_POINT('Ctrl Pts',(5.40904552559427,2.40306318372778,11.8030636355835));
#16122=CARTESIAN_POINT('Ctrl Pts',(5.34165476246286,2.54453433090572,11.8104427492357));
#16123=CARTESIAN_POINT('Ctrl Pts',(5.27052877161072,2.6938467151623,11.8182308606287));
#16124=CARTESIAN_POINT('Ctrl Pts',(5.19312568894896,2.8402016684873,11.8260189720216));
#16125=CARTESIAN_POINT('Ctrl Pts',(5.10971664201412,2.98307331469141,11.8338070834146));
#16126=CARTESIAN_POINT('Ctrl Pts',(5.02632397099162,3.12591691053838,11.8415936657477));
#16127=CARTESIAN_POINT('Ctrl Pts',(4.93692784948212,3.26527828804663,11.8493802480808));
#16128=CARTESIAN_POINT('Ctrl Pts',(4.84184464944875,3.40065742954278,11.8571668304138));
#16129=CARTESIAN_POINT('Ctrl Pts',(4.74675782391412,3.53604173301549,11.8649537096476));
#16130=CARTESIAN_POINT('Ctrl Pts',(4.6459836663555,3.66744323290245,11.8727405888813));
#16131=CARTESIAN_POINT('Ctrl Pts',(4.5398814790422,3.79439148200995,11.880527468115));
#16132=CARTESIAN_POINT('Ctrl Pts',(4.43378629441189,3.92133135260641,11.8883138334192));
#16133=CARTESIAN_POINT('Ctrl Pts',(4.32236398874528,4.04381831547097,11.8961001987234));
#16134=CARTESIAN_POINT('Ctrl Pts',(4.20601378560764,4.16141545604119,11.9038865640276));
#16135=CARTESIAN_POINT('Ctrl Pts',(4.08963303126935,4.2790434752325,11.9116749738732));
#16136=CARTESIAN_POINT('Ctrl Pts',(3.9683220173478,4.39177887783712,11.9194633837188));
#16137=CARTESIAN_POINT('Ctrl Pts',(3.84251706040394,4.49922139964291,11.9272517935644));
#16138=CARTESIAN_POINT('Ctrl Pts',(3.72332340037689,4.60101760646711,11.9346309072166));
#16139=CARTESIAN_POINT('Ctrl Pts',(3.60009617753248,4.69806275771776,11.9420100208687));
#16140=CARTESIAN_POINT('Ctrl Pts',(3.47323402452313,4.79004968381277,11.9493891345208));
#16141=CARTESIAN_POINT('Ctrl Pts',(3.33934035845881,4.88713511451598,11.9571772459138));
#16142=CARTESIAN_POINT('Ctrl Pts',(3.20134957404015,4.97862037553502,11.9649653573067));
#16143=CARTESIAN_POINT('Ctrl Pts',(3.05975135225921,5.06417339995857,11.9727534686997));
#16144=CARTESIAN_POINT('Ctrl Pts',(2.91818093082082,5.1497096275371,11.9805400510327));
#16145=CARTESIAN_POINT('Ctrl Pts',(2.7730047585213,5.22931577728854,11.9883266333658));
#16146=CARTESIAN_POINT('Ctrl Pts',(2.62473987489058,5.30270413578387,11.9961132156988));
#16147=CARTESIAN_POINT('Ctrl Pts',(2.47646933795271,5.37609529256104,12.0039000949326));
#16148=CARTESIAN_POINT('Ctrl Pts',(2.32511013862664,5.44326803839932,12.0116869741663));
#16149=CARTESIAN_POINT('Ctrl Pts',(2.17120286696385,5.5039811657552,12.0194738534));
#16150=CARTESIAN_POINT('Ctrl Pts',(2.01730575309196,5.56469028607979,12.0272602187042));
#16151=CARTESIAN_POINT('Ctrl Pts',(1.86086120072366,5.61894052392279,12.0350465840083));
#16152=CARTESIAN_POINT('Ctrl Pts',(1.70242881251837,5.66653921726545,12.0428329493125));
#16153=CARTESIAN_POINT('Ctrl Pts',(1.54395482318527,5.71415040905838,12.0506213591581));
#16154=CARTESIAN_POINT('Ctrl Pts',(1.38349226067852,5.75510647250128,12.0584097690037));
#16155=CARTESIAN_POINT('Ctrl Pts',(1.22161576504376,5.78926467568175,12.0661981788493));
#16156=CARTESIAN_POINT('Ctrl Pts',(1.06824619633969,5.82162779837571,12.0735772925015));
#16157=CARTESIAN_POINT('Ctrl Pts',(0.913607736579875,5.84788911203013,12.0809564061537));
#16158=CARTESIAN_POINT('Ctrl Pts',(0.758197394955816,5.86796960394157,12.0883355198059));
#16159=CARTESIAN_POINT('Ctrl Pts',(0.594173216818297,5.88916308532738,12.0961236311989));
#16160=CARTESIAN_POINT('Ctrl Pts',(0.429230584190746,5.90347872398087,12.1039117425918));
#16161=CARTESIAN_POINT('Ctrl Pts',(0.263958369650268,5.91085920502185,12.1116998539848));
#16162=CARTESIAN_POINT('Ctrl Pts',(0.0987186034279958,5.91823823703405,
12.1194864363179));
#16163=CARTESIAN_POINT('Ctrl Pts',(-0.0668502965829588,5.91868481397916,
12.1272730186509));
#16164=CARTESIAN_POINT('Ctrl Pts',(-0.232156653918887,5.91219365807153,
12.135059600984));
#16165=CARTESIAN_POINT('Ctrl Pts',(-0.397469314349455,5.90570225465757,
12.1428464802177));
#16166=CARTESIAN_POINT('Ctrl Pts',(-0.562519092648928,5.89227259764935,
12.1506333594514));
#16167=CARTESIAN_POINT('Ctrl Pts',(-0.726715882158628,5.87195151454084,
12.1584202386851));
#16168=CARTESIAN_POINT('Ctrl Pts',(-0.890901834775293,5.85163177261204,
12.1662066039893));
#16169=CARTESIAN_POINT('Ctrl Pts',(-1.05423459414129,5.82442155413361,12.1739929692935));
#16170=CARTESIAN_POINT('Ctrl Pts',(-1.21613058408384,5.79041941183503,12.1817793345977));
#16171=CARTESIAN_POINT('Ctrl Pts',(-1.3780690846256,5.75640834126439,12.1895677444433));
#16172=CARTESIAN_POINT('Ctrl Pts',(-1.53856974857601,5.71560184704553,12.1973561542889));
#16173=CARTESIAN_POINT('Ctrl Pts',(-1.69705968341381,5.66814952108988,12.2051445641345));
#16174=CARTESIAN_POINT('Ctrl Pts',(-1.84722066172463,5.62319090781317,12.2125236777867));
#16175=CARTESIAN_POINT('Ctrl Pts',(-1.99557656161878,5.57226707450899,12.2199027914389));
#16176=CARTESIAN_POINT('Ctrl Pts',(-2.1416531455166,5.51554642504248,12.2272819050911));
#16177=CARTESIAN_POINT('Ctrl Pts',(-2.2958262292934,5.45568195389499,12.2350700164841));
#16178=CARTESIAN_POINT('Ctrl Pts',(-2.44751522642145,5.389338471031,12.2428581278771));
#16179=CARTESIAN_POINT('Ctrl Pts',(-2.59617561298909,5.31674738435265,12.25064623927));
#16180=CARTESIAN_POINT('Ctrl Pts',(-2.74480681268132,5.24417054966874,12.2584328216031));
#16181=CARTESIAN_POINT('Ctrl Pts',(-2.89041030129804,5.16534869873573,12.2662194039361));
#16182=CARTESIAN_POINT('Ctrl Pts',(-3.0324639891518,5.08056027589454,12.2740059862692));
#16183=CARTESIAN_POINT('Ctrl Pts',(-3.17452309348098,4.9957686200897,12.2817928655029));
#16184=CARTESIAN_POINT('Ctrl Pts',(-3.31303184982197,4.90501009750941,12.2895797447366));
#16185=CARTESIAN_POINT('Ctrl Pts',(-3.44749447597213,4.80860815627991,12.2973666239703));
#16186=CARTESIAN_POINT('Ctrl Pts',(-3.58194822766667,4.71221257752282,12.3051529892745));
#16187=CARTESIAN_POINT('Ctrl Pts',(-3.71235612392713,4.61017451175995,12.3129393545787));
#16188=CARTESIAN_POINT('Ctrl Pts',(-3.83825286429633,4.50285970381279,12.3207257198829));
#16189=CARTESIAN_POINT('Ctrl Pts',(-3.96418266259308,4.39551671717622,12.3285141297285));
#16190=CARTESIAN_POINT('Ctrl Pts',(-4.08559869345287,4.28289442564719,12.336302539574));
#16191=CARTESIAN_POINT('Ctrl Pts',(-4.20206945692127,4.16539828128228,12.3440909494196));
#16192=CARTESIAN_POINT('Ctrl Pts',(-4.31241945362519,4.0540767894565,12.3514700630718));
#16193=CARTESIAN_POINT('Ctrl Pts',(-4.41833039815079,3.93838071492787,12.358849176724));
#16194=CARTESIAN_POINT('Ctrl Pts',(-4.51946642200182,3.81868482895592,12.3662282903762));
#16195=CARTESIAN_POINT('Ctrl Pts',(-4.62620805205678,3.69235463034798,12.3740164017692));
#16196=CARTESIAN_POINT('Ctrl Pts',(-4.72766856124315,3.56152353830952,12.3818045131622));
#16197=CARTESIAN_POINT('Ctrl Pts',(-4.82348050438523,3.42665527684294,12.3895926245551));
#16198=CARTESIAN_POINT('Ctrl Pts',(-4.91927363652244,3.29181349440852,12.3973792068882));
#16199=CARTESIAN_POINT('Ctrl Pts',(-5.00942023045605,3.15293638440082,12.4051657892213));
#16200=CARTESIAN_POINT('Ctrl Pts',(-5.0935950449057,3.01051824126879,12.4129523715543));
#16201=CARTESIAN_POINT('Ctrl Pts',(-5.17777306892231,2.86809466776462,12.4207392507881));
#16202=CARTESIAN_POINT('Ctrl Pts',(-5.2559786918491,2.72213006401831,12.4285261300218));
#16203=CARTESIAN_POINT('Ctrl Pts',(-5.32793130500654,2.57314565690154,12.4363130092555));
#16204=CARTESIAN_POINT('Ctrl Pts',(-5.39987916933312,2.42417108266951,12.4440993745597));
#16205=CARTESIAN_POINT('Ctrl Pts',(-5.46557471089158,2.27217739171107,12.4518857398639));
#16206=CARTESIAN_POINT('Ctrl Pts',(-5.52478432394942,2.1177083690496,12.4596721051681));
#16207=CARTESIAN_POINT('Ctrl Pts',(-5.58400948424929,1.96319878595958,12.4674605150137));
#16208=CARTESIAN_POINT('Ctrl Pts',(-5.63674519670071,1.80621287024954,12.4752489248593));
#16209=CARTESIAN_POINT('Ctrl Pts',(-5.68280653390567,1.64731310341993,12.4830373347049));
#16210=CARTESIAN_POINT('Ctrl Pts',(-5.72644725761465,1.49676383059325,12.4904164483571));
#16211=CARTESIAN_POINT('Ctrl Pts',(-5.76409699364876,1.34449693593846,12.4977955620092));
#16212=CARTESIAN_POINT('Ctrl Pts',(-5.79564011200116,1.19100220598584,12.5051746756613));
#16213=CARTESIAN_POINT('Ctrl Pts',(-5.82972444891384,1.02514142990224,12.51314827526));
#16214=CARTESIAN_POINT('Ctrl Pts',(-5.85668801831256,0.857799885178385,
12.5211218748587));
#16215=CARTESIAN_POINT('Ctrl Pts',(-5.87642730860905,0.689588753630612,
12.5290954744574));
#16216=CARTESIAN_POINT('Ctrl Pts',(-5.89616094744817,0.521425781769642,
12.5370667911747));
#16217=CARTESIAN_POINT('Ctrl Pts',(-5.90867440354806,0.352394003831148,
12.5450381078921));
#16218=CARTESIAN_POINT('Ctrl Pts',(-5.91391586784887,0.18311108788216,12.5530094246094));
#16219=CARTESIAN_POINT('Ctrl Pts',(-5.91580418922297,0.122124209004174,
12.5558812189922));
#16220=CARTESIAN_POINT('Ctrl Pts',(-5.91674915582728,0.0611047797757011,
12.5587530133751));
#16221=CARTESIAN_POINT('Ctrl Pts',(-5.91674999943461,8.1795633684796E-5,
12.5616248077579));
#16222=CARTESIAN_POINT('Origin',(0.,0.,0.));
#16223=CARTESIAN_POINT('',(-5.91713904777553,-9.26149740448912E-5,14.5633751922049));
#16224=CARTESIAN_POINT('',(-5.9167499999999,1.1077521759692E-6,14.3116248077956));
#16225=CARTESIAN_POINT('',(-5.91675,-7.2459289488551E-16,0.));
#16226=CARTESIAN_POINT('Ctrl Pts',(-5.91713904777553,-9.26149740448912E-5,
14.5633751922049));
#16227=CARTESIAN_POINT('Ctrl Pts',(-5.9164724942665,0.8898205116778,14.5214752186586));
#16228=CARTESIAN_POINT('Ctrl Pts',(-5.48777132288459,2.76456885274308,14.4332352466081));
#16229=CARTESIAN_POINT('Ctrl Pts',(-3.58563248749387,5.01883832767618,14.2986552760536));
#16230=CARTESIAN_POINT('Ctrl Pts',(-0.74581831746291,6.12284684865313,14.159635280541));
#16231=CARTESIAN_POINT('Ctrl Pts',(2.27598096591196,5.73283604662921,14.0206152850285));
#16232=CARTESIAN_POINT('Ctrl Pts',(4.74242428074643,3.94397140406846,13.8815952895159));
#16233=CARTESIAN_POINT('Ctrl Pts',(6.05168145514075,1.19274895104965,13.7425752940035));
#16234=CARTESIAN_POINT('Ctrl Pts',(5.88428418200233,-1.8495129521476,13.6035552984909));
#16235=CARTESIAN_POINT('Ctrl Pts',(4.28107861784435,-4.44048019504202,13.4645353029784));
#16236=CARTESIAN_POINT('Ctrl Pts',(1.63325862245189,-5.94793785835978,13.3255153074659));
#16237=CARTESIAN_POINT('Ctrl Pts',(-1.41308839831272,-6.00405526900601,
13.1864953119534));
#16238=CARTESIAN_POINT('Ctrl Pts',(-4.11463153546355,-4.59513936916963,
13.0474753164408));
#16239=CARTESIAN_POINT('Ctrl Pts',(-5.63332781710766,-2.33154439788799,
12.9231019431914));
#16240=CARTESIAN_POINT('Ctrl Pts',(-5.91592312484681,-0.67320658652368,
12.845068568446));
#16241=CARTESIAN_POINT('Ctrl Pts',(-5.91650109564654,0.000137871390016447,
12.8133751922049));
#16242=CARTESIAN_POINT('Ctrl Pts',(-5.91674999943462,8.17948436890362E-5,
12.5616248077951));
#16243=CARTESIAN_POINT('Ctrl Pts',(-5.91675229657022,-0.166084878407706,
12.5694447550752));
#16244=CARTESIAN_POINT('Ctrl Pts',(-5.90975028468448,-0.332249809338274,
12.5772647023552));
#16245=CARTESIAN_POINT('Ctrl Pts',(-5.89577044899758,-0.497816608026388,
12.5850846496353));
#16246=CARTESIAN_POINT('Ctrl Pts',(-5.88179051581164,-0.663384561420722,
12.5929046514537));
#16247=CARTESIAN_POINT('Ctrl Pts',(-5.86083269146452,-0.828354061912414,
12.6007246532721));
#16248=CARTESIAN_POINT('Ctrl Pts',(-5.83297537516117,-0.992133476536006,
12.6085446550905));
#16249=CARTESIAN_POINT('Ctrl Pts',(-5.80511105887375,-1.15595404563694,
12.6163666219184));
#16250=CARTESIAN_POINT('Ctrl Pts',(-5.77034383978369,-1.31858362209411,
12.6241885887462));
#16251=CARTESIAN_POINT('Ctrl Pts',(-5.72880346599528,-1.47943955959696,
12.632010555574));
#16252=CARTESIAN_POINT('Ctrl Pts',(-5.70736491432772,-1.56245562355329,
12.6360473906981));
#16253=CARTESIAN_POINT('Ctrl Pts',(-5.68412317400547,-1.64499946397032,
12.6400842258223));
#16254=CARTESIAN_POINT('Ctrl Pts',(-5.65910133104918,-1.72699238198012,
12.6441210609464));
#16255=CARTESIAN_POINT('Ctrl Pts',(-5.61082764777827,-1.88517817834122,
12.6519091723394));
#16256=CARTESIAN_POINT('Ctrl Pts',(-5.5559086689182,-2.0413668953765,12.6596972837324));
#16257=CARTESIAN_POINT('Ctrl Pts',(-5.49453480994079,-2.19499835645699,
12.6674853951253));
#16258=CARTESIAN_POINT('Ctrl Pts',(-5.43317300065069,-2.34859965467829,
12.6752719774584));
#16259=CARTESIAN_POINT('Ctrl Pts',(-5.36535895835549,-2.49964440218507,
12.6830585597914));
#16260=CARTESIAN_POINT('Ctrl Pts',(-5.29133166826683,-2.64759130888749,
12.6908451421245));
#16261=CARTESIAN_POINT('Ctrl Pts',(-5.21730155553412,-2.79554385677244,
12.6986320213582));
#16262=CARTESIAN_POINT('Ctrl Pts',(-5.13705786039537,-2.94039803998609,
12.7064189005919));
#16263=CARTESIAN_POINT('Ctrl Pts',(-5.0508863977957,-3.08163546823151,12.7142057798256));
#16264=CARTESIAN_POINT('Ctrl Pts',(-4.96472062246255,-3.22286357488861,
12.7219921451298));
#16265=CARTESIAN_POINT('Ctrl Pts',(-4.87262802911266,-3.36047513153216,
12.729778510434));
#16266=CARTESIAN_POINT('Ctrl Pts',(-4.77493887214427,-3.49397901106827,
12.7375648757382));
#16267=CARTESIAN_POINT('Ctrl Pts',(-4.67722406398722,-3.62751794601184,
12.7453532855838));
#16268=CARTESIAN_POINT('Ctrl Pts',(-4.57390994300305,-3.75694678941308,
12.7531416954294));
#16269=CARTESIAN_POINT('Ctrl Pts',(-4.46536886666572,-3.88180517892288,
12.7609301052749));
#16270=CARTESIAN_POINT('Ctrl Pts',(-4.36253183650075,-4.00010201549067,
12.7683092189272));
#16271=CARTESIAN_POINT('Ctrl Pts',(-4.25500326494473,-4.11429621906942,
12.7756883325794));
#16272=CARTESIAN_POINT('Ctrl Pts',(-4.14313200053735,-4.22402506960167,
12.7830674462316));
#16273=CARTESIAN_POINT('Ctrl Pts',(-4.02506011413759,-4.3398357958275,12.7908555576246));
#16274=CARTESIAN_POINT('Ctrl Pts',(-3.90210831516608,-4.45071349736323,
12.7986436690175));
#16275=CARTESIAN_POINT('Ctrl Pts',(-3.77471182004837,-4.55625737180058,
12.8064317804105));
#16276=CARTESIAN_POINT('Ctrl Pts',(-3.64734033701145,-4.66178052453823,
12.8142183627436));
#16277=CARTESIAN_POINT('Ctrl Pts',(-3.51552614490619,-4.76197173593689,
12.8220049450766));
#16278=CARTESIAN_POINT('Ctrl Pts',(-3.379738074369,-4.85647002576568,12.8297915274097));
#16279=CARTESIAN_POINT('Ctrl Pts',(-3.24394482626307,-4.95097191879312,
12.8375784066434));
#16280=CARTESIAN_POINT('Ctrl Pts',(-3.10417765653071,-5.03978027014071,
12.8453652858771));
#16281=CARTESIAN_POINT('Ctrl Pts',(-2.96093556199778,-5.12257661340432,
12.8531521651108));
#16282=CARTESIAN_POINT('Ctrl Pts',(-2.81770292136031,-5.20536749215713,
12.860938530415));
#16283=CARTESIAN_POINT('Ctrl Pts',(-2.67099609159335,-5.28214699704896,
12.8687248957192));
#16284=CARTESIAN_POINT('Ctrl Pts',(-2.52134004914326,-5.35264186351808,
12.8765112610233));
#16285=CARTESIAN_POINT('Ctrl Pts',(-2.37164471005547,-5.42315524050759,
12.8842996708689));
#16286=CARTESIAN_POINT('Ctrl Pts',(-2.2189988992925,-5.48738054358563,12.8920880807145));
#16287=CARTESIAN_POINT('Ctrl Pts',(-2.06394984603373,-5.54509166701123,
12.8998764905601));
#16288=CARTESIAN_POINT('Ctrl Pts',(-1.91704892423512,-5.59976995785576,
12.9072556042123));
#16289=CARTESIAN_POINT('Ctrl Pts',(-1.76799109714567,-5.64860103418118,
12.9146347178645));
#16290=CARTESIAN_POINT('Ctrl Pts',(-1.61725623469744,-5.69143328466848,
12.9220138315167));
#16291=CARTESIAN_POINT('Ctrl Pts',(-1.45816668073688,-5.73663957281228,
12.9298019429097));
#16292=CARTESIAN_POINT('Ctrl Pts',(-1.29715209712433,-5.77517933711375,
12.9375900543026));
#16293=CARTESIAN_POINT('Ctrl Pts',(-1.13478641534345,-5.80690884671457,
12.9453781656956));
#16294=CARTESIAN_POINT('Ctrl Pts',(-0.972452611234238,-5.83863212677921,
12.9531647480287));
#16295=CARTESIAN_POINT('Ctrl Pts',(-0.808768551641325,-5.86354775875977,
12.9609513303617));
#16296=CARTESIAN_POINT('Ctrl Pts',(-0.644318633120283,-5.88156306278476,
12.9687379126948));
#16297=CARTESIAN_POINT('Ctrl Pts',(-0.479862444159993,-5.89957905372933,
12.9765247919285));
#16298=CARTESIAN_POINT('Ctrl Pts',(-0.31464065502396,-5.91069415151979,
12.9843116711622));
#16299=CARTESIAN_POINT('Ctrl Pts',(-0.149243811773383,-5.91486744121518,
12.992098550396));
#16300=CARTESIAN_POINT('Ctrl Pts',(0.0161421153806483,-5.91904045547584,
12.9998849157002));
#16301=CARTESIAN_POINT('Ctrl Pts',(0.181702754074313,-5.91627257053815,
13.0076712810043));
#16302=CARTESIAN_POINT('Ctrl Pts',(0.346846371104012,-5.90657499379733,
13.0154576463085));
#16303=CARTESIAN_POINT('Ctrl Pts',(0.512033351494504,-5.89687487066976,
13.0232460561541));
#16304=CARTESIAN_POINT('Ctrl Pts',(0.676802772111731,-5.88024143661172,
13.0310344659997));
#16305=CARTESIAN_POINT('Ctrl Pts',(0.840565921562127,-5.85673795674763,
13.0388228758453));
#16306=CARTESIAN_POINT('Ctrl Pts',(0.99572299672694,-5.8344696307894,13.0462019894975));
#16307=CARTESIAN_POINT('Ctrl Pts',(1.14997658604171,-5.8060347927389,13.0535811031497));
#16308=CARTESIAN_POINT('Ctrl Pts',(1.30283276856397,-5.77152989593366,13.0609602168018));
#16309=CARTESIAN_POINT('Ctrl Pts',(1.46416121974405,-5.73511251674843,13.0687483281948));
#16310=CARTESIAN_POINT('Ctrl Pts',(1.62399058331058,-5.69192010873466,13.0765364395878));
#16311=CARTESIAN_POINT('Ctrl Pts',(1.78174811101581,-5.64210104760554,13.0843245509807));
#16312=CARTESIAN_POINT('Ctrl Pts',(1.93947466578125,-5.5922917675804,13.0921111333138));
#16313=CARTESIAN_POINT('Ctrl Pts',(2.09512989180203,-5.53585852653935,13.0998977156469));
#16314=CARTESIAN_POINT('Ctrl Pts',(2.24815627580423,-5.47299953609189,13.10768429798));
#16315=CARTESIAN_POINT('Ctrl Pts',(2.40118849466776,-5.41013814884538,13.1154711772137));
#16316=CARTESIAN_POINT('Ctrl Pts',(2.55159137388544,-5.34085063967505,13.1232580564474));
#16317=CARTESIAN_POINT('Ctrl Pts',(2.69882676633028,-5.26538361829784,13.1310449356811));
#16318=CARTESIAN_POINT('Ctrl Pts',(2.84605244132441,-5.18992157770038,13.1388313009852));
#16319=CARTESIAN_POINT('Ctrl Pts',(2.99011076357107,-5.10828098691886,13.1466176662894));
#16320=CARTESIAN_POINT('Ctrl Pts',(3.13048748065006,-5.02075479345419,13.1544040315936));
#16321=CARTESIAN_POINT('Ctrl Pts',(3.27090105780461,-4.93320561738834,13.1621924414392));
#16322=CARTESIAN_POINT('Ctrl Pts',(3.40763082574729,-4.83976791805148,13.1699808512848));
#16323=CARTESIAN_POINT('Ctrl Pts',(3.5401900918317,-4.74077891028433,13.1777692611304));
#16324=CARTESIAN_POINT('Ctrl Pts',(3.66578310882499,-4.64699196877597,13.1851483747826));
#16325=CARTESIAN_POINT('Ctrl Pts',(3.78763247743074,-4.54822233173038,13.1925274884348));
#16326=CARTESIAN_POINT('Ctrl Pts',(3.90535062107284,-4.44479100622132,13.199906602087));
#16327=CARTESIAN_POINT('Ctrl Pts',(4.0295934582035,-4.33562685418967,13.20769471348));
#16328=CARTESIAN_POINT('Ctrl Pts',(4.14927849957738,-4.2212306110712,13.215482824873));
#16329=CARTESIAN_POINT('Ctrl Pts',(4.26397379005778,-4.10200659192551,13.2232709362659));
#16330=CARTESIAN_POINT('Ctrl Pts',(4.37864656211684,-3.9828059803381,13.231057518599));
#16331=CARTESIAN_POINT('Ctrl Pts',(4.4883313165885,-3.85877971409506,13.238844100932));
#16332=CARTESIAN_POINT('Ctrl Pts',(4.59263331976451,-3.73036858134539,13.246630683265));
#16333=CARTESIAN_POINT('Ctrl Pts',(4.69693929995296,-3.60195255230748,13.2544175624988));
#16334=CARTESIAN_POINT('Ctrl Pts',(4.79586191364239,-3.46915156772926,13.2622044417325));
#16335=CARTESIAN_POINT('Ctrl Pts',(4.8890465883415,-3.33243964979509,13.2699913209662));
#16336=CARTESIAN_POINT('Ctrl Pts',(4.98222511290619,-3.1957367547681,13.2777776862704));
#16337=CARTESIAN_POINT('Ctrl Pts',(5.06966627643691,-3.05512370703689,13.2855640515746));
#16338=CARTESIAN_POINT('Ctrl Pts',(5.15105865855979,-2.91110378698119,13.2933504168788));
#16339=CARTESIAN_POINT('Ctrl Pts',(5.23247241266918,-2.76704605021946,13.3011388267244));
#16340=CARTESIAN_POINT('Ctrl Pts',(5.30783405263702,-2.61957993099091,13.30892723657));
#16341=CARTESIAN_POINT('Ctrl Pts',(5.37687753801227,-2.46923439626924,13.3167156464155));
#16342=CARTESIAN_POINT('Ctrl Pts',(5.44229265298793,-2.32678981389564,13.3240947600677));
#16343=CARTESIAN_POINT('Ctrl Pts',(5.50203648760668,-2.18176090623693,13.3314738737199));
#16344=CARTESIAN_POINT('Ctrl Pts',(5.55592228313402,-2.03461498723343,13.3388529873721));
#16345=CARTESIAN_POINT('Ctrl Pts',(5.61279477458043,-1.87931329894982,13.3466410987651));
#16346=CARTESIAN_POINT('Ctrl Pts',(5.66316174465532,-1.72159780226747,13.354429210158));
#16347=CARTESIAN_POINT('Ctrl Pts',(5.70683732227528,-1.56203019803906,13.362217321551));
#16348=CARTESIAN_POINT('Ctrl Pts',(5.75050432495694,-1.4024939221281,13.3700039038841));
#16349=CARTESIAN_POINT('Ctrl Pts',(5.78748247217824,-1.24110657222112,13.3777904862172));
#16350=CARTESIAN_POINT('Ctrl Pts',(5.81763602785388,-1.07844406897924,13.3855770685502));
#16351=CARTESIAN_POINT('Ctrl Pts',(5.84779073327786,-0.915775363452519,
13.3933639477839));
#16352=CARTESIAN_POINT('Ctrl Pts',(5.87112026433525,-0.751831720743396,
13.4011508270176));
#16353=CARTESIAN_POINT('Ctrl Pts',(5.8875400517566,-0.587199030535578,13.4089377062514));
#16354=CARTESIAN_POINT('Ctrl Pts',(5.90395875548152,-0.422577205989584,
13.4167240715556));
#16355=CARTESIAN_POINT('Ctrl Pts',(5.91346859657836,-0.257266742938307,
13.4245104368598));
#16356=CARTESIAN_POINT('Ctrl Pts',(5.9160368967894,-0.0918585778600394,
13.432296802164));
#16357=CARTESIAN_POINT('Ctrl Pts',(5.91860587138391,0.0735930200429167,
13.4400852120096));
#16358=CARTESIAN_POINT('Ctrl Pts',(5.91422965603774,0.239142051566006,13.4478736218552));
#16359=CARTESIAN_POINT('Ctrl Pts',(5.90292771101162,0.404196735601776,13.4556620317008));
#16360=CARTESIAN_POINT('Ctrl Pts',(5.89221970533505,0.560577472679632,13.4630411453529));
#16361=CARTESIAN_POINT('Ctrl Pts',(5.87529518657233,0.716514224268211,13.470420259005));
#16362=CARTESIAN_POINT('Ctrl Pts',(5.85221373708393,0.871507279364983,13.4777993726572));
#16363=CARTESIAN_POINT('Ctrl Pts',(5.82785296583125,1.03509104228522,13.4855874840502));
#16364=CARTESIAN_POINT('Ctrl Pts',(5.79662469670607,1.1976819546261,13.4933755954432));
#16365=CARTESIAN_POINT('Ctrl Pts',(5.75863444956288,1.35869784676641,13.5011637068362));
#16366=CARTESIAN_POINT('Ctrl Pts',(5.72065166114231,1.51968212624377,13.5089502891693));
#16367=CARTESIAN_POINT('Ctrl Pts',(5.67590961698329,1.67909169172433,13.5167368715024));
#16368=CARTESIAN_POINT('Ctrl Pts',(5.62456466488435,1.83635587319953,13.5245234538355));
#16369=CARTESIAN_POINT('Ctrl Pts',(5.57321775501406,1.9936260511222,13.5323103330692));
#16370=CARTESIAN_POINT('Ctrl Pts',(5.51526752883052,2.14875037638898,13.540097212303));
#16371=CARTESIAN_POINT('Ctrl Pts',(5.45092003441312,2.30117390497409,13.5478840915367));
#16372=CARTESIAN_POINT('Ctrl Pts',(5.38657678689338,2.45358737369387,13.5556704568408));
#16373=CARTESIAN_POINT('Ctrl Pts',(5.31583724044993,2.60330010809086,13.563456822145));
#16374=CARTESIAN_POINT('Ctrl Pts',(5.2389554244086,2.74977755892357,13.5712431874492));
#16375=CARTESIAN_POINT('Ctrl Pts',(5.16205342076334,2.89629347176089,13.5790315972948));
#16376=CARTESIAN_POINT('Ctrl Pts',(5.07900607161702,3.03957211950319,13.5868200071404));
#16377=CARTESIAN_POINT('Ctrl Pts',(4.990113594419,3.17910315612669,13.594608416986));
#16378=CARTESIAN_POINT('Ctrl Pts',(4.90589259102248,3.31130156345884,13.6019875306381));
#16379=CARTESIAN_POINT('Ctrl Pts',(4.81642514389851,3.44013589792041,13.6093666442902));
#16380=CARTESIAN_POINT('Ctrl Pts',(4.72200265304312,3.56519585817578,13.6167457579423));
#16381=CARTESIAN_POINT('Ctrl Pts',(4.62234666298081,3.69718744242121,13.6245338693353));
#16382=CARTESIAN_POINT('Ctrl Pts',(4.51713518100456,3.82502152875385,13.6323219807282));
#16383=CARTESIAN_POINT('Ctrl Pts',(4.40673939698348,3.94823738515983,13.6401100921212));
#16384=CARTESIAN_POINT('Ctrl Pts',(4.29636528725013,4.07142905028035,13.6478966744543));
#16385=CARTESIAN_POINT('Ctrl Pts',(4.18080911946914,4.1900040567933,13.6556832567873));
#16386=CARTESIAN_POINT('Ctrl Pts',(4.0604812148673,4.30353608863801,13.6634698391204));
#16387=CARTESIAN_POINT('Ctrl Pts',(3.94014872218915,4.41707244943392,13.6712567183541));
#16388=CARTESIAN_POINT('Ctrl Pts',(3.81504435830708,4.52556522864861,13.6790435975878));
#16389=CARTESIAN_POINT('Ctrl Pts',(3.68561456353431,4.62862569793279,13.6868304768215));
#16390=CARTESIAN_POINT('Ctrl Pts',(3.55619331105306,4.73167936528567,13.6946168421257));
#16391=CARTESIAN_POINT('Ctrl Pts',(3.42244744901976,4.82930124121891,13.7024032074299));
#16392=CARTESIAN_POINT('Ctrl Pts',(3.28485579359134,4.92114346242918,13.7101895727341));
#16393=CARTESIAN_POINT('Ctrl Pts',(3.14722800938819,5.01300979954175,13.7179779825797));
#16394=CARTESIAN_POINT('Ctrl Pts',(3.00575267880336,5.09909327028345,13.7257663924253));
#16395=CARTESIAN_POINT('Ctrl Pts',(2.86093759716649,5.17908936277597,13.7335548022709));
#16396=CARTESIAN_POINT('Ctrl Pts',(2.72373283173475,5.25488150391093,13.7409339159231));
#16397=CARTESIAN_POINT('Ctrl Pts',(2.58353053539893,5.32520949217967,13.7483130295753));
#16398=CARTESIAN_POINT('Ctrl Pts',(2.44078289577494,5.3898524486476,13.7556921432275));
#16399=CARTESIAN_POINT('Ctrl Pts',(2.2901232676854,5.45807833179158,13.7634802546205));
#16400=CARTESIAN_POINT('Ctrl Pts',(2.13657432894415,5.51999547787825,13.7712683660134));
#16401=CARTESIAN_POINT('Ctrl Pts',(1.9806824602908,5.57537689793223,13.7790564774064));
#16402=CARTESIAN_POINT('Ctrl Pts',(1.82482119828813,5.63074744480987,13.7868430597394));
#16403=CARTESIAN_POINT('Ctrl Pts',(1.66661822510406,5.67958471907336,13.7946296420725));
#16404=CARTESIAN_POINT('Ctrl Pts',(1.50663781781091,5.72171067500289,13.8024162244055));
#16405=CARTESIAN_POINT('Ctrl Pts',(1.3466513105004,5.76383823718574,13.8102031036392));
#16406=CARTESIAN_POINT('Ctrl Pts',(1.18488754144456,5.7992538837969,13.8179899828729));
#16407=CARTESIAN_POINT('Ctrl Pts',(1.02192452142343,5.82782985638853,13.8257768621066));
#16408=CARTESIAN_POINT('Ctrl Pts',(0.85897225686742,5.85640394298248,13.8335632274108));
#16409=CARTESIAN_POINT('Ctrl Pts',(0.694821214508458,5.87813920383052,13.8413495927149));
#16410=CARTESIAN_POINT('Ctrl Pts',(0.530058283814878,5.8929592547598,13.8491359580191));
#16411=CARTESIAN_POINT('Ctrl Pts',(0.365252089721593,5.90778319713351,13.8569243678647));
#16412=CARTESIAN_POINT('Ctrl Pts',(0.199834004521786,5.91568827067656,13.8647127777103));
#16413=CARTESIAN_POINT('Ctrl Pts',(0.0343956241064442,5.91665002375012,
13.8725011875558));
#16414=CARTESIAN_POINT('Ctrl Pts',(-0.12234864535721,5.91756123481579,13.8798803012081));
#16415=CARTESIAN_POINT('Ctrl Pts',(-0.279110871713278,5.91224012403344,
13.8872594148603));
#16416=CARTESIAN_POINT('Ctrl Pts',(-0.435388302423011,5.90070907506998,
13.8946385285126));
#16417=CARTESIAN_POINT('Ctrl Pts',(-0.600327629276045,5.88853890151834,
13.9024266399056));
#16418=CARTESIAN_POINT('Ctrl Pts',(-0.764785803487357,5.86944653384659,
13.9102147512985));
#16419=CARTESIAN_POINT('Ctrl Pts',(-0.928174436127251,5.84349405566737,
13.9180028626915));
#16420=CARTESIAN_POINT('Ctrl Pts',(-1.09153099025755,5.81754667280479,13.9257894450246));
#16421=CARTESIAN_POINT('Ctrl Pts',(-1.25381810642313,5.7847419169213,13.9335760273576));
#16422=CARTESIAN_POINT('Ctrl Pts',(-1.41445509669538,5.74519341205607,13.9413626096907));
#16423=CARTESIAN_POINT('Ctrl Pts',(-1.57509821202015,5.70564339921519,13.9491494889244));
#16424=CARTESIAN_POINT('Ctrl Pts',(-1.73409076435548,5.6593491954094,13.9569363681581));
#16425=CARTESIAN_POINT('Ctrl Pts',(-1.89086406509477,5.60647515376937,13.9647232473918));
#16426=CARTESIAN_POINT('Ctrl Pts',(-2.04762701888733,5.55360460178535,13.972509612696));
#16427=CARTESIAN_POINT('Ctrl Pts',(-2.20217071143322,5.49415518323302,13.9802959780003));
#16428=CARTESIAN_POINT('Ctrl Pts',(-2.35394323681174,5.42834061204419,13.9880823433045));
#16429=CARTESIAN_POINT('Ctrl Pts',(-2.50575561457341,5.36250875928545,13.9958707531501));
#16430=CARTESIAN_POINT('Ctrl Pts',(-2.6547950770493,5.29030853958997,14.0036591629957));
#16431=CARTESIAN_POINT('Ctrl Pts',(-2.8005304318572,5.21200152175167,14.0114475728413));
#16432=CARTESIAN_POINT('Ctrl Pts',(-2.93860710830029,5.1378096910903,14.0188266864935));
#16433=CARTESIAN_POINT('Ctrl Pts',(-3.07371779055359,5.05813652514174,14.0262058001456));
#16434=CARTESIAN_POINT('Ctrl Pts',(-3.20543170927236,4.97324221405828,14.0335849137977));
#16435=CARTESIAN_POINT('Ctrl Pts',(-3.3444460569765,4.8836425165179,14.0413730251907));
#16436=CARTESIAN_POINT('Ctrl Pts',(-3.47972607179349,4.78819448270224,14.0491611365836));
#16437=CARTESIAN_POINT('Ctrl Pts',(-3.61078477896287,4.68723413566146,14.0569492479766));
#16438=CARTESIAN_POINT('Ctrl Pts',(-3.74181775503953,4.58629361042503,14.0647358303096));
#16439=CARTESIAN_POINT('Ctrl Pts',(-3.86863082415813,4.47984312624384,14.0725224126427));
#16440=CARTESIAN_POINT('Ctrl Pts',(-3.99076843274064,4.3682602805626,14.0803089949757));
#16441=CARTESIAN_POINT('Ctrl Pts',(-4.11291069840339,4.25667318025191,14.0880958742094));
#16442=CARTESIAN_POINT('Ctrl Pts',(-4.23037690824559,4.13995353944782,14.0958827534431));
#16443=CARTESIAN_POINT('Ctrl Pts',(-4.34274631615404,4.01851776106944,14.1036696326768));
#16444=CARTESIAN_POINT('Ctrl Pts',(-4.45510830774686,3.89708999738186,14.111455997981));
#16445=CARTESIAN_POINT('Ctrl Pts',(-4.56237395361935,3.770946953628,14.1192423632853));
#16446=CARTESIAN_POINT('Ctrl Pts',(-4.66416086086581,3.64054034814443,14.1270287285895));
#16447=CARTESIAN_POINT('Ctrl Pts',(-4.76597449528655,3.51009950053516,14.134817138435));
#16448=CARTESIAN_POINT('Ctrl Pts',(-4.86230631818407,3.37539310500728,14.1426055482806));
#16449=CARTESIAN_POINT('Ctrl Pts',(-4.95281502113717,3.23690499225695,14.1503939581262));
#16450=CARTESIAN_POINT('Ctrl Pts',(-5.03856731446105,3.10569470110308,14.1577730717784));
#16451=CARTESIAN_POINT('Ctrl Pts',(-5.11909263648977,2.97109016052616,14.1651521854306));
#16452=CARTESIAN_POINT('Ctrl Pts',(-5.19413720297289,2.83352594468323,14.1725312990828));
#16453=CARTESIAN_POINT('Ctrl Pts',(-5.27334530227268,2.68832955566769,14.1803198118866));
#16454=CARTESIAN_POINT('Ctrl Pts',(-5.34647549203921,2.53978395594202,14.1881083246904));
#16455=CARTESIAN_POINT('Ctrl Pts',(-5.41326089867347,2.38841725948228,14.1958968374942));
#16456=CARTESIAN_POINT('Ctrl Pts',(-5.48003320542014,2.2370802534416,14.2036838225893));
#16457=CARTESIAN_POINT('Ctrl Pts',(-5.54046308335368,2.0829235468732,14.2114708076845));
#16458=CARTESIAN_POINT('Ctrl Pts',(-5.59433114166826,1.9264967271866,14.2192577927796));
#16459=CARTESIAN_POINT('Ctrl Pts',(-5.64820127053387,1.77006389485125,14.2270450771867));
#16460=CARTESIAN_POINT('Ctrl Pts',(-5.69550896734166,1.61136107555123,14.2348323615937));
#16461=CARTESIAN_POINT('Ctrl Pts',(-5.73608397242631,1.4509552797292,14.2426196460007));
#16462=CARTESIAN_POINT('Ctrl Pts',(-5.77665628716277,1.29056011970228,14.2504064140676));
#16463=CARTESIAN_POINT('Ctrl Pts',(-5.81049672527585,1.12846251887456,14.2581931821344));
#16464=CARTESIAN_POINT('Ctrl Pts',(-5.83748560214795,0.965242149522809,
14.2659799502012));
#16465=CARTESIAN_POINT('Ctrl Pts',(-5.86448157733698,0.801978851748411,
14.273768766258));
#16466=CARTESIAN_POINT('Ctrl Pts',(-5.88462233636885,0.637592510450985,
14.2815575823147));
#16467=CARTESIAN_POINT('Ctrl Pts',(-5.89783963535104,0.472671342670865,
14.2893463983715));
#16468=CARTESIAN_POINT('Ctrl Pts',(-5.91044148206916,0.315429588531977,
14.2967725348457));
#16469=CARTESIAN_POINT('Ctrl Pts',(-5.91674997047388,0.157701949386365,
14.30419867132));
#16470=CARTESIAN_POINT('Ctrl Pts',(-5.9167499999999,1.10778128295403E-6,
14.3116248077942));
#16471=CARTESIAN_POINT('Origin',(0.,0.,0.));
#16472=CARTESIAN_POINT('',(-5.91670008156886,7.08465806803855E-6,16.3133751922624));
#16473=CARTESIAN_POINT('',(-5.91674999941157,-8.34454905785101E-5,16.0616248078328));
#16474=CARTESIAN_POINT('',(-5.91675,-7.2459289488551E-16,0.));
#16475=CARTESIAN_POINT('Ctrl Pts',(-5.91624282479069,7.08533173049419E-6,
16.3133751922049));
#16476=CARTESIAN_POINT('Ctrl Pts',(-5.9162630038869,0.48475024959515,16.2905618658795));
#16477=CARTESIAN_POINT('Ctrl Pts',(-5.7377459192182,1.95412248637943,16.2214085410499));
#16478=CARTESIAN_POINT('Ctrl Pts',(-4.53467287003993,4.18117692240458,16.1059152177163));
#16479=CARTESIAN_POINT('Ctrl Pts',(-1.98003345441907,5.84165781384912,15.9668952222037));
#16480=CARTESIAN_POINT('Ctrl Pts',(1.05774857675516,6.07673155924276,15.8278752266912));
#16481=CARTESIAN_POINT('Ctrl Pts',(3.83743223447477,4.82903844885686,15.6888552311787));
#16482=CARTESIAN_POINT('Ctrl Pts',(5.68075441676886,2.40302470879641,15.5498352356661));
#16483=CARTESIAN_POINT('Ctrl Pts',(6.13793105636612,-0.609344600385745,
15.4108152401537));
#16484=CARTESIAN_POINT('Ctrl Pts',(5.0974077161784,-3.47302937934159,15.2717952446411));
#16485=CARTESIAN_POINT('Ctrl Pts',(2.81307968620657,-5.48926963937609,15.1327752491286));
#16486=CARTESIAN_POINT('Ctrl Pts',(-0.157660320451772,-6.16608804008501,
14.9937552536161));
#16487=CARTESIAN_POINT('Ctrl Pts',(-3.08993005812401,-5.33833595145761,
14.8547352581036));
#16488=CARTESIAN_POINT('Ctrl Pts',(-5.2682343075742,-3.20799092505311,14.715715262591));
#16489=CARTESIAN_POINT('Ctrl Pts',(-5.89196019578445,-1.17287284551572,
14.6185952406248));
#16490=CARTESIAN_POINT('Ctrl Pts',(-5.91720968061764,-0.0943942614492433,
14.5678152171628));
#16491=CARTESIAN_POINT('Ctrl Pts',(-5.91713904777553,-9.26149740448912E-5,
14.5633751922049));
#16492=CARTESIAN_POINT('Ctrl Pts',(-5.9167499999999,1.10775218765784E-6,
14.3116248077956));
#16493=CARTESIAN_POINT('Ctrl Pts',(-5.91675003096271,-0.165378134030277,
14.3194125203214));
#16494=CARTESIAN_POINT('Ctrl Pts',(-5.90981193875335,-0.330786962771931,
14.3272002328471));
#16495=CARTESIAN_POINT('Ctrl Pts',(-5.8959543270468,-0.495634074573328,
14.3349879453728));
#16496=CARTESIAN_POINT('Ctrl Pts',(-5.88209943852473,-0.660448791968869,
14.342774127521));
#16497=CARTESIAN_POINT('Ctrl Pts',(-5.8613277703964,-0.824701694397815,
14.3505603096692));
#16498=CARTESIAN_POINT('Ctrl Pts',(-5.83370989376855,-0.987805364354207,
14.3583464918173));
#16499=CARTESIAN_POINT('Ctrl Pts',(-5.80609097249611,-1.15091520369749,
14.3661329684774));
#16500=CARTESIAN_POINT('Ctrl Pts',(-5.77162537401302,-1.31287540782977,
14.3739194451375));
#16501=CARTESIAN_POINT('Ctrl Pts',(-5.7304351438749,-1.47310679325821,14.3817059217975));
#16502=CARTESIAN_POINT('Ctrl Pts',(-5.68924761963206,-1.63332765266267,
14.3894918869433));
#16503=CARTESIAN_POINT('Ctrl Pts',(-5.64133642746416,-1.79181961111337,
14.3972778520891));
#16504=CARTESIAN_POINT('Ctrl Pts',(-5.5868740747597,-1.94801659009309,14.4050638172349));
#16505=CARTESIAN_POINT('Ctrl Pts',(-5.53239744487556,-2.10425451574928,
14.4128518234534));
#16506=CARTESIAN_POINT('Ctrl Pts',(-5.47136632627987,-2.25819595716394,
14.4206398296719));
#16507=CARTESIAN_POINT('Ctrl Pts',(-5.40400247469969,-2.40929197399145,
14.4284278358904));
#16508=CARTESIAN_POINT('Ctrl Pts',(-5.340582262263,-2.55154247274941,14.4357599138113));
#16509=CARTESIAN_POINT('Ctrl Pts',(-5.27154958777164,-2.69127090072943,
14.4430919917322));
#16510=CARTESIAN_POINT('Ctrl Pts',(-5.19712781468605,-2.82803695879609,
14.4504240696531));
#16511=CARTESIAN_POINT('Ctrl Pts',(-5.11807722833013,-2.97330945951067,
14.4582121810461));
#16512=CARTESIAN_POINT('Ctrl Pts',(-5.03291762851382,-3.11529133204175,
14.4660002924391));
#16513=CARTESIAN_POINT('Ctrl Pts',(-4.94194802326531,-3.25347203735396,
14.473788403832));
#16514=CARTESIAN_POINT('Ctrl Pts',(-4.85099627831309,-3.39162561329332,
14.4815749861651));
#16515=CARTESIAN_POINT('Ctrl Pts',(-4.75423697954309,-3.52597924436967,
14.4893615684982));
#16516=CARTESIAN_POINT('Ctrl Pts',(-4.65201292374638,-3.65605064513563,
14.4971481508312));
#16517=CARTESIAN_POINT('Ctrl Pts',(-4.54978497016906,-3.78612700549529,
14.5049350300649));
#16518=CARTESIAN_POINT('Ctrl Pts',(-4.44209203694593,-3.91192055516285,
14.5127219092987));
#16519=CARTESIAN_POINT('Ctrl Pts',(-4.32931819929146,-4.03298084446031,
14.5205087885324));
#16520=CARTESIAN_POINT('Ctrl Pts',(-4.21655180464509,-4.15403314384864,
14.5282951538366));
#16521=CARTESIAN_POINT('Ctrl Pts',(-4.09870539452829,-4.27035257427359,
14.5360815191408));
#16522=CARTESIAN_POINT('Ctrl Pts',(-3.97620110490398,-4.38152431647484,
14.5438678844449));
#16523=CARTESIAN_POINT('Ctrl Pts',(-3.85366464814084,-4.4927252501181,14.5516562942906));
#16524=CARTESIAN_POINT('Ctrl Pts',(-3.72646810340338,-4.59877557829264,
14.5594447041362));
#16525=CARTESIAN_POINT('Ctrl Pts',(-3.59506867557559,-4.69929907330819,
14.5672331139818));
#16526=CARTESIAN_POINT('Ctrl Pts',(-3.47057454506767,-4.79453986175346,
14.5746122276339));
#16527=CARTESIAN_POINT('Ctrl Pts',(-3.34230811575963,-4.88481961000261,
14.5819913412861));
#16528=CARTESIAN_POINT('Ctrl Pts',(-3.21068395809315,-4.96985302436031,
14.5893704549382));
#16529=CARTESIAN_POINT('Ctrl Pts',(-3.07176434657417,-5.05959953516903,
14.5971585663312));
#16530=CARTESIAN_POINT('Ctrl Pts',(-2.92905462345105,-5.14353370279028,
14.6049466777241));
#16531=CARTESIAN_POINT('Ctrl Pts',(-2.78306161437668,-5.22135026722811,
14.6127347891171));
#16532=CARTESIAN_POINT('Ctrl Pts',(-2.63709726848453,-5.2991515537401,14.6205213714501));
#16533=CARTESIAN_POINT('Ctrl Pts',(-2.48785120464156,-5.37083748338602,
14.6283079537832));
#16534=CARTESIAN_POINT('Ctrl Pts',(-2.33585518290006,-5.43614855637877,
14.6360945361162));
#16535=CARTESIAN_POINT('Ctrl Pts',(-2.1838533655841,-5.50146211966818,14.6438814153499));
#16536=CARTESIAN_POINT('Ctrl Pts',(-2.02910167255777,-5.5604002101492,14.6516682945836));
#16537=CARTESIAN_POINT('Ctrl Pts',(-1.87215288004449,-5.61275103280389,
14.6594551738174));
#16538=CARTESIAN_POINT('Ctrl Pts',(-1.71521444606072,-5.66509840033457,
14.6672415391215));
#16539=CARTESIAN_POINT('Ctrl Pts',(-1.55607950594408,-5.71085926905235,
14.6750279044257));
#16540=CARTESIAN_POINT('Ctrl Pts',(-1.39531721108171,-5.74987134142662,
14.6828142697299));
#16541=CARTESIAN_POINT('Ctrl Pts',(-1.23451270330536,-5.78889365757886,
14.6906026795755));
#16542=CARTESIAN_POINT('Ctrl Pts',(-1.07208029719107,-5.82116355907977,
14.6983910894211));
#16543=CARTESIAN_POINT('Ctrl Pts',(-0.908601475378053,-5.84656941474578,
14.7061794992667));
#16544=CARTESIAN_POINT('Ctrl Pts',(-0.753713785874834,-5.87064014293137,
14.7135586129189));
#16545=CARTESIAN_POINT('Ctrl Pts',(-0.59788709126143,-5.88854966770614,
14.7209377265711));
#16546=CARTESIAN_POINT('Ctrl Pts',(-0.441621929870274,-5.90024581128258,
14.7283168402233));
#16547=CARTESIAN_POINT('Ctrl Pts',(-0.276695552379318,-5.91259023004812,
14.7361049516163));
#16548=CARTESIAN_POINT('Ctrl Pts',(-0.111221821319569,-5.91801737454039,
14.7438930630093));
#16549=CARTESIAN_POINT('Ctrl Pts',(0.0542081609874399,-5.91650167225383,
14.7516811744022));
#16550=CARTESIAN_POINT('Ctrl Pts',(0.21960566400132,-5.914986267549,14.7594677567353));
#16551=CARTESIAN_POINT('Ctrl Pts',(0.384959116082934,-5.90653073879459,
14.7672543390683));
#16552=CARTESIAN_POINT('Ctrl Pts',(0.549677412743056,-5.89116162606494,
14.7750409214014));
#16553=CARTESIAN_POINT('Ctrl Pts',(0.71440199007518,-5.87579192731444,14.7828278006351));
#16554=CARTESIAN_POINT('Ctrl Pts',(0.878491045024127,-5.85350814285044,
14.7906146798688));
#16555=CARTESIAN_POINT('Ctrl Pts',(1.0413578419649,-5.8243887582714,14.7984015591025));
#16556=CARTESIAN_POINT('Ctrl Pts',(1.20421388979135,-5.79527129555488,14.8061879244067));
#16557=CARTESIAN_POINT('Ctrl Pts',(1.365847526495,-5.75931919189307,14.8139742897109));
#16558=CARTESIAN_POINT('Ctrl Pts',(1.52568131838922,-5.71666223221367,14.8217606550151));
#16559=CARTESIAN_POINT('Ctrl Pts',(1.68555707939135,-5.67399407168291,14.8295490648607));
#16560=CARTESIAN_POINT('Ctrl Pts',(1.84363174179873,-5.62461761774218,14.8373374747063));
#16561=CARTESIAN_POINT('Ctrl Pts',(1.99934128413789,-5.5687130463009,14.8451258845519));
#16562=CARTESIAN_POINT('Ctrl Pts',(2.14686798502193,-5.51574636959522,14.8525049982041));
#16563=CARTESIAN_POINT('Ctrl Pts',(2.29227151074867,-5.45692014637828,14.8598841118563));
#16564=CARTESIAN_POINT('Ctrl Pts',(2.43508736348934,-5.3924280333329,14.8672632255085));
#16565=CARTESIAN_POINT('Ctrl Pts',(2.58581898550395,-5.32436135431982,14.8750513369015));
#16566=CARTESIAN_POINT('Ctrl Pts',(2.73372178324025,-5.24995858562116,14.8828394482945));
#16567=CARTESIAN_POINT('Ctrl Pts',(2.87826446146846,-5.16948007563117,14.8906275596874));
#16568=CARTESIAN_POINT('Ctrl Pts',(3.02277876126157,-5.08901736619366,14.8984141420205));
#16569=CARTESIAN_POINT('Ctrl Pts',(3.16393397884555,-5.00248145092886,14.9062007243536));
#16570=CARTESIAN_POINT('Ctrl Pts',(3.30122374958302,-4.91017844051405,14.9139873066866));
#16571=CARTESIAN_POINT('Ctrl Pts',(3.4385187551488,-4.81787191060606,14.9217741859203));
#16572=CARTESIAN_POINT('Ctrl Pts',(3.57194775158137,-4.71979802052766,14.929561065154));
#16573=CARTESIAN_POINT('Ctrl Pts',(3.70103306321329,-4.61630640528789,14.9373479443878));
#16574=CARTESIAN_POINT('Ctrl Pts',(3.83010985528933,-4.51282162043485,14.9451343096919));
#16575=CARTESIAN_POINT('Ctrl Pts',(3.95484328701192,-4.40392002594475,14.9529206749961));
#16576=CARTESIAN_POINT('Ctrl Pts',(4.07478839436612,-4.28999185356326,14.9607070403003));
#16577=CARTESIAN_POINT('Ctrl Pts',(4.19476499686976,-4.17603376595728,14.9684954501459));
#16578=CARTESIAN_POINT('Ctrl Pts',(4.30995052945779,-4.05704668186232,14.9762838599915));
#16579=CARTESIAN_POINT('Ctrl Pts',(4.41993591450846,-3.93345866561964,14.9840722698371));
#16580=CARTESIAN_POINT('Ctrl Pts',(4.52414135213382,-3.81636544171644,14.9914513834893));
#16581=CARTESIAN_POINT('Ctrl Pts',(4.62367896750848,-3.69514261813513,14.9988304971414));
#16582=CARTESIAN_POINT('Ctrl Pts',(4.71823352667229,-3.5701824813706,15.0062096107936));
#16583=CARTESIAN_POINT('Ctrl Pts',(4.81802890511365,-3.43829625347443,15.0139977221866));
#16584=CARTESIAN_POINT('Ctrl Pts',(4.91230881964435,-3.30219956988426,15.0217858335795));
#16585=CARTESIAN_POINT('Ctrl Pts',(5.00073128764819,-3.16237523884129,15.0295739449725));
#16586=CARTESIAN_POINT('Ctrl Pts',(5.08913639544186,-3.02257835986821,15.0373605273055));
#16587=CARTESIAN_POINT('Ctrl Pts',(5.17168618063996,-2.8790555636108,15.0451471096386));
#16588=CARTESIAN_POINT('Ctrl Pts',(5.24808244703849,-2.73231791554102,15.0529336919716));
#16589=CARTESIAN_POINT('Ctrl Pts',(5.32448162640965,-2.5855746723974,15.0607205712053));
#16590=CARTESIAN_POINT('Ctrl Pts',(5.39472666642934,-2.43561661373874,15.068507450439));
#16591=CARTESIAN_POINT('Ctrl Pts',(5.45856538690808,-2.28297929893134,15.0762943296727));
#16592=CARTESIAN_POINT('Ctrl Pts',(5.5223998940682,-2.13035205809842,15.0840806949769));
#16593=CARTESIAN_POINT('Ctrl Pts',(5.57982880461097,-1.97504620983258,15.0918670602811));
#16594=CARTESIAN_POINT('Ctrl Pts',(5.63064808610609,-1.81761731201314,15.0996534255853));
#16595=CARTESIAN_POINT('Ctrl Pts',(5.68148071171253,-1.66014707656208,15.1074418354309));
#16596=CARTESIAN_POINT('Ctrl Pts',(5.72570014020122,-1.50055298129828,15.1152302452764));
#16597=CARTESIAN_POINT('Ctrl Pts',(5.76315195225073,-1.33940663645087,15.123018655122));
#16598=CARTESIAN_POINT('Ctrl Pts',(5.79863559821622,-1.18672884767953,15.1303977687743));
#16599=CARTESIAN_POINT('Ctrl Pts',(5.82804457680214,-1.03265801393605,15.1377768824265));
#16600=CARTESIAN_POINT('Ctrl Pts',(5.85128975756504,-0.877689429989035,
15.1451559960787));
#16601=CARTESIAN_POINT('Ctrl Pts',(5.87582333512782,-0.714131494568395,
15.1529441074717));
#16602=CARTESIAN_POINT('Ctrl Pts',(5.8934992274515,-0.549515054323571,15.1607322188647));
#16603=CARTESIAN_POINT('Ctrl Pts',(5.90424812428272,-0.384427690735162,
15.1685203302576));
#16604=CARTESIAN_POINT('Ctrl Pts',(5.91499491075543,-0.219372739172725,
15.1763069125907));
#16605=CARTESIAN_POINT('Ctrl Pts',(5.91881739458184,-0.0538473674034925,
15.1840934949238));
#16606=CARTESIAN_POINT('Ctrl Pts',(5.91569823461231,0.111556978736245,15.1918800772569));
#16607=CARTESIAN_POINT('Ctrl Pts',(5.91257895570991,0.276967631706899,15.1996669564906));
#16608=CARTESIAN_POINT('Ctrl Pts',(5.90251750545671,0.442256930280642,15.2074538357243));
#16609=CARTESIAN_POINT('Ctrl Pts',(5.88554866915859,0.60683393565751,15.215240714958));
#16610=CARTESIAN_POINT('Ctrl Pts',(5.86858095279385,0.771400079047217,15.2230270802622));
#16611=CARTESIAN_POINT('Ctrl Pts',(5.84470679556843,0.935253705460038,15.2308134455664));
#16612=CARTESIAN_POINT('Ctrl Pts',(5.81401283042844,1.09780935053107,15.2385998108706));
#16613=CARTESIAN_POINT('Ctrl Pts',(5.78331080567652,1.26040767941348,15.2463882207162));
#16614=CARTESIAN_POINT('Ctrl Pts',(5.74578545214969,1.4217070313706,15.2541766305619));
#16615=CARTESIAN_POINT('Ctrl Pts',(5.70157464920767,1.58113158276359,15.2619650404075));
#16616=CARTESIAN_POINT('Ctrl Pts',(5.65968721056133,1.7321780616966,15.2693441540596));
#16617=CARTESIAN_POINT('Ctrl Pts',(5.61179898598714,1.88154147012821,15.2767232677117));
#16618=CARTESIAN_POINT('Ctrl Pts',(5.55806867449139,2.02874423526907,15.2841023813638));
#16619=CARTESIAN_POINT('Ctrl Pts',(5.50136028499707,2.18410592046812,15.2918904927568));
#16620=CARTESIAN_POINT('Ctrl Pts',(5.43812357952267,2.33711614446931,15.2996786041497));
#16621=CARTESIAN_POINT('Ctrl Pts',(5.36857881485322,2.48722577809277,15.3074667155427));
#16622=CARTESIAN_POINT('Ctrl Pts',(5.29904770408597,2.63730594030648,15.3152532978758));
#16623=CARTESIAN_POINT('Ctrl Pts',(5.22321113949174,2.78448635867911,15.3230398802088));
#16624=CARTESIAN_POINT('Ctrl Pts',(5.14133686195587,2.92823937450369,15.3308264625419));
#16625=CARTESIAN_POINT('Ctrl Pts',(5.05945946257203,3.07199787159876,15.3386133417756));
#16626=CARTESIAN_POINT('Ctrl Pts',(4.97154404428249,3.21232842504674,15.3464002210093));
#16627=CARTESIAN_POINT('Ctrl Pts',(4.877903878819,3.34872876051533,15.354187100243));
#16628=CARTESIAN_POINT('Ctrl Pts',(4.78426989355225,3.48512009364071,15.3619734655472));
#16629=CARTESIAN_POINT('Ctrl Pts',(4.68491209816364,3.61758146448982,15.3697598308514));
#16630=CARTESIAN_POINT('Ctrl Pts',(4.58018667381851,3.74564021169617,15.3775461961556));
#16631=CARTESIAN_POINT('Ctrl Pts',(4.47543375070362,3.87373258452904,15.3853346060012));
#16632=CARTESIAN_POINT('Ctrl Pts',(4.36531058320663,3.99741977497081,15.3931230158467));
#16633=CARTESIAN_POINT('Ctrl Pts',(4.25021374067511,4.116262105488,15.4009114256923));
#16634=CARTESIAN_POINT('Ctrl Pts',(4.14116546267098,4.22885903874746,15.4082905393446));
#16635=CARTESIAN_POINT('Ctrl Pts',(4.02765299784576,4.33710704178295,15.4156696529968));
#16636=CARTESIAN_POINT('Ctrl Pts',(3.91004419108284,4.44066267422772,15.423048766649));
#16637=CARTESIAN_POINT('Ctrl Pts',(3.78591675098202,4.54995802308117,15.430836878042));
#16638=CARTESIAN_POINT('Ctrl Pts',(3.65718166955882,4.65406512360351,15.4386249894349));
#16639=CARTESIAN_POINT('Ctrl Pts',(3.52429508208788,4.75260715154021,15.4464131008279));
#16640=CARTESIAN_POINT('Ctrl Pts',(3.39143458458177,4.85112983246763,15.454199683161));
#16641=CARTESIAN_POINT('Ctrl Pts',(3.25442446384809,4.94408943067253,15.461986265494));
#16642=CARTESIAN_POINT('Ctrl Pts',(3.11375227980248,5.03115069368081,15.4697728478271));
#16643=CARTESIAN_POINT('Ctrl Pts',(2.97307473195789,5.11821527631561,15.4775597270608));
#16644=CARTESIAN_POINT('Ctrl Pts',(2.82873511100821,5.1993809022184,15.4853466062945));
#16645=CARTESIAN_POINT('Ctrl Pts',(2.68124881376462,5.27435639307639,15.4931334855282));
#16646=CARTESIAN_POINT('Ctrl Pts',(2.53377225053131,5.34932693559537,15.5009198508324));
#16647=CARTESIAN_POINT('Ctrl Pts',(2.38314971151354,5.41810801592708,15.5087062161366));
#16648=CARTESIAN_POINT('Ctrl Pts',(2.22992010538849,5.48045498896617,15.5164925814408));
#16649=CARTESIAN_POINT('Ctrl Pts',(2.07665026428052,5.54281833305429,15.5242809912864));
#16650=CARTESIAN_POINT('Ctrl Pts',(1.92077228359581,5.59874407164264,15.532069401132));
#16651=CARTESIAN_POINT('Ctrl Pts',(1.76284475716744,5.64803584661316,15.5398578109775));
#16652=CARTESIAN_POINT('Ctrl Pts',(1.61321663160311,5.69473724225569,15.5472369246297));
#16653=CARTESIAN_POINT('Ctrl Pts',(1.46174908326808,5.73548391859867,15.5546160382819));
#16654=CARTESIAN_POINT('Ctrl Pts',(1.30892943913352,5.7701502827803,15.5619951519341));
#16655=CARTESIAN_POINT('Ctrl Pts',(1.14763955153279,5.80673807889805,15.5697832633271));
#16656=CARTESIAN_POINT('Ctrl Pts',(0.984785829869154,5.83656549763545,15.57757137472));
#16657=CARTESIAN_POINT('Ctrl Pts',(0.820949102950824,5.85951987221344,15.585359486113));
#16658=CARTESIAN_POINT('Ctrl Pts',(0.657144542517688,5.88246974010015,15.5931460684461));
#16659=CARTESIAN_POINT('Ctrl Pts',(0.49235767815655,5.89854921197925,15.6009326507791));
#16660=CARTESIAN_POINT('Ctrl Pts',(0.327177043964479,5.90769716085741,15.6087192331122));
#16661=CARTESIAN_POINT('Ctrl Pts',(0.161990111471635,5.91684545854481,15.6165061123459));
#16662=CARTESIAN_POINT('Ctrl Pts',(-0.00359030208728486,5.91906168276146,
15.6242929915796));
#16663=CARTESIAN_POINT('Ctrl Pts',(-0.168972305034811,5.91433672719361,
15.6320798708133));
#16664=CARTESIAN_POINT('Ctrl Pts',(-0.334343392865846,5.90961208347009,
15.6398662361175));
#16665=CARTESIAN_POINT('Ctrl Pts',(-0.499515776870923,5.89794718596203,
15.6476526014217));
#16666=CARTESIAN_POINT('Ctrl Pts',(-0.663899182193702,5.87938503913314,
15.6554389667259));
#16667=CARTESIAN_POINT('Ctrl Pts',(-0.828325751260559,5.86081801826143,
15.6632273765715));
#16668=CARTESIAN_POINT('Ctrl Pts',(-0.991962609739375,5.83535016310612,
15.6710157864171));
#16669=CARTESIAN_POINT('Ctrl Pts',(-1.15422529898659,5.80307629810942,15.6788041962627));
#16670=CARTESIAN_POINT('Ctrl Pts',(-1.30796076607134,5.77249848793681,15.6861833099149));
#16671=CARTESIAN_POINT('Ctrl Pts',(-1.4604625245801,5.7358116581035,15.693562423567));
#16672=CARTESIAN_POINT('Ctrl Pts',(-1.61124255352161,5.69313867705866,15.7009415372192));
#16673=CARTESIAN_POINT('Ctrl Pts',(-1.77037977739198,5.64810048608985,15.7087296486122));
#16674=CARTESIAN_POINT('Ctrl Pts',(-1.92765583671498,5.59637766006532,15.7165177600051));
#16675=CARTESIAN_POINT('Ctrl Pts',(-2.08250678869568,5.53814915269862,15.7243058713981));
#16676=CARTESIAN_POINT('Ctrl Pts',(-2.23732733839127,5.47993207748432,15.7320924537311));
#16677=CARTESIAN_POINT('Ctrl Pts',(-2.38972343186278,5.41521198186983,15.7398790360642));
#16678=CARTESIAN_POINT('Ctrl Pts',(-2.53914901857623,5.34421676431293,15.7476656183972));
#16679=CARTESIAN_POINT('Ctrl Pts',(-2.68858030285425,5.27321883972409,15.7554524976309));
#16680=CARTESIAN_POINT('Ctrl Pts',(-2.83504056343902,5.195945447968,15.7632393768646));
#16681=CARTESIAN_POINT('Ctrl Pts',(-2.97800568995612,5.1126717744335,15.7710262560983));
#16682=CARTESIAN_POINT('Ctrl Pts',(-3.1209613808575,5.02940359691332,15.7788126214025));
#16683=CARTESIAN_POINT('Ctrl Pts',(-3.26042212324386,4.94013609104064,15.7865989867066));
#16684=CARTESIAN_POINT('Ctrl Pts',(-3.39589015814186,4.84518942832324,15.7943853520108));
#16685=CARTESIAN_POINT('Ctrl Pts',(-3.53139376419482,4.75021783454032,15.8021737618564));
#16686=CARTESIAN_POINT('Ctrl Pts',(-3.66290230488369,4.64956428604458,15.809962171702));
#16687=CARTESIAN_POINT('Ctrl Pts',(-3.78994792108942,4.54359167596847,15.8177505815476));
#16688=CARTESIAN_POINT('Ctrl Pts',(-3.91031704130632,4.44318813413124,15.8251296951998));
#16689=CARTESIAN_POINT('Ctrl Pts',(-4.02668004342882,4.33801037237021,15.8325088088521));
#16690=CARTESIAN_POINT('Ctrl Pts',(-4.13866716968353,4.22839977072695,15.8398879225043));
#16691=CARTESIAN_POINT('Ctrl Pts',(-4.25686133973629,4.1127138475009,15.8476760338973));
#16692=CARTESIAN_POINT('Ctrl Pts',(-4.37022301358027,3.99204844039662,15.8554641452903));
#16693=CARTESIAN_POINT('Ctrl Pts',(-4.47834259794153,3.86683050287471,15.8632522566833));
#16694=CARTESIAN_POINT('Ctrl Pts',(-4.58644095490732,3.74163714971184,15.8710388390164));
#16695=CARTESIAN_POINT('Ctrl Pts',(-4.68929906724063,3.61189329124728,15.8788254213495));
#16696=CARTESIAN_POINT('Ctrl Pts',(-4.78654647016189,3.47806030015018,15.8866120036826));
#16697=CARTESIAN_POINT('Ctrl Pts',(-4.88379758110478,3.3442222060312,15.8943988829163));
#16698=CARTESIAN_POINT('Ctrl Pts',(-4.97543736353533,3.20629492344992,15.90218576215));
#16699=CARTESIAN_POINT('Ctrl Pts',(-5.06113724256425,3.06477085186301,15.9099726413837));
#16700=CARTESIAN_POINT('Ctrl Pts',(-5.14683146545077,2.92325612078289,15.9177590066879));
#16701=CARTESIAN_POINT('Ctrl Pts',(-5.22658640402623,2.77814534914727,15.9255453719922));
#16702=CARTESIAN_POINT('Ctrl Pts',(-5.30011814611382,2.62995783231119,15.9333317372964));
#16703=CARTESIAN_POINT('Ctrl Pts',(-5.37366919614364,2.4817314044425,15.941120147142));
#16704=CARTESIAN_POINT('Ctrl Pts',(-5.44099364058232,2.3304269025924,15.9489085569876));
#16705=CARTESIAN_POINT('Ctrl Pts',(-5.50185426252937,2.17658683180511,15.9566969668332));
#16706=CARTESIAN_POINT('Ctrl Pts',(-5.55951653957791,2.03083135808319,15.9640760804853));
#16707=CARTESIAN_POINT('Ctrl Pts',(-5.61137679771396,1.88280020103458,15.9714551941374));
#16708=CARTESIAN_POINT('Ctrl Pts',(-5.65727367244669,1.73297003942408,15.9788343077895));
#16709=CARTESIAN_POINT('Ctrl Pts',(-5.70591845315597,1.57416934988649,15.9866552186364));
#16710=CARTESIAN_POINT('Ctrl Pts',(-5.74788083090549,1.41329275660616,15.9944761294833));
#16711=CARTESIAN_POINT('Ctrl Pts',(-5.78300440114525,1.25091592796425,16.0022970403302));
#16712=CARTESIAN_POINT('Ctrl Pts',(-5.81812005154061,1.08857571289005,16.0101161876776));
#16713=CARTESIAN_POINT('Ctrl Pts',(-5.8463999057942,0.924736244257924,16.017935335025));
#16714=CARTESIAN_POINT('Ctrl Pts',(-5.86773839626611,0.759984654769045,
16.0257544823725));
#16715=CARTESIAN_POINT('Ctrl Pts',(-5.88907483684367,0.595248892236278,
16.033572878569));
#16716=CARTESIAN_POINT('Ctrl Pts',(-5.9034712026441,0.429601494728204,16.0413912747655));
#16717=CARTESIAN_POINT('Ctrl Pts',(-5.91087356280468,0.263636657232531,
16.0492096709621));
#16718=CARTESIAN_POINT('Ctrl Pts',(-5.91479172845615,0.175789306992596,
16.0533480499064));
#16719=CARTESIAN_POINT('Ctrl Pts',(-5.91675123959221,0.0878531121041889,
16.0574864288508));
#16720=CARTESIAN_POINT('Ctrl Pts',(-5.91674999941158,-8.34446900113325E-5,
16.0616248077951));
#16721=CARTESIAN_POINT('Origin',(0.,0.,0.));
#16722=CARTESIAN_POINT('',(-5.9167499994649,7.95746162001808E-5,18.0633751922476));
#16723=CARTESIAN_POINT('',(-5.91674999819064,0.000146325028563304,17.8116248078341));
#16724=CARTESIAN_POINT('',(-5.91675,-7.2459289488551E-16,0.));
#16725=CARTESIAN_POINT('Ctrl Pts',(-5.91674999946489,7.95755227456555E-5,
18.0633751922049));
#16726=CARTESIAN_POINT('Ctrl Pts',(-5.91674893504203,0.0792235603697716,
18.0596485131004));
#16727=CARTESIAN_POINT('Ctrl Pts',(-5.9151597379013,0.158363133491373,18.055921833996));
#16728=CARTESIAN_POINT('Ctrl Pts',(-5.91198387910413,0.23743878308492,18.0521951548916));
#16729=CARTESIAN_POINT('Ctrl Pts',(-5.90534700026585,0.402690306823815,
18.0444071771304));
#16730=CARTESIAN_POINT('Ctrl Pts',(-5.89177593913822,0.567692935344161,
18.0366191993691));
#16731=CARTESIAN_POINT('Ctrl Pts',(-5.87131301784458,0.731856549460908,
18.0288312216077));
#16732=CARTESIAN_POINT('Ctrl Pts',(-5.85085411973669,0.895987887603674,
18.0210447750296));
#16733=CARTESIAN_POINT('Ctrl Pts',(-5.82350610458599,1.05928022357998,18.0132583284514));
#16734=CARTESIAN_POINT('Ctrl Pts',(-5.78936306414922,1.22114940689694,18.0054718818733));
#16735=CARTESIAN_POINT('Ctrl Pts',(-5.75521872123245,1.38302476515821,17.9976851382597));
#16736=CARTESIAN_POINT('Ctrl Pts',(-5.7142788964161,1.54347654864934,17.9898983946461));
#16737=CARTESIAN_POINT('Ctrl Pts',(-5.66668878439145,1.70193089852442,17.9821116510325));
#16738=CARTESIAN_POINT('Ctrl Pts',(-5.61910182009667,1.86037476782972,17.9743254224537));
#16739=CARTESIAN_POINT('Ctrl Pts',(-5.56486554086642,2.01682116186363,17.9665391938749));
#16740=CARTESIAN_POINT('Ctrl Pts',(-5.50417503703645,2.1707113405897,17.9587529652961));
#16741=CARTESIAN_POINT('Ctrl Pts',(-5.44346855664941,2.32464203035241,17.9509646870206));
#16742=CARTESIAN_POINT('Ctrl Pts',(-5.37630457209364,2.47601486199876,17.9431764087451));
#16743=CARTESIAN_POINT('Ctrl Pts',(-5.30292669648032,2.62429019246278,17.9353881304696));
#16744=CARTESIAN_POINT('Ctrl Pts',(-5.23316627909153,2.76525569269255,17.9279838067726));
#16745=CARTESIAN_POINT('Ctrl Pts',(-5.15779000658236,2.90342150635967,17.9205794830756));
#16746=CARTESIAN_POINT('Ctrl Pts',(-5.07704608213876,3.03834389797131,17.9131751593787));
#16747=CARTESIAN_POINT('Ctrl Pts',(-4.9921184218028,3.18025727567085,17.9053871816171));
#16748=CARTESIAN_POINT('Ctrl Pts',(-4.90122171273217,3.31863295778427,17.8975992038555));
#16749=CARTESIAN_POINT('Ctrl Pts',(-4.80467558436886,3.45297308003838,17.8898112260939));
#16750=CARTESIAN_POINT('Ctrl Pts',(-4.70814843780226,3.58728678987252,17.8820247795155));
#16751=CARTESIAN_POINT('Ctrl Pts',(-4.60597427453763,3.71756626363497,17.8742383329372));
#16752=CARTESIAN_POINT('Ctrl Pts',(-4.49851532054828,3.84334365797444,17.8664518863588));
#16753=CARTESIAN_POINT('Ctrl Pts',(-4.39105226724193,3.96912585043815,17.8586651427451));
#16754=CARTESIAN_POINT('Ctrl Pts',(-4.27830422435648,4.09040537430116,17.8508783991313));
#16755=CARTESIAN_POINT('Ctrl Pts',(-4.1606733597801,4.2067478835457,17.8430916555176));
#16756=CARTESIAN_POINT('Ctrl Pts',(-4.04305027560537,4.32308269760365,17.8353054269387));
#16757=CARTESIAN_POINT('Ctrl Pts',(-3.92054524333074,4.43448092586513,17.8275191983598));
#16758=CARTESIAN_POINT('Ctrl Pts',(-3.79359700215806,4.54054537998657,17.8197329697809));
#16759=CARTESIAN_POINT('Ctrl Pts',(-3.66661534231701,4.64663775519448,17.8119446915053));
#16760=CARTESIAN_POINT('Ctrl Pts',(-3.53518838048702,4.74739334405995,17.8041564132298));
#16761=CARTESIAN_POINT('Ctrl Pts',(-3.3997883175939,4.84245495157694,17.7963681349542));
#16762=CARTESIAN_POINT('Ctrl Pts',(-3.27106334673067,4.93283011386543,17.7889638112583));
#16763=CARTESIAN_POINT('Ctrl Pts',(-3.13874779404817,5.01805903521906,17.7815594875624));
#16764=CARTESIAN_POINT('Ctrl Pts',(-3.0032719827193,5.09787092424997,17.7741551638666));
#16765=CARTESIAN_POINT('Ctrl Pts',(-2.86077650991355,5.18181825589113,17.7663671861051));
#16766=CARTESIAN_POINT('Ctrl Pts',(-2.7147336133888,5.25980231512419,17.7585792083436));
#16767=CARTESIAN_POINT('Ctrl Pts',(-2.5656622379888,5.3315389751045,17.750791230582));
#16768=CARTESIAN_POINT('Ctrl Pts',(-2.41662017129931,5.4032615310424,17.7430047840037));
#16769=CARTESIAN_POINT('Ctrl Pts',(-2.26455110155002,5.4687390000518,17.7352183374254));
#16770=CARTESIAN_POINT('Ctrl Pts',(-2.10999700314931,5.52773400311565,17.7274318908471));
#16771=CARTESIAN_POINT('Ctrl Pts',(-1.95543700885806,5.58673125670591,17.7196451472334));
#16772=CARTESIAN_POINT('Ctrl Pts',(-1.7983920933421,5.63924543186964,17.7118584036196));
#16773=CARTESIAN_POINT('Ctrl Pts',(-1.63942326578623,5.68508767901594,17.7040716600059));
#16774=CARTESIAN_POINT('Ctrl Pts',(-1.4804649528289,5.73092689404058,17.696285431427));
#16775=CARTESIAN_POINT('Ctrl Pts',(-1.31958328957831,5.77009497571143,17.6884992028481));
#16776=CARTESIAN_POINT('Ctrl Pts',(-1.15735360853468,5.80245320423282,17.6807129742692));
#16777=CARTESIAN_POINT('Ctrl Pts',(-0.995081221110475,5.8348199509416,17.6729246959936));
#16778=CARTESIAN_POINT('Ctrl Pts',(-0.831460420009935,5.86037319790401,
17.665136417718));
#16779=CARTESIAN_POINT('Ctrl Pts',(-0.667076773500843,5.87902535636271,
17.6573481394424));
#16780=CARTESIAN_POINT('Ctrl Pts',(-0.510797081630046,5.89675798146596,
17.6499438157462));
#16781=CARTESIAN_POINT('Ctrl Pts',(-0.353828209411745,5.90825353161256,
17.64253949205));
#16782=CARTESIAN_POINT('Ctrl Pts',(-0.196677598010754,5.91348023459458,
17.6351351683539));
#16783=CARTESIAN_POINT('Ctrl Pts',(-0.03138424820307,5.91897775850903,17.6273471905923));
#16784=CARTESIAN_POINT('Ctrl Pts',(0.13416930302721,5.91754151518804,17.6195592128308));
#16785=CARTESIAN_POINT('Ctrl Pts',(0.299391421764328,5.90917044423952,17.6117712350693));
#16786=CARTESIAN_POINT('Ctrl Pts',(0.46458105641641,5.90080101911532,17.603984788491));
#16787=CARTESIAN_POINT('Ctrl Pts',(0.629439069648811,5.88549950300046,17.5961983419126));
#16788=CARTESIAN_POINT('Ctrl Pts',(0.793375984329712,5.86331690342496,17.5884118953343));
#16789=CARTESIAN_POINT('Ctrl Pts',(0.957319152834323,5.8411334576333,17.5806251517206));
#16790=CARTESIAN_POINT('Ctrl Pts',(1.12034083529254,5.8120684420466,17.5728384081069));
#16791=CARTESIAN_POINT('Ctrl Pts',(1.28185807155892,5.77622458417947,17.5650516644932));
#16792=CARTESIAN_POINT('Ctrl Pts',(1.44336462466847,5.74038309711538,17.5572654359143));
#16793=CARTESIAN_POINT('Ctrl Pts',(1.60336661875418,5.6977637343724,17.5494792073355));
#16794=CARTESIAN_POINT('Ctrl Pts',(1.76129251334702,5.64852009334549,17.5416929787566));
#16795=CARTESIAN_POINT('Ctrl Pts',(1.91925998136431,5.59926348910697,17.533904700481));
#16796=CARTESIAN_POINT('Ctrl Pts',(2.075149951966,5.54337921538932,17.5261164222055));
#16797=CARTESIAN_POINT('Ctrl Pts',(2.22840637247383,5.48107066198001,17.5183281439299));
#16798=CARTESIAN_POINT('Ctrl Pts',(2.37410739981275,5.42183385993508,17.5109238202338));
#16799=CARTESIAN_POINT('Ctrl Pts',(2.51742804099188,5.35679104072722,17.5035194965376));
#16800=CARTESIAN_POINT('Ctrl Pts',(2.65790755620268,5.28615720397916,17.4961151728415));
#16801=CARTESIAN_POINT('Ctrl Pts',(2.80566599914875,5.21186348420414,17.4883271950799));
#16802=CARTESIAN_POINT('Ctrl Pts',(2.95033393017463,5.13135739218281,17.4805392173184));
#16803=CARTESIAN_POINT('Ctrl Pts',(3.09139138928646,5.04492119271902,17.4727512395569));
#16804=CARTESIAN_POINT('Ctrl Pts',(3.23242111529251,4.95850198735309,17.4649647929786));
#16805=CARTESIAN_POINT('Ctrl Pts',(3.36984151344637,4.86615516773485,17.4571783464002));
#16806=CARTESIAN_POINT('Ctrl Pts',(3.50315944061564,4.76820768173174,17.4493918998219));
#16807=CARTESIAN_POINT('Ctrl Pts',(3.63648245356332,4.67025645925282,17.4416051562082));
#16808=CARTESIAN_POINT('Ctrl Pts',(3.76570242251492,4.56670432887035,17.4338184125945));
#16809=CARTESIAN_POINT('Ctrl Pts',(3.89035668289502,4.45792052894105,17.4260316689807));
#16810=CARTESIAN_POINT('Ctrl Pts',(4.01500269832836,4.34914392424628,17.4182454404019));
#16811=CARTESIAN_POINT('Ctrl Pts',(4.13508336880468,4.23513655268629,17.410459211823));
#16812=CARTESIAN_POINT('Ctrl Pts',(4.25017040593234,4.11630684996113,17.4026729832441));
#16813=CARTESIAN_POINT('Ctrl Pts',(4.36528773930906,3.99744586574364,17.3948847049685));
#16814=CARTESIAN_POINT('Ctrl Pts',(4.47540858871175,3.8737602420439,17.3870964266929));
#16815=CARTESIAN_POINT('Ctrl Pts',(4.58014209796389,3.74569471860147,17.3793081484173));
#16816=CARTESIAN_POINT('Ctrl Pts',(4.67971234659843,3.62394270148939,17.3719038247212));
#16817=CARTESIAN_POINT('Ctrl Pts',(4.77441347416384,3.49823243557518,17.3644995010251));
#16818=CARTESIAN_POINT('Ctrl Pts',(4.86394386608415,3.36897323083493,17.3570951773289));
#16819=CARTESIAN_POINT('Ctrl Pts',(4.95811326357019,3.23301647728081,17.3493071995674));
#16820=CARTESIAN_POINT('Ctrl Pts',(5.04659554326005,3.09308461064301,17.3415192218059));
#16821=CARTESIAN_POINT('Ctrl Pts',(5.12906929311559,2.94967434624888,17.3337312440443));
#16822=CARTESIAN_POINT('Ctrl Pts',(5.21152682792484,2.80629227754222,17.325944797466));
#16823=CARTESIAN_POINT('Ctrl Pts',(5.28797803079056,2.65943345246605,17.3181583508877));
#16824=CARTESIAN_POINT('Ctrl Pts',(5.35814642310363,2.50962098155912,17.3103719043093));
#16825=CARTESIAN_POINT('Ctrl Pts',(5.4283174921827,2.35980279564414,17.3025851606956));
#16826=CARTESIAN_POINT('Ctrl Pts',(5.49220513200002,2.20703102612777,17.2947984170819));
#16827=CARTESIAN_POINT('Ctrl Pts',(5.54957986708367,2.05185132535463,17.2870116734682));
#16828=CARTESIAN_POINT('Ctrl Pts',(5.60695080725784,1.89668188855775,17.2792254448893));
#16829=CARTESIAN_POINT('Ctrl Pts',(5.65780959403473,1.73910513900488,17.2714392163104));
#16830=CARTESIAN_POINT('Ctrl Pts',(5.70197569659381,1.57968468940912,17.2636529877316));
#16831=CARTESIAN_POINT('Ctrl Pts',(5.74615342572071,1.42022227295274,17.255864709456));
#16832=CARTESIAN_POINT('Ctrl Pts',(5.78363486287517,1.25891549426072,17.2480764311804));
#16833=CARTESIAN_POINT('Ctrl Pts',(5.81428972014246,1.096341923282,17.2402881529048));
#16834=CARTESIAN_POINT('Ctrl Pts',(5.84343332262229,0.941783071971193,17.2328838292087));
#16835=CARTESIAN_POINT('Ctrl Pts',(5.86640717020521,0.786079581818818,17.2254795055126));
#16836=CARTESIAN_POINT('Ctrl Pts',(5.88314236970594,0.629735198532512,17.2180751818164));
#16837=CARTESIAN_POINT('Ctrl Pts',(5.90074470138335,0.465289851443275,17.2102872040549));
#16838=CARTESIAN_POINT('Ctrl Pts',(5.91145100764235,0.30007660704057,17.2024992262934));
#16839=CARTESIAN_POINT('Ctrl Pts',(5.91521685128385,0.134685429009756,17.1947112485319));
#16840=CARTESIAN_POINT('Ctrl Pts',(5.91898195452821,-0.0306732316975447,
17.1869248019535));
#16841=CARTESIAN_POINT('Ctrl Pts',(5.9158093105734,-0.196209436959831,17.1791383553752));
#16842=CARTESIAN_POINT('Ctrl Pts',(5.90570656813228,-0.361331556356784,
17.1713519087969));
#16843=CARTESIAN_POINT('Ctrl Pts',(5.89560344029432,-0.526459974790323,
17.1635651651832));
#16844=CARTESIAN_POINT('Ctrl Pts',(5.87856970053289,-0.691173956565553,
17.1557784215695));
#16845=CARTESIAN_POINT('Ctrl Pts',(5.85466505616971,-0.854884578504832,
17.1479916779557));
#16846=CARTESIAN_POINT('Ctrl Pts',(5.8307619929199,-1.01858437221124,17.1402054493769));
#16847=CARTESIAN_POINT('Ctrl Pts',(5.79998898079507,-1.18128062268044,17.132419220798));
#16848=CARTESIAN_POINT('Ctrl Pts',(5.76245729738374,-1.34239206580227,17.1246329922191));
#16849=CARTESIAN_POINT('Ctrl Pts',(5.72491573389159,-1.5035459209327,17.1168447139435));
#16850=CARTESIAN_POINT('Ctrl Pts',(5.68061201454751,-1.66311382320429,17.109056435668));
#16851=CARTESIAN_POINT('Ctrl Pts',(5.62970821090074,-1.82052630374207,17.1012681573924));
#16852=CARTESIAN_POINT('Ctrl Pts',(5.58131391549526,-1.97017850137579,17.0938638336962));
#16853=CARTESIAN_POINT('Ctrl Pts',(5.52695469659419,-2.11788242765818,17.08645951));
#16854=CARTESIAN_POINT('Ctrl Pts',(5.46681119284299,-2.26316281877965,17.0790551863038));
#16855=CARTESIAN_POINT('Ctrl Pts',(5.40355136129935,-2.4159708943942,17.0712672085423));
#16856=CARTESIAN_POINT('Ctrl Pts',(5.33386927725262,-2.56615227900246,17.0634792307807));
#16857=CARTESIAN_POINT('Ctrl Pts',(5.25800832134371,-2.71316771600656,17.0556912530192));
#16858=CARTESIAN_POINT('Ctrl Pts',(5.18216228034909,-2.86015424851539,17.0479048064409));
#16859=CARTESIAN_POINT('Ctrl Pts',(5.10013993785626,-3.00397579159731,17.0401183598625));
#16860=CARTESIAN_POINT('Ctrl Pts',(5.01223120355831,-3.14411655709142,17.0323319132842));
#16861=CARTESIAN_POINT('Ctrl Pts',(4.92431911574033,-3.28426266863981,17.0245451696704));
#16862=CARTESIAN_POINT('Ctrl Pts',(4.83052035323439,-3.42072744883984,17.0167584260567));
#16863=CARTESIAN_POINT('Ctrl Pts',(4.73116923713355,-3.55302240523489,17.008971682443));
#16864=CARTESIAN_POINT('Ctrl Pts',(4.63182469236578,-3.68530861130829,17.0011854538641));
#16865=CARTESIAN_POINT('Ctrl Pts',(4.52692872091587,-3.81342529002623,16.9933992252852));
#16866=CARTESIAN_POINT('Ctrl Pts',(4.41685725623758,-3.9369153585671,16.9856129967063));
#16867=CARTESIAN_POINT('Ctrl Pts',(4.30675681564162,-4.06043793542488,16.9778247184307));
#16868=CARTESIAN_POINT('Ctrl Pts',(4.19147837070045,-4.17933122840309,16.9700364401551));
#16869=CARTESIAN_POINT('Ctrl Pts',(4.07143680578625,-4.29317282426285,16.9622481618795));
#16870=CARTESIAN_POINT('Ctrl Pts',(3.95731317381578,-4.40140213965138,16.9548438381835));
#16871=CARTESIAN_POINT('Ctrl Pts',(3.83888493462339,-4.50506566592638,16.9474395144874));
#16872=CARTESIAN_POINT('Ctrl Pts',(3.71653818153727,-4.6038325890149,16.9400351907913));
#16873=CARTESIAN_POINT('Ctrl Pts',(3.58785204741612,-4.7077171073262,16.9322472130298));
#16874=CARTESIAN_POINT('Ctrl Pts',(3.45478451019537,-4.80622127808978,16.9244592352683));
#16875=CARTESIAN_POINT('Ctrl Pts',(3.31780738170305,-4.89898813434129,16.9166712575068));
#16876=CARTESIAN_POINT('Ctrl Pts',(3.18085718408845,-4.9917367518336,16.9088848109284));
#16877=CARTESIAN_POINT('Ctrl Pts',(3.03999919332433,-5.07875012643922,16.9010983643501));
#16878=CARTESIAN_POINT('Ctrl Pts',(2.89573484000276,-5.15971416833279,16.8933119177718));
#16879=CARTESIAN_POINT('Ctrl Pts',(2.75146498332143,-5.24068129882199,16.8855251741581));
#16880=CARTESIAN_POINT('Ctrl Pts',(2.60378878077965,-5.31559847499263,16.8777384305444));
#16881=CARTESIAN_POINT('Ctrl Pts',(2.45323359045479,-5.38419683083413,16.8699516869307));
#16882=CARTESIAN_POINT('Ctrl Pts',(2.30268835822943,-5.4527906494076,16.8621654583518));
#16883=CARTESIAN_POINT('Ctrl Pts',(2.14926481014631,-5.51506635161638,16.8543792297729));
#16884=CARTESIAN_POINT('Ctrl Pts',(1.99351180501769,-5.57080256747222,16.846593001194));
#16885=CARTESIAN_POINT('Ctrl Pts',(1.83771779847005,-5.62655345568664,16.8388047229185));
#16886=CARTESIAN_POINT('Ctrl Pts',(1.67959340993951,-5.6757613080575,16.8310164446429));
#16887=CARTESIAN_POINT('Ctrl Pts',(1.51970510180609,-5.71825383889563,16.8232281663673));
#16888=CARTESIAN_POINT('Ctrl Pts',(1.3676991324811,-5.75865152909903,16.8158238426712));
#16889=CARTESIAN_POINT('Ctrl Pts',(1.21409922779002,-5.79297999829685,16.808419518975));
#16890=CARTESIAN_POINT('Ctrl Pts',(1.05940272615352,-5.82113360320123,16.8010151952788));
#16891=CARTESIAN_POINT('Ctrl Pts',(0.896690645486941,-5.85074598346707,
16.7932272175173));
#16892=CARTESIAN_POINT('Ctrl Pts',(0.732707105461285,-5.87353720371765,
16.7854392397558));
#16893=CARTESIAN_POINT('Ctrl Pts',(0.568037223561832,-5.88941968916702,
16.7776512619942));
#16894=CARTESIAN_POINT('Ctrl Pts',(0.403399717172985,-5.90529905198358,
16.7698648154159));
#16895=CARTESIAN_POINT('Ctrl Pts',(0.238076456035561,-5.91427235958073,
16.7620783688376));
#16896=CARTESIAN_POINT('Ctrl Pts',(0.0726580389161019,-5.91630386067863,
16.7542919222593));
#16897=CARTESIAN_POINT('Ctrl Pts',(-0.0927666885429905,-5.91833543927372,
16.7465051786456));
#16898=CARTESIAN_POINT('Ctrl Pts',(-0.258286259781496,-5.91342467359364,
16.7387184350319));
#16899=CARTESIAN_POINT('Ctrl Pts',(-0.423308958957855,-5.90158792934292,
16.7309316914181));
#16900=CARTESIAN_POINT('Ctrl Pts',(-0.588320743117305,-5.88975196800427,
16.7231454628393));
#16901=CARTESIAN_POINT('Ctrl Pts',(-0.752835402231415,-5.87099096780191,
16.7153592342604));
#16902=CARTESIAN_POINT('Ctrl Pts',(-0.916265077685874,-5.84537328747389,
16.7075730056815));
#16903=CARTESIAN_POINT('Ctrl Pts',(-1.07973777541529,-5.81974886338355,
16.6997847274059));
#16904=CARTESIAN_POINT('Ctrl Pts',(-1.24212460255152,-5.78726419999045,
16.6919964491304));
#16905=CARTESIAN_POINT('Ctrl Pts',(-1.40284573966221,-5.7480391781208,16.6842081708548));
#16906=CARTESIAN_POINT('Ctrl Pts',(-1.55564348030185,-5.71074791185695,
16.6768038471586));
#16907=CARTESIAN_POINT('Ctrl Pts',(-1.70693555258789,-5.66736492692143,
16.6693995234625));
#16908=CARTESIAN_POINT('Ctrl Pts',(-1.85623472721197,-5.61803552854486,
16.6619951997663));
#16909=CARTESIAN_POINT('Ctrl Pts',(-2.01326981907195,-5.56615013383342,
16.6542072220048));
#16910=CARTESIAN_POINT('Ctrl Pts',(-2.16815618118622,-5.50766717947198,
16.6464192442433));
#16911=CARTESIAN_POINT('Ctrl Pts',(-2.32033816334955,-5.44278985173997,
16.6386312664818));
#16912=CARTESIAN_POINT('Ctrl Pts',(-2.47249022523054,-5.37792527944679,
16.6308448199034));
#16913=CARTESIAN_POINT('Ctrl Pts',(-2.62193867429505,-5.30666896748374,
16.6230583733251));
#16914=CARTESIAN_POINT('Ctrl Pts',(-2.768147854012,-5.22927222668975,16.6152719267468));
#16915=CARTESIAN_POINT('Ctrl Pts',(-2.91436261127951,-5.15187253338459,
16.6074851831331));
#16916=CARTESIAN_POINT('Ctrl Pts',(-3.05733756767092,-5.06833208852439,
16.5996984395194));
#16917=CARTESIAN_POINT('Ctrl Pts',(-3.19656103256491,-4.97894849617744,
16.5919116959056));
#16918=CARTESIAN_POINT('Ctrl Pts',(-3.3357752888681,-4.88957081588652,16.5841254673268));
#16919=CARTESIAN_POINT('Ctrl Pts',(-3.47123828136255,-4.79435093426291,
16.5763392387479));
#16920=CARTESIAN_POINT('Ctrl Pts',(-3.60246659342468,-4.69363025873994,
16.568553010169));
#16921=CARTESIAN_POINT('Ctrl Pts',(-3.73372945086859,-4.59288306886093,
16.5607647318935));
#16922=CARTESIAN_POINT('Ctrl Pts',(-3.86075514549399,-4.48663238468414,
16.5529764536179));
#16923=CARTESIAN_POINT('Ctrl Pts',(-3.98309198098985,-4.37526100175456,
16.5451881753423));
#16924=CARTESIAN_POINT('Ctrl Pts',(-4.09939772892601,-4.26938012018846,
16.5377838516462));
#16925=CARTESIAN_POINT('Ctrl Pts',(-4.21146559885731,-4.1588714461052,16.53037952795));
#16926=CARTESIAN_POINT('Ctrl Pts',(-4.31893735809536,-4.04409577771697,
16.5229752042538));
#16927=CARTESIAN_POINT('Ctrl Pts',(-4.43197775250338,-3.92337302306,16.5151872264923));
#16928=CARTESIAN_POINT('Ctrl Pts',(-4.53997353380287,-3.79788616182981,
16.5073992487308));
#16929=CARTESIAN_POINT('Ctrl Pts',(-4.64253410177453,-3.66807956243599,
16.4996112709692));
#16930=CARTESIAN_POINT('Ctrl Pts',(-4.74507450545943,-3.53829848413223,
16.4918248243909));
#16931=CARTESIAN_POINT('Ctrl Pts',(-4.84218163002422,-3.40419961284222,
16.4840383778125));
#16932=CARTESIAN_POINT('Ctrl Pts',(-4.93350546527673,-3.26625999984457,
16.4762519312342));
#16933=CARTESIAN_POINT('Ctrl Pts',(-5.0248327843276,-3.12831512476175,16.4684651876205));
#16934=CARTESIAN_POINT('Ctrl Pts',(-5.1103761929086,-2.98652947904605,16.4606784440067));
#16935=CARTESIAN_POINT('Ctrl Pts',(-5.18982888186515,-2.8414092875646,16.452891700393));
#16936=CARTESIAN_POINT('Ctrl Pts',(-5.26927631562065,-2.69629869469827,
16.4451054718141));
#16937=CARTESIAN_POINT('Ctrl Pts',(-5.34263368255457,-2.54785427779887,
16.4373192432352));
#16938=CARTESIAN_POINT('Ctrl Pts',(-5.40963996521877,-2.39660718708926,
16.4295330146564));
#16939=CARTESIAN_POINT('Ctrl Pts',(-5.47666388704616,-2.24532028112637,
16.4217447363808));
#16940=CARTESIAN_POINT('Ctrl Pts',(-5.53733325248533,-2.09122951865049,
16.4139564581052));
#16941=CARTESIAN_POINT('Ctrl Pts',(-5.59143470554352,-1.93488720501827,
16.4061681798296));
#16942=CARTESIAN_POINT('Ctrl Pts',(-5.64286900933923,-1.78625241609988,
16.3987638561335));
#16943=CARTESIAN_POINT('Ctrl Pts',(-5.68836729864528,-1.63558297597227,
16.3913595324374));
#16944=CARTESIAN_POINT('Ctrl Pts',(-5.72778774878402,-1.48336713843192,
16.3839552087413));
#16945=CARTESIAN_POINT('Ctrl Pts',(-5.76973707593995,-1.32138644199592,
16.376075887323));
#16946=CARTESIAN_POINT('Ctrl Pts',(-5.8048168140385,-1.15760282851791,16.3681965659048));
#16947=CARTESIAN_POINT('Ctrl Pts',(-5.83289481012724,-0.99260702016997,
16.3603172444865));
#16948=CARTESIAN_POINT('Ctrl Pts',(-5.86096757812148,-0.827641933874796,
16.3524393901899));
#16949=CARTESIAN_POINT('Ctrl Pts',(-5.8820411538682,-0.661465402049517,
16.3445615358933));
#16950=CARTESIAN_POINT('Ctrl Pts',(-5.89603466904057,-0.494677414050429,
16.3366836815967));
#16951=CARTESIAN_POINT('Ctrl Pts',(-5.90983570702114,-0.330183551806171,
16.328914185154));
#16952=CARTESIAN_POINT('Ctrl Pts',(-5.9167501976856,-0.165095237549104,
16.3211446887113));
#16953=CARTESIAN_POINT('Ctrl Pts',(-5.91674999999576,7.08458452474372E-6,
16.3133751922686));
#16954=CARTESIAN_POINT('Ctrl Pts',(-5.91674999941157,-8.34454905555866E-5,
16.0616248078328));
#16955=CARTESIAN_POINT('Ctrl Pts',(-5.91674760998257,-0.16950726878363,
16.0695980559169));
#16956=CARTESIAN_POINT('Ctrl Pts',(-5.90946380488815,-0.338903242213537,
16.0775713040011));
#16957=CARTESIAN_POINT('Ctrl Pts',(-5.89493172683878,-0.507651946130016,
16.0855445520852));
#16958=CARTESIAN_POINT('Ctrl Pts',(-5.88039486884334,-0.676456155508387,
16.0935204227603));
#16959=CARTESIAN_POINT('Ctrl Pts',(-5.85860500012414,-0.844612385715935,
16.1014962934354));
#16960=CARTESIAN_POINT('Ctrl Pts',(-5.82964715749152,-1.01150609570632,
16.1094721641104));
#16961=CARTESIAN_POINT('Ctrl Pts',(-5.81959195123027,-1.06945760469643,
16.1122416737652));
#16962=CARTESIAN_POINT('Ctrl Pts',(-5.80867293760191,-1.12725695627872,
16.1150111834199));
#16963=CARTESIAN_POINT('Ctrl Pts',(-5.79689512537895,-1.18487867220983,
16.1177806930746));
#16964=CARTESIAN_POINT('Ctrl Pts',(-5.76377485320318,-1.34691614391897,
16.1255688044675));
#16965=CARTESIAN_POINT('Ctrl Pts',(-5.72385039390528,-1.50759298455844,
16.1333569158605));
#16966=CARTESIAN_POINT('Ctrl Pts',(-5.67725841384133,-1.66633353953158,
16.1411450272535));
#16967=CARTESIAN_POINT('Ctrl Pts',(-5.63067558130054,-1.82504292856367,
16.1489316095865));
#16968=CARTESIAN_POINT('Ctrl Pts',(-5.57742792987381,-1.98181648404794,
16.1567181919195));
#16969=CARTESIAN_POINT('Ctrl Pts',(-5.51770226209812,-2.13609276702518,
16.1645047742525));
#16970=CARTESIAN_POINT('Ctrl Pts',(-5.45797431699597,-2.29037493252289,
16.1722916534862));
#16971=CARTESIAN_POINT('Ctrl Pts',(-5.39176797295808,-2.4421593355855,16.1800785327199));
#16972=CARTESIAN_POINT('Ctrl Pts',(-5.31931881544833,-2.59090291252245,
16.1878654119536));
#16973=CARTESIAN_POINT('Ctrl Pts',(-5.24687443954099,-2.73963667246955,
16.1956517772578));
#16974=CARTESIAN_POINT('Ctrl Pts',(-5.16818821471741,-2.88532972067255,
16.203438142562));
#16975=CARTESIAN_POINT('Ctrl Pts',(-5.0835425418119,-3.02746193833855,16.2112245078661));
#16976=CARTESIAN_POINT('Ctrl Pts',(-4.99887464267158,-3.16963147703863,
16.2190129177117));
#16977=CARTESIAN_POINT('Ctrl Pts',(-4.90824433052758,-3.30823804116743,
16.2268013275573));
#16978=CARTESIAN_POINT('Ctrl Pts',(-4.81197882630275,-3.44278816335163,
16.2345897374029));
#16979=CARTESIAN_POINT('Ctrl Pts',(-4.7207722628896,-3.57026741305853,16.2419688510552));
#16980=CARTESIAN_POINT('Ctrl Pts',(-4.62450770574258,-3.69410539135892,
16.2493479647074));
#16981=CARTESIAN_POINT('Ctrl Pts',(-4.52349819239377,-3.81390805682443,
16.2567270783597));
#16982=CARTESIAN_POINT('Ctrl Pts',(-4.41689008486494,-3.94035095332748,
16.2645151897527));
#16983=CARTESIAN_POINT('Ctrl Pts',(-4.30495803919303,-4.06234368556955,
16.2723033011456));
#16984=CARTESIAN_POINT('Ctrl Pts',(-4.18809747868372,-4.17944614411325,
16.2800914125386));
#16985=CARTESIAN_POINT('Ctrl Pts',(-4.07125986170831,-4.29652561163057,
16.2878779948716));
#16986=CARTESIAN_POINT('Ctrl Pts',(-3.94949588616863,-4.4087164951398,16.2956645772047));
#16987=CARTESIAN_POINT('Ctrl Pts',(-3.82323819983297,-4.51561515519624,
16.3034511595377));
#16988=CARTESIAN_POINT('Ctrl Pts',(-3.69697569931977,-4.62251789127485,
16.3112380387714));
#16989=CARTESIAN_POINT('Ctrl Pts',(-3.56621938645127,-4.72412779064063,
16.3190249180052));
#16990=CARTESIAN_POINT('Ctrl Pts',(-3.43143595502093,-4.8200806890642,16.3268117972389));
#16991=CARTESIAN_POINT('Ctrl Pts',(-3.29666141921912,-4.91602725465195,
16.3345981625431));
#16992=CARTESIAN_POINT('Ctrl Pts',(-3.15786055712963,-5.00631738121599,
16.3423845278472));
#16993=CARTESIAN_POINT('Ctrl Pts',(-3.0155301945431,-5.09062945108941,16.3501708931514));
#16994=CARTESIAN_POINT('Ctrl Pts',(-2.87316245889367,-5.17496365960025,
16.357959302997));
#16995=CARTESIAN_POINT('Ctrl Pts',(-2.72726364496336,-5.2533165101719,16.3657477128426));
#16996=CARTESIAN_POINT('Ctrl Pts',(-2.57835718510673,-5.32541123186825,
16.3735361226882));
#16997=CARTESIAN_POINT('Ctrl Pts',(-2.43727605139484,-5.39371723471968,
16.3809152363404));
#16998=CARTESIAN_POINT('Ctrl Pts',(-2.2934954905747,-5.45640583146567,16.3882943499926));
#16999=CARTESIAN_POINT('Ctrl Pts',(-2.14747891136345,-5.51328077352761,
16.3956734636448));
#17000=CARTESIAN_POINT('Ctrl Pts',(-1.99336915811693,-5.57330808915453,
16.4034615750378));
#17001=CARTESIAN_POINT('Ctrl Pts',(-1.83671344877192,-5.62688045421262,
16.4112496864308));
#17002=CARTESIAN_POINT('Ctrl Pts',(-1.67806957743404,-5.67380058301227,
16.4190377978238));
#17003=CARTESIAN_POINT('Ctrl Pts',(-1.51945685305472,-5.72071149986257,
16.4268243801568));
#17004=CARTESIAN_POINT('Ctrl Pts',(-1.35885705174777,-5.76097269584713,
16.4346109624899));
#17005=CARTESIAN_POINT('Ctrl Pts',(-1.19684320673853,-5.79443671990504,
16.442397544823));
#17006=CARTESIAN_POINT('Ctrl Pts',(-1.03482318417745,-5.82790201993873,
16.4501844240567));
#17007=CARTESIAN_POINT('Ctrl Pts',(-0.871389322137765,-5.85456956093857,
16.4579713032905));
#17008=CARTESIAN_POINT('Ctrl Pts',(-0.707125664101611,-5.87434284475028,
16.4657581825242));
#17009=CARTESIAN_POINT('Ctrl Pts',(-0.542872847371819,-5.89411482353671,
16.4735445478284));
#17010=CARTESIAN_POINT('Ctrl Pts',(-0.377790661517953,-5.90699341762036,
16.4813309131326));
#17011=CARTESIAN_POINT('Ctrl Pts',(-0.212469253840867,-5.91293390616471,
16.4891172784368));
#17012=CARTESIAN_POINT('Ctrl Pts',(-0.0471044361194315,-5.91887595456072,
16.4969056882824));
#17013=CARTESIAN_POINT('Ctrl Pts',(0.118499409479502,-5.91787624364827,
16.504694098128));
#17014=CARTESIAN_POINT('Ctrl Pts',(0.283750228081456,-5.90994216304726,
16.5124825079736));
#17015=CARTESIAN_POINT('Ctrl Pts',(0.440316792469277,-5.90242503392326,
16.5198616216258));
#17016=CARTESIAN_POINT('Ctrl Pts',(0.596566220247805,-5.88868363115203,
16.5272407352779));
#17017=CARTESIAN_POINT('Ctrl Pts',(0.751997689404057,-5.86876733544881,
16.53461984893));
#17018=CARTESIAN_POINT('Ctrl Pts',(0.916044166098635,-5.84774715107652,
16.542407960323));
#17019=CARTESIAN_POINT('Ctrl Pts',(1.0792380289808,-5.81984065208844,16.5501960717159));
#17020=CARTESIAN_POINT('Ctrl Pts',(1.24099507788301,-5.78514146578717,16.5579841831089));
#17021=CARTESIAN_POINT('Ctrl Pts',(1.40272036860826,-5.7504490920663,16.5657707654419));
#17022=CARTESIAN_POINT('Ctrl Pts',(1.56300909598557,-5.70896675898949,16.573557347775));
#17023=CARTESIAN_POINT('Ctrl Pts',(1.72128752067219,-5.66083914571666,16.581343930108));
#17024=CARTESIAN_POINT('Ctrl Pts',(1.87957198048011,-5.6127096973486,16.5891308093417));
#17025=CARTESIAN_POINT('Ctrl Pts',(2.03584567737109,-5.55793455094008,16.5969176885754));
#17026=CARTESIAN_POINT('Ctrl Pts',(2.18954958131189,-5.49670839625652,16.6047045678091));
#17027=CARTESIAN_POINT('Ctrl Pts',(2.343243340884,-5.43548628246374,16.6124909331133));
#17028=CARTESIAN_POINT('Ctrl Pts',(2.49436735008731,-5.36781413077603,16.6202772984175));
#17029=CARTESIAN_POINT('Ctrl Pts',(2.64238199108072,-5.29393501808554,16.6280636637217));
#17030=CARTESIAN_POINT('Ctrl Pts',(2.79043549771314,-5.22003650624031,16.6358520735673));
#17031=CARTESIAN_POINT('Ctrl Pts',(2.9353777177355,-5.13992791772467,16.6436404834128));
#17032=CARTESIAN_POINT('Ctrl Pts',(3.0766922897027,-5.05389900146253,16.6514288932584));
#17033=CARTESIAN_POINT('Ctrl Pts',(3.21058050410514,-4.97239107326396,16.6588080069107));
#17034=CARTESIAN_POINT('Ctrl Pts',(3.34121232160782,-4.88556919763453,16.6661871205629));
#17035=CARTESIAN_POINT('Ctrl Pts',(3.46817158444463,-4.79371634781938,16.6735662342151));
#17036=CARTESIAN_POINT('Ctrl Pts',(3.60216774278325,-4.6967724247635,16.6813543456081));
#17037=CARTESIAN_POINT('Ctrl Pts',(3.73212054572166,-4.59418939216722,16.689142457001));
#17038=CARTESIAN_POINT('Ctrl Pts',(3.85756178836071,-4.4863289682634,16.696930568394));
#17039=CARTESIAN_POINT('Ctrl Pts',(3.98297840279855,-4.37848972087351,16.704717150727));
#17040=CARTESIAN_POINT('Ctrl Pts',(4.10388498217366,-4.2653753577464,16.7125037330601));
#17041=CARTESIAN_POINT('Ctrl Pts',(4.21984693248474,-4.14738742208865,16.7202903153932));
#17042=CARTESIAN_POINT('Ctrl Pts',(4.33581330439915,-4.0293949875772,16.7280771946269));
#17043=CARTESIAN_POINT('Ctrl Pts',(4.44683444320285,-3.90652883380487,16.7358640738606));
#17044=CARTESIAN_POINT('Ctrl Pts',(4.55251259831223,-3.77922738198013,16.7436509530943));
#17045=CARTESIAN_POINT('Ctrl Pts',(4.6581837787245,-3.65193433197759,16.7514373183985));
#17046=CARTESIAN_POINT('Ctrl Pts',(4.75851247709818,-3.52020681566315,16.7592236837026));
#17047=CARTESIAN_POINT('Ctrl Pts',(4.85314113924644,-3.3845164566085,16.7670100490068));
#17048=CARTESIAN_POINT('Ctrl Pts',(4.94779464895975,-3.24879046802104,16.7747984588524));
#17049=CARTESIAN_POINT('Ctrl Pts',(5.03674494721138,-3.10909981858482,16.782586868698));
#17050=CARTESIAN_POINT('Ctrl Pts',(5.11967723133251,-2.96594598896802,16.7903752785436));
#17051=CARTESIAN_POINT('Ctrl Pts',(5.19825126147458,-2.83031517350858,16.7977543921958));
#17052=CARTESIAN_POINT('Ctrl Pts',(5.27142339532634,-2.69157603462084,16.805133505848));
#17053=CARTESIAN_POINT('Ctrl Pts',(5.33896357963309,-2.55017616212124,16.8125126195002));
#17054=CARTESIAN_POINT('Ctrl Pts',(5.41024727353926,-2.40093900304194,16.8203007308932));
#17055=CARTESIAN_POINT('Ctrl Pts',(5.47528245591269,-2.24868449696134,16.8280888422862));
#17056=CARTESIAN_POINT('Ctrl Pts',(5.5338310441021,-2.09395428265087,16.8358769536791));
#17057=CARTESIAN_POINT('Ctrl Pts',(5.59236813729686,-1.93925444692065,16.8436635360122));
#17058=CARTESIAN_POINT('Ctrl Pts',(5.64442106436579,-1.7820801714638,16.8514501183452));
#17059=CARTESIAN_POINT('Ctrl Pts',(5.68980031082602,-1.6229919856315,16.8592367006783));
#17060=CARTESIAN_POINT('Ctrl Pts',(5.73518128758682,-1.4638977338021,16.867023579912));
#17061=CARTESIAN_POINT('Ctrl Pts',(5.77388798311082,-1.30288973174729,16.8748104591457));
#17062=CARTESIAN_POINT('Ctrl Pts',(5.8057808796978,-1.14054326504322,16.8825973383794));
#17063=CARTESIAN_POINT('Ctrl Pts',(5.83767167137206,-0.978207513112043,
16.8903837036836));
#17064=CARTESIAN_POINT('Ctrl Pts',(5.86274950255863,-0.814533786892136,
16.8981700689878));
#17065=CARTESIAN_POINT('Ctrl Pts',(5.88092603811226,-0.650107296339016,
16.905956434292));
#17066=CARTESIAN_POINT('Ctrl Pts',(5.89910734645501,-0.485637630728497,
16.9137448441376));
#17067=CARTESIAN_POINT('Ctrl Pts',(5.91038370107013,-0.320415123407121,
16.9215332539832));
#17068=CARTESIAN_POINT('Ctrl Pts',(5.91471859258403,-0.155030748694557,
16.9293216638288));
#17069=CARTESIAN_POINT('Ctrl Pts',(5.91882567705765,0.00166235317050914,
16.936700777481));
#17070=CARTESIAN_POINT('Ctrl Pts',(5.91670210155318,0.158500487113797,16.9440798911332));
#17071=CARTESIAN_POINT('Ctrl Pts',(5.90835999380824,0.314980548711032,16.9514590047854));
#17072=CARTESIAN_POINT('Ctrl Pts',(5.89955551302207,0.48013373755449,16.9592471161784));
#17073=CARTESIAN_POINT('Ctrl Pts',(5.88382046641899,0.644947019412175,16.9670352275714));
#17074=CARTESIAN_POINT('Ctrl Pts',(5.86120492727678,0.808830861779118,16.9748233389643));
#17075=CARTESIAN_POINT('Ctrl Pts',(5.83859382830144,0.9726825284105,16.9826099212974));
#17076=CARTESIAN_POINT('Ctrl Pts',(5.80910497581698,1.13560480331814,16.9903965036305));
#17077=CARTESIAN_POINT('Ctrl Pts',(5.77284012983798,1.29701480247227,16.9981830859636));
#17078=CARTESIAN_POINT('Ctrl Pts',(5.73657390108848,1.45843095615374,17.0059699651973));
#17079=CARTESIAN_POINT('Ctrl Pts',(5.69353122804064,1.61833440608861,17.013756844431));
#17080=CARTESIAN_POINT('Ctrl Pts',(5.64386483392354,1.77615323069302,17.0215437236647));
#17081=CARTESIAN_POINT('Ctrl Pts',(5.5942017177597,1.93396163934636,17.0293300889689));
#17082=CARTESIAN_POINT('Ctrl Pts',(5.53791585139387,2.08968539321618,17.0371164542731));
#17083=CARTESIAN_POINT('Ctrl Pts',(5.475209650798,2.24276834343373,17.0449028195773));
#17084=CARTESIAN_POINT('Ctrl Pts',(5.41248698482726,2.39589149012528,17.0526912294229));
#17085=CARTESIAN_POINT('Ctrl Pts',(5.34334073534985,2.54637215095016,17.0604796392685));
#17086=CARTESIAN_POINT('Ctrl Pts',(5.26802158560594,2.69367391049657,17.0682680491141));
#17087=CARTESIAN_POINT('Ctrl Pts',(5.19666060471776,2.83323467404113,17.0756471627663));
#17088=CARTESIAN_POINT('Ctrl Pts',(5.11975895061818,2.96994182611438,17.0830262764184));
#17089=CARTESIAN_POINT('Ctrl Pts',(5.03756797584835,3.10335938157461,17.0904053900705));
#17090=CARTESIAN_POINT('Ctrl Pts',(4.9508214508346,3.24417179248001,17.0981935014635));
#17091=CARTESIAN_POINT('Ctrl Pts',(4.85815166126487,3.38136989621794,17.1059816128564));
#17092=CARTESIAN_POINT('Ctrl Pts',(4.75988463076687,3.51445996766066,17.1137697242494));
#17093=CARTESIAN_POINT('Ctrl Pts',(4.66163689328724,3.64752390918798,17.1215563065824));
#17094=CARTESIAN_POINT('Ctrl Pts',(4.55779429723068,3.77648117081394,17.1293428889155));
#17095=CARTESIAN_POINT('Ctrl Pts',(4.44872507266335,3.9008685943462,17.1371294712485));
#17096=CARTESIAN_POINT('Ctrl Pts',(4.3396516893108,4.02526076074319,17.1449163504822));
#17097=CARTESIAN_POINT('Ctrl Pts',(4.22535148635334,4.14508249753556,17.152703229716));
#17098=CARTESIAN_POINT('Ctrl Pts',(4.10623220099838,4.25990465550392,17.1604901089497));
#17099=CARTESIAN_POINT('Ctrl Pts',(3.98712077744725,4.37471923527638,17.1682764742538));
#17100=CARTESIAN_POINT('Ctrl Pts',(3.8631911381307,4.48453467485856,17.176062839558));
#17101=CARTESIAN_POINT('Ctrl Pts',(3.73488711036484,4.58895945017284,17.1838492048622));
#17102=CARTESIAN_POINT('Ctrl Pts',(3.60654939256685,4.69341164531248,17.1916376147078));
#17103=CARTESIAN_POINT('Ctrl Pts',(3.47383523788627,4.79247014442481,17.1994260245534));
#17104=CARTESIAN_POINT('Ctrl Pts',(3.33722141704751,4.88578384459438,17.207214434399));
#17105=CARTESIAN_POINT('Ctrl Pts',(3.20778692009416,4.97419372703635,17.2145935480512));
#17106=CARTESIAN_POINT('Ctrl Pts',(3.0748522998765,5.05744693465817,17.2219726617034));
#17107=CARTESIAN_POINT('Ctrl Pts',(2.93884686546465,5.13528087487419,17.2293517753556));
#17108=CARTESIAN_POINT('Ctrl Pts',(2.79530313878258,5.2174288705721,17.2371398867486));
#17109=CARTESIAN_POINT('Ctrl Pts',(2.64828727028938,5.29356916200429,17.2449279981415));
#17110=CARTESIAN_POINT('Ctrl Pts',(2.49832176428621,5.36342417906638,17.2527161095345));
#17111=CARTESIAN_POINT('Ctrl Pts',(2.34838570139589,5.43326548131361,17.2605026918675));
#17112=CARTESIAN_POINT('Ctrl Pts',(2.1955014459598,5.49682383655954,17.2682892742006));
#17113=CARTESIAN_POINT('Ctrl Pts',(2.04021394041632,5.55386870927202,17.2760758565336));
#17114=CARTESIAN_POINT('Ctrl Pts',(1.88492051379484,5.6109157570928,17.2838627357674));
#17115=CARTESIAN_POINT('Ctrl Pts',(1.72722395226152,5.66144871153472,17.2916496150011));
#17116=CARTESIAN_POINT('Ctrl Pts',(1.56768761928538,5.7052858027306,17.2994364942348));
#17117=CARTESIAN_POINT('Ctrl Pts',(1.40816181561484,5.74912000070385,17.3072228595389));
#17118=CARTESIAN_POINT('Ctrl Pts',(1.24679679165303,5.78625913523272,17.3150092248431));
#17119=CARTESIAN_POINT('Ctrl Pts',(1.08416960122261,5.81657174272654,17.3227955901473));
#17120=CARTESIAN_POINT('Ctrl Pts',(0.921499708194478,5.84689230969552,17.3305839999929));
#17121=CARTESIAN_POINT('Ctrl Pts',(0.757567300422326,5.8703827073296,17.3383724098385));
#17122=CARTESIAN_POINT('Ctrl Pts',(0.592959021178191,5.88696272807153,17.3461608196841));
#17123=CARTESIAN_POINT('Ctrl Pts',(0.437001229444464,5.90267143624639,17.3535399333363));
#17124=CARTESIAN_POINT('Ctrl Pts',(0.280437034654325,5.91217736815578,17.3609190469885));
#17125=CARTESIAN_POINT('Ctrl Pts',(0.123769056454859,5.91545533185437,17.3682981606407));
#17126=CARTESIAN_POINT('Ctrl Pts',(-0.0415824645321675,5.91891498129602,
17.3760862720337));
#17127=CARTESIAN_POINT('Ctrl Pts',(-0.207108654925602,5.91543793340395,
17.3838743834266));
#17128=CARTESIAN_POINT('Ctrl Pts',(-0.372217892445571,5.9050304320167,17.3916624948196));
#17129=CARTESIAN_POINT('Ctrl Pts',(-0.537294713644905,5.89462497396093,
17.3994490771526));
#17130=CARTESIAN_POINT('Ctrl Pts',(-0.701954426610032,5.87729179744747,
17.4072356594857));
#17131=CARTESIAN_POINT('Ctrl Pts',(-0.865608208618556,5.85308918364245,
17.4150222418188));
#17132=CARTESIAN_POINT('Ctrl Pts',(-1.02926823070942,5.82888564699714,17.4228091210525));
#17133=CARTESIAN_POINT('Ctrl Pts',(-1.19192192843783,5.79781219177657,17.4305960002862));
#17134=CARTESIAN_POINT('Ctrl Pts',(-1.35298763436772,5.7599787346611,17.4383828795199));
#17135=CARTESIAN_POINT('Ctrl Pts',(-1.51404271005432,5.72214777453188,17.4461692448241));
#17136=CARTESIAN_POINT('Ctrl Pts',(-1.67350969261694,5.67755777852217,17.4539556101283));
#17137=CARTESIAN_POINT('Ctrl Pts',(-1.83081896110411,5.62636938834998,17.4617419754324));
#17138=CARTESIAN_POINT('Ctrl Pts',(-1.98816953581057,5.57516755714605,17.469530385278));
#17139=CARTESIAN_POINT('Ctrl Pts',(-2.14336095966549,5.51736396676577,17.4773187951236));
#17140=CARTESIAN_POINT('Ctrl Pts',(-2.29583971369687,5.45316885595085,17.4851072049692));
#17141=CARTESIAN_POINT('Ctrl Pts',(-2.44030541052709,5.39234732395523,17.4924863186214));
#17142=CARTESIAN_POINT('Ctrl Pts',(-2.58233597682478,5.32578886792703,17.4998654322736));
#17143=CARTESIAN_POINT('Ctrl Pts',(-2.72147799808978,5.25371183720741,17.5072445459258));
#17144=CARTESIAN_POINT('Ctrl Pts',(-2.86833216135817,5.17763983580216,17.5150326573188));
#17145=CARTESIAN_POINT('Ctrl Pts',(-3.01202094520114,5.09539299412413,17.5228207687118));
#17146=CARTESIAN_POINT('Ctrl Pts',(-3.1520278198626,5.00725984799194,17.5306088801048));
#17147=CARTESIAN_POINT('Ctrl Pts',(-3.2920072066145,4.91914400526685,17.5383954624378));
#17148=CARTESIAN_POINT('Ctrl Pts',(-3.42830585629749,4.82514433411655,17.5461820447709));
#17149=CARTESIAN_POINT('Ctrl Pts',(-3.56043459400334,4.72559372611784,17.5539686271039));
#17150=CARTESIAN_POINT('Ctrl Pts',(-3.69256836974889,4.62603932227635,17.5617555063376));
#17151=CARTESIAN_POINT('Ctrl Pts',(-3.82053165779555,4.52093374717946,17.5695423855714));
#17152=CARTESIAN_POINT('Ctrl Pts',(-3.94386627070621,4.41065181138638,17.5773292648051));
#17153=CARTESIAN_POINT('Ctrl Pts',(-4.06719274360384,4.30037715413719,17.5851156301093));
#17154=CARTESIAN_POINT('Ctrl Pts',(-4.18589091456465,4.1849270329488,17.5929019954135));
#17155=CARTESIAN_POINT('Ctrl Pts',(-4.29953744309141,4.06471503773081,17.6006883607177));
#17156=CARTESIAN_POINT('Ctrl Pts',(-4.41321381288865,3.94447147728412,17.6084767705633));
#17157=CARTESIAN_POINT('Ctrl Pts',(-4.52183566864467,3.81946377531669,17.6162651804089));
#17158=CARTESIAN_POINT('Ctrl Pts',(-4.62501753834308,3.69014137026198,17.6240535902545));
#17159=CARTESIAN_POINT('Ctrl Pts',(-4.72277699867455,3.56761511091167,17.6314327039067));
#17160=CARTESIAN_POINT('Ctrl Pts',(-4.81565336853743,3.44121617993303,17.6388118175589));
#17161=CARTESIAN_POINT('Ctrl Pts',(-4.90335296033389,3.31135324435266,17.646190931211));
#17162=CARTESIAN_POINT('Ctrl Pts',(-4.99591342521148,3.17429247312825,17.653979042604));
#17163=CARTESIAN_POINT('Ctrl Pts',(-5.0827400368267,3.03332386285053,17.661767153997));
#17164=CARTESIAN_POINT('Ctrl Pts',(-5.16351726432063,2.88894790945818,17.6695552653899));
#17165=CARTESIAN_POINT('Ctrl Pts',(-5.24427863261406,2.7446003017675,17.677341847723));
#17166=CARTESIAN_POINT('Ctrl Pts',(-5.31899283066456,2.59684696443971,17.685128430056));
#17167=CARTESIAN_POINT('Ctrl Pts',(-5.38738956988842,2.44621425569338,17.6929150123891));
#17168=CARTESIAN_POINT('Ctrl Pts',(-5.45578891706479,2.29557580335522,17.7007018916228));
#17169=CARTESIAN_POINT('Ctrl Pts',(-5.51787018771155,2.14205804920599,17.7084887708565));
#17170=CARTESIAN_POINT('Ctrl Pts',(-5.5734103595701,1.98620933598065,17.7162756500902));
#17171=CARTESIAN_POINT('Ctrl Pts',(-5.62894686580935,1.83037090868046,17.7240620153944));
#17172=CARTESIAN_POINT('Ctrl Pts',(-5.6779430300153,1.6722021312153,17.7318483806986));
#17173=CARTESIAN_POINT('Ctrl Pts',(-5.72022498323144,1.51226872734805,17.7396347460028));
#17174=CARTESIAN_POINT('Ctrl Pts',(-5.7625180388299,1.35229332821658,17.7474231558484));
#17175=CARTESIAN_POINT('Ctrl Pts',(-5.79809327696699,1.19055268542543,17.755211565694));
#17176=CARTESIAN_POINT('Ctrl Pts',(-5.82682723306159,1.02762588452792,17.7629999755396));
#17177=CARTESIAN_POINT('Ctrl Pts',(-5.85405116347902,0.873261206160452,
17.7703790891917));
#17178=CARTESIAN_POINT('Ctrl Pts',(-5.87513431802023,0.717832089112757,
17.7777582028439));
#17179=CARTESIAN_POINT('Ctrl Pts',(-5.89001432361835,0.561837903732653,
17.7851373164961));
#17180=CARTESIAN_POINT('Ctrl Pts',(-5.9067386364072,0.386508967709382,17.7934310368183));
#17181=CARTESIAN_POINT('Ctrl Pts',(-5.91563053670214,0.210427895121147,
17.8017247571405));
#17182=CARTESIAN_POINT('Ctrl Pts',(-5.91665077471695,0.0342662011513159,
17.8100184774627));
#17183=CARTESIAN_POINT('Ctrl Pts',(-5.91671664138899,0.0228931839191246,
17.8105539209068));
#17184=CARTESIAN_POINT('Ctrl Pts',(-5.91674971691492,0.0115198317854237,
17.811089364351));
#17185=CARTESIAN_POINT('Ctrl Pts',(-5.91674999819062,0.000146325857716349,
17.8116248077951));
#17186=CARTESIAN_POINT('Origin',(0.,0.,0.));
#17187=CARTESIAN_POINT('',(-5.91674999855416,-0.000130802689547563,19.8133751922466));
#17188=CARTESIAN_POINT('',(-5.91674999805254,-0.000151806595337599,19.5616248077951));
#17189=CARTESIAN_POINT('',(-5.91675,-7.2459289488551E-16,0.));
#17190=CARTESIAN_POINT('Ctrl Pts',(-5.91674999855418,-0.000130801803848009,
19.8133751922049));
#17191=CARTESIAN_POINT('Ctrl Pts',(-5.91675365556631,0.165292196264256,
19.8055894898337));
#17192=CARTESIAN_POINT('Ctrl Pts',(-5.90981551862249,0.33072426090592,19.7978037874625));
#17193=CARTESIAN_POINT('Ctrl Pts',(-5.89595937446898,0.495574027882227,
19.7900180850912));
#17194=CARTESIAN_POINT('Ctrl Pts',(-5.8821040729587,0.660413769736061,19.7822328561973));
#17195=CARTESIAN_POINT('Ctrl Pts',(-5.86133163332367,0.824670966230145,
19.7744476273033));
#17196=CARTESIAN_POINT('Ctrl Pts',(-5.83371778357321,0.987758768182621,
19.7666623984094));
#17197=CARTESIAN_POINT('Ctrl Pts',(-5.80609621641889,1.15089214923559,19.7588749937321));
#17198=CARTESIAN_POINT('Ctrl Pts',(-5.77162946994277,1.31285516693262,19.7510875890547));
#17199=CARTESIAN_POINT('Ctrl Pts',(-5.73044469308286,1.47306964601761,19.7433001843774));
#17200=CARTESIAN_POINT('Ctrl Pts',(-5.6901362979207,1.6298748790683,19.7356784899321));
#17201=CARTESIAN_POINT('Ctrl Pts',(-5.64339299006378,1.78500495803461,19.7280567954869));
#17202=CARTESIAN_POINT('Ctrl Pts',(-5.59038061120507,1.93793064487932,19.7204351010416));
#17203=CARTESIAN_POINT('Ctrl Pts',(-5.53621165565258,2.09419272765823,19.7126471232801));
#17204=CARTESIAN_POINT('Ctrl Pts',(-5.47547716308906,2.24821013749588,19.7048591455185));
#17205=CARTESIAN_POINT('Ctrl Pts',(-5.40838839782343,2.39943024503503,19.697071167757));
#17206=CARTESIAN_POINT('Ctrl Pts',(-5.34131282278406,2.55062062140498,19.6892847211786));
#17207=CARTESIAN_POINT('Ctrl Pts',(-5.26788559728104,2.69901450092035,19.6814982746002));
#17208=CARTESIAN_POINT('Ctrl Pts',(-5.1883658136253,2.8440799472772,19.6737118280218));
#17209=CARTESIAN_POINT('Ctrl Pts',(-5.10884299646939,2.98915092755322,19.6659250844081));
#17210=CARTESIAN_POINT('Ctrl Pts',(-5.02322730621899,3.13089293849438,19.6581383407944));
#17211=CARTESIAN_POINT('Ctrl Pts',(-4.93182377414891,3.2687986819686,19.6503515971806));
#17212=CARTESIAN_POINT('Ctrl Pts',(-4.8404262877386,3.40669530400968,19.6425653686017));
#17213=CARTESIAN_POINT('Ctrl Pts',(-4.74324190224314,3.54075590004021,19.6347791400228));
#17214=CARTESIAN_POINT('Ctrl Pts',(-4.64061903550317,3.67050208143595,19.6269929114439));
#17215=CARTESIAN_POINT('Ctrl Pts',(-4.53796915366221,3.80028241804782,19.6192046331684));
#17216=CARTESIAN_POINT('Ctrl Pts',(-4.42987812665055,3.9257458185392,19.6114163548928));
#17217=CARTESIAN_POINT('Ctrl Pts',(-4.31673529364155,4.04644621453559,19.6036280766172));
#17218=CARTESIAN_POINT('Ctrl Pts',(-4.20917029277264,4.16119619785267,19.5962237529212));
#17219=CARTESIAN_POINT('Ctrl Pts',(-4.09703976589781,4.27164129489342,19.5888194292251));
#17220=CARTESIAN_POINT('Ctrl Pts',(-3.98070969479159,4.37742857032439,19.5814151055291));
#17221=CARTESIAN_POINT('Ctrl Pts',(-3.85835199624035,4.48869719961906,19.5736271277676));
#17222=CARTESIAN_POINT('Ctrl Pts',(-3.73130423174891,4.59485230622068,19.5658391500061));
#17223=CARTESIAN_POINT('Ctrl Pts',(-3.60001641622602,4.69550980889223,19.5580511722446));
#17224=CARTESIAN_POINT('Ctrl Pts',(-3.468754413013,4.79614752143597,19.5502647256662));
#17225=CARTESIAN_POINT('Ctrl Pts',(-3.33325427554463,4.89128959240634,19.5424782790879));
#17226=CARTESIAN_POINT('Ctrl Pts',(-3.19399810645238,4.98059300269342,19.5346918325095));
#17227=CARTESIAN_POINT('Ctrl Pts',(-3.05473662505157,5.06989981970404,19.5269050888958));
#17228=CARTESIAN_POINT('Ctrl Pts',(-2.91171909215923,5.15336735451814,19.5191183452821));
#17229=CARTESIAN_POINT('Ctrl Pts',(-2.76545615116162,5.23069620973178,19.5113316016684));
#17230=CARTESIAN_POINT('Ctrl Pts',(-2.61920288436343,5.3080199502201,19.5035453730895));
#17231=CARTESIAN_POINT('Ctrl Pts',(-2.46970492160015,5.37920567436201,19.4957591445106));
#17232=CARTESIAN_POINT('Ctrl Pts',(-2.3174971614677,5.44400013492736,19.4879729159318));
#17233=CARTESIAN_POINT('Ctrl Pts',(-2.16524933318927,5.50881165240165,19.4801846376562));
#17234=CARTESIAN_POINT('Ctrl Pts',(-2.01029057557699,5.56722841730974,19.4723963593806));
#17235=CARTESIAN_POINT('Ctrl Pts',(-1.85317624536007,5.61904514718766,19.4646080811051));
#17236=CARTESIAN_POINT('Ctrl Pts',(-1.70380749952587,5.66830736244459,19.4572037574089));
#17237=CARTESIAN_POINT('Ctrl Pts',(-1.55249084692207,5.71160453513816,19.4497994337128));
#17238=CARTESIAN_POINT('Ctrl Pts',(-1.39971655682327,5.74880197285094,19.4423951100166));
#17239=CARTESIAN_POINT('Ctrl Pts',(-1.2390262868339,5.78792679094116,19.4346071322551));
#17240=CARTESIAN_POINT('Ctrl Pts',(-1.07666583229832,5.82031697344828,19.4268191544936));
#17241=CARTESIAN_POINT('Ctrl Pts',(-0.913214151802569,5.84585070588084,
19.419031176732));
#17242=CARTESIAN_POINT('Ctrl Pts',(-0.7497946073091,5.8713794181626,19.4112447301537));
#17243=CARTESIAN_POINT('Ctrl Pts',(-0.585284580461871,5.89005432080999,
19.4034582835754));
#17244=CARTESIAN_POINT('Ctrl Pts',(-0.420271547651839,5.90180501107367,
19.3956718369971));
#17245=CARTESIAN_POINT('Ctrl Pts',(-0.255252219966307,5.91355614959972,
19.3878850933834));
#17246=CARTESIAN_POINT('Ctrl Pts',(-0.0897301663723069,5.91838252054568,
19.3800983497697));
#17247=CARTESIAN_POINT('Ctrl Pts',(0.0757029583459906,5.91626568238764,
19.372311606156));
#17248=CARTESIAN_POINT('Ctrl Pts',(0.241125140900588,5.9141489842426,19.3645253775772));
#17249=CARTESIAN_POINT('Ctrl Pts',(0.406458086801056,5.90509000020647,19.3567391489983));
#17250=CARTESIAN_POINT('Ctrl Pts',(0.571110935857952,5.88912241861582,19.3489529204195));
#17251=CARTESIAN_POINT('Ctrl Pts',(0.735807129185999,5.87315063361667,19.3411646421439));
#17252=CARTESIAN_POINT('Ctrl Pts',(0.899822549465971,5.85026664590831,19.3333763638684));
#17253=CARTESIAN_POINT('Ctrl Pts',(1.06257133350844,5.82055604935698,19.3255880855928));
#17254=CARTESIAN_POINT('Ctrl Pts',(1.21729676005063,5.79231015645354,19.3181837618966));
#17255=CARTESIAN_POINT('Ctrl Pts',(1.37087717065595,5.75789457862528,19.3107794382004));
#17256=CARTESIAN_POINT('Ctrl Pts',(1.52281763783132,5.71742573230382,19.3033751145041));
#17257=CARTESIAN_POINT('Ctrl Pts',(1.68263088047024,5.67485999799536,19.2955871367426));
#17258=CARTESIAN_POINT('Ctrl Pts',(1.8406868890411,5.62558181545351,19.2877991589811));
#17259=CARTESIAN_POINT('Ctrl Pts',(1.99641903140144,5.56976136055739,19.2800111812195));
#17260=CARTESIAN_POINT('Ctrl Pts',(2.15212055548781,5.51395188044115,19.2722247346411));
#17261=CARTESIAN_POINT('Ctrl Pts',(2.30549882437239,5.45160280220751,19.2644382880628));
#17262=CARTESIAN_POINT('Ctrl Pts',(2.45600433643221,5.3829335182525,19.2566518414844));
#17263=CARTESIAN_POINT('Ctrl Pts',(2.60651558993775,5.31426161471922,19.2488650978707));
#17264=CARTESIAN_POINT('Ctrl Pts',(2.75415357497749,5.23926915205707,19.2410783542569));
#17265=CARTESIAN_POINT('Ctrl Pts',(2.89838999345532,5.15822314448862,19.2332916106432));
#17266=CARTESIAN_POINT('Ctrl Pts',(3.04261687177272,5.07718249750748,19.2255053820643));
#17267=CARTESIAN_POINT('Ctrl Pts',(3.18344235521173,4.9900892635211,19.2177191534855));
#17268=CARTESIAN_POINT('Ctrl Pts',(3.32036379618839,4.89725584623281,19.2099329249066));
#17269=CARTESIAN_POINT('Ctrl Pts',(3.45732128124291,4.80439799088065,19.202144646631));
#17270=CARTESIAN_POINT('Ctrl Pts',(3.59037240446021,4.70579711059089,19.1943563683554));
#17271=CARTESIAN_POINT('Ctrl Pts',(3.71904375108522,4.6018087900318,19.1865680900798));
#17272=CARTESIAN_POINT('Ctrl Pts',(3.84137172488175,4.50294699301051,19.1791637663837));
#17273=CARTESIAN_POINT('Ctrl Pts',(3.95974115228138,4.39921631685875,19.1717594426877));
#17274=CARTESIAN_POINT('Ctrl Pts',(4.07377321349348,4.2909558803981,19.1643551189916));
#17275=CARTESIAN_POINT('Ctrl Pts',(4.19371383106715,4.17708594355872,19.1565671412301));
#17276=CARTESIAN_POINT('Ctrl Pts',(4.30889857389756,4.0581636322002,19.1487791634686));
#17277=CARTESIAN_POINT('Ctrl Pts',(4.41891139866457,3.93460958841565,19.1409911857071));
#17278=CARTESIAN_POINT('Ctrl Pts',(4.52890259396773,3.81107983641461,19.1332047391287));
#17279=CARTESIAN_POINT('Ctrl Pts',(4.6337236877407,3.68292040748779,19.1254182925504));
#17280=CARTESIAN_POINT('Ctrl Pts',(4.73299723553544,3.55058695583053,19.117631845972));
#17281=CARTESIAN_POINT('Ctrl Pts',(4.83227457039175,3.41824845595105,19.1098451023583));
#17282=CARTESIAN_POINT('Ctrl Pts',(4.92600374088628,3.28173586795651,19.1020583587446));
#17283=CARTESIAN_POINT('Ctrl Pts',(5.01384871420258,3.14153650839667,19.0942716151309));
#17284=CARTESIAN_POINT('Ctrl Pts',(5.10168787723106,3.00134642197563,19.086485386552));
#17285=CARTESIAN_POINT('Ctrl Pts',(5.18364345233471,2.85747032284362,19.0786991579731));
#17286=CARTESIAN_POINT('Ctrl Pts',(5.2594236542145,2.71042310128678,19.0709129293942));
#17287=CARTESIAN_POINT('Ctrl Pts',(5.3352238049602,2.5633371700771,19.0631246511187));
#17288=CARTESIAN_POINT('Ctrl Pts',(5.40484518588127,2.41307873170581,19.0553363728431));
#17289=CARTESIAN_POINT('Ctrl Pts',(5.4680423473127,2.26018659638867,19.0475480945675));
#17290=CARTESIAN_POINT('Ctrl Pts',(5.52812394986432,2.11483189533364,19.0401437708714));
#17291=CARTESIAN_POINT('Ctrl Pts',(5.58239938977393,1.96709716298893,19.0327394471753));
#17292=CARTESIAN_POINT('Ctrl Pts',(5.63069838974732,1.81746147309837,19.0253351234791));
#17293=CARTESIAN_POINT('Ctrl Pts',(5.68149999609703,1.66007242947687,19.0175471457176));
#17294=CARTESIAN_POINT('Ctrl Pts',(5.7257075551797,1.50052390131145,19.0097591679561));
#17295=CARTESIAN_POINT('Ctrl Pts',(5.76315713010442,1.33938435716808,19.0019711901946));
#17296=CARTESIAN_POINT('Ctrl Pts',(5.80059934212158,1.17827649444091,18.9941847436163));
#17297=CARTESIAN_POINT('Ctrl Pts',(5.83128614879123,1.01557855094246,18.986398297038));
#17298=CARTESIAN_POINT('Ctrl Pts',(5.85510426204067,0.851871259717815,18.9786118504597));
#17299=CARTESIAN_POINT('Ctrl Pts',(5.87892328389751,0.688157723428518,18.9708251068459));
#17300=CARTESIAN_POINT('Ctrl Pts',(5.89587303809803,0.523435078005543,18.9630383632322));
#17301=CARTESIAN_POINT('Ctrl Pts',(5.90589175156542,0.358292033530678,18.9552516196185));
#17302=CARTESIAN_POINT('Ctrl Pts',(5.91590980236986,0.193159912032734,18.9474653910396));
#17303=CARTESIAN_POINT('Ctrl Pts',(5.91899771060221,0.0276077661245249,
18.9396791624607));
#17304=CARTESIAN_POINT('Ctrl Pts',(5.9151457509911,-0.13777266431309,18.9318929338819));
#17305=CARTESIAN_POINT('Ctrl Pts',(5.91129277736546,-0.303196630554846,
18.9241046556063));
#17306=CARTESIAN_POINT('Ctrl Pts',(5.90049629086504,-0.468448471278026,
18.9163163773307));
#17307=CARTESIAN_POINT('Ctrl Pts',(5.88279869842481,-0.632937624344924,
18.9085280990551));
#17308=CARTESIAN_POINT('Ctrl Pts',(5.86597358015943,-0.789317621402037,
18.9011237753589));
#17309=CARTESIAN_POINT('Ctrl Pts',(5.84291142907199,-0.945008056900892,
18.8937194516628));
#17310=CARTESIAN_POINT('Ctrl Pts',(5.81369205926739,-1.09950679966579,18.8863151279666));
#17311=CARTESIAN_POINT('Ctrl Pts',(5.78295869163224,-1.26201087461043,18.8785271502051));
#17312=CARTESIAN_POINT('Ctrl Pts',(5.74540209987075,-1.42325461413253,18.8707391724436));
#17313=CARTESIAN_POINT('Ctrl Pts',(5.70115045531926,-1.5826604336727,18.862951194682));
#17314=CARTESIAN_POINT('Ctrl Pts',(5.65690751102047,-1.74203491266206,18.8551647481037));
#17315=CARTESIAN_POINT('Ctrl Pts',(5.60597222577068,-1.89957188495373,18.8473783015254));
#17316=CARTESIAN_POINT('Ctrl Pts',(5.54852311098912,-2.05470724175479,18.839591854947));
#17317=CARTESIAN_POINT('Ctrl Pts',(5.49107180465324,-2.20984851662026,18.8318051113333));
#17318=CARTESIAN_POINT('Ctrl Pts',(5.42710627881486,-2.3625876916437,18.8240183677196));
#17319=CARTESIAN_POINT('Ctrl Pts',(5.35685409321845,-2.51237831276836,18.8162316241059));
#17320=CARTESIAN_POINT('Ctrl Pts',(5.28660655427863,-2.66215902636385,18.808445395527));
#17321=CARTESIAN_POINT('Ctrl Pts',(5.21007332349161,-2.80899128704693,18.8006591669481));
#17322=CARTESIAN_POINT('Ctrl Pts',(5.12752910865091,-2.95235089419222,18.7928729383692));
#17323=CARTESIAN_POINT('Ctrl Pts',(5.04496316434218,-3.0957482402391,18.7850846600937));
#17324=CARTESIAN_POINT('Ctrl Pts',(4.95638323193211,-3.23567082797014,18.7772963818181));
#17325=CARTESIAN_POINT('Ctrl Pts',(4.86210922735398,-3.37162044479791,18.7695081035425));
#17326=CARTESIAN_POINT('Ctrl Pts',(4.7724828399381,-3.50086787712427,18.7621037798463));
#17327=CARTESIAN_POINT('Ctrl Pts',(4.67771043105415,-3.62652441309787,18.7546994561502));
#17328=CARTESIAN_POINT('Ctrl Pts',(4.57810243098197,-3.74818738778319,18.747295132454));
#17329=CARTESIAN_POINT('Ctrl Pts',(4.47333325539396,-3.87615431361373,18.7395071546925));
#17330=CARTESIAN_POINT('Ctrl Pts',(4.36317659531128,-3.9997486150978,18.731719176931));
#17331=CARTESIAN_POINT('Ctrl Pts',(4.24802145555584,-4.11852452653098,18.7239311991694));
#17332=CARTESIAN_POINT('Ctrl Pts',(4.13288895628821,-4.2372770856016,18.7161447525911));
#17333=CARTESIAN_POINT('Ctrl Pts',(4.01276016050691,-4.35121291555212,18.7083583060127));
#17334=CARTESIAN_POINT('Ctrl Pts',(3.88806182103385,-4.4599221785048,18.7005718594344));
#17335=CARTESIAN_POINT('Ctrl Pts',(3.76335872460007,-4.56863558847094,18.6927851158207));
#17336=CARTESIAN_POINT('Ctrl Pts',(3.63408597392483,-4.67212181951422,18.684998372207));
#17337=CARTESIAN_POINT('Ctrl Pts',(3.50070493533526,-4.77001001238145,18.6772116285933));
#17338=CARTESIAN_POINT('Ctrl Pts',(3.36733271890335,-4.8678917306772,18.6694254000144));
#17339=CARTESIAN_POINT('Ctrl Pts',(3.22985301604037,-4.96017596276984,18.6616391714354));
#17340=CARTESIAN_POINT('Ctrl Pts',(3.08875793689795,-5.04653395606826,18.6538529428565));
#17341=CARTESIAN_POINT('Ctrl Pts',(2.94762571498308,-5.13291468279802,18.646064664581));
#17342=CARTESIAN_POINT('Ctrl Pts',(2.8028764867344,-5.2133658848067,18.6382763863054));
#17343=CARTESIAN_POINT('Ctrl Pts',(2.65502961526059,-5.28760326656503,18.6304881080298));
#17344=CARTESIAN_POINT('Ctrl Pts',(2.51447145142661,-5.35818081726851,18.6230837843337));
#17345=CARTESIAN_POINT('Ctrl Pts',(2.37111394427869,-5.42314234174564,18.6156794606376));
#17346=CARTESIAN_POINT('Ctrl Pts',(2.22542239301741,-5.48228289448444,18.6082751369415));
#17347=CARTESIAN_POINT('Ctrl Pts',(2.07218185305225,-5.5444878072407,18.60048715918));
#17348=CARTESIAN_POINT('Ctrl Pts',(1.91630415376516,-5.60027475898381,18.5926991814185));
#17349=CARTESIAN_POINT('Ctrl Pts',(1.75834421344769,-5.64943857294997,18.584911203657));
#17350=CARTESIAN_POINT('Ctrl Pts',(1.60041532940884,-5.69859272088878,18.5771247570786));
#17351=CARTESIAN_POINT('Ctrl Pts',(1.44040532611202,-5.74112623434872,18.5693383105003));
#17352=CARTESIAN_POINT('Ctrl Pts',(1.27888506697831,-5.77688354980087,18.561551863922));
#17353=CARTESIAN_POINT('Ctrl Pts',(1.11735864621065,-5.81264222931404,18.5537651203083));
#17354=CARTESIAN_POINT('Ctrl Pts',(0.954322165452405,-5.84162412063496,
18.5459783766946));
#17355=CARTESIAN_POINT('Ctrl Pts',(0.790358220861857,-5.86372445167882,
18.5381916330809));
#17356=CARTESIAN_POINT('Ctrl Pts',(0.626405121259873,-5.88582332095108,
18.530405404502));
#17357=CARTESIAN_POINT('Ctrl Pts',(0.4615249973136,-5.90104149822039,18.5226191759231));
#17358=CARTESIAN_POINT('Ctrl Pts',(0.296307283063741,-5.9093258969618,18.5148329473443));
#17359=CARTESIAN_POINT('Ctrl Pts',(0.13104607584411,-5.91761247654142,18.5070446690687));
#17360=CARTESIAN_POINT('Ctrl Pts',(-0.0345525799950898,-5.91896161230755,
18.4992563907931));
#17361=CARTESIAN_POINT('Ctrl Pts',(-0.199896602559165,-5.91337229597336,
18.4914681125176));
#17362=CARTESIAN_POINT('Ctrl Pts',(-0.357089324875416,-5.9080585275236,
18.4840637888214));
#17363=CARTESIAN_POINT('Ctrl Pts',(-0.514051652149983,-5.89647395436541,
18.4766594651252));
#17364=CARTESIAN_POINT('Ctrl Pts',(-0.670276952662783,-5.87866135861125,
18.469255141429));
#17365=CARTESIAN_POINT('Ctrl Pts',(-0.834597046719215,-5.85992580553435,
18.4614671636675));
#17366=CARTESIAN_POINT('Ctrl Pts',(-0.998160488801119,-5.83429298411085,
18.453679185906));
#17367=CARTESIAN_POINT('Ctrl Pts',(-1.16038185126092,-5.80184837114555,
18.4458912081445));
#17368=CARTESIAN_POINT('Ctrl Pts',(-1.32257131960991,-5.76941013706935,
18.4381047615662));
#17369=CARTESIAN_POINT('Ctrl Pts',(-1.48341892167171,-5.73016284629375,
18.4303183149878));
#17370=CARTESIAN_POINT('Ctrl Pts',(-1.6423489782677,-5.68424316827518,18.4225318684095));
#17371=CARTESIAN_POINT('Ctrl Pts',(-1.80128509768769,-5.63832173852423,
18.4147451247958));
#17372=CARTESIAN_POINT('Ctrl Pts',(-1.9583032171875,-5.58572749709572,18.4069583811821));
#17373=CARTESIAN_POINT('Ctrl Pts',(-2.11284166849272,-5.52664732422659,
18.3991716375683));
#17374=CARTESIAN_POINT('Ctrl Pts',(-2.26736989823559,-5.46757105906888,
18.3913854089894));
#17375=CARTESIAN_POINT('Ctrl Pts',(-2.41941848952946,-5.40200983518058,
18.3835991804105));
#17376=CARTESIAN_POINT('Ctrl Pts',(-2.56844451065284,-5.33019918560248,
18.3758129518316));
#17377=CARTESIAN_POINT('Ctrl Pts',(-2.71750976234046,-5.25836963212907,
18.3680246735561));
#17378=CARTESIAN_POINT('Ctrl Pts',(-2.86355056500712,-5.18028750267804,
18.3602363952805));
#17379=CARTESIAN_POINT('Ctrl Pts',(-3.00604659027617,-5.09623532223435,
18.3524481170049));
#17380=CARTESIAN_POINT('Ctrl Pts',(-3.14151769944448,-5.01632683291879,
18.3450437933088));
#17381=CARTESIAN_POINT('Ctrl Pts',(-3.27378489328733,-4.93102288253372,
18.3376394696127));
#17382=CARTESIAN_POINT('Ctrl Pts',(-3.40242382940286,-4.84060354166829,
18.3302351459165));
#17383=CARTESIAN_POINT('Ctrl Pts',(-3.5377281751942,-4.74549913446382,18.322447168155));
#17384=CARTESIAN_POINT('Ctrl Pts',(-3.66906668631932,-4.64470113540048,
18.3146591903935));
#17385=CARTESIAN_POINT('Ctrl Pts',(-3.79596627439377,-4.53856481788737,
18.306871212632));
#17386=CARTESIAN_POINT('Ctrl Pts',(-3.92284091292092,-4.43244936768452,
18.2990847660537));
#17387=CARTESIAN_POINT('Ctrl Pts',(-4.0452781247844,-4.3209978980971,18.2912983194754));
#17388=CARTESIAN_POINT('Ctrl Pts',(-4.16283788496959,-4.20460596322199,
18.2835118728971));
#17389=CARTESIAN_POINT('Ctrl Pts',(-4.28040212979489,-4.08820958825667,
18.2757251292834));
#17390=CARTESIAN_POINT('Ctrl Pts',(-4.39308832076967,-3.96687259288409,
18.2679383856697));
#17391=CARTESIAN_POINT('Ctrl Pts',(-4.50049276866213,-3.84102790952108,
18.260151642056));
#17392=CARTESIAN_POINT('Ctrl Pts',(-4.60789011255429,-3.71519154984192,
18.2523654134771));
#17393=CARTESIAN_POINT('Ctrl Pts',(-4.71000620508511,-3.58484834196991,
18.2445791848983));
#17394=CARTESIAN_POINT('Ctrl Pts',(-4.80647709615534,-3.45046496673044,
18.2367929563194));
#17395=CARTESIAN_POINT('Ctrl Pts',(-4.90297338284109,-3.3160462155502,18.2290046780438));
#17396=CARTESIAN_POINT('Ctrl Pts',(-4.99382131050251,-3.17758543040561,
18.2212163997682));
#17397=CARTESIAN_POINT('Ctrl Pts',(-5.07869926820291,-3.03557973139485,
18.2134281214926));
#17398=CARTESIAN_POINT('Ctrl Pts',(-5.15939282475632,-2.90057477587416,
18.2060237977964));
#17399=CARTESIAN_POINT('Ctrl Pts',(-5.23469072442586,-2.76236623480627,
18.1986194741002));
#17400=CARTESIAN_POINT('Ctrl Pts',(-5.30435445677128,-2.62140312798902,
18.191215150404));
#17401=CARTESIAN_POINT('Ctrl Pts',(-5.3774115817258,-2.47357356213026,18.183450154426));
#17402=CARTESIAN_POINT('Ctrl Pts',(-5.44429948401845,-2.32265849524358,
18.175685158448));
#17403=CARTESIAN_POINT('Ctrl Pts',(-5.50477361220699,-2.16919294689283,
18.16792016247));
#17404=CARTESIAN_POINT('Ctrl Pts',(-5.56523522785852,-2.01575915168033,
18.1601567731261));
#17405=CARTESIAN_POINT('Ctrl Pts',(-5.61928559859745,-1.85977622850732,
18.1523933837822));
#17406=CARTESIAN_POINT('Ctrl Pts',(-5.6667284601636,-1.70179878989023,18.1446299944383));
#17407=CARTESIAN_POINT('Ctrl Pts',(-5.71417181700182,-1.54381970209328,
18.1368665240498));
#17408=CARTESIAN_POINT('Ctrl Pts',(-5.75500742999307,-1.38384636573191,
18.1291030536613));
#17409=CARTESIAN_POINT('Ctrl Pts',(-5.7890888339399,-1.22244878635157,18.1213395832728));
#17410=CARTESIAN_POINT('Ctrl Pts',(-5.82316860033722,-1.06105896183154,
18.1135764859049));
#17411=CARTESIAN_POINT('Ctrl Pts',(-5.85049474115828,-0.898245347765023,
18.105813388537));
#17412=CARTESIAN_POINT('Ctrl Pts',(-5.87097182966171,-0.734588550018744,
18.0980502911692));
#17413=CARTESIAN_POINT('Ctrl Pts',(-5.89145331993988,-0.570896572449048,
18.0902855250384));
#17414=CARTESIAN_POINT('Ctrl Pts',(-5.90508277646522,-0.40636137001757,
18.0825207589076));
#17415=CARTESIAN_POINT('Ctrl Pts',(-5.91181652145501,-0.241569822518524,
18.0747559927768));
#17416=CARTESIAN_POINT('Ctrl Pts',(-5.91510639983007,-0.161058287060608,
18.0709623926004));
#17417=CARTESIAN_POINT('Ctrl Pts',(-5.91675108298957,-0.0804856220266957,
18.067168792424));
#17418=CARTESIAN_POINT('Ctrl Pts',(-5.9167499994649,7.95746161645733E-5,
18.0633751922476));
#17419=CARTESIAN_POINT('Ctrl Pts',(-5.91674999819064,0.000146325028583011,
17.8116248078341));
#17420=CARTESIAN_POINT('Ctrl Pts',(-5.9167540725871,-0.164604609812423,
17.8193809745373));
#17421=CARTESIAN_POINT('Ctrl Pts',(-5.90987261000619,-0.329380941156183,
17.8271371412406));
#17422=CARTESIAN_POINT('Ctrl Pts',(-5.89612531645656,-0.493595801380071,
17.8348933079438));
#17423=CARTESIAN_POINT('Ctrl Pts',(-5.88237802530819,-0.657810632920316,
17.8426494732922));
#17424=CARTESIAN_POINT('Ctrl Pts',(-5.86176492750662,-0.821463669676354,
17.8504056386407));
#17425=CARTESIAN_POINT('Ctrl Pts',(-5.83435771645861,-0.983971848631785,
17.8581618039891));
#17426=CARTESIAN_POINT('Ctrl Pts',(-5.80695247133969,-1.14646837081722,
17.865917412985));
#17427=CARTESIAN_POINT('Ctrl Pts',(-5.77275414191316,-1.30781987939427,
17.8736730219809));
#17428=CARTESIAN_POINT('Ctrl Pts',(-5.73188581331638,-1.46745207267648,
17.8814286309768));
#17429=CARTESIAN_POINT('Ctrl Pts',(-5.69100690643398,-1.62712558487214,
17.8891862474208));
#17430=CARTESIAN_POINT('Ctrl Pts',(-5.64345462981406,-1.78507857753726,
17.8969438638648));
#17431=CARTESIAN_POINT('Ctrl Pts',(-5.58940257527164,-1.94074970412125,
17.9047014803088));
#17432=CARTESIAN_POINT('Ctrl Pts',(-5.54438664803198,-2.0703965818754,17.9111622207996));
#17433=CARTESIAN_POINT('Ctrl Pts',(-5.4948634147778,-2.1984609143109,17.9176229612904));
#17434=CARTESIAN_POINT('Ctrl Pts',(-5.44095909162526,-2.3246278682319,17.9240837017813));
#17435=CARTESIAN_POINT('Ctrl Pts',(-5.37598002709395,-2.47671605264993,
17.9318718131742));
#17436=CARTESIAN_POINT('Ctrl Pts',(-5.30460850959539,-2.62610519568956,
17.9396599245672));
#17437=CARTESIAN_POINT('Ctrl Pts',(-5.22709400012667,-2.77225880399717,
17.9474480359602));
#17438=CARTESIAN_POINT('Ctrl Pts',(-5.14959470928051,-2.91838371759179,
17.9552346182932));
#17439=CARTESIAN_POINT('Ctrl Pts',(-5.06595498255194,-3.06127408183878,
17.9630212006263));
#17440=CARTESIAN_POINT('Ctrl Pts',(-4.97647054204924,-3.20041739568703,
17.9708077829594));
#17441=CARTESIAN_POINT('Ctrl Pts',(-4.88698268952489,-3.33956601503862,
17.9785946621931));
#17442=CARTESIAN_POINT('Ctrl Pts',(-4.79164984679594,-3.4749670272255,17.9863815414268));
#17443=CARTESIAN_POINT('Ctrl Pts',(-4.69081183623025,-3.60613572672773,
17.9941684206605));
#17444=CARTESIAN_POINT('Ctrl Pts',(-4.58998048091514,-3.73729576917142,
18.0019547859646));
#17445=CARTESIAN_POINT('Ctrl Pts',(-4.48364487971286,-3.86422380464239,
18.0097411512688));
#17446=CARTESIAN_POINT('Ctrl Pts',(-4.37218611028819,-3.98646700469263,
18.0175275165729));
#17447=CARTESIAN_POINT('Ctrl Pts',(-4.26069807405392,-4.10874230332498,
18.0253159264185));
#17448=CARTESIAN_POINT('Ctrl Pts',(-4.14408439551994,-4.2263300708761,18.0331043362641));
#17449=CARTESIAN_POINT('Ctrl Pts',(-4.02276470881542,-4.33881258641223,
18.0408927461097));
#17450=CARTESIAN_POINT('Ctrl Pts',(-3.90782060928847,-4.44538392542597,
18.0482718597619));
#17451=CARTESIAN_POINT('Ctrl Pts',(-3.78865259034154,-4.54737261642784,
18.0556509734142));
#17452=CARTESIAN_POINT('Ctrl Pts',(-3.66564642919633,-4.64445549215623,
18.0630300870664));
#17453=CARTESIAN_POINT('Ctrl Pts',(-3.53582247876412,-4.74691932265901,
18.0708181984594));
#17454=CARTESIAN_POINT('Ctrl Pts',(-3.4016764860377,-4.84395468839645,18.0786063098524));
#17455=CARTESIAN_POINT('Ctrl Pts',(-3.26368418575208,-4.93520983324638,
18.0863944212453));
#17456=CARTESIAN_POINT('Ctrl Pts',(-3.12571897784921,-5.02644706173934,
18.0941810035784));
#17457=CARTESIAN_POINT('Ctrl Pts',(-2.9839092355035,-5.11190615755588,18.1019675859115));
#17458=CARTESIAN_POINT('Ctrl Pts',(-2.8387598376241,-5.19127856570926,18.1097541682446));
#17459=CARTESIAN_POINT('Ctrl Pts',(-2.69360490523057,-5.27065400031484,
18.1175410474783));
#17460=CARTESIAN_POINT('Ctrl Pts',(-2.54511034093988,-5.34394212609427,
18.125327926712));
#17461=CARTESIAN_POINT('Ctrl Pts',(-2.39380645074351,-5.41087989507056,
18.1331148059457));
#17462=CARTESIAN_POINT('Ctrl Pts',(-2.24251254651653,-5.47781324619274,
18.1409011712499));
#17463=CARTESIAN_POINT('Ctrl Pts',(-2.08840997970543,-5.53839695005758,
18.1486875365541));
#17464=CARTESIAN_POINT('Ctrl Pts',(-1.93205003240429,-5.59241568866144,
18.1564739018583));
#17465=CARTESIAN_POINT('Ctrl Pts',(-1.77564902815592,-5.64644861148919,
18.1642623117039));
#17466=CARTESIAN_POINT('Ctrl Pts',(-1.61698976057277,-5.69391301824909,
18.1720507215495));
#17467=CARTESIAN_POINT('Ctrl Pts',(-1.45664057238756,-5.73464286641936,
18.1798391313951));
#17468=CARTESIAN_POINT('Ctrl Pts',(-1.30471804813656,-5.77323228128587,
18.1872182450472));
#17469=CARTESIAN_POINT('Ctrl Pts',(-1.15127890423576,-5.80577669632586,
18.1945973586994));
#17470=CARTESIAN_POINT('Ctrl Pts',(-0.996816515083505,-5.83217690041693,
18.2019764723515));
#17471=CARTESIAN_POINT('Ctrl Pts',(-0.833792831013664,-5.86004037290847,
18.2097645837445));
#17472=CARTESIAN_POINT('Ctrl Pts',(-0.669571031919846,-5.88106916913186,
18.2175526951374));
#17473=CARTESIAN_POINT('Ctrl Pts',(-0.504737163865283,-5.8951820122803,
18.2253408065304));
#17474=CARTESIAN_POINT('Ctrl Pts',(-0.339935658066676,-5.90929208461806,
18.2331273888635));
#17475=CARTESIAN_POINT('Ctrl Pts',(-0.174522641247447,-5.916488885908,18.2409139711966));
#17476=CARTESIAN_POINT('Ctrl Pts',(-0.00908908268880194,-5.9167430188471,
18.2487005535297));
#17477=CARTESIAN_POINT('Ctrl Pts',(0.156350783813921,-5.91699716147622,
18.2564874327634));
#17478=CARTESIAN_POINT('Ctrl Pts',(0.321810874114001,-5.9103081016057,18.2642743119971));
#17479=CARTESIAN_POINT('Ctrl Pts',(0.486699662987048,-5.89669856788935,
18.2720611912308));
#17480=CARTESIAN_POINT('Ctrl Pts',(0.651577569295335,-5.88308993239436,
18.279847556535));
#17481=CARTESIAN_POINT('Ctrl Pts',(0.815883931170508,-5.86256176347832,
18.2876339218391));
#17482=CARTESIAN_POINT('Ctrl Pts',(0.979031639496074,-5.83518873828136,
18.2954202871433));
#17483=CARTESIAN_POINT('Ctrl Pts',(1.1422221870969,-5.80780852548383,18.3032086969889));
#17484=CARTESIAN_POINT('Ctrl Pts',(1.30425315756301,-5.77357991597678,18.3109971068345));
#17485=CARTESIAN_POINT('Ctrl Pts',(1.46454603556983,-5.73262901923687,18.3187855166801));
#17486=CARTESIAN_POINT('Ctrl Pts',(1.61641520885367,-5.69383017233578,18.3261646303323));
#17487=CARTESIAN_POINT('Ctrl Pts',(1.76672401938484,-5.64899746877865,18.3335437439844));
#17488=CARTESIAN_POINT('Ctrl Pts',(1.91499175774266,-5.59827983672464,18.3409228576366));
#17489=CARTESIAN_POINT('Ctrl Pts',(2.07147744379432,-5.54475110866289,18.3487109690296));
#17490=CARTESIAN_POINT('Ctrl Pts',(2.22574527185444,-5.48464747488087,18.3564990804225));
#17491=CARTESIAN_POINT('Ctrl Pts',(2.37724173580704,-5.41817794946208,18.3642871918155));
#17492=CARTESIAN_POINT('Ctrl Pts',(2.52870845606942,-5.35172147417609,18.3720737741485));
#17493=CARTESIAN_POINT('Ctrl Pts',(2.67740460546071,-5.2789017293409,18.3798603564816));
#17494=CARTESIAN_POINT('Ctrl Pts',(2.8227971756589,-5.19997564105758,18.3876469388146));
#17495=CARTESIAN_POINT('Ctrl Pts',(2.96819528964393,-5.1210465433398,18.3954338180483));
#17496=CARTESIAN_POINT('Ctrl Pts',(3.11028928968802,-5.03601078524024,18.403220697282));
#17497=CARTESIAN_POINT('Ctrl Pts',(3.24857061817865,-4.94517133183537,18.4110075765157));
#17498=CARTESIAN_POINT('Ctrl Pts',(3.38684282018164,-4.85433787378184,18.4187939418199));
#17499=CARTESIAN_POINT('Ctrl Pts',(3.52130258717436,-4.75770166249414,18.4265803071241));
#17500=CARTESIAN_POINT('Ctrl Pts',(3.65147009341721,-4.65560916737861,18.4343666724283));
#17501=CARTESIAN_POINT('Ctrl Pts',(3.78167177900373,-4.55348986484716,18.4421550822739));
#17502=CARTESIAN_POINT('Ctrl Pts',(3.90757869895332,-4.44591161143244,18.4499434921195));
#17503=CARTESIAN_POINT('Ctrl Pts',(4.02874318097474,-4.33326192887639,18.4577319019651));
#17504=CARTESIAN_POINT('Ctrl Pts',(4.14354023212818,-4.22653220779757,18.4651110156173));
#17505=CARTESIAN_POINT('Ctrl Pts',(4.2540802833303,-4.11525055202227,18.4724901292695));
#17506=CARTESIAN_POINT('Ctrl Pts',(4.36001246514896,-3.99977772710506,18.4798692429217));
#17507=CARTESIAN_POINT('Ctrl Pts',(4.47181608696418,-3.87790465864433,18.4876573543147));
#17508=CARTESIAN_POINT('Ctrl Pts',(4.57852649029881,-3.75131911686164,18.4954454657077));
#17509=CARTESIAN_POINT('Ctrl Pts',(4.67975762850595,-3.62046945863936,18.5032335771007));
#17510=CARTESIAN_POINT('Ctrl Pts',(4.78096889174362,-3.48964549046668,18.5110201594337));
#17511=CARTESIAN_POINT('Ctrl Pts',(4.87670284091196,-3.35455932885706,18.5188067417668));
#17512=CARTESIAN_POINT('Ctrl Pts',(4.96661435174363,-3.21569159646167,18.5265933240998));
#17513=CARTESIAN_POINT('Ctrl Pts',(5.05652929088143,-3.07681856907019,18.5343802033335));
#17514=CARTESIAN_POINT('Ctrl Pts',(5.14062117047605,-2.93416394842851,18.5421670825673));
#17515=CARTESIAN_POINT('Ctrl Pts',(5.2185883636556,-2.78823708698138,18.549953961801));
#17516=CARTESIAN_POINT('Ctrl Pts',(5.29655041104549,-2.6423198566227,18.5577403271052));
#17517=CARTESIAN_POINT('Ctrl Pts',(5.36838843045436,-2.49313109954214,18.5655266924094));
#17518=CARTESIAN_POINT('Ctrl Pts',(5.4338468391293,-2.34120462398836,18.5733130577136));
#17519=CARTESIAN_POINT('Ctrl Pts',(5.49932243585305,-2.18923825562739,18.5811014675592));
#17520=CARTESIAN_POINT('Ctrl Pts',(5.55841494623099,-2.03453302521722,18.5888898774048));
#17521=CARTESIAN_POINT('Ctrl Pts',(5.61091666307221,-1.87764340665598,18.5966782872504));
#17522=CARTESIAN_POINT('Ctrl Pts',(5.66065931185227,-1.72899864486787,18.6040574009026));
#17523=CARTESIAN_POINT('Ctrl Pts',(5.70448598572576,-1.5783934242125,18.6114365145548));
#17524=CARTESIAN_POINT('Ctrl Pts',(5.74226118119846,-1.42631240946761,18.6188156282069));
#17525=CARTESIAN_POINT('Ctrl Pts',(5.78213011994918,-1.26580209082761,18.6266037395999));
#17526=CARTESIAN_POINT('Ctrl Pts',(5.81527197387513,-1.10359041712131,18.6343918509929));
#17527=CARTESIAN_POINT('Ctrl Pts',(5.84156225634684,-0.940255799090872,
18.6421799623858));
#17528=CARTESIAN_POINT('Ctrl Pts',(5.86784737717978,-0.776953248966031,
18.6499665447189));
#17529=CARTESIAN_POINT('Ctrl Pts',(5.8872835598595,-0.612528509694548,18.6577531270519));
#17530=CARTESIAN_POINT('Ctrl Pts',(5.89979768971373,-0.447568746617209,
18.6655397093849));
#17531=CARTESIAN_POINT('Ctrl Pts',(5.91231229672898,-0.282602693660528,
18.6733265886186));
#17532=CARTESIAN_POINT('Ctrl Pts',(5.91790429467534,-0.117101894378561,
18.6811134678523));
#17533=CARTESIAN_POINT('Ctrl Pts',(5.91655251028279,0.0483420682882251,
18.688900347086));
#17534=CARTESIAN_POINT('Ctrl Pts',(5.91520081510723,0.213775111749494,18.6966867123902));
#17535=CARTESIAN_POINT('Ctrl Pts',(5.90690625742143,0.37915100656057,18.7044730776944));
#17536=CARTESIAN_POINT('Ctrl Pts',(5.89169979686626,0.543878723711526,18.7122594429986));
#17537=CARTESIAN_POINT('Ctrl Pts',(5.87648934340334,0.708649695015895,18.7200478528442));
#17538=CARTESIAN_POINT('Ctrl Pts',(5.85436338792983,0.872771830005027,18.7278362626898));
#17539=CARTESIAN_POINT('Ctrl Pts',(5.82540481788583,1.03565885804763,18.7356246725353));
#17540=CARTESIAN_POINT('Ctrl Pts',(5.79796807742191,1.18998585370229,18.7430037861876));
#17541=CARTESIAN_POINT('Ctrl Pts',(5.76439843169625,1.34320396202403,18.7503828998398));
#17542=CARTESIAN_POINT('Ctrl Pts',(5.72480877271826,1.49482275815833,18.757762013492));
#17543=CARTESIAN_POINT('Ctrl Pts',(5.68302480127369,1.65484523907078,18.765550124885));
#17544=CARTESIAN_POINT('Ctrl Pts',(5.63451963482885,1.81314324410065,18.7733382362779));
#17545=CARTESIAN_POINT('Ctrl Pts',(5.57946069092875,1.96914929877876,18.7811263476709));
#17546=CARTESIAN_POINT('Ctrl Pts',(5.52441255689239,2.12512472438785,18.788912930004));
#17547=CARTESIAN_POINT('Ctrl Pts',(5.46281331906599,2.27880879637063,18.7966995123371));
#17548=CARTESIAN_POINT('Ctrl Pts',(5.39487969439156,2.42965093080089,18.8044860946702));
#17549=CARTESIAN_POINT('Ctrl Pts',(5.32694347942315,2.58049881680816,18.8122729739039));
#17550=CARTESIAN_POINT('Ctrl Pts',(5.2526725219132,2.72850425547445,18.8200598531376));
#17551=CARTESIAN_POINT('Ctrl Pts',(5.17233126327013,2.87313763427693,18.8278467323714));
#17552=CARTESIAN_POINT('Ctrl Pts',(5.09199530710365,3.01776146736008,18.8356330976756));
#17553=CARTESIAN_POINT('Ctrl Pts',(5.00559000681519,3.15901340665284,18.8434194629798));
#17554=CARTESIAN_POINT('Ctrl Pts',(4.91342531789231,3.29638926827443,18.851205828284));
#17555=CARTESIAN_POINT('Ctrl Pts',(4.82123642839389,3.43380120200731,18.8589942381296));
#17556=CARTESIAN_POINT('Ctrl Pts',(4.72328530489684,3.56733475773288,18.8667826479752));
#17557=CARTESIAN_POINT('Ctrl Pts',(4.61992522529848,3.69651477410152,18.8745710578208));
#17558=CARTESIAN_POINT('Ctrl Pts',(4.521996920347,3.81890612756933,18.8819501714729));
#17559=CARTESIAN_POINT('Ctrl Pts',(4.41921370209614,3.93738954361189,18.889329285125));
#17560=CARTESIAN_POINT('Ctrl Pts',(4.31190934014089,4.05158838048805,18.8967083987771));
#17561=CARTESIAN_POINT('Ctrl Pts',(4.19865748317581,4.17211684833235,18.9044965101701));
#17562=CARTESIAN_POINT('Ctrl Pts',(4.08032864153333,4.28791535783792,18.912284621563));
#17563=CARTESIAN_POINT('Ctrl Pts',(3.95734132817861,4.39856569517719,18.920072732956));
#17564=CARTESIAN_POINT('Ctrl Pts',(3.83437816123921,4.50919430825134,18.927859315289));
#17565=CARTESIAN_POINT('Ctrl Pts',(3.70675858489957,4.61467655233321,18.935645897622));
#17566=CARTESIAN_POINT('Ctrl Pts',(3.57493632201928,4.7146326321366,18.9434324799551));
#17567=CARTESIAN_POINT('Ctrl Pts',(3.44310903278497,4.81459252324342,18.9512193591888));
#17568=CARTESIAN_POINT('Ctrl Pts',(3.30707898856819,4.90902563223852,18.9590062384225));
#17569=CARTESIAN_POINT('Ctrl Pts',(3.16733178671294,4.99759341237138,18.9667931176562));
#17570=CARTESIAN_POINT('Ctrl Pts',(3.02759380809268,5.08615534708166,18.9745794829604));
#17571=CARTESIAN_POINT('Ctrl Pts',(2.88413943275194,5.16885255663049,18.9823658482645));
#17572=CARTESIAN_POINT('Ctrl Pts',(2.73748205902751,5.24539059927881,18.9901522135687));
#17573=CARTESIAN_POINT('Ctrl Pts',(2.59078617605451,5.32194873926308,18.9979406234143));
#17574=CARTESIAN_POINT('Ctrl Pts',(2.44088589668048,5.39234433104655,19.0057290332599));
#17575=CARTESIAN_POINT('Ctrl Pts',(2.28831877623673,5.45632914520582,19.0135174431055));
#17576=CARTESIAN_POINT('Ctrl Pts',(2.14376935682108,5.51695143204743,19.0208965567577));
#17577=CARTESIAN_POINT('Ctrl Pts',(1.99682642228916,5.5718193081064,19.02827567041));
#17578=CARTESIAN_POINT('Ctrl Pts',(1.84796326203191,5.62076172281661,19.0356547840622));
#17579=CARTESIAN_POINT('Ctrl Pts',(1.69084915198724,5.67241683961881,19.0434428954552));
#17580=CARTESIAN_POINT('Ctrl Pts',(1.53153980467278,5.71748946353226,19.0512310068482));
#17581=CARTESIAN_POINT('Ctrl Pts',(1.3706028141193,5.75581258280951,19.0590191182411));
#17582=CARTESIAN_POINT('Ctrl Pts',(1.20969742073803,5.79412817801044,19.0668057005742));
#17583=CARTESIAN_POINT('Ctrl Pts',(1.04716533237892,5.82569683866613,19.0745922829073));
#17584=CARTESIAN_POINT('Ctrl Pts',(0.883586680899844,5.85040213488239,19.0823788652404));
#17585=CARTESIAN_POINT('Ctrl Pts',(0.720001792203485,5.87510837310604,19.0901657444741));
#17586=CARTESIAN_POINT('Ctrl Pts',(0.555370575880033,5.89295067161186,19.0979526237078));
#17587=CARTESIAN_POINT('Ctrl Pts',(0.390281418745612,5.90386407166374,19.1057395029415));
#17588=CARTESIAN_POINT('Ctrl Pts',(0.225203157400029,5.91477675143752,19.1135258682457));
#17589=CARTESIAN_POINT('Ctrl Pts',(0.0596673345911858,5.91876142693074,
19.1213122335499));
#17590=CARTESIAN_POINT('Ctrl Pts',(-0.105734351571204,5.91580516999992,
19.1290985988541));
#17591=CARTESIAN_POINT('Ctrl Pts',(-0.271179468857582,5.91284813681607,
19.1368870086997));
#17592=CARTESIAN_POINT('Ctrl Pts',(-0.436490059395146,5.90294653315044,
19.1446754185453));
#17593=CARTESIAN_POINT('Ctrl Pts',(-0.601075321867329,5.88613956850686,
19.1524638283909));
#17594=CARTESIAN_POINT('Ctrl Pts',(-0.757011306404463,5.87021584277703,
19.1598429420431));
#17595=CARTESIAN_POINT('Ctrl Pts',(-0.912295978160383,5.84809389555017,
19.1672220556953));
#17596=CARTESIAN_POINT('Ctrl Pts',(-1.06643189429465,5.81984996175427,19.1746011693474));
#17597=CARTESIAN_POINT('Ctrl Pts',(-1.22911101012078,5.79004056824881,19.1823892807404));
#17598=CARTESIAN_POINT('Ctrl Pts',(-1.39056851718186,5.75340065856032,19.1901773921334));
#17599=CARTESIAN_POINT('Ctrl Pts',(-1.55022609389384,5.71005513286086,19.1979655035264));
#17600=CARTESIAN_POINT('Ctrl Pts',(-1.7098523246219,5.66671811730028,19.2057520858594));
#17601=CARTESIAN_POINT('Ctrl Pts',(-1.86767902193326,5.61667819626607,19.2135386681923));
#17602=CARTESIAN_POINT('Ctrl Pts',(-2.02314105463405,5.56011068554883,19.2213252505253));
#17603=CARTESIAN_POINT('Ctrl Pts',(-2.17860901506916,5.5035410179244,19.229112129759));
#17604=CARTESIAN_POINT('Ctrl Pts',(-2.33171182886849,5.44044336811981,19.2368990089928));
#17605=CARTESIAN_POINT('Ctrl Pts',(-2.48190174158795,5.37104219938763,19.2446858882265));
#17606=CARTESIAN_POINT('Ctrl Pts',(-2.6320817418598,5.30164561109255,19.2524722535306));
#17607=CARTESIAN_POINT('Ctrl Pts',(-2.77934893574198,5.2259464705573,19.2602586188348));
#17608=CARTESIAN_POINT('Ctrl Pts',(-2.92317755433823,5.14421651452514,19.268044984139));
#17609=CARTESIAN_POINT('Ctrl Pts',(-3.06704393940887,5.06246509786629,19.2758333939846));
#17610=CARTESIAN_POINT('Ctrl Pts',(-3.20746966606069,4.97467985768772,19.2836218038302));
#17611=CARTESIAN_POINT('Ctrl Pts',(-3.34395469738098,4.88117788493348,19.2914102136757));
#17612=CARTESIAN_POINT('Ctrl Pts',(-3.47326717295838,4.79258962399922,19.298789327328));
#17613=CARTESIAN_POINT('Ctrl Pts',(-3.59904226817873,4.69887017428683,19.3061684409802));
#17614=CARTESIAN_POINT('Ctrl Pts',(-3.72087964060683,4.60032447362331,19.3135475546325));
#17615=CARTESIAN_POINT('Ctrl Pts',(-3.84947002056502,4.49631673905857,19.3213356660255));
#17616=CARTESIAN_POINT('Ctrl Pts',(-3.97371971817014,4.38689543302841,19.3291237774184));
#17617=CARTESIAN_POINT('Ctrl Pts',(-4.09318065268493,4.27244692266455,19.3369118888114));
#17618=CARTESIAN_POINT('Ctrl Pts',(-4.21261813312735,4.15802088227095,19.3446984711445));
#17619=CARTESIAN_POINT('Ctrl Pts',(-4.32726849585139,4.03856982782181,19.3524850534775));
#17620=CARTESIAN_POINT('Ctrl Pts',(-4.43671936351229,3.91451808680649,19.3602716358106));
#17621=CARTESIAN_POINT('Ctrl Pts',(-4.54617440451051,3.79046161572578,19.3680585150443));
#17622=CARTESIAN_POINT('Ctrl Pts',(-4.65042933938387,3.66180434403611,19.375845394278));
#17623=CARTESIAN_POINT('Ctrl Pts',(-4.7491105635871,3.52900544308526,19.3836322735117));
#17624=CARTESIAN_POINT('Ctrl Pts',(-4.84778527488706,3.39621530678447,19.3914186388159));
#17625=CARTESIAN_POINT('Ctrl Pts',(-4.94088682116381,3.25928434478957,19.3992050041201));
#17626=CARTESIAN_POINT('Ctrl Pts',(-5.02808352118854,3.11870272171817,19.4069913694243));
#17627=CARTESIAN_POINT('Ctrl Pts',(-5.11530311729573,2.97808418476775,19.4147797792699));
#17628=CARTESIAN_POINT('Ctrl Pts',(-5.19661459876018,2.83381334197159,19.4225681891156));
#17629=CARTESIAN_POINT('Ctrl Pts',(-5.27173057924417,2.68640787341795,19.4303565989612));
#17630=CARTESIAN_POINT('Ctrl Pts',(-5.34289906781531,2.54674885097706,19.4377357126133));
#17631=CARTESIAN_POINT('Ctrl Pts',(-5.40850636029273,2.40427642204715,19.4451148262655));
#17632=CARTESIAN_POINT('Ctrl Pts',(-5.46834679985539,2.25944989743329,19.4524939399176));
#17633=CARTESIAN_POINT('Ctrl Pts',(-5.5312699114988,2.10716265416091,19.4602531876029));
#17634=CARTESIAN_POINT('Ctrl Pts',(-5.5878403187911,1.95221414694597,19.4680124352882));
#17635=CARTESIAN_POINT('Ctrl Pts',(-5.63785008126168,1.79515376046669,19.4757716829735));
#17636=CARTESIAN_POINT('Ctrl Pts',(-5.68785351891928,1.63811323766045,19.4835299493346));
#17637=CARTESIAN_POINT('Ctrl Pts',(-5.73129786566256,1.47896167632964,19.4912882156957));
#17638=CARTESIAN_POINT('Ctrl Pts',(-5.76802463240211,1.31826492121368,19.4990464820568));
#17639=CARTESIAN_POINT('Ctrl Pts',(-5.80474645082447,1.15758981729621,19.5068037031214));
#17640=CARTESIAN_POINT('Ctrl Pts',(-5.83475242452542,0.995370251430543,
19.5145609241859));
#17641=CARTESIAN_POINT('Ctrl Pts',(-5.85793484294928,0.832183836817834,
19.5223181452504));
#17642=CARTESIAN_POINT('Ctrl Pts',(-5.88112019170124,0.668976794946629,
19.5300763468513));
#17643=CARTESIAN_POINT('Ctrl Pts',(-5.89748021436318,0.504802981008405,
19.5378345484521));
#17644=CARTESIAN_POINT('Ctrl Pts',(-5.90695879742514,0.340247451161346,
19.5455927500529));
#17645=CARTESIAN_POINT('Ctrl Pts',(-5.91348785311707,0.226897996737223,
19.5509367693003));
#17646=CARTESIAN_POINT('Ctrl Pts',(-5.91675291062979,0.113367578874178,
19.5562807885477));
#17647=CARTESIAN_POINT('Ctrl Pts',(-5.91674999805254,-0.000151806595337599,
19.5616248077951));
#17648=CARTESIAN_POINT('Origin',(0.,0.,0.));
#17649=CARTESIAN_POINT('',(-5.91674999800917,0.00015348778061909,21.563375191845));
#17650=CARTESIAN_POINT('',(-5.91674999913571,0.000101131768199252,21.3116248077951));
#17651=CARTESIAN_POINT('',(-5.91675,-7.2459289488551E-16,0.));
#17652=CARTESIAN_POINT('Ctrl Pts',(-5.91674999800917,0.00015348778061909,
21.563375191845));
#17653=CARTESIAN_POINT('Ctrl Pts',(-5.91674549259033,0.173831397393708,
21.5551998572909));
#17654=CARTESIAN_POINT('Ctrl Pts',(-5.90908954177321,0.347471023012969,
21.5470245227368));
#17655=CARTESIAN_POINT('Ctrl Pts',(-5.89381820093561,0.520420576860854,
21.5388491881826));
#17656=CARTESIAN_POINT('Ctrl Pts',(-5.88687297008201,0.599076052517767,
21.5351311396899));
#17657=CARTESIAN_POINT('Ctrl Pts',(-5.87835333985223,0.677588845261338,
21.5314130911971));
#17658=CARTESIAN_POINT('Ctrl Pts',(-5.86826625301487,0.755897973424231,
21.5276950427043));
#17659=CARTESIAN_POINT('Ctrl Pts',(-5.84713742478124,0.919927503927489,
21.5199070649428));
#17660=CARTESIAN_POINT('Ctrl Pts',(-5.81912309060505,1.08309992255365,21.5121190871813));
#17661=CARTESIAN_POINT('Ctrl Pts',(-5.78431725188757,1.24483110983611,21.5043311094198));
#17662=CARTESIAN_POINT('Ctrl Pts',(-5.74951825629639,1.40653049938053,21.4965446628415));
#17663=CARTESIAN_POINT('Ctrl Pts',(-5.70793048760599,1.56678891075884,21.4887582162632));
#17664=CARTESIAN_POINT('Ctrl Pts',(-5.65969899232843,1.72503271816409,21.4809717696849));
#17665=CARTESIAN_POINT('Ctrl Pts',(-5.61146565712806,1.88328256221384,21.4731850260712));
#17666=CARTESIAN_POINT('Ctrl Pts',(-5.55658817757557,2.03951734169757,21.4653982824576));
#17667=CARTESIAN_POINT('Ctrl Pts',(-5.49526160139424,2.19317817213787,21.4576115388439));
#17668=CARTESIAN_POINT('Ctrl Pts',(-5.43393908150707,2.34682883906394,21.4498253102651));
#17669=CARTESIAN_POINT('Ctrl Pts',(-5.36616843716412,2.49790560086805,21.4420390816862));
#17670=CARTESIAN_POINT('Ctrl Pts',(-5.29219309060373,2.64586901683853,21.4342528531074));
#17671=CARTESIAN_POINT('Ctrl Pts',(-5.2181982702991,2.79387138364675,21.4264645748319));
#17672=CARTESIAN_POINT('Ctrl Pts',(-5.13799562521156,2.93875848004927,21.4186762965563));
#17673=CARTESIAN_POINT('Ctrl Pts',(-5.05187523504577,3.08001415127126,21.4108880182808));
#17674=CARTESIAN_POINT('Ctrl Pts',(-4.97000049674338,3.21430605464936,21.4034836945845));
#17675=CARTESIAN_POINT('Ctrl Pts',(-4.88277757354901,3.34531573440166,21.3960793708882));
#17676=CARTESIAN_POINT('Ctrl Pts',(-4.79049269186125,3.47262297575247,21.388675047192));
#17677=CARTESIAN_POINT('Ctrl Pts',(-4.69342608108215,3.60652662518631,21.3808870694305));
#17678=CARTESIAN_POINT('Ctrl Pts',(-4.59072429266484,3.73638186680453,21.3730990916689));
#17679=CARTESIAN_POINT('Ctrl Pts',(-4.48274945839955,3.86172084124662,21.3653111139074));
#17680=CARTESIAN_POINT('Ctrl Pts',(-4.37479585291232,3.98703517297184,21.3575246673291));
#17681=CARTESIAN_POINT('Ctrl Pts',(-4.26157147858543,4.10783476726198,21.3497382207507));
#17682=CARTESIAN_POINT('Ctrl Pts',(-4.14347826165807,4.22368541177809,21.3419517741724));
#17683=CARTESIAN_POINT('Ctrl Pts',(-4.02538053974076,4.33954047573507,21.3341650305587));
#17684=CARTESIAN_POINT('Ctrl Pts',(-3.90241382889769,4.45044598554865,21.3263782869449));
#17685=CARTESIAN_POINT('Ctrl Pts',(-3.7750169000562,4.55600460565944,21.3185915433312));
#17686=CARTESIAN_POINT('Ctrl Pts',(-3.64762839756833,4.66155624385736,21.3108053147523));
#17687=CARTESIAN_POINT('Ctrl Pts',(-3.51581050962268,4.76176149626284,21.3030190861734));
#17688=CARTESIAN_POINT('Ctrl Pts',(-3.38003517269896,4.85626325417166,21.2952328575945));
#17689=CARTESIAN_POINT('Ctrl Pts',(-3.24422409340564,4.9507898893287,21.2874445793189));
#17690=CARTESIAN_POINT('Ctrl Pts',(-3.10445374476293,5.03960984555176,21.2796563010433));
#17691=CARTESIAN_POINT('Ctrl Pts',(-2.96122588211857,5.12240879250876,21.2718680227677));
#17692=CARTESIAN_POINT('Ctrl Pts',(-2.82505901444918,5.20112583153527,21.2644636990716));
#17693=CARTESIAN_POINT('Ctrl Pts',(-2.68576755316882,5.27440108883777,21.2570593753754));
#17694=CARTESIAN_POINT('Ctrl Pts',(-2.54380394709372,5.34200262460161,21.2496550516793));
#17695=CARTESIAN_POINT('Ctrl Pts',(-2.3944845153085,5.41310692511313,21.2418670739178));
#17696=CARTESIAN_POINT('Ctrl Pts',(-2.24215525866555,5.4779593629277,21.2340790961562));
#17697=CARTESIAN_POINT('Ctrl Pts',(-2.08735807654392,5.53632249988987,21.2262911183947));
#17698=CARTESIAN_POINT('Ctrl Pts',(-1.93259132887547,5.59467416215894,21.2185046718164));
#17699=CARTESIAN_POINT('Ctrl Pts',(-1.77535792269628,5.64653895661215,21.210718225238));
#17700=CARTESIAN_POINT('Ctrl Pts',(-1.61621859103658,5.69172803535866,21.2029317786597));
#17701=CARTESIAN_POINT('Ctrl Pts',(-1.4570731885701,5.73691883796666,21.195145035046));
#17702=CARTESIAN_POINT('Ctrl Pts',(-1.29602202144189,5.77543332419271,21.1873582914323));
#17703=CARTESIAN_POINT('Ctrl Pts',(-1.13364052047444,5.80713266017218,21.1795715478186));
#17704=CARTESIAN_POINT('Ctrl Pts',(-0.971269759828443,5.83882989947773,
21.1717853192397));
#17705=CARTESIAN_POINT('Ctrl Pts',(-0.807569155105439,5.86371282947817,
21.1639990906608));
#17706=CARTESIAN_POINT('Ctrl Pts',(-0.643124001080646,5.88169381060711,
21.1562128620819));
#17707=CARTESIAN_POINT('Ctrl Pts',(-0.478635557459758,5.89967952516475,
21.1484245838063));
#17708=CARTESIAN_POINT('Ctrl Pts',(-0.313402490543813,5.91075962357427,
21.1406363055308));
#17709=CARTESIAN_POINT('Ctrl Pts',(-0.148015799356357,5.91489829884174,
21.1328480272552));
#17710=CARTESIAN_POINT('Ctrl Pts',(0.00921748805967901,5.91883294142501,
21.1254437035591));
#17711=CARTESIAN_POINT('Ctrl Pts',(0.166589354157765,5.91649407864731,21.118039379863));
#17712=CARTESIAN_POINT('Ctrl Pts',(0.3235915285177,5.90789464066274,21.1106350561669));
#17713=CARTESIAN_POINT('Ctrl Pts',(0.488728750039722,5.89884962392198,21.1028470784053));
#17714=CARTESIAN_POINT('Ctrl Pts',(0.653516024404402,5.88287478973465,21.0950591006438));
#17715=CARTESIAN_POINT('Ctrl Pts',(0.817363912047738,5.8600210577934,21.0872711228823));
#17716=CARTESIAN_POINT('Ctrl Pts',(0.981179585791571,5.83717181909178,21.079484676304));
#17717=CARTESIAN_POINT('Ctrl Pts',(1.14405592503593,5.80744642528962,21.0716982297256));
#17718=CARTESIAN_POINT('Ctrl Pts',(1.30541021291187,5.77094747320796,21.0639117831473));
#17719=CARTESIAN_POINT('Ctrl Pts',(1.46677065609019,5.73444712877356,21.0561250395336));
#17720=CARTESIAN_POINT('Ctrl Pts',(1.62660861917815,5.69117277564768,21.0483382959199));
#17721=CARTESIAN_POINT('Ctrl Pts',(1.78435242077902,5.6412779581368,21.0405515523062));
#17722=CARTESIAN_POINT('Ctrl Pts',(1.94208578880742,5.59138644079485,21.0327653237273));
#17723=CARTESIAN_POINT('Ctrl Pts',(2.09772496787048,5.53487543184463,21.0249790951484));
#17724=CARTESIAN_POINT('Ctrl Pts',(2.25071412109479,5.4719481455515,21.0171928665695));
#17725=CARTESIAN_POINT('Ctrl Pts',(2.40374354816416,5.40900429387628,21.0094045882939));
#17726=CARTESIAN_POINT('Ctrl Pts',(2.55412125895511,5.3396409095845,21.0016163100184));
#17727=CARTESIAN_POINT('Ctrl Pts',(2.70131121884384,5.26410944618825,20.9938280317428));
#17728=CARTESIAN_POINT('Ctrl Pts',(2.84124485619953,5.19230161081806,20.9864237080466));
#17729=CARTESIAN_POINT('Ctrl Pts',(2.97829724309839,5.11491932754957,20.9790193843505));
#17730=CARTESIAN_POINT('Ctrl Pts',(3.11202830920875,5.03221724145365,20.9716150606543));
#17731=CARTESIAN_POINT('Ctrl Pts',(3.25268863304541,4.94522995756689,20.9638270828928));
#17732=CARTESIAN_POINT('Ctrl Pts',(3.38972462737038,4.85232582752308,20.9560391051313));
#17733=CARTESIAN_POINT('Ctrl Pts',(3.52264313999077,4.75383170408629,20.9482511273697));
#17734=CARTESIAN_POINT('Ctrl Pts',(3.65553551969221,4.65535694543846,20.9404646807914));
#17735=CARTESIAN_POINT('Ctrl Pts',(3.78431177635822,4.55129457644037,20.9326782342131));
#17736=CARTESIAN_POINT('Ctrl Pts',(3.90850939645054,4.44201360425178,20.9248917876347));
#17737=CARTESIAN_POINT('Ctrl Pts',(4.03271175440191,4.33272846324059,20.917105044021));
#17738=CARTESIAN_POINT('Ctrl Pts',(4.15233488376581,4.21822452879402,20.9093183004073));
#17739=CARTESIAN_POINT('Ctrl Pts',(4.26695034700485,4.09891025745809,20.9015315567936));
#17740=CARTESIAN_POINT('Ctrl Pts',(4.38155822928846,3.9796038778686,20.8937453282147));
#17741=CARTESIAN_POINT('Ctrl Pts',(4.49115888695785,3.85548802863711,20.8859590996359));
#17742=CARTESIAN_POINT('Ctrl Pts',(4.59536156929568,3.72700719209668,20.878172871057));
#17743=CARTESIAN_POINT('Ctrl Pts',(4.69959168261532,3.59849253343756,20.8703845927814));
#17744=CARTESIAN_POINT('Ctrl Pts',(4.7984207782104,3.46561083850935,20.8625963145059));
#17745=CARTESIAN_POINT('Ctrl Pts',(4.89149858221775,3.32883946483782,20.8548080362303));
#17746=CARTESIAN_POINT('Ctrl Pts',(4.97998774059283,3.19881078748481,20.8474037125341));
#17747=CARTESIAN_POINT('Ctrl Pts',(5.06327886551453,3.06526692567246,20.839999388838));
#17748=CARTESIAN_POINT('Ctrl Pts',(5.14110746711278,2.92864210413243,20.8325950651418));
#17749=CARTESIAN_POINT('Ctrl Pts',(5.2229687475391,2.78493808530632,20.8248070873803));
#17750=CARTESIAN_POINT('Ctrl Pts',(5.29881567895497,2.63777394526328,20.8170191096188));
#17751=CARTESIAN_POINT('Ctrl Pts',(5.36837172927331,2.48767271537859,20.8092311318573));
#17752=CARTESIAN_POINT('Ctrl Pts',(5.43791410427586,2.33760099668251,20.801444685279));
#17753=CARTESIAN_POINT('Ctrl Pts',(5.50116793177215,2.18459363009707,20.7936582387006));
#17754=CARTESIAN_POINT('Ctrl Pts',(5.55790375823388,2.02919599268029,20.7858717921223));
#17755=CARTESIAN_POINT('Ctrl Pts',(5.61464174903946,1.873792427194,20.7780850485086));
#17756=CARTESIAN_POINT('Ctrl Pts',(5.66486112796053,1.7159987072197,20.7702983048949));
#17757=CARTESIAN_POINT('Ctrl Pts',(5.70838124320544,1.55637853516435,20.7625115612812));
#17758=CARTESIAN_POINT('Ctrl Pts',(5.75189847992031,1.39676892078923,20.7547253327023));
#17759=CARTESIAN_POINT('Ctrl Pts',(5.78871725572671,1.23533340443635,20.7469391041234));
#17760=CARTESIAN_POINT('Ctrl Pts',(5.81870725209061,1.07264927957283,20.7391528755446));
#17761=CARTESIAN_POINT('Ctrl Pts',(5.84870514321332,0.90992232869787,20.731364597269));
#17762=CARTESIAN_POINT('Ctrl Pts',(5.8718706029133,0.745946426626859,20.7235763189934));
#17763=CARTESIAN_POINT('Ctrl Pts',(5.8881245874673,0.581308356178614,20.7157880407178));
#17764=CARTESIAN_POINT('Ctrl Pts',(5.90357726631772,0.424786783222787,20.7083837170217));
#17765=CARTESIAN_POINT('Ctrl Pts',(5.91278348682232,0.267667019912706,20.7009793933255));
#17766=CARTESIAN_POINT('Ctrl Pts',(5.91571887703152,0.110456916636793,20.6935750696293));
#17767=CARTESIAN_POINT('Ctrl Pts',(5.91880636410107,-0.0548990076101417,
20.6857870918678));
#17768=CARTESIAN_POINT('Ctrl Pts',(5.9149570277199,-0.220414033300817,20.6779991141062));
#17769=CARTESIAN_POINT('Ctrl Pts',(5.90417843175445,-0.385496573922004,
20.6702111363447));
#17770=CARTESIAN_POINT('Ctrl Pts',(5.89340195495337,-0.550546657900466,
20.6624246897664));
#17771=CARTESIAN_POINT('Ctrl Pts',(5.87569895766807,-0.715164107794478,
20.654638243188));
#17772=CARTESIAN_POINT('Ctrl Pts',(5.85112903471598,-0.878760252630747,
20.6468517966097));
#17773=CARTESIAN_POINT('Ctrl Pts',(5.82655817447672,-1.0423626382911,20.6390650529959));
#17774=CARTESIAN_POINT('Ctrl Pts',(5.79511990793638,-1.20494332435077,20.6312783093822));
#17775=CARTESIAN_POINT('Ctrl Pts',(5.75692544940485,-1.36592091004376,20.6234915657685));
#17776=CARTESIAN_POINT('Ctrl Pts',(5.71873351715102,-1.52688784827371,20.6157053371896));
#17777=CARTESIAN_POINT('Ctrl Pts',(5.67378636104957,-1.68625158740696,20.6079191086107));
#17778=CARTESIAN_POINT('Ctrl Pts',(5.62224589342328,-1.84344288666208,20.6001328800318));
#17779=CARTESIAN_POINT('Ctrl Pts',(5.57069185795404,-2.00067556596206,20.5923446017562));
#17780=CARTESIAN_POINT('Ctrl Pts',(5.51254114050233,-2.15573435817686,20.5845563234806));
#17781=CARTESIAN_POINT('Ctrl Pts',(5.44800521473027,-2.30806623448544,20.576768045205));
#17782=CARTESIAN_POINT('Ctrl Pts',(5.38665084762466,-2.45288829675714,20.569363721509));
#17783=CARTESIAN_POINT('Ctrl Pts',(5.31952577871153,-2.5952455924653,20.5619593978129));
#17784=CARTESIAN_POINT('Ctrl Pts',(5.24685170089538,-2.73468056476643,20.5545550741168));
#17785=CARTESIAN_POINT('Ctrl Pts',(5.17041202522699,-2.88134034194989,20.5467670963553));
#17786=CARTESIAN_POINT('Ctrl Pts',(5.08780568722297,-3.02481937889032,20.5389791185938));
#17787=CARTESIAN_POINT('Ctrl Pts',(4.99932250106465,-3.1646018853639,20.5311911408323));
#17788=CARTESIAN_POINT('Ctrl Pts',(4.9108567114593,-3.30435690939833,20.523404694254));
#17789=CARTESIAN_POINT('Ctrl Pts',(4.81651654994812,-3.44041658324902,20.5156182476756));
#17790=CARTESIAN_POINT('Ctrl Pts',(4.71663611812378,-3.57229258204171,20.5078318010973));
#17791=CARTESIAN_POINT('Ctrl Pts',(4.61675187608618,-3.7041736116064,20.5000450574836));
#17792=CARTESIAN_POINT('Ctrl Pts',(4.5113271305951,-3.83187038964192,20.4922583138699));
#17793=CARTESIAN_POINT('Ctrl Pts',(4.40073782495855,-3.95492568305387,20.4844715702562));
#17794=CARTESIAN_POINT('Ctrl Pts',(4.29015583397724,-4.07797283727874,20.4766853416773));
#17795=CARTESIAN_POINT('Ctrl Pts',(4.17441018013583,-4.19637888361416,20.4688991130985));
#17796=CARTESIAN_POINT('Ctrl Pts',(4.0539154988253,-4.30972153287008,20.4611128845196));
#17797=CARTESIAN_POINT('Ctrl Pts',(3.93338909772275,-4.42309401917127,20.453324606244));
#17798=CARTESIAN_POINT('Ctrl Pts',(3.80811140263233,-4.53140022442251,20.4455363279685));
#17799=CARTESIAN_POINT('Ctrl Pts',(3.67853280348437,-4.63425581686956,20.4377480496929));
#17800=CARTESIAN_POINT('Ctrl Pts',(3.55534230383321,-4.73204072818043,20.4303437259967));
#17801=CARTESIAN_POINT('Ctrl Pts',(3.42826495227513,-4.82489933704216,20.4229394023005));
#17802=CARTESIAN_POINT('Ctrl Pts',(3.29771441188184,-4.91253602736579,20.4155350786043));
#17803=CARTESIAN_POINT('Ctrl Pts',(3.16039941228764,-5.0047136013534,20.4077471008428));
#17804=CARTESIAN_POINT('Ctrl Pts',(3.0191926220945,-5.09114671724739,20.3999591230813));
#17805=CARTESIAN_POINT('Ctrl Pts',(2.874595389023,-5.1715212376928,20.3921711453197));
#17806=CARTESIAN_POINT('Ctrl Pts',(2.73002658500716,-5.25187995581844,20.3843846987414));
#17807=CARTESIAN_POINT('Ctrl Pts',(2.5820689472871,-5.32618230007899,20.3765982521631));
#17808=CARTESIAN_POINT('Ctrl Pts',(2.43124956100348,-5.39415944653292,20.3688118055848));
#17809=CARTESIAN_POINT('Ctrl Pts',(2.28042442130029,-5.46213918616175,20.361025061971));
#17810=CARTESIAN_POINT('Ctrl Pts',(2.12673760427511,-5.52379311024771,20.3532383183573));
#17811=CARTESIAN_POINT('Ctrl Pts',(1.97073804932283,-5.57889972158052,20.3454515747436));
#17812=CARTESIAN_POINT('Ctrl Pts',(1.814748812574,-5.63400268802328,20.3376653461647));
#17813=CARTESIAN_POINT('Ctrl Pts',(1.65644744538103,-5.68255910198523,20.3298791175859));
#17814=CARTESIAN_POINT('Ctrl Pts',(1.49640013214125,-5.72439666751245,20.322092889007));
#17815=CARTESIAN_POINT('Ctrl Pts',(1.33631068702129,-5.76624524662848,20.3143046107314));
#17816=CARTESIAN_POINT('Ctrl Pts',(1.17447468632175,-5.80137136028579,20.3065163324558));
#17817=CARTESIAN_POINT('Ctrl Pts',(1.01147153781069,-5.82965315355029,20.2987280541803));
#17818=CARTESIAN_POINT('Ctrl Pts',(0.856504286722892,-5.85654068178559,
20.2913237304841));
#17819=CARTESIAN_POINT('Ctrl Pts',(0.700482453865207,-5.87724242544195,
20.2839194067879));
#17820=CARTESIAN_POINT('Ctrl Pts',(0.543910735667616,-5.89169684166841,
20.2765150830917));
#17821=CARTESIAN_POINT('Ctrl Pts',(0.379226274338735,-5.906900211584,20.2687271053302));
#17822=CARTESIAN_POINT('Ctrl Pts',(0.213874519460731,-5.91519709526017,
20.2609391275686));
#17823=CARTESIAN_POINT('Ctrl Pts',(0.0484460197901521,-5.9165516600184,
20.2531511498071));
#17824=CARTESIAN_POINT('Ctrl Pts',(-0.116949955219131,-5.91790595845758,
20.2453647032287));
#17825=CARTESIAN_POINT('Ctrl Pts',(-0.282422325571391,-5.9123206587801,
20.2375782566504));
#17826=CARTESIAN_POINT('Ctrl Pts',(-0.447379635199591,-5.89981203298111,
20.2297918100721));
#17827=CARTESIAN_POINT('Ctrl Pts',(-0.612343237577325,-5.88730293000623,
20.2220050664583));
#17828=CARTESIAN_POINT('Ctrl Pts',(-0.776791420991008,-5.86786999264067,
20.2142183228446));
#17829=CARTESIAN_POINT('Ctrl Pts',(-0.940136195178037,-5.8415815064943,
20.2064315792309));
#17830=CARTESIAN_POINT('Ctrl Pts',(-1.10347016533019,-5.81529475913462,
20.198645350652));
#17831=CARTESIAN_POINT('Ctrl Pts',(-1.26570055680538,-5.78215342129273,
20.1908591220731));
#17832=CARTESIAN_POINT('Ctrl Pts',(-1.42624778932565,-5.7422772317212,20.1830728934942));
#17833=CARTESIAN_POINT('Ctrl Pts',(-1.58683728532817,-5.70239054488601,
20.1752846152186));
#17834=CARTESIAN_POINT('Ctrl Pts',(-1.7457424261921,-5.65576553882389,20.167496336943));
#17835=CARTESIAN_POINT('Ctrl Pts',(-1.90239616603626,-5.60257256891426,
20.1597080586674));
#17836=CARTESIAN_POINT('Ctrl Pts',(-2.05132702815484,-5.55200196092769,
20.1523037349713));
#17837=CARTESIAN_POINT('Ctrl Pts',(-2.19822287625689,-5.49549546282115,
20.1448994112753));
#17838=CARTESIAN_POINT('Ctrl Pts',(-2.34261113016698,-5.43324062188652,
20.1374950875792));
#17839=CARTESIAN_POINT('Ctrl Pts',(-2.49448084259927,-5.36776005449806,
20.1297071098177));
#17840=CARTESIAN_POINT('Ctrl Pts',(-2.64363052703416,-5.29589620577876,
20.1219191320562));
#17841=CARTESIAN_POINT('Ctrl Pts',(-2.78952453188628,-5.21790029116163,
20.1141311542947));
#17842=CARTESIAN_POINT('Ctrl Pts',(-2.93538985272581,-5.13991971121024,
20.1063447077164));
#17843=CARTESIAN_POINT('Ctrl Pts',(-3.0780004895258,-5.05580962148474,20.0985582611381));
#17844=CARTESIAN_POINT('Ctrl Pts',(-3.21684493489036,-4.96586741943139,
20.0907718145598));
#17845=CARTESIAN_POINT('Ctrl Pts',(-3.35569467685802,-4.87592178628547,
20.0829850709461));
#17846=CARTESIAN_POINT('Ctrl Pts',(-3.49077766956498,-4.78014376603094,
20.0751983273324));
#17847=CARTESIAN_POINT('Ctrl Pts',(-3.62161034579687,-4.67887476491059,
20.0674115837187));
#17848=CARTESIAN_POINT('Ctrl Pts',(-3.75243436842581,-4.5776124619772,20.0596253551398));
#17849=CARTESIAN_POINT('Ctrl Pts',(-3.87900838450918,-4.470860100671,20.0518391265609));
#17850=CARTESIAN_POINT('Ctrl Pts',(-4.00088083970663,-4.35900023732144,
20.0440528979821));
#17851=CARTESIAN_POINT('Ctrl Pts',(-4.12278537739019,-4.24711092726461,
20.0362646197065));
#17852=CARTESIAN_POINT('Ctrl Pts',(-4.23998564416529,-4.13011164328848,
20.0284763414309));
#17853=CARTESIAN_POINT('Ctrl Pts',(-4.35206531937162,-4.00842338312993,
20.0206880631554));
#17854=CARTESIAN_POINT('Ctrl Pts',(-4.45861957509171,-3.89273423639395,
20.0132837394592));
#17855=CARTESIAN_POINT('Ctrl Pts',(-4.56054577928273,-3.77280749451314,
20.0058794157629));
#17856=CARTESIAN_POINT('Ctrl Pts',(-4.657518781036,-3.64903403201408,19.9984750920667));
#17857=CARTESIAN_POINT('Ctrl Pts',(-4.75951642621038,-3.51884726372052,
19.9906871143052));
#17858=CARTESIAN_POINT('Ctrl Pts',(-4.85607042852624,-3.38435798624226,
19.9828991365437));
#17859=CARTESIAN_POINT('Ctrl Pts',(-4.94683073646605,-3.24604316472452,
19.9751111587822));
#17860=CARTESIAN_POINT('Ctrl Pts',(-5.03757320015121,-3.10775553708648,
19.9673247122038));
#17861=CARTESIAN_POINT('Ctrl Pts',(-5.1225240670765,-2.96564413314225,19.9595382656255));
#17862=CARTESIAN_POINT('Ctrl Pts',(-5.2013765900554,-2.82021490864148,19.9517518190472));
#17863=CARTESIAN_POINT('Ctrl Pts',(-5.28023212108028,-2.67478013634366,
19.9439650754335));
#17864=CARTESIAN_POINT('Ctrl Pts',(-5.35298868686169,-2.52602756924558,
19.9361783318197));
#17865=CARTESIAN_POINT('Ctrl Pts',(-5.41938513716345,-2.37448842860771,
19.928391588206));
#17866=CARTESIAN_POINT('Ctrl Pts',(-5.48577719583674,-2.22295931115032,
19.9206053596272));
#17867=CARTESIAN_POINT('Ctrl Pts',(-5.54580985271459,-2.0686442817455,19.9128191310483));
#17868=CARTESIAN_POINT('Ctrl Pts',(-5.59926976194931,-1.91209536776284,
19.9050329024694));
#17869=CARTESIAN_POINT('Ctrl Pts',(-5.6527437443131,-1.75550524284093,19.8972446241938));
#17870=CARTESIAN_POINT('Ctrl Pts',(-5.69964141643763,-1.59668036024238,
19.8894563459182));
#17871=CARTESIAN_POINT('Ctrl Pts',(-5.73979876816339,-1.43618963354078,
19.8816680676427));
#17872=CARTESIAN_POINT('Ctrl Pts',(-5.77797640132398,-1.28361094430023,
19.8742637439465));
#17873=CARTESIAN_POINT('Ctrl Pts',(-5.81006222379734,-1.12952695903671,
19.8668594202504));
#17874=CARTESIAN_POINT('Ctrl Pts',(-5.83595785313665,-0.974436503273903,
19.8594550965542));
#17875=CARTESIAN_POINT('Ctrl Pts',(-5.86416048920803,-0.805529247740106,
19.8513911316348));
#17876=CARTESIAN_POINT('Ctrl Pts',(-5.88502802230486,-0.635384442677772,
19.8433271667155));
#17877=CARTESIAN_POINT('Ctrl Pts',(-5.89847849780617,-0.464631007809766,
19.8352632017961));
#17878=CARTESIAN_POINT('Ctrl Pts',(-5.91064803389095,-0.310139065348279,
19.8279671986129));
#17879=CARTESIAN_POINT('Ctrl Pts',(-5.91674657153479,-0.155149150800852,
19.8206711954297));
#17880=CARTESIAN_POINT('Ctrl Pts',(-5.91674999855416,-0.000130802689547563,
19.8133751922466));
#17881=CARTESIAN_POINT('Ctrl Pts',(-5.91680020033354,-0.000151807883381276,
19.5616248077951));
#17882=CARTESIAN_POINT('Ctrl Pts',(-5.9170183524464,-0.211270559939811,
19.5715633135977));
#17883=CARTESIAN_POINT('Ctrl Pts',(-5.85430236710503,-1.40611676514098,
19.6278172811617));
#17884=CARTESIAN_POINT('Ctrl Pts',(-5.0698198637438,-3.51270083870888,19.7303867104881));
#17885=CARTESIAN_POINT('Ctrl Pts',(-2.77132459642368,-5.51016339270765,
19.8693330957729));
#17886=CARTESIAN_POINT('Ctrl Pts',(0.202693088224149,-6.1644996670503,20.0082794810581));
#17887=CARTESIAN_POINT('Ctrl Pts',(3.12730345151057,-5.31621235046608,20.1472258663432));
#17888=CARTESIAN_POINT('Ctrl Pts',(5.28962000410132,-3.17207516387753,20.2861722516285));
#17889=CARTESIAN_POINT('Ctrl Pts',(6.16256868671121,-0.254730867081438,
20.4251186369135));
#17890=CARTESIAN_POINT('Ctrl Pts',(5.53336446324569,2.7247051858812,20.5640650221986));
#17891=CARTESIAN_POINT('Ctrl Pts',(3.55537859832565,5.03998250548997,20.7030114074838));
#17892=CARTESIAN_POINT('Ctrl Pts',(0.710753744830798,6.1267421805791,20.8419577927689));
#17893=CARTESIAN_POINT('Ctrl Pts',(-2.30712042361359,5.7200818162001,20.980904178054));
#17894=CARTESIAN_POINT('Ctrl Pts',(-4.76262395974796,3.91912664392358,21.1198505633391));
#17895=CARTESIAN_POINT('Ctrl Pts',(-5.78975558509219,1.73230762618957,21.230090769941));
#17896=CARTESIAN_POINT('Ctrl Pts',(-5.91658562683898,0.374246943367566,
21.2940155147812));
#17897=CARTESIAN_POINT('Ctrl Pts',(-5.91635768454612,0.000101336159654947,
21.3116247978597));
#17898=CARTESIAN_POINT('Origin',(0.,0.,0.));
#17899=CARTESIAN_POINT('',(-5.91674999852046,-0.000132318339550427,23.3133751922049));
#17900=CARTESIAN_POINT('',(-5.91679629007161,-2.60102882507938E-5,23.0616248077951));
#17901=CARTESIAN_POINT('',(-5.91675,-7.2459289488551E-16,0.));
#17902=CARTESIAN_POINT('Ctrl Pts',(-5.91698239427519,-0.000132148689059992,
23.3133751839731));
#17903=CARTESIAN_POINT('Ctrl Pts',(-5.91617566770858,0.831368591535416,
23.274228452267));
#17904=CARTESIAN_POINT('Ctrl Pts',(-5.52980190076119,2.64788537604627,23.1887417220566));
#17905=CARTESIAN_POINT('Ctrl Pts',(-3.73287084581987,4.9103129984913,23.0569149933421));
#17906=CARTESIAN_POINT('Ctrl Pts',(-0.927040587802708,6.0980401969232,22.9178949978296));
#17907=CARTESIAN_POINT('Ctrl Pts',(2.10499434029924,5.79780107644536,22.7788750023171));
#17908=CARTESIAN_POINT('Ctrl Pts',(4.62339528457857,4.08285617396229,22.6398550068045));
#17909=CARTESIAN_POINT('Ctrl Pts',(6.01365403229901,1.37166456341826,22.5008350112921));
#17910=CARTESIAN_POINT('Ctrl Pts',(5.9365373012305,-1.67422321266426,22.3618150157795));
#17911=CARTESIAN_POINT('Ctrl Pts',(4.41086213664457,-4.31158830435354,22.222795020267));
#17912=CARTESIAN_POINT('Ctrl Pts',(1.80890441491952,-5.89689437860388,22.0837750247545));
#17913=CARTESIAN_POINT('Ctrl Pts',(-1.2344391876144,-6.04331518181912,21.9447550292419));
#17914=CARTESIAN_POINT('Ctrl Pts',(-3.97657061794283,-4.71512296925953,
21.8057350337294));
#17915=CARTESIAN_POINT('Ctrl Pts',(-5.59680782494173,-2.44846451161869,
21.6786084213838));
#17916=CARTESIAN_POINT('Ctrl Pts',(-5.9159378649533,-0.731625187597263,
21.5978218075423));
#17917=CARTESIAN_POINT('Ctrl Pts',(-5.91666999553354,0.000153478058687734,
21.5633751922049));
#17918=CARTESIAN_POINT('Ctrl Pts',(-5.91674999913571,0.000101131768199252,
21.3116248077951));
#17919=CARTESIAN_POINT('Ctrl Pts',(-5.91675283436531,-0.165774982607078,
21.3194313027863));
#17920=CARTESIAN_POINT('Ctrl Pts',(-5.90977581898218,-0.331653191667966,
21.3272377977775));
#17921=CARTESIAN_POINT('Ctrl Pts',(-5.89584447824603,-0.496939081614436,
21.3350442927687));
#17922=CARTESIAN_POINT('Ctrl Pts',(-5.88191337714267,-0.662222128480592,
21.3428506534805));
#17923=CARTESIAN_POINT('Ctrl Pts',(-5.86102821913857,-0.826912561854687,
21.3506570141923));
#17924=CARTESIAN_POINT('Ctrl Pts',(-5.83326645319524,-0.990420642215763,
21.3584633749042));
#17925=CARTESIAN_POINT('Ctrl Pts',(-5.80549747038832,-1.15397122763628,
21.3662717649336));
#17926=CARTESIAN_POINT('Ctrl Pts',(-5.77084836046043,-1.31633853411121,
21.374080154963));
#17927=CARTESIAN_POINT('Ctrl Pts',(-5.72944794534782,-1.47694170638169,
21.3818885449924));
#17928=CARTESIAN_POINT('Ctrl Pts',(-5.70142702425242,-1.58564227872186,
21.3871734746314));
#17929=CARTESIAN_POINT('Ctrl Pts',(-5.67031442946143,-1.69353490763636,
21.3924584042704));
#17930=CARTESIAN_POINT('Ctrl Pts',(-5.63616319163506,-1.80044301208289,
21.3977433339094));
#17931=CARTESIAN_POINT('Ctrl Pts',(-5.58583638265805,-1.95798763104894,
21.4055314453024));
#17932=CARTESIAN_POINT('Ctrl Pts',(-5.52889081211639,-2.11344891743199,
21.4133195566954));
#17933=CARTESIAN_POINT('Ctrl Pts',(-5.46552416448239,-2.26626921833198,
21.4211076680883));
#17934=CARTESIAN_POINT('Ctrl Pts',(-5.40216995778514,-2.41905951562963,
21.4288942504214));
#17935=CARTESIAN_POINT('Ctrl Pts',(-5.33239731171228,-2.56920956705058,
21.4366808327544));
#17936=CARTESIAN_POINT('Ctrl Pts',(-5.2564522307488,-2.71618123628671,21.4444674150875));
#17937=CARTESIAN_POINT('Ctrl Pts',(-5.18050425401615,-2.86315850952013,
21.4522542943212));
#17938=CARTESIAN_POINT('Ctrl Pts',(-5.09838351462145,-3.00695687239445,
21.4600411735549));
#17939=CARTESIAN_POINT('Ctrl Pts',(-5.01038254501075,-3.14706169547908,
21.4678280527886));
#17940=CARTESIAN_POINT('Ctrl Pts',(-4.9223873834131,-3.28715727172648,21.4756144180927));
#17941=CARTESIAN_POINT('Ctrl Pts',(-4.82851293829791,-3.42355952546908,
21.4834007833969));
#17942=CARTESIAN_POINT('Ctrl Pts',(-4.72909582324789,-3.55578166610935,
21.4911871487011));
#17943=CARTESIAN_POINT('Ctrl Pts',(-4.62965260328237,-3.68803852559864,
21.4989755585467));
#17944=CARTESIAN_POINT('Ctrl Pts',(-4.52466399580566,-3.81611282200139,
21.5067639683923));
#17945=CARTESIAN_POINT('Ctrl Pts',(-4.41450831381967,-3.9395490744141,21.5145523782378));
#17946=CARTESIAN_POINT('Ctrl Pts',(-4.3101415286957,-4.0564985099748,21.5219314918901));
#17947=CARTESIAN_POINT('Ctrl Pts',(-4.20113695372893,-4.16928464594976,
21.5293106055423));
#17948=CARTESIAN_POINT('Ctrl Pts',(-4.08784812513602,-4.27754932973565,
21.5366897191945));
#17949=CARTESIAN_POINT('Ctrl Pts',(-3.96828010406435,-4.3918147357162,21.5444778305874));
#17950=CARTESIAN_POINT('Ctrl Pts',(-3.8438967371534,-4.5010840708657,21.5522659419804));
#17951=CARTESIAN_POINT('Ctrl Pts',(-3.71513841646305,-4.60496222666597,
21.5600540533733));
#17952=CARTESIAN_POINT('Ctrl Pts',(-3.58640537522402,-4.70881998780151,
21.5678406357064));
#17953=CARTESIAN_POINT('Ctrl Pts',(-3.45329934259107,-4.80728848102971,
21.5756272180395));
#17954=CARTESIAN_POINT('Ctrl Pts',(-3.31629380410436,-4.90001285379528,
21.5834138003725));
#17955=CARTESIAN_POINT('Ctrl Pts',(-3.17928304162731,-4.99274076212033,
21.5912006796062));
#17956=CARTESIAN_POINT('Ctrl Pts',(-3.03837273817019,-5.0797239293635,21.5989875588399));
#17957=CARTESIAN_POINT('Ctrl Pts',(-2.89406599001871,-5.16065040551257,
21.6067744380736));
#17958=CARTESIAN_POINT('Ctrl Pts',(-2.74976876602898,-5.24157154056111,
21.6145608033778));
#17959=CARTESIAN_POINT('Ctrl Pts',(-2.60207582470565,-5.31643662825231,
21.622347168682));
#17960=CARTESIAN_POINT('Ctrl Pts',(-2.45151565190734,-5.38497925445896,
21.6301335339862));
#17961=CARTESIAN_POINT('Ctrl Pts',(-2.30091594506516,-5.45353987856731,
21.6379219438318));
#17962=CARTESIAN_POINT('Ctrl Pts',(-2.14744779254099,-5.5157745896197,21.6457103536774));
#17963=CARTESIAN_POINT('Ctrl Pts',(-1.99166131774356,-5.57146441771856,
21.653498763523));
#17964=CARTESIAN_POINT('Ctrl Pts',(-1.84406172735252,-5.62422763626515,
21.6608778771752));
#17965=CARTESIAN_POINT('Ctrl Pts',(-1.69438145717131,-5.6711160842054,21.6682569908274));
#17966=CARTESIAN_POINT('Ctrl Pts',(-1.543102308257,-5.71198440375601,21.6756361044796));
#17967=CARTESIAN_POINT('Ctrl Pts',(-1.38343829998868,-5.75511790733183,
21.6834242158726));
#17968=CARTESIAN_POINT('Ctrl Pts',(-1.22193612308707,-5.79156041581149,
21.6912123272656));
#17969=CARTESIAN_POINT('Ctrl Pts',(-1.05917152972064,-5.82117567447756,
21.6990004386586));
#17970=CARTESIAN_POINT('Ctrl Pts',(-0.896438892344492,-5.8507851187039,
21.7067870209916));
#17971=CARTESIAN_POINT('Ctrl Pts',(-0.732444647217814,-5.87356993047183,
21.7145736033247));
#17972=CARTESIAN_POINT('Ctrl Pts',(-0.567774346777329,-5.8894450378318,
21.7223601856578));
#17973=CARTESIAN_POINT('Ctrl Pts',(-0.403097767495121,-5.90532075050606,
21.7301470648915));
#17974=CARTESIAN_POINT('Ctrl Pts',(-0.23774539898002,-5.91428619698674,
21.7379339441252));
#17975=CARTESIAN_POINT('Ctrl Pts',(-0.0723082694507838,-5.91630814585152,
21.745720823359));
#17976=CARTESIAN_POINT('Ctrl Pts',(0.0931179413234977,-5.91832996126884,
21.7535071886632));
#17977=CARTESIAN_POINT('Ctrl Pts',(0.258628582386181,-5.91340919234525,
21.7612935539674));
#17978=CARTESIAN_POINT('Ctrl Pts',(0.423632116328124,-5.9015647410255,21.7690799192715));
#17979=CARTESIAN_POINT('Ctrl Pts',(0.588678976847425,-5.88971717959335,
21.7768683291171));
#17980=CARTESIAN_POINT('Ctrl Pts',(0.75321814511539,-5.87094232394192,21.7846567389628));
#17981=CARTESIAN_POINT('Ctrl Pts',(0.916661782288731,-5.84531109004399,
21.7924451488084));
#17982=CARTESIAN_POINT('Ctrl Pts',(1.07151613617246,-5.82102682769429,21.7998242624605));
#17983=CARTESIAN_POINT('Ctrl Pts',(1.2253868850502,-5.79058832459067,21.8072033761127));
#17984=CARTESIAN_POINT('Ctrl Pts',(1.37778140412653,-5.75409844936139,21.8145824897648));
#17985=CARTESIAN_POINT('Ctrl Pts',(1.53862260351614,-5.71558607153424,21.8223706011578));
#17986=CARTESIAN_POINT('Ctrl Pts',(1.69787673273818,-5.67031873348632,21.8301587125507));
#17987=CARTESIAN_POINT('Ctrl Pts',(1.85497302160941,-5.61845224698059,21.8379468239437));
#17988=CARTESIAN_POINT('Ctrl Pts',(2.01203846736361,-5.56659594355509,21.8457334062768));
#17989=CARTESIAN_POINT('Ctrl Pts',(2.16694661485152,-5.50814317694852,21.8535199886099));
#17990=CARTESIAN_POINT('Ctrl Pts',(2.31914257569174,-5.44329939247456,21.861306570943));
#17991=CARTESIAN_POINT('Ctrl Pts',(2.47134433972939,-5.37845313552182,21.8690934501767));
#17992=CARTESIAN_POINT('Ctrl Pts',(2.62083341468959,-5.30721549468745,21.8768803294104));
#17993=CARTESIAN_POINT('Ctrl Pts',(2.76707490611802,-5.22984005744267,21.8846672086441));
#17994=CARTESIAN_POINT('Ctrl Pts',(2.9133067456928,-5.15246972693189,21.8924535739483));
#17995=CARTESIAN_POINT('Ctrl Pts',(3.05629114826095,-5.06896256020916,21.9002399392525));
#17996=CARTESIAN_POINT('Ctrl Pts',(3.1955177146777,-4.97961816785996,21.9080263045567));
#17997=CARTESIAN_POINT('Ctrl Pts',(3.33478083916337,-4.89025031548775,21.9158147144023));
#17998=CARTESIAN_POINT('Ctrl Pts',(3.47028388565757,-4.79504234581187,21.9236031242479));
#17999=CARTESIAN_POINT('Ctrl Pts',(3.60154458815585,-4.69433777459881,21.9313915340935));
#18000=CARTESIAN_POINT('Ctrl Pts',(3.72590728362201,-4.59892542586494,21.9387706477456));
#18001=CARTESIAN_POINT('Ctrl Pts',(3.84646184728199,-4.49857948916574,21.9461497613978));
#18002=CARTESIAN_POINT('Ctrl Pts',(3.96282491003736,-4.39362598486574,21.9535288750499));
#18003=CARTESIAN_POINT('Ctrl Pts',(4.08563755902043,-4.28285528514432,21.9613169864429));
#18004=CARTESIAN_POINT('Ctrl Pts',(4.20382475428739,-4.16691221099511,21.9691050978358));
#18005=CARTESIAN_POINT('Ctrl Pts',(4.31695983535354,-4.04620666086698,21.9768932092288));
#18006=CARTESIAN_POINT('Ctrl Pts',(4.43007270431869,-3.92552480916948,21.9846797915619));
#18007=CARTESIAN_POINT('Ctrl Pts',(4.53813521983098,-3.80008258014354,21.9924663738949));
#18008=CARTESIAN_POINT('Ctrl Pts',(4.64075841401936,-3.67032585817778,22.000252956228));
#18009=CARTESIAN_POINT('Ctrl Pts',(4.74338552120726,-3.54056418861716,22.0080398354617));
#18010=CARTESIAN_POINT('Ctrl Pts',(4.84057269076204,-3.40648794509135,22.0158267146954));
#18011=CARTESIAN_POINT('Ctrl Pts',(4.93197154484231,-3.26857572091665,22.0236135939291));
#18012=CARTESIAN_POINT('Ctrl Pts',(5.023364366651,-3.13067259886908,22.0313999592333));
#18013=CARTESIAN_POINT('Ctrl Pts',(5.10896946104505,-2.98893426924202,22.0391863245374));
#18014=CARTESIAN_POINT('Ctrl Pts',(5.1884819791543,-2.84386801987909,22.0469726898416));
#18015=CARTESIAN_POINT('Ctrl Pts',(5.26801537563628,-2.69876367906471,22.0547610996872));
#18016=CARTESIAN_POINT('Ctrl Pts',(5.34145284374213,-2.55032995184205,22.0625495095328));
#18017=CARTESIAN_POINT('Ctrl Pts',(5.40853524474125,-2.39909922030992,22.0703379193784));
#18018=CARTESIAN_POINT('Ctrl Pts',(5.47209233416618,-2.25581595995212,22.0777170330306));
#18019=CARTESIAN_POINT('Ctrl Pts',(5.52994501366636,-2.11002234793038,22.0850961466828));
#18020=CARTESIAN_POINT('Ctrl Pts',(5.58191261772456,-1.96218808746443,22.092475260335));
#18021=CARTESIAN_POINT('Ctrl Pts',(5.63676059924473,-1.80615990542622,22.100263371728));
#18022=CARTESIAN_POINT('Ctrl Pts',(5.68507221795039,-1.64780272350431,22.1080514831209));
#18023=CARTESIAN_POINT('Ctrl Pts',(5.72666892340327,-1.48768061230469,22.1158395945139));
#18024=CARTESIAN_POINT('Ctrl Pts',(5.7682574620681,-1.32758993829054,22.1236261768469));
#18025=CARTESIAN_POINT('Ctrl Pts',(5.8031336377015,-1.16573533546769,22.13141275918));
#18026=CARTESIAN_POINT('Ctrl Pts',(5.83116921555223,-1.00269444104172,22.139199341513));
#18027=CARTESIAN_POINT('Ctrl Pts',(5.85920586239332,-0.839647329902619,
22.1469862207467));
#18028=CARTESIAN_POINT('Ctrl Pts',(5.88040133149115,-0.675414150874227,
22.1547730999804));
#18029=CARTESIAN_POINT('Ctrl Pts',(5.89467868023039,-0.510581843916649,
22.1625599792141));
#18030=CARTESIAN_POINT('Ctrl Pts',(5.9089550866729,-0.345760415795667,22.1703463445183));
#18031=CARTESIAN_POINT('Ctrl Pts',(5.91631425900929,-0.180340257246796,
22.1781327098225));
#18032=CARTESIAN_POINT('Ctrl Pts',(5.91673120688126,-0.0149126797547105,
22.1859190751267));
#18033=CARTESIAN_POINT('Ctrl Pts',(5.91714826423527,0.150558335659481,22.1937074849723));
#18034=CARTESIAN_POINT('Ctrl Pts',(5.91061945186923,0.316036454176732,22.2014958948179));
#18035=CARTESIAN_POINT('Ctrl Pts',(5.8971719245184,0.480930197816694,22.2092843046635));
#18036=CARTESIAN_POINT('Ctrl Pts',(5.88443109107096,0.637158452233363,22.2166634183157));
#18037=CARTESIAN_POINT('Ctrl Pts',(5.86548004429649,0.792861912881908,22.2240425319679));
#18038=CARTESIAN_POINT('Ctrl Pts',(5.84038486026414,0.947541685889016,22.2314216456201));
#18039=CARTESIAN_POINT('Ctrl Pts',(5.81389874040172,1.11079480261757,22.2392097570131));
#18040=CARTESIAN_POINT('Ctrl Pts',(5.78055861547604,1.27296584083992,22.246997868406));
#18041=CARTESIAN_POINT('Ctrl Pts',(5.74047756754068,1.43347405245517,22.254785979799));
#18042=CARTESIAN_POINT('Ctrl Pts',(5.70040438882025,1.59395075108161,22.2625725621321));
#18043=CARTESIAN_POINT('Ctrl Pts',(5.65359300515733,1.75276496468208,22.2703591444652));
#18044=CARTESIAN_POINT('Ctrl Pts',(5.60020717269849,1.90934810481389,22.2781457267983));
#18045=CARTESIAN_POINT('Ctrl Pts',(5.54681930464972,2.06593721542604,22.285932606032));
#18046=CARTESIAN_POINT('Ctrl Pts',(5.48685658556098,2.2202947786477,22.2937194852657));
#18047=CARTESIAN_POINT('Ctrl Pts',(5.42053226314005,2.37186857704169,22.3015063644995));
#18048=CARTESIAN_POINT('Ctrl Pts',(5.35421231808629,2.52343237165208,22.3092927298036));
#18049=CARTESIAN_POINT('Ctrl Pts',(5.28153173811755,2.67221247639429,22.3170790951078));
#18050=CARTESIAN_POINT('Ctrl Pts',(5.2027514828959,2.81767769088739,22.324865460412));
#18051=CARTESIAN_POINT('Ctrl Pts',(5.12395054157881,2.96318110159224,22.3326538702576));
#18052=CARTESIAN_POINT('Ctrl Pts',(5.03904687513562,3.10536760068265,22.3404422801032));
#18053=CARTESIAN_POINT('Ctrl Pts',(4.94834731268275,3.24373078962564,22.3482306899489));
#18054=CARTESIAN_POINT('Ctrl Pts',(4.86241418990062,3.37482272196152,22.355609803601));
#18055=CARTESIAN_POINT('Ctrl Pts',(4.77127881688351,3.50248263585952,22.3629889172532));
#18056=CARTESIAN_POINT('Ctrl Pts',(4.6752379049579,3.62630405434306,22.3703680309053));
#18057=CARTESIAN_POINT('Ctrl Pts',(4.57387379056434,3.75698844889836,22.3781561422983));
#18058=CARTESIAN_POINT('Ctrl Pts',(4.46700872238724,3.88344344789723,22.3859442536913));
#18059=CARTESIAN_POINT('Ctrl Pts',(4.35501985072996,4.00521318561796,22.3937323650843));
#18060=CARTESIAN_POINT('Ctrl Pts',(4.24305296613534,4.12695901597349,22.4015189474173));
#18061=CARTESIAN_POINT('Ctrl Pts',(4.12596450143291,4.2440211854203,22.4093055297504));
#18062=CARTESIAN_POINT('Ctrl Pts',(4.00417028739454,4.35597875018311,22.4170921120835));
#18063=CARTESIAN_POINT('Ctrl Pts',(3.88237142937008,4.46794058386276,22.4248789913172));
#18064=CARTESIAN_POINT('Ctrl Pts',(3.75586669553092,4.57479720424914,22.4326658705509));
#18065=CARTESIAN_POINT('Ctrl Pts',(3.62510754385212,4.67616572182878,22.4404527497846));
#18066=CARTESIAN_POINT('Ctrl Pts',(3.49435702220181,4.7775275491448,22.4482391150888));
#18067=CARTESIAN_POINT('Ctrl Pts',(3.35935289723786,4.87340180280263,22.456025480393));
#18068=CARTESIAN_POINT('Ctrl Pts',(3.22057846859065,4.96344687592708,22.4638118456971));
#18069=CARTESIAN_POINT('Ctrl Pts',(3.08176760059654,5.05351559305921,22.4716002555427));
#18070=CARTESIAN_POINT('Ctrl Pts',(2.93918471784839,5.13775189548406,22.4793886653883));
#18071=CARTESIAN_POINT('Ctrl Pts',(2.79334153291282,5.21585790095975,22.4871770752339));
#18072=CARTESIAN_POINT('Ctrl Pts',(2.65516269302536,5.28985928285252,22.4945561888861));
#18073=CARTESIAN_POINT('Ctrl Pts',(2.51405763710387,5.35835799105085,22.5019353025382));
#18074=CARTESIAN_POINT('Ctrl Pts',(2.37048138705646,5.4211390460049,22.5093144161904));
#18075=CARTESIAN_POINT('Ctrl Pts',(2.21894722164553,5.48739982912841,22.5171025275834));
#18076=CARTESIAN_POINT('Ctrl Pts',(2.06460603512822,5.54731483319738,22.5248906389763));
#18077=CARTESIAN_POINT('Ctrl Pts',(1.90800711403173,5.60066419412058,22.5326787503693));
#18078=CARTESIAN_POINT('Ctrl Pts',(1.75143893840424,5.65400308082652,22.5404653327023));
#18079=CARTESIAN_POINT('Ctrl Pts',(1.59261421491847,5.70077879344744,22.5482519150353));
#18080=CARTESIAN_POINT('Ctrl Pts',(1.43209948841326,5.7408206397506,22.5560384973683));
#18081=CARTESIAN_POINT('Ctrl Pts',(1.2715786415162,5.78086401284071,22.563825376602));
#18082=CARTESIAN_POINT('Ctrl Pts',(1.10936797171594,5.81417292466735,22.5716122558357));
#18083=CARTESIAN_POINT('Ctrl Pts',(0.94604710241093,5.8406271446241,22.5793991350695));
#18084=CARTESIAN_POINT('Ctrl Pts',(0.782737012188957,5.86707961861761,22.5871855003736));
#18085=CARTESIAN_POINT('Ctrl Pts',(0.618317184552772,5.8866782550966,22.5949718656778));
#18086=CARTESIAN_POINT('Ctrl Pts',(0.453375452715306,5.89935430885238,22.602758230982));
#18087=CARTESIAN_POINT('Ctrl Pts',(0.288390410528627,5.91203369108247,22.6105466408276));
#18088=CARTESIAN_POINT('Ctrl Pts',(0.122883508953181,5.91778683195085,22.6183350506732));
#18089=CARTESIAN_POINT('Ctrl Pts',(-0.0425533881567151,5.91659697559808,
22.6261234605188));
#18090=CARTESIAN_POINT('Ctrl Pts',(-0.199296252265106,5.91546964852735,
22.633502574171));
#18091=CARTESIAN_POINT('Ctrl Pts',(-0.355976020328041,5.90811029313864,
22.6408816878233));
#18092=CARTESIAN_POINT('Ctrl Pts',(-0.512090273423788,5.89454782950862,
22.6482608014755));
#18093=CARTESIAN_POINT('Ctrl Pts',(-0.676857378314673,5.88023364727865,
22.6560489128685));
#18094=CARTESIAN_POINT('Ctrl Pts',(-0.841053348037998,5.85900411372562,
22.6638370242614));
#18095=CARTESIAN_POINT('Ctrl Pts',(-1.00409065082147,5.83092895921678,22.6716251356544));
#18096=CARTESIAN_POINT('Ctrl Pts',(-1.16709594407423,5.80285931677485,22.6794117179876));
#18097=CARTESIAN_POINT('Ctrl Pts',(-1.32894270958611,5.76794678928466,22.6871983003207));
#18098=CARTESIAN_POINT('Ctrl Pts',(-1.4890517862185,5.72631254302972,22.6949848826538));
#18099=CARTESIAN_POINT('Ctrl Pts',(-1.64916696777306,5.68467670927057,22.7027717618876));
#18100=CARTESIAN_POINT('Ctrl Pts',(-1.807544017641,5.63631872048542,22.7105586411213));
#18101=CARTESIAN_POINT('Ctrl Pts',(-1.96361643272343,5.58141031170783,22.718345520355));
#18102=CARTESIAN_POINT('Ctrl Pts',(-2.11967854711662,5.5265055268535,22.7261318856592));
#18103=CARTESIAN_POINT('Ctrl Pts',(-2.27343602970581,5.4650512933161,22.7339182509634));
#18104=CARTESIAN_POINT('Ctrl Pts',(-2.42433980059651,5.39726848449692,22.7417046162676));
#18105=CARTESIAN_POINT('Ctrl Pts',(-2.57528319575281,5.32946787728872,22.7494930261132));
#18106=CARTESIAN_POINT('Ctrl Pts',(-2.72337108943805,5.25533550350466,22.7572814359588));
#18107=CARTESIAN_POINT('Ctrl Pts',(-2.86807573589755,5.17513981798132,22.7650698458044));
#18108=CARTESIAN_POINT('Ctrl Pts',(-3.00517586973449,5.09915857282157,22.7724489594565));
#18109=CARTESIAN_POINT('Ctrl Pts',(-3.1392389753819,5.0177350287138,22.7798280731085));
#18110=CARTESIAN_POINT('Ctrl Pts',(-3.26983770370068,4.93113495596678,22.7872071867606));
#18111=CARTESIAN_POINT('Ctrl Pts',(-3.40767505001123,4.8397349525256,22.7949952981536));
#18112=CARTESIAN_POINT('Ctrl Pts',(-3.54170232156009,4.74253567243889,22.8027834095466));
#18113=CARTESIAN_POINT('Ctrl Pts',(-3.6714369547534,4.63987944345228,22.8105715209395));
#18114=CARTESIAN_POINT('Ctrl Pts',(-3.801146116813,4.53724336922675,22.8183581032726));
#18115=CARTESIAN_POINT('Ctrl Pts',(-3.92656407170557,4.42915268196657,22.8261446856056));
#18116=CARTESIAN_POINT('Ctrl Pts',(-4.04724021503789,4.3159908716632,22.8339312679387));
#18117=CARTESIAN_POINT('Ctrl Pts',(-4.16792095972478,4.20282474652511,22.8417181471724));
#18118=CARTESIAN_POINT('Ctrl Pts',(-4.28385929528953,4.0845873271073,22.8495050264061));
#18119=CARTESIAN_POINT('Ctrl Pts',(-4.39463992652577,3.96170045292241,22.8572919056399));
#18120=CARTESIAN_POINT('Ctrl Pts',(-4.50541324630485,3.83882168919966,22.8650782709441));
#18121=CARTESIAN_POINT('Ctrl Pts',(-4.61102932908215,3.71129432221224,22.8728646362483));
#18122=CARTESIAN_POINT('Ctrl Pts',(-4.71111168889278,3.57957500511971,22.8806510015525));
#18123=CARTESIAN_POINT('Ctrl Pts',(-4.81122032829831,3.44782110120989,22.8884394113981));
#18124=CARTESIAN_POINT('Ctrl Pts',(-4.90579214626941,3.31187330113712,22.8962278212437));
#18125=CARTESIAN_POINT('Ctrl Pts',(-4.99449215547285,3.17221983340061,22.9040162310893));
#18126=CARTESIAN_POINT('Ctrl Pts',(-5.0785308054458,3.03990542894886,22.9113953447415));
#18127=CARTESIAN_POINT('Ctrl Pts',(-5.1572987839082,2.90426503894494,22.9187744583936));
#18128=CARTESIAN_POINT('Ctrl Pts',(-5.23054797971386,2.7657365012617,22.9261535720458));
#18129=CARTESIAN_POINT('Ctrl Pts',(-5.30777049503581,2.61969364022941,22.9339329573455));
#18130=CARTESIAN_POINT('Ctrl Pts',(-5.37888704971622,2.47038729732537,22.9417123426452));
#18131=CARTESIAN_POINT('Ctrl Pts',(-5.44363799286681,2.3183476799473,22.949491727945));
#18132=CARTESIAN_POINT('Ctrl Pts',(-5.50837596849685,2.16633851118923,22.9572695552853));
#18133=CARTESIAN_POINT('Ctrl Pts',(-5.56675075047658,2.01159745524634,22.9650473826256));
#18134=CARTESIAN_POINT('Ctrl Pts',(-5.6185504355893,1.85467559568763,22.972825209966));
#18135=CARTESIAN_POINT('Ctrl Pts',(-5.67035169468284,1.69774896791468,22.9806032736427));
#18136=CARTESIAN_POINT('Ctrl Pts',(-5.71557735280554,1.53864170748293,22.9883813373194));
#18137=CARTESIAN_POINT('Ctrl Pts',(-5.75406486082589,1.37792167408336,22.9961594009962));
#18138=CARTESIAN_POINT('Ctrl Pts',(-5.79255008650999,1.21721117149464,23.0039370034283));
#18139=CARTESIAN_POINT('Ctrl Pts',(-5.82429788733408,1.05488839958225,23.0117146058604));
#18140=CARTESIAN_POINT('Ctrl Pts',(-5.84919644761066,0.891533218539163,
23.0194922082925));
#18141=CARTESIAN_POINT('Ctrl Pts',(-5.8741012472323,0.728137102223913,23.0272717597186));
#18142=CARTESIAN_POINT('Ctrl Pts',(-5.89215332718016,0.563708377132532,
23.0350513111447));
#18143=CARTESIAN_POINT('Ctrl Pts',(-5.90329242289988,0.398834717938238,
23.0428308625709));
#18144=CARTESIAN_POINT('Ctrl Pts',(-5.91226241544131,0.266066714999467,
23.0490955109789));
#18145=CARTESIAN_POINT('Ctrl Pts',(-5.91675058477204,0.133010396746608,
23.055360159387));
#18146=CARTESIAN_POINT('Ctrl Pts',(-5.91674999994283,-2.60100847582463E-5,
23.0616248077951));
#18147=CARTESIAN_POINT('Origin',(0.,0.,0.));
#18148=CARTESIAN_POINT('',(-5.91671817690238,6.02334792636984E-5,25.0633751914214));
#18149=CARTESIAN_POINT('',(-5.91628298387923,-6.23028472571992E-5,24.8116248077951));
#18150=CARTESIAN_POINT('',(-5.91675,-7.2459289488551E-16,0.));
#18151=CARTESIAN_POINT('Ctrl Pts',(-5.91674999969339,6.02350095563548E-5,
25.0633751913646));
#18152=CARTESIAN_POINT('Ctrl Pts',(-5.9167482813348,0.168850748591878,25.0554319459057));
#18153=CARTESIAN_POINT('Ctrl Pts',(-5.90951944838277,0.337616774232801,
25.0474887004468));
#18154=CARTESIAN_POINT('Ctrl Pts',(-5.89509576569253,0.505743488157823,
25.0395454549879));
#18155=CARTESIAN_POINT('Ctrl Pts',(-5.88066728875627,0.673926085233122,
25.0315995692967));
#18156=CARTESIAN_POINT('Ctrl Pts',(-5.8590392095019,0.841468655864555,25.0236536836055));
#18157=CARTESIAN_POINT('Ctrl Pts',(-5.83029570048855,1.00776118568081,25.0157077979143));
#18158=CARTESIAN_POINT('Ctrl Pts',(-5.81520765237642,1.0950514914465,25.0115368421153));
#18159=CARTESIAN_POINT('Ctrl Pts',(-5.79815987057062,1.18199747634926,25.0073658863163));
#18160=CARTESIAN_POINT('Ctrl Pts',(-5.77917018964272,1.2685119162408,25.0031949305173));
#18161=CARTESIAN_POINT('Ctrl Pts',(-5.74371279812575,1.43005103734313,24.9954069527558));
#18162=CARTESIAN_POINT('Ctrl Pts',(-5.70147182161497,1.59013145782957,24.9876189749943));
#18163=CARTESIAN_POINT('Ctrl Pts',(-5.65259221389059,1.74817957486165,24.9798309972328));
#18164=CARTESIAN_POINT('Ctrl Pts',(-5.60372221631618,1.90619661827886,24.9720445506545));
#18165=CARTESIAN_POINT('Ctrl Pts',(-5.54821628616727,2.06218185040195,24.9642581040762));
#18166=CARTESIAN_POINT('Ctrl Pts',(-5.48626930308796,2.21557660587369,24.9564716574979));
#18167=CARTESIAN_POINT('Ctrl Pts',(-5.4243199568709,2.36897721300953,24.9486849138842));
#18168=CARTESIAN_POINT('Ctrl Pts',(-5.35592918203759,2.51978684798059,24.9408981702705));
#18169=CARTESIAN_POINT('Ctrl Pts',(-5.28134037106795,2.66746592244922,24.9331114266568));
#18170=CARTESIAN_POINT('Ctrl Pts',(-5.20675649359011,2.81513522905196,24.925325198078));
#18171=CARTESIAN_POINT('Ctrl Pts',(-5.12597554453162,2.95967410431085,24.9175389694991));
#18172=CARTESIAN_POINT('Ctrl Pts',(-5.03928739568512,3.10056657825455,24.9097527409203));
#18173=CARTESIAN_POINT('Ctrl Pts',(-4.9525764264949,3.2414961416358,24.9019644626447));
#18174=CARTESIAN_POINT('Ctrl Pts',(-4.85995531610111,3.37877711224864,24.8941761843692));
#18175=CARTESIAN_POINT('Ctrl Pts',(-4.76175836765831,3.51192081495812,24.8863879060936));
#18176=CARTESIAN_POINT('Ctrl Pts',(-4.66840243371112,3.63850066201793,24.8789835823973));
#18177=CARTESIAN_POINT('Ctrl Pts',(-4.57000734182423,3.7613411293395,24.8715792587011));
#18178=CARTESIAN_POINT('Ctrl Pts',(-4.46689512826243,3.88004877232302,24.8641749350048));
#18179=CARTESIAN_POINT('Ctrl Pts',(-4.35844016882194,4.00490723632386,24.8563869572433));
#18180=CARTESIAN_POINT('Ctrl Pts',(-4.24472747883706,4.12523788601996,24.8485989794818));
#18181=CARTESIAN_POINT('Ctrl Pts',(-4.1261588921345,4.24060648485089,24.8408110017203));
#18182=CARTESIAN_POINT('Ctrl Pts',(-4.00761361703259,4.35595240122621,24.8330245551419));
#18183=CARTESIAN_POINT('Ctrl Pts',(-3.88421457902726,4.46633799060161,24.8252381085636));
#18184=CARTESIAN_POINT('Ctrl Pts',(-3.75640029658728,4.57136602935042,24.8174516619852));
#18185=CARTESIAN_POINT('Ctrl Pts',(-3.62858113832047,4.67639807468222,24.8096649183715));
#18186=CARTESIAN_POINT('Ctrl Pts',(-3.49634664295428,4.77607195449989,24.8018781747578));
#18187=CARTESIAN_POINT('Ctrl Pts',(-3.36016879150439,4.87003041623971,24.7940914311441));
#18188=CARTESIAN_POINT('Ctrl Pts',(-3.22399994720072,4.96398266333013,24.7863052025652));
#18189=CARTESIAN_POINT('Ctrl Pts',(-3.08388853186571,5.05222006744478,24.7785189739863));
#18190=CARTESIAN_POINT('Ctrl Pts',(-2.94033602984172,5.13442836098768,24.7707327454074));
#18191=CARTESIAN_POINT('Ctrl Pts',(-2.79674573813725,5.21665829556854,24.7629444671318));
#18192=CARTESIAN_POINT('Ctrl Pts',(-2.64971282616872,5.29285578753019,24.7551561888563));
#18193=CARTESIAN_POINT('Ctrl Pts',(-2.49976472370573,5.36275180188459,24.7473679105807));
#18194=CARTESIAN_POINT('Ctrl Pts',(-2.35720891753562,5.42920201039475,24.7399635868846));
#18195=CARTESIAN_POINT('Ctrl Pts',(-2.21201866798456,5.48995697688745,24.7325592631884));
#18196=CARTESIAN_POINT('Ctrl Pts',(-2.0646650507921,5.54482540667762,24.7251549394923));
#18197=CARTESIAN_POINT('Ctrl Pts',(-1.90967632516718,5.60253683699231,24.7173669617308));
#18198=CARTESIAN_POINT('Ctrl Pts',(-1.75223864807743,5.65375615905325,24.7095789839693));
#18199=CARTESIAN_POINT('Ctrl Pts',(-1.59291268300926,5.6982944594684,24.7017910062078));
#18200=CARTESIAN_POINT('Ctrl Pts',(-1.43361804279171,5.74282400327186,24.6940045596294));
#18201=CARTESIAN_POINT('Ctrl Pts',(-1.27243616291889,5.78067506036408,24.6862181130511));
#18202=CARTESIAN_POINT('Ctrl Pts',(-1.10994219897708,5.81170877431328,24.6784316664728));
#18203=CARTESIAN_POINT('Ctrl Pts',(-0.94744203625693,5.84274367212869,24.6706449228591));
#18204=CARTESIAN_POINT('Ctrl Pts',(-0.783630002435057,5.86696064257649,
24.6628581792454));
#18205=CARTESIAN_POINT('Ctrl Pts',(-0.619091500249949,5.88427194110013,
24.6550714356317));
#18206=CARTESIAN_POINT('Ctrl Pts',(-0.454563881055785,5.90158209461088,
24.6472852070528));
#18207=CARTESIAN_POINT('Ctrl Pts',(-0.289310207488934,5.9119874569139,24.6394989784739));
#18208=CARTESIAN_POINT('Ctrl Pts',(-0.123921210601472,5.91545214637589,
24.6317127498951));
#18209=CARTESIAN_POINT('Ctrl Pts',(0.041511324345274,5.91891774790493,24.6239244716195));
#18210=CARTESIAN_POINT('Ctrl Pts',(0.207078934143699,5.91543901699516,24.6161361933439));
#18211=CARTESIAN_POINT('Ctrl Pts',(0.372189759122767,5.90503220530626,24.6083479150683));
#18212=CARTESIAN_POINT('Ctrl Pts',(0.529160780268899,5.89513843935912,24.6009435913722));
#18213=CARTESIAN_POINT('Ctrl Pts',(0.685718706823125,5.87898324973805,24.593539267676));
#18214=CARTESIAN_POINT('Ctrl Pts',(0.84135836949002,5.85662416897218,24.5861349439798));
#18215=CARTESIAN_POINT('Ctrl Pts',(1.00506248095244,5.83310655535638,24.5783469662183));
#18216=CARTESIAN_POINT('Ctrl Pts',(1.16780920276732,5.80271666133896,24.5705589884567));
#18217=CARTESIAN_POINT('Ctrl Pts',(1.32901584777162,5.76555699294282,24.5627710106952));
#18218=CARTESIAN_POINT('Ctrl Pts',(1.49019079816758,5.72840463045604,24.5549845641169));
#18219=CARTESIAN_POINT('Ctrl Pts',(1.6498259647194,5.68448522105184,24.5471981175385));
#18220=CARTESIAN_POINT('Ctrl Pts',(1.80734989688456,5.63395215747626,24.5394116709602));
#18221=CARTESIAN_POINT('Ctrl Pts',(1.96487983823253,5.58341716617824,24.5316249273465));
#18222=CARTESIAN_POINT('Ctrl Pts',(2.12029807856014,5.52626810970226,24.5238381837327));
#18223=CARTESIAN_POINT('Ctrl Pts',(2.27304863594725,5.46270816181117,24.516051440119));
#18224=CARTESIAN_POINT('Ctrl Pts',(2.42578909002772,5.39915241793514,24.5082652115401));
#18225=CARTESIAN_POINT('Ctrl Pts',(2.57586191925568,5.32918675407356,24.5004789829612));
#18226=CARTESIAN_POINT('Ctrl Pts',(2.72273128855789,5.25306242993626,24.4926927543823));
#18227=CARTESIAN_POINT('Ctrl Pts',(2.869639320694,5.17691806634409,24.4849044761067));
#18228=CARTESIAN_POINT('Ctrl Pts',(3.01334192301967,5.09461194829665,24.4771161978311));
#18229=CARTESIAN_POINT('Ctrl Pts',(3.15332722404223,5.00644164857777,24.4693279195556));
#18230=CARTESIAN_POINT('Ctrl Pts',(3.28641138523839,4.922618059281,24.4619235958594));
#18231=CARTESIAN_POINT('Ctrl Pts',(3.41613571196547,4.83349469773388,24.4545192721633));
#18232=CARTESIAN_POINT('Ctrl Pts',(3.54208420636763,4.73936388532269,24.4471149484672));
#18233=CARTESIAN_POINT('Ctrl Pts',(3.67455870556014,4.64035569715858,24.4393269707057));
#18234=CARTESIAN_POINT('Ctrl Pts',(3.80290308405491,4.53577194302518,24.4315389929441));
#18235=CARTESIAN_POINT('Ctrl Pts',(3.92665481093323,4.42598153614256,24.4237510151826));
#18236=CARTESIAN_POINT('Ctrl Pts',(4.05038220716116,4.31621271499514,24.4159645686043));
#18237=CARTESIAN_POINT('Ctrl Pts',(4.16951851454271,4.20123949556612,24.408178122026));
#18238=CARTESIAN_POINT('Ctrl Pts',(4.28363542568264,4.08147009082961,24.4003916754476));
#18239=CARTESIAN_POINT('Ctrl Pts',(4.39775669012543,3.96169611716037,24.3926049318339));
#18240=CARTESIAN_POINT('Ctrl Pts',(4.50685795188849,3.83712582068368,24.3848181882202));
#18241=CARTESIAN_POINT('Ctrl Pts',(4.61054831351678,3.70820371760069,24.3770314446065));
#18242=CARTESIAN_POINT('Ctrl Pts',(4.7142318168034,3.5792901417503,24.3692452160276));
#18243=CARTESIAN_POINT('Ctrl Pts',(4.81250493594786,3.44602558440039,24.3614589874487));
#18244=CARTESIAN_POINT('Ctrl Pts',(4.90501747952483,3.30888713740071,24.3536727588699));
#18245=CARTESIAN_POINT('Ctrl Pts',(4.99755437669653,3.17171258919756,24.3458844805943));
#18246=CARTESIAN_POINT('Ctrl Pts',(5.0843274876665,3.03066237758575,24.3380962023187));
#18247=CARTESIAN_POINT('Ctrl Pts',(5.16502982950096,2.88624278654192,24.3303079240431));
#18248=CARTESIAN_POINT('Ctrl Pts',(5.24175362400793,2.7489429415293,24.322903600347));
#18249=CARTESIAN_POINT('Ctrl Pts',(5.31299066830321,2.60859815880302,24.3154992766509));
#18250=CARTESIAN_POINT('Ctrl Pts',(5.3785156424838,2.46566422005453,24.3080949529547));
#18251=CARTESIAN_POINT('Ctrl Pts',(5.44743578464466,2.31532417793549,24.3003069751932));
#18252=CARTESIAN_POINT('Ctrl Pts',(5.51006085465446,2.16206576307322,24.2925189974317));
#18253=CARTESIAN_POINT('Ctrl Pts',(5.56616133875906,2.00643427836646,24.2847310196702));
#18254=CARTESIAN_POINT('Ctrl Pts',(5.62225079302755,1.85083339214381,24.2769445730918));
#18255=CARTESIAN_POINT('Ctrl Pts',(5.67181811263725,1.69286066744404,24.2691581265135));
#18256=CARTESIAN_POINT('Ctrl Pts',(5.71468264347095,1.53307953052407,24.2613716799352));
#18257=CARTESIAN_POINT('Ctrl Pts',(5.75754880948986,1.37329229831397,24.2535849363215));
#18258=CARTESIAN_POINT('Ctrl Pts',(5.79371158846556,1.21169682344131,24.2457981927078));
#18259=CARTESIAN_POINT('Ctrl Pts',(5.82304054924039,1.04887049934782,24.2380114490941));
#18260=CARTESIAN_POINT('Ctrl Pts',(5.85236757012388,0.886054944997556,24.2302252205152));
#18261=CARTESIAN_POINT('Ctrl Pts',(5.87486162079779,0.72200901887839,24.2224389919363));
#18262=CARTESIAN_POINT('Ctrl Pts',(5.89044360274856,0.557319231086268,24.2146527633574));
#18263=CARTESIAN_POINT('Ctrl Pts',(5.9060296866001,0.392586089299144,24.2068644850818));
#18264=CARTESIAN_POINT('Ctrl Pts',(5.91470003376294,0.227209065310917,24.1990762068063));
#18265=CARTESIAN_POINT('Ctrl Pts',(5.91642745593873,0.0617796173052993,
24.1912879285307));
#18266=CARTESIAN_POINT('Ctrl Pts',(5.91806971787351,-0.0954943190601781,
24.1838836048345));
#18267=CARTESIAN_POINT('Ctrl Pts',(5.91343712095454,-0.252815371574824,
24.1764792811384));
#18268=CARTESIAN_POINT('Ctrl Pts',(5.90255000293267,-0.409675512301578,
24.1690749574422));
#18269=CARTESIAN_POINT('Ctrl Pts',(5.89109877031226,-0.574663340735441,
24.1612869796807));
#18270=CARTESIAN_POINT('Ctrl Pts',(5.87272355764134,-0.739200244435326,
24.1534990019192));
#18271=CARTESIAN_POINT('Ctrl Pts',(5.84748387136165,-0.902697588711379,
24.1457110241576));
#18272=CARTESIAN_POINT('Ctrl Pts',(5.82224914742067,-1.06616278800784,24.1379245775793));
#18273=CARTESIAN_POINT('Ctrl Pts',(5.79015269147166,-1.22858852007599,24.130138131001));
#18274=CARTESIAN_POINT('Ctrl Pts',(5.75130558359864,-1.38939362549535,24.1223516844227));
#18275=CARTESIAN_POINT('Ctrl Pts',(5.71245699379602,-1.55020486526699,24.114564940809));
#18276=CARTESIAN_POINT('Ctrl Pts',(5.66685730795468,-1.70939504314789,24.1067781971952));
#18277=CARTESIAN_POINT('Ctrl Pts',(5.61466838736882,-1.86639477667005,24.0989914535815));
#18278=CARTESIAN_POINT('Ctrl Pts',(5.56248291868962,-2.02338412583436,24.0912052250026));
#18279=CARTESIAN_POINT('Ctrl Pts',(5.50370918833982,-2.1781830173446,24.0834189964238));
#18280=CARTESIAN_POINT('Ctrl Pts',(5.43855849133229,-2.33023863560311,24.0756327678449));
#18281=CARTESIAN_POINT('Ctrl Pts',(5.37339064363782,-2.48233428195688,24.0678444895693));
#18282=CARTESIAN_POINT('Ctrl Pts',(5.30184259899911,-2.63168491734729,24.0600562112937));
#18283=CARTESIAN_POINT('Ctrl Pts',(5.22417359789647,-2.77775822949756,24.0522679330182));
#18284=CARTESIAN_POINT('Ctrl Pts',(5.15033360335965,-2.91663026876711,24.044863609322));
#18285=CARTESIAN_POINT('Ctrl Pts',(5.07096175268888,-3.05254010593703,24.0374592856259));
#18286=CARTESIAN_POINT('Ctrl Pts',(4.9863190787292,-3.18505142934948,24.0300549619297));
#18287=CARTESIAN_POINT('Ctrl Pts',(4.89729065567169,-3.32442880968005,24.0222669841682));
#18288=CARTESIAN_POINT('Ctrl Pts',(4.8023988463361,-3.4600959967259,24.0144790064067));
#18289=CARTESIAN_POINT('Ctrl Pts',(4.70197765735391,-3.59156465516697,24.0066910286451));
#18290=CARTESIAN_POINT('Ctrl Pts',(4.60157621203836,-3.72300746574274,23.9989045820668));
#18291=CARTESIAN_POINT('Ctrl Pts',(4.49564775006068,-3.85025314097573,23.9911181354884));
#18292=CARTESIAN_POINT('Ctrl Pts',(4.38456798135483,-3.97284459542254,23.9833316889101));
#18293=CARTESIAN_POINT('Ctrl Pts',(4.27348397520632,-4.09544072645685,23.9755449452964));
#18294=CARTESIAN_POINT('Ctrl Pts',(4.15724848073465,-4.21338204198094,23.9677582016827));
#18295=CARTESIAN_POINT('Ctrl Pts',(4.03627615634867,-4.32624610397874,23.9599714580689));
#18296=CARTESIAN_POINT('Ctrl Pts',(3.91531183337691,-4.43910270086322,23.9521852294901));
#18297=CARTESIAN_POINT('Ctrl Pts',(3.78961154121021,-4.54688249832685,23.9443990009112));
#18298=CARTESIAN_POINT('Ctrl Pts',(3.65962541086249,-4.64920126631119,23.9366127723323));
#18299=CARTESIAN_POINT('Ctrl Pts',(3.52960506213299,-4.75154696934357,23.9288244940567));
#18300=CARTESIAN_POINT('Ctrl Pts',(3.39529687082847,-4.8484285709596,23.9210362157811));
#18301=CARTESIAN_POINT('Ctrl Pts',(3.25718324963848,-4.9395027928704,23.9132479375055));
#18302=CARTESIAN_POINT('Ctrl Pts',(3.12587849627114,-5.02608714380615,23.9058436138094));
#18303=CARTESIAN_POINT('Ctrl Pts',(2.99113470276452,-5.10742277332757,23.8984392901133));
#18304=CARTESIAN_POINT('Ctrl Pts',(2.85338990313831,-5.18325154928529,23.8910349664172));
#18305=CARTESIAN_POINT('Ctrl Pts',(2.70850787470688,-5.26300938336715,23.8832469886557));
#18306=CARTESIAN_POINT('Ctrl Pts',(2.56025376281976,-5.33670306985653,23.8754590108942));
#18307=CARTESIAN_POINT('Ctrl Pts',(2.40915457424209,-5.40406373018568,23.8676710331327));
#18308=CARTESIAN_POINT('Ctrl Pts',(2.25808509306037,-5.4714111468315,23.8598845865543));
#18309=CARTESIAN_POINT('Ctrl Pts',(2.10417194297083,-5.53242789167951,23.852098139976));
#18310=CARTESIAN_POINT('Ctrl Pts',(1.94796378779114,-5.58689248544792,23.8443116933977));
#18311=CARTESIAN_POINT('Ctrl Pts',(1.79174967362238,-5.64135915691783,23.836524949784));
#18312=CARTESIAN_POINT('Ctrl Pts',(1.63324067959868,-5.689273068219,23.8287382061703));
#18313=CARTESIAN_POINT('Ctrl Pts',(1.47300308156508,-5.73046180374669,23.8209514625565));
#18314=CARTESIAN_POINT('Ctrl Pts',(1.31277608204974,-5.77164781494769,23.8131652339777));
#18315=CARTESIAN_POINT('Ctrl Pts',(1.15082101686754,-5.80610946107637,23.8053790053988));
#18316=CARTESIAN_POINT('Ctrl Pts',(0.987717017780421,-5.83372485255235,
23.7975927768199));
#18317=CARTESIAN_POINT('Ctrl Pts',(0.824570082151646,-5.8613475136809,23.7898044985443));
#18318=CARTESIAN_POINT('Ctrl Pts',(0.660273923203239,-5.8821202635693,23.7820162202687));
#18319=CARTESIAN_POINT('Ctrl Pts',(0.49541641361652,-5.89597262032477,23.7742279419932));
#18320=CARTESIAN_POINT('Ctrl Pts',(0.338686219659731,-5.90914206930217,
23.766823618297));
#18321=CARTESIAN_POINT('Ctrl Pts',(0.181448952454521,-5.91605700388703,
23.7594192946009));
#18322=CARTESIAN_POINT('Ctrl Pts',(0.0242127636971383,-5.91670045756705,
23.7520149709047));
#18323=CARTESIAN_POINT('Ctrl Pts',(-0.141170597647017,-5.91737725171548,
23.7442269931432));
#18324=CARTESIAN_POINT('Ctrl Pts',(-0.30661192664777,-5.91111564023968,
23.7364390153817));
#18325=CARTESIAN_POINT('Ctrl Pts',(-0.471519809903724,-5.89793180965738,
23.7286510376201));
#18326=CARTESIAN_POINT('Ctrl Pts',(-0.636395270856173,-5.88475057112919,
23.7208645910418));
#18327=CARTESIAN_POINT('Ctrl Pts',(-0.800737176992085,-5.86464985447569,
23.7130781444635));
#18328=CARTESIAN_POINT('Ctrl Pts',(-0.963957788586457,-5.83769782913808,
23.7052916978851));
#18329=CARTESIAN_POINT('Ctrl Pts',(-1.12718462667905,-5.81074477564149,
23.6975049542714));
#18330=CARTESIAN_POINT('Ctrl Pts',(-1.28928976872298,-5.77693993862877,
23.6897182106577));
#18331=CARTESIAN_POINT('Ctrl Pts',(-1.44969349687653,-5.73640299557256,
23.681931467044));
#18332=CARTESIAN_POINT('Ctrl Pts',(-1.61008661552351,-5.69586873373187,
23.6741452384651));
#18333=CARTESIAN_POINT('Ctrl Pts',(-1.76877823567306,-5.64860333532758,
23.6663590098862));
#18334=CARTESIAN_POINT('Ctrl Pts',(-1.92520153719232,-5.59477699320467,
23.6585727813074));
#18335=CARTESIAN_POINT('Ctrl Pts',(-2.08166601658374,-5.54093648149058,
23.6507845030318));
#18336=CARTESIAN_POINT('Ctrl Pts',(-2.235860681161,-5.48053167705407,23.6429962247562));
#18337=CARTESIAN_POINT('Ctrl Pts',(-2.38723564347627,-5.41378209249472,
23.6352079464806));
#18338=CARTESIAN_POINT('Ctrl Pts',(-2.5311479666905,-5.35032319783607,23.6278036227845));
#18339=CARTESIAN_POINT('Ctrl Pts',(-2.6725116666884,-5.28113014297149,23.6203992990883));
#18340=CARTESIAN_POINT('Ctrl Pts',(-2.81087246682014,-5.20643126697861,
23.6129949753921));
#18341=CARTESIAN_POINT('Ctrl Pts',(-2.95640241374202,-5.12786187848116,
23.6052069976306));
#18342=CARTESIAN_POINT('Ctrl Pts',(-3.09866206799006,-5.04317284794488,
23.597419019869));
#18343=CARTESIAN_POINT('Ctrl Pts',(-3.2371399187134,-4.9526614773445,23.5896310421075));
#18344=CARTESIAN_POINT('Ctrl Pts',(-3.37559054350388,-4.86216790205569,
23.5818445955292));
#18345=CARTESIAN_POINT('Ctrl Pts',(-3.51026058102323,-4.76585444548336,
23.5740581489508));
#18346=CARTESIAN_POINT('Ctrl Pts',(-3.64066662842203,-4.66406229195046,
23.5662717023725));
#18347=CARTESIAN_POINT('Ctrl Pts',(-3.77107765051768,-4.56226625527628,
23.5584849587588));
#18348=CARTESIAN_POINT('Ctrl Pts',(-3.8972241026844,-4.45499129692908,23.5506982151451));
#18349=CARTESIAN_POINT('Ctrl Pts',(-4.01865428046869,-4.342619985282,23.5429114715314));
#18350=CARTESIAN_POINT('Ctrl Pts',(-4.14007642655515,-4.23025610615654,
23.5351252429525));
#18351=CARTESIAN_POINT('Ctrl Pts',(-4.25678268803283,-4.11279676542965,
23.5273390143736));
#18352=CARTESIAN_POINT('Ctrl Pts',(-4.36835686464773,-3.99066271007524,
23.5195527857947));
#18353=CARTESIAN_POINT('Ctrl Pts',(-4.4799604127638,-3.86849650336952,23.5117645075191));
#18354=CARTESIAN_POINT('Ctrl Pts',(-4.5864289593144,-3.74165335779748,23.5039762292435));
#18355=CARTESIAN_POINT('Ctrl Pts',(-4.68738477863621,-3.61058921777452,
23.4961879509679));
#18356=CARTESIAN_POINT('Ctrl Pts',(-4.78336357379655,-3.48598641297699,
23.4887836272718));
#18357=CARTESIAN_POINT('Ctrl Pts',(-4.87435993194359,-3.3575689791053,23.4813793035757));
#18358=CARTESIAN_POINT('Ctrl Pts',(-4.96008429829237,-3.22575484442533,
23.4739749798796));
#18359=CARTESIAN_POINT('Ctrl Pts',(-5.05025046148925,-3.08711077756978,
23.4661870021181));
#18360=CARTESIAN_POINT('Ctrl Pts',(-5.13461604696483,-2.94465906958686,
23.4583990243566));
#18361=CARTESIAN_POINT('Ctrl Pts',(-5.21287425880004,-2.79890559405636,
23.450611046595));
#18362=CARTESIAN_POINT('Ctrl Pts',(-5.29111708439974,-2.65318077490898,
23.4428246000167));
#18363=CARTESIAN_POINT('Ctrl Pts',(-5.36325478116319,-2.50415576483357,
23.4350381534384));
#18364=CARTESIAN_POINT('Ctrl Pts',(-5.42902623694026,-2.35236151156965,
23.4272517068601));
#18365=CARTESIAN_POINT('Ctrl Pts',(-5.49480020175021,-2.20056146769693,
23.4194649632464));
#18366=CARTESIAN_POINT('Ctrl Pts',(-5.55420730894161,-2.04599226087433,
23.4116782196326));
#18367=CARTESIAN_POINT('Ctrl Pts',(-5.60703408663292,-1.88920600089999,
23.4038914760189));
#18368=CARTESIAN_POINT('Ctrl Pts',(-5.65985737022805,-1.73243011116394,
23.39610524744));
#18369=CARTESIAN_POINT('Ctrl Pts',(-5.70610109336985,-1.57343776461223,
23.3883190188612));
#18370=CARTESIAN_POINT('Ctrl Pts',(-5.74560123158306,-1.41279759701494,
23.3805327902823));
#18371=CARTESIAN_POINT('Ctrl Pts',(-5.78511176806576,-1.25211514147062,
23.3727445120067));
#18372=CARTESIAN_POINT('Ctrl Pts',(-5.81787509409511,-1.08978430813744,
23.3649562337311));
#18373=CARTESIAN_POINT('Ctrl Pts',(-5.84377781361127,-0.926386219481219,
23.3571679554556));
#18374=CARTESIAN_POINT('Ctrl Pts',(-5.86840355413074,-0.771043498416085,
23.3497636317594));
#18375=CARTESIAN_POINT('Ctrl Pts',(-5.88682879483896,-0.614736476746315,
23.3423593080633));
#18376=CARTESIAN_POINT('Ctrl Pts',(-5.89899935629682,-0.457970694378671,
23.3349549843671));
#18377=CARTESIAN_POINT('Ctrl Pts',(-5.9108229968946,-0.305673507830525,
23.3277617203131));
#18378=CARTESIAN_POINT('Ctrl Pts',(-5.91674658177293,-0.152915681688521,
23.320568456259));
#18379=CARTESIAN_POINT('Ctrl Pts',(-5.91674999852046,-0.000132318339550427,
23.3133751922049));
#18380=CARTESIAN_POINT('Ctrl Pts',(-5.91724902186819,-2.6012278470935E-5,
23.0616248077951));
#18381=CARTESIAN_POINT('Ctrl Pts',(-5.91725507970182,-0.0246275738384623,
23.0627831909737));
#18382=CARTESIAN_POINT('Ctrl Pts',(-5.91710486183363,-0.0492290611478781,
23.0639415741523));
#18383=CARTESIAN_POINT('Ctrl Pts',(-5.90452526107738,-1.05738799629361,
23.1114154190926));
#18384=CARTESIAN_POINT('Ctrl Pts',(-5.37887374875949,-3.01825410262035,
23.204046342616));
#18385=CARTESIAN_POINT('Ctrl Pts',(-3.27927262205552,-5.2238407042437,23.3429927279011));
#18386=CARTESIAN_POINT('Ctrl Pts',(-0.380334538725489,-6.15609342616977,
23.4819391131863));
#18387=CARTESIAN_POINT('Ctrl Pts',(2.61131174173346,-5.58777161492509,23.6208854984714));
#18388=CARTESIAN_POINT('Ctrl Pts',(4.96643943377135,-3.65740618249594,23.7598318837565));
#18389=CARTESIAN_POINT('Ctrl Pts',(6.11097592471195,-0.83553209433702,23.8987782690417));
#18390=CARTESIAN_POINT('Ctrl Pts',(5.76593546958871,2.19000657387534,24.0377246543268));
#18391=CARTESIAN_POINT('Ctrl Pts',(4.01542317922815,4.68172161974577,24.1766710396119));
#18392=CARTESIAN_POINT('Ctrl Pts',(1.28613403388383,6.03224666935662,24.315617424897));
#18393=CARTESIAN_POINT('Ctrl Pts',(-1.75665587304459,5.91238537113191,24.4545638101821));
#18394=CARTESIAN_POINT('Ctrl Pts',(-4.37125327473482,4.35135443755144,24.5935101954673));
#18395=CARTESIAN_POINT('Ctrl Pts',(-5.69818711861276,2.10563417864119,24.7125305280049));
#18396=CARTESIAN_POINT('Ctrl Pts',(-5.9160758600808,0.560655488508289,24.7852353987809));
#18397=CARTESIAN_POINT('Ctrl Pts',(-5.91628298387923,-6.23028472571992E-5,
24.8116248077951));
#18398=CARTESIAN_POINT('Origin',(0.,0.,0.));
#18399=CARTESIAN_POINT('',(-5.91679775669098,2.19428441319584E-5,26.8133751922049));
#18400=CARTESIAN_POINT('',(-5.91695430380796,0.0001364654751753,26.5616248077951));
#18401=CARTESIAN_POINT('',(-5.91675,-7.2459289488551E-16,0.));
#18402=CARTESIAN_POINT('Ctrl Pts',(-5.91725285177388,2.19445318853841E-5,
26.8133751922049));
#18403=CARTESIAN_POINT('Ctrl Pts',(-5.91725718695043,0.020695672166474,
26.8124017521966));
#18404=CARTESIAN_POINT('Ctrl Pts',(-5.9171511099118,0.0413693551410023,
26.8114283121884));
#18405=CARTESIAN_POINT('Ctrl Pts',(-5.90661556573244,1.04614428635966,26.7641148736759));
#18406=CARTESIAN_POINT('Ctrl Pts',(-5.38431816636206,3.00908896148112,26.6714348766675));
#18407=CARTESIAN_POINT('Ctrl Pts',(-3.28705913345889,5.21926630359759,26.532414881155));
#18408=CARTESIAN_POINT('Ctrl Pts',(-0.387733679065683,6.15590457112853,
26.3933948856425));
#18409=CARTESIAN_POINT('Ctrl Pts',(2.60620162316863,5.59045719008011,26.25437489013));
#18410=CARTESIAN_POINT('Ctrl Pts',(4.96420470614338,3.66089744874507,26.1153548946175));
#18411=CARTESIAN_POINT('Ctrl Pts',(6.110905606059,0.838052008266846,25.976334899105));
#18412=CARTESIAN_POINT('Ctrl Pts',(5.7665009333289,-2.18928423934433,25.8373149035924));
#18413=CARTESIAN_POINT('Ctrl Pts',(4.01502794197995,-4.68241915251552,25.69829490808));
#18414=CARTESIAN_POINT('Ctrl Pts',(1.28385882626606,-6.03300961452435,25.5592749125674));
#18415=CARTESIAN_POINT('Ctrl Pts',(-1.76058121420839,-5.91150169440051,
25.4202549170549));
#18416=CARTESIAN_POINT('Ctrl Pts',(-4.37542658756877,-4.34754421156596,
25.2812349215424));
#18417=CARTESIAN_POINT('Ctrl Pts',(-5.69937917119131,-2.10150200017265,
25.162275013259));
#18418=CARTESIAN_POINT('Ctrl Pts',(-5.91608000283946,-0.558332029564552,
25.0896551034799));
#18419=CARTESIAN_POINT('Ctrl Pts',(-5.91627901576061,6.02123609064198E-5,
25.0633751922049));
#18420=CARTESIAN_POINT('Ctrl Pts',(-5.91628298387923,-6.23028472571992E-5,
24.8116248077951));
#18421=CARTESIAN_POINT('Ctrl Pts',(-5.91643937842867,-0.423447770894904,
24.8315508605426));
#18422=CARTESIAN_POINT('Ctrl Pts',(-5.76745479447041,-1.83082804996811,
24.8977923750519));
#18423=CARTESIAN_POINT('Ctrl Pts',(-4.66335225933688,-4.03674204506728,
25.0103493513227));
#18424=CARTESIAN_POINT('Ctrl Pts',(-2.16367632199188,-5.77586750252553,
25.1492957366078));
#18425=CARTESIAN_POINT('Ctrl Pts',(0.863405124340446,-6.10710014854341,
25.2882421218929));
#18426=CARTESIAN_POINT('Ctrl Pts',(3.68002781839282,-4.94970058578635,25.427188507178));
#18427=CARTESIAN_POINT('Ctrl Pts',(5.59962773462851,-2.58578998889243,25.5661348924632));
#18428=CARTESIAN_POINT('Ctrl Pts',(6.15429404896376,0.40841815822461,25.7050812777483));
#18429=CARTESIAN_POINT('Ctrl Pts',(5.20882443614428,3.30307260388006,25.8440276630334));
#18430=CARTESIAN_POINT('Ctrl Pts',(2.99368122425189,5.39258874388175,25.9829740483185));
#18431=CARTESIAN_POINT('Ctrl Pts',(0.0488152004140352,6.16763793597564,
26.1219204336038));
#18432=CARTESIAN_POINT('Ctrl Pts',(-2.90794974072443,5.43929857044995,26.2608668188888));
#18433=CARTESIAN_POINT('Ctrl Pts',(-5.15588929170198,3.38510653374309,26.3998132041739));
#18434=CARTESIAN_POINT('Ctrl Pts',(-5.87103811602415,1.30761350995423,26.5000658671427));
#18435=CARTESIAN_POINT('Ctrl Pts',(-5.91711432678824,0.162029141072471,
26.5540030683498));
#18436=CARTESIAN_POINT('Ctrl Pts',(-5.91695430380796,0.0001364654751753,
26.5616248077951));
#18437=CARTESIAN_POINT('Origin',(0.,0.,0.));
#18438=CARTESIAN_POINT('',(-5.91674757964165,-9.37334433651367E-5,28.5633751922614));
#18439=CARTESIAN_POINT('',(-5.91674999800012,-0.00015383611583252,28.3116248078268));
#18440=CARTESIAN_POINT('',(-5.91675,-7.2459289488551E-16,0.));
#18441=CARTESIAN_POINT('Ctrl Pts',(-5.91674999925755,-9.3732281115321E-5,
28.5633751922049));
#18442=CARTESIAN_POINT('Ctrl Pts',(-5.91675262882337,0.165894797763913,
28.5555635075889));
#18443=CARTESIAN_POINT('Ctrl Pts',(-5.90976595002247,0.331883858816857,
28.5477518229729));
#18444=CARTESIAN_POINT('Ctrl Pts',(-5.89581587907907,0.497278274710596,
28.5399401383569));
#18445=CARTESIAN_POINT('Ctrl Pts',(-5.88186591041835,0.662671477923394,
28.5321285110166));
#18446=CARTESIAN_POINT('Ctrl Pts',(-5.86095268125918,0.827469730883103,
28.5243168836763));
#18447=CARTESIAN_POINT('Ctrl Pts',(-5.83315402760025,0.991082566081681,
28.516505256336));
#18448=CARTESIAN_POINT('Ctrl Pts',(-5.80534823376329,1.15473742578916,28.5086916225529));
#18449=CARTESIAN_POINT('Ctrl Pts',(-5.77065353462187,1.31720594854534,28.5008779887697));
#18450=CARTESIAN_POINT('Ctrl Pts',(-5.72919912930452,1.47790659355603,28.4930643549866));
#18451=CARTESIAN_POINT('Ctrl Pts',(-5.70378711174193,1.57641789970232,28.4882745094345));
#18452=CARTESIAN_POINT('Ctrl Pts',(-5.67583591392416,1.67426507088607,28.4834846638823));
#18453=CARTESIAN_POINT('Ctrl Pts',(-5.64538465570273,1.77131664353277,28.4786948183302));
#18454=CARTESIAN_POINT('Ctrl Pts',(-5.59587288768143,1.92911619703704,28.4709068405688));
#18455=CARTESIAN_POINT('Ctrl Pts',(-5.53973191207739,2.08486674110341,28.4631188628075));
#18456=CARTESIAN_POINT('Ctrl Pts',(-5.47715651414356,2.23800962510771,28.4553308850461));
#18457=CARTESIAN_POINT('Ctrl Pts',(-5.41459341906945,2.39112239990808,28.4475444384679));
#18458=CARTESIAN_POINT('Ctrl Pts',(-5.34559854663349,2.54162824198346,28.4397579918897));
#18459=CARTESIAN_POINT('Ctrl Pts',(-5.27041510263627,2.68898776650314,28.4319715453116));
#18460=CARTESIAN_POINT('Ctrl Pts',(-5.19522879056015,2.83635291245648,28.424184801698));
#18461=CARTESIAN_POINT('Ctrl Pts',(-5.11385357622112,2.98057121425195,28.4163980580844));
#18462=CARTESIAN_POINT('Ctrl Pts',(-5.02657931473763,3.12112655224869,28.4086113144709));
#18463=CARTESIAN_POINT('Ctrl Pts',(-4.93931082579369,3.26167259356124,28.4008250858922));
#18464=CARTESIAN_POINT('Ctrl Pts',(-4.8461442391848,3.39855588447202,28.3930388573135));
#18465=CARTESIAN_POINT('Ctrl Pts',(-4.7474136347221,3.53128791566968,28.3852526287347));
#18466=CARTESIAN_POINT('Ctrl Pts',(-4.64865703978238,3.66405488809782,28.3774643504593));
#18467=CARTESIAN_POINT('Ctrl Pts',(-4.5443336894687,3.79266815942464,28.3696760721839));
#18468=CARTESIAN_POINT('Ctrl Pts',(-4.43481952526852,3.91667031300786,28.3618877939085));
#18469=CARTESIAN_POINT('Ctrl Pts',(-4.33070430333401,4.0345592804758,28.3544834702116));
#18470=CARTESIAN_POINT('Ctrl Pts',(-4.22189791747622,4.14828062816423,28.3470791465147));
#18471=CARTESIAN_POINT('Ctrl Pts',(-4.10875572356729,4.25747072409817,28.3396748228178));
#18472=CARTESIAN_POINT('Ctrl Pts',(-3.98975108166709,4.37231849058331,28.3318868450562));
#18473=CARTESIAN_POINT('Ctrl Pts',(-3.86590681357093,4.48219404919458,28.3240988672946));
#18474=CARTESIAN_POINT('Ctrl Pts',(-3.73766134782034,4.58670014405889,28.316310889533));
#18475=CARTESIAN_POINT('Ctrl Pts',(-3.60944109622796,4.69118569212886,28.3085244429546));
#18476=CARTESIAN_POINT('Ctrl Pts',(-3.47682162110087,4.79030368111094,28.3007379963762));
#18477=CARTESIAN_POINT('Ctrl Pts',(-3.34027464213883,4.88369694776246,28.2929515497978));
#18478=CARTESIAN_POINT('Ctrl Pts',(-3.20372245421738,4.97709377715655,28.285164806184));
#18479=CARTESIAN_POINT('Ctrl Pts',(-3.06324272417338,5.06476526356921,28.2773780625702));
#18480=CARTESIAN_POINT('Ctrl Pts',(-2.91933699335127,5.14639700001377,28.2695913189564));
#18481=CARTESIAN_POINT('Ctrl Pts',(-2.77544078081694,5.22802333712952,28.2618050903775));
#18482=CARTESIAN_POINT('Ctrl Pts',(-2.62811929899789,5.30361056612377,28.2540188617986));
#18483=CARTESIAN_POINT('Ctrl Pts',(-2.4778997021947,5.37288969069377,28.2462326332197));
#18484=CARTESIAN_POINT('Ctrl Pts',(-2.32764056062208,5.44218705274454,28.238444354944));
#18485=CARTESIAN_POINT('Ctrl Pts',(-2.17448206914537,5.50517285647967,28.2306560766684));
#18486=CARTESIAN_POINT('Ctrl Pts',(-2.01897325341945,5.56162544266304,28.2228677983927));
#18487=CARTESIAN_POINT('Ctrl Pts',(-1.87113087177371,5.61529497099461,28.2154634746969));
#18488=CARTESIAN_POINT('Ctrl Pts',(-1.72116456873923,5.66305983748205,28.2080591510011));
#18489=CARTESIAN_POINT('Ctrl Pts',(-1.56956040421967,5.7047708718235,28.2006548273052));
#18490=CARTESIAN_POINT('Ctrl Pts',(-1.41010088970494,5.74864315796466,28.1928668495436));
#18491=CARTESIAN_POINT('Ctrl Pts',(-1.24877223449866,5.78583329281053,28.185078871782));
#18492=CARTESIAN_POINT('Ctrl Pts',(-1.08614953066657,5.81620234857186,28.1772908940204));
#18493=CARTESIAN_POINT('Ctrl Pts',(-0.923558799852407,5.84656543351644,
28.1695044474419));
#18494=CARTESIAN_POINT('Ctrl Pts',(-0.759674841984277,5.87011005660676,
28.1617180008635));
#18495=CARTESIAN_POINT('Ctrl Pts',(-0.595082787611209,5.88674842662644,
28.1539315542851));
#18496=CARTESIAN_POINT('Ctrl Pts',(-0.430484454422606,5.9033874313624,28.1461448106713));
#18497=CARTESIAN_POINT('Ctrl Pts',(-0.265178288197985,5.91311961977152,
28.1383580670575));
#18498=CARTESIAN_POINT('Ctrl Pts',(-0.0997551367588218,5.91590901512103,
28.1305713234437));
#18499=CARTESIAN_POINT('Ctrl Pts',(0.0656570731764681,5.9186982259729,28.1227850948648));
#18500=CARTESIAN_POINT('Ctrl Pts',(0.231185933308759,5.91454555744609,28.1149988662858));
#18501=CARTESIAN_POINT('Ctrl Pts',(0.396239844345193,5.90346716330779,28.1072126377069));
#18502=CARTESIAN_POINT('Ctrl Pts',(0.561337205230819,5.89238585282202,28.0994243594312));
#18503=CARTESIAN_POINT('Ctrl Pts',(0.72595904801083,5.87437519310494,28.0916360811556));
#18504=CARTESIAN_POINT('Ctrl Pts',(0.889517229130205,5.84950336879812,28.0838478028799));
#18505=CARTESIAN_POINT('Ctrl Pts',(1.04501215024488,5.82585770135368,28.0764434791842));
#18506=CARTESIAN_POINT('Ctrl Pts',(1.19954549789333,5.79601111058879,28.0690391554884));
#18507=CARTESIAN_POINT('Ctrl Pts',(1.35261911030467,5.76006528651704,28.0616348317927));
#18508=CARTESIAN_POINT('Ctrl Pts',(1.51362421195892,5.72225693426383,28.0538468540313));
#18509=CARTESIAN_POINT('Ctrl Pts',(1.67307188482846,5.67768698098481,28.0460588762699));
#18510=CARTESIAN_POINT('Ctrl Pts',(1.83039069998508,5.62650872636915,28.0382708985086));
#18511=CARTESIAN_POINT('Ctrl Pts',(1.98767858491353,5.57534053383723,28.0304844519304));
#18512=CARTESIAN_POINT('Ctrl Pts',(2.14283814357463,5.51756673114694,28.0226980053522));
#18513=CARTESIAN_POINT('Ctrl Pts',(2.29531361069508,5.45339032080576,28.0149115587741));
#18514=CARTESIAN_POINT('Ctrl Pts',(2.44779489441133,5.389211462279,28.0071248151605));
#18515=CARTESIAN_POINT('Ctrl Pts',(2.59759158564982,5.31862962767838,27.9993380715469));
#18516=CARTESIAN_POINT('Ctrl Pts',(2.74416770129323,5.24189604911038,27.9915513279334));
#18517=CARTESIAN_POINT('Ctrl Pts',(2.89073412202315,5.16516754589455,27.9837650993546));
#18518=CARTESIAN_POINT('Ctrl Pts',(3.03408011036302,5.08228826128183,27.9759788707759));
#18519=CARTESIAN_POINT('Ctrl Pts',(3.17369397657337,4.99355555747224,27.9681926421971));
#18520=CARTESIAN_POINT('Ctrl Pts',(3.31334459563241,4.90479949509717,27.9604043639217));
#18521=CARTESIAN_POINT('Ctrl Pts',(3.44926085846503,4.81018710436662,27.9526160856463));
#18522=CARTESIAN_POINT('Ctrl Pts',(3.58095901493649,4.71005977624967,27.9448278073708));
#18523=CARTESIAN_POINT('Ctrl Pts',(3.70616457980042,4.61486862846837,27.937423483674));
#18524=CARTESIAN_POINT('Ctrl Pts',(3.8275577072866,4.51469336644065,27.9300191599771));
#18525=CARTESIAN_POINT('Ctrl Pts',(3.94474968886493,4.4098617273901,27.9226148362803));
#18526=CARTESIAN_POINT('Ctrl Pts',(4.06801395765482,4.2995982506609,27.9148268585186));
#18527=CARTESIAN_POINT('Ctrl Pts',(4.18667425217489,4.18414360317922,27.907038880757));
#18528=CARTESIAN_POINT('Ctrl Pts',(4.30030223946391,4.06390590586959,27.8992509029953));
#18529=CARTESIAN_POINT('Ctrl Pts',(4.41390788651618,3.94369184832238,27.8914644564169));
#18530=CARTESIAN_POINT('Ctrl Pts',(4.52248298112377,3.8186968494063,27.8836780098385));
#18531=CARTESIAN_POINT('Ctrl Pts',(4.62563673407239,3.68936517125916,27.87589156326));
#18532=CARTESIAN_POINT('Ctrl Pts',(4.72879442210443,3.56002855939969,27.8681048196462));
#18533=CARTESIAN_POINT('Ctrl Pts',(4.82653015230451,3.42635518461736,27.8603180760324));
#18534=CARTESIAN_POINT('Ctrl Pts',(4.91849359005227,3.28882218539019,27.8525313324185));
#18535=CARTESIAN_POINT('Ctrl Pts',(5.01045094510655,3.15129828294213,27.8447451038395));
#18536=CARTESIAN_POINT('Ctrl Pts',(5.09663659419305,3.00991553263504,27.8369588752605));
#18537=CARTESIAN_POINT('Ctrl Pts',(5.17674361315702,2.86517994655449,27.8291726466816));
#18538=CARTESIAN_POINT('Ctrl Pts',(5.25687172000597,2.72040625935084,27.8213843684059));
#18539=CARTESIAN_POINT('Ctrl Pts',(5.33091784268429,2.57227825153229,27.8135960901302));
#18540=CARTESIAN_POINT('Ctrl Pts',(5.39862066304133,2.42132721850707,27.8058078118545));
#18541=CARTESIAN_POINT('Ctrl Pts',(5.46298579988965,2.27781792529263,27.7984034881589));
#18542=CARTESIAN_POINT('Ctrl Pts',(5.52161789799881,2.13175748716479,27.7909991644633));
#18543=CARTESIAN_POINT('Ctrl Pts',(5.57433254979846,1.98361971828206,27.7835948407677));
#18544=CARTESIAN_POINT('Ctrl Pts',(5.6297786044005,1.82780621024045,27.7758068630063));
#18545=CARTESIAN_POINT('Ctrl Pts',(5.67869754257536,1.66963864527529,27.7680188852448));
#18546=CARTESIAN_POINT('Ctrl Pts',(5.72090864369786,1.50968038106187,27.7602309074834));
#18547=CARTESIAN_POINT('Ctrl Pts',(5.76311144575601,1.34975356601448,27.7524444609052));
#18548=CARTESIAN_POINT('Ctrl Pts',(5.79860896070824,1.1880370629793,27.7446580143269));
#18549=CARTESIAN_POINT('Ctrl Pts',(5.82727073082005,1.02510799052,27.7368715677487));
#18550=CARTESIAN_POINT('Ctrl Pts',(5.85593359431377,0.86217270268391,27.7290848241351));
#18551=CARTESIAN_POINT('Ctrl Pts',(5.87776013190894,0.698025066884494,27.7212980805215));
#18552=CARTESIAN_POINT('Ctrl Pts',(5.89267114168673,0.533251702699923,27.7135113369078));
#18553=CARTESIAN_POINT('Ctrl Pts',(5.9075811652128,0.368489237040522,27.705725108329));
#18554=CARTESIAN_POINT('Ctrl Pts',(5.915576547579,0.203101444104479,27.6979388797502));
#18555=CARTESIAN_POINT('Ctrl Pts',(5.91663002194938,0.0376795152204819,
27.6901526511714));
#18556=CARTESIAN_POINT('Ctrl Pts',(5.91768377364311,-0.127785960391721,
27.682364372896));
#18557=CARTESIAN_POINT('Ctrl Pts',(5.91179196175398,-0.293285270164019,
27.6745760946205));
#18558=CARTESIAN_POINT('Ctrl Pts',(5.89897946365164,-0.45822685420669,27.666787816345));
#18559=CARTESIAN_POINT('Ctrl Pts',(5.88679860930157,-0.615036977841214,
27.6593834926484));
#18560=CARTESIAN_POINT('Ctrl Pts',(5.868363018147,-0.771342779077537,27.6519791689518));
#18561=CARTESIAN_POINT('Ctrl Pts',(5.84373758037036,-0.926639980934974,
27.6445748452553));
#18562=CARTESIAN_POINT('Ctrl Pts',(5.81783617875235,-1.0899838870189,27.6367868674936));
#18563=CARTESIAN_POINT('Ctrl Pts',(5.78507718260018,-1.25227032912556,27.628998889732));
#18564=CARTESIAN_POINT('Ctrl Pts',(5.74557158077637,-1.41291817621364,27.6212109119704));
#18565=CARTESIAN_POINT('Ctrl Pts',(5.70607374609244,-1.57353443855826,27.6134244653919));
#18566=CARTESIAN_POINT('Ctrl Pts',(5.65983202863783,-1.73251243857735,27.6056380188135));
#18567=CARTESIAN_POINT('Ctrl Pts',(5.60700813479728,-1.88928302242335,27.597851572235));
#18568=CARTESIAN_POINT('Ctrl Pts',(5.55418222584456,-2.04605958671284,27.5900648286212));
#18569=CARTESIAN_POINT('Ctrl Pts',(5.49477373634509,-2.20062826225394,27.5822780850074));
#18570=CARTESIAN_POINT('Ctrl Pts',(5.42899392292789,-2.35243608782727,27.5744913413936));
#18571=CARTESIAN_POINT('Ctrl Pts',(5.36321846035328,-2.50423387244855,27.5667051128146));
#18572=CARTESIAN_POINT('Ctrl Pts',(5.29107264434056,-2.65327087934423,27.5589188842357));
#18573=CARTESIAN_POINT('Ctrl Pts',(5.21281551867958,-2.79901499294187,27.5511326556567));
#18574=CARTESIAN_POINT('Ctrl Pts',(5.13453779211136,-2.94479747315392,27.5433443773811));
#18575=CARTESIAN_POINT('Ctrl Pts',(5.05014569075875,-3.08728504528919,27.5355560991054));
#18576=CARTESIAN_POINT('Ctrl Pts',(4.95994421725192,-3.22597022990746,27.5277678208298));
#18577=CARTESIAN_POINT('Ctrl Pts',(4.87418958907396,-3.35781836917131,27.520363497134));
#18578=CARTESIAN_POINT('Ctrl Pts',(4.78318472746382,-3.48622977707173,27.5129591734383));
#18579=CARTESIAN_POINT('Ctrl Pts',(4.68722798667849,-3.61079276107033,27.5055548497426));
#18580=CARTESIAN_POINT('Ctrl Pts',(4.58629925989531,-3.7418099598247,27.4977668719811));
#18581=CARTESIAN_POINT('Ctrl Pts',(4.47985576359286,-3.86861620263012,27.4899788942196));
#18582=CARTESIAN_POINT('Ctrl Pts',(4.36827311402875,-3.99075438529528,27.4821909164581));
#18583=CARTESIAN_POINT('Ctrl Pts',(4.25671240257029,-4.11286855454648,27.4744044698799));
#18584=CARTESIAN_POINT('Ctrl Pts',(4.14001476929804,-4.23031625912445,27.4666180233016));
#18585=CARTESIAN_POINT('Ctrl Pts',(4.01859462717775,-4.34267518759096,27.4588315767233));
#18586=CARTESIAN_POINT('Ctrl Pts',(3.89716985315276,-4.45503840229727,27.4510448331097));
#18587=CARTESIAN_POINT('Ctrl Pts',(3.77102244163432,-4.56231223251412,27.443258089496));
#18588=CARTESIAN_POINT('Ctrl Pts',(3.64060255963977,-4.66411230195461,27.4354713458823));
#18589=CARTESIAN_POINT('Ctrl Pts',(3.51019130394476,-4.76590563808207,27.4276851173035));
#18590=CARTESIAN_POINT('Ctrl Pts',(3.37550839527123,-4.86222574139844,27.4198988887247));
#18591=CARTESIAN_POINT('Ctrl Pts',(3.23703597945929,-4.95272941217124,27.4121126601459));
#18592=CARTESIAN_POINT('Ctrl Pts',(3.09852711128112,-5.04325690771038,27.4043243818703));
#18593=CARTESIAN_POINT('Ctrl Pts',(2.95622700919494,-5.12796473455706,27.3965361035948));
#18594=CARTESIAN_POINT('Ctrl Pts',(2.81064637822338,-5.20655332240819,27.3887478253193));
#18595=CARTESIAN_POINT('Ctrl Pts',(2.67224273142234,-5.28126756895975,27.3813435016229));
#18596=CARTESIAN_POINT('Ctrl Pts',(2.53087444983944,-5.35045126271971,27.3739391779265));
#18597=CARTESIAN_POINT('Ctrl Pts',(2.38700055118997,-5.41388575157611,27.3665348542302));
#18598=CARTESIAN_POINT('Ctrl Pts',(2.23567184527486,-5.48060709018675,27.3587468764686));
#18599=CARTESIAN_POINT('Ctrl Pts',(2.08151683887124,-5.54099148486481,27.3509588987071));
#18600=CARTESIAN_POINT('Ctrl Pts',(1.92508412252328,-5.59481739502808,27.3431709209456));
#18601=CARTESIAN_POINT('Ctrl Pts',(1.76868216218759,-5.64863272255625,27.3353844743672));
#18602=CARTESIAN_POINT('Ctrl Pts',(1.61000368741266,-5.69589203450496,27.3275980277888));
#18603=CARTESIAN_POINT('Ctrl Pts',(1.44961469795676,-5.73642290891874,27.3198115812104));
#18604=CARTESIAN_POINT('Ctrl Pts',(1.28921959002358,-5.77695532949373,27.3120248375967));
#18605=CARTESIAN_POINT('Ctrl Pts',(1.12711414566991,-5.81075871680186,27.304238093983));
#18606=CARTESIAN_POINT('Ctrl Pts',(0.963877598263364,-5.83771107010839,
27.2964513503692));
#18607=CARTESIAN_POINT('Ctrl Pts',(0.800651847733722,-5.86466164071831,
27.2886651217904));
#18608=CARTESIAN_POINT('Ctrl Pts',(0.636295459191402,-5.88476203218761,
27.2808788932115));
#18609=CARTESIAN_POINT('Ctrl Pts',(0.471396033422478,-5.89794170386361,
27.2730926646327));
#18610=CARTESIAN_POINT('Ctrl Pts',(0.306453198471773,-5.91112484504086,
27.2653043863571));
#18611=CARTESIAN_POINT('Ctrl Pts',(0.140967359235795,-5.91738359854969,
27.2575161080815));
#18612=CARTESIAN_POINT('Ctrl Pts',(-0.0244696926235903,-5.91669940056472,
27.249727829806));
#18613=CARTESIAN_POINT('Ctrl Pts',(-0.181750857979391,-5.91604893287806,
27.2423235061098));
#18614=CARTESIAN_POINT('Ctrl Pts',(-0.338987666939524,-5.90912358622243,
27.2349191824137));
#18615=CARTESIAN_POINT('Ctrl Pts',(-0.495672442003575,-5.89595110162374,
27.2275148587176));
#18616=CARTESIAN_POINT('Ctrl Pts',(-0.660475818227291,-5.88209608645566,
27.2197268809561));
#18617=CARTESIAN_POINT('Ctrl Pts',(-0.82472738795972,-5.86132439994564,
27.2119389031945));
#18618=CARTESIAN_POINT('Ctrl Pts',(-0.987839446467213,-5.83370412263969,
27.204150925433));
#18619=CARTESIAN_POINT('Ctrl Pts',(-1.1509194357451,-5.80608927571714,27.1963644788546));
#18620=CARTESIAN_POINT('Ctrl Pts',(-1.31286004594762,-5.77162857796424,
27.1885780322763));
#18621=CARTESIAN_POINT('Ctrl Pts',(-1.47308179859639,-5.73044156912397,
27.180791585698));
#18622=CARTESIAN_POINT('Ctrl Pts',(-1.63330966334435,-5.68925298909204,
27.1730048420842));
#18623=CARTESIAN_POINT('Ctrl Pts',(-1.79181822886907,-5.64133766024962,
27.1652180984705));
#18624=CARTESIAN_POINT('Ctrl Pts',(-1.9480405326223,-5.58686572648391,27.1574313548567));
#18625=CARTESIAN_POINT('Ctrl Pts',(-2.10425250343885,-5.53239739562912,
27.1496451262778));
#18626=CARTESIAN_POINT('Ctrl Pts',(-2.25817821337433,-5.47137343301536,
27.1418588976989));
#18627=CARTESIAN_POINT('Ctrl Pts',(-2.40926798557749,-5.40401316950388,
27.13407266912));
#18628=CARTESIAN_POINT('Ctrl Pts',(-2.56039753162051,-5.33663517364497,
27.1262843908444));
#18629=CARTESIAN_POINT('Ctrl Pts',(-2.70868935531687,-5.26291767227535,
27.1184961125688));
#18630=CARTESIAN_POINT('Ctrl Pts',(-2.85361497985062,-5.1831276377562,27.1107078342932));
#18631=CARTESIAN_POINT('Ctrl Pts',(-2.99139591138917,-5.10727117469862,
27.1033035105972));
#18632=CARTESIAN_POINT('Ctrl Pts',(-3.12613431863912,-5.02592662276455,
27.0958991869012));
#18633=CARTESIAN_POINT('Ctrl Pts',(-3.25739774133065,-4.93936134710491,
27.0884948632051));
#18634=CARTESIAN_POINT('Ctrl Pts',(-3.3954625611294,-4.8483107029901,27.0807068854436));
#18635=CARTESIAN_POINT('Ctrl Pts',(-3.52973211226876,-4.7514513784177,27.0729189076821));
#18636=CARTESIAN_POINT('Ctrl Pts',(-3.65972298007034,-4.64912446291181,
27.0651309299206));
#18637=CARTESIAN_POINT('Ctrl Pts',(-3.78968829055197,-4.5468176657555,27.0573444833423));
#18638=CARTESIAN_POINT('Ctrl Pts',(-3.91537634525469,-4.43904562008982,
27.0495580367641));
#18639=CARTESIAN_POINT('Ctrl Pts',(-4.03633558395846,-4.32619065878641,
27.0417715901858));
#18640=CARTESIAN_POINT('Ctrl Pts',(-4.15729943698521,-4.21333139231997,
27.0339848465721));
#18641=CARTESIAN_POINT('Ctrl Pts',(-4.27353387670501,-4.09538903730922,
27.0261981029584));
#18642=CARTESIAN_POINT('Ctrl Pts',(-4.38462255438919,-3.97278436591286,
27.0184113593447));
#18643=CARTESIAN_POINT('Ctrl Pts',(-4.49570388438817,-3.85018780389856,
27.0106251307659));
#18644=CARTESIAN_POINT('Ctrl Pts',(-4.6016399189553,-3.72292977950718,27.002838902187));
#18645=CARTESIAN_POINT('Ctrl Pts',(-4.70205303033806,-3.59146597678283,
26.9950526736082));
#18646=CARTESIAN_POINT('Ctrl Pts',(-4.80249257511188,-3.45996756668441,
26.9872643953326));
#18647=CARTESIAN_POINT('Ctrl Pts',(-4.89740609587291,-3.32426141885105,
26.979476117057));
#18648=CARTESIAN_POINT('Ctrl Pts',(-4.98645738285165,-3.18483489862572,
26.9716878387815));
#18649=CARTESIAN_POINT('Ctrl Pts',(-5.07111852759153,-3.05228197087081,
26.9642835150852));
#18650=CARTESIAN_POINT('Ctrl Pts',(-5.15048137828395,-2.91636687807601,
26.9568791913889));
#18651=CARTESIAN_POINT('Ctrl Pts',(-5.22429421535204,-2.77753137046897,
26.9494748676926));
#18652=CARTESIAN_POINT('Ctrl Pts',(-5.30185754954526,-2.63164150493682,
26.9416943236011));
#18653=CARTESIAN_POINT('Ctrl Pts',(-5.37332042517392,-2.4824735504262,26.9339137795095));
#18654=CARTESIAN_POINT('Ctrl Pts',(-5.43842194674002,-2.33055729209056,
26.926133235418));
#18655=CARTESIAN_POINT('Ctrl Pts',(-5.50351045007573,-2.17867141216702,
26.9183542471874));
#18656=CARTESIAN_POINT('Ctrl Pts',(-5.56224001114736,-2.02403861961598,
26.9105752589568));
#18657=CARTESIAN_POINT('Ctrl Pts',(-5.61439743588298,-1.86720968143661,
26.9027962707262));
#18658=CARTESIAN_POINT('Ctrl Pts',(-5.66655651357155,-1.71037577309514,
26.8950170359669));
#18659=CARTESIAN_POINT('Ctrl Pts',(-5.71214293319581,-1.55134588299275,
26.8872378012077));
#18660=CARTESIAN_POINT('Ctrl Pts',(-5.75099281623643,-1.39068766806103,
26.8794585664484));
#18661=CARTESIAN_POINT('Ctrl Pts',(-5.78984035089331,-1.23003916453923,
26.8716798019255));
#18662=CARTESIAN_POINT('Ctrl Pts',(-5.82195208878417,-1.06776284505455,
26.8639010374026));
#18663=CARTESIAN_POINT('Ctrl Pts',(-5.84721485783825,-0.904438482582201,
26.8561222728797));
#18664=CARTESIAN_POINT('Ctrl Pts',(-5.87248402761934,-0.741072739267766,
26.8483415374823));
#18665=CARTESIAN_POINT('Ctrl Pts',(-5.89090071076948,-0.576658739365433,
26.8405608020848));
#18666=CARTESIAN_POINT('Ctrl Pts',(-5.90240326791351,-0.411784197637469,
26.8327800666874));
#18667=CARTESIAN_POINT('Ctrl Pts',(-5.91196558930545,-0.274720470188791,
26.8263117751932));
#18668=CARTESIAN_POINT('Ctrl Pts',(-5.91675050937049,-0.137338687105534,
26.8198434836991));
#18669=CARTESIAN_POINT('Ctrl Pts',(-5.91674999995931,2.19426670226234E-5,
26.8133751922049));
#18670=CARTESIAN_POINT('Ctrl Pts',(-5.91695430380796,0.0001364654751753,
26.5616248077951));
#18671=CARTESIAN_POINT('Ctrl Pts',(-5.91614190595471,-0.821753377324698,
26.6003185301115));
#18672=CARTESIAN_POINT('Ctrl Pts',(-5.53662360997084,-2.6281524630163,26.6853277141895));
#18673=CARTESIAN_POINT('Ctrl Pts',(-3.75791298936681,-4.89083127877313,
26.8166523600294));
#18674=CARTESIAN_POINT('Ctrl Pts',(-0.959963023245171,-6.09266867859071,
26.9555987453144));
#18675=CARTESIAN_POINT('Ctrl Pts',(2.07198210275202,-5.80939160316744,27.0945451305995));
#18676=CARTESIAN_POINT('Ctrl Pts',(4.59887258429633,-4.11005007104363,27.2334915158847));
#18677=CARTESIAN_POINT('Ctrl Pts',(6.00476788211649,-1.40886596771288,27.3724379011698));
#18678=CARTESIAN_POINT('Ctrl Pts',(5.94697490594146,1.63573533958923,27.5113842864549));
#18679=CARTESIAN_POINT('Ctrl Pts',(4.43958094493993,4.28161904732342,27.6503306717401));
#18680=CARTESIAN_POINT('Ctrl Pts',(1.85001982974811,5.8838395000729,27.7892770570252));
#18681=CARTESIAN_POINT('Ctrl Pts',(-1.19049166098134,6.05184849762528,27.9282234423103));
#18682=CARTESIAN_POINT('Ctrl Pts',(-3.94081563427965,4.74469311649309,28.0671698275954));
#18683=CARTESIAN_POINT('Ctrl Pts',(-5.58698077633417,2.47862958568841,28.194970282757));
#18684=CARTESIAN_POINT('Ctrl Pts',(-5.91595772284066,0.74696456590951,28.276455276157));
#18685=CARTESIAN_POINT('Ctrl Pts',(-5.91671909124951,-0.000153834640280791,
28.3116248077952));
#18686=CARTESIAN_POINT('Origin',(0.,0.,0.));
#18687=CARTESIAN_POINT('',(-5.9167499981344,0.000148581922998542,30.3133751922049));
#18688=CARTESIAN_POINT('',(-5.91674999882181,0.000118076772239281,30.0616248064854));
#18689=CARTESIAN_POINT('',(-5.91675,-7.2459289488551E-16,0.));
#18690=CARTESIAN_POINT('Ctrl Pts',(-5.91685455241636,0.000148584548576164,
30.3133751922049));
#18691=CARTESIAN_POINT('Ctrl Pts',(-5.91705466625152,0.194302987475124,
30.3042350481343));
#18692=CARTESIAN_POINT('Ctrl Pts',(-5.86018956337674,1.37269220639489,30.2487549055594));
#18693=CARTESIAN_POINT('Ctrl Pts',(-5.09914682414872,3.4704754948657,30.1469347644806));
#18694=CARTESIAN_POINT('Ctrl Pts',(-2.81582907770545,5.48785979229666,30.0079147689679));
#18695=CARTESIAN_POINT('Ctrl Pts',(0.154571517014471,6.16616624336598,29.8688947734555));
#18696=CARTESIAN_POINT('Ctrl Pts',(3.08725553333882,5.33988312293554,29.7298747779429));
#18697=CARTESIAN_POINT('Ctrl Pts',(5.26662666500381,3.21062954359113,29.5908547824305));
#18698=CARTESIAN_POINT('Ctrl Pts',(6.16090244821295,0.297958920558667,29.4518347869178));
#18699=CARTESIAN_POINT('Ctrl Pts',(5.55187306434934,-2.68741585395062,29.3128147914055));
#18700=CARTESIAN_POINT('Ctrl Pts',(3.58814612851256,-5.01704154409505,29.1737947958928));
#18701=CARTESIAN_POINT('Ctrl Pts',(0.748885346697635,-6.1224724770483,29.0347748003804));
#18702=CARTESIAN_POINT('Ctrl Pts',(-2.27310892598541,-5.73397543640903,
28.8957548048678));
#18703=CARTESIAN_POINT('Ctrl Pts',(-4.74044802882859,-3.94634653580834,
28.7567348093554));
#18704=CARTESIAN_POINT('Ctrl Pts',(-5.78497019753788,-1.75425870356025,
28.6459416083429));
#18705=CARTESIAN_POINT('Ctrl Pts',(-5.91655400292455,-0.384950057342253,
28.5814884058347));
#18706=CARTESIAN_POINT('Ctrl Pts',(-5.9163378217224,-9.39302684334942E-5,
28.5633752018305));
#18707=CARTESIAN_POINT('Ctrl Pts',(-5.91674999800012,-0.00015383611583252,
28.3116248078268));
#18708=CARTESIAN_POINT('Ctrl Pts',(-5.91674546782816,-0.174390521601554,
28.3198267083227));
#18709=CARTESIAN_POINT('Ctrl Pts',(-5.90904020723868,-0.348588844823986,
28.3280286088185));
#18710=CARTESIAN_POINT('Ctrl Pts',(-5.8936703221145,-0.522092613170047,
28.3362305093143));
#18711=CARTESIAN_POINT('Ctrl Pts',(-5.88815338161512,-0.584370890375815,
28.3391745389314));
#18712=CARTESIAN_POINT('Ctrl Pts',(-5.88164940694164,-0.646559714065766,
28.3421185685486));
#18713=CARTESIAN_POINT('Ctrl Pts',(-5.87416169919864,-0.708628883244091,
28.3450625981657));
#18714=CARTESIAN_POINT('Ctrl Pts',(-5.85435377959027,-0.872826145669539,
28.3528507095587));
#18715=CARTESIAN_POINT('Ctrl Pts',(-5.82765343558209,-1.03622168171102,
28.3606388209517));
#18716=CARTESIAN_POINT('Ctrl Pts',(-5.79414997686327,-1.19823061558089,
28.3684269323447));
#18717=CARTESIAN_POINT('Ctrl Pts',(-5.76065309596446,-1.36020774182113,
28.3762135146778));
#18718=CARTESIAN_POINT('Ctrl Pts',(-5.72035583008903,-1.52079849636549,
28.3840000970109));
#18719=CARTESIAN_POINT('Ctrl Pts',(-5.67339861665725,-1.67942808688303,
28.391786679344));
#18720=CARTESIAN_POINT('Ctrl Pts',(-5.62643961275753,-1.83806372591105,
28.3995735585777));
#18721=CARTESIAN_POINT('Ctrl Pts',(-5.57282024006913,-1.99473774378487,
28.4073604378114));
#18722=CARTESIAN_POINT('Ctrl Pts',(-5.51273105390054,-2.14888968769004,
28.4151473170452));
#18723=CARTESIAN_POINT('Ctrl Pts',(-5.45264583358346,-2.30303145765614,
28.4229336823494));
#18724=CARTESIAN_POINT('Ctrl Pts',(-5.38609177045433,-2.45465118906632,
28.4307200476536));
#18725=CARTESIAN_POINT('Ctrl Pts',(-5.31330794901207,-2.60320748336838,
28.4385064129578));
#18726=CARTESIAN_POINT('Ctrl Pts',(-5.24050501601631,-2.75180278553662,
28.4462948228034));
#18727=CARTESIAN_POINT('Ctrl Pts',(-5.16146919495497,-2.89733275526208,
28.454083232649));
#18728=CARTESIAN_POINT('Ctrl Pts',(-5.07648641286356,-3.03927890502199,
28.4618716424946));
#18729=CARTESIAN_POINT('Ctrl Pts',(-4.99596964243807,-3.17376550656331,
28.4692507561467));
#18730=CARTESIAN_POINT('Ctrl Pts',(-4.9101150169179,-3.3050350502794,28.4766298697987));
#18731=CARTESIAN_POINT('Ctrl Pts',(-4.81920242797586,-3.43266929964009,
28.4840089834508));
#18732=CARTESIAN_POINT('Ctrl Pts',(-4.7232508810693,-3.56737785658398,28.4917970948438));
#18733=CARTESIAN_POINT('Ctrl Pts',(-4.6216305131412,-3.69808482040399,28.4995852062369));
#18734=CARTESIAN_POINT('Ctrl Pts',(-4.51469957426996,-3.824319327225,28.5073733176299));
#18735=CARTESIAN_POINT('Ctrl Pts',(-4.40778962942439,-3.95052905010128,
28.5151598999631));
#18736=CARTESIAN_POINT('Ctrl Pts',(-4.29557140040973,-4.07226782436561,
28.5229464822963));
#18737=CARTESIAN_POINT('Ctrl Pts',(-4.17844320945086,-4.18909810196586,
28.5307330646294));
#18738=CARTESIAN_POINT('Ctrl Pts',(-4.06131055242033,-4.3059328342784,28.5385199438632));
#18739=CARTESIAN_POINT('Ctrl Pts',(-3.93926778225771,-4.41785846698047,
28.546306823097));
#18740=CARTESIAN_POINT('Ctrl Pts',(-3.81275037031918,-4.52447402204178,
28.5540937023308));
#18741=CARTESIAN_POINT('Ctrl Pts',(-3.68624130845656,-4.63108254053821,
28.5618800676351));
#18742=CARTESIAN_POINT('Ctrl Pts',(-3.55525844024118,-4.73238147689246,
28.5696664329394));
#18743=CARTESIAN_POINT('Ctrl Pts',(-3.42027073538813,-4.82800980313292,
28.5774527982437));
#18744=CARTESIAN_POINT('Ctrl Pts',(-3.28524758550497,-4.92366323942992,
28.5852412080894));
#18745=CARTESIAN_POINT('Ctrl Pts',(-3.146217757472,-5.01364290389254,28.593029617935));
#18746=CARTESIAN_POINT('Ctrl Pts',(-3.00368039306052,-5.09763029836843,
28.6008180277807));
#18747=CARTESIAN_POINT('Ctrl Pts',(-2.86863364636253,-5.17720399074333,
28.6081971414325));
#18748=CARTESIAN_POINT('Ctrl Pts',(-2.73043876117063,-5.2513988930982,28.6155762550842));
#18749=CARTESIAN_POINT('Ctrl Pts',(-2.58954161585625,-5.31998165243533,
28.6229553687359));
#18750=CARTESIAN_POINT('Ctrl Pts',(-2.44083504831392,-5.39236570756186,
28.6307434801289));
#18751=CARTESIAN_POINT('Ctrl Pts',(-2.28906506289486,-5.45852370854368,
28.6385315915218));
#18752=CARTESIAN_POINT('Ctrl Pts',(-2.13477152505278,-5.51821357853462,
28.6463197029148));
#18753=CARTESIAN_POINT('Ctrl Pts',(-1.98050828005729,-5.57789172946006,
28.6541062852478));
#18754=CARTESIAN_POINT('Ctrl Pts',(-1.82372276904173,-5.63110416801707,
28.6618928675808));
#18755=CARTESIAN_POINT('Ctrl Pts',(-1.66497410626174,-5.67765724467213,
28.6696794499138));
#18756=CARTESIAN_POINT('Ctrl Pts',(-1.50621939043053,-5.72421209638565,
28.6774663291475));
#18757=CARTESIAN_POINT('Ctrl Pts',(-1.34550167854417,-5.76410698440258,
28.6852532083812));
#18758=CARTESIAN_POINT('Ctrl Pts',(-1.18339520997047,-5.79719814561474,
28.6930400876149));
#18759=CARTESIAN_POINT('Ctrl Pts',(-1.02129944032978,-5.83028712282942,
28.700826452919));
#18760=CARTESIAN_POINT('Ctrl Pts',(-0.857815410541906,-5.85657320804385,
28.7086128182232));
#18761=CARTESIAN_POINT('Ctrl Pts',(-0.693527662131371,-5.87596374600445,
28.7163991835274));
#18762=CARTESIAN_POINT('Ctrl Pts',(-0.529196775094446,-5.89535937552653,
28.7241875933729));
#18763=CARTESIAN_POINT('Ctrl Pts',(-0.364062065039663,-5.90785580037143,
28.7319760032185));
#18764=CARTESIAN_POINT('Ctrl Pts',(-0.198714220497542,-5.91341214706637,
28.7397644130641));
#18765=CARTESIAN_POINT('Ctrl Pts',(-0.0420557290678969,-5.91867649685876,
28.7471435267164));
#18766=CARTESIAN_POINT('Ctrl Pts',(0.114793811812508,-5.91771142788405,
28.7545226403687));
#18767=CARTESIAN_POINT('Ctrl Pts',(0.271331221864757,-5.91052535148453,
28.761901754021));
#18768=CARTESIAN_POINT('Ctrl Pts',(0.436544937778181,-5.90294097670534,
28.769689865414));
#18769=CARTESIAN_POINT('Ctrl Pts',(0.601469946999545,-5.8884237145229,28.7774779768069));
#18770=CARTESIAN_POINT('Ctrl Pts',(0.765516363250975,-5.86701928240354,
28.7852660881998));
#18771=CARTESIAN_POINT('Ctrl Pts',(0.929530571848269,-5.84561905267131,
28.7930526705328));
#18772=CARTESIAN_POINT('Ctrl Pts',(1.09266621501012,-5.81733439231027,28.8008392528659));
#18773=CARTESIAN_POINT('Ctrl Pts',(1.25433967298034,-5.78226275322106,28.8086258351989));
#18774=CARTESIAN_POINT('Ctrl Pts',(1.41601929552353,-5.74718977685805,28.8164127144326));
#18775=CARTESIAN_POINT('Ctrl Pts',(1.57623630822345,-5.70532936781408,28.8241995936662));
#18776=CARTESIAN_POINT('Ctrl Pts',(1.7344176770428,-5.65683002078562,28.8319864728999));
#18777=CARTESIAN_POINT('Ctrl Pts',(1.89258860598323,-5.60833387468603,28.8397728382041));
#18778=CARTESIAN_POINT('Ctrl Pts',(2.04872385441977,-5.55319976122519,28.8475592035082));
#18779=CARTESIAN_POINT('Ctrl Pts',(2.202265793556,-5.49162598298838,28.8553455688124));
#18780=CARTESIAN_POINT('Ctrl Pts',(2.35584804968757,-5.43003603672776,28.8631339786579));
#18781=CARTESIAN_POINT('Ctrl Pts',(2.50683533835034,-5.36200316407788,28.8709223885035));
#18782=CARTESIAN_POINT('Ctrl Pts',(2.65468940715157,-5.28777407933218,28.878710798349));
#18783=CARTESIAN_POINT('Ctrl Pts',(2.79477345502364,-5.21744587838834,28.8860899120014));
#18784=CARTESIAN_POINT('Ctrl Pts',(2.93204489416862,-5.14155607783481,28.8934690256538));
#18785=CARTESIAN_POINT('Ctrl Pts',(3.06606589478054,-5.06035280305273,28.9008481393062));
#18786=CARTESIAN_POINT('Ctrl Pts',(3.20751519762847,-4.97464872268883,28.9086362506992));
#18787=CARTESIAN_POINT('Ctrl Pts',(3.34539404272668,-4.88299484310485,28.9164243620922));
#18788=CARTESIAN_POINT('Ctrl Pts',(3.47920631031759,-4.78571353224849,28.9242124734852));
#18789=CARTESIAN_POINT('Ctrl Pts',(3.61299230620244,-4.68845132088164,28.9319990558183));
#18790=CARTESIAN_POINT('Ctrl Pts',(3.74271305934025,-4.58556407051792,28.9397856381514));
#18791=CARTESIAN_POINT('Ctrl Pts',(3.86790270432689,-4.47741658016771,28.9475722204845));
#18792=CARTESIAN_POINT('Ctrl Pts',(3.99309712276678,-4.36926496617781,28.9553590997182));
#18793=CARTESIAN_POINT('Ctrl Pts',(4.11375984297218,-4.25585291674345,28.9631459789519));
#18794=CARTESIAN_POINT('Ctrl Pts',(4.22945871577383,-4.13758498813798,28.9709328581857));
#18795=CARTESIAN_POINT('Ctrl Pts',(4.34514995251681,-4.01932486514739,28.9787192234899));
#18796=CARTESIAN_POINT('Ctrl Pts',(4.45587777407664,-3.89620973283399,28.9865055887941));
#18797=CARTESIAN_POINT('Ctrl Pts',(4.56124738882818,-3.76868051450479,28.9942919540983));
#18798=CARTESIAN_POINT('Ctrl Pts',(4.66664467150083,-3.64111780959257,29.0020803639439));
#18799=CARTESIAN_POINT('Ctrl Pts',(4.76668073081876,-3.50913894789375,29.0098687737895));
#18800=CARTESIAN_POINT('Ctrl Pts',(4.86100095188754,-3.37321809378647,29.0176571836351));
#18801=CARTESIAN_POINT('Ctrl Pts',(4.95036446058173,-3.24444014680858,29.0250362972872));
#18802=CARTESIAN_POINT('Ctrl Pts',(5.0345972879751,-3.11212408346002,29.0324154109392));
#18803=CARTESIAN_POINT('Ctrl Pts',(5.11343367765309,-2.97669726152043,29.0397945245913));
#18804=CARTESIAN_POINT('Ctrl Pts',(5.19663968498426,-2.83376421771706,29.0475826359842));
#18805=CARTESIAN_POINT('Ctrl Pts',(5.27386379810543,-2.6873147523006,29.0553707473772));
#18806=CARTESIAN_POINT('Ctrl Pts',(5.34482459512685,-2.5378693051115,29.0631588587702));
#18807=CARTESIAN_POINT('Ctrl Pts',(5.41577146023278,-2.38845319893079,29.0709454411032));
#18808=CARTESIAN_POINT('Ctrl Pts',(5.48045732587137,-2.2360425730928,29.0787320234362));
#18809=CARTESIAN_POINT('Ctrl Pts',(5.53864763770795,-2.08118065237311,29.0865186057693));
#18810=CARTESIAN_POINT('Ctrl Pts',(5.59684016832818,-1.92631282680282,29.094305485003));
#18811=CARTESIAN_POINT('Ctrl Pts',(5.64853653346676,-1.76899381703139,29.1020923642367));
#18812=CARTESIAN_POINT('Ctrl Pts',(5.69355080706104,-1.60978562855883,29.1098792434704));
#18813=CARTESIAN_POINT('Ctrl Pts',(5.73856210973932,-1.45058794773457,29.1176656087745));
#18814=CARTESIAN_POINT('Ctrl Pts',(5.77689211658219,-1.28950164525325,29.1254519740787));
#18815=CARTESIAN_POINT('Ctrl Pts',(5.80840510531055,-1.12710278817076,29.1332383393829));
#18816=CARTESIAN_POINT('Ctrl Pts',(5.83992636870982,-0.964661288446265,
29.1410267492285));
#18817=CARTESIAN_POINT('Ctrl Pts',(5.86462697436654,-0.800906858951679,
29.1488151590741));
#18818=CARTESIAN_POINT('Ctrl Pts',(5.88242238380661,-0.636425534521513,
29.1566035689197));
#18819=CARTESIAN_POINT('Ctrl Pts',(5.89928260962293,-0.480588025876346,
29.1639826825719));
#18820=CARTESIAN_POINT('Ctrl Pts',(5.90994470743427,-0.324098315344506,
29.1713617962242));
#18821=CARTESIAN_POINT('Ctrl Pts',(5.9143797734987,-0.167458822787721,29.1787409098764));
#18822=CARTESIAN_POINT('Ctrl Pts',(5.91906065933036,-0.00213736630104985,
29.1865290212694));
#18823=CARTESIAN_POINT('Ctrl Pts',(5.91680632720862,0.1634099911377,29.1943171326624));
#18824=CARTESIAN_POINT('Ctrl Pts',(5.90761865092055,0.328591597268764,29.2021052440554));
#18825=CARTESIAN_POINT('Ctrl Pts',(5.89843277847256,0.49374077287092,29.2098918263884));
#18826=CARTESIAN_POINT('Ctrl Pts',(5.88231629567359,0.658524021607163,29.2176784087215));
#18827=CARTESIAN_POINT('Ctrl Pts',(5.85932313289708,0.822352106337153,29.2254649910546));
#18828=CARTESIAN_POINT('Ctrl Pts',(5.83632909339638,0.986186437795591,29.2332518702883));
#18829=CARTESIAN_POINT('Ctrl Pts',(5.80645788974177,1.14906521540755,29.241038749522));
#18830=CARTESIAN_POINT('Ctrl Pts',(5.76981513926322,1.31040597573004,29.2488256287557));
#18831=CARTESIAN_POINT('Ctrl Pts',(5.73317480718499,1.47173608765572,29.2566119940599));
#18832=CARTESIAN_POINT('Ctrl Pts',(5.68976389352247,1.631528073834,29.2643983593641));
#18833=CARTESIAN_POINT('Ctrl Pts',(5.63973882823814,1.78921114230912,29.2721847246683));
#18834=CARTESIAN_POINT('Ctrl Pts',(5.58970062738754,1.94693561515591,29.2799731345139));
#18835=CARTESIAN_POINT('Ctrl Pts',(5.53304489938063,2.10254975841753,29.2877615443595));
#18836=CARTESIAN_POINT('Ctrl Pts',(5.46997778878417,2.25549851534152,29.2955499542052));
#18837=CARTESIAN_POINT('Ctrl Pts',(5.41022497838645,2.40040951549063,29.3029290678573));
#18838=CARTESIAN_POINT('Ctrl Pts',(5.34471741392448,2.54292782599727,29.3103081815095));
#18839=CARTESIAN_POINT('Ctrl Pts',(5.27367008974176,2.68259843194301,29.3176872951616));
#18840=CARTESIAN_POINT('Ctrl Pts',(5.1986848678045,2.8300104774413,29.3254754065546));
#18841=CARTESIAN_POINT('Ctrl Pts',(5.11750159369404,2.97430283889159,29.3332635179475));
#18842=CARTESIAN_POINT('Ctrl Pts',(5.0304049801305,3.11495686942504,29.3410516293405));
#18843=CARTESIAN_POINT('Ctrl Pts',(4.94332546646876,3.25558328499151,29.3488382116736));
#18844=CARTESIAN_POINT('Ctrl Pts',(4.85033509797285,3.39257252343312,29.3566247940066));
#18845=CARTESIAN_POINT('Ctrl Pts',(4.75176314396138,3.52543296435916,29.3644113763397));
#18846=CARTESIAN_POINT('Ctrl Pts',(4.65318743142322,3.65829847122428,29.3721982555734));
#18847=CARTESIAN_POINT('Ctrl Pts',(4.54902989471648,3.78703460659917,29.3799851348071));
#18848=CARTESIAN_POINT('Ctrl Pts',(4.43966194988044,3.91118042709408,29.3877720140408));
#18849=CARTESIAN_POINT('Ctrl Pts',(4.33030122326549,4.03531805403664,29.395558379345));
#18850=CARTESIAN_POINT('Ctrl Pts',(4.21573098801031,4.15486573266453,29.4033447446491));
#18851=CARTESIAN_POINT('Ctrl Pts',(4.0963616958356,4.26939707914254,29.4111311099533));
#18852=CARTESIAN_POINT('Ctrl Pts',(3.9769610597088,4.38395849922635,29.4189195197989));
#18853=CARTESIAN_POINT('Ctrl Pts',(3.85275907802271,4.49350073237972,29.4267079296445));
#18854=CARTESIAN_POINT('Ctrl Pts',(3.72420232975072,4.59763499742849,29.4344963394901));
#18855=CARTESIAN_POINT('Ctrl Pts',(3.60240149041853,4.69629680286982,29.4418754531423));
#18856=CARTESIAN_POINT('Ctrl Pts',(3.4766920172817,4.79010425564088,29.4492545667945));
#18857=CARTESIAN_POINT('Ctrl Pts',(3.34748039696332,4.87876065763082,29.4566336804467));
#18858=CARTESIAN_POINT('Ctrl Pts',(3.21110704106634,4.97233096524966,29.4644217918396));
#18859=CARTESIAN_POINT('Ctrl Pts',(3.07078360093657,5.06019644036851,29.4722099032325));
#18860=CARTESIAN_POINT('Ctrl Pts',(2.92700822826401,5.14203786393826,29.4799980146254));
#18861=CARTESIAN_POINT('Ctrl Pts',(2.78326108337941,5.22386321937126,29.4877845969584));
#18862=CARTESIAN_POINT('Ctrl Pts',(2.63606363573782,5.29966672515556,29.4955711792914));
#18863=CARTESIAN_POINT('Ctrl Pts',(2.48594023277524,5.36917421225735,29.5033577616244));
#18864=CARTESIAN_POINT('Ctrl Pts',(2.33581110564082,5.43868434966413,29.511144640858));
#18865=CARTESIAN_POINT('Ctrl Pts',(2.18275608822847,5.50189785018816,29.5189315200916));
#18866=CARTESIAN_POINT('Ctrl Pts',(2.02732186101265,5.55858764744788,29.5267183993253));
#18867=CARTESIAN_POINT('Ctrl Pts',(1.87189789236584,5.61527370321381,29.5345047646294));
#18868=CARTESIAN_POINT('Ctrl Pts',(1.71409532839968,5.66543680795208,29.5422911299335));
#18869=CARTESIAN_POINT('Ctrl Pts',(1.55447859320192,5.70889891886141,29.5500774952376));
#18870=CARTESIAN_POINT('Ctrl Pts',(1.39481994589086,5.75237244203847,29.5578659050831));
#18871=CARTESIAN_POINT('Ctrl Pts',(1.23334648346908,5.78914136957265,29.5656543149287));
#18872=CARTESIAN_POINT('Ctrl Pts',(1.07063636375053,5.81907796296931,29.5734427247742));
#18873=CARTESIAN_POINT('Ctrl Pts',(0.916476979533205,5.84744132974438,29.5808218384267));
#18874=CARTESIAN_POINT('Ctrl Pts',(0.76120782825153,5.86967195038614,29.5882009520792));
#18875=CARTESIAN_POINT('Ctrl Pts',(0.605327805926907,5.88570376504558,29.5955800657317));
#18876=CARTESIAN_POINT('Ctrl Pts',(0.440807914380117,5.90262416555449,29.6033681771249));
#18877=CARTESIAN_POINT('Ctrl Pts',(0.275548756743581,5.91264516283174,29.611156288518));
#18878=CARTESIAN_POINT('Ctrl Pts',(0.110140497037312,5.91572477667888,29.6189443999111));
#18879=CARTESIAN_POINT('Ctrl Pts',(-0.0552352876407673,5.91880378589753,
29.6267309822443));
#18880=CARTESIAN_POINT('Ctrl Pts',(-0.220759796703246,5.91494412497204,
29.6345175645775));
#18881=CARTESIAN_POINT('Ctrl Pts',(-0.385841416563542,5.90415590611937,
29.6423041469107));
#18882=CARTESIAN_POINT('Ctrl Pts',(-0.550929330949217,5.89336727591432,
29.6500910261445));
#18883=CARTESIAN_POINT('Ctrl Pts',(-0.715574003248115,5.87564957604523,
29.6578779053784));
#18884=CARTESIAN_POINT('Ctrl Pts',(-0.879186744292628,5.85106496555628,
29.6656647846122));
#18885=CARTESIAN_POINT('Ctrl Pts',(-1.04278868699086,5.82648197763741,29.6734511499165));
#18886=CARTESIAN_POINT('Ctrl Pts',(-1.20535851873871,5.79503303364574,29.6812375152208));
#18887=CARTESIAN_POINT('Ctrl Pts',(-1.3663154239063,5.75683183052065,29.6890238805252));
#18888=CARTESIAN_POINT('Ctrl Pts',(-1.5273145930885,5.7186205965354,29.6968122903709));
#18889=CARTESIAN_POINT('Ctrl Pts',(-1.68669967786058,5.67365363252723,29.7046007002166));
#18890=CARTESIAN_POINT('Ctrl Pts',(-1.8439018700484,5.62209537949438,29.7123891100623));
#18891=CARTESIAN_POINT('Ctrl Pts',(-1.9928427790917,5.57324661365641,29.7197682237139));
#18892=CARTESIAN_POINT('Ctrl Pts',(-2.13982407791312,5.51848159175311,29.7271473373654));
#18893=CARTESIAN_POINT('Ctrl Pts',(-2.28437606916714,5.45798099457267,29.734526451017));
#18894=CARTESIAN_POINT('Ctrl Pts',(-2.43694005762399,5.3941270667935,29.7423145624099));
#18895=CARTESIAN_POINT('Ctrl Pts',(-2.58685229470455,5.32386092458106,29.7501026738028));
#18896=CARTESIAN_POINT('Ctrl Pts',(-2.73357445910418,5.24742805944334,29.7578907851957));
#18897=CARTESIAN_POINT('Ctrl Pts',(-2.88026781716449,5.17101020056631,29.7656773675288));
#18898=CARTESIAN_POINT('Ctrl Pts',(-3.02377206902146,5.08842818206036,29.7734639498618));
#18899=CARTESIAN_POINT('Ctrl Pts',(-3.16357254332143,4.99997393249633,29.7812505321948));
#18900=CARTESIAN_POINT('Ctrl Pts',(-3.30337834818231,4.91151631019148,29.7890374114285));
#18901=CARTESIAN_POINT('Ctrl Pts',(-3.43947982077722,4.81718617629317,29.7968242906622));
#18902=CARTESIAN_POINT('Ctrl Pts',(-3.57138975878909,4.71731976373411,29.8046111698958));
#18903=CARTESIAN_POINT('Ctrl Pts',(-3.70329099082135,4.61745994230051,29.8123975352));
#18904=CARTESIAN_POINT('Ctrl Pts',(-3.83100098716438,4.51206476638862,29.8201839005041));
#18905=CARTESIAN_POINT('Ctrl Pts',(-3.95406411698081,4.40151195855524,29.8279702658083));
#18906=CARTESIAN_POINT('Ctrl Pts',(-4.07715956067603,4.29093012179957,29.8357586756538));
#18907=CARTESIAN_POINT('Ctrl Pts',(-4.19560546053188,4.17518815920172,29.8435470854994));
#18908=CARTESIAN_POINT('Ctrl Pts',(-4.30898100747911,4.05470260804468,29.8513354953449));
#18909=CARTESIAN_POINT('Ctrl Pts',(-4.41639844735659,3.94054880860553,29.8587146089973));
#18910=CARTESIAN_POINT('Ctrl Pts',(-4.51926456323526,3.82213735630032,29.8660937226497));
#18911=CARTESIAN_POINT('Ctrl Pts',(-4.6172533472149,3.69985163082694,29.8734728363021));
#18912=CARTESIAN_POINT('Ctrl Pts',(-4.72067329720334,3.57078804722963,29.881260947695));
#18913=CARTESIAN_POINT('Ctrl Pts',(-4.81869685427459,3.43736244313912,29.8890490590879));
#18914=CARTESIAN_POINT('Ctrl Pts',(-4.91096875799744,3.30004794214768,29.8968371704808));
#18915=CARTESIAN_POINT('Ctrl Pts',(-5.00322254574043,3.1627604004649,29.9046237528138));
#18916=CARTESIAN_POINT('Ctrl Pts',(-5.08972675519242,3.02158575037327,29.9124103351468));
#18917=CARTESIAN_POINT('Ctrl Pts',(-5.1701691106124,2.87702657793935,29.9201969174798));
#18918=CARTESIAN_POINT('Ctrl Pts',(-5.25061453328166,2.73246189349605,29.9279837967135));
#18919=CARTESIAN_POINT('Ctrl Pts',(-5.32499748059826,2.58451270575827,29.9357706759472));
#18920=CARTESIAN_POINT('Ctrl Pts',(-5.39305099477828,2.43370736330829,29.9435575551808));
#18921=CARTESIAN_POINT('Ctrl Pts',(-5.46110001746565,2.28291197392387,29.9513439204849));
#18922=CARTESIAN_POINT('Ctrl Pts',(-5.52282031164343,2.12926109837163,29.9591302857891));
#18923=CARTESIAN_POINT('Ctrl Pts',(-5.57799249326393,1.97330441331064,29.9669166510932));
#18924=CARTESIAN_POINT('Ctrl Pts',(-5.63317916197895,1.81730677719116,29.9747050609387));
#18925=CARTESIAN_POINT('Ctrl Pts',(-5.68181417394764,1.65900242251507,29.9824934707843));
#18926=CARTESIAN_POINT('Ctrl Pts',(-5.72372729324552,1.49895845007668,29.9902818806298));
#18927=CARTESIAN_POINT('Ctrl Pts',(-5.76343779602619,1.3473251018791,29.9976609942823));
#18928=CARTESIAN_POINT('Ctrl Pts',(-5.79711466604073,1.19413052541016,30.0050401079347));
#18929=CARTESIAN_POINT('Ctrl Pts',(-5.82465505067723,1.03986734880957,30.0124192215872));
#18930=CARTESIAN_POINT('Ctrl Pts',(-5.85526262764347,0.868423771924959,
30.0206201524036));
#18931=CARTESIAN_POINT('Ctrl Pts',(-5.87829868295137,0.695613700489109,
30.0288210832199));
#18932=CARTESIAN_POINT('Ctrl Pts',(-5.89366966581137,0.522100021829988,
30.0370220140363));
#18933=CARTESIAN_POINT('Ctrl Pts',(-5.90904064867138,0.348586343170895,
30.0452229448527));
#18934=CARTESIAN_POINT('Ctrl Pts',(-5.91674652140112,0.174369358341535,
30.053423875669));
#18935=CARTESIAN_POINT('Ctrl Pts',(-5.91674999882181,0.000118076772239281,
30.0616248064854));
#18936=CARTESIAN_POINT('Origin',(0.,0.,0.));
#18937=CARTESIAN_POINT('',(-5.91674999804183,-0.000152223442091875,32.0633751922049));
#18938=CARTESIAN_POINT('',(-5.91722096325101,-5.21647111771487E-5,31.8116248077951));
#18939=CARTESIAN_POINT('',(-5.91675,-7.2459289488551E-16,0.));
#18940=CARTESIAN_POINT('Ctrl Pts',(-5.91674999804183,-0.000152223442091875,
32.0633751922049));
#18941=CARTESIAN_POINT('Ctrl Pts',(-5.91675423770661,0.164638666811161,
32.0556175243838));
#18942=CARTESIAN_POINT('Ctrl Pts',(-5.90986960240032,0.329452771156317,
32.0478598565627));
#18943=CARTESIAN_POINT('Ctrl Pts',(-5.89611634297487,0.493702980145559,
32.0401021887416));
#18944=CARTESIAN_POINT('Ctrl Pts',(-5.88236290911205,0.657955272377488,
32.0323444225272));
#18945=CARTESIAN_POINT('Ctrl Pts',(-5.86174069949175,0.821643331426469,
32.0245866563129));
#18946=CARTESIAN_POINT('Ctrl Pts',(-5.83432194704467,0.984183916111654,
32.0168288900986));
#18947=CARTESIAN_POINT('Ctrl Pts',(-5.8069047507725,1.14671527566602,32.009071564183));
#18948=CARTESIAN_POINT('Ctrl Pts',(-5.77269183800966,1.30809897145918,32.0013142382674));
#18949=CARTESIAN_POINT('Ctrl Pts',(-5.73180682219263,1.46776057842075,31.9935569123517));
#18950=CARTESIAN_POINT('Ctrl Pts',(-5.69091162717361,1.62746193656537,31.9857976550834));
#18951=CARTESIAN_POINT('Ctrl Pts',(-5.64334108984841,1.78544003472309,31.978038397815));
#18952=CARTESIAN_POINT('Ctrl Pts',(-5.58926930129603,1.94113349362938,31.9702791405467));
#18953=CARTESIAN_POINT('Ctrl Pts',(-5.55190687059043,2.048714289927,31.9649176624122));
#18954=CARTESIAN_POINT('Ctrl Pts',(-5.51144146350675,2.1552045628405,31.9595561842777));
#18955=CARTESIAN_POINT('Ctrl Pts',(-5.46794419499389,2.26042404051377,31.9541947061432));
#18956=CARTESIAN_POINT('Ctrl Pts',(-5.40476091766596,2.41326378575352,31.9464067283818));
#18957=CARTESIAN_POINT('Ctrl Pts',(-5.33515407285044,2.56348005742101,31.9386187506204));
#18958=CARTESIAN_POINT('Ctrl Pts',(-5.25936677102741,2.71053347706918,31.930830772859));
#18959=CARTESIAN_POINT('Ctrl Pts',(-5.18359436963759,2.85755798475445,31.9230443262808));
#18960=CARTESIAN_POINT('Ctrl Pts',(-5.1016440820839,3.00142059730995,31.9152578797026));
#18961=CARTESIAN_POINT('Ctrl Pts',(-5.01380555964883,3.14160538141481,31.9074714331244));
#18962=CARTESIAN_POINT('Ctrl Pts',(-4.92596368637224,3.281795513253,31.8996846895109));
#18963=CARTESIAN_POINT('Ctrl Pts',(-4.8322332950541,3.4183072630218,31.8918979458973));
#18964=CARTESIAN_POINT('Ctrl Pts',(-4.73294846204454,3.55065197085412,31.8841112022837));
#18965=CARTESIAN_POINT('Ctrl Pts',(-4.63367019598387,3.68298792507418,31.876324973705));
#18966=CARTESIAN_POINT('Ctrl Pts',(-4.52883841529292,3.81115713334293,31.8685387451263));
#18967=CARTESIAN_POINT('Ctrl Pts',(-4.4188288244114,3.93470232457945,31.8607525165475));
#18968=CARTESIAN_POINT('Ctrl Pts',(-4.30879027390029,4.05828003864374,31.8529642382721));
#18969=CARTESIAN_POINT('Ctrl Pts',(-4.19357140074275,4.17723106323152,31.8451759599966));
#18970=CARTESIAN_POINT('Ctrl Pts',(-4.07358687765908,4.29113277732858,31.8373876817212));
#18971=CARTESIAN_POINT('Ctrl Pts',(-3.9595174753985,4.39941924719643,31.8299833580244));
#18972=CARTESIAN_POINT('Ctrl Pts',(-3.84114117931065,4.50314208483321,31.8225790343276));
#18973=CARTESIAN_POINT('Ctrl Pts',(-3.7188439169604,4.60197028280134,31.8151747106308));
#18974=CARTESIAN_POINT('Ctrl Pts',(-3.59020983794156,4.70591925093371,31.8073867328691));
#18975=CARTESIAN_POINT('Ctrl Pts',(-3.45719166119068,4.80449006697312,31.7995987551075));
#18976=CARTESIAN_POINT('Ctrl Pts',(-3.32026101966087,4.89732552765492,31.7918107773458));
#18977=CARTESIAN_POINT('Ctrl Pts',(-3.18335729986928,4.99014273608914,31.7840243307673));
#18978=CARTESIAN_POINT('Ctrl Pts',(-3.04254291445834,5.07722665989015,31.7762378841889));
#18979=CARTESIAN_POINT('Ctrl Pts',(-2.89831913661993,5.15826295808993,31.7684514376104));
#18980=CARTESIAN_POINT('Ctrl Pts',(-2.75408985696947,5.23930234764184,31.7606646939966));
#18981=CARTESIAN_POINT('Ctrl Pts',(-2.60645120127714,5.31429348997774,31.7528779503828));
#18982=CARTESIAN_POINT('Ctrl Pts',(-2.45593039287091,5.38296725495083,31.7450912067689));
#18983=CARTESIAN_POINT('Ctrl Pts',(-2.30541954029006,5.45163647766815,31.7373049781899));
#18984=CARTESIAN_POINT('Ctrl Pts',(-2.15202720727318,5.51398902665044,31.7295187496109));
#18985=CARTESIAN_POINT('Ctrl Pts',(-1.99630214167263,5.5698032569969,31.7217325210319));
#18986=CARTESIAN_POINT('Ctrl Pts',(-1.84053608200802,5.62563218023898,31.7139442427562));
#18987=CARTESIAN_POINT('Ctrl Pts',(-1.68243636304442,5.67491923581839,31.7061559644805));
#18988=CARTESIAN_POINT('Ctrl Pts',(-1.52256936078756,5.71749185430911,31.6983676862048));
#18989=CARTESIAN_POINT('Ctrl Pts',(-1.37058364699569,5.75796568391719,31.6909633625092));
#18990=CARTESIAN_POINT('Ctrl Pts',(-1.21700095777804,5.79237109173358,31.6835590388137));
#18991=CARTESIAN_POINT('Ctrl Pts',(-1.06231857857277,5.82060218535154,31.6761547151182));
#18992=CARTESIAN_POINT('Ctrl Pts',(-0.899621352077626,5.85029606940069,
31.6683667373567));
#18993=CARTESIAN_POINT('Ctrl Pts',(-0.735649249453548,5.87316943120378,
31.6605787595953));
#18994=CARTESIAN_POINT('Ctrl Pts',(-0.570987344243469,5.88913440288246,
31.6527907818339));
#18995=CARTESIAN_POINT('Ctrl Pts',(-0.406357812975587,5.90509623571085,
31.6450043352556));
#18996=CARTESIAN_POINT('Ctrl Pts',(-0.24103906758913,5.91415235770217,31.6372178886774));
#18997=CARTESIAN_POINT('Ctrl Pts',(-0.0756216888676104,5.91626672173194,
31.6294314420992));
#18998=CARTESIAN_POINT('Ctrl Pts',(0.0898020001540977,5.91838116641994,
31.6216446984855));
#18999=CARTESIAN_POINT('Ctrl Pts',(0.255324010577674,5.91355331521411,31.6138579548719));
#19000=CARTESIAN_POINT('Ctrl Pts',(0.420352618437727,5.90179923740825,31.6060712112583));
#19001=CARTESIAN_POINT('Ctrl Pts',(0.58537031089004,5.89004593704669,31.5982849826795));
#19002=CARTESIAN_POINT('Ctrl Pts',(0.749894347324935,5.87136734966515,31.5904987541007));
#19003=CARTESIAN_POINT('Ctrl Pts',(0.913336834958877,5.84583153951662,31.5827125255219));
#19004=CARTESIAN_POINT('Ctrl Pts',(1.0768223482404,5.82028900715783,31.5749242472464));
#19005=CARTESIAN_POINT('Ctrl Pts',(1.23922542757045,5.78788569241109,31.5671359689709));
#19006=CARTESIAN_POINT('Ctrl Pts',(1.39996619353742,5.74874118563815,31.5593476906954));
#19007=CARTESIAN_POINT('Ctrl Pts',(1.55278259536065,5.71152646515204,31.5519433669988));
#19008=CARTESIAN_POINT('Ctrl Pts',(1.70409638054876,5.66821927252212,31.5445390433023));
#19009=CARTESIAN_POINT('Ctrl Pts',(1.85342024706657,5.61896466889263,31.5371347196057));
#19010=CARTESIAN_POINT('Ctrl Pts',(2.0104813102203,5.56715794441072,31.529346741844));
#19011=CARTESIAN_POINT('Ctrl Pts',(2.16539694881891,5.50875258474142,31.5215587640824));
#19012=CARTESIAN_POINT('Ctrl Pts',(2.31761141094465,5.44395149779635,31.5137707863208));
#19013=CARTESIAN_POINT('Ctrl Pts',(2.46979594640208,5.37916315130057,31.5059843397424));
#19014=CARTESIAN_POINT('Ctrl Pts',(2.61928007120168,5.30798171161369,31.498197893164));
#19015=CARTESIAN_POINT('Ctrl Pts',(2.76552800299021,5.23065822121623,31.4904114465855));
#19016=CARTESIAN_POINT('Ctrl Pts',(2.91178151380771,5.1533317811019,31.4826247029717));
#19017=CARTESIAN_POINT('Ctrl Pts',(3.05479830024734,5.06986296728665,31.4748379593579));
#19018=CARTESIAN_POINT('Ctrl Pts',(3.19406652267289,4.98054912747985,31.4670512157441));
#19019=CARTESIAN_POINT('Ctrl Pts',(3.3333255335475,4.89124119511534,31.4592649871651));
#19020=CARTESIAN_POINT('Ctrl Pts',(3.46883620762272,4.79608918302724,31.4514787585862));
#19021=CARTESIAN_POINT('Ctrl Pts',(3.6001149573141,4.69543425644778,31.4436925300072));
#19022=CARTESIAN_POINT('Ctrl Pts',(3.73142826566444,4.59475283282071,31.4359042517315));
#19023=CARTESIAN_POINT('Ctrl Pts',(3.85850716859779,4.48856579306073,31.4281159734559));
#19024=CARTESIAN_POINT('Ctrl Pts',(3.98089977810571,4.37725570639618,31.4203276951802));
#19025=CARTESIAN_POINT('Ctrl Pts',(4.09725855044077,4.27143309925618,31.4129233714845));
#19026=CARTESIAN_POINT('Ctrl Pts',(4.20938176350715,4.16098057729643,31.4055190477888));
#19027=CARTESIAN_POINT('Ctrl Pts',(4.31691100392656,4.04625875923398,31.3981147240931));
#19028=CARTESIAN_POINT('Ctrl Pts',(4.4300118579012,3.92559264514468,31.3903267463317));
#19029=CARTESIAN_POINT('Ctrl Pts',(4.53807048588826,3.80015989807773,31.3825387685702));
#19030=CARTESIAN_POINT('Ctrl Pts',(4.64069606511964,3.67040469072323,31.3747507908088));
#19031=CARTESIAN_POINT('Ctrl Pts',(4.7433014672825,3.54067499435469,31.3669643442305));
#19032=CARTESIAN_POINT('Ctrl Pts',(4.84047575392274,3.40662478384465,31.3591778976523));
#19033=CARTESIAN_POINT('Ctrl Pts',(4.93186867592241,3.26873093508097,31.351391451074));
#19034=CARTESIAN_POINT('Ctrl Pts',(5.02326508435588,3.13083182597805,31.3436047074604));
#19035=CARTESIAN_POINT('Ctrl Pts',(5.10887950700577,2.98908904938508,31.3358179638468));
#19036=CARTESIAN_POINT('Ctrl Pts',(5.18840488117236,2.84400867641553,31.3280312202332));
#19037=CARTESIAN_POINT('Ctrl Pts',(5.26792499533063,2.69893789942685,31.3202449916543));
#19038=CARTESIAN_POINT('Ctrl Pts',(5.3413567134468,2.55053024812114,31.3124587630755));
#19039=CARTESIAN_POINT('Ctrl Pts',(5.40843875203596,2.39931674190294,31.3046725344967));
#19040=CARTESIAN_POINT('Ctrl Pts',(5.4755384497306,2.24806342927286,31.2968842562212));
#19041=CARTESIAN_POINT('Ctrl Pts',(5.53628499637266,2.09400307728836,31.2890959779457));
#19042=CARTESIAN_POINT('Ctrl Pts',(5.59046475932937,1.93768788436022,31.2813076996702));
#19043=CARTESIAN_POINT('Ctrl Pts',(5.641973512425,1.78907887911106,31.2739033759737));
#19044=CARTESIAN_POINT('Ctrl Pts',(5.68754727099459,1.63843224937503,31.2664990522772));
#19045=CARTESIAN_POINT('Ctrl Pts',(5.72704396579689,1.48623617784303,31.2590947285807));
#19046=CARTESIAN_POINT('Ctrl Pts',(5.76858717668051,1.32615408674753,31.2513067508191));
#19047=CARTESIAN_POINT('Ctrl Pts',(5.80342170008898,1.16430045812298,31.2435187730576));
#19048=CARTESIAN_POINT('Ctrl Pts',(5.83141700601195,1.0012523480595,31.235730795296));
#19049=CARTESIAN_POINT('Ctrl Pts',(5.85940680781769,0.838236294652721,31.2279443487177));
#19050=CARTESIAN_POINT('Ctrl Pts',(5.8805600210661,0.674026543140648,31.2201579021394));
#19051=CARTESIAN_POINT('Ctrl Pts',(5.89479739321582,0.509209441621024,31.212371455561));
#19052=CARTESIAN_POINT('Ctrl Pts',(5.90903530848922,0.344386052700126,31.2045847119473));
#19053=CARTESIAN_POINT('Ctrl Pts',(5.91635682330807,0.178955585423101,31.1967979683336));
#19054=CARTESIAN_POINT('Ctrl Pts',(5.91673457744916,0.0135093492618925,
31.1890112247198));
#19055=CARTESIAN_POINT('Ctrl Pts',(5.91711230660464,-0.151925943868504,
31.1812249961409));
#19056=CARTESIAN_POINT('Ctrl Pts',(5.91054719354971,-0.317376684219718,
31.173438767562));
#19057=CARTESIAN_POINT('Ctrl Pts',(5.89706401397647,-0.482251570825563,
31.1656525389831));
#19058=CARTESIAN_POINT('Ctrl Pts',(5.88357728500462,-0.647169860153286,
31.1578642607075));
#19059=CARTESIAN_POINT('Ctrl Pts',(5.86316887457396,-0.811511673965455,
31.1500759824319));
#19060=CARTESIAN_POINT('Ctrl Pts',(5.83591553334913,-0.974689925111726,
31.1422877041563));
#19061=CARTESIAN_POINT('Ctrl Pts',(5.81000575546414,-1.12982364644094,31.1348833804602));
#19062=CARTESIAN_POINT('Ctrl Pts',(5.77790972978252,-1.28390550667541,31.1274790567642));
#19063=CARTESIAN_POINT('Ctrl Pts',(5.73973639713207,-1.43643887929052,31.1200747330681));
#19064=CARTESIAN_POINT('Ctrl Pts',(5.69958511823431,-1.59687574869264,31.1122867553065));
#19065=CARTESIAN_POINT('Ctrl Pts',(5.65269565908585,-1.7556567920871,31.1044987775449));
#19066=CARTESIAN_POINT('Ctrl Pts',(5.59922963270945,-1.91221287588188,31.0967107997832));
#19067=CARTESIAN_POINT('Ctrl Pts',(5.54577411821231,-2.06873817940807,31.0889243532048));
#19068=CARTESIAN_POINT('Ctrl Pts',(5.48574471963275,-2.22303909395251,31.0811379066263));
#19069=CARTESIAN_POINT('Ctrl Pts',(5.41935251920459,-2.37456287242324,31.0733514600479));
#19070=CARTESIAN_POINT('Ctrl Pts',(5.35295778606354,-2.52609243118478,31.0655647164341));
#19071=CARTESIAN_POINT('Ctrl Pts',(5.28019988999216,-2.67484434761829,31.0577779728203));
#19072=CARTESIAN_POINT('Ctrl Pts',(5.20133784933792,-2.82028635772057,31.0499912292064));
#19073=CARTESIAN_POINT('Ctrl Pts',(5.12248102481789,-2.9657187479216,31.0422050006275));
#19074=CARTESIAN_POINT('Ctrl Pts',(5.03752101609575,-3.10784138901246,31.0344187720485));
#19075=CARTESIAN_POINT('Ctrl Pts',(4.94676261259091,-3.24614698021713,31.0266325434695));
#19076=CARTESIAN_POINT('Ctrl Pts',(4.85598031726238,-3.38448897987184,31.0188442651938));
#19077=CARTESIAN_POINT('Ctrl Pts',(4.75939675086768,-3.51901165337453,31.0110559869182));
#19078=CARTESIAN_POINT('Ctrl Pts',(4.65736031964647,-3.64923627838519,31.0032677086425));
#19079=CARTESIAN_POINT('Ctrl Pts',(4.56035418571463,-3.77304095543843,30.9958633849469));
#19080=CARTESIAN_POINT('Ctrl Pts',(4.4584200403325,-3.8929609476009,30.9884590612512));
#19081=CARTESIAN_POINT('Ctrl Pts',(4.35189125203963,-4.00861236501123,30.9810547375556));
#19082=CARTESIAN_POINT('Ctrl Pts',(4.23984268848743,-4.13025624551777,30.9732667597942));
#19083=CARTESIAN_POINT('Ctrl Pts',(4.12267061707401,-4.24722097011238,30.9654787820328));
#19084=CARTESIAN_POINT('Ctrl Pts',(4.00078935909797,-4.35908420045179,30.9576908042715));
#19085=CARTESIAN_POINT('Ctrl Pts',(3.87893206402275,-4.47092543752055,30.9499043576933));
#19086=CARTESIAN_POINT('Ctrl Pts',(3.75236766504075,-4.57766696566869,30.9421179111152));
#19087=CARTESIAN_POINT('Ctrl Pts',(3.62154607355516,-4.67892451313518,30.934331464537));
#19088=CARTESIAN_POINT('Ctrl Pts',(3.49071949152024,-4.78018592334923,30.9265447209235));
#19089=CARTESIAN_POINT('Ctrl Pts',(3.35563564228066,-4.87596273555414,30.9187579773099));
#19090=CARTESIAN_POINT('Ctrl Pts',(3.21677672038713,-4.96591160751734,30.9109712336963));
#19091=CARTESIAN_POINT('Ctrl Pts',(3.07792698297249,-5.05585453003556,30.9031850051176));
#19092=CARTESIAN_POINT('Ctrl Pts',(2.93530294085811,-5.13997011005445,30.8953987765389));
#19093=CARTESIAN_POINT('Ctrl Pts',(2.7894150263476,-5.21795883208043,30.8876125479601));
#19094=CARTESIAN_POINT('Ctrl Pts',(2.64348870736769,-5.29596808435732,30.8798242696847));
#19095=CARTESIAN_POINT('Ctrl Pts',(2.49429708019934,-5.36784710330527,30.8720359914093));
#19096=CARTESIAN_POINT('Ctrl Pts',(2.34237519299164,-5.43334234313994,30.8642477131339));
#19097=CARTESIAN_POINT('Ctrl Pts',(2.19794290773552,-5.49560873106195,30.856843389437));
#19098=CARTESIAN_POINT('Ctrl Pts',(2.05104331813828,-5.55210550176354,30.8494390657401));
#19099=CARTESIAN_POINT('Ctrl Pts',(1.90215287609457,-5.60265517397467,30.8420347420432));
#19100=CARTESIAN_POINT('Ctrl Pts',(1.74554769525376,-5.65582407084546,30.8342467642815));
#19101=CARTESIAN_POINT('Ctrl Pts',(1.58668385225636,-5.70243223009608,30.8264587865199));
#19102=CARTESIAN_POINT('Ctrl Pts',(1.42612727925578,-5.74230716227045,30.8186708087582));
#19103=CARTESIAN_POINT('Ctrl Pts',(1.26560227305297,-5.78217425469154,30.8108843621797));
#19104=CARTESIAN_POINT('Ctrl Pts',(1.10338551082985,-5.8153106844528,30.8030979156012));
#19105=CARTESIAN_POINT('Ctrl Pts',(0.940055951492666,-5.84159442023864,
30.7953114690227));
#19106=CARTESIAN_POINT('Ctrl Pts',(0.776720161501561,-5.86787915868966,
30.7875247254089));
#19107=CARTESIAN_POINT('Ctrl Pts',(0.61227180430364,-5.8873106253971,30.779737981795));
#19108=CARTESIAN_POINT('Ctrl Pts',(0.447298591662922,-5.89981817790992,
30.7719512381812));
#19109=CARTESIAN_POINT('Ctrl Pts',(0.282336290765825,-5.91232490314173,
30.7641650096022));
#19110=CARTESIAN_POINT('Ctrl Pts',(0.116849522567173,-5.9179086065891,30.7563787810232));
#19111=CARTESIAN_POINT('Ctrl Pts',(-0.0485701869529832,-5.9165506420075,
30.7485925524441));
#19112=CARTESIAN_POINT('Ctrl Pts',(-0.21403344261702,-5.9151923199466,30.7408042741684));
#19113=CARTESIAN_POINT('Ctrl Pts',(-0.379429284559895,-5.9068886790572,
30.7330159958927));
#19114=CARTESIAN_POINT('Ctrl Pts',(-0.544166578376835,-5.8916732171326,
30.725227717617));
#19115=CARTESIAN_POINT('Ctrl Pts',(-0.70078248306895,-5.87720786275282,
30.7178233939215));
#19116=CARTESIAN_POINT('Ctrl Pts',(-0.856802944722839,-5.85649578754204,
30.710419070226));
#19117=CARTESIAN_POINT('Ctrl Pts',(-1.0117246858293,-5.82960922554708,30.7030147465305));
#19118=CARTESIAN_POINT('Ctrl Pts',(-1.17467367673134,-5.80132953985149,
30.6952267687691));
#19119=CARTESIAN_POINT('Ctrl Pts',(-1.33646535403249,-5.76620840269573,
30.6874387910077));
#19120=CARTESIAN_POINT('Ctrl Pts',(-1.49652026630087,-5.72436526219727,
30.6796508132462));
#19121=CARTESIAN_POINT('Ctrl Pts',(-1.65654371040109,-5.68253034841901,
30.671864366668));
#19122=CARTESIAN_POINT('Ctrl Pts',(-1.81483076181751,-5.63397614906018,
30.6640779200898));
#19123=CARTESIAN_POINT('Ctrl Pts',(-1.97081468433998,-5.57887264978238,
30.6562914735116));
#19124=CARTESIAN_POINT('Ctrl Pts',(-2.12680455729794,-5.52376704843013,
30.648504729898));
#19125=CARTESIAN_POINT('Ctrl Pts',(-2.28049082294545,-5.46211174992959,
30.6407179862844));
#19126=CARTESIAN_POINT('Ctrl Pts',(-2.43132365826553,-5.39412604888487,
30.6329312426708));
#19127=CARTESIAN_POINT('Ctrl Pts',(-2.58214651712199,-5.32614484458566,
30.625145014092));
#19128=CARTESIAN_POINT('Ctrl Pts',(-2.73011603203206,-5.2518342070657,30.6173587855132));
#19129=CARTESIAN_POINT('Ctrl Pts',(-2.87470391999606,-5.1714609091493,30.6095725569345));
#19130=CARTESIAN_POINT('Ctrl Pts',(-3.0193298702023,-5.09106645325087,30.601784278659));
#19131=CARTESIAN_POINT('Ctrl Pts',(-3.16057213421785,-5.00460630151462,
30.5939960003835));
#19132=CARTESIAN_POINT('Ctrl Pts',(-3.29792773249191,-4.91239282160545,
30.586207722108));
#19133=CARTESIAN_POINT('Ctrl Pts',(-3.4285118327504,-4.82472537698032,30.5788033984114));
#19134=CARTESIAN_POINT('Ctrl Pts',(-3.55558303503887,-4.73185835338873,
30.5713990747147));
#19135=CARTESIAN_POINT('Ctrl Pts',(-3.67873403961881,-4.63409607455972,
30.5639947510181));
#19136=CARTESIAN_POINT('Ctrl Pts',(-3.80826609741086,-4.53126825602626,
30.5562067732565));
#19137=CARTESIAN_POINT('Ctrl Pts',(-3.93350725881053,-4.42298763628546,
30.5484187954949));
#19138=CARTESIAN_POINT('Ctrl Pts',(-4.05400594348632,-4.30963645481584,
30.5406308177334));
#19139=CARTESIAN_POINT('Ctrl Pts',(-4.174480937088,-4.19630755915994,30.532844371155));
#19140=CARTESIAN_POINT('Ctrl Pts',(-4.29021508179072,-4.07791030972912,
30.5250579245766));
#19141=CARTESIAN_POINT('Ctrl Pts',(-4.40079215185238,-3.95486523141996,
30.5172714779982));
#19142=CARTESIAN_POINT('Ctrl Pts',(-4.51137344017982,-3.83181545921865,
30.5094847343844));
#19143=CARTESIAN_POINT('Ctrl Pts',(-4.61679704367759,-3.70411773837552,
30.5016979907706));
#19144=CARTESIAN_POINT('Ctrl Pts',(-4.71668518890512,-3.57222779106583,
30.4939112471568));
#19145=CARTESIAN_POINT('Ctrl Pts',(-4.81656672727858,-3.44034656729019,
30.486125018578));
#19146=CARTESIAN_POINT('Ctrl Pts',(-4.91091334720752,-3.30427392676269,
30.4783387899991));
#19147=CARTESIAN_POINT('Ctrl Pts',(-4.99938891358065,-3.16449696686011,
30.4705525614202));
#19148=CARTESIAN_POINT('Ctrl Pts',(-5.08788777082924,-3.02468321117427,
30.4627642831445));
#19149=CARTESIAN_POINT('Ctrl Pts',(-5.1705123135461,-2.88116345669998,30.4549760048689));
#19150=CARTESIAN_POINT('Ctrl Pts',(-5.24697044771608,-2.73445272098352,
30.4471877265933));
#19151=CARTESIAN_POINT('Ctrl Pts',(-5.31965926988517,-2.59497468251761,
30.4397834028974));
#19152=CARTESIAN_POINT('Ctrl Pts',(-5.38677491189971,-2.45261294217291,
30.4323790792014));
#19153=CARTESIAN_POINT('Ctrl Pts',(-5.44810543590136,-2.30782965614928,
30.4249747555055));
#19154=CARTESIAN_POINT('Ctrl Pts',(-5.51236203188601,-2.15613877682301,
30.4172171724094));
#19155=CARTESIAN_POINT('Ctrl Pts',(-5.5702925797576,-2.00173137472667,30.4094595893134));
#19156=CARTESIAN_POINT('Ctrl Pts',(-5.62168432073377,-1.84515472535939,
30.4017020062173));
#19157=CARTESIAN_POINT('Ctrl Pts',(-5.67306999690491,-1.68859655380263,
30.3939453386035));
#19158=CARTESIAN_POINT('Ctrl Pts',(-5.71791830102514,-1.52986995280867,
30.3861886709897));
#19159=CARTESIAN_POINT('Ctrl Pts',(-5.75606577235692,-1.3695391147394,30.378432003376));
#19160=CARTESIAN_POINT('Ctrl Pts',(-5.79420809090005,-1.20922993343773,
30.3706763834979));
#19161=CARTESIAN_POINT('Ctrl Pts',(-5.82565130915184,-1.04731726351005,
30.3629207636199));
#19162=CARTESIAN_POINT('Ctrl Pts',(-5.85028264031402,-0.884377516075805,
30.3551651437418));
#19163=CARTESIAN_POINT('Ctrl Pts',(-5.87491763671083,-0.721413522594905,
30.3474083697984));
#19164=CARTESIAN_POINT('Ctrl Pts',(-5.89273866988787,-0.557422466907766,
30.3396515958549));
#19165=CARTESIAN_POINT('Ctrl Pts',(-5.90368448065427,-0.392988696252073,
30.3318948219115));
#19166=CARTESIAN_POINT('Ctrl Pts',(-5.91239567784829,-0.262124475034702,
30.3257216120093));
#19167=CARTESIAN_POINT('Ctrl Pts',(-5.91675329104785,-0.130980059209622,
30.3195484021071));
#19168=CARTESIAN_POINT('Ctrl Pts',(-5.9167499981344,0.000148581922998542,
30.3133751922049));
#19169=CARTESIAN_POINT('Ctrl Pts',(-5.9164103286161,0.000118042167123383,
30.0616248077951));
#19170=CARTESIAN_POINT('Ctrl Pts',(-5.91595291218416,-0.635441998150383,
30.0915384074875));
#19171=CARTESIAN_POINT('Ctrl Pts',(-5.65595799765652,-2.255409947711,30.1677674689416));
#19172=CARTESIAN_POINT('Ctrl Pts',(-4.20296797278849,-4.51411130265866,
30.2903119921576));
#19173=CARTESIAN_POINT('Ctrl Pts',(-1.53101208436,-5.97479226673378,30.4292583774426));
#19174=CARTESIAN_POINT('Ctrl Pts',(1.51413465494195,-5.97909164336706,30.5682047627277));
#19175=CARTESIAN_POINT('Ctrl Pts',(4.19020449015913,-4.52596144081387,30.7071511480129));
#19176=CARTESIAN_POINT('Ctrl Pts',(5.84489376607425,-1.96960846270841,30.8460975332978));
#19177=CARTESIAN_POINT('Ctrl Pts',(6.07486477875718,1.06684514007426,30.9850439185832));
#19178=CARTESIAN_POINT('Ctrl Pts',(4.82406109417456,3.84325060238692,31.1239903038682));
#19179=CARTESIAN_POINT('Ctrl Pts',(2.39737154769186,5.68284702375448,31.2629366891533));
#19180=CARTESIAN_POINT('Ctrl Pts',(-0.613687734916818,6.13722477974293,
31.4018830744384));
#19181=CARTESIAN_POINT('Ctrl Pts',(-3.47515796443823,5.09562731714936,31.5408294597237));
#19182=CARTESIAN_POINT('Ctrl Pts',(-5.45524486659344,2.8508322079064,31.6774100375091));
#19183=CARTESIAN_POINT('Ctrl Pts',(-5.9167884154252,0.93335663078454,31.767675153533));
#19184=CARTESIAN_POINT('Ctrl Pts',(-5.91722096325101,-5.21647111771487E-5,
31.8116248077951));
#19185=CARTESIAN_POINT('Origin',(0.,0.,0.));
#19186=CARTESIAN_POINT('',(-5.91674999904992,0.000106031776716273,33.8133751922049));
#19187=CARTESIAN_POINT('',(-5.91670774978332,-3.97126980083329E-5,33.56162480823));
#19188=CARTESIAN_POINT('',(-5.91675,-7.2459289488551E-16,0.));
#19189=CARTESIAN_POINT('Ctrl Pts',(-5.91636959244526,0.000106239940256803,
33.8133751820867));
#19190=CARTESIAN_POINT('Ctrl Pts',(-5.9166048932696,0.367823780660049,33.7960683373264));
#19191=CARTESIAN_POINT('Ctrl Pts',(-5.79252506850152,1.71996775282403,33.7324214940625));
#19192=CARTESIAN_POINT('Ctrl Pts',(-4.77454453173828,3.90502535320764,33.622434652293));
#19193=CARTESIAN_POINT('Ctrl Pts',(-2.32282463106996,5.71401647075006,33.4834146567811));
#19194=CARTESIAN_POINT('Ctrl Pts',(0.695681434355644,6.12874586164393,33.3443946612684));
#19195=CARTESIAN_POINT('Ctrl Pts',(3.54443615188194,5.04801652730713,33.2053746657559));
#19196=CARTESIAN_POINT('Ctrl Pts',(5.52832257676672,2.73553431378993,33.0663546702434));
#19197=CARTESIAN_POINT('Ctrl Pts',(6.16325794055338,-0.244438239528186,
32.9273346747308));
#19198=CARTESIAN_POINT('Ctrl Pts',(5.29431337994305,-3.16476607819079,32.7883146792184));
#19199=CARTESIAN_POINT('Ctrl Pts',(3.13351771033575,-5.31286789349685,32.6492946837058));
#19200=CARTESIAN_POINT('Ctrl Pts',(0.208120847213036,-6.16459116305909,
32.5102746881934));
#19201=CARTESIAN_POINT('Ctrl Pts',(-2.76805902175141,-5.51210919220924,
32.3712546926806));
#19202=CARTESIAN_POINT('Ctrl Pts',(-5.06881228476578,-3.51463234443077,
32.2322346971683));
#19203=CARTESIAN_POINT('Ctrl Pts',(-5.85421735044904,-1.40697777682088,
32.1296081970096));
#19204=CARTESIAN_POINT('Ctrl Pts',(-5.91701880353749,-0.211440859014669,
32.0733216953552));
#19205=CARTESIAN_POINT('Ctrl Pts',(-5.91680012105169,-0.000152224731632677,
32.0633751922049));
#19206=CARTESIAN_POINT('Ctrl Pts',(-5.91722096325101,-5.21647111771487E-5,
31.8116248077951));
#19207=CARTESIAN_POINT('Ctrl Pts',(-5.91724424727696,-0.050297509426912,
31.8139906152947));
#19208=CARTESIAN_POINT('Ctrl Pts',(-5.90434996303826,-1.08418501485665,
31.8626718845569));
#19209=CARTESIAN_POINT('Ctrl Pts',(-5.33916643390619,-3.0879511693204,31.9576686155781));
#19210=CARTESIAN_POINT('Ctrl Pts',(-3.21105918801344,-5.2660459098046,32.0966150008645));
#19211=CARTESIAN_POINT('Ctrl Pts',(-0.300242306566234,-6.16051906826172,
32.235561386149));
#19212=CARTESIAN_POINT('Ctrl Pts',(2.6837599422594,-5.55333892405331,32.3745077714344));
#19213=CARTESIAN_POINT('Ctrl Pts',(5.01358403885356,-3.59250827673778,32.5134541567195));
#19214=CARTESIAN_POINT('Ctrl Pts',(6.1213252319243,-0.755988120332833,32.6524005420046));
#19215=CARTESIAN_POINT('Ctrl Pts',(5.7369667903094,2.26480742668442,32.7913469272897));
#19216=CARTESIAN_POINT('Ctrl Pts',(3.95419775495737,4.73354631832987,32.9302933125749));
#19217=CARTESIAN_POINT('Ctrl Pts',(1.20757582793818,6.04846271814959,33.06923969786));
#19218=CARTESIAN_POINT('Ctrl Pts',(-1.8333979564773,5.889040037754,33.2081860831451));
#19219=CARTESIAN_POINT('Ctrl Pts',(-4.42747301921854,4.29413824849268,33.3471324684302));
#19220=CARTESIAN_POINT('Ctrl Pts',(-5.71192511593987,2.05430638991628,33.4649453766469));
#19221=CARTESIAN_POINT('Ctrl Pts',(-5.91613373494868,0.535029129699535,
33.5364428231019));
#19222=CARTESIAN_POINT('Ctrl Pts',(-5.9162590580326,-3.97004485813632E-5,
33.5616248077952));
#19223=CARTESIAN_POINT('Origin',(0.,0.,0.));
#19224=CARTESIAN_POINT('',(-5.91674999986659,-3.97331449317638E-5,35.5633751921781));
#19225=CARTESIAN_POINT('',(-5.91674999872832,0.00012267210750124,35.3116248077951));
#19226=CARTESIAN_POINT('',(-5.91675,-7.2459289488551E-16,0.));
#19227=CARTESIAN_POINT('Ctrl Pts',(-5.91674999986659,-3.97331450085524E-5,
35.5633751921782));
#19228=CARTESIAN_POINT('Ctrl Pts',(-5.91675110866355,0.165073659927082,
35.5556001046463));
#19229=CARTESIAN_POINT('Ctrl Pts',(-5.9098363688167,0.330218136453832,35.5478250171145));
#19230=CARTESIAN_POINT('Ctrl Pts',(-5.89602402821719,0.494804225108879,
35.5400499295826));
#19231=CARTESIAN_POINT('Ctrl Pts',(-5.88221443243717,0.659357606844919,
35.5322763871337));
#19232=CARTESIAN_POINT('Ctrl Pts',(-5.86150999764133,0.823352501753403,
35.5245028446848));
#19233=CARTESIAN_POINT('Ctrl Pts',(-5.83398094014339,0.986203301831642,
35.5167293022359));
#19234=CARTESIAN_POINT('Ctrl Pts',(-5.8064510162699,1.1490592270382,35.5089555151434));
#19235=CARTESIAN_POINT('Ctrl Pts',(-5.77209608983898,1.31077066758484,35.501181728051));
#19236=CARTESIAN_POINT('Ctrl Pts',(-5.73103784694762,1.47076026576528,35.4934079409585));
#19237=CARTESIAN_POINT('Ctrl Pts',(-5.68998178598665,1.63074136172688,35.4856345669831));
#19238=CARTESIAN_POINT('Ctrl Pts',(-5.6422232020614,1.78900048701338,35.4778611930077));
#19239=CARTESIAN_POINT('Ctrl Pts',(-5.58793423630245,1.94497340168418,35.4700878190323));
#19240=CARTESIAN_POINT('Ctrl Pts',(-5.53363178425725,2.10098506263328,35.4623125140209));
#19241=CARTESIAN_POINT('Ctrl Pts',(-5.47279581395889,2.25470907396168,35.4545372090096));
#19242=CARTESIAN_POINT('Ctrl Pts',(-5.40564767678358,2.40559841972517,35.4467619039982));
#19243=CARTESIAN_POINT('Ctrl Pts',(-5.35651613899646,2.51600245928474,35.4410728006508));
#19244=CARTESIAN_POINT('Ctrl Pts',(-5.30400629601034,2.62488925785952,35.4353836973035));
#19245=CARTESIAN_POINT('Ctrl Pts',(-5.24822092842375,2.73205191183385,35.4296945939561));
#19246=CARTESIAN_POINT('Ctrl Pts',(-5.17185472875216,2.87874996160537,35.4219066161947));
#19247=CARTESIAN_POINT('Ctrl Pts',(-5.08932027418793,3.02227036060439,35.4141186384333));
#19248=CARTESIAN_POINT('Ctrl Pts',(-5.00090712050078,3.16209717349493,35.4063306606719));
#19249=CARTESIAN_POINT('Ctrl Pts',(-4.91251134959801,3.30189649523468,35.3985442140937));
#19250=CARTESIAN_POINT('Ctrl Pts',(-4.81823935641177,3.43800340990853,35.3907577675155));
#19251=CARTESIAN_POINT('Ctrl Pts',(-4.71842499787582,3.56992942534171,35.3829713209373));
#19252=CARTESIAN_POINT('Ctrl Pts',(-4.61860683164668,3.70186047345553,35.3751845773237));
#19253=CARTESIAN_POINT('Ctrl Pts',(-4.5132460666387,3.82961004597432,35.3673978337101));
#19254=CARTESIAN_POINT('Ctrl Pts',(-4.40271841707057,3.95272072153948,35.3596110900965));
#19255=CARTESIAN_POINT('Ctrl Pts',(-4.2921980780796,4.07582325425445,35.3518248615177));
#19256=CARTESIAN_POINT('Ctrl Pts',(-4.17651175200243,4.19428726630036,35.344038632939));
#19257=CARTESIAN_POINT('Ctrl Pts',(-4.05607386264036,4.30769026083651,35.3362524043602));
#19258=CARTESIAN_POINT('Ctrl Pts',(-3.93560426843669,4.42112310830347,35.3284641260848));
#19259=CARTESIAN_POINT('Ctrl Pts',(-3.81038084298499,4.52949205542597,35.3206758478093));
#19260=CARTESIAN_POINT('Ctrl Pts',(-3.68085378363544,4.63241254488379,35.3128875695338));
#19261=CARTESIAN_POINT('Ctrl Pts',(-3.55771228290983,4.7302591538541,35.3054832458371));
#19262=CARTESIAN_POINT('Ctrl Pts',(-3.43068146302759,4.82318140803664,35.2980789221404));
#19263=CARTESIAN_POINT('Ctrl Pts',(-3.30017483892539,4.91088348416289,35.2906745984437));
#19264=CARTESIAN_POINT('Ctrl Pts',(-3.16290603114694,5.00312983190472,35.2828866206821));
#19265=CARTESIAN_POINT('Ctrl Pts',(-3.02174255568152,5.08963367179141,35.2750986429204));
#19266=CARTESIAN_POINT('Ctrl Pts',(-2.87718560282573,5.17008061536688,35.2673106651588));
#19267=CARTESIAN_POINT('Ctrl Pts',(-2.73265707110554,5.25051174238391,35.2595242185803));
#19268=CARTESIAN_POINT('Ctrl Pts',(-2.58473667228175,5.32488819386679,35.2517377720018));
#19269=CARTESIAN_POINT('Ctrl Pts',(-2.43395135676673,5.39294088187451,35.2439513254234));
#19270=CARTESIAN_POINT('Ctrl Pts',(-2.28316028913237,5.46099616593862,35.2361645818095));
#19271=CARTESIAN_POINT('Ctrl Pts',(-2.12950437573891,5.52272706875576,35.2283778381957));
#19272=CARTESIAN_POINT('Ctrl Pts',(-1.97353244495761,5.57791181816275,35.2205910945819));
#19273=CARTESIAN_POINT('Ctrl Pts',(-1.81757083055295,5.63309291751131,35.2128048660029));
#19274=CARTESIAN_POINT('Ctrl Pts',(-1.65929380662418,5.68172862341769,35.2050186374239));
#19275=CARTESIAN_POINT('Ctrl Pts',(-1.49926747118925,5.72364635633036,35.1972324088449));
#19276=CARTESIAN_POINT('Ctrl Pts',(-1.33919900939618,5.76557512393569,35.1894441305692));
#19277=CARTESIAN_POINT('Ctrl Pts',(-1.17738062475237,5.80078230182907,35.1816558522935));
#19278=CARTESIAN_POINT('Ctrl Pts',(-1.01439166391229,5.82914574484849,35.1738675740179));
#19279=CARTESIAN_POINT('Ctrl Pts',(-0.859437901071764,5.85611089758226,
35.1664632503223));
#19280=CARTESIAN_POINT('Ctrl Pts',(-0.70342645794359,5.87689079478672,35.1590589266267));
#19281=CARTESIAN_POINT('Ctrl Pts',(-0.546862000065591,5.89142364080061,
35.1516546029311));
#19282=CARTESIAN_POINT('Ctrl Pts',(-0.382185175238075,5.90670950433382,
35.1438666251696));
#19283=CARTESIAN_POINT('Ctrl Pts',(-0.216837597273207,5.91508921676225,
35.1360786474082));
#19284=CARTESIAN_POINT('Ctrl Pts',(-0.0514097969037414,5.91652664958777,
35.1282906696468));
#19285=CARTESIAN_POINT('Ctrl Pts',(0.113985478942169,5.91796379980169,35.1205042230685));
#19286=CARTESIAN_POINT('Ctrl Pts',(0.279460626380191,5.91246139103857,35.1127177764903));
#19287=CARTESIAN_POINT('Ctrl Pts',(0.44442418126637,5.90003539901293,35.104931329912));
#19288=CARTESIAN_POINT('Ctrl Pts',(0.609394029139934,5.88760893296375,35.0971445862984));
#19289=CARTESIAN_POINT('Ctrl Pts',(0.773851926476321,5.86825837520351,35.0893578426848));
#19290=CARTESIAN_POINT('Ctrl Pts',(0.937209848880338,5.84205171679109,35.0815710990711));
#19291=CARTESIAN_POINT('Ctrl Pts',(1.10055696638013,5.81584679175302,35.0737848704924));
#19292=CARTESIAN_POINT('Ctrl Pts',(1.26280393901722,5.78278672427633,35.0659986419136));
#19293=CARTESIAN_POINT('Ctrl Pts',(1.42337112660555,5.74299096276894,35.0582124133348));
#19294=CARTESIAN_POINT('Ctrl Pts',(1.58398058292904,5.70318472517032,35.0504241350593));
#19295=CARTESIAN_POINT('Ctrl Pts',(1.74290905975723,5.65663932544496,35.0426358567838));
#19296=CARTESIAN_POINT('Ctrl Pts',(1.89958942594384,5.60352483490011,35.0348475785083));
#19297=CARTESIAN_POINT('Ctrl Pts',(2.04854560176359,5.55302883731768,35.0274432548117));
#19298=CARTESIAN_POINT('Ctrl Pts',(2.19546973729231,5.49659593095798,35.0200389311152));
#19299=CARTESIAN_POINT('Ctrl Pts',(2.33988915846553,5.43441342635942,35.0126346074187));
#19300=CARTESIAN_POINT('Ctrl Pts',(2.4917916530807,5.36900894340825,35.0048466296571));
#19301=CARTESIAN_POINT('Ctrl Pts',(2.64097731762214,5.29721981738107,34.9970586518954));
#19302=CARTESIAN_POINT('Ctrl Pts',(2.78691037473011,5.219296995355,34.9892706741338));
#19303=CARTESIAN_POINT('Ctrl Pts',(2.93281474014825,5.14138949362361,34.9814842275554));
#19304=CARTESIAN_POINT('Ctrl Pts',(3.07546749239553,5.05735085251538,34.973697780977));
#19305=CARTESIAN_POINT('Ctrl Pts',(3.21435697516471,4.96747821320939,34.9659113343985));
#19306=CARTESIAN_POINT('Ctrl Pts',(3.35325175625443,4.8776021454649,34.9581245907847));
#19307=CARTESIAN_POINT('Ctrl Pts',(3.48838271017851,4.78189180446256,34.9503378471709));
#19308=CARTESIAN_POINT('Ctrl Pts',(3.61926609876232,4.68068835416863,34.9425511035571));
#19309=CARTESIAN_POINT('Ctrl Pts',(3.75014083038907,4.57949159772585,34.9347648749781));
#19310=CARTESIAN_POINT('Ctrl Pts',(3.8767683061429,4.4728026546396,34.9269786463992));
#19311=CARTESIAN_POINT('Ctrl Pts',(3.99869678010585,4.36100385499384,34.9191924178202));
#19312=CARTESIAN_POINT('Ctrl Pts',(4.12065735130146,4.24917562471578,34.9114041395445));
#19313=CARTESIAN_POINT('Ctrl Pts',(4.23791621192222,4.13223506464507,34.9036158612689));
#19314=CARTESIAN_POINT('Ctrl Pts',(4.35005683046932,4.01060296391792,34.8958275829932));
#19315=CARTESIAN_POINT('Ctrl Pts',(4.45666902507436,3.89496720801654,34.8884232592975));
#19316=CARTESIAN_POINT('Ctrl Pts',(4.55865529147366,3.77509153916883,34.8810189356017));
#19317=CARTESIAN_POINT('Ctrl Pts',(4.6556902829983,3.65136666897412,34.873614611906));
#19318=CARTESIAN_POINT('Ctrl Pts',(4.75775312994153,3.52123101078173,34.8658266341446));
#19319=CARTESIAN_POINT('Ctrl Pts',(4.85437448996887,3.38679011705594,34.8580386563831));
#19320=CARTESIAN_POINT('Ctrl Pts',(4.94520407268016,3.24852077753053,34.8502506786217));
#19321=CARTESIAN_POINT('Ctrl Pts',(5.03601579751637,3.11027862294332,34.8424642320434));
#19322=CARTESIAN_POINT('Ctrl Pts',(5.121037841767,2.96820979134034,34.8346777854652));
#19323=CARTESIAN_POINT('Ctrl Pts',(5.19996320483517,2.82282008474864,34.826891338887));
#19324=CARTESIAN_POINT('Ctrl Pts',(5.27889157872833,2.67742483186683,34.8191045952734));
#19325=CARTESIAN_POINT('Ctrl Pts',(5.35172265012908,2.52870872944132,34.8113178516598));
#19326=CARTESIAN_POINT('Ctrl Pts',(5.41819500272893,2.37720286784769,34.8035311080461));
#19327=CARTESIAN_POINT('Ctrl Pts',(5.48466295867994,2.22570702723337,34.7957448794673));
#19328=CARTESIAN_POINT('Ctrl Pts',(5.54477290918273,2.07142208940072,34.7879586508885));
#19329=CARTESIAN_POINT('Ctrl Pts',(5.59831123188888,1.91489997477854,34.7801724223098));
#19330=CARTESIAN_POINT('Ctrl Pts',(5.65186364836615,1.75833665627195,34.7723841440343));
#19331=CARTESIAN_POINT('Ctrl Pts',(5.69884087488843,1.59953528609254,34.7645958657588));
#19332=CARTESIAN_POINT('Ctrl Pts',(5.73907861633046,1.43906469558475,34.7568075874833));
#19333=CARTESIAN_POINT('Ctrl Pts',(5.77733267607449,1.28650514983369,34.7494032637867));
#19334=CARTESIAN_POINT('Ctrl Pts',(5.80949567994419,1.13243725667251,34.7419989400902));
#19335=CARTESIAN_POINT('Ctrl Pts',(5.83546899562796,0.977359792279616,34.7345946163937));
#19336=CARTESIAN_POINT('Ctrl Pts',(5.86278811527093,0.81424700932731,34.7268066386321));
#19337=CARTESIAN_POINT('Ctrl Pts',(5.88326885368145,0.649958907278902,34.7190186608704));
#19338=CARTESIAN_POINT('Ctrl Pts',(5.8968318808334,0.485081778349647,34.7112306831088));
#19339=CARTESIAN_POINT('Ctrl Pts',(5.91039224137791,0.320237065677669,34.7034442365304));
#19340=CARTESIAN_POINT('Ctrl Pts',(5.91703757824452,0.154803875474242,34.695657789952));
#19341=CARTESIAN_POINT('Ctrl Pts',(5.91674045693324,-0.0106267487721454,
34.6878713433735));
#19342=CARTESIAN_POINT('Ctrl Pts',(5.91644332428745,-0.176063683823728,
34.6800845997597));
#19343=CARTESIAN_POINT('Ctrl Pts',(5.90920320013566,-0.341497733176881,
34.672297856146));
#19344=CARTESIAN_POINT('Ctrl Pts',(5.89504477752286,-0.506337469974766,
34.6645111125322));
#19345=CARTESIAN_POINT('Ctrl Pts',(5.88088729138377,-0.671166303857542,
34.6567248839532));
#19346=CARTESIAN_POINT('Ctrl Pts',(5.85981244995845,-0.83540058545418,34.6489386553742));
#19347=CARTESIAN_POINT('Ctrl Pts',(5.83189687988024,-0.99845347660424,34.6411524267952));
#19348=CARTESIAN_POINT('Ctrl Pts',(5.80397396112855,-1.16154929084184,34.6333641485196));
#19349=CARTESIAN_POINT('Ctrl Pts',(5.76920676738394,-1.32346277768841,34.6255758702439));
#19350=CARTESIAN_POINT('Ctrl Pts',(5.72772332910448,-1.48361586259124,34.6177875919682));
#19351=CARTESIAN_POINT('Ctrl Pts',(5.68828498417602,-1.63587355543733,34.6103832682725));
#19352=CARTESIAN_POINT('Ctrl Pts',(5.64277671780008,-1.78653998237889,34.6029789445767));
#19353=CARTESIAN_POINT('Ctrl Pts',(5.59135067902643,-1.93513000768699,34.595574620881));
#19354=CARTESIAN_POINT('Ctrl Pts',(5.53726000676726,-2.09141920575841,34.5877866431195));
#19355=CARTESIAN_POINT('Ctrl Pts',(5.47660267389509,-2.24546702005026,34.5799986653581));
#19356=CARTESIAN_POINT('Ctrl Pts',(5.40958966786325,-2.39672071544583,34.5722106875966));
#19357=CARTESIAN_POINT('Ctrl Pts',(5.34258983716308,-2.54794467306778,34.5644242410184));
#19358=CARTESIAN_POINT('Ctrl Pts',(5.2692369559449,-2.69637531592374,34.5566377944402));
#19359=CARTESIAN_POINT('Ctrl Pts',(5.18978985002381,-2.8414805779892,34.548851347862));
#19360=CARTESIAN_POINT('Ctrl Pts',(5.1103397133744,-2.98659137549389,34.5410646042483));
#19361=CARTESIAN_POINT('Ctrl Pts',(5.02479503681166,-3.12837625618952,34.5332778606347));
#19362=CARTESIAN_POINT('Ctrl Pts',(4.93346059745086,-3.26632776920807,34.525491117021));
#19363=CARTESIAN_POINT('Ctrl Pts',(4.84213219917998,-3.40427015776601,34.5177048884422));
#19364=CARTESIAN_POINT('Ctrl Pts',(4.74501498096641,-3.53837941963102,34.5099186598634));
#19365=CARTESIAN_POINT('Ctrl Pts',(4.64245712096745,-3.66817699170564,34.5021324312846));
#19366=CARTESIAN_POINT('Ctrl Pts',(4.53987226298036,-3.79800873252471,34.4943441530091));
#19367=CARTESIAN_POINT('Ctrl Pts',(4.43184409801895,-3.92352626340246,34.4865558747336));
#19368=CARTESIAN_POINT('Ctrl Pts',(4.31876174175831,-4.04428332098837,34.4787675964581));
#19369=CARTESIAN_POINT('Ctrl Pts',(4.21125423618384,-4.15908717254282,34.4713632727616));
#19370=CARTESIAN_POINT('Ctrl Pts',(4.09917904872532,-4.26958842537327,34.4639589490651));
#19371=CARTESIAN_POINT('Ctrl Pts',(3.98290198431529,-4.37543396085889,34.4565546253686));
#19372=CARTESIAN_POINT('Ctrl Pts',(3.86060003900228,-4.48676386893895,34.448766647607));
#19373=CARTESIAN_POINT('Ctrl Pts',(3.73360546681623,-4.59298260436608,34.4409786698454));
#19374=CARTESIAN_POINT('Ctrl Pts',(3.60236809021128,-4.69370586052509,34.4331906920838));
#19375=CARTESIAN_POINT('Ctrl Pts',(3.47115651599929,-4.79440931362872,34.4254042455053));
#19376=CARTESIAN_POINT('Ctrl Pts',(3.33570405512727,-4.88961924886052,34.4176177989269));
#19377=CARTESIAN_POINT('Ctrl Pts',(3.19649263833734,-4.9789924056535,34.4098313523484));
#19378=CARTESIAN_POINT('Ctrl Pts',(3.05727591094641,-5.06836897183047,34.4020446087346));
#19379=CARTESIAN_POINT('Ctrl Pts',(2.9143002074586,-5.15190813806547,34.3942578651209));
#19380=CARTESIAN_POINT('Ctrl Pts',(2.76807602121874,-5.22931025119507,34.3864711215071));
#19381=CARTESIAN_POINT('Ctrl Pts',(2.6218615066143,-5.30670724475425,34.3786848929281));
#19382=CARTESIAN_POINT('Ctrl Pts',(2.47239922173012,-5.37796784810523,34.3708986643491));
#19383=CARTESIAN_POINT('Ctrl Pts',(2.32022393823567,-5.44283854610241,34.3631124357702));
#19384=CARTESIAN_POINT('Ctrl Pts',(2.16800859514482,-5.50772632107767,34.3553241574945));
#19385=CARTESIAN_POINT('Ctrl Pts',(2.01307911973145,-5.56622070227697,34.3475358792188));
#19386=CARTESIAN_POINT('Ctrl Pts',(1.85599076582274,-5.61811612906682,34.3397476009432));
#19387=CARTESIAN_POINT('Ctrl Pts',(1.70664671570023,-5.66745316155069,34.3323432772474));
#19388=CARTESIAN_POINT('Ctrl Pts',(1.55535177097899,-5.71082612798686,34.3249389535517));
#19389=CARTESIAN_POINT('Ctrl Pts',(1.40259613340041,-5.7481000903838,34.317534629856));
#19390=CARTESIAN_POINT('Ctrl Pts',(1.24192548240169,-5.78730539827653,34.3097466520945));
#19391=CARTESIAN_POINT('Ctrl Pts',(1.07958127347967,-5.8197769080782,34.3019586743331));
#19392=CARTESIAN_POINT('Ctrl Pts',(0.91614240412713,-5.84539251529443,34.2941706965716));
#19393=CARTESIAN_POINT('Ctrl Pts',(0.752735668256952,-5.87100308626276,
34.2863842499934));
#19394=CARTESIAN_POINT('Ctrl Pts',(0.588235016885216,-5.88976039471291,
34.2785978034151));
#19395=CARTESIAN_POINT('Ctrl Pts',(0.423227891062269,-5.90159374361934,
34.2708113568368));
#19396=CARTESIAN_POINT('Ctrl Pts',(0.258214470590112,-5.91342754394132,
34.2630246132232));
#19397=CARTESIAN_POINT('Ctrl Pts',(0.092694855442932,-5.91833682938305,
34.2552378696095));
#19398=CARTESIAN_POINT('Ctrl Pts',(-0.0727393089072741,-5.91630286204482,
34.2474511259959));
#19399=CARTESIAN_POINT('Ctrl Pts',(-0.238162531025157,-5.91426902923831,
34.2396648974171));
#19400=CARTESIAN_POINT('Ctrl Pts',(-0.403499994105207,-5.90529286671043,
34.2318786688383));
#19401=CARTESIAN_POINT('Ctrl Pts',(-0.568160821156598,-5.88940776681346,
34.2240924402595));
#19402=CARTESIAN_POINT('Ctrl Pts',(-0.732864994579319,-5.87351848522099,
34.216304161984));
#19403=CARTESIAN_POINT('Ctrl Pts',(-0.896891857574877,-5.85071666076646,
34.2085158837085));
#19404=CARTESIAN_POINT('Ctrl Pts',(-1.05965550415079,-5.8210875938284,34.200727605433));
#19405=CARTESIAN_POINT('Ctrl Pts',(-1.21439506052433,-5.79291921120607,
34.1933232817365));
#19406=CARTESIAN_POINT('Ctrl Pts',(-1.36799269169004,-5.75858057085879,
34.18591895804));
#19407=CARTESIAN_POINT('Ctrl Pts',(-1.51995341190027,-5.71818784127915,
34.1785146343436));
#19408=CARTESIAN_POINT('Ctrl Pts',(-1.67978795697809,-5.67570216769271,
34.170726656582));
#19409=CARTESIAN_POINT('Ctrl Pts',(-1.83786863068062,-5.62650316646222,
34.1629386788204));
#19410=CARTESIAN_POINT('Ctrl Pts',(-1.99362871569015,-5.57076072960198,
34.1551507010588));
#19411=CARTESIAN_POINT('Ctrl Pts',(-2.14935817693191,-5.51502925218261,
34.1473642544804));
#19412=CARTESIAN_POINT('Ctrl Pts',(-2.30276765914971,-5.45275701367609,
34.139577807902));
#19413=CARTESIAN_POINT('Ctrl Pts',(-2.45330755088909,-5.38416313118859,
34.1317913613236));
#19414=CARTESIAN_POINT('Ctrl Pts',(-2.60385318538635,-5.31556663199895,
34.1240046177098));
#19415=CARTESIAN_POINT('Ctrl Pts',(-2.75152871794123,-5.24064813516452,
34.1162178740959));
#19416=CARTESIAN_POINT('Ctrl Pts',(-2.89580571676823,-5.1596743902336,34.1084311304821));
#19417=CARTESIAN_POINT('Ctrl Pts',(-3.0400731727512,-5.07870600111008,34.1006449019031));
#19418=CARTESIAN_POINT('Ctrl Pts',(-3.18094226620991,-4.99168332187697,
34.0928586733242));
#19419=CARTESIAN_POINT('Ctrl Pts',(-3.31791019313083,-4.89891850440672,
34.0850724447452));
#19420=CARTESIAN_POINT('Ctrl Pts',(-3.45491417636605,-4.8061292669318,34.0772841664695));
#19421=CARTESIAN_POINT('Ctrl Pts',(-3.58801467511241,-4.70759504842265,
34.0694958881938));
#19422=CARTESIAN_POINT('Ctrl Pts',(-3.71673809655088,-4.60367119635485,
34.0617076099182));
#19423=CARTESIAN_POINT('Ctrl Pts',(-3.83911557791681,-4.50487068959563,
34.0543032862224));
#19424=CARTESIAN_POINT('Ctrl Pts',(-3.95753695235454,-4.40119932135926,
34.0468989625267));
#19425=CARTESIAN_POINT('Ctrl Pts',(-4.07162323024594,-4.29299602066222,
34.039494638831));
#19426=CARTESIAN_POINT('Ctrl Pts',(-4.19162087373384,-4.17918618006405,
34.0317066610695));
#19427=CARTESIAN_POINT('Ctrl Pts',(-4.30686517396541,-4.06032158321635,
34.023918683308));
#19428=CARTESIAN_POINT('Ctrl Pts',(-4.41693987696012,-3.93682266375049,
34.0161307055465));
#19429=CARTESIAN_POINT('Ctrl Pts',(-4.52699293832519,-3.81334802523024,
34.0083442589681));
#19430=CARTESIAN_POINT('Ctrl Pts',(-4.63187821795671,-3.68524112050179,
34.0005578123898));
#19431=CARTESIAN_POINT('Ctrl Pts',(-4.73121804320277,-3.55295741462976,
33.9927713658114));
#19432=CARTESIAN_POINT('Ctrl Pts',(-4.83056165803863,-3.42066866243333,
33.9849846221977));
#19433=CARTESIAN_POINT('Ctrl Pts',(-4.92435920013832,-3.28420304339894,
33.977197878584));
#19434=CARTESIAN_POINT('Ctrl Pts',(-5.01227439261565,-3.144047705686,33.9694111349703));
#19435=CARTESIAN_POINT('Ctrl Pts',(-5.10018377016078,-3.00390163820001,
33.9616249063915));
#19436=CARTESIAN_POINT('Ctrl Pts',(-5.18221140695674,-2.86006661119489,
33.9538386778126));
#19437=CARTESIAN_POINT('Ctrl Pts',(-5.25806525981668,-2.71305736872793,
33.9460524492337));
#19438=CARTESIAN_POINT('Ctrl Pts',(-5.33393908093073,-2.56600942660631,
33.9382641709582));
#19439=CARTESIAN_POINT('Ctrl Pts',(-5.4036357222021,-2.41578588258479,33.9304758926827));
#19440=CARTESIAN_POINT('Ctrl Pts',(-5.46690946408993,-2.26292542385823,
33.9226876144071));
#19441=CARTESIAN_POINT('Ctrl Pts',(-5.52706387175656,-2.11760083776615,
33.9152832907109));
#19442=CARTESIAN_POINT('Ctrl Pts',(-5.58141330974059,-1.96989331219703,
33.9078789670147));
#19443=CARTESIAN_POINT('Ctrl Pts',(-5.62978726078636,-1.82028183553745,
33.9004746433185));
#19444=CARTESIAN_POINT('Ctrl Pts',(-5.68077981371215,-1.66257151878761,
33.8926695052266));
#19445=CARTESIAN_POINT('Ctrl Pts',(-5.72515014096265,-1.50268947405148,
33.8848643671348));
#19446=CARTESIAN_POINT('Ctrl Pts',(-5.76273333894475,-1.34120655631962,
33.877059229043));
#19447=CARTESIAN_POINT('Ctrl Pts',(-5.8003080494266,-1.17976010664736,33.8692558536035));
#19448=CARTESIAN_POINT('Ctrl Pts',(-5.8310986179747,-1.01671381375499,33.8614524781641));
#19449=CARTESIAN_POINT('Ctrl Pts',(-5.85499079240215,-0.852650798032842,
33.8536491027246));
#19450=CARTESIAN_POINT('Ctrl Pts',(-5.87888163475403,-0.688596929420129,
33.8458461623516));
#19451=CARTESIAN_POINT('Ctrl Pts',(-5.89587480235716,-0.523526763995115,
33.8380432219787));
#19452=CARTESIAN_POINT('Ctrl Pts',(-5.90590756190641,-0.358031329239078,
33.8302402816058));
#19453=CARTESIAN_POINT('Ctrl Pts',(-5.91313575105257,-0.238798699435666,
33.8246185851388));
#19454=CARTESIAN_POINT('Ctrl Pts',(-5.91675213969457,-0.119345510029993,
33.8189968886719));
#19455=CARTESIAN_POINT('Ctrl Pts',(-5.91674999904992,0.000106031776716273,
33.8133751922049));
#19456=CARTESIAN_POINT('Ctrl Pts',(-5.91674999986672,-3.97138514489972E-5,
33.5616248082709));
#19457=CARTESIAN_POINT('Ctrl Pts',(-5.9167488701323,-0.168352679007752,
33.569545476781));
#19458=CARTESIAN_POINT('Ctrl Pts',(-5.90956143709304,-0.336644184720461,
33.5774661452911));
#19459=CARTESIAN_POINT('Ctrl Pts',(-5.89521918275979,-0.504302835329105,
33.5853868138013));
#19460=CARTESIAN_POINT('Ctrl Pts',(-5.88087213540043,-0.672017515643508,
33.593310129313));
#19461=CARTESIAN_POINT('Ctrl Pts',(-5.85936551470131,-0.839098623772593,
33.6012334448248));
#19462=CARTESIAN_POINT('Ctrl Pts',(-5.83078272279159,-1.00493950170897,
33.6091567603366));
#19463=CARTESIAN_POINT('Ctrl Pts',(-5.81170125692052,-1.11565251611173,
33.6144462532245));
#19464=CARTESIAN_POINT('Ctrl Pts',(-5.78946721870051,-1.22581291257659,
33.6197357461125));
#19465=CARTESIAN_POINT('Ctrl Pts',(-5.76411814781709,-1.3352425025087,33.6250252390004));
#19466=CARTESIAN_POINT('Ctrl Pts',(-5.72679483688146,-1.496363777106,33.6328133503934));
#19467=CARTESIAN_POINT('Ctrl Pts',(-5.6827050274659,-1.65594791878048,33.6406014617864));
#19468=CARTESIAN_POINT('Ctrl Pts',(-5.63200031122108,-1.81342302205131,
33.6483895731793));
#19469=CARTESIAN_POINT('Ctrl Pts',(-5.58130554996344,-1.97086720783061,
33.6561761555124));
#19470=CARTESIAN_POINT('Ctrl Pts',(-5.52399857108406,-2.12620287744186,
33.6639627378455));
#19471=CARTESIAN_POINT('Ctrl Pts',(-5.46028071573764,-2.27887364016606,
33.6717493201785));
#19472=CARTESIAN_POINT('Ctrl Pts',(-5.39656043084349,-2.43155022419266,
33.6795361994123));
#19473=CARTESIAN_POINT('Ctrl Pts',(-5.32642889976689,-2.58156140161961,
33.687323078646));
#19474=CARTESIAN_POINT('Ctrl Pts',(-5.2501357521873,-2.72837041951872,33.6951099578797));
#19475=CARTESIAN_POINT('Ctrl Pts',(-5.17384763991122,-2.87516974810775,
33.7028963231839));
#19476=CARTESIAN_POINT('Ctrl Pts',(-5.09139887238669,-3.01876705659778,
33.7106826884881));
#19477=CARTESIAN_POINT('Ctrl Pts',(-5.00308528208094,-3.15864974676286,
33.7184690537924));
#19478=CARTESIAN_POINT('Ctrl Pts',(-4.91474850241982,-3.29856916728168,
33.726257463638));
#19479=CARTESIAN_POINT('Ctrl Pts',(-4.82054399182033,-3.43477174905532,
33.7340458734836));
#19480=CARTESIAN_POINT('Ctrl Pts',(-4.72081169453193,-3.56677270193526,
33.7418342833292));
#19481=CARTESIAN_POINT('Ctrl Pts',(-4.62632052482366,-3.69183674617524,
33.7492133969813));
#19482=CARTESIAN_POINT('Ctrl Pts',(-4.5268677738479,-3.81312920329694,33.7565925106335));
#19483=CARTESIAN_POINT('Ctrl Pts',(-4.42277662140855,-3.93026430658575,
33.7639716242856));
#19484=CARTESIAN_POINT('Ctrl Pts',(-4.31291607061109,-4.0538917875335,33.7717597356786));
#19485=CARTESIAN_POINT('Ctrl Pts',(-4.19784912163827,-4.1729321454896,33.7795478470716));
#19486=CARTESIAN_POINT('Ctrl Pts',(-4.07798251032837,-4.28695570398808,
33.7873359584645));
#19487=CARTESIAN_POINT('Ctrl Pts',(-3.9581394327382,-4.4009568759484,33.7951225407976));
#19488=CARTESIAN_POINT('Ctrl Pts',(-3.83349880440956,-4.50994299364982,
33.8029091231306));
#19489=CARTESIAN_POINT('Ctrl Pts',(-3.70450362454666,-4.61352180641001,
33.8106957054637));
#19490=CARTESIAN_POINT('Ctrl Pts',(-3.5755035261262,-4.71710456860731,33.8184825846974));
#19491=CARTESIAN_POINT('Ctrl Pts',(-3.44214879059609,-4.81527941016946,
33.8262694639311));
#19492=CARTESIAN_POINT('Ctrl Pts',(-3.30491542500478,-4.90769442773951,
33.8340563431648));
#19493=CARTESIAN_POINT('Ctrl Pts',(-3.16769111673621,-5.00010334597187,
33.841842708469));
#19494=CARTESIAN_POINT('Ctrl Pts',(-3.02658895579834,-5.0867530225459,33.8496290737731));
#19495=CARTESIAN_POINT('Ctrl Pts',(-2.88211396450086,-5.16733486994303,
33.8574154390773));
#19496=CARTESIAN_POINT('Ctrl Pts',(-2.73760103700449,-5.24793787649692,
33.8652038489229));
#19497=CARTESIAN_POINT('Ctrl Pts',(-2.58971378775667,-5.3224697127073,33.8729922587685));
#19498=CARTESIAN_POINT('Ctrl Pts',(-2.43898267026516,-5.39066731459531,
33.8807806686141));
#19499=CARTESIAN_POINT('Ctrl Pts',(-2.29617276825122,-5.45528099891807,
33.8881597822663));
#19500=CARTESIAN_POINT('Ctrl Pts',(-2.15081044874833,-5.51420897105778,
33.8955388959185));
#19501=CARTESIAN_POINT('Ctrl Pts',(-2.0033640677192,-5.56726710107137,33.9029180095707));
#19502=CARTESIAN_POINT('Ctrl Pts',(-1.84774526388196,-5.62326605247949,
33.9107061209636));
#19503=CARTESIAN_POINT('Ctrl Pts',(-1.68974924436139,-5.67274602199669,
33.9184942323565));
#19504=CARTESIAN_POINT('Ctrl Pts',(-1.52993874555476,-5.71552429767824,
33.9262823437494));
#19505=CARTESIAN_POINT('Ctrl Pts',(-1.37015962275342,-5.75829417459116,
33.9340689260824));
#19506=CARTESIAN_POINT('Ctrl Pts',(-1.20856703994434,-5.79436490043047,
33.9418555084154));
#19507=CARTESIAN_POINT('Ctrl Pts',(-1.04573767139948,-5.82360397735938,
33.9496420907484));
#19508=CARTESIAN_POINT('Ctrl Pts',(-0.882902094207371,-5.85284416916773,
33.9574289699821));
#19509=CARTESIAN_POINT('Ctrl Pts',(-0.718829950703475,-5.87525213046855,
33.9652158492157));
#19510=CARTESIAN_POINT('Ctrl Pts',(-0.554107596518002,-5.89074658544917,
33.9730027284493));
#19511=CARTESIAN_POINT('Ctrl Pts',(-0.3893961139125,-5.90624001780474,33.9807890937535));
#19512=CARTESIAN_POINT('Ctrl Pts',(-0.224034824661971,-5.91482082713235,
33.9885754590576));
#19513=CARTESIAN_POINT('Ctrl Pts',(-0.0586148395352926,-5.91645965616992,
33.9963618243617));
#19514=CARTESIAN_POINT('Ctrl Pts',(0.106848581520312,-5.91809891553071,
34.0041502342073));
#19515=CARTESIAN_POINT('Ctrl Pts',(0.272370409545367,-5.91279254711233,
34.0119386440528));
#19516=CARTESIAN_POINT('Ctrl Pts',(0.437358982122217,-5.90056333609402,
34.0197270538983));
#19517=CARTESIAN_POINT('Ctrl Pts',(0.593677082036207,-5.88897679406888,
34.0271061675508));
#19518=CARTESIAN_POINT('Ctrl Pts',(0.749516272802175,-5.87117633185597,
34.0344852812033));
#19519=CARTESIAN_POINT('Ctrl Pts',(0.904377186100404,-5.84722433875776,
34.0418643948558));
#19520=CARTESIAN_POINT('Ctrl Pts',(1.06782148307199,-5.82194477279352,34.0496525062489));
#19521=CARTESIAN_POINT('Ctrl Pts',(1.23023435657831,-5.78980339621259,34.057440617642));
#19522=CARTESIAN_POINT('Ctrl Pts',(1.39103423910614,-5.75090899842229,34.0652287290351));
#19523=CARTESIAN_POINT('Ctrl Pts',(1.55180255138019,-5.71202223686896,34.0730153113683));
#19524=CARTESIAN_POINT('Ctrl Pts',(1.71095819417121,-5.66638517462235,34.0808018937014));
#19525=CARTESIAN_POINT('Ctrl Pts',(1.86793138500003,-5.61415736361494,34.0885884760346));
#19526=CARTESIAN_POINT('Ctrl Pts',(2.02491056118163,-5.56192756117274,34.0963753552685));
#19527=CARTESIAN_POINT('Ctrl Pts',(2.17970681446322,-5.50310660423615,34.1041622345023));
#19528=CARTESIAN_POINT('Ctrl Pts',(2.33176636736659,-5.43790365586942,34.1119491137361));
#19529=CARTESIAN_POINT('Ctrl Pts',(2.48381588442738,-5.37270501085959,34.1197354790405));
#19530=CARTESIAN_POINT('Ctrl Pts',(2.63312876891438,-5.30112534336405,34.1275218443448));
#19531=CARTESIAN_POINT('Ctrl Pts',(2.77917190741901,-5.22342168233745,34.1353082096491));
#19532=CARTESIAN_POINT('Ctrl Pts',(2.92525339388609,-5.1456976179074,34.1430966194948));
#19533=CARTESIAN_POINT('Ctrl Pts',(3.06806313558781,-5.06184649522597,34.1508850293405));
#19534=CARTESIAN_POINT('Ctrl Pts',(3.20709248148285,-4.97217139464401,34.1586734391862));
#19535=CARTESIAN_POINT('Ctrl Pts',(3.33881556290646,-4.88720889626222,34.1660525528378));
#19536=CARTESIAN_POINT('Ctrl Pts',(3.46714514473233,-4.79701893974729,34.1734316664894));
#19537=CARTESIAN_POINT('Ctrl Pts',(3.59167256948262,-4.70189522598347,34.1808107801411));
#19538=CARTESIAN_POINT('Ctrl Pts',(3.72310210170258,-4.60149914674169,34.188598891534));
#19539=CARTESIAN_POINT('Ctrl Pts',(3.85034298526206,-4.49557102432411,34.1963870029269));
#19540=CARTESIAN_POINT('Ctrl Pts',(3.97293658114135,-4.38448463159912,34.2041751143198));
#19541=CARTESIAN_POINT('Ctrl Pts',(4.09550610790508,-4.27342004875094,34.2119616966528));
#19542=CARTESIAN_POINT('Ctrl Pts',(4.21342993089196,-4.15719943072787,34.2197482789858));
#19543=CARTESIAN_POINT('Ctrl Pts',(4.32628404637179,-4.03623548775451,34.2275348613189));
#19544=CARTESIAN_POINT('Ctrl Pts',(4.43914246495403,-3.91526693245282,34.2353217405525));
#19545=CARTESIAN_POINT('Ctrl Pts',(4.54693056837072,-3.78955492123015,34.2431086197862));
#19546=CARTESIAN_POINT('Ctrl Pts',(4.64926214296325,-3.65954807162151,34.2508954990199));
#19547=CARTESIAN_POINT('Ctrl Pts',(4.75158696373108,-3.52954980238971,34.258681864324));
#19548=CARTESIAN_POINT('Ctrl Pts',(4.84845577879255,-3.39525751318412,34.2664682296282));
#19549=CARTESIAN_POINT('Ctrl Pts',(4.93952342081019,-3.25715196725108,34.2742545949323));
#19550=CARTESIAN_POINT('Ctrl Pts',(5.03061497534125,-3.11901015760628,34.2820430047779));
#19551=CARTESIAN_POINT('Ctrl Pts',(5.11590213538125,-2.97705335632145,34.2898314146234));
#19552=CARTESIAN_POINT('Ctrl Pts',(5.19508324716767,-2.83179106176601,34.297619824469));
#19553=CARTESIAN_POINT('Ctrl Pts',(5.27010323643119,-2.69416258532658,34.3049989381213));
#19554=CARTESIAN_POINT('Ctrl Pts',(5.33964231592452,-2.55356732845023,34.3123780517737));
#19555=CARTESIAN_POINT('Ctrl Pts',(5.4034821510481,-2.41045871273593,34.3197571654261));
#19556=CARTESIAN_POINT('Ctrl Pts',(5.47086039871731,-2.25941810095286,34.327545276819));
#19557=CARTESIAN_POINT('Ctrl Pts',(5.53191377384975,-2.10552367300649,34.335333388212));
#19558=CARTESIAN_POINT('Ctrl Pts',(5.58641836117397,-1.94932307646484,34.3431214996049));
#19559=CARTESIAN_POINT('Ctrl Pts',(5.64091224747261,-1.79315314718736,34.3509080819379));
#19560=CARTESIAN_POINT('Ctrl Pts',(5.68885980619092,-1.63467825424026,34.358694664271));
#19561=CARTESIAN_POINT('Ctrl Pts',(5.73008616510002,-1.47446366622898,34.366481246604));
#19562=CARTESIAN_POINT('Ctrl Pts',(5.771314095961,-1.31424296927113,34.3742681258377));
#19563=CARTESIAN_POINT('Ctrl Pts',(5.80582023075301,-1.15228275296601,34.3820550050714));
#19564=CARTESIAN_POINT('Ctrl Pts',(5.83348006089518,-0.989161736845068,
34.389841884305));
#19565=CARTESIAN_POINT('Ctrl Pts',(5.86113806550457,-0.826051486616828,
34.3976282496092));
#19566=CARTESIAN_POINT('Ctrl Pts',(5.88195061638305,-0.661780904961187,
34.4054146149133));
#19567=CARTESIAN_POINT('Ctrl Pts',(5.89584462830319,-0.496937301285056,
34.4132009802175));
#19568=CARTESIAN_POINT('Ctrl Pts',(5.9097422885087,-0.33205041302612,34.4209893900631));
#19569=CARTESIAN_POINT('Ctrl Pts',(5.91671775088616,-0.166590520534307,
34.4287777999086));
#19570=CARTESIAN_POINT('Ctrl Pts',(5.91674988836775,-0.0011493477552802,
34.4365662097542));
#19571=CARTESIAN_POINT('Ctrl Pts',(5.91678033696172,0.155597567330028,34.4439453234065));
#19572=CARTESIAN_POINT('Ctrl Pts',(5.9105784611958,0.312327419526829,34.4513244370589));
#19573=CARTESIAN_POINT('Ctrl Pts',(5.89816946935658,0.468537590007321,34.4587035507112));
#19574=CARTESIAN_POINT('Ctrl Pts',(5.88507269171204,0.63340592863688,34.4664916621042));
#19575=CARTESIAN_POINT('Ctrl Pts',(5.86505653282944,0.797754226321862,34.4742797734972));
#19576=CARTESIAN_POINT('Ctrl Pts',(5.83818638150636,0.96099445226995,34.4820678848902));
#19577=CARTESIAN_POINT('Ctrl Pts',(5.81132150566908,1.12420262884537,34.4898544672233));
#19578=CARTESIAN_POINT('Ctrl Pts',(5.77760537425251,1.28630285267095,34.4976410495564));
#19579=CARTESIAN_POINT('Ctrl Pts',(5.73715487239508,1.4467150834402,34.5054276318894));
#19580=CARTESIAN_POINT('Ctrl Pts',(5.69670282816903,1.60713343069206,34.5132145111232));
#19581=CARTESIAN_POINT('Ctrl Pts',(5.64951597398198,1.76586334531487,34.5210013903569));
#19582=CARTESIAN_POINT('Ctrl Pts',(5.59576185583864,1.92233707118217,34.5287882695907));
#19583=CARTESIAN_POINT('Ctrl Pts',(5.54201128543601,2.07880046987409,34.5365746348949));
#19584=CARTESIAN_POINT('Ctrl Pts',(5.48169442238196,2.23300767561758,34.5443610001991));
#19585=CARTESIAN_POINT('Ctrl Pts',(5.41502807840099,2.38440799206614,34.5521473655033));
#19586=CARTESIAN_POINT('Ctrl Pts',(5.34834422919189,2.53584806316329,34.5599357753489));
#19587=CARTESIAN_POINT('Ctrl Pts',(5.27530769462908,2.68447947881351,34.5677241851945));
#19588=CARTESIAN_POINT('Ctrl Pts',(5.19618302415405,2.82977252477885,34.5755125950401));
#19589=CARTESIAN_POINT('Ctrl Pts',(5.121216510104,2.9674301365748,34.5828917086922));
#19590=CARTESIAN_POINT('Ctrl Pts',(5.04078541325933,3.10209100131029,34.5902708223443));
#19591=CARTESIAN_POINT('Ctrl Pts',(4.95515234016332,3.23332581845288,34.5976499359964));
#19592=CARTESIAN_POINT('Ctrl Pts',(4.8647729336875,3.37183450970365,34.6054380473894));
#19593=CARTESIAN_POINT('Ctrl Pts',(4.76856626652781,3.50657606514283,34.6132261587823));
#19594=CARTESIAN_POINT('Ctrl Pts',(4.66687109274718,3.63706540581562,34.6210142701753));
#19595=CARTESIAN_POINT('Ctrl Pts',(4.56519588504112,3.76752912718114,34.6288008525083));
#19596=CARTESIAN_POINT('Ctrl Pts',(4.4580345170868,3.89374204767642,34.6365874348414));
#19597=CARTESIAN_POINT('Ctrl Pts',(4.34576714012937,4.01525074264009,34.6443740171744));
#19598=CARTESIAN_POINT('Ctrl Pts',(4.23349548244188,4.13676407070322,34.6521608964081));
#19599=CARTESIAN_POINT('Ctrl Pts',(4.1161176401057,4.25357257695394,34.6599477756418));
#19600=CARTESIAN_POINT('Ctrl Pts',(3.99405237364415,4.36525786169471,34.6677346548755));
#19601=CARTESIAN_POINT('Ctrl Pts',(3.8719951634196,4.47693577527128,34.6755210201797));
#19602=CARTESIAN_POINT('Ctrl Pts',(3.74525138400069,4.58349092836249,34.6833073854839));
#19603=CARTESIAN_POINT('Ctrl Pts',(3.61427489526354,4.68454347231058,34.691093750788));
#19604=CARTESIAN_POINT('Ctrl Pts',(3.4832640147602,4.78562255060464,34.6988821606336));
#19605=CARTESIAN_POINT('Ctrl Pts',(3.34801845604771,4.88119593574642,34.7066705704792));
#19606=CARTESIAN_POINT('Ctrl Pts',(3.20902396000049,4.97092504335388,34.7144589803248));
#19607=CARTESIAN_POINT('Ctrl Pts',(3.0773338969834,5.05593871059491,34.721838093977));
#19608=CARTESIAN_POINT('Ctrl Pts',(2.94227900854711,5.13570641672617,34.7292172076293));
#19609=CARTESIAN_POINT('Ctrl Pts',(2.80429528800515,5.20997682338147,34.7365963212815));
#19610=CARTESIAN_POINT('Ctrl Pts',(2.65866362590547,5.28836377166456,34.7443844326745));
#19611=CARTESIAN_POINT('Ctrl Pts',(2.50971724379881,5.36065474499884,34.7521725440674));
#19612=CARTESIAN_POINT('Ctrl Pts',(2.35798568823811,5.42658585637086,34.7599606554604));
#19613=CARTESIAN_POINT('Ctrl Pts',(2.20628392252322,5.49250402331854,34.7677472377935));
#19614=CARTESIAN_POINT('Ctrl Pts',(2.0517983672999,5.55206469246588,34.7755338201266));
#19615=CARTESIAN_POINT('Ctrl Pts',(1.8950797764015,5.60505157902887,34.7833204024596));
#19616=CARTESIAN_POINT('Ctrl Pts',(1.73835520985823,5.65804048597001,34.7911072816934));
#19617=CARTESIAN_POINT('Ctrl Pts',(1.57939773868323,5.70445500268399,34.7988941609271));
#19618=CARTESIAN_POINT('Ctrl Pts',(1.41877526322053,5.74412807264719,34.8066810401608));
#19619=CARTESIAN_POINT('Ctrl Pts',(1.25816338874814,5.78379852421076,34.814467405465));
#19620=CARTESIAN_POINT('Ctrl Pts',(1.09588704015207,5.81672834288891,34.8222537707692));
#19621=CARTESIAN_POINT('Ctrl Pts',(0.932526495142294,5.84280111747419,34.8300401360734));
#19622=CARTESIAN_POINT('Ctrl Pts',(0.769123054970881,5.86888073824059,34.837828545919));
#19623=CARTESIAN_POINT('Ctrl Pts',(0.604635164956452,5.88809966478843,34.8456169557646));
#19624=CARTESIAN_POINT('Ctrl Pts',(0.439651355956734,5.90039297400651,34.8534053656102));
#19625=CARTESIAN_POINT('Ctrl Pts',(0.283337769293297,5.91204024574482,34.8607844792623));
#19626=CARTESIAN_POINT('Ctrl Pts',(0.126579305409158,5.91747106814903,34.8681635929145));
#19627=CARTESIAN_POINT('Ctrl Pts',(-0.0301209308773817,5.91667332983857,
34.8755427065666));
#19628=CARTESIAN_POINT('Ctrl Pts',(-0.195506497902827,5.91583137576155,
34.8833308179596));
#19629=CARTESIAN_POINT('Ctrl Pts',(-0.36088626684752,5.90805052799148,34.8911189293525));
#19630=CARTESIAN_POINT('Ctrl Pts',(-0.525668977942791,5.89335241506297,
34.8989070407455));
#19631=CARTESIAN_POINT('Ctrl Pts',(-0.690419336825323,5.87865718785271,
34.9066936230786));
#19632=CARTESIAN_POINT('Ctrl Pts',(-0.854572553682613,5.85704743363695,
34.9144802054116));
#19633=CARTESIAN_POINT('Ctrl Pts',(-1.01754152073414,5.8285967278653,34.9222667877447));
#19634=CARTESIAN_POINT('Ctrl Pts',(-1.18051670175601,5.80014493727459,34.9300536669784));
#19635=CARTESIAN_POINT('Ctrl Pts',(-1.3423072271822,5.76485172423875,34.9378405462121));
#19636=CARTESIAN_POINT('Ctrl Pts',(-1.50233448502554,5.72284209616193,34.9456274254458));
#19637=CARTESIAN_POINT('Ctrl Pts',(-1.66235118116235,5.68083524069628,34.95341379075));
#19638=CARTESIAN_POINT('Ctrl Pts',(-1.82060453354907,5.63211293851259,34.9612001560542));
#19639=CARTESIAN_POINT('Ctrl Pts',(-1.9765292918561,5.57685059159153,34.9689865213583));
#19640=CARTESIAN_POINT('Ctrl Pts',(-2.13249499283837,5.52157373390036,34.9767749312039));
#19641=CARTESIAN_POINT('Ctrl Pts',(-2.28613057593417,5.45975350496361,34.9845633410495));
#19642=CARTESIAN_POINT('Ctrl Pts',(-2.4368881772574,5.39161446823149,34.9923517508951));
#19643=CARTESIAN_POINT('Ctrl Pts',(-2.5797231713256,5.32705627135107,34.9997308645473));
#19644=CARTESIAN_POINT('Ctrl Pts',(-2.71997465365962,5.2568264234601,35.0071099781995));
#19645=CARTESIAN_POINT('Ctrl Pts',(-2.85719504192284,5.18115499236527,35.0144890918517));
#19646=CARTESIAN_POINT('Ctrl Pts',(-3.00202106297927,5.10128936589519,35.0222772032446));
#19647=CARTESIAN_POINT('Ctrl Pts',(-3.14352218117468,5.015333312489,35.0300653146375));
#19648=CARTESIAN_POINT('Ctrl Pts',(-3.28118954566347,4.92358870417998,35.0378534260304));
#19649=CARTESIAN_POINT('Ctrl Pts',(-3.41882988156519,4.83186210832544,35.0456400083634));
#19650=CARTESIAN_POINT('Ctrl Pts',(-3.55263769987251,4.73434940227533,35.0534265906964));
#19651=CARTESIAN_POINT('Ctrl Pts',(-3.68213264893139,4.63139608737728,35.0612131730294));
#19652=CARTESIAN_POINT('Ctrl Pts',(-3.81163253560394,4.52843884689216,35.069000052263));
#19653=CARTESIAN_POINT('Ctrl Pts',(-3.93681897140464,4.42004077820467,35.0767869314966));
#19654=CARTESIAN_POINT('Ctrl Pts',(-4.05724367189022,4.30658848154856,35.0845738107303));
#19655=CARTESIAN_POINT('Ctrl Pts',(-4.17766042441529,4.19314367267836,35.0923601760344));
#19656=CARTESIAN_POINT('Ctrl Pts',(-4.29331583802088,4.07464552258709,35.1001465413386));
#19657=CARTESIAN_POINT('Ctrl Pts',(-4.40379747198279,3.95151849144832,35.1079329066427));
#19658=CARTESIAN_POINT('Ctrl Pts',(-4.51430811617819,3.82835912965155,35.1157213164882));
#19659=CARTESIAN_POINT('Ctrl Pts',(-4.61964205112156,3.70056869476739,35.1235097263338));
#19660=CARTESIAN_POINT('Ctrl Pts',(-4.71942562410225,3.56860649849029,35.1312981361793));
#19661=CARTESIAN_POINT('Ctrl Pts',(-4.8139653748704,3.44357917411025,35.1386772498318));
#19662=CARTESIAN_POINT('Ctrl Pts',(-4.90352296716482,3.31480748663149,35.1460563634843));
#19663=CARTESIAN_POINT('Ctrl Pts',(-4.9878154412707,3.18270760302003,35.1534354771368));
#19664=CARTESIAN_POINT('Ctrl Pts',(-5.07677994417001,3.04328589778231,35.1612235885298));
#19665=CARTESIAN_POINT('Ctrl Pts',(-5.15991089895353,2.90010680040592,35.1690116999229));
#19666=CARTESIAN_POINT('Ctrl Pts',(-5.2369058983043,2.75367884380253,35.1767998113159));
#19667=CARTESIAN_POINT('Ctrl Pts',(-5.3138857810293,2.60727963577555,35.1845863936491));
#19668=CARTESIAN_POINT('Ctrl Pts',(-5.38473196341406,2.45763312387514,35.1923729759822));
#19669=CARTESIAN_POINT('Ctrl Pts',(-5.44918793773478,2.3052725178915,35.2001595583154));
#19670=CARTESIAN_POINT('Ctrl Pts',(-5.51364636974735,2.15290610243209,35.2079464375492));
#19671=CARTESIAN_POINT('Ctrl Pts',(-5.57171397801221,1.99782567853851,35.2157333167829));
#19672=CARTESIAN_POINT('Ctrl Pts',(-5.62318207691178,1.8405852037866,35.2235201960167));
#19673=CARTESIAN_POINT('Ctrl Pts',(-5.67464677894655,1.68335510681517,35.231306561321));
#19674=CARTESIAN_POINT('Ctrl Pts',(-5.7195127439514,1.52396554800902,35.2390929266252));
#19675=CARTESIAN_POINT('Ctrl Pts',(-5.75762087502688,1.36298658172217,35.2468792919295));
#19676=CARTESIAN_POINT('Ctrl Pts',(-5.79573901252374,1.20196534562771,35.2546677017752));
#19677=CARTESIAN_POINT('Ctrl Pts',(-5.82709569478609,1.03935417880022,35.2624561116208));
#19678=CARTESIAN_POINT('Ctrl Pts',(-5.85158255975117,0.875735181956287,
35.2702445214665));
#19679=CARTESIAN_POINT('Ctrl Pts',(-5.87478259199587,0.720714683904022,
35.2776236351184));
#19680=CARTESIAN_POINT('Ctrl Pts',(-5.89181624181401,0.564789815447571,
35.2850027487702));
#19681=CARTESIAN_POINT('Ctrl Pts',(-5.90263414477321,0.408461400205068,
35.292381862422));
#19682=CARTESIAN_POINT('Ctrl Pts',(-5.9120376370948,0.272572489209566,35.2987961775464));
#19683=CARTESIAN_POINT('Ctrl Pts',(-5.91674717417702,0.1363570960496,35.3052104926708));
#19684=CARTESIAN_POINT('Ctrl Pts',(-5.91674999872832,0.00012267210750124,
35.3116248077951));
#19685=CARTESIAN_POINT('Origin',(0.,0.,0.));
#19686=CARTESIAN_POINT('',(-5.91674999982786,-4.51337720214345E-5,37.3133751922485));
#19687=CARTESIAN_POINT('',(-5.91674999805201,-0.000151827279522968,37.0616248082411));
#19688=CARTESIAN_POINT('',(-5.91675,-7.2459289488551E-16,0.));
#19689=CARTESIAN_POINT('Ctrl Pts',(-5.91674999982786,-4.51328457496523E-5,
37.3133751922049));
#19690=CARTESIAN_POINT('Ctrl Pts',(-5.9167512716958,0.166692072992805,37.3055286593146));
#19691=CARTESIAN_POINT('Ctrl Pts',(-5.90970008426505,0.333421001495371,
37.2976821264244));
#19692=CARTESIAN_POINT('Ctrl Pts',(-5.89562456490874,0.499541341777265,
37.2898355935341));
#19693=CARTESIAN_POINT('Ctrl Pts',(-5.88154835837704,0.665669792154845,
37.2819886775713));
#19694=CARTESIAN_POINT('Ctrl Pts',(-5.86044716515415,0.831189287417103,
37.2741417616085));
#19695=CARTESIAN_POINT('Ctrl Pts',(-5.83240101010933,0.995504404699285,
37.2662948456457));
#19696=CARTESIAN_POINT('Ctrl Pts',(-5.80434815606936,1.1598587696492,37.2584460553992));
#19697=CARTESIAN_POINT('Ctrl Pts',(-5.76934707958976,1.32300787753653,37.2505972651527));
#19698=CARTESIAN_POINT('Ctrl Pts',(-5.72752911738174,1.48436544423679,37.2427484749062));
#19699=CARTESIAN_POINT('Ctrl Pts',(-5.71723917772028,1.52406990465518,37.2408171618104));
#19700=CARTESIAN_POINT('Ctrl Pts',(-5.70653672951455,1.56366594835795,37.2388858487146));
#19701=CARTESIAN_POINT('Ctrl Pts',(-5.69542419792215,1.60314496169961,37.2369545356188));
#19702=CARTESIAN_POINT('Ctrl Pts',(-5.65061315765045,1.76234321837312,37.2291665578575));
#19703=CARTESIAN_POINT('Ctrl Pts',(-5.59911506889175,1.91968993099315,37.2213785800963));
#19704=CARTESIAN_POINT('Ctrl Pts',(-5.5411080665506,2.07462091894106,37.213590602335));
#19705=CARTESIAN_POINT('Ctrl Pts',(-5.48311246888355,2.22952144612814,37.2058041557569));
#19706=CARTESIAN_POINT('Ctrl Pts',(-5.41861062300551,2.38200689723374,37.1980177091788));
#19707=CARTESIAN_POINT('Ctrl Pts',(-5.34782963433365,2.53153091323074,37.1902312626008));
#19708=CARTESIAN_POINT('Ctrl Pts',(-5.2770459455265,2.68106063323216,37.1824445189873));
#19709=CARTESIAN_POINT('Ctrl Pts',(-5.19998276775482,2.82762840156007,37.1746577753738));
#19710=CARTESIAN_POINT('Ctrl Pts',(-5.11691452508468,2.97070973093593,37.1668710317604));
#19711=CARTESIAN_POINT('Ctrl Pts',(-5.03385177675738,3.1137815965522,37.1590848031817));
#19712=CARTESIAN_POINT('Ctrl Pts',(-4.94478491892114,3.25336720836627,37.1512985746031));
#19713=CARTESIAN_POINT('Ctrl Pts',(-4.85003339957065,3.38896836597056,37.1435123460245));
#19714=CARTESIAN_POINT('Ctrl Pts',(-4.75525693722305,3.52460522009249,37.1357240677492));
#19715=CARTESIAN_POINT('Ctrl Pts',(-4.65479300465449,3.65625526086087,37.1279357894738));
#19716=CARTESIAN_POINT('Ctrl Pts',(-4.54900381506683,3.78345012561384,37.1201475111985));
#19717=CARTESIAN_POINT('Ctrl Pts',(-4.44842993009576,3.90437440669057,37.1127431875012));
#19718=CARTESIAN_POINT('Ctrl Pts',(-4.3430433686534,4.02127199945382,37.1053388638038));
#19719=CARTESIAN_POINT('Ctrl Pts',(-4.23318854821258,4.13376889506197,37.0979345401065));
#19720=CARTESIAN_POINT('Ctrl Pts',(-4.11764161461318,4.25209480260808,37.0901465623448));
#19721=CARTESIAN_POINT('Ctrl Pts',(-3.99710975048733,4.36559418961599,37.0823585845831));
#19722=CARTESIAN_POINT('Ctrl Pts',(-3.8720194124591,4.47385697491995,37.0745706068215));
#19723=CARTESIAN_POINT('Ctrl Pts',(-3.7469536682634,4.58209847483247,37.066784160243));
#19724=CARTESIAN_POINT('Ctrl Pts',(-3.61733147989254,4.68510521832739,37.0589977136645));
#19725=CARTESIAN_POINT('Ctrl Pts',(-3.48361376928839,4.7825062121156,37.051211267086));
#19726=CARTESIAN_POINT('Ctrl Pts',(-3.34989095765504,4.87991092153214,37.0434245234721));
#19727=CARTESIAN_POINT('Ctrl Pts',(-3.21207256711454,4.97170926199926,37.0356377798582));
#19728=CARTESIAN_POINT('Ctrl Pts',(-3.07065059591841,5.05757209343435,37.0278510362443));
#19729=CARTESIAN_POINT('Ctrl Pts',(-2.92923797872759,5.14342924568554,37.0200648076653));
#19730=CARTESIAN_POINT('Ctrl Pts',(-2.78422253108445,5.22335150877934,37.0122785790863));
#19731=CARTESIAN_POINT('Ctrl Pts',(-2.63612319941929,5.29705437389342,37.0044923505072));
#19732=CARTESIAN_POINT('Ctrl Pts',(-2.48798488113741,5.37077664102182,36.9967040722315));
#19733=CARTESIAN_POINT('Ctrl Pts',(-2.33676134204432,5.43827609441476,36.9889157939557));
#19734=CARTESIAN_POINT('Ctrl Pts',(-2.18299479391218,5.49931489298915,36.98112751568));
#19735=CARTESIAN_POINT('Ctrl Pts',(-2.03680878776444,5.55734453787641,36.9737231919846));
#19736=CARTESIAN_POINT('Ctrl Pts',(-1.88832471336697,5.60953509414731,36.9663188682892));
#19737=CARTESIAN_POINT('Ctrl Pts',(-1.73802399381556,5.65572304479466,36.9589145445938));
#19738=CARTESIAN_POINT('Ctrl Pts',(-1.57993546209493,5.70430421807726,36.9511265668323));
#19739=CARTESIAN_POINT('Ctrl Pts',(-1.41978047724363,5.74626160057876,36.9433385890709));
#19740=CARTESIAN_POINT('Ctrl Pts',(-1.25812975907609,5.78143927338402,36.9355506113095));
#19741=CARTESIAN_POINT('Ctrl Pts',(-1.09651082282591,5.81661002995716,36.9277641647313));
#19742=CARTESIAN_POINT('Ctrl Pts',(-0.933397052074306,5.84500366855293,
36.9199777181531));
#19743=CARTESIAN_POINT('Ctrl Pts',(-0.769370716969568,5.86651508669071,
36.9121912715749));
#19744=CARTESIAN_POINT('Ctrl Pts',(-0.605338124629431,5.88802732544067,
36.9044045279612));
#19745=CARTESIAN_POINT('Ctrl Pts',(-0.44039321458797,5.90265677291185,36.8966177843476));
#19746=CARTESIAN_POINT('Ctrl Pts',(-0.275125508117482,5.91034994880025,
36.888831040734));
#19747=CARTESIAN_POINT('Ctrl Pts',(-0.109868732869458,5.91804261584261,
36.8810448121553));
#19748=CARTESIAN_POINT('Ctrl Pts',(0.0557104768455538,5.91879991464769,
36.8732585835765));
#19749=CARTESIAN_POINT('Ctrl Pts',(0.221020302878597,5.9126204502078,36.8654723549977));
#19750=CARTESIAN_POINT('Ctrl Pts',(0.386373646129538,5.90643935904609,36.8576840767222));
#19751=CARTESIAN_POINT('Ctrl Pts',(0.551457144383887,5.893317865741,36.8498957984468));
#19752=CARTESIAN_POINT('Ctrl Pts',(0.715680890929399,5.87330668574854,36.8421075201713));
#19753=CARTESIAN_POINT('Ctrl Pts',(0.871808565761582,5.85428203755611,36.8347031964746));
#19754=CARTESIAN_POINT('Ctrl Pts',(1.02715895519726,5.82903068068344,36.827298872778));
#19755=CARTESIAN_POINT('Ctrl Pts',(1.18123110126656,5.79763948930085,36.8198945490814));
#19756=CARTESIAN_POINT('Ctrl Pts',(1.34328647545535,5.76462176743793,36.8121065713198));
#19757=CARTESIAN_POINT('Ctrl Pts',(1.50398559573187,5.72479923784935,36.8043185935582));
#19758=CARTESIAN_POINT('Ctrl Pts',(1.66275273889179,5.67830818922396,36.7965306157965));
#19759=CARTESIAN_POINT('Ctrl Pts',(1.82148866706992,5.63182628113739,36.7887441692181));
#19760=CARTESIAN_POINT('Ctrl Pts',(1.97829306954646,5.578678559767,36.7809577226397));
#19761=CARTESIAN_POINT('Ctrl Pts',(2.13260440613291,5.51905145921312,36.7731712760613));
#19762=CARTESIAN_POINT('Ctrl Pts',(2.28692162934912,5.45942208401973,36.7653845324475));
#19763=CARTESIAN_POINT('Ctrl Pts',(2.43874529688261,5.39331294652846,36.7575977888337));
#19764=CARTESIAN_POINT('Ctrl Pts',(2.5875322119337,5.32095927579845,36.7498110452199));
#19765=CARTESIAN_POINT('Ctrl Pts',(2.73630928584353,5.24861039072242,36.742024816641));
#19766=CARTESIAN_POINT('Ctrl Pts',(2.88204972187158,5.1700179388011,36.734238588062));
#19767=CARTESIAN_POINT('Ctrl Pts',(3.02423323809834,5.08546397923348,36.7264523594831));
#19768=CARTESIAN_POINT('Ctrl Pts',(3.16645418362486,5.00088776113982,36.7186640812074));
#19769=CARTESIAN_POINT('Ctrl Pts',(3.30511606249578,4.91034706127661,36.7108758029317));
#19770=CARTESIAN_POINT('Ctrl Pts',(3.43972521460233,4.81416877669748,36.7030875246561));
#19771=CARTESIAN_POINT('Ctrl Pts',(3.56769826581228,4.72273198844711,36.6956832009603));
#19772=CARTESIAN_POINT('Ctrl Pts',(3.69200834128986,4.62620023382378,36.6882788772645));
#19773=CARTESIAN_POINT('Ctrl Pts',(3.81225718559272,4.52488958024355,36.6808745535688));
#19774=CARTESIAN_POINT('Ctrl Pts',(3.93873670806515,4.41832952837376,36.6730865758073));
#19775=CARTESIAN_POINT('Ctrl Pts',(4.06076820543666,4.30644407458904,36.6652985980459));
#19776=CARTESIAN_POINT('Ctrl Pts',(4.17791143177724,4.18962845974736,36.6575106202844));
#19777=CARTESIAN_POINT('Ctrl Pts',(4.29503162675513,4.07283581185714,36.6497241737062));
#19778=CARTESIAN_POINT('Ctrl Pts',(4.40726524219837,3.95111516247358,36.6419377271279));
#19779=CARTESIAN_POINT('Ctrl Pts',(4.51420848778309,3.82489899099664,36.6341512805497));
#19780=CARTESIAN_POINT('Ctrl Pts',(4.62115581301153,3.69867800465731,36.626364536936));
#19781=CARTESIAN_POINT('Ctrl Pts',(4.72281215496097,3.56796139429931,36.6185777933224));
#19782=CARTESIAN_POINT('Ctrl Pts',(4.81881318528843,3.43321570073748,36.6107910497088));
#19783=CARTESIAN_POINT('Ctrl Pts',(4.91480786586589,3.29847891959528,36.60300482113));
#19784=CARTESIAN_POINT('Ctrl Pts',(5.00514779802127,3.15971384888359,36.5952185925512));
#19785=CARTESIAN_POINT('Ctrl Pts',(5.08951118865056,3.01741717750475,36.5874323639724));
#19786=CARTESIAN_POINT('Ctrl Pts',(5.17389678763945,2.87508304703822,36.5796440856969));
#19787=CARTESIAN_POINT('Ctrl Pts',(5.25230253655634,2.72921573226415,36.5718558074214));
#19788=CARTESIAN_POINT('Ctrl Pts',(5.32445147856587,2.58033854656665,36.5640675291459));
#19789=CARTESIAN_POINT('Ctrl Pts',(5.39304354758304,2.43880086199333,36.5566632054494));
#19790=CARTESIAN_POINT('Ctrl Pts',(5.4559807433462,2.29454316233653,36.5492588817529));
#19791=CARTESIAN_POINT('Ctrl Pts',(5.51306469017522,2.14803358550169,36.5418545580564));
#19792=CARTESIAN_POINT('Ctrl Pts',(5.57310643425227,1.99393263408177,36.5340665802948));
#19793=CARTESIAN_POINT('Ctrl Pts',(5.62669373263113,1.83728512349577,36.5262786025332));
#19794=CARTESIAN_POINT('Ctrl Pts',(5.67362923987644,1.67864880511651,36.5184906247716));
#19795=CARTESIAN_POINT('Ctrl Pts',(5.72055551919885,1.52004367599674,36.5107041781931));
#19796=CARTESIAN_POINT('Ctrl Pts',(5.76083252622775,1.35945082550867,36.5029177316147));
#19797=CARTESIAN_POINT('Ctrl Pts',(5.79431274829024,1.19744325022155,36.4951312850362));
#19798=CARTESIAN_POINT('Ctrl Pts',(5.82779424754762,1.03542949471123,36.4873445414224));
#19799=CARTESIAN_POINT('Ctrl Pts',(5.8544783744694,0.872001218536192,36.4795577978086));
#19800=CARTESIAN_POINT('Ctrl Pts',(5.87426856794425,0.70774243490282,36.4717710541949));
#19801=CARTESIAN_POINT('Ctrl Pts',(5.89405745244584,0.543494515759324,36.4639848256159));
#19802=CARTESIAN_POINT('Ctrl Pts',(5.90695327787479,0.378416516380153,36.456198597037));
#19803=CARTESIAN_POINT('Ctrl Pts',(5.9129112598088,0.213098559653396,36.448412368458));
#19804=CARTESIAN_POINT('Ctrl Pts',(5.91887081016015,0.0477370835681996,
36.4406240901824));
#19805=CARTESIAN_POINT('Ctrl Pts',(5.91788885408841,-0.117864156602236,
36.4328358119067));
#19806=CARTESIAN_POINT('Ctrl Pts',(5.90997271752099,-0.283113123428823,
36.425047533631));
#19807=CARTESIAN_POINT('Ctrl Pts',(5.90244683882346,-0.440215476153025,
36.4176432099352));
#19808=CARTESIAN_POINT('Ctrl Pts',(5.88865401970231,-0.596999189135951,
36.4102388862395));
#19809=CARTESIAN_POINT('Ctrl Pts',(5.86864416935359,-0.75295828304897,36.4028345625437));
#19810=CARTESIAN_POINT('Ctrl Pts',(5.84759751122135,-0.916998377052583,
36.3950465847823));
#19811=CARTESIAN_POINT('Ctrl Pts',(5.81966491865678,-1.08018480844891,36.3872586070208));
#19812=CARTESIAN_POINT('Ctrl Pts',(5.78494010044588,-1.24193341075646,36.3794706292594));
#19813=CARTESIAN_POINT('Ctrl Pts',(5.75022210943202,-1.40365021190179,36.3716841826812));
#19814=CARTESIAN_POINT('Ctrl Pts',(5.7087146243404,-1.56392943576761,36.3638977361029));
#19815=CARTESIAN_POINT('Ctrl Pts',(5.66056240431804,-1.72219738396072,36.3561112895247));
#19816=CARTESIAN_POINT('Ctrl Pts',(5.61240834739688,-1.88047136971978,36.3483245459111));
#19817=CARTESIAN_POINT('Ctrl Pts',(5.55760913754932,-2.03673361942248,36.3405378022974));
#19818=CARTESIAN_POINT('Ctrl Pts',(5.49635954251166,-2.1904251509561,36.3327510586838));
#19819=CARTESIAN_POINT('Ctrl Pts',(5.43511399867645,-2.3441065169448,36.324964830105));
#19820=CARTESIAN_POINT('Ctrl Pts',(5.36741904184612,-2.49521720819887,36.3171786015262));
#19821=CARTESIAN_POINT('Ctrl Pts',(5.29351782400595,-2.64321766213668,36.3093923729474));
#19822=CARTESIAN_POINT('Ctrl Pts',(5.21959715193585,-2.79125707666196,36.3016040946719));
#19823=CARTESIAN_POINT('Ctrl Pts',(5.13946709532679,-2.93618433086334,36.2938158163964));
#19824=CARTESIAN_POINT('Ctrl Pts',(5.0534174752892,-3.07748312472087,36.2860275381209));
#19825=CARTESIAN_POINT('Ctrl Pts',(4.9716100182128,-3.21181602483592,36.2786232144244));
#19826=CARTESIAN_POINT('Ctrl Pts',(4.88445273274803,-3.34286938080751,36.2712188907279));
#19827=CARTESIAN_POINT('Ctrl Pts',(4.79223163475909,-3.47022283453299,36.2638145670314));
#19828=CARTESIAN_POINT('Ctrl Pts',(4.69523211262594,-3.60417509082536,36.2560265892698));
#19829=CARTESIAN_POINT('Ctrl Pts',(4.5925953855893,-3.73408176264429,36.2482386115083));
#19830=CARTESIAN_POINT('Ctrl Pts',(4.48468335102875,-3.85947480928501,36.2404506337468));
#19831=CARTESIAN_POINT('Ctrl Pts',(4.37679253289999,-3.98484320257699,36.2326641871685));
#19832=CARTESIAN_POINT('Ctrl Pts',(4.26362868502172,-4.10569949929104,36.2248777405902));
#19833=CARTESIAN_POINT('Ctrl Pts',(4.14559351607236,-4.22160928580545,36.2170912940119));
#19834=CARTESIAN_POINT('Ctrl Pts',(4.02755384434665,-4.33752349401765,36.2093045503982));
#19835=CARTESIAN_POINT('Ctrl Pts',(3.90464270492175,-4.44849058773415,36.2015178067844));
#19836=CARTESIAN_POINT('Ctrl Pts',(3.77729866963234,-4.55411301165153,36.1937310631707));
#19837=CARTESIAN_POINT('Ctrl Pts',(3.64996305719867,-4.65972844943534,36.1859448345919));
#19838=CARTESIAN_POINT('Ctrl Pts',(3.51819538169348,-4.75999972091334,36.178158606013));
#19839=CARTESIAN_POINT('Ctrl Pts',(3.38246740065049,-4.85456948101855,36.1703723774342));
#19840=CARTESIAN_POINT('Ctrl Pts',(3.24670368970339,-4.94916413627386,36.1625840991586));
#19841=CARTESIAN_POINT('Ctrl Pts',(3.10697785125219,-5.03805409663128,36.154795820883));
#19842=CARTESIAN_POINT('Ctrl Pts',(2.9637914831239,-5.12092478045345,36.1470075426074));
#19843=CARTESIAN_POINT('Ctrl Pts',(2.82766406432971,-5.19971001978793,36.1396032189111));
#19844=CARTESIAN_POINT('Ctrl Pts',(2.68840932636022,-5.27305504328633,36.1321988952149));
#19845=CARTESIAN_POINT('Ctrl Pts',(2.54647960178911,-5.34072768451753,36.1247945715187));
#19846=CARTESIAN_POINT('Ctrl Pts',(2.397195807073,-5.41190677481721,36.1170065937571));
#19847=CARTESIAN_POINT('Ctrl Pts',(2.24489905612588,-5.47683551091822,36.1092186159954));
#19848=CARTESIAN_POINT('Ctrl Pts',(2.09013112931874,-5.53527618324079,36.1014306382338));
#19849=CARTESIAN_POINT('Ctrl Pts',(1.93539363121317,-5.59370536562605,36.0936441916553));
#19850=CARTESIAN_POINT('Ctrl Pts',(1.77818622543415,-5.64564891663448,36.0858577450769));
#19851=CARTESIAN_POINT('Ctrl Pts',(1.61906955034184,-5.69091770751044,36.0780712984984));
#19852=CARTESIAN_POINT('Ctrl Pts',(1.45994680530705,-5.73618822528873,36.0702845548846));
#19853=CARTESIAN_POINT('Ctrl Pts',(1.29891495147683,-5.77478338217882,36.0624978112708));
#19854=CARTESIAN_POINT('Ctrl Pts',(1.13654935005534,-5.80656405608246,36.054711067657));
#19855=CARTESIAN_POINT('Ctrl Pts',(0.974194487903553,-5.8383426279323,36.046924839078));
#19856=CARTESIAN_POINT('Ctrl Pts',(0.810506368343906,-5.86330755749171,
36.039138610499));
#19857=CARTESIAN_POINT('Ctrl Pts',(0.646070242176841,-5.88137091201308,
36.03135238192));
#19858=CARTESIAN_POINT('Ctrl Pts',(0.481590828790343,-5.89943902164763,
36.0235641036443));
#19859=CARTESIAN_POINT('Ctrl Pts',(0.316363332966109,-5.91060188900507,
36.0157758253686));
#19860=CARTESIAN_POINT('Ctrl Pts',(0.150978735716734,-5.9148234110463,36.0079875470929));
#19861=CARTESIAN_POINT('Ctrl Pts',(-0.00625256097642329,-5.91883681613723,
36.0005832233973));
#19862=CARTESIAN_POINT('Ctrl Pts',(-0.16362557892651,-5.91657678607358,
35.9931788997018));
#19863=CARTESIAN_POINT('Ctrl Pts',(-0.320632041300111,-5.90805599639947,
35.9857745760062));
#19864=CARTESIAN_POINT('Ctrl Pts',(-0.485773773027661,-5.89909370312061,
35.9779865982448));
#19865=CARTESIAN_POINT('Ctrl Pts',(-0.650569029001088,-5.88320141796559,
35.9701986204834));
#19866=CARTESIAN_POINT('Ctrl Pts',(-0.814428344223128,-5.86042976535219,
35.9624106427221));
#19867=CARTESIAN_POINT('Ctrl Pts',(-0.978255443297349,-5.83766258984115,
35.954624196144));
#19868=CARTESIAN_POINT('Ctrl Pts',(-1.14114665246819,-5.80801878955106,
35.9468377495659));
#19869=CARTESIAN_POINT('Ctrl Pts',(-1.30251920354592,-5.77160066938922,
35.9390513029878));
#19870=CARTESIAN_POINT('Ctrl Pts',(-1.4638979106241,-5.73518115995788,35.9312645593742));
#19871=CARTESIAN_POINT('Ctrl Pts',(-1.62375753111289,-5.69198688002801,
35.9234778157606));
#19872=CARTESIAN_POINT('Ctrl Pts',(-1.78152630677224,-5.64217108751396,
35.9156910721471));
#19873=CARTESIAN_POINT('Ctrl Pts',(-1.93928464720688,-5.59235858994206,
35.9079048435684));
#19874=CARTESIAN_POINT('Ctrl Pts',(-2.09495211484654,-5.53592555254885,
35.9001186149897));
#19875=CARTESIAN_POINT('Ctrl Pts',(-2.24797277109128,-5.47307491113836,
35.892332386411));
#19876=CARTESIAN_POINT('Ctrl Pts',(-2.40103370947464,-5.41020772452207,
35.8845441081356));
#19877=CARTESIAN_POINT('Ctrl Pts',(-2.55144614765425,-5.34091967776843,
35.8767558298601));
#19878=CARTESIAN_POINT('Ctrl Pts',(-2.69867392511282,-5.26546195584169,
35.8689675515847));
#19879=CARTESIAN_POINT('Ctrl Pts',(-2.83864351568707,-5.19372422654856,
35.8615632278877));
#19880=CARTESIAN_POINT('Ctrl Pts',(-2.97573464857824,-5.11641060674806,
35.8541589041908));
#19881=CARTESIAN_POINT('Ctrl Pts',(-3.10950712595014,-5.03377552103441,
35.8467545804938));
#19882=CARTESIAN_POINT('Ctrl Pts',(-3.25021100675418,-4.9468587091542,35.8389666027321));
#19883=CARTESIAN_POINT('Ctrl Pts',(-3.38729352243181,-4.85402323632069,
35.8311786249705));
#19884=CARTESIAN_POINT('Ctrl Pts',(-3.52026135712141,-4.75559570822181,
35.8233906472088));
#19885=CARTESIAN_POINT('Ctrl Pts',(-3.65320304919531,-4.65718753181839,
35.8156042006303));
#19886=CARTESIAN_POINT('Ctrl Pts',(-3.78203141775639,-4.55318968387259,
35.8078177540518));
#19887=CARTESIAN_POINT('Ctrl Pts',(-3.9062837644773,-4.4439709398106,35.8000313074734));
#19888=CARTESIAN_POINT('Ctrl Pts',(-4.0305408511444,-4.33474802930037,35.7922445638595));
#19889=CARTESIAN_POINT('Ctrl Pts',(-4.15022132405298,-4.2203040321326,35.7844578202457));
#19890=CARTESIAN_POINT('Ctrl Pts',(-4.26489654111093,-4.10104719018448,
35.7766710766319));
#19891=CARTESIAN_POINT('Ctrl Pts',(-4.37956417326116,-3.9817982361843,35.7688848480529));
#19892=CARTESIAN_POINT('Ctrl Pts',(-4.4892269906369,-3.85773730487219,35.7610986194739));
#19893=CARTESIAN_POINT('Ctrl Pts',(-4.59349401991493,-3.72930868278637,
35.7533123908949));
#19894=CARTESIAN_POINT('Ctrl Pts',(-4.69778849711381,-3.60084625232721,
35.7455241126192));
#19895=CARTESIAN_POINT('Ctrl Pts',(-4.79668414484876,-3.46801408061042,
35.7377358343436));
#19896=CARTESIAN_POINT('Ctrl Pts',(-4.88983045017742,-3.33128934963892,
35.7299475560679));
#19897=CARTESIAN_POINT('Ctrl Pts',(-4.97838473281677,-3.20130501555805,
35.7225432323723));
#19898=CARTESIAN_POINT('Ctrl Pts',(-5.06174274352001,-3.06780289360419,
35.7151389086767));
#19899=CARTESIAN_POINT('Ctrl Pts',(-5.13963977493379,-2.93121707596326,
35.7077345849812));
#19900=CARTESIAN_POINT('Ctrl Pts',(-5.22157303086326,-2.78755408200825,
35.6999466072197));
#19901=CARTESIAN_POINT('Ctrl Pts',(-5.2974936718184,-2.64042795449758,35.6921586294583));
#19902=CARTESIAN_POINT('Ctrl Pts',(-5.36712490374431,-2.49036158621748,
35.6843706516968));
#19903=CARTESIAN_POINT('Ctrl Pts',(-5.43674244557314,-2.34032472227175,
35.6765842051186));
#19904=CARTESIAN_POINT('Ctrl Pts',(-5.50007291124137,-2.18734906067767,
35.6687977585403));
#19905=CARTESIAN_POINT('Ctrl Pts',(-5.5568865740533,-2.03197986348443,35.661011311962));
#19906=CARTESIAN_POINT('Ctrl Pts',(-5.61370240417827,-1.8766047393069,35.6532245683484));
#19907=CARTESIAN_POINT('Ctrl Pts',(-5.6640008205388,-1.71883619556755,35.6454378247348));
#19908=CARTESIAN_POINT('Ctrl Pts',(-5.70760088899002,-1.55923784410856,
35.6376510811211));
#19909=CARTESIAN_POINT('Ctrl Pts',(-5.75119807362305,-1.39965004888596,
35.6298648525423));
#19910=CARTESIAN_POINT('Ctrl Pts',(-5.78809771283873,-1.23823299644907,
35.6220786239635));
#19911=CARTESIAN_POINT('Ctrl Pts',(-5.81816919893528,-1.07556391491199,
35.6142923953847));
#19912=CARTESIAN_POINT('Ctrl Pts',(-5.84824860124243,-0.912852011324053,
35.6065041171092));
#19913=CARTESIAN_POINT('Ctrl Pts',(-5.87149619862239,-0.748887734121178,
35.5987158388337));
#19914=CARTESIAN_POINT('Ctrl Pts',(-5.8878326534242,-0.584257826453108,
35.5909275605582));
#19915=CARTESIAN_POINT('Ctrl Pts',(-5.90336373681984,-0.427744013852536,
35.5835232368617));
#19916=CARTESIAN_POINT('Ctrl Pts',(-5.91264866230486,-0.27062888192908,
35.5761189131652));
#19917=CARTESIAN_POINT('Ctrl Pts',(-5.91566280353483,-0.113420268798857,
35.5687145894688));
#19918=CARTESIAN_POINT('Ctrl Pts',(-5.91638732153701,-0.0756315715813799,
35.5669347903808));
#19919=CARTESIAN_POINT('Ctrl Pts',(-5.9167497460477,-0.0378359212400649,
35.5651549912929));
#19920=CARTESIAN_POINT('Ctrl Pts',(-5.91674999986659,-3.97337130474773E-5,
35.5633751922049));
#19921=CARTESIAN_POINT('Ctrl Pts',(-5.91702973121491,0.000122477731109751,
35.3116248172195));
#19922=CARTESIAN_POINT('Ctrl Pts',(-5.91624721053643,-0.84738287545781,
35.3515259607155));
#19923=CARTESIAN_POINT('Ctrl Pts',(-5.51859916564424,-2.67934504448225,
35.437742565973));
#19924=CARTESIAN_POINT('Ctrl Pts',(-3.69398986882353,-4.93928937015303,
35.5702746329922));
#19925=CARTESIAN_POINT('Ctrl Pts',(-0.880646612225805,-6.10463775972444,
35.7092210182773));
#19926=CARTESIAN_POINT('Ctrl Pts',(2.14735808427326,-5.78195415849901,35.8481674035626));
#19927=CARTESIAN_POINT('Ctrl Pts',(4.65193491316365,-4.04989409698157,35.9871137888476));
#19928=CARTESIAN_POINT('Ctrl Pts',(6.02258238500697,-1.3306547444329,36.1260601741327));
#19929=CARTESIAN_POINT('Ctrl Pts',(5.92519922033558,1.71293748643058,36.265006559418));
#19930=CARTESIAN_POINT('Ctrl Pts',(4.38352298886376,4.33899375883021,36.4039529447029));
#19931=CARTESIAN_POINT('Ctrl Pts',(1.77334397367895,5.90740144091314,36.5428993299881));
#19932=CARTESIAN_POINT('Ctrl Pts',(-1.26909534381814,6.03585434229275,36.6818457152732));
#19933=CARTESIAN_POINT('Ctrl Pts',(-4.0021871545,4.69304150987745,36.8207921005585));
#19934=CARTESIAN_POINT('Ctrl Pts',(-5.60347011563501,2.42737082897272,36.947385131399));
#19935=CARTESIAN_POINT('Ctrl Pts',(-5.91593150251293,0.721344592538736,
37.0276627004779));
#19936=CARTESIAN_POINT('Ctrl Pts',(-5.91663997003447,-0.000151814981789717,
37.0616248077951));
#19937=CARTESIAN_POINT('Origin',(0.,0.,0.));
#19938=CARTESIAN_POINT('',(-5.91674999872984,0.000122598544046725,39.0633751922447));
#19939=CARTESIAN_POINT('',(-5.91674999852514,0.000132108695946752,38.8116248077543));
#19940=CARTESIAN_POINT('',(-5.91675,-7.2459289488551E-16,0.));
#19941=CARTESIAN_POINT('Ctrl Pts',(-5.91674999872983,0.000122599388472625,
39.0633751922049));
#19942=CARTESIAN_POINT('Ctrl Pts',(-5.9167471879205,0.135774630831213,39.0569882872305));
#19943=CARTESIAN_POINT('Ctrl Pts',(-5.91207783419387,0.271407816372676,
39.050601382256));
#19944=CARTESIAN_POINT('Ctrl Pts',(-5.90275448146221,0.406718691576558,
39.0442144772815));
#19945=CARTESIAN_POINT('Ctrl Pts',(-5.89138589776885,0.571712235600173,
39.0364264995193));
#19946=CARTESIAN_POINT('Ctrl Pts',(-5.87309310901039,0.736258323381238,
39.028638521757));
#19947=CARTESIAN_POINT('Ctrl Pts',(-5.8479353267559,0.899768290495045,39.0208505439948));
#19948=CARTESIAN_POINT('Ctrl Pts',(-5.82278249073704,1.06324611014776,39.0130640974158));
#19949=CARTESIAN_POINT('Ctrl Pts',(-5.79076740286871,1.22568789995535,39.0052776508368));
#19950=CARTESIAN_POINT('Ctrl Pts',(-5.75200085210035,1.38651244492677,38.9974912042578));
#19951=CARTESIAN_POINT('Ctrl Pts',(-5.71323282247546,1.54734312499211,38.9897044606434));
#19952=CARTESIAN_POINT('Ctrl Pts',(-5.66771288561786,1.70655612520183,38.981917717029));
#19953=CARTESIAN_POINT('Ctrl Pts',(-5.61560261758027,1.86358198207797,38.9741309734147));
#19954=CARTESIAN_POINT('Ctrl Pts',(-5.5634957962471,2.02059745286828,38.9663447448352));
#19955=CARTESIAN_POINT('Ctrl Pts',(-5.50479961680108,2.17542576654225,38.9585585162557));
#19956=CARTESIAN_POINT('Ctrl Pts',(-5.43972509730625,2.32751400172728,38.9507722876762));
#19957=CARTESIAN_POINT('Ctrl Pts',(-5.37463344717792,2.47964227359391,38.9429840094));
#19958=CARTESIAN_POINT('Ctrl Pts',(-5.30316022584418,2.62902873087834,38.9351957311238));
#19959=CARTESIAN_POINT('Ctrl Pts',(-5.22556440710126,2.77514093150896,38.9274074528476));
#19960=CARTESIAN_POINT('Ctrl Pts',(-5.15179398714427,2.91404994201986,38.9200031291548));
#19961=CARTESIAN_POINT('Ctrl Pts',(-5.07249022789409,3.04999952188263,38.912598805462));
#19962=CARTESIAN_POINT('Ctrl Pts',(-4.98791394360065,3.18255322873542,38.9051944817693));
#19963=CARTESIAN_POINT('Ctrl Pts',(-4.89895535014512,3.3219751886554,38.8974065040081));
#19964=CARTESIAN_POINT('Ctrl Pts',(-4.80413151259739,3.45768989290758,38.8896185262469));
#19965=CARTESIAN_POINT('Ctrl Pts',(-4.70377619292479,3.58920883891896,38.8818305484857));
#19966=CARTESIAN_POINT('Ctrl Pts',(-4.6034406039686,3.72070192717776,38.8740441019077));
#19967=CARTESIAN_POINT('Ctrl Pts',(-4.49757589656964,3.84800064927392,38.8662576553297));
#19968=CARTESIAN_POINT('Ctrl Pts',(-4.3865575516465,3.97064773161672,38.8584712087517));
#19969=CARTESIAN_POINT('Ctrl Pts',(-4.27553497162364,4.09329949266939,38.8506844651383));
#19970=CARTESIAN_POINT('Ctrl Pts',(-4.15935857218371,4.21129901933567,38.8428977215249));
#19971=CARTESIAN_POINT('Ctrl Pts',(-4.03844280007124,4.32422366593737,38.8351109779115));
#19972=CARTESIAN_POINT('Ctrl Pts',(-3.91753502563239,4.43714084341859,38.8273247493329));
#19973=CARTESIAN_POINT('Ctrl Pts',(-3.79188873946776,4.54498359450944,38.8195385207543));
#19974=CARTESIAN_POINT('Ctrl Pts',(-3.66195388006204,4.64736746371519,38.8117522921757));
#19975=CARTESIAN_POINT('Ctrl Pts',(-3.53198481577141,4.74977828510667,38.8039640139004));
#19976=CARTESIAN_POINT('Ctrl Pts',(-3.39772517230712,4.84672715368042,38.7961757356252));
#19977=CARTESIAN_POINT('Ctrl Pts',(-3.25965719033948,4.93787054953531,38.7883874573499));
#19978=CARTESIAN_POINT('Ctrl Pts',(-3.12839582619023,5.02452066422961,38.7809831336521));
#19979=CARTESIAN_POINT('Ctrl Pts',(-2.99369279308517,5.10592378088708,38.7735788099543));
#19980=CARTESIAN_POINT('Ctrl Pts',(-2.85598599568298,5.1818215479658,38.7661744862566));
#19981=CARTESIAN_POINT('Ctrl Pts',(-2.71114393858502,5.26165194791852,38.7583865084949));
#19982=CARTESIAN_POINT('Ctrl Pts',(-2.56292676073579,5.33541989021992,38.7505985307332));
#19983=CARTESIAN_POINT('Ctrl Pts',(-2.41186133414479,5.40285623234205,38.7428105529715));
#19984=CARTESIAN_POINT('Ctrl Pts',(-2.2608256083118,5.47027931590116,38.735024106393));
#19985=CARTESIAN_POINT('Ctrl Pts',(-2.10694304269897,5.53137315293793,38.7272376598145));
#19986=CARTESIAN_POINT('Ctrl Pts',(-1.95076219010932,5.58591598935572,38.719451213236));
#19987=CARTESIAN_POINT('Ctrl Pts',(-1.79457537957215,5.64046090645979,38.7116644696221));
#19988=CARTESIAN_POINT('Ctrl Pts',(-1.63609040698825,5.68845421379307,38.7038777260083));
#19989=CARTESIAN_POINT('Ctrl Pts',(-1.47587346176335,5.72972321210743,38.6960909823944));
#19990=CARTESIAN_POINT('Ctrl Pts',(-1.31566711369084,5.77098948078627,38.6883047538154));
#19991=CARTESIAN_POINT('Ctrl Pts',(-1.15372933172641,5.80553225087759,38.6805185252363));
#19992=CARTESIAN_POINT('Ctrl Pts',(-0.990639186501122,5.83322934271133,
38.6727322966573));
#19993=CARTESIAN_POINT('Ctrl Pts',(-0.827506108380989,5.86093372570499,
38.6649440183816));
#19994=CARTESIAN_POINT('Ctrl Pts',(-0.663220375753615,5.88178877399905,
38.6571557401059));
#19995=CARTESIAN_POINT('Ctrl Pts',(-0.498369825920027,5.895723711226,38.6493674618301));
#19996=CARTESIAN_POINT('Ctrl Pts',(-0.341646248626712,5.90897166953594,
38.6419631381348));
#19997=CARTESIAN_POINT('Ctrl Pts',(-0.184412465069586,5.91596536824798,
38.6345588144394));
#19998=CARTESIAN_POINT('Ctrl Pts',(-0.027176618381928,5.91668758630311,
38.627154490744));
#19999=CARTESIAN_POINT('Ctrl Pts',(0.138206383183557,5.91744722599252,38.6193665129826));
#20000=CARTESIAN_POINT('Ctrl Pts',(0.303650828059728,5.91126848996617,38.6115785352211));
#20001=CARTESIAN_POINT('Ctrl Pts',(0.468565294811073,5.89816726848253,38.6037905574597));
#20002=CARTESIAN_POINT('Ctrl Pts',(0.633447337964542,5.88506862281134,38.5960041108814));
#20003=CARTESIAN_POINT('Ctrl Pts',(0.797799292548417,5.86505023260907,38.5882176643032));
#20004=CARTESIAN_POINT('Ctrl Pts',(0.961033384763278,5.83817997289142,38.5804312177249));
#20005=CARTESIAN_POINT('Ctrl Pts',(1.12427370399059,5.81130868813396,38.5726444741113));
#20006=CARTESIAN_POINT('Ctrl Pts',(1.28639575957966,5.77758505882802,38.5648577304977));
#20007=CARTESIAN_POINT('Ctrl Pts',(1.4468197738114,5.7371284720327,38.557070986884));
#20008=CARTESIAN_POINT('Ctrl Pts',(1.6072331771948,5.69667456113793,38.5492847583052));
#20009=CARTESIAN_POINT('Ctrl Pts',(1.76594845412817,5.64948866219114,38.5414985297264));
#20010=CARTESIAN_POINT('Ctrl Pts',(1.92239869929495,5.5957406840783,38.5337123011476));
#20011=CARTESIAN_POINT('Ctrl Pts',(2.07889012942669,5.54197855700332,38.5259240228721));
#20012=CARTESIAN_POINT('Ctrl Pts',(2.23311503328575,5.4816510010094,38.5181357445966));
#20013=CARTESIAN_POINT('Ctrl Pts',(2.38452341353271,5.41497725321301,38.5103474663211));
#20014=CARTESIAN_POINT('Ctrl Pts',(2.52846750721535,5.35159045663462,38.5029431426246));
#20015=CARTESIAN_POINT('Ctrl Pts',(2.66986585041888,5.28246822388523,38.4955388189281));
#20016=CARTESIAN_POINT('Ctrl Pts',(2.8082640521683,5.20783866645265,38.4881344952316));
#20017=CARTESIAN_POINT('Ctrl Pts',(2.95383333866183,5.12934218825087,38.48034651747));
#20018=CARTESIAN_POINT('Ctrl Pts',(3.09613539840919,5.04472443058755,38.4725585397084));
#20019=CARTESIAN_POINT('Ctrl Pts',(3.234658571696,4.95428243916852,38.4647705619468));
#20020=CARTESIAN_POINT('Ctrl Pts',(3.37315451013931,4.86385822942041,38.4569841153684));
#20021=CARTESIAN_POINT('Ctrl Pts',(3.50787277714379,4.76761224530614,38.44919766879));
#20022=CARTESIAN_POINT('Ctrl Pts',(3.63832979901089,4.66588542895444,38.4414112222116));
#20023=CARTESIAN_POINT('Ctrl Pts',(3.76879179751932,4.564154731954,38.4336244785978));
#20024=CARTESIAN_POINT('Ctrl Pts',(3.89499197119463,4.45694297771329,38.4258377349841));
#20025=CARTESIAN_POINT('Ctrl Pts',(4.01647842399972,4.34463250828476,38.4180509913703));
#20026=CARTESIAN_POINT('Ctrl Pts',(4.13795684138479,4.23232946735359,38.4102647627913));
#20027=CARTESIAN_POINT('Ctrl Pts',(4.25472192722656,4.11492860312819,38.4024785342124));
#20028=CARTESIAN_POINT('Ctrl Pts',(4.36635727055808,3.99285045404215,38.3946923056335));
#20029=CARTESIAN_POINT('Ctrl Pts',(4.47802200149266,3.87074016832195,38.3869040273578));
#20030=CARTESIAN_POINT('Ctrl Pts',(4.58455407432886,3.74395037204153,38.3791157490822));
#20031=CARTESIAN_POINT('Ctrl Pts',(4.68557553505414,3.61293682034465,38.3713274708065));
#20032=CARTESIAN_POINT('Ctrl Pts',(4.78161673555627,3.48838210992292,38.3639231471107));
#20033=CARTESIAN_POINT('Ctrl Pts',(4.87267741053592,3.36001027504955,38.3565188234148));
#20034=CARTESIAN_POINT('Ctrl Pts',(4.95846779589131,3.22823909889103,38.349114499719));
#20035=CARTESIAN_POINT('Ctrl Pts',(5.04870339886322,3.08964021644371,38.3413265219575));
#20036=CARTESIAN_POINT('Ctrl Pts',(5.13314033220658,2.94723078765855,38.3335385441961));
#20037=CARTESIAN_POINT('Ctrl Pts',(5.21147154663315,2.80151653236834,38.3257505664346));
#20038=CARTESIAN_POINT('Ctrl Pts',(5.28978736047149,2.65583092574979,38.3179641198564));
#20039=CARTESIAN_POINT('Ctrl Pts',(5.36199969940708,2.50684207037001,38.3101776732781));
#20040=CARTESIAN_POINT('Ctrl Pts',(5.42784718535444,2.35508078310276,38.3023912266998));
#20041=CARTESIAN_POINT('Ctrl Pts',(5.49369718323489,2.20331370648465,38.2946044830862));
#20042=CARTESIAN_POINT('Ctrl Pts',(5.55318171145486,2.0487742779088,38.2868177394725));
#20043=CARTESIAN_POINT('Ctrl Pts',(5.60608702159078,1.89201450016945,38.2790309958589));
#20044=CARTESIAN_POINT('Ctrl Pts',(5.65898883243623,1.73526509091662,38.2712447672801));
#20045=CARTESIAN_POINT('Ctrl Pts',(5.70531219394555,1.57629592922152,38.2634585387013));
#20046=CARTESIAN_POINT('Ctrl Pts',(5.74489279681686,1.41567556861795,38.2556723101225));
#20047=CARTESIAN_POINT('Ctrl Pts',(5.78448381913969,1.25501292528147,38.2478840318469));
#20048=CARTESIAN_POINT('Ctrl Pts',(5.81732845757911,1.09269852447719,38.2400957535714));
#20049=CARTESIAN_POINT('Ctrl Pts',(5.84331302498732,0.929313431794404,38.2323074752959));
#20050=CARTESIAN_POINT('Ctrl Pts',(5.86801657837826,0.773983066006007,38.2249031515995));
#20051=CARTESIAN_POINT('Ctrl Pts',(5.88652011578327,0.617685293712312,38.217498827903));
#20052=CARTESIAN_POINT('Ctrl Pts',(5.89876920452956,0.460925627616558,38.2100945042066));
#20053=CARTESIAN_POINT('Ctrl Pts',(5.91165297820922,0.296043479898478,38.202306526445));
#20054=CARTESIAN_POINT('Ctrl Pts',(5.91762155709263,0.130591320086449,38.1945185486834));
#20055=CARTESIAN_POINT('Ctrl Pts',(5.91664742458522,-0.0348398571903262,
38.1867305709218));
#20056=CARTESIAN_POINT('Ctrl Pts',(5.91567348360062,-0.200238509279394,
38.1789441243434));
#20057=CARTESIAN_POINT('Ctrl Pts',(5.90775955667576,-0.36561586771609,38.171157677765));
#20058=CARTESIAN_POINT('Ctrl Pts',(5.89293023949894,-0.530380764073326,
38.1633712311866));
#20059=CARTESIAN_POINT('Ctrl Pts',(5.8781003566171,-0.695151945839907,38.1555844875728));
#20060=CARTESIAN_POINT('Ctrl Pts',(5.85635458030705,-0.859310300168159,
38.147797743959));
#20061=CARTESIAN_POINT('Ctrl Pts',(5.82776946593429,-1.02226885623303,38.1400110003452));
#20062=CARTESIAN_POINT('Ctrl Pts',(5.79918624225299,-1.18521663380852,38.1322247717663));
#20063=CARTESIAN_POINT('Ctrl Pts',(5.76376464109781,-1.34696445717608,38.1244385431873));
#20064=CARTESIAN_POINT('Ctrl Pts',(5.72163254750092,-1.5069344889139,38.1166523146084));
#20065=CARTESIAN_POINT('Ctrl Pts',(5.67948936278175,-1.66694663218784,38.1088640363327));
#20066=CARTESIAN_POINT('Ctrl Pts',(5.63063223530453,-1.82517973895856,38.1010757580571));
#20067=CARTESIAN_POINT('Ctrl Pts',(5.5752394852801,-1.98106921743631,38.0932874797814));
#20068=CARTESIAN_POINT('Ctrl Pts',(5.52257754421092,-2.12927349552827,38.0858831560856));
#20069=CARTESIAN_POINT('Ctrl Pts',(5.46400894584996,-2.27535940793032,38.0784788323898));
#20070=CARTESIAN_POINT('Ctrl Pts',(5.39972787092285,-2.41885706119212,38.071074508694));
#20071=CARTESIAN_POINT('Ctrl Pts',(5.33211608049055,-2.56979002662347,38.0632865309325));
#20072=CARTESIAN_POINT('Ctrl Pts',(5.25815992810046,-2.7179133827933,38.055498553171));
#20073=CARTESIAN_POINT('Ctrl Pts',(5.17811814410162,-2.86269506727936,38.0477105754096));
#20074=CARTESIAN_POINT('Ctrl Pts',(5.09809209700367,-3.00744828644511,38.0399241288313));
#20075=CARTESIAN_POINT('Ctrl Pts',(5.01198296015422,-3.14886086535153,38.032137682253));
#20076=CARTESIAN_POINT('Ctrl Pts',(4.92009530148782,-3.28642553342951,38.0243512356748));
#20077=CARTESIAN_POINT('Ctrl Pts',(4.82820413751447,-3.42399544928935,38.0165644920611));
#20078=CARTESIAN_POINT('Ctrl Pts',(4.73053418482264,-3.55771689268298,38.0087777484475));
#20079=CARTESIAN_POINT('Ctrl Pts',(4.62743362249892,-3.68711114992029,38.0009910048338));
#20080=CARTESIAN_POINT('Ctrl Pts',(4.52433987950609,-3.81649684869549,37.993204776255));
#20081=CARTESIAN_POINT('Ctrl Pts',(4.41581644492041,-3.94155568419812,37.9854185476762));
#20082=CARTESIAN_POINT('Ctrl Pts',(4.30225219322678,-4.06184153166706,37.9776323190974));
#20083=CARTESIAN_POINT('Ctrl Pts',(4.18865804615181,-4.18215904395327,37.9698440408218));
#20084=CARTESIAN_POINT('Ctrl Pts',(4.07002064848399,-4.29770082365773,37.9620557625463));
#20085=CARTESIAN_POINT('Ctrl Pts',(3.94676681635972,-4.40805651730802,37.9542674842708));
#20086=CARTESIAN_POINT('Ctrl Pts',(3.82958927883582,-4.51297178209789,37.9468631605744));
#20087=CARTESIAN_POINT('Ctrl Pts',(3.70823971020562,-4.61319980569276,37.9394588368779));
#20088=CARTESIAN_POINT('Ctrl Pts',(3.58311352307887,-4.70842097132673,37.9320545131815));
#20089=CARTESIAN_POINT('Ctrl Pts',(3.45150393891052,-4.80857600921993,37.9242665354199));
#20090=CARTESIAN_POINT('Ctrl Pts',(3.31566889624897,-4.90322738166368,37.9164785576583));
#20091=CARTESIAN_POINT('Ctrl Pts',(3.17609024029319,-4.9920317855573,37.9086905798967));
#20092=CARTESIAN_POINT('Ctrl Pts',(3.03653902669779,-5.08081872974378,37.9009041333183));
#20093=CARTESIAN_POINT('Ctrl Pts',(2.89324593784037,-5.16376082767102,37.8931176867399));
#20094=CARTESIAN_POINT('Ctrl Pts',(2.74672119710268,-5.24055848434943,37.8853312401615));
#20095=CARTESIAN_POINT('Ctrl Pts',(2.60019086677646,-5.31735907068531,37.8775444965477));
#20096=CARTESIAN_POINT('Ctrl Pts',(2.45042891906903,-5.38801459489937,37.8697577529339));
#20097=CARTESIAN_POINT('Ctrl Pts',(2.29797019854953,-5.45227141007106,37.8619710093201));
#20098=CARTESIAN_POINT('Ctrl Pts',(2.14552156203383,-5.51652397513513,37.8541847807412));
#20099=CARTESIAN_POINT('Ctrl Pts',(1.9903768041871,-5.57437855408287,37.8463985521622));
#20100=CARTESIAN_POINT('Ctrl Pts',(1.83309090073417,-5.6256295925119,37.8386123235833));
#20101=CARTESIAN_POINT('Ctrl Pts',(1.6757635923322,-5.67689412259268,37.8308240453077));
#20102=CARTESIAN_POINT('Ctrl Pts',(1.51629431545865,-5.72155153762187,37.823035767032));
#20103=CARTESIAN_POINT('Ctrl Pts',(1.35525423592285,-5.75944585168688,37.8152474887563));
#20104=CARTESIAN_POINT('Ctrl Pts',(1.20215327641925,-5.79547201275068,37.8078431650605));
#20105=CARTESIAN_POINT('Ctrl Pts',(1.04763291803855,-5.82538577818048,37.8004388413647));
#20106=CARTESIAN_POINT('Ctrl Pts',(0.892193321711462,-5.84909579671879,
37.7930345176689));
#20107=CARTESIAN_POINT('Ctrl Pts',(0.728699642994194,-5.87403434677219,
37.7852465399075));
#20108=CARTESIAN_POINT('Ctrl Pts',(0.56413045196339,-5.89211810973065,37.777458562146));
#20109=CARTESIAN_POINT('Ctrl Pts',(0.399073134922297,-5.90327631027748,
37.7696705843846));
#20110=CARTESIAN_POINT('Ctrl Pts',(0.23404826956456,-5.91443231702644,37.7618841378063));
#20111=CARTESIAN_POINT('Ctrl Pts',(0.0685357883111578,-5.91866545666666,
37.754097691228));
#20112=CARTESIAN_POINT('Ctrl Pts',(-0.0968729282384096,-5.9159569131523,
37.7463112446498));
#20113=CARTESIAN_POINT('Ctrl Pts',(-0.262287954757499,-5.91324826631312,
37.7385245010362));
#20114=CARTESIAN_POINT('Ctrl Pts',(-0.427598889091094,-5.90359740770875,
37.7307377574225));
#20115=CARTESIAN_POINT('Ctrl Pts',(-0.59221472716635,-5.88703764888822,
37.7229510138089));
#20116=CARTESIAN_POINT('Ctrl Pts',(-0.75681967713536,-5.87047898537185,
37.7151647852301));
#20117=CARTESIAN_POINT('Ctrl Pts',(-0.920729304889136,-5.84701236820843,
37.7073785566513));
#20118=CARTESIAN_POINT('Ctrl Pts',(-1.08335795159065,-5.81672297012891,
37.6995923280725));
#20119=CARTESIAN_POINT('Ctrl Pts',(-1.2460294096993,-5.78642559847414,37.691804049797));
#20120=CARTESIAN_POINT('Ctrl Pts',(-1.40741889821639,-5.74930191359766,
37.6840157715215));
#20121=CARTESIAN_POINT('Ctrl Pts',(-1.56695027028627,-5.70548835884798,
37.676227493246));
#20122=CARTESIAN_POINT('Ctrl Pts',(-1.71861690015822,-5.66383476993079,
37.6688231695495));
#20123=CARTESIAN_POINT('Ctrl Pts',(-1.86860395299201,-5.61613510008907,
37.661418845853));
#20124=CARTESIAN_POINT('Ctrl Pts',(-2.01642856245358,-5.56254855394732,
37.6540145221565));
#20125=CARTESIAN_POINT('Ctrl Pts',(-2.17191268474426,-5.50618542791717,
37.6462265443949));
#20126=CARTESIAN_POINT('Ctrl Pts',(-2.32505994031396,-5.44328901123178,
37.6384385666333));
#20127=CARTESIAN_POINT('Ctrl Pts',(-2.47532072830056,-5.37407832605235,
37.6306505888717));
#20128=CARTESIAN_POINT('Ctrl Pts',(-2.6255519737283,-5.30488124828685,37.6228641422933));
#20129=CARTESIAN_POINT('Ctrl Pts',(-2.77289759384758,-5.22937251266861,
37.6150776957148));
#20130=CARTESIAN_POINT('Ctrl Pts',(-2.916829352024,-5.14781867334809,37.6072912491364));
#20131=CARTESIAN_POINT('Ctrl Pts',(-3.06076660087231,-5.06626172293257,
37.5995045055226));
#20132=CARTESIAN_POINT('Ctrl Pts',(-3.20128944722143,-4.97865936145136,
37.5917177619088));
#20133=CARTESIAN_POINT('Ctrl Pts',(-3.33789493680239,-4.88532373066197,
37.583931018295));
#20134=CARTESIAN_POINT('Ctrl Pts',(-3.47449139095203,-4.7919942733264,37.5761447897161));
#20135=CARTESIAN_POINT('Ctrl Pts',(-3.6071707430359,-4.69293248592507,37.5683585611371));
#20136=CARTESIAN_POINT('Ctrl Pts',(-3.73545955613584,-4.58849348555421,
37.5605723325582));
#20137=CARTESIAN_POINT('Ctrl Pts',(-3.86378214080505,-4.48402699199162,
37.5527840542825));
#20138=CARTESIAN_POINT('Ctrl Pts',(-3.98771162775715,-4.37418065728952,
37.5449957760069));
#20139=CARTESIAN_POINT('Ctrl Pts',(-4.10680747312832,-4.25935006088457,
37.5372074977312));
#20140=CARTESIAN_POINT('Ctrl Pts',(-4.22003200860839,-4.15018050172547,
37.5298031740354));
#20141=CARTESIAN_POINT('Ctrl Pts',(-4.32888782019247,-4.03650646423048,
37.5223988503397));
#20142=CARTESIAN_POINT('Ctrl Pts',(-4.43302715905347,-3.91869886181553,
37.5149945266439));
#20143=CARTESIAN_POINT('Ctrl Pts',(-4.54256246416287,-3.79478707386043,
37.5072065488824));
#20144=CARTESIAN_POINT('Ctrl Pts',(-4.64691873605409,-3.66625766229791,
37.4994185711209));
#20145=CARTESIAN_POINT('Ctrl Pts',(-4.74571826592819,-3.53356600376101,
37.4916305933594));
#20146=CARTESIAN_POINT('Ctrl Pts',(-4.84449837096764,-3.40090043354185,
37.4838441467811));
#20147=CARTESIAN_POINT('Ctrl Pts',(-4.93772372313274,-3.26407450531249,
37.4760577002028));
#20148=CARTESIAN_POINT('Ctrl Pts',(-5.02505812334871,-3.12357510226137,
37.4682712536245));
#20149=CARTESIAN_POINT('Ctrl Pts',(-5.11239585517522,-2.98307033947468,
37.4604845100108));
#20150=CARTESIAN_POINT('Ctrl Pts',(-5.19384201332127,-2.8388920907489,37.4526977663971));
#20151=CARTESIAN_POINT('Ctrl Pts',(-5.2691044178346,-2.69155516318278,37.4449110227835));
#20152=CARTESIAN_POINT('Ctrl Pts',(-5.34436184430279,-2.54422798085243,
37.4371247942046));
#20153=CARTESIAN_POINT('Ctrl Pts',(-5.4134361903507,-2.39374282241546,37.4293385656258));
#20154=CARTESIAN_POINT('Ctrl Pts',(-5.47608176304281,-2.2406380981698,37.421552337047));
#20155=CARTESIAN_POINT('Ctrl Pts',(-5.53874382695698,-2.08749306965524,
37.4137640587714));
#20156=CARTESIAN_POINT('Ctrl Pts',(-5.59497361293785,-1.93172739259032,
37.4059757804958));
#20157=CARTESIAN_POINT('Ctrl Pts',(-5.64457367603185,-1.77389925822983,
37.3981875022203));
#20158=CARTESIAN_POINT('Ctrl Pts',(-5.69172850403234,-1.62385189810238,
37.390783178524));
#20159=CARTESIAN_POINT('Ctrl Pts',(-5.73289146179677,-1.47194078781932,
37.3833788548277));
#20160=CARTESIAN_POINT('Ctrl Pts',(-5.76793477125694,-1.31865804400732,
37.3759745311315));
#20161=CARTESIAN_POINT('Ctrl Pts',(-5.80546095191119,-1.15451498719907,
37.3680455999623));
#20162=CARTESIAN_POINT('Ctrl Pts',(-5.83598056412886,-0.988749824618148,
37.3601166687931));
#20163=CARTESIAN_POINT('Ctrl Pts',(-5.8593775349695,-0.821964394116137,
37.352187737624));
#20164=CARTESIAN_POINT('Ctrl Pts',(-5.88276867425801,-0.655220533864368,
37.3442607826925));
#20165=CARTESIAN_POINT('Ctrl Pts',(-5.89904067508326,-0.487457204634034,
37.3363338277611));
#20166=CARTESIAN_POINT('Ctrl Pts',(-5.90812900489858,-0.319283923767114,
37.3284068728296));
#20167=CARTESIAN_POINT('Ctrl Pts',(-5.91387366019098,-0.212983035968757,
37.3233963126359));
#20168=CARTESIAN_POINT('Ctrl Pts',(-5.91674918763453,-0.106518504630412,
37.3183857524422));
#20169=CARTESIAN_POINT('Ctrl Pts',(-5.91674999982786,-4.51337719426076E-5,
37.3133751922485));
#20170=CARTESIAN_POINT('Ctrl Pts',(-5.91674999805201,-0.000151827279522968,
37.0616248082411));
#20171=CARTESIAN_POINT('Ctrl Pts',(-5.91674555035387,-0.17347982250265,
37.0697835109022));
#20172=CARTESIAN_POINT('Ctrl Pts',(-5.9091204396543,-0.346769807533754,
37.0779422135633));
#20173=CARTESIAN_POINT('Ctrl Pts',(-5.89391063127059,-0.519372730411945,
37.0861009162245));
#20174=CARTESIAN_POINT('Ctrl Pts',(-5.88609077923648,-0.608113448474336,
37.0902955678592));
#20175=CARTESIAN_POINT('Ctrl Pts',(-5.87626689374088,-0.696672605295589,
37.0944902194939));
#20176=CARTESIAN_POINT('Ctrl Pts',(-5.86444920173335,-0.784962497695989,
37.0986848711286));
#20177=CARTESIAN_POINT('Ctrl Pts',(-5.84250756991799,-0.948888271936102,
37.1064729825216));
#20178=CARTESIAN_POINT('Ctrl Pts',(-5.81368452304766,-1.11192275153252,
37.1142610939145));
#20179=CARTESIAN_POINT('Ctrl Pts',(-5.77807696957521,-1.27348227163338,
37.1220492053075));
#20180=CARTESIAN_POINT('Ctrl Pts',(-5.7424764070251,-1.43501007233914,37.1298357876406));
#20181=CARTESIAN_POINT('Ctrl Pts',(-5.70009406437873,-1.59506317950582,
37.1376223699736));
#20182=CARTESIAN_POINT('Ctrl Pts',(-5.65107784236079,-1.75306867580222,
37.1454089523067));
#20183=CARTESIAN_POINT('Ctrl Pts',(-5.60205975136534,-1.91108019681262,
37.1531958315404));
#20184=CARTESIAN_POINT('Ctrl Pts',(-5.54640736574657,-2.0670436443859,37.1609827107741));
#20185=CARTESIAN_POINT('Ctrl Pts',(-5.48431851339339,-2.22040109127846,
37.1687695900078));
#20186=CARTESIAN_POINT('Ctrl Pts',(-5.42223375886856,-2.37374841666818,
37.176555955312));
#20187=CARTESIAN_POINT('Ctrl Pts',(-5.35371350773485,-2.52448978941045,
37.1843423206161));
#20188=CARTESIAN_POINT('Ctrl Pts',(-5.27900386516668,-2.67208696603522,
37.1921286859203));
#20189=CARTESIAN_POINT('Ctrl Pts',(-5.20427460536344,-2.8197228986814,37.1999170957659));
#20190=CARTESIAN_POINT('Ctrl Pts',(-5.12335284928681,-2.9642126993332,37.2077055056115));
#20191=CARTESIAN_POINT('Ctrl Pts',(-5.03653124272813,-3.1050416428002,37.215493915457));
#20192=CARTESIAN_POINT('Ctrl Pts',(-4.95427228166071,-3.23846974943158,
37.2228730291093));
#20193=CARTESIAN_POINT('Ctrl Pts',(-4.86671775478904,-3.36861165143155,
37.2302521427615));
#20194=CARTESIAN_POINT('Ctrl Pts',(-4.77415296928689,-3.49505278763414,
37.2376312564137));
#20195=CARTESIAN_POINT('Ctrl Pts',(-4.67645765050916,-3.62850210144088,
37.2454193678066));
#20196=CARTESIAN_POINT('Ctrl Pts',(-4.57314603088103,-3.75787643744925,
37.2532074791995));
#20197=CARTESIAN_POINT('Ctrl Pts',(-4.46458245377437,-3.882709630651,37.2609955905924));
#20198=CARTESIAN_POINT('Ctrl Pts',(-4.35604019123365,-4.0075183150313,37.2687821729254));
#20199=CARTESIAN_POINT('Ctrl Pts',(-4.24224823817848,-4.12778739460402,
37.2765687552584));
#20200=CARTESIAN_POINT('Ctrl Pts',(-4.12361057346573,-4.24308453850517,
37.2843553375914));
#20201=CARTESIAN_POINT('Ctrl Pts',(-4.00496838512514,-4.35838607866085,
37.2921422168251));
#20202=CARTESIAN_POINT('Ctrl Pts',(-3.88148034179317,-4.46871507828333,
37.2999290960587));
#20203=CARTESIAN_POINT('Ctrl Pts',(-3.75358709272272,-4.5736762565627,37.3077159752924));
#20204=CARTESIAN_POINT('Ctrl Pts',(-3.62570228453273,-4.67863050746502,
37.3155023405965));
#20205=CARTESIAN_POINT('Ctrl Pts',(-3.49341309951283,-4.77821744334559,
37.3232887059007));
#20206=CARTESIAN_POINT('Ctrl Pts',(-3.35719316289092,-4.87208216572119,
37.3310750712048));
#20207=CARTESIAN_POINT('Ctrl Pts',(-3.22093745767984,-4.96597153506679,
37.3388634810503));
#20208=CARTESIAN_POINT('Ctrl Pts',(-3.08074920062857,-5.05413550550532,
37.3466518908959));
#20209=CARTESIAN_POINT('Ctrl Pts',(-2.93713163336884,-5.13626209716405,
37.3544403007414));
#20210=CARTESIAN_POINT('Ctrl Pts',(-2.80106145058167,-5.21407277556443,
37.3618194143939));
#20211=CARTESIAN_POINT('Ctrl Pts',(-2.66191334676182,-5.28646417724288,
37.3691985280464));
#20212=CARTESIAN_POINT('Ctrl Pts',(-2.52013619733201,-5.35320876758949,
37.3765776416989));
#20213=CARTESIAN_POINT('Ctrl Pts',(-2.37050085022191,-5.42365277062102,
37.384365753092));
#20214=CARTESIAN_POINT('Ctrl Pts',(-2.21788331421212,-5.48783140625146,
37.3921538644851));
#20215=CARTESIAN_POINT('Ctrl Pts',(-2.06282655731286,-5.54550963906337,
37.3999419758781));
#20216=CARTESIAN_POINT('Ctrl Pts',(-1.90780024310472,-5.60317654775977,
37.4077285582113));
#20217=CARTESIAN_POINT('Ctrl Pts',(-1.75033596284705,-5.65434548878523,
37.4155151405445));
#20218=CARTESIAN_POINT('Ctrl Pts',(-1.59099530192642,-5.69883010027041,
37.4233017228777));
#20219=CARTESIAN_POINT('Ctrl Pts',(-1.43164856538189,-5.74331640794392,
37.4310886021115));
#20220=CARTESIAN_POINT('Ctrl Pts',(-1.27042561169685,-5.78111778635841,
37.4388754813454));
#20221=CARTESIAN_POINT('Ctrl Pts',(-1.10790250131735,-5.81209795255334,
37.4466623605792));
#20222=CARTESIAN_POINT('Ctrl Pts',(-0.945390117368948,-5.84307607407526,
37.4544487258835));
#20223=CARTESIAN_POINT('Ctrl Pts',(-0.781578062367603,-5.86723382456904,
37.4622350911878));
#20224=CARTESIAN_POINT('Ctrl Pts',(-0.617052033386599,-5.88448615858628,
37.4700214564921));
#20225=CARTESIAN_POINT('Ctrl Pts',(-0.452482803211596,-5.90174302271607,
37.4778098663378));
#20226=CARTESIAN_POINT('Ctrl Pts',(-0.287199542235393,-5.91209081189761,
37.4855982761836));
#20227=CARTESIAN_POINT('Ctrl Pts',(-0.121793420594745,-5.91549633802607,
37.4933866860293));
#20228=CARTESIAN_POINT('Ctrl Pts',(0.0349202853391011,-5.91872289708538,
37.5007657996809));
#20229=CARTESIAN_POINT('Ctrl Pts',(0.191744010902166,-5.91571807959255,
37.5081449133325));
#20230=CARTESIAN_POINT('Ctrl Pts',(0.348174727758624,-5.90649684004404,
37.515524026984));
#20231=CARTESIAN_POINT('Ctrl Pts',(0.513275836872115,-5.89676450033829,
37.523312138377));
#20232=CARTESIAN_POINT('Ctrl Pts',(0.677998101426518,-5.88010361416883,
37.5311002497699));
#20233=CARTESIAN_POINT('Ctrl Pts',(0.841752279586095,-5.85656756661371,
37.5388883611628));
#20234=CARTESIAN_POINT('Ctrl Pts',(1.00547430746745,-5.83303613995124,37.5466749434958));
#20235=CARTESIAN_POINT('Ctrl Pts',(1.16822831211086,-5.80263229062148,37.5544615258288));
#20236=CARTESIAN_POINT('Ctrl Pts',(1.32943199047928,-5.76546105226549,37.5622481081618));
#20237=CARTESIAN_POINT('Ctrl Pts',(1.49064181550798,-5.72828839657848,37.5700349873955));
#20238=CARTESIAN_POINT('Ctrl Pts',(1.65030088374228,-5.68434790347346,37.5778218666292));
#20239=CARTESIAN_POINT('Ctrl Pts',(1.80783814078094,-5.63379550740331,37.5856087458628));
#20240=CARTESIAN_POINT('Ctrl Pts',(1.96536500045176,-5.58324644776206,37.593395111167));
#20241=CARTESIAN_POINT('Ctrl Pts',(2.12077002492968,-5.5260864561731,37.6011814764711));
#20242=CARTESIAN_POINT('Ctrl Pts',(2.2734982115037,-5.46252107042064,37.6089678417752));
#20243=CARTESIAN_POINT('Ctrl Pts',(2.42626650139811,-5.39893899368868,37.6167562516208));
#20244=CARTESIAN_POINT('Ctrl Pts',(2.57635625294304,-5.32894828302026,37.6245446614664));
#20245=CARTESIAN_POINT('Ctrl Pts',(2.72323246778739,-5.25280263182319,37.6323330713119));
#20246=CARTESIAN_POINT('Ctrl Pts',(2.86239004984366,-5.18065858374901,37.6397121849643));
#20247=CARTESIAN_POINT('Ctrl Pts',(2.99866293236299,-5.10298998441233,37.6470912986167));
#20248=CARTESIAN_POINT('Ctrl Pts',(3.13161654943962,-5.02005063219246,37.6544704122691));
#20249=CARTESIAN_POINT('Ctrl Pts',(3.27193930751913,-4.93251424986062,37.662258523662));
#20250=CARTESIAN_POINT('Ctrl Pts',(3.40861453258895,-4.83907500532104,37.670046635055));
#20251=CARTESIAN_POINT('Ctrl Pts',(3.54115033924669,-4.74006169130245,37.6778347464479));
#20252=CARTESIAN_POINT('Ctrl Pts',(3.67366012480919,-4.64106781682205,37.6856213287809));
#20253=CARTESIAN_POINT('Ctrl Pts',(3.80203185771857,-4.53650224757727,37.693407911114));
#20254=CARTESIAN_POINT('Ctrl Pts',(3.9258044561838,-4.42673581031299,37.701194493447));
#20255=CARTESIAN_POINT('Ctrl Pts',(4.04958177407063,-4.31696518767893,37.7089813726807));
#20256=CARTESIAN_POINT('Ctrl Pts',(4.16875936493796,-4.20199350925795,37.7167682519144));
#20257=CARTESIAN_POINT('Ctrl Pts',(4.28291037742195,-4.08223091721565,37.724555131148));
#20258=CARTESIAN_POINT('Ctrl Pts',(4.39705385600517,-3.96247622943515,37.7323414964522));
#20259=CARTESIAN_POINT('Ctrl Pts',(4.50617119970149,-3.83793149218703,37.7401278617563));
#20260=CARTESIAN_POINT('Ctrl Pts',(4.60987338448563,-3.70904272575971,37.7479142270605));
#20261=CARTESIAN_POINT('Ctrl Pts',(4.7136027993576,-3.58012011575968,37.7557026369061));
#20262=CARTESIAN_POINT('Ctrl Pts',(4.81191401209567,-3.44685144521499,37.7634910467516));
#20263=CARTESIAN_POINT('Ctrl Pts',(4.90445860430809,-3.30971545017519,37.7712794565972));
#20264=CARTESIAN_POINT('Ctrl Pts',(4.99213979692452,-3.17978622029505,37.7786585702496));
#20265=CARTESIAN_POINT('Ctrl Pts',(5.07464472888979,-3.04638589782895,37.7860376839019));
#20266=CARTESIAN_POINT('Ctrl Pts',(5.15171322405697,-2.90994526058079,37.7934167975542));
#20267=CARTESIAN_POINT('Ctrl Pts',(5.23305334883766,-2.76594220933593,37.8012049089472));
#20268=CARTESIAN_POINT('Ctrl Pts',(5.30836635418492,-2.6185008284622,37.8089930203402));
#20269=CARTESIAN_POINT('Ctrl Pts',(5.37737761033478,-2.4681451736821,37.8167811317332));
#20270=CARTESIAN_POINT('Ctrl Pts',(5.44637531732751,-2.31781903861378,37.8245677140663));
#20271=CARTESIAN_POINT('Ctrl Pts',(5.50907361057417,-2.16458006150297,37.8323542963994));
#20272=CARTESIAN_POINT('Ctrl Pts',(5.56524502022065,-2.00897447156734,37.8401408787325));
#20273=CARTESIAN_POINT('Ctrl Pts',(5.62141857167049,-1.85336294842517,37.8479277579662));
#20274=CARTESIAN_POINT('Ctrl Pts',(5.67106462933165,-1.69538493108427,37.8557146371999));
#20275=CARTESIAN_POINT('Ctrl Pts',(5.71400459175321,-1.53560479548718,37.8635015164337));
#20276=CARTESIAN_POINT('Ctrl Pts',(5.7569417201621,-1.37583520528655,37.8712878817379));
#20277=CARTESIAN_POINT('Ctrl Pts',(5.79317355621734,-1.21426404347849,37.8790742470421));
#20278=CARTESIAN_POINT('Ctrl Pts',(5.82257188087655,-1.05146909347147,37.8868606123463));
#20279=CARTESIAN_POINT('Ctrl Pts',(5.85197792493881,-0.888631396816528,
37.894649022192));
#20280=CARTESIAN_POINT('Ctrl Pts',(5.87454681340574,-0.724569584158841,
37.9024374320376));
#20281=CARTESIAN_POINT('Ctrl Pts',(5.89020163634249,-0.559870740196556,
37.9102258418832));
#20282=CARTESIAN_POINT('Ctrl Pts',(5.90503376766878,-0.403827143101491,
37.9176049555353));
#20283=CARTESIAN_POINT('Ctrl Pts',(5.91365981326503,-0.247212006003625,
37.9249840691874));
#20284=CARTESIAN_POINT('Ctrl Pts',(5.91605740580995,-0.0905280821691331,
37.9323631828394));
#20285=CARTESIAN_POINT('Ctrl Pts',(5.91858788828999,0.0748402682650383,
37.9401512942324));
#20286=CARTESIAN_POINT('Ctrl Pts',(5.91418080147477,0.240344307955706,37.9479394056253));
#20287=CARTESIAN_POINT('Ctrl Pts',(5.90284571343753,0.405392459047019,37.9557275170183));
#20288=CARTESIAN_POINT('Ctrl Pts',(5.89151285084722,0.570408205811078,37.9635140993513));
#20289=CARTESIAN_POINT('Ctrl Pts',(5.87325472290218,0.734967923985702,37.9713006816844));
#20290=CARTESIAN_POINT('Ctrl Pts',(5.84813291845099,0.898483127626742,37.9790872640174));
#20291=CARTESIAN_POINT('Ctrl Pts',(5.82301015611099,1.06200456606606,37.9868741432511));
#20292=CARTESIAN_POINT('Ctrl Pts',(5.79102323819929,1.22448109386781,37.9946610224848));
#20293=CARTESIAN_POINT('Ctrl Pts',(5.7522853480579,1.38533167040185,38.0024479017185));
#20294=CARTESIAN_POINT('Ctrl Pts',(5.71355001459484,1.54617163089094,38.0102342670227));
#20295=CARTESIAN_POINT('Ctrl Pts',(5.6680646754706,1.7053855442165,38.0180206323268));
#20296=CARTESIAN_POINT('Ctrl Pts',(5.61599317057472,1.86240470106745,38.025806997631));
#20297=CARTESIAN_POINT('Ctrl Pts',(5.56390799275907,2.01946508796038,38.0335954074766));
#20298=CARTESIAN_POINT('Ctrl Pts',(5.50523329228426,2.17432926271722,38.0413838173222));
#20299=CARTESIAN_POINT('Ctrl Pts',(5.44018241480332,2.32644489643848,38.0491722271678));
#20300=CARTESIAN_POINT('Ctrl Pts',(5.37855008835583,2.4705665556432,38.05655134082));
#20301=CARTESIAN_POINT('Ctrl Pts',(5.31119461147333,2.61222088690754,38.0639304544722));
#20302=CARTESIAN_POINT('Ctrl Pts',(5.23833687779192,2.75095570979708,38.0713095681245));
#20303=CARTESIAN_POINT('Ctrl Pts',(5.16144090186704,2.89738010514689,38.0790976795175));
#20304=CARTESIAN_POINT('Ctrl Pts',(5.07838796945833,3.04060447453471,38.0868857909104));
#20305=CARTESIAN_POINT('Ctrl Pts',(4.98946951421679,3.18011391764529,38.0946739023034));
#20306=CARTESIAN_POINT('Ctrl Pts',(4.9005685165638,3.31959597050883,38.1024604846365));
#20307=CARTESIAN_POINT('Ctrl Pts',(4.80580446548167,3.45536428310203,38.1102470669695));
#20308=CARTESIAN_POINT('Ctrl Pts',(4.70551299597211,3.58693155876128,38.1180336493026));
#20309=CARTESIAN_POINT('Ctrl Pts',(4.60521770237119,3.71850385105139,38.1258205285363));
#20310=CARTESIAN_POINT('Ctrl Pts',(4.49939475917456,3.84587452937775,38.13360740777));
#20311=CARTESIAN_POINT('Ctrl Pts',(4.38842154558554,3.96858751960199,38.1413942870037));
#20312=CARTESIAN_POINT('Ctrl Pts',(4.27745565616441,4.09129241083986,38.1491806523079));
#20313=CARTESIAN_POINT('Ctrl Pts',(4.16134039099671,4.20933999220777,38.1569670176121));
#20314=CARTESIAN_POINT('Ctrl Pts',(4.04049171221856,4.32230925385876,38.1647533829163));
#20315=CARTESIAN_POINT('Ctrl Pts',(3.91961130103145,4.43530817894379,38.1725417927619));
#20316=CARTESIAN_POINT('Ctrl Pts',(3.79399522491412,4.54322590000898,38.1803302026075));
#20317=CARTESIAN_POINT('Ctrl Pts',(3.66409508117712,4.64567947652371,38.1881186124531));
#20318=CARTESIAN_POINT('Ctrl Pts',(3.54102144444373,4.74274891690509,38.1954977261053));
#20319=CARTESIAN_POINT('Ctrl Pts',(3.4141026353678,4.83491358331393,38.2028768397574));
#20320=CARTESIAN_POINT('Ctrl Pts',(3.28374896475881,4.92188208909411,38.2102559534096));
#20321=CARTESIAN_POINT('Ctrl Pts',(3.14617025882768,5.01367094648573,38.2180440648026));
#20322=CARTESIAN_POINT('Ctrl Pts',(3.00471599413142,5.09970408293563,38.2258321761955));
#20323=CARTESIAN_POINT('Ctrl Pts',(2.85988843167947,5.17966878485931,38.2336202875885));
#20324=CARTESIAN_POINT('Ctrl Pts',(2.7150893035948,5.2596177871077,38.2414068699215));
#20325=CARTESIAN_POINT('Ctrl Pts',(2.5669184787667,5.33350057773942,38.2491934522546));
#20326=CARTESIAN_POINT('Ctrl Pts',(2.41590382585929,5.40104983005142,38.2569800345876));
#20327=CARTESIAN_POINT('Ctrl Pts',(2.26488341479661,5.46860165800145,38.2647669138213));
#20328=CARTESIAN_POINT('Ctrl Pts',(2.11101924873187,5.52981933032966,38.272553793055));
#20329=CARTESIAN_POINT('Ctrl Pts',(1.95486091490845,5.58448290944321,38.2803406722888));
#20330=CARTESIAN_POINT('Ctrl Pts',(1.79871288744472,5.63914288079217,38.2881270375929));
#20331=CARTESIAN_POINT('Ctrl Pts',(1.6402712968716,5.68724951909089,38.2959134028971));
#20332=CARTESIAN_POINT('Ctrl Pts',(1.48010283499295,5.72863213693686,38.3036997682013));
#20333=CARTESIAN_POINT('Ctrl Pts',(1.31989231612876,5.77002562101793,38.3114881780469));
#20334=CARTESIAN_POINT('Ctrl Pts',(1.15795432897601,5.80469147476326,38.3192765878925));
#20335=CARTESIAN_POINT('Ctrl Pts',(0.994868643695197,5.83250948943009,38.3270649977381));
#20336=CARTESIAN_POINT('Ctrl Pts',(0.840353430629375,5.85886561293605,38.3344441113903));
#20337=CARTESIAN_POINT('Ctrl Pts',(0.684808300786823,5.87907507641403,38.3418232250425));
#20338=CARTESIAN_POINT('Ctrl Pts',(0.528732967106978,5.89307831375031,38.3492023386947));
#20339=CARTESIAN_POINT('Ctrl Pts',(0.364006938796237,5.90785770018834,38.3569904500876));
#20340=CARTESIAN_POINT('Ctrl Pts',(0.198631433735107,5.91572865270471,38.3647785614805));
#20341=CARTESIAN_POINT('Ctrl Pts',(0.0331971119871187,5.9166568697412,38.3725666728734));
#20342=CARTESIAN_POINT('Ctrl Pts',(-0.132204729615795,5.91758490453846,
38.3803532552064));
#20343=CARTESIAN_POINT('Ctrl Pts',(-0.297665045538489,5.91157292182418,
38.3881398375394));
#20344=CARTESIAN_POINT('Ctrl Pts',(-0.462592403735932,5.89863872690181,
38.3959264198724));
#20345=CARTESIAN_POINT('Ctrl Pts',(-0.627526050576847,5.88570403880147,
38.4037132991061));
#20346=CARTESIAN_POINT('Ctrl Pts',(-0.791926380182615,5.86584663138872,
38.4115001783397));
#20347=CARTESIAN_POINT('Ctrl Pts',(-0.955205561549463,5.83913631436063,
38.4192870575734));
#20348=CARTESIAN_POINT('Ctrl Pts',(-1.11847396658491,5.81242776019798,38.4270734228775));
#20349=CARTESIAN_POINT('Ctrl Pts',(-1.28062105611454,5.77886725322325,38.4348597881816));
#20350=CARTESIAN_POINT('Ctrl Pts',(-1.44106754225738,5.73857603427473,38.4426461534858));
#20351=CARTESIAN_POINT('Ctrl Pts',(-1.60155615838923,5.69827423567032,38.4504345633313));
#20352=CARTESIAN_POINT('Ctrl Pts',(-1.7603429682634,5.65123826955373,38.4582229731768));
#20353=CARTESIAN_POINT('Ctrl Pts',(-1.91686135036628,5.59763996037366,38.4660113830224));
#20354=CARTESIAN_POINT('Ctrl Pts',(-2.06515438490714,5.54685834732741,38.4733904966749));
#20355=CARTESIAN_POINT('Ctrl Pts',(-2.21141103396735,5.49018646329872,38.4807696103274));
#20356=CARTESIAN_POINT('Ctrl Pts',(-2.35516398967869,5.42781108221544,38.4881487239799));
#20357=CARTESIAN_POINT('Ctrl Pts',(-2.50688465490904,5.36197845800871,38.495936835373));
#20358=CARTESIAN_POINT('Ctrl Pts',(-2.65587040209376,5.28976864769933,38.5037249467661));
#20359=CARTESIAN_POINT('Ctrl Pts',(-2.80158614807328,5.21143412290935,38.5115130581591));
#20360=CARTESIAN_POINT('Ctrl Pts',(-2.94727328530633,5.13311497773771,38.5192996404923));
#20361=CARTESIAN_POINT('Ctrl Pts',(-3.08969142106573,5.04867366859599,38.5270862228255));
#20362=CARTESIAN_POINT('Ctrl Pts',(-3.22832972405745,4.95840879267403,38.5348728051587));
#20363=CARTESIAN_POINT('Ctrl Pts',(-3.36697331329682,4.86814047497244,38.5426596843925));
#20364=CARTESIAN_POINT('Ctrl Pts',(-3.50183651145808,4.77204831719295,38.5504465636264));
#20365=CARTESIAN_POINT('Ctrl Pts',(-3.63243653013948,4.67047485990539,38.5582334428602));
#20366=CARTESIAN_POINT('Ctrl Pts',(-3.76302792929524,4.56890810640722,38.5660198081645));
#20367=CARTESIAN_POINT('Ctrl Pts',(-3.8893564598587,4.46186097361815,38.5738061734689));
#20368=CARTESIAN_POINT('Ctrl Pts',(-4.01097144181087,4.34971707763592,38.5815925387732));
#20369=CARTESIAN_POINT('Ctrl Pts',(-4.13261835738758,4.237543734944,38.5893809486189));
#20370=CARTESIAN_POINT('Ctrl Pts',(-4.2495490148332,4.12027117016764,38.5971693584646));
#20371=CARTESIAN_POINT('Ctrl Pts',(-4.36134805773805,3.99832135799069,38.6049577683103));
#20372=CARTESIAN_POINT('Ctrl Pts',(-4.46727184193451,3.88278024733178,38.6123368819619));
#20373=CARTESIAN_POINT('Ctrl Pts',(-4.56858931620707,3.76304103389447,38.6197159956135));
#20374=CARTESIAN_POINT('Ctrl Pts',(-4.6649794860832,3.63949130469121,38.627095109265));
#20375=CARTESIAN_POINT('Ctrl Pts',(-4.76671221654703,3.50909365816702,38.634883220658));
#20376=CARTESIAN_POINT('Ctrl Pts',(-4.86299228233177,3.37440454019386,38.6426713320509));
#20377=CARTESIAN_POINT('Ctrl Pts',(-4.95347060602803,3.23590165451862,38.6504594434438));
#20378=CARTESIAN_POINT('Ctrl Pts',(-5.04393116588276,3.09742596147043,38.6582460257768));
#20379=CARTESIAN_POINT('Ctrl Pts',(-5.12859208179027,2.95513826207483,38.6660326081098));
#20380=CARTESIAN_POINT('Ctrl Pts',(-5.20714764055606,2.80954516104502,38.6738191904429));
#20381=CARTESIAN_POINT('Ctrl Pts',(-5.28570619462777,2.66394650858276,38.6816060696765));
#20382=CARTESIAN_POINT('Ctrl Pts',(-5.35815877053739,2.51504248161278,38.6893929489102));
#20383=CARTESIAN_POINT('Ctrl Pts',(-5.42424530425686,2.36336485582473,38.6971798281439));
#20384=CARTESIAN_POINT('Ctrl Pts',(-5.49032747630335,2.21169724067218,38.704966193448));
#20385=CARTESIAN_POINT('Ctrl Pts',(-5.55004431942148,2.05725668602571,38.7127525587522));
#20386=CARTESIAN_POINT('Ctrl Pts',(-5.60318361666804,1.90059567515106,38.7205389240563));
#20387=CARTESIAN_POINT('Ctrl Pts',(-5.65633686721495,1.74389352827628,38.7283273339019));
#20388=CARTESIAN_POINT('Ctrl Pts',(-5.70290901617878,1.58497006229457,38.7361157437475));
#20389=CARTESIAN_POINT('Ctrl Pts',(-5.74273721718423,1.42439454396143,38.743904153593));
#20390=CARTESIAN_POINT('Ctrl Pts',(-5.78047236821199,1.27225758364953,38.7512832672454));
#20391=CARTESIAN_POINT('Ctrl Pts',(-5.8121540929384,1.11863799456283,38.7586623808978));
#20392=CARTESIAN_POINT('Ctrl Pts',(-5.83768595408446,0.964029700779509,
38.7660414945501));
#20393=CARTESIAN_POINT('Ctrl Pts',(-5.86560263673436,0.79498011023452,38.7741098595194));
#20394=CARTESIAN_POINT('Ctrl Pts',(-5.88617396736588,0.624704945254722,
38.7821782244886));
#20395=CARTESIAN_POINT('Ctrl Pts',(-5.89931905236653,0.453833979430056,
38.7902465894579));
#20396=CARTESIAN_POINT('Ctrl Pts',(-5.9109289426702,0.302918776583512,38.7973726622233));
#20397=CARTESIAN_POINT('Ctrl Pts',(-5.9167466179235,0.151539059100074,38.8044987349888));
#20398=CARTESIAN_POINT('Ctrl Pts',(-5.91674999852514,0.000132108695950693,
38.8116248077543));
#20399=CARTESIAN_POINT('Origin',(0.,0.,0.));
#20400=CARTESIAN_POINT('',(-5.91674999807463,-0.000150943316464095,40.8133751922049));
#20401=CARTESIAN_POINT('',(-5.91674999950574,-7.64775397920275E-5,40.5616248077532));
#20402=CARTESIAN_POINT('',(-5.91675,-7.2459289488551E-16,0.));
#20403=CARTESIAN_POINT('Ctrl Pts',(-5.91674999807463,-0.000150943316464095,
40.8133751922049));
#20404=CARTESIAN_POINT('Ctrl Pts',(-5.91675420785041,0.16486590810397,40.8056078136878));
#20405=CARTESIAN_POINT('Ctrl Pts',(-5.90985064980782,0.329899361430627,
40.7978404351708));
#20406=CARTESIAN_POINT('Ctrl Pts',(-5.89606122030937,0.494360848838174,
40.7900730566537));
#20407=CARTESIAN_POINT('Ctrl Pts',(-5.88227108254778,0.658830783441378,
40.7823052791827));
#20408=CARTESIAN_POINT('Ctrl Pts',(-5.86159439040863,0.822728371697022,
40.7745375017117));
#20409=CARTESIAN_POINT('Ctrl Pts',(-5.83410500661337,0.985469093533016,
40.7667697242406));
#20410=CARTESIAN_POINT('Ctrl Pts',(-5.80661608301405,1.14820709094933,40.7590020768088));
#20411=CARTESIAN_POINT('Ctrl Pts',(-5.77231475214443,1.30978794303029,40.7512344293771));
#20412=CARTESIAN_POINT('Ctrl Pts',(-5.73132622610735,1.46963609524063,40.7434667819453));
#20413=CARTESIAN_POINT('Ctrl Pts',(-5.69032839687805,1.62952052828923,40.7356973714856));
#20414=CARTESIAN_POINT('Ctrl Pts',(-5.64264042152028,1.78767116355322,40.7279279610259));
#20415=CARTESIAN_POINT('Ctrl Pts',(-5.58843791706703,1.94352571621461,40.7201585505662));
#20416=CARTESIAN_POINT('Ctrl Pts',(-5.57052222974968,1.99504070543204,40.717590508188));
#20417=CARTESIAN_POINT('Ctrl Pts',(-5.55189522117018,2.04630497463979,40.7150224658099));
#20418=CARTESIAN_POINT('Ctrl Pts',(-5.53256441396586,2.09729863582148,40.7124544234318));
#20419=CARTESIAN_POINT('Ctrl Pts',(-5.47394081106185,2.25194464269218,40.7046664456704));
#20420=CARTESIAN_POINT('Ctrl Pts',(-5.40881867575399,2.4041587964738,40.6968784679091));
#20421=CARTESIAN_POINT('Ctrl Pts',(-5.33742501837016,2.55339474734643,40.6890904901478));
#20422=CARTESIAN_POINT('Ctrl Pts',(-5.26604539759129,2.702601357152,40.6813040435696));
#20423=CARTESIAN_POINT('Ctrl Pts',(-5.18839685282266,2.84883064428859,40.6735175969914));
#20424=CARTESIAN_POINT('Ctrl Pts',(-5.10475360990861,2.99155831375974,40.6657311504133));
#20425=CARTESIAN_POINT('Ctrl Pts',(-5.02110717619358,3.13429142796942,40.6579444067998));
#20426=CARTESIAN_POINT('Ctrl Pts',(-4.93146574488197,3.27352237953437,40.6501576631862));
#20427=CARTESIAN_POINT('Ctrl Pts',(-4.83614875604487,3.4087528176601,40.6423709195727));
#20428=CARTESIAN_POINT('Ctrl Pts',(-4.74083807171344,3.5439743113041,40.634584690994));
#20429=CARTESIAN_POINT('Ctrl Pts',(-4.63985276528638,3.67519555987536,40.6267984624153));
#20430=CARTESIAN_POINT('Ctrl Pts',(-4.53355481733812,3.80194835323815,40.6190122338366));
#20431=CARTESIAN_POINT('Ctrl Pts',(-4.42722888683693,3.92873451381845,40.6112239555612));
#20432=CARTESIAN_POINT('Ctrl Pts',(-4.31558772422202,4.05104962241858,40.6034356772858));
#20433=CARTESIAN_POINT('Ctrl Pts',(-4.19903328863283,4.16845894827493,40.5956473990104));
#20434=CARTESIAN_POINT('Ctrl Pts',(-4.08822487387036,4.2800801080421,40.5882430753134));
#20435=CARTESIAN_POINT('Ctrl Pts',(-3.97297614149774,4.38726734707188,40.5808387516164));
#20436=CARTESIAN_POINT('Ctrl Pts',(-3.85366303459733,4.4896783602256,40.5734344279194));
#20437=CARTESIAN_POINT('Ctrl Pts',(-3.72816773465678,4.59739578664105,40.5656464501577));
#20438=CARTESIAN_POINT('Ctrl Pts',(-3.59813079559704,4.69986741979239,40.557858472396));
#20439=CARTESIAN_POINT('Ctrl Pts',(-3.46401305146472,4.79672222895824,40.5500704946344));
#20440=CARTESIAN_POINT('Ctrl Pts',(-3.32992167603034,4.89355799563852,40.5422840480559));
#20441=CARTESIAN_POINT('Ctrl Pts',(-3.19175135529146,4.98477895479982,40.5344976014774));
#20442=CARTESIAN_POINT('Ctrl Pts',(-3.04999382142249,5.07005604030021,40.5267111548989));
#20443=CARTESIAN_POINT('Ctrl Pts',(-2.90823087982341,5.15533637892902,40.5189244112851));
#20444=CARTESIAN_POINT('Ctrl Pts',(-2.76288072304099,5.23467222206963,40.5111376676712));
#20445=CARTESIAN_POINT('Ctrl Pts',(-2.61446236253391,5.30777892506778,40.5033509240574));
#20446=CARTESIAN_POINT('Ctrl Pts',(-2.46605381879135,5.38088079260429,40.4955646954784));
#20447=CARTESIAN_POINT('Ctrl Pts',(-2.31457776416987,5.44775420338287,40.4877784668994));
#20448=CARTESIAN_POINT('Ctrl Pts',(-2.16057613318633,5.50816133888665,40.4799922383204));
#20449=CARTESIAN_POINT('Ctrl Pts',(-2.00653396182636,5.56858437635197,40.4722039600447));
#20450=CARTESIAN_POINT('Ctrl Pts',(-1.84996518256331,5.62253761855439,40.464415681769));
#20451=CARTESIAN_POINT('Ctrl Pts',(-1.69143080546665,5.66983177817636,40.4566274034933));
#20452=CARTESIAN_POINT('Ctrl Pts',(-1.54071201970464,5.71479438150819,40.4492230797978));
#20453=CARTESIAN_POINT('Ctrl Pts',(-1.38821702426881,5.75373858366138,40.4418187561022));
#20454=CARTESIAN_POINT('Ctrl Pts',(-1.23443974609842,5.78654379364336,40.4344144324067));
#20455=CARTESIAN_POINT('Ctrl Pts',(-1.07269451833015,5.82104880129892,40.4266264546453));
#20456=CARTESIAN_POINT('Ctrl Pts',(-0.909472737823357,5.8487740873626,40.4188384768839));
#20457=CARTESIAN_POINT('Ctrl Pts',(-0.745356615472228,5.86961447441583,
40.4110504991224));
#20458=CARTESIAN_POINT('Ctrl Pts',(-0.581272759757513,5.89045076407032,
40.4032640525442));
#20459=CARTESIAN_POINT('Ctrl Pts',(-0.416295229851423,5.90440481537482,
40.395477605966));
#20460=CARTESIAN_POINT('Ctrl Pts',(-0.251013278018535,5.91142308558256,
40.3876911593877));
#20461=CARTESIAN_POINT('Ctrl Pts',(-0.0857250210519691,5.91844162352147,
40.3799044157741));
#20462=CARTESIAN_POINT('Ctrl Pts',(0.079867361995723,5.91852383341869,40.3721176721605));
#20463=CARTESIAN_POINT('Ctrl Pts',(0.245171930862612,5.91166823213356,40.3643309285469));
#20464=CARTESIAN_POINT('Ctrl Pts',(0.410465566068641,5.90481308429517,40.3565446999682));
#20465=CARTESIAN_POINT('Ctrl Pts',(0.575471105891679,5.89102105692617,40.3487584713894));
#20466=CARTESIAN_POINT('Ctrl Pts',(0.739598897850327,5.87034275258256,40.3409722428106));
#20467=CARTESIAN_POINT('Ctrl Pts',(0.903769895860926,5.84965900474957,40.3331839645352));
#20468=CARTESIAN_POINT('Ctrl Pts',(1.06706236679312,5.82208539564029,40.3253956862597));
#20469=CARTESIAN_POINT('Ctrl Pts',(1.22889314019929,5.78772426887038,40.3176074079842));
#20470=CARTESIAN_POINT('Ctrl Pts',(1.38274581315085,5.75505711238395,40.3102030842876));
#20471=CARTESIAN_POINT('Ctrl Pts',(1.53527717971602,5.71625560809119,40.302798760591));
#20472=CARTESIAN_POINT('Ctrl Pts',(1.68599585087666,5.67145030422789,40.2953944368944));
#20473=CARTESIAN_POINT('Ctrl Pts',(1.84452399029271,5.62432341939856,40.2876064591328));
#20474=CARTESIAN_POINT('Ctrl Pts',(2.00110330642086,5.57053718620394,40.2798184813711));
#20475=CARTESIAN_POINT('Ctrl Pts',(2.15517227522717,5.51027794458611,40.2720305036095));
#20476=CARTESIAN_POINT('Ctrl Pts',(2.30921095275264,5.45003055045208,40.2642440570311));
#20477=CARTESIAN_POINT('Ctrl Pts',(2.46073997033066,5.38331280352874,40.2564576104528));
#20478=CARTESIAN_POINT('Ctrl Pts',(2.60921633746004,5.31035974928551,40.2486711638744));
#20479=CARTESIAN_POINT('Ctrl Pts',(2.75769836862895,5.23740391204731,40.2408844202606));
#20480=CARTESIAN_POINT('Ctrl Pts',(2.9031272277931,5.15821242888512,40.2330976766468));
#20481=CARTESIAN_POINT('Ctrl Pts',(3.04498248363186,5.07306734006904,40.225310933033));
#20482=CARTESIAN_POINT('Ctrl Pts',(3.18682835680653,4.9879278829637,40.217524704454));
#20483=CARTESIAN_POINT('Ctrl Pts',(3.32510082571255,4.89683577279358,40.209738475875));
#20484=CARTESIAN_POINT('Ctrl Pts',(3.4593063994134,4.80011768579454,40.2019522472961));
#20485=CARTESIAN_POINT('Ctrl Pts',(3.59354730224935,4.70337413810659,40.1941639690204));
#20486=CARTESIAN_POINT('Ctrl Pts',(3.72371891004499,4.60100183957025,40.1863756907447));
#20487=CARTESIAN_POINT('Ctrl Pts',(3.84935818982042,4.49336979214514,40.1785874124691));
#20488=CARTESIAN_POINT('Ctrl Pts',(3.96880357472292,4.39104390046926,40.1711830887733));
#20489=CARTESIAN_POINT('Ctrl Pts',(4.08415254558197,4.28396454000282,40.1637787650775));
#20490=CARTESIAN_POINT('Ctrl Pts',(4.19503615380803,4.17248154348746,40.1563744413817));
#20491=CARTESIAN_POINT('Ctrl Pts',(4.31166518171814,4.0552220700621,40.1485864636202));
#20492=CARTESIAN_POINT('Ctrl Pts',(4.42339553742123,3.93304855110767,40.1407984858588));
#20493=CARTESIAN_POINT('Ctrl Pts',(4.5298233997066,3.80639337562088,40.1330105080973));
#20494=CARTESIAN_POINT('Ctrl Pts',(4.63623033736126,3.6797631016281,40.1252240615191));
#20495=CARTESIAN_POINT('Ctrl Pts',(4.73733665627559,3.54865317371616,40.1174376149409));
#20496=CARTESIAN_POINT('Ctrl Pts',(4.83277812135753,3.41352987276046,40.1096511683627));
#20497=CARTESIAN_POINT('Ctrl Pts',(4.92822322731687,3.27840141715449,40.1018644247491));
#20498=CARTESIAN_POINT('Ctrl Pts',(5.01800285944072,3.13925954086346,40.0940776811355));
#20499=CARTESIAN_POINT('Ctrl Pts',(5.10179508439075,2.99660098768361,40.0862909375218));
#20500=CARTESIAN_POINT('Ctrl Pts',(5.18558176711191,2.85395187029991,40.078504708943));
#20501=CARTESIAN_POINT('Ctrl Pts',(5.26338167340363,2.70778681711519,40.0707184803642));
#20502=CARTESIAN_POINT('Ctrl Pts',(5.3349178892649,2.55862886665912,40.0629322517854));
#20503=CARTESIAN_POINT('Ctrl Pts',(5.40647293677808,2.40943165090829,40.0551439735099));
#20504=CARTESIAN_POINT('Ctrl Pts',(5.4717608589818,2.25724025102981,40.0473556952344));
#20505=CARTESIAN_POINT('Ctrl Pts',(5.53055174379081,2.10260028815569,40.0395674169589));
#20506=CARTESIAN_POINT('Ctrl Pts',(5.58644429489555,1.95558392574076,40.0321630932624));
#20507=CARTESIAN_POINT('Ctrl Pts',(5.63646487922549,1.80635485463067,40.0247587695658));
#20508=CARTESIAN_POINT('Ctrl Pts',(5.68045701476837,1.65539683033067,40.0173544458693));
#20509=CARTESIAN_POINT('Ctrl Pts',(5.72672859706751,1.49661693572192,40.0095664681077));
#20510=CARTESIAN_POINT('Ctrl Pts',(5.76634697001505,1.3358673613977,40.0017784903461));
#20511=CARTESIAN_POINT('Ctrl Pts',(5.79916455054649,1.1737210393381,39.9939905125845));
#20512=CARTESIAN_POINT('Ctrl Pts',(5.83197567886009,1.01160659663632,39.9862040660061));
#20513=CARTESIAN_POINT('Ctrl Pts',(5.857988619303,0.848096267139428,39.9784176194277));
#20514=CARTESIAN_POINT('Ctrl Pts',(5.87710676821336,0.68377379119174,39.9706311728493));
#20515=CARTESIAN_POINT('Ctrl Pts',(5.89622564643809,0.519445046711268,39.9628444292356));
#20516=CARTESIAN_POINT('Ctrl Pts',(5.9084491659655,0.354304410726337,39.9550576856218));
#20517=CARTESIAN_POINT('Ctrl Pts',(5.91373244552398,0.188942121447266,39.947270942008));
#20518=CARTESIAN_POINT('Ctrl Pts',(5.91901537563306,0.023590769645819,39.939484713429));
#20519=CARTESIAN_POINT('Ctrl Pts',(5.91735897429893,-0.141981886694097,
39.93169848485));
#20520=CARTESIAN_POINT('Ctrl Pts',(5.90877047349355,-0.307184071967987,
39.923912256271));
#20521=CARTESIAN_POINT('Ctrl Pts',(5.90017971179623,-0.472429746122778,
39.9161239779954));
#20522=CARTESIAN_POINT('Ctrl Pts',(5.88465321884044,-0.637304434902332,
39.9083356997197));
#20523=CARTESIAN_POINT('Ctrl Pts',(5.86225030366254,-0.801219033541034,
39.900547421444));
#20524=CARTESIAN_POINT('Ctrl Pts',(5.84095183051669,-0.95705280113766,39.8931430977483));
#20525=CARTESIAN_POINT('Ctrl Pts',(5.81343864062051,-1.1120186002606,39.8857387740525));
#20526=CARTESIAN_POINT('Ctrl Pts',(5.7798049012923,-1.2656167925156,39.8783344503567));
#20527=CARTESIAN_POINT('Ctrl Pts',(5.74442843415169,-1.42717365505005,39.8705464725952));
#20528=CARTESIAN_POINT('Ctrl Pts',(5.70226765216034,-1.58727521525857,39.8627584948338));
#20529=CARTESIAN_POINT('Ctrl Pts',(5.65346722174493,-1.74534779776285,39.8549705170723));
#20530=CARTESIAN_POINT('Ctrl Pts',(5.60467638591247,-1.9033893018424,39.8471840704941));
#20531=CARTESIAN_POINT('Ctrl Pts',(5.54924860054122,-2.05940231902604,39.8393976239158));
#20532=CARTESIAN_POINT('Ctrl Pts',(5.48737846539814,-2.21282808640544,39.8316111773375));
#20533=CARTESIAN_POINT('Ctrl Pts',(5.42550597004899,-2.36625970663171,39.8238244337239));
#20534=CARTESIAN_POINT('Ctrl Pts',(5.35719074899398,-2.51710358172856,39.8160376901103));
#20535=CARTESIAN_POINT('Ctrl Pts',(5.28267592438608,-2.66482000150323,39.8082509464966));
#20536=CARTESIAN_POINT('Ctrl Pts',(5.20816602837638,-2.8125266509418,39.8004647179178));
#20537=CARTESIAN_POINT('Ctrl Pts',(5.12745749343406,-2.9571059737336,39.792678489339));
#20538=CARTESIAN_POINT('Ctrl Pts',(5.04083993285009,-3.09804185476631,39.7848922607602));
#20539=CARTESIAN_POINT('Ctrl Pts',(4.95419957050444,-3.23901483666345,39.7771039824847));
#20540=CARTESIAN_POINT('Ctrl Pts',(4.86164724000419,-3.37634218682199,39.7693157042092));
#20541=CARTESIAN_POINT('Ctrl Pts',(4.7635169996695,-3.50953506270556,39.7615274259337));
#20542=CARTESIAN_POINT('Ctrl Pts',(4.67022448518173,-3.63616165875438,39.7541231022373));
#20543=CARTESIAN_POINT('Ctrl Pts',(4.57189094021556,-3.75905139980351,39.7467187785408));
#20544=CARTESIAN_POINT('Ctrl Pts',(4.46883820390687,-3.87781067998457,39.7393144548443));
#20545=CARTESIAN_POINT('Ctrl Pts',(4.36044580352792,-4.00272345675493,39.7315264770827));
#20546=CARTESIAN_POINT('Ctrl Pts',(4.24679340514233,-4.12311105354791,39.7237384993211));
#20547=CARTESIAN_POINT('Ctrl Pts',(4.12828262500392,-4.23853903256662,39.7159505215595));
#20548=CARTESIAN_POINT('Ctrl Pts',(4.00979514510056,-4.35394431745539,39.708164074981));
#20549=CARTESIAN_POINT('Ctrl Pts',(3.88645141812188,-4.46439170736599,39.7003776284026));
#20550=CARTESIAN_POINT('Ctrl Pts',(3.75868976350009,-4.56948375905415,39.6925911818242));
#20551=CARTESIAN_POINT('Ctrl Pts',(3.63092323505921,-4.67457981976716,39.6848044382104));
#20552=CARTESIAN_POINT('Ctrl Pts',(3.4987386860025,-4.7743199274167,39.6770176945966));
#20553=CARTESIAN_POINT('Ctrl Pts',(3.36260791832758,-4.86834659305402,39.6692309509828));
#20554=CARTESIAN_POINT('Ctrl Pts',(3.22648615468537,-4.96236703953025,39.6614447224038));
#20555=CARTESIAN_POINT('Ctrl Pts',(3.08641895776537,-5.05067461870308,39.6536584938249));
#20556=CARTESIAN_POINT('Ctrl Pts',(2.94290765442067,-5.13295481180696,39.645872265246));
#20557=CARTESIAN_POINT('Ctrl Pts',(2.79935857224034,-5.21525666487643,39.6380839869703));
#20558=CARTESIAN_POINT('Ctrl Pts',(2.65236384839128,-5.29152780059809,39.6302957086946));
#20559=CARTESIAN_POINT('Ctrl Pts',(2.50245077780901,-5.3614989198118,39.622507430419));
#20560=CARTESIAN_POINT('Ctrl Pts',(2.35992827648972,-5.42802053058072,39.6151031067232));
#20561=CARTESIAN_POINT('Ctrl Pts',(2.21476847919791,-5.48884821972119,39.6076987830274));
#20562=CARTESIAN_POINT('Ctrl Pts',(2.06744236578854,-5.5437904565958,39.6002944593317));
#20563=CARTESIAN_POINT('Ctrl Pts',(1.91248256904622,-5.60157951830139,39.5925064815702));
#20564=CARTESIAN_POINT('Ctrl Pts',(1.75507056904914,-5.65287769932322,39.5847185038088));
#20565=CARTESIAN_POINT('Ctrl Pts',(1.5957669345808,-5.69749580543932,39.5769305260473));
#20566=CARTESIAN_POINT('Ctrl Pts',(1.4364946205718,-5.7421051392535,39.569144079469));
#20567=CARTESIAN_POINT('Ctrl Pts',(1.27533172168438,-5.78003693257096,39.5613576328907));
#20568=CARTESIAN_POINT('Ctrl Pts',(1.11285332387517,-5.81115204086419,39.5535711863125));
#20569=CARTESIAN_POINT('Ctrl Pts',(0.950368727881924,-5.84226833612854,
39.5457844426988));
#20570=CARTESIAN_POINT('Ctrl Pts',(0.786568845641503,-5.8665673620375,39.5379976990851));
#20571=CARTESIAN_POINT('Ctrl Pts',(0.622039035864958,-5.88396108079924,
39.5302109554715));
#20572=CARTESIAN_POINT('Ctrl Pts',(0.457520108504363,-5.90135364909662,
39.5224247268927));
#20573=CARTESIAN_POINT('Ctrl Pts',(0.292271668039328,-5.9118417907557,39.5146384983139));
#20574=CARTESIAN_POINT('Ctrl Pts',(0.126884427473591,-5.91538932823231,
39.506852269735));
#20575=CARTESIAN_POINT('Ctrl Pts',(-0.0385463506887493,-5.91893779958541,
39.4990639914595));
#20576=CARTESIAN_POINT('Ctrl Pts',(-0.204115682316106,-5.91554200703426,
39.491275713184));
#20577=CARTESIAN_POINT('Ctrl Pts',(-0.369231699670738,-5.90521790575574,
39.4834874349085));
#20578=CARTESIAN_POINT('Ctrl Pts',(-0.526207657220763,-5.89540277267536,
39.4760831112121));
#20579=CARTESIAN_POINT('Ctrl Pts',(-0.68277365677089,-5.87932600977436,
39.4686787875156));
#20580=CARTESIAN_POINT('Ctrl Pts',(-0.838424500269211,-5.85704489651977,
39.4612744638192));
#20581=CARTESIAN_POINT('Ctrl Pts',(-1.00214037189203,-5.8336092902923,39.4534864860575));
#20582=CARTESIAN_POINT('Ctrl Pts',(-1.16490229652459,-5.80330092493929,
39.4456985082959));
#20583=CARTESIAN_POINT('Ctrl Pts',(-1.3261275357285,-5.76622201458482,39.4379105305343));
#20584=CARTESIAN_POINT('Ctrl Pts',(-1.48732107666961,-5.72915039426169,
39.4301240839558));
#20585=CARTESIAN_POINT('Ctrl Pts',(-1.64697822378216,-5.68531095654473,
39.4223376373773));
#20586=CARTESIAN_POINT('Ctrl Pts',(-1.80452744975621,-5.63485680790349,
39.4145511907989));
#20587=CARTESIAN_POINT('Ctrl Pts',(-1.96208268587634,-5.58440073455079,
39.4067644471851));
#20588=CARTESIAN_POINT('Ctrl Pts',(-2.11752953443022,-5.52732953903367,
39.3989777035713));
#20589=CARTESIAN_POINT('Ctrl Pts',(-2.27031191179147,-5.46384611658105,
39.3911909599575));
#20590=CARTESIAN_POINT('Ctrl Pts',(-2.42308418374147,-5.40036689308187,
39.3834047313786));
#20591=CARTESIAN_POINT('Ctrl Pts',(-2.57319204210018,-5.33047641410572,
39.3756185027996));
#20592=CARTESIAN_POINT('Ctrl Pts',(-2.72009952599787,-5.25442567091458,
39.3678322742207));
#20593=CARTESIAN_POINT('Ctrl Pts',(-2.86704568276299,-5.17835490763848,
39.360043995945));
#20594=CARTESIAN_POINT('Ctrl Pts',(-3.01078949673259,-5.09612078498146,
39.3522557176694));
#20595=CARTESIAN_POINT('Ctrl Pts',(-3.15081894741486,-5.00802061927779,
39.3444674393937));
#20596=CARTESIAN_POINT('Ctrl Pts',(-3.28394508172679,-4.92426370646248,
39.337063115698));
#20597=CARTESIAN_POINT('Ctrl Pts',(-3.41371403681091,-4.83520533901766,
39.3296587920023));
#20598=CARTESIAN_POINT('Ctrl Pts',(-3.53970966843084,-4.74113762990669,
39.3222544683066));
#20599=CARTESIAN_POINT('Ctrl Pts',(-3.67223374725513,-4.64219581472816,
39.3144664905452));
#20600=CARTESIAN_POINT('Ctrl Pts',(-3.80063049887293,-4.53767636537523,
39.3066785127838));
#20601=CARTESIAN_POINT('Ctrl Pts',(-3.92443720762358,-4.42794796332564,
39.2988905350224));
#20602=CARTESIAN_POINT('Ctrl Pts',(-4.04821957491413,-4.31824113482038,
39.2911040884441));
#20603=CARTESIAN_POINT('Ctrl Pts',(-4.16741346097805,-4.20332760886863,
39.2833176418659));
#20604=CARTESIAN_POINT('Ctrl Pts',(-4.28159035398739,-4.0836153838409,39.2755311952876));
#20605=CARTESIAN_POINT('Ctrl Pts',(-4.39577160258792,-3.96389859206155,
39.267744451674));
#20606=CARTESIAN_POINT('Ctrl Pts',(-4.50493525176469,-3.83938296340247,
39.2599577080604));
#20607=CARTESIAN_POINT('Ctrl Pts',(-4.60869018143983,-3.71051281819644,
39.2521709644468));
#20608=CARTESIAN_POINT('Ctrl Pts',(-4.71243824850303,-3.58165119678587,
39.244384735868));
#20609=CARTESIAN_POINT('Ctrl Pts',(-4.81077811164378,-3.44843588419347,
39.2365985072891));
#20610=CARTESIAN_POINT('Ctrl Pts',(-4.90335934049069,-3.31134379678745,
39.2288122787103));
#20611=CARTESIAN_POINT('Ctrl Pts',(-4.99596494101312,-3.17421562038246,
39.2210240004348));
#20612=CARTESIAN_POINT('Ctrl Pts',(-5.08280869749645,-3.0332088937969,39.2132357221593));
#20613=CARTESIAN_POINT('Ctrl Pts',(-5.16358337343216,-2.88882974716666,
39.2054474438838));
#20614=CARTESIAN_POINT('Ctrl Pts',(-5.24037593604437,-2.75156835268795,
39.1980431201873));
#20615=CARTESIAN_POINT('Ctrl Pts',(-5.31168327443589,-2.61125927239488,
39.1906387964907));
#20616=CARTESIAN_POINT('Ctrl Pts',(-5.37727984041684,-2.46835817505213,
39.1832344727942));
#20617=CARTESIAN_POINT('Ctrl Pts',(-5.44600563262427,-2.31864010711172,
39.1754769323773));
#20618=CARTESIAN_POINT('Ctrl Pts',(-5.50848877556581,-2.16601916666619,
39.1677193919604));
#20619=CARTESIAN_POINT('Ctrl Pts',(-5.56450037895025,-2.01103607505249,
39.1599618515435));
#20620=CARTESIAN_POINT('Ctrl Pts',(-5.62261559505141,-1.85023232516988,
39.1519129632686));
#20621=CARTESIAN_POINT('Ctrl Pts',(-5.67376357479425,-1.6868858800762,39.1438640749937));
#20622=CARTESIAN_POINT('Ctrl Pts',(-5.71774411285594,-1.52162177376679,
39.1358151867188));
#20623=CARTESIAN_POINT('Ctrl Pts',(-5.76012303573033,-1.36237599998007,
39.1280594104036));
#20624=CARTESIAN_POINT('Ctrl Pts',(-5.79584726755631,-1.20135010997528,
39.1203036340885));
#20625=CARTESIAN_POINT('Ctrl Pts',(-5.82478889000928,-1.03911738957853,
39.1125478577733));
#20626=CARTESIAN_POINT('Ctrl Pts',(-5.85372943094268,-0.876890731656749,
39.1047923712838));
#20627=CARTESIAN_POINT('Ctrl Pts',(-5.87588781401548,-0.713457653276527,
39.0970368847942));
#20628=CARTESIAN_POINT('Ctrl Pts',(-5.89118746677025,-0.549400394857105,
39.0892813983047));
#20629=CARTESIAN_POINT('Ctrl Pts',(-5.90648969860401,-0.385315481128406,
39.0815246044644));
#20630=CARTESIAN_POINT('Ctrl Pts',(-5.91493086209221,-0.220606500444764,
39.0737678106242));
#20631=CARTESIAN_POINT('Ctrl Pts',(-5.91648630544981,-0.0558601819265851,
39.0660110167839));
#20632=CARTESIAN_POINT('Ctrl Pts',(-5.91666248974519,-0.0371994483791566,
39.0651324086042));
#20633=CARTESIAN_POINT('Ctrl Pts',(-5.91675038539335,-0.0185382371664036,
39.0642538004244));
#20634=CARTESIAN_POINT('Ctrl Pts',(-5.91674999872984,0.000122598544141182,
39.0633751922447));
#20635=CARTESIAN_POINT('Ctrl Pts',(-5.91674999852516,0.000132107828751824,
38.8116248077951));
#20636=CARTESIAN_POINT('Ctrl Pts',(-5.9167536915139,-0.165266803763928,
38.8194094218845));
#20637=CARTESIAN_POINT('Ctrl Pts',(-5.90981761062779,-0.330675236470803,
38.8271940359738));
#20638=CARTESIAN_POINT('Ctrl Pts',(-5.89596542934449,-0.495501986347875,
38.8349786500631));
#20639=CARTESIAN_POINT('Ctrl Pts',(-5.88211413062991,-0.660318234562368,
38.8427627681687));
#20640=CARTESIAN_POINT('Ctrl Pts',(-5.86134764036802,-0.824552555352156,
38.8505468862743));
#20641=CARTESIAN_POINT('Ctrl Pts',(-5.83374157440724,-0.987618248885952,
38.8583310043799));
#20642=CARTESIAN_POINT('Ctrl Pts',(-5.80612776919019,-1.1507296572707,38.8661173047336));
#20643=CARTESIAN_POINT('Ctrl Pts',(-5.77167060808896,-1.31267146776595,
38.8739036050873));
#20644=CARTESIAN_POINT('Ctrl Pts',(-5.73049713102611,-1.47286564010488,
38.881689905441));
#20645=CARTESIAN_POINT('Ctrl Pts',(-5.68943104611784,-1.63264198041826,
38.8894558969057));
#20646=CARTESIAN_POINT('Ctrl Pts',(-5.64168374426802,-1.79067948835634,
38.8972218883705));
#20647=CARTESIAN_POINT('Ctrl Pts',(-5.58743109435409,-1.94641833333565,
38.9049878798353));
#20648=CARTESIAN_POINT('Ctrl Pts',(-5.53302391623533,-2.10260077036387,
38.9127759912283));
#20649=CARTESIAN_POINT('Ctrl Pts',(-5.47205439836578,-2.25652843993273,
38.9205641026212));
#20650=CARTESIAN_POINT('Ctrl Pts',(-5.40473466168731,-2.40764901911715,
38.9283522140142));
#20651=CARTESIAN_POINT('Ctrl Pts',(-5.33742814206569,-2.55873992841001,
38.9361387963472));
#20652=CARTESIAN_POINT('Ctrl Pts',(-5.26377402122413,-2.70702455527588,
38.9439253786802));
#20653=CARTESIAN_POINT('Ctrl Pts',(-5.18403221618832,-2.85197134347834,
38.9517119610133));
#20654=CARTESIAN_POINT('Ctrl Pts',(-5.10428737061506,-2.99692365846989,
38.959498840247));
#20655=CARTESIAN_POINT('Ctrl Pts',(-5.01845452692368,-3.13853759827777,
38.9672857194807));
#20656=CARTESIAN_POINT('Ctrl Pts',(-4.92683950299966,-3.27630631568267,
38.9750725987144));
#20657=CARTESIAN_POINT('Ctrl Pts',(-4.83523052561402,-3.41406594043219,
38.9828589640186));
#20658=CARTESIAN_POINT('Ctrl Pts',(-4.73784030872284,-3.54798058461169,
38.9906453293228));
#20659=CARTESIAN_POINT('Ctrl Pts',(-4.63501801240989,-3.67757237687254,
38.998431694627));
#20660=CARTESIAN_POINT('Ctrl Pts',(-4.53216871705015,-3.80719819730614,
39.0062201044726));
#20661=CARTESIAN_POINT('Ctrl Pts',(-4.42388468933028,-3.93249864598739,
39.0140085143182));
#20662=CARTESIAN_POINT('Ctrl Pts',(-4.31055596035097,-4.05302823518203,
39.0217969241637));
#20663=CARTESIAN_POINT('Ctrl Pts',(-4.20318287806859,-4.16722375837033,
39.029176037816));
#20664=CARTESIAN_POINT('Ctrl Pts',(-4.09128185308816,-4.27713677143141,
39.0365551514682));
#20665=CARTESIAN_POINT('Ctrl Pts',(-3.9752156168088,-4.38241843761859,39.0439342651204));
#20666=CARTESIAN_POINT('Ctrl Pts',(-3.85271624632737,-4.49353548805973,
39.0517223765134));
#20667=CARTESIAN_POINT('Ctrl Pts',(-3.72553309577955,-4.59953292097697,
39.0595104879064));
#20668=CARTESIAN_POINT('Ctrl Pts',(-3.59411668417073,-4.70002721514095,
39.0672985992993));
#20669=CARTESIAN_POINT('Ctrl Pts',(-3.46272607388376,-4.80050177900188,
39.0750851816324));
#20670=CARTESIAN_POINT('Ctrl Pts',(-3.32710411454507,-4.89547516594232,
39.0828717639654));
#20671=CARTESIAN_POINT('Ctrl Pts',(-3.18773336047609,-4.98460495776825,
39.0906583462985));
#20672=CARTESIAN_POINT('Ctrl Pts',(-3.0483572922309,-5.07373814809355,39.0984452255322));
#20673=CARTESIAN_POINT('Ctrl Pts',(-2.9052324102819,-5.1570271219814,39.106232104766));
#20674=CARTESIAN_POINT('Ctrl Pts',(-2.75886975387813,-5.23417311937964,
39.1140189839997));
#20675=CARTESIAN_POINT('Ctrl Pts',(-2.61251675732482,-5.31131402518679,
39.1218053493039));
#20676=CARTESIAN_POINT('Ctrl Pts',(-2.46292669668928,-5.3823126169404,39.1295917146081));
#20677=CARTESIAN_POINT('Ctrl Pts',(-2.31063480791587,-5.44691631539788,
39.1373780799123));
#20678=CARTESIAN_POINT('Ctrl Pts',(-2.15830293038553,-5.51153697747447,
39.1451664897579));
#20679=CARTESIAN_POINT('Ctrl Pts',(-2.00326810068891,-5.56975926427218,
39.1529548996035));
#20680=CARTESIAN_POINT('Ctrl Pts',(-1.8460859510802,-5.62137858747517,39.1607433094491));
#20681=CARTESIAN_POINT('Ctrl Pts',(-1.69716403132471,-5.67028521413096,
39.1681224231012));
#20682=CARTESIAN_POINT('Ctrl Pts',(-1.54631492559119,-5.71326494343056,
39.1755015367534));
#20683=CARTESIAN_POINT('Ctrl Pts',(-1.39402405240194,-5.7501849973566,39.1828806504055));
#20684=CARTESIAN_POINT('Ctrl Pts',(-1.23329224361816,-5.78915139713915,
39.1906687617985));
#20685=CARTESIAN_POINT('Ctrl Pts',(-1.07089690620403,-5.82138125835975,
39.1984568731914));
#20686=CARTESIAN_POINT('Ctrl Pts',(-0.907417141262457,-5.84675334645161,
39.2062449845844));
#20687=CARTESIAN_POINT('Ctrl Pts',(-0.743969472723136,-5.87212045317623,
39.2140315669174));
#20688=CARTESIAN_POINT('Ctrl Pts',(-0.579438117025394,-5.89063242427489,
39.2218181492504));
#20689=CARTESIAN_POINT('Ctrl Pts',(-0.414410641072862,-5.90221944551925,
39.2296047315835));
#20690=CARTESIAN_POINT('Ctrl Pts',(-0.249376872659111,-5.91380690857418,
39.2373916108172));
#20691=CARTESIAN_POINT('Ctrl Pts',(-0.0838472645923005,-5.91846886709936,
39.2451784900509));
#20692=CARTESIAN_POINT('Ctrl Pts',(0.081586490553414,-5.91618747227124,
39.2529653692846));
#20693=CARTESIAN_POINT('Ctrl Pts',(0.247009327167273,-5.91390622801386,
39.2607517345888));
#20694=CARTESIAN_POINT('Ctrl Pts',(0.41233600399847,-5.90468255197068,39.268538099893));
#20695=CARTESIAN_POINT('Ctrl Pts',(0.576975675330162,-5.88855072429348,
39.2763244651972));
#20696=CARTESIAN_POINT('Ctrl Pts',(0.741658577696028,-5.87241466072594,
39.2841128750428));
#20697=CARTESIAN_POINT('Ctrl Pts',(0.905653795694052,-5.849366850141,39.2919012848884));
#20698=CARTESIAN_POINT('Ctrl Pts',(1.06837553369385,-5.81949347293254,39.299689694734));
#20699=CARTESIAN_POINT('Ctrl Pts',(1.2225459256214,-5.79119000021253,39.3070688083862));
#20700=CARTESIAN_POINT('Ctrl Pts',(1.37557298684746,-5.75675994990192,39.3144479220384));
#20701=CARTESIAN_POINT('Ctrl Pts',(1.52696693460137,-5.71631896793156,39.3218270356906));
#20702=CARTESIAN_POINT('Ctrl Pts',(1.68675210459546,-5.67363648772193,39.3296151470836));
#20703=CARTESIAN_POINT('Ctrl Pts',(1.84477505944887,-5.62424260847048,39.3374032584765));
#20704=CARTESIAN_POINT('Ctrl Pts',(2.00046927437237,-5.56830793372565,39.3451913698695));
#20705=CARTESIAN_POINT('Ctrl Pts',(2.15613292145087,-5.51238424077915,39.3529779522025));
#20706=CARTESIAN_POINT('Ctrl Pts',(2.30946844033886,-5.44992242260928,39.3607645345356));
#20707=CARTESIAN_POINT('Ctrl Pts',(2.4599264735374,-5.38114228647504,39.3685511168686));
#20708=CARTESIAN_POINT('Ctrl Pts',(2.61039024366752,-5.3123595277694,39.3763379961023));
#20709=CARTESIAN_POINT('Ctrl Pts',(2.75797601632913,-5.23725809827598,39.3841248753361));
#20710=CARTESIAN_POINT('Ctrl Pts',(2.90215567325997,-5.15610541112815,39.3919117545698));
#20711=CARTESIAN_POINT('Ctrl Pts',(3.04632581441721,-5.07495808001053,39.399698119874));
#20712=CARTESIAN_POINT('Ctrl Pts',(3.18709001129192,-4.98776044730135,39.4074844851782));
#20713=CARTESIAN_POINT('Ctrl Pts',(3.32394582960667,-4.89482529661074,39.4152708504824));
#20714=CARTESIAN_POINT('Ctrl Pts',(3.4608375834798,-4.80186574303705,39.423059260328));
#20715=CARTESIAN_POINT('Ctrl Pts',(3.59381864250501,-4.70316583908828,39.4308476701736));
#20716=CARTESIAN_POINT('Ctrl Pts',(3.72241583790705,-4.59908152702241,39.4386360800192));
#20717=CARTESIAN_POINT('Ctrl Pts',(3.84425499879354,-4.50046704943674,39.4460151936714));
#20718=CARTESIAN_POINT('Ctrl Pts',(3.96215900412751,-4.39701969394617,39.4533943073236));
#20719=CARTESIAN_POINT('Ctrl Pts',(4.07575309356943,-4.28907534123139,39.4607734209758));
#20720=CARTESIAN_POINT('Ctrl Pts',(4.19564329500173,-4.1751480211214,39.4685615323688));
#20721=CARTESIAN_POINT('Ctrl Pts',(4.31077508512322,-4.0561703741806,39.4763496437617));
#20722=CARTESIAN_POINT('Ctrl Pts',(4.42073260833838,-3.93256325671612,39.4841377551547));
#20723=CARTESIAN_POINT('Ctrl Pts',(4.53066854331052,-3.80898040735458,39.4919243374877));
#20724=CARTESIAN_POINT('Ctrl Pts',(4.63543202611002,-3.68077013961672,39.4997109198207));
#20725=CARTESIAN_POINT('Ctrl Pts',(4.73464581692109,-3.54838830327398,39.5074975021538));
#20726=CARTESIAN_POINT('Ctrl Pts',(4.83386339073217,-3.41600141924096,39.5152843813875));
#20727=CARTESIAN_POINT('Ctrl Pts',(4.92753065434675,-3.27944290163392,39.5230712606212));
#20728=CARTESIAN_POINT('Ctrl Pts',(5.01531179493667,-3.13920024242944,39.5308581398549));
#20729=CARTESIAN_POINT('Ctrl Pts',(5.10308714202204,-2.99896683915944,39.5386445051591));
#20730=CARTESIAN_POINT('Ctrl Pts',(5.18497697404958,-2.85505005180575,39.5464308704633));
#20731=CARTESIAN_POINT('Ctrl Pts',(5.26068973872044,-2.70796492507224,39.5542172357675));
#20732=CARTESIAN_POINT('Ctrl Pts',(5.33642238402598,-2.56084117677096,39.5620056456131));
#20733=CARTESIAN_POINT('Ctrl Pts',(5.40597457287245,-2.41054771009415,39.5697940554587));
#20734=CARTESIAN_POINT('Ctrl Pts',(5.4691011002856,-2.2576234666912,39.5775824653043));
#20735=CARTESIAN_POINT('Ctrl Pts',(5.52891020503042,-2.11273569182839,39.5849615789565));
#20736=CARTESIAN_POINT('Ctrl Pts',(5.5829515406437,-1.96548677374418,39.5923406926087));
#20737=CARTESIAN_POINT('Ctrl Pts',(5.63105671867893,-1.81635095549315,39.5997198062609));
#20738=CARTESIAN_POINT('Ctrl Pts',(5.68182819378697,-1.65894907500318,39.6075079176538));
#20739=CARTESIAN_POINT('Ctrl Pts',(5.72600494485602,-1.49938897901227,39.6152960290467));
#20740=CARTESIAN_POINT('Ctrl Pts',(5.76342315209342,-1.33823919103186,39.6230841404395));
#20741=CARTESIAN_POINT('Ctrl Pts',(5.80083401291802,-1.1771210420035,39.6308707227725));
#20742=CARTESIAN_POINT('Ctrl Pts',(5.83148890528973,-1.01441413479051,39.6386573051055));
#20743=CARTESIAN_POINT('Ctrl Pts',(5.85527466092086,-0.850699246313389,
39.6464438874384));
#20744=CARTESIAN_POINT('Ctrl Pts',(5.87906132349765,-0.686978115423271,
39.6542307666721));
#20745=CARTESIAN_POINT('Ctrl Pts',(5.8959782753877,-0.52224924199067,39.6620176459057));
#20746=CARTESIAN_POINT('Ctrl Pts',(5.90596386503354,-0.357101368546964,
39.6698045251393));
#20747=CARTESIAN_POINT('Ctrl Pts',(5.9159487956362,-0.191964394767925,39.6775908904434));
#20748=CARTESIAN_POINT('Ctrl Pts',(5.91900326028553,-0.0264087952951148,
39.6853772557475));
#20749=CARTESIAN_POINT('Ctrl Pts',(5.91511765580153,0.138973668459359,39.6931636210516));
#20750=CARTESIAN_POINT('Ctrl Pts',(5.91123103103668,0.30439955829094,39.7009520308971));
#20751=CARTESIAN_POINT('Ctrl Pts',(5.90040070133012,0.469651901865704,39.7087404407427));
#20752=CARTESIAN_POINT('Ctrl Pts',(5.88266919528697,0.634140127512631,39.7165288505882));
#20753=CARTESIAN_POINT('Ctrl Pts',(5.865869514618,0.789984174710317,39.7239079642408));
#20754=CARTESIAN_POINT('Ctrl Pts',(5.8428753700362,0.945142091521705,39.7312870778934));
#20755=CARTESIAN_POINT('Ctrl Pts',(5.81376579040385,1.09911687132437,39.738666191546));
#20756=CARTESIAN_POINT('Ctrl Pts',(5.7830427714266,1.26162591960481,39.7464543029391));
#20757=CARTESIAN_POINT('Ctrl Pts',(5.74549620833344,1.42287499764621,39.7542424143322));
#20758=CARTESIAN_POINT('Ctrl Pts',(5.70125424892118,1.58228649481003,39.7620305257253));
#20759=CARTESIAN_POINT('Ctrl Pts',(5.65702097564673,1.74166669430414,39.7698171080585));
#20760=CARTESIAN_POINT('Ctrl Pts',(5.60609501431728,1.89920972507734,39.7776036903916));
#20761=CARTESIAN_POINT('Ctrl Pts',(5.54865485343531,2.05435144995903,39.7853902727248));
#20762=CARTESIAN_POINT('Ctrl Pts',(5.49121250237248,2.209499090361,39.7931771519586));
#20763=CARTESIAN_POINT('Ctrl Pts',(5.42725556197475,2.36224494064844,39.8009640311925));
#20764=CARTESIAN_POINT('Ctrl Pts',(5.3570115697905,2.51204251628645,39.8087509104263));
#20765=CARTESIAN_POINT('Ctrl Pts',(5.28677221366921,2.66183020537087,39.8165372757307));
#20766=CARTESIAN_POINT('Ctrl Pts',(5.21024677190148,2.8086697199264,39.824323641035));
#20767=CARTESIAN_POINT('Ctrl Pts',(5.12770993124302,2.95203682624924,39.8321100063393));
#20768=CARTESIAN_POINT('Ctrl Pts',(5.04515141808631,3.09544157786278,39.839898416185));
#20769=CARTESIAN_POINT('Ctrl Pts',(4.95657850976868,3.23537182124153,39.8476868260307));
#20770=CARTESIAN_POINT('Ctrl Pts',(4.86231110194224,3.37132930910483,39.8554752358764));
#20771=CARTESIAN_POINT('Ctrl Pts',(4.77299763105797,3.50014196465312,39.862854349528));
#20772=CARTESIAN_POINT('Ctrl Pts',(4.67857292898766,3.6253884634724,39.8702334631796));
#20773=CARTESIAN_POINT('Ctrl Pts',(4.57934417827356,3.74667018289735,39.8776125768312));
#20774=CARTESIAN_POINT('Ctrl Pts',(4.47461553464101,3.87467411201458,39.8854006882241));
#20775=CARTESIAN_POINT('Ctrl Pts',(4.36449779535653,3.99830700837581,39.893188799617));
#20776=CARTESIAN_POINT('Ctrl Pts',(4.24937983922382,4.1171229693195,39.9009769110099));
#20777=CARTESIAN_POINT('Ctrl Pts',(4.13428448449529,4.2359156028202,39.9087634933429));
#20778=CARTESIAN_POINT('Ctrl Pts',(4.01419109391674,4.34989295855654,39.9165500756759));
#20779=CARTESIAN_POINT('Ctrl Pts',(3.88952630543241,4.45864504999549,39.9243366580089));
#20780=CARTESIAN_POINT('Ctrl Pts',(3.76485676350681,4.56740128812804,39.9321235372425));
#20781=CARTESIAN_POINT('Ctrl Pts',(3.635615713068,4.6709316502703,39.9399104164762));
#20782=CARTESIAN_POINT('Ctrl Pts',(3.50226441750365,4.76886511786482,39.9476972957099));
#20783=CARTESIAN_POINT('Ctrl Pts',(3.36892192304767,4.86679212190712,39.955483661014));
#20784=CARTESIAN_POINT('Ctrl Pts',(3.23146998395461,4.95912278155527,39.9632700263182));
#20785=CARTESIAN_POINT('Ctrl Pts',(3.09040062082509,5.04552817505798,39.9710563916224));
#20786=CARTESIAN_POINT('Ctrl Pts',(2.94929421574576,5.13195625686223,39.9788448014679));
#20787=CARTESIAN_POINT('Ctrl Pts',(2.80456876025181,5.21245579493993,39.9866332113135));
#20788=CARTESIAN_POINT('Ctrl Pts',(2.65674354108654,5.28674231634141,39.994421621159));
#20789=CARTESIAN_POINT('Ctrl Pts',(2.51668682674466,5.35712493553271,40.0018007348115));
#20790=CARTESIAN_POINT('Ctrl Pts',(2.37384799876125,5.42193063785565,40.0091798484639));
#20791=CARTESIAN_POINT('Ctrl Pts',(2.22868751627878,5.48095635060918,40.0165589621163));
#20792=CARTESIAN_POINT('Ctrl Pts',(2.07548131013064,5.54325364641247,40.0243470735092));
#20793=CARTESIAN_POINT('Ctrl Pts',(1.91963407228572,5.59913430517782,40.0321351849022));
#20794=CARTESIAN_POINT('Ctrl Pts',(1.76170062165578,5.6483928229327,40.0399232962951));
#20795=CARTESIAN_POINT('Ctrl Pts',(1.60379817850537,5.69764166963643,40.0477098786281));
#20796=CARTESIAN_POINT('Ctrl Pts',(1.44381064467451,5.74027087441918,40.0554964609612));
#20797=CARTESIAN_POINT('Ctrl Pts',(1.28230881269572,5.77612453738516,40.0632830432942));
#20798=CARTESIAN_POINT('Ctrl Pts',(1.12080082268818,5.81197956744329,40.0710699225279));
#20799=CARTESIAN_POINT('Ctrl Pts',(0.957778730061289,5.8410584656247,40.0788568017616));
#20800=CARTESIAN_POINT('Ctrl Pts',(0.793825089086202,5.86325611673559,40.0866436809953));
#20801=CARTESIAN_POINT('Ctrl Pts',(0.629882268956349,5.88545230281437,40.0944300462994));
#20802=CARTESIAN_POINT('Ctrl Pts',(0.465008340192592,5.90076810790694,40.1022164116036));
#20803=CARTESIAN_POINT('Ctrl Pts',(0.299792725080259,5.90915009832116,40.1100027769077));
#20804=CARTESIAN_POINT('Ctrl Pts',(0.134533727702779,5.91753428967583,40.1177911867533));
#20805=CARTESIAN_POINT('Ctrl Pts',(-0.0310668160726866,5.91898101011672,
40.1255795965989));
#20806=CARTESIAN_POINT('Ctrl Pts',(-0.196416806812622,5.9134889025432,40.1333680064444));
#20807=CARTESIAN_POINT('Ctrl Pts',(-0.353077331653457,5.90828541598054,
40.1407471200967));
#20808=CARTESIAN_POINT('Ctrl Pts',(-0.509512700296116,5.89685365014063,
40.1481262337491));
#20809=CARTESIAN_POINT('Ctrl Pts',(-0.665221415915665,5.87923558214052,
40.1555053474014));
#20810=CARTESIAN_POINT('Ctrl Pts',(-0.829560505843994,5.86064100797096,
40.1632934587944));
#20811=CARTESIAN_POINT('Ctrl Pts',(-0.993148800557225,5.83514827565258,
40.1710815701873));
#20812=CARTESIAN_POINT('Ctrl Pts',(-1.1554007805571,5.80284237238856,40.1788696815803));
#20813=CARTESIAN_POINT('Ctrl Pts',(-1.31762090520955,5.77054281182538,40.1866562639134));
#20814=CARTESIAN_POINT('Ctrl Pts',(-1.47850492545557,5.73143281167847,40.1944428462465));
#20815=CARTESIAN_POINT('Ctrl Pts',(-1.63747702733532,5.6856485599665,40.2022294285796));
#20816=CARTESIAN_POINT('Ctrl Pts',(-1.79645519078654,5.63986256251102,40.2100163078133));
#20817=CARTESIAN_POINT('Ctrl Pts',(-1.9535209818679,5.58740188889311,40.2178031870471));
#20818=CARTESIAN_POINT('Ctrl Pts',(-2.10811255556077,5.52845294956799,40.2255900662808));
#20819=CARTESIAN_POINT('Ctrl Pts',(-2.26269392629927,5.46950790083875,40.2333764315851));
#20820=CARTESIAN_POINT('Ctrl Pts',(-2.41480110789138,5.40407555730555,40.2411627968893));
#20821=CARTESIAN_POINT('Ctrl Pts',(-2.56389095061131,5.33239099803019,40.2489491621936));
#20822=CARTESIAN_POINT('Ctrl Pts',(-2.71301994129586,5.26068761584551,40.2567375720392));
#20823=CARTESIAN_POINT('Ctrl Pts',(-2.85912972094247,5.18272887425217,40.2645259818848));
#20824=CARTESIAN_POINT('Ctrl Pts',(-3.0016997042382,5.09879686279776,40.2723143917305));
#20825=CARTESIAN_POINT('Ctrl Pts',(-3.13677735564056,5.01927564295431,40.2796935053825));
#20826=CARTESIAN_POINT('Ctrl Pts',(-3.26867746380742,4.93439295157321,40.2870726190345));
#20827=CARTESIAN_POINT('Ctrl Pts',(-3.39697973626252,4.84442558348478,40.2944517326865));
#20828=CARTESIAN_POINT('Ctrl Pts',(-3.53239334241727,4.74947164762701,40.3022398440794));
#20829=CARTESIAN_POINT('Ctrl Pts',(-3.6638473360425,4.64881948854476,40.3100279554724));
#20830=CARTESIAN_POINT('Ctrl Pts',(-3.79086821997638,4.54282386861665,40.3178160668653));
#20831=CARTESIAN_POINT('Ctrl Pts',(-3.91786416557537,4.43684905907959,40.3256026491984));
#20832=CARTESIAN_POINT('Ctrl Pts',(-4.04042849293809,4.32553308654958,40.3333892315315));
#20833=CARTESIAN_POINT('Ctrl Pts',(-4.15812072383325,4.20927103053824,40.3411758138646));
#20834=CARTESIAN_POINT('Ctrl Pts',(-4.27581744230611,4.09300454148144,40.3489626930983));
#20835=CARTESIAN_POINT('Ctrl Pts',(-4.38864146249824,3.97179181330609,40.356749572332));
#20836=CARTESIAN_POINT('Ctrl Pts',(-4.49618860080912,3.84606534375772,40.3645364515657));
#20837=CARTESIAN_POINT('Ctrl Pts',(-4.60372864107145,3.72034717208317,40.3723228168699));
#20838=CARTESIAN_POINT('Ctrl Pts',(-4.70599228876691,3.59011609809584,40.3801091821741));
#20839=CARTESIAN_POINT('Ctrl Pts',(-4.80261506183598,3.45583841206822,40.3878955474783));
#20840=CARTESIAN_POINT('Ctrl Pts',(-4.89926320608298,3.32152546744725,40.3956839573239));
#20841=CARTESIAN_POINT('Ctrl Pts',(-4.99026732767116,3.18316404597082,40.4034723671695));
#20842=CARTESIAN_POINT('Ctrl Pts',(-5.07530525034122,3.04125092328122,40.4112607770151));
#20843=CARTESIAN_POINT('Ctrl Pts',(-5.15587426360153,2.90679561317031,40.4186398906673));
#20844=CARTESIAN_POINT('Ctrl Pts',(-5.23108788656526,2.76915252125431,40.4260190043195));
#20845=CARTESIAN_POINT('Ctrl Pts',(-5.30070947922281,2.62876579013374,40.4333981179716));
#20846=CARTESIAN_POINT('Ctrl Pts',(-5.37397943633849,2.48102240512659,40.4411639176353));
#20847=CARTESIAN_POINT('Ctrl Pts',(-5.44108311045085,2.3301844437189,40.448929717299));
#20848=CARTESIAN_POINT('Ctrl Pts',(-5.50177518626529,2.1767867057421,40.4566955169627));
#20849=CARTESIAN_POINT('Ctrl Pts',(-5.562454740084,2.0234206168034,40.4644597143858));
#20850=CARTESIAN_POINT('Ctrl Pts',(-5.61672521602865,1.86749610535429,40.4722239118089));
#20851=CARTESIAN_POINT('Ctrl Pts',(-5.66438955980109,1.7095676287636,40.4799881092319));
#20852=CARTESIAN_POINT('Ctrl Pts',(-5.712054462803,1.55163729925204,40.4877523977497));
#20853=CARTESIAN_POINT('Ctrl Pts',(-5.75311298151021,1.39170326583823,40.4955166862674));
#20854=CARTESIAN_POINT('Ctrl Pts',(-5.78741783925445,1.23033544872096,40.5032809747851));
#20855=CARTESIAN_POINT('Ctrl Pts',(-5.82172103481773,1.06897545039469,40.5110448870981));
#20856=CARTESIAN_POINT('Ctrl Pts',(-5.8492711578878,0.90618212369588,40.518808799411));
#20857=CARTESIAN_POINT('Ctrl Pts',(-5.86997195585913,0.742536059681504,
40.5265727117239));
#20858=CARTESIAN_POINT('Ctrl Pts',(-5.89067724266346,0.578854510085715,
40.5343383075906));
#20859=CARTESIAN_POINT('Ctrl Pts',(-5.904530196549,0.414320174490498,40.5421039034572));
#20860=CARTESIAN_POINT('Ctrl Pts',(-5.9114863050132,0.249519995474125,40.5498694993239));
#20861=CARTESIAN_POINT('Ctrl Pts',(-5.91499628252033,0.166363597827879,
40.553787935467));
#20862=CARTESIAN_POINT('Ctrl Pts',(-5.91675107512313,0.0831395781098299,
40.5577063716101));
#20863=CARTESIAN_POINT('Ctrl Pts',(-5.91674999950574,-7.64775397288306E-5,
40.5616248077532));
#20864=CARTESIAN_POINT('Origin',(0.,0.,0.));
#20865=CARTESIAN_POINT('',(-5.91650634169521,0.000138707710825164,42.5633751922049));
#20866=CARTESIAN_POINT('',(-5.91670122177708,-1.61732529071579E-5,42.3116248079793));
#20867=CARTESIAN_POINT('',(-5.91675,-7.2459289488551E-16,0.));
#20868=CARTESIAN_POINT('Ctrl Pts',(-5.91650634169521,0.000138707710825164,
42.5633751922049));
#20869=CARTESIAN_POINT('Ctrl Pts',(-5.91677370638019,0.309337923053453,
42.5488215831681));
#20870=CARTESIAN_POINT('Ctrl Pts',(-5.81712789539372,1.60288454477205,42.4879279756271));
#20871=CARTESIAN_POINT('Ctrl Pts',(-4.88823415802477,3.76173700716183,42.380694369582));
#20872=CARTESIAN_POINT('Ctrl Pts',(-2.49123115743396,5.64262933524277,42.2416743740696));
#20873=CARTESIAN_POINT('Ctrl Pts',(0.513650429588109,6.14667891880822,42.102654378557));
#20874=CARTESIAN_POINT('Ctrl Pts',(3.39319756254412,5.1508939802966,41.9636343830446));
#20875=CARTESIAN_POINT('Ctrl Pts',(5.44477972259265,2.89825331314937,41.8246143875318));
#20876=CARTESIAN_POINT('Ctrl Pts',(6.16779588774671,-0.0615823173574553,
41.6855943920195));
#20877=CARTESIAN_POINT('Ctrl Pts',(5.38582483627265,-3.00639141292502,41.546574396507));
#20878=CARTESIAN_POINT('Ctrl Pts',(3.28967321249204,-5.21761905947031,41.4075544009944));
#20879=CARTESIAN_POINT('Ctrl Pts',(0.39081731286073,-6.15570957101441,41.268534405482));
#20880=CARTESIAN_POINT('Ctrl Pts',(-2.60340086377102,-5.59176201543438,
41.1295144099693));
#20881=CARTESIAN_POINT('Ctrl Pts',(-4.96237022687324,-3.6633837126559,40.9904944144569));
#20882=CARTESIAN_POINT('Ctrl Pts',(-5.83266256480556,-1.52405015064227,
40.8851146769589));
#20883=CARTESIAN_POINT('Ctrl Pts',(-5.91687951771807,-0.269949220235747,
40.8260749379652));
#20884=CARTESIAN_POINT('Ctrl Pts',(-5.91661801913444,-0.000151051921165636,
40.8133751974756));
#20885=CARTESIAN_POINT('Ctrl Pts',(-5.91674999950573,-7.64784292123484E-5,
40.5616248077951));
#20886=CARTESIAN_POINT('Ctrl Pts',(-5.9167490186361,-0.075961409857763,
40.5651980396157));
#20887=CARTESIAN_POINT('Ctrl Pts',(-5.91528801894685,-0.151842421823986,
40.5687712714362));
#20888=CARTESIAN_POINT('Ctrl Pts',(-5.91236824443533,-0.227667091808765,
40.5723445032567));
#20889=CARTESIAN_POINT('Ctrl Pts',(-5.90600438944925,-0.39293232110902,
40.5801326146495));
#20890=CARTESIAN_POINT('Ctrl Pts',(-5.89270570371615,-0.557960059762128,
40.5879207260422));
#20891=CARTESIAN_POINT('Ctrl Pts',(-5.87251354639665,-0.722160099900164,
40.595708837435));
#20892=CARTESIAN_POINT('Ctrl Pts',(-5.85232535345526,-0.886327902222636,
40.6034954197679));
#20893=CARTESIAN_POINT('Ctrl Pts',(-5.82524642836426,-1.0496680133305,40.6112820021008));
#20894=CARTESIAN_POINT('Ctrl Pts',(-5.79136990959353,-1.21159610958217,
40.6190685844337));
#20895=CARTESIAN_POINT('Ctrl Pts',(-5.75749209911871,-1.37353038011595,
40.6268554636673));
#20896=CARTESIAN_POINT('Ctrl Pts',(-5.7168162378872,-1.53405221450648,40.6346423429009));
#20897=CARTESIAN_POINT('Ctrl Pts',(-5.6694865839613,-1.69258749752646,40.6424292221345));
#20898=CARTESIAN_POINT('Ctrl Pts',(-5.62216005376524,-1.85111231730925,
40.6502155874385));
#20899=CARTESIAN_POINT('Ctrl Pts',(-5.56818070120106,-2.00765054192988,
40.6580019527426));
#20900=CARTESIAN_POINT('Ctrl Pts',(-5.50774270464845,-2.16164309308725,
40.6657883180467));
#20901=CARTESIAN_POINT('Ctrl Pts',(-5.44728883830516,-2.31567607956168,
40.6735767278921));
#20902=CARTESIAN_POINT('Ctrl Pts',(-5.38037305420142,-2.46716175854072,
40.6813651377377));
#20903=CARTESIAN_POINT('Ctrl Pts',(-5.30723808422377,-2.61556007001651,
40.6891535475831));
#20904=CARTESIAN_POINT('Ctrl Pts',(-5.23794650016763,-2.75615975955705,
40.6965326612361));
#20905=CARTESIAN_POINT('Ctrl Pts',(-5.16307269353119,-2.89398799656402,
40.7039117748891));
#20906=CARTESIAN_POINT('Ctrl Pts',(-5.08286154899847,-3.02860513045409,
40.7112908885421));
#20907=CARTESIAN_POINT('Ctrl Pts',(-4.99820458910354,-3.17068360809325,
40.719078999935));
#20908=CARTESIAN_POINT('Ctrl Pts',(-4.90757161993195,-3.30923567219652,
40.726867111328));
#20909=CARTESIAN_POINT('Ctrl Pts',(-4.81128133616373,-3.44376283544361,
40.7346552227209));
#20910=CARTESIAN_POINT('Ctrl Pts',(-4.7150099573142,-3.57826358662725,40.742441805054));
#20911=CARTESIAN_POINT('Ctrl Pts',(-4.61308366593718,-3.70874075400858,
40.750228387387));
#20912=CARTESIAN_POINT('Ctrl Pts',(-4.50586381008473,-3.83472579038824,
40.7580149697201));
#20913=CARTESIAN_POINT('Ctrl Pts',(-4.39863986596291,-3.96071563054944,
40.7658018489537));
#20914=CARTESIAN_POINT('Ctrl Pts',(-4.28612215755448,-4.08221275108543,
40.7735887281874));
#20915=CARTESIAN_POINT('Ctrl Pts',(-4.16871203812706,-4.19878202645416,
40.7813756074211));
#20916=CARTESIAN_POINT('Ctrl Pts',(-4.05130966769977,-4.31534360831799,
40.7891619727252));
#20917=CARTESIAN_POINT('Ctrl Pts',(-3.92901575927058,-4.42697777079846,
40.7969483380294));
#20918=CARTESIAN_POINT('Ctrl Pts',(-3.80226830808157,-4.53328647626184,
40.8047347033335));
#20919=CARTESIAN_POINT('Ctrl Pts',(-3.67548757558562,-4.63962309623258,
40.8125231131791));
#20920=CARTESIAN_POINT('Ctrl Pts',(-3.54425120733451,-4.74063125801737,
40.8203115230246));
#20921=CARTESIAN_POINT('Ctrl Pts',(-3.40903073549084,-4.83595285408975,
40.8280999328702));
#20922=CARTESIAN_POINT('Ctrl Pts',(-3.28091636431262,-4.92626511357244,
40.8354790465224));
#20923=CARTESIAN_POINT('Ctrl Pts',(-3.14922607668857,-5.01147296519138,
40.8428581601746));
#20924=CARTESIAN_POINT('Ctrl Pts',(-3.01438525579226,-5.09130750320212,
40.8502372738269));
#20925=CARTESIAN_POINT('Ctrl Pts',(-2.87207069296472,-5.1755669826388,40.8580253852199));
#20926=CARTESIAN_POINT('Ctrl Pts',(-2.72619562056994,-5.25387070427942,
40.865813496613));
#20927=CARTESIAN_POINT('Ctrl Pts',(-2.57727838559369,-5.3259334098026,40.8736016080061));
#20928=CARTESIAN_POINT('Ctrl Pts',(-2.42839038792047,-5.39798196706982,
40.8813881903392));
#20929=CARTESIAN_POINT('Ctrl Pts',(-2.27646170685251,-5.46379181398922,
40.8891747726724));
#20930=CARTESIAN_POINT('Ctrl Pts',(-2.12203381986554,-5.52312439022035,
40.8969613550056));
#20931=CARTESIAN_POINT('Ctrl Pts',(-1.96760004457754,-5.58245922878942,
40.9047482342394));
#20932=CARTESIAN_POINT('Ctrl Pts',(-1.81066716953002,-5.63531618418975,
40.9125351134732));
#20933=CARTESIAN_POINT('Ctrl Pts',(-1.65179581159229,-5.6815051843069,40.9203219927071));
#20934=CARTESIAN_POINT('Ctrl Pts',(-1.49293493907222,-5.72769113597678,
40.9281083580114));
#20935=CARTESIAN_POINT('Ctrl Pts',(-1.33213614656812,-5.76720992393617,
40.9358947233157));
#20936=CARTESIAN_POINT('Ctrl Pts',(-1.16997448294024,-5.79992157462226,
40.94368108862));
#20937=CARTESIAN_POINT('Ctrl Pts',(-1.00777023895262,-5.83264181472352,
40.9514694984657));
#20938=CARTESIAN_POINT('Ctrl Pts',(-0.844202721799262,-5.85855128079383,
40.9592579083114));
#20939=CARTESIAN_POINT('Ctrl Pts',(-0.679857325904446,-5.87756110805443,
40.9670463181571));
#20940=CARTESIAN_POINT('Ctrl Pts',(-0.524148602498533,-5.89557193165432,
40.9744254318088));
#20941=CARTESIAN_POINT('Ctrl Pts',(-0.36774191395847,-5.90738961366641,
40.9818045454605));
#20942=CARTESIAN_POINT('Ctrl Pts',(-0.211139452949608,-5.91298154012915,
40.9891836591122));
#20943=CARTESIAN_POINT('Ctrl Pts',(-0.0458570805245572,-5.91888340697234,
40.9969717705051));
#20944=CARTESIAN_POINT('Ctrl Pts',(0.11970241207362,-5.91785191361215,41.0047598818981));
#20945=CARTESIAN_POINT('Ctrl Pts',(0.284947374884473,-5.90988456368197,
41.012547993291));
#20946=CARTESIAN_POINT('Ctrl Pts',(0.450159894727242,-5.90191877800207,
41.020334575624));
#20947=CARTESIAN_POINT('Ctrl Pts',(0.615057689036556,-5.88701986819625,
41.028121157957));
#20948=CARTESIAN_POINT('Ctrl Pts',(0.779051138401559,-5.86523741090292,
41.03590774029));
#20949=CARTESIAN_POINT('Ctrl Pts',(0.943050840800521,-5.84345412304932,
41.0436946195237));
#20950=CARTESIAN_POINT('Ctrl Pts',(1.10614581200184,-5.81478680066557,41.0514814987574));
#20951=CARTESIAN_POINT('Ctrl Pts',(1.26775282433349,-5.77933675596902,41.0592683779911));
#20952=CARTESIAN_POINT('Ctrl Pts',(1.42934917069571,-5.74388905095493,41.0670547432952));
#20953=CARTESIAN_POINT('Ctrl Pts',(1.58945744260377,-5.70165958804027,41.0748411085993));
#20954=CARTESIAN_POINT('Ctrl Pts',(1.74750570823874,-5.65280057689753,41.0826274739035));
#20955=CARTESIAN_POINT('Ctrl Pts',(1.90559547413876,-5.60392873637065,41.090415883749));
#20956=CARTESIAN_POINT('Ctrl Pts',(2.06162384685479,-5.54842396174471,41.0982042935946));
#20957=CARTESIAN_POINT('Ctrl Pts',(2.21503426213652,-5.48648829216479,41.1059927034401));
#20958=CARTESIAN_POINT('Ctrl Pts',(2.36038265959799,-5.42780746333963,41.1133718170925));
#20959=CARTESIAN_POINT('Ctrl Pts',(2.50338093884655,-5.3633543643843,41.1207509307449));
#20960=CARTESIAN_POINT('Ctrl Pts',(2.64357250937003,-5.29334062291508,41.1281300443973));
#20961=CARTESIAN_POINT('Ctrl Pts',(2.79153439463449,-5.21944627146783,41.1359181557902));
#20962=CARTESIAN_POINT('Ctrl Pts',(2.9364224614312,-5.13933099409852,41.1437062671832));
#20963=CARTESIAN_POINT('Ctrl Pts',(3.07771597407476,-5.0532756648955,41.1514943785761));
#20964=CARTESIAN_POINT('Ctrl Pts',(3.21898174620004,-4.96723723115631,41.1592809609092));
#20965=CARTESIAN_POINT('Ctrl Pts',(3.35665409958061,-4.87526123865677,41.1670675432422));
#20966=CARTESIAN_POINT('Ctrl Pts',(3.49023899516495,-4.77767331649307,41.1748541255752));
#20967=CARTESIAN_POINT('Ctrl Pts',(3.62382898431173,-4.68008167332355,41.1826410048089));
#20968=CARTESIAN_POINT('Ctrl Pts',(3.75333094346604,-4.57687785760383,41.1904278840426));
#20969=CARTESIAN_POINT('Ctrl Pts',(3.87828119843344,-4.46842987058964,41.1982147632763));
#20970=CARTESIAN_POINT('Ctrl Pts',(4.00322320675625,-4.35998904107989,41.2060011285804));
#20971=CARTESIAN_POINT('Ctrl Pts',(4.1236138708036,-4.24630494244777,41.2137874938846));
#20972=CARTESIAN_POINT('Ctrl Pts',(4.23902378666487,-4.12778486583172,41.2215738591887));
#20973=CARTESIAN_POINT('Ctrl Pts',(4.35446400682645,-4.00923366825032,41.2293622690343));
#20974=CARTESIAN_POINT('Ctrl Pts',(4.46492064100376,-3.88584418302148,41.2371506788799));
#20975=CARTESIAN_POINT('Ctrl Pts',(4.57000162007585,-3.75806010529423,41.2449390887255));
#20976=CARTESIAN_POINT('Ctrl Pts',(4.66956038786608,-3.63699133115378,41.2523182023778));
#20977=CARTESIAN_POINT('Ctrl Pts',(4.76429380562663,-3.51197817427837,41.2596973160301));
#20978=CARTESIAN_POINT('Ctrl Pts',(4.85390218092079,-3.38342491871068,41.2670764296824));
#20979=CARTESIAN_POINT('Ctrl Pts',(4.94847722630117,-3.24774641835624,41.2748645410754));
#20980=CARTESIAN_POINT('Ctrl Pts',(5.03737677118627,-3.10807580409691,41.2826526524684));
#20981=CARTESIAN_POINT('Ctrl Pts',(5.12027792575269,-2.96490885619604,41.2904407638614));
#20982=CARTESIAN_POINT('Ctrl Pts',(5.20316280412257,-2.82177001662966,41.2982273461944));
#20983=CARTESIAN_POINT('Ctrl Pts',(5.28005148197605,-2.67513648942692,41.3060139285275));
#20984=CARTESIAN_POINT('Ctrl Pts',(5.35066592478731,-2.52553058263406,41.3138005108606));
#20985=CARTESIAN_POINT('Ctrl Pts',(5.42128306011157,-2.37591897140127,41.3215873900943));
#20986=CARTESIAN_POINT('Ctrl Pts',(5.48562534172978,-2.22333504105345,41.3293742693281));
#20987=CARTESIAN_POINT('Ctrl Pts',(5.54346167152561,-2.06832377997896,41.3371611485618));
#20988=CARTESIAN_POINT('Ctrl Pts',(5.60129418415714,-1.91332274955802,41.344947513866));
#20989=CARTESIAN_POINT('Ctrl Pts',(5.65262149264367,-1.75589500843399,41.3527338791702));
#20990=CARTESIAN_POINT('Ctrl Pts',(5.69726139005274,-1.5966036502258,41.3605202444744));
#20991=CARTESIAN_POINT('Ctrl Pts',(5.74191300899237,-1.43727046534168,41.36830865432));
#20992=CARTESIAN_POINT('Ctrl Pts',(5.77987361989471,-1.27607299290788,41.3760970641656));
#20993=CARTESIAN_POINT('Ctrl Pts',(5.81101121732072,-1.11358843145604,41.3838854740112));
#20994=CARTESIAN_POINT('Ctrl Pts',(5.84051247300888,-0.959642751987385,
41.3912645876633));
#20995=CARTESIAN_POINT('Ctrl Pts',(5.86388934689645,-0.804542037616839,
41.3986437013154));
#20996=CARTESIAN_POINT('Ctrl Pts',(5.88107209595643,-0.648784682820597,
41.4060228149675));
#20997=CARTESIAN_POINT('Ctrl Pts',(5.89920722302258,-0.484394257816035,
41.4138109263604));
#20998=CARTESIAN_POINT('Ctrl Pts',(5.91044859548314,-0.319213626041863,
41.4215990377534));
#20999=CARTESIAN_POINT('Ctrl Pts',(5.91474987517481,-0.153832625342049,
41.4293871491464));
#21000=CARTESIAN_POINT('Ctrl Pts',(5.91905031038518,0.0115159056812921,
41.4371737314794));
#21001=CARTESIAN_POINT('Ctrl Pts',(5.91641336324894,0.177064407914185,41.4449603138124));
#21002=CARTESIAN_POINT('Ctrl Pts',(5.90684477589026,0.342221209217062,41.4527468961455));
#21003=CARTESIAN_POINT('Ctrl Pts',(5.89727582368347,0.507384307912026,41.4605337753792));
#21004=CARTESIAN_POINT('Ctrl Pts',(5.88077471692483,0.672155356581829,41.4683206546129));
#21005=CARTESIAN_POINT('Ctrl Pts',(5.85739926474652,0.835945222994252,41.4761075338466));
#21006=CARTESIAN_POINT('Ctrl Pts',(5.83402535533454,0.999724279370245,41.4838938991507));
#21007=CARTESIAN_POINT('Ctrl Pts',(5.80377805369661,1.16252196674723,41.4916802644549));
#21008=CARTESIAN_POINT('Ctrl Pts',(5.76676676361029,1.32375664554318,41.4994666297591));
#21009=CARTESIAN_POINT('Ctrl Pts',(5.72974575511078,1.48503366129158,41.5072550396047));
#21010=CARTESIAN_POINT('Ctrl Pts',(5.68595727881599,1.64474653629759,41.5150434494503));
#21011=CARTESIAN_POINT('Ctrl Pts',(5.63556156986838,1.80232526329813,41.5228318592959));
#21012=CARTESIAN_POINT('Ctrl Pts',(5.58781425414112,1.95162291952944,41.5302109729481));
#21013=CARTESIAN_POINT('Ctrl Pts',(5.53413636952841,2.09900471805148,41.5375900866004));
#21014=CARTESIAN_POINT('Ctrl Pts',(5.4747051225789,2.24399963977456,41.5449692002526));
#21015=CARTESIAN_POINT('Ctrl Pts',(5.41197981527528,2.39703110873013,41.5527573116456));
#21016=CARTESIAN_POINT('Ctrl Pts',(5.34282288190796,2.54745826098493,41.5605454230386));
#21017=CARTESIAN_POINT('Ctrl Pts',(5.26747583110242,2.69474097665283,41.5683335344316));
#21018=CARTESIAN_POINT('Ctrl Pts',(5.19214357337682,2.84199477592703,41.5761201167646));
#21019=CARTESIAN_POINT('Ctrl Pts',(5.11062376857809,2.98610508613235,41.5839066990977));
#21020=CARTESIAN_POINT('Ctrl Pts',(5.02320453581267,3.12655509369194,41.5916932814308));
#21021=CARTESIAN_POINT('Ctrl Pts',(4.93578196977136,3.26701045657907,41.5994801606645));
#21022=CARTESIAN_POINT('Ctrl Pts',(4.8424596911384,3.40380496419873,41.6072670398982));
#21023=CARTESIAN_POINT('Ctrl Pts',(4.74357032506724,3.53644894401736,41.615053919132));
#21024=CARTESIAN_POINT('Ctrl Pts',(4.64468748563703,3.66908416941007,41.6228402844362));
#21025=CARTESIAN_POINT('Ctrl Pts',(4.54023848513357,3.79756915906116,41.6306266497403));
#21026=CARTESIAN_POINT('Ctrl Pts',(4.43059767039804,3.92144550460203,41.6384130150445));
#21027=CARTESIAN_POINT('Ctrl Pts',(4.32092806621105,4.04535437755567,41.6462014248902));
#21028=CARTESIAN_POINT('Ctrl Pts',(4.20606413416399,4.16465194758013,41.6539898347358));
#21029=CARTESIAN_POINT('Ctrl Pts',(4.0864192919683,4.27891434042904,41.6617782445814));
#21030=CARTESIAN_POINT('Ctrl Pts',(3.9730620205924,4.38717202071458,41.6691573582335));
#21031=CARTESIAN_POINT('Ctrl Pts',(3.85541359519258,4.49090994932463,41.6765364718857));
#21032=CARTESIAN_POINT('Ctrl Pts',(3.73385497702661,4.58979929550668,41.6839155855378));
#21033=CARTESIAN_POINT('Ctrl Pts',(3.6055588016756,4.69416972262684,41.6917036969308));
#21034=CARTESIAN_POINT('Ctrl Pts',(3.47286086561413,4.79317612309264,41.6994918083237));
#21035=CARTESIAN_POINT('Ctrl Pts',(3.3362316554792,4.88645975154595,41.7072799197167));
#21036=CARTESIAN_POINT('Ctrl Pts',(3.19962927010773,4.97972506538509,41.7150665020498));
#21037=CARTESIAN_POINT('Ctrl Pts',(3.05909741443301,5.06726966900224,41.7228530843828));
#21038=CARTESIAN_POINT('Ctrl Pts',(2.9151363542591,5.14877758293918,41.7306396667159));
#21039=CARTESIAN_POINT('Ctrl Pts',(2.77116980488214,5.23028860475466,41.7384265459496));
#21040=CARTESIAN_POINT('Ctrl Pts',(2.62377406546405,5.30576231544556,41.7462134251833));
#21041=CARTESIAN_POINT('Ctrl Pts',(2.47347549835246,5.37492786198569,41.754000304417));
#21042=CARTESIAN_POINT('Ctrl Pts',(2.3231868508594,5.44408884363974,41.7617866697211));
#21043=CARTESIAN_POINT('Ctrl Pts',(2.16999604940352,5.50694236081271,41.7695730350253));
#21044=CARTESIAN_POINT('Ctrl Pts',(2.01445113521985,5.56326497538195,41.7773594003295));
#21045=CARTESIAN_POINT('Ctrl Pts',(1.85886537810032,5.61960237912604,41.7851478101751));
#21046=CARTESIAN_POINT('Ctrl Pts',(1.7009245730516,5.6694053428885,41.7929362200207));
#21047=CARTESIAN_POINT('Ctrl Pts',(1.54119454798986,5.71249944662985,41.8007246298663));
#21048=CARTESIAN_POINT('Ctrl Pts',(1.38985864862549,5.75332887080653,41.8081037435185));
#21049=CARTESIAN_POINT('Ctrl Pts',(1.23691699754553,5.78813635845961,41.8154828571707));
#21050=CARTESIAN_POINT('Ctrl Pts',(1.08286144975423,5.81681542109909,41.8228619708229));
#21051=CARTESIAN_POINT('Ctrl Pts',(0.92026715680235,5.84708406107501,41.8306500822158));
#21052=CARTESIAN_POINT('Ctrl Pts',(0.756373916800877,5.87053646925751,41.8384381936087));
#21053=CARTESIAN_POINT('Ctrl Pts',(0.591766511235335,5.88708272055696,41.8462263050016));
#21054=CARTESIAN_POINT('Ctrl Pts',(0.427191423464346,5.90362572328842,41.8540128873346));
#21055=CARTESIAN_POINT('Ctrl Pts',(0.261902767627809,5.91326524262942,41.8617994696676));
#21056=CARTESIAN_POINT('Ctrl Pts',(0.096491014262999,5.91596315460691,41.8695860520006));
#21057=CARTESIAN_POINT('Ctrl Pts',(-0.068927046215219,5.91866116945518,
41.8773729312342));
#21058=CARTESIAN_POINT('Ctrl Pts',(-0.234467894204855,5.91441703815268,
41.8851598104678));
#21059=CARTESIAN_POINT('Ctrl Pts',(-0.39953973327443,5.90324474878308,41.8929466897015));
#21060=CARTESIAN_POINT('Ctrl Pts',(-0.564600677698008,5.89207319677812,
41.9007330550056));
#21061=CARTESIAN_POINT('Ctrl Pts',(-0.729192356329885,5.87397442343852,
41.9085194203097));
#21062=CARTESIAN_POINT('Ctrl Pts',(-0.892726620974606,5.84901442490128,
41.9163057856139));
#21063=CARTESIAN_POINT('Ctrl Pts',(-1.05630382639649,5.82404787237526,41.9240941954594));
#21064=CARTESIAN_POINT('Ctrl Pts',(-1.21882274664656,5.79221654096599,41.9318826053049));
#21065=CARTESIAN_POINT('Ctrl Pts',(-1.37970306661821,5.75363798048368,41.9396710151504));
#21066=CARTESIAN_POINT('Ctrl Pts',(-1.5321288106491,5.71708679892093,41.9470501288029));
#21067=CARTESIAN_POINT('Ctrl Pts',(-1.68308349512621,5.67447936919105,41.9544292424555));
#21068=CARTESIAN_POINT('Ctrl Pts',(-1.83208426309407,5.62595750209891,41.961808356108));
#21069=CARTESIAN_POINT('Ctrl Pts',(-1.98934360794733,5.57474624235821,41.9695964675011));
#21070=CARTESIAN_POINT('Ctrl Pts',(-2.14448246219937,5.51692803181443,41.9773845788942));
#21071=CARTESIAN_POINT('Ctrl Pts',(-2.29694429254527,5.45270368527795,41.9851726902873));
#21072=CARTESIAN_POINT('Ctrl Pts',(-2.44937618966847,5.38849194807236,41.9929592726205));
#21073=CARTESIAN_POINT('Ctrl Pts',(-2.59913181730158,5.31787670839332,42.0007458549537));
#21074=CARTESIAN_POINT('Ctrl Pts',(-2.7456744299343,5.24110699063709,42.0085324372868));
#21075=CARTESIAN_POINT('Ctrl Pts',(-2.89222263020433,5.16433434566855,42.0163193165207));
#21076=CARTESIAN_POINT('Ctrl Pts',(-3.03555728546627,5.08140689782442,42.0241061957545));
#21077=CARTESIAN_POINT('Ctrl Pts',(-3.17516541815747,4.99262006664206,42.0318930749884));
#21078=CARTESIAN_POINT('Ctrl Pts',(-3.31476433679263,4.90383909533922,42.0396794402927));
#21079=CARTESIAN_POINT('Ctrl Pts',(-3.45063695545803,4.80919968616075,42.047465805597));
#21080=CARTESIAN_POINT('Ctrl Pts',(-3.58229838267708,4.70904118265802,42.0552521709013));
#21081=CARTESIAN_POINT('Ctrl Pts',(-3.71399438151316,4.60885637956626,42.063040580747));
#21082=CARTESIAN_POINT('Ctrl Pts',(-3.84147672368727,4.50314977838328,42.0708289905928));
#21083=CARTESIAN_POINT('Ctrl Pts',(-3.96429206123212,4.39230224549176,42.0786174004385));
#21084=CARTESIAN_POINT('Ctrl Pts',(-4.08065321220568,4.28727996759325,42.0859965140901));
#21085=CARTESIAN_POINT('Ctrl Pts',(-4.19282506951788,4.17764336670298,42.0933756277416));
#21086=CARTESIAN_POINT('Ctrl Pts',(-4.30045147274419,4.06374798592042,42.1007547413932));
#21087=CARTESIAN_POINT('Ctrl Pts',(-4.41404322057784,3.94353979364195,42.1085428527862));
#21088=CARTESIAN_POINT('Ctrl Pts',(-4.52261191896151,3.8185444045299,42.1163309641791));
#21089=CARTESIAN_POINT('Ctrl Pts',(-4.6257649401832,3.68920442381171,42.124119075572));
#21090=CARTESIAN_POINT('Ctrl Pts',(-4.7288977091075,3.55988983674388,42.1319056579051));
#21091=CARTESIAN_POINT('Ctrl Pts',(-4.82661672330823,3.42623260968398,42.1396922402381));
#21092=CARTESIAN_POINT('Ctrl Pts',(-4.91856979635348,3.28870821461851,42.1474788225711));
#21093=CARTESIAN_POINT('Ctrl Pts',(-5.01052637554886,3.15117857577859,42.1552657018048));
#21094=CARTESIAN_POINT('Ctrl Pts',(-5.09671639278192,3.00978173729458,42.1630525810385));
#21095=CARTESIAN_POINT('Ctrl Pts',(-5.17683072986968,2.86502254036107,42.1708394602721));
#21096=CARTESIAN_POINT('Ctrl Pts',(-5.25693977945754,2.72027289745082,42.1786258255763));
#21097=CARTESIAN_POINT('Ctrl Pts',(-5.33097379671375,2.57216161982321,42.1864121908804));
#21098=CARTESIAN_POINT('Ctrl Pts',(-5.39866934128585,2.42121868197818,42.1941985561846));
#21099=CARTESIAN_POINT('Ctrl Pts',(-5.46638266133319,2.27023610958305,42.2019869660302));
#21100=CARTESIAN_POINT('Ctrl Pts',(-5.52775405035683,2.11642068217709,42.2097753758757));
#21101=CARTESIAN_POINT('Ctrl Pts',(-5.58256763306664,1.96032374487907,42.2175637857213));
#21102=CARTESIAN_POINT('Ctrl Pts',(-5.63450065463665,1.81243000739747,42.2249428993736));
#21103=CARTESIAN_POINT('Ctrl Pts',(-5.68054730697709,1.66248863338524,42.2323220130259));
#21104=CARTESIAN_POINT('Ctrl Pts',(-5.72056494184579,1.51098223306064,42.2397011266782));
#21105=CARTESIAN_POINT('Ctrl Pts',(-5.76325408235672,1.34936153676051,42.2475728567438));
#21106=CARTESIAN_POINT('Ctrl Pts',(-5.79909574989067,1.18590779273446,42.2554445868094));
#21107=CARTESIAN_POINT('Ctrl Pts',(-5.82795511545164,1.02120993668349,42.263316316875));
#21108=CARTESIAN_POINT('Ctrl Pts',(-5.85747324313865,0.85275258323201,42.2713677320283));
#21109=CARTESIAN_POINT('Ctrl Pts',(-5.87968639419594,0.68299395580701,42.2794191471817));
#21110=CARTESIAN_POINT('Ctrl Pts',(-5.89450570957145,0.512574874852035,
42.287470562335));
#21111=CARTESIAN_POINT('Ctrl Pts',(-5.90932502494696,0.342155793897115,
42.2955219774884));
#21112=CARTESIAN_POINT('Ctrl Pts',(-5.91675046754537,0.171076599197924,
42.3035733926417));
#21113=CARTESIAN_POINT('Ctrl Pts',(-5.91674999997791,-1.61694723147206E-5,
42.3116248077951));
#21114=CARTESIAN_POINT('Origin',(0.,0.,0.));
#21115=CARTESIAN_POINT('',(-5.917134484543,-9.42401903047951E-5,44.3133751922049));
#21116=CARTESIAN_POINT('',(-5.91674999906443,0.000105219438300132,44.0616248077951));
#21117=CARTESIAN_POINT('',(-5.91675,-7.2459289488551E-16,0.));
#21118=CARTESIAN_POINT('Ctrl Pts',(-5.917134484543,-9.42401903047951E-5,
44.3133751922049));
#21119=CARTESIAN_POINT('Ctrl Pts',(-5.91646026956298,0.887845364419518,
44.2715682318849));
#21120=CARTESIAN_POINT('Ctrl Pts',(-5.48922520664388,2.76062880404801,44.1834212730605));
#21121=CARTESIAN_POINT('Ctrl Pts',(-3.59065886915233,5.01524350157563,44.0489343157323));
#21122=CARTESIAN_POINT('Ctrl Pts',(-0.75195218801304,6.12209656912254,43.9099143202198));
#21123=CARTESIAN_POINT('Ctrl Pts',(2.2702363156626,5.73511338735183,43.7708943247072));
#21124=CARTESIAN_POINT('Ctrl Pts',(4.73847058738315,3.94872067728464,43.6318743291948));
#21125=CARTESIAN_POINT('Ctrl Pts',(6.0504834487093,1.19881129942669,43.492854333682));
#21126=CARTESIAN_POINT('Ctrl Pts',(5.8861341848116,-1.84361678585946,43.3538343381697));
#21127=CARTESIAN_POINT('Ctrl Pts',(4.28552521570779,-4.43618891846033,43.214814342657));
#21128=CARTESIAN_POINT('Ctrl Pts',(1.63921681303447,-5.94629857428774,43.0757943471447));
#21129=CARTESIAN_POINT('Ctrl Pts',(-1.40707245700614,-6.00546797472697,
42.936774351632));
#21130=CARTESIAN_POINT('Ctrl Pts',(-4.11002577701861,-4.59925935417381,
42.7977543561197));
#21131=CARTESIAN_POINT('Ctrl Pts',(-5.6321265650094,-2.33549534064642,42.6732879696438));
#21132=CARTESIAN_POINT('Ctrl Pts',(-5.9159223932062,-0.675180153545571,
42.5951615816723));
#21133=CARTESIAN_POINT('Ctrl Pts',(-5.91650634169521,0.000138707710825164,
42.5633751922049));
#21134=CARTESIAN_POINT('Ctrl Pts',(-5.91624600190987,-1.62085350774297E-5,
42.3116248096983));
#21135=CARTESIAN_POINT('Ctrl Pts',(-5.9162911582345,-0.474720455898875,
42.3339657104534));
#21136=CARTESIAN_POINT('Ctrl Pts',(-5.74279880125224,-1.9335131105899,42.4026220729701));
#21137=CARTESIAN_POINT('Ctrl Pts',(-4.55678795407543,-4.15666021881412,
42.5175938972485));
#21138=CARTESIAN_POINT('Ctrl Pts',(-2.01272668996952,-5.8301862667123,42.6565402825336));
#21139=CARTESIAN_POINT('Ctrl Pts',(1.02194545414071,-6.08257906827687,42.7954866678188));
#21140=CARTESIAN_POINT('Ctrl Pts',(3.80751395140674,-4.85231678097389,42.9344330531039));
#21141=CARTESIAN_POINT('Ctrl Pts',(5.66498437175318,-2.43928118528315,43.0733794383891));
#21142=CARTESIAN_POINT('Ctrl Pts',(6.14159022579141,0.568339802872113,43.212325823674));
#21143=CARTESIAN_POINT('Ctrl Pts',(5.12115676480036,3.43742549350886,43.3512722089594));
#21144=CARTESIAN_POINT('Ctrl Pts',(2.85241908071542,5.46862377761041,43.4902185942444));
#21145=CARTESIAN_POINT('Ctrl Pts',(-0.111608153759956,6.16682124380889,
43.6291649795295));
#21146=CARTESIAN_POINT('Ctrl Pts',(-3.04843041559615,5.36182922465329,43.7681113648146));
#21147=CARTESIAN_POINT('Ctrl Pts',(-5.24218451210158,3.24986802411406,43.9070577500999));
#21148=CARTESIAN_POINT('Ctrl Pts',(-5.88714142667184,1.20495123427865,44.0048955644266));
#21149=CARTESIAN_POINT('Ctrl Pts',(-5.91719016898237,0.110696514981872,
44.0564179169917));
#21150=CARTESIAN_POINT('Ctrl Pts',(-5.91709874397735,0.00010522564014079,
44.0616248077951));
#21151=CARTESIAN_POINT('Origin',(0.,0.,0.));
#21152=CARTESIAN_POINT('',(-5.91670022645612,8.9340538150264E-6,46.0633751921059));
#21153=CARTESIAN_POINT('',(-5.9167499982011,-0.000145901520602546,45.811624807825));
#21154=CARTESIAN_POINT('',(-5.91675,-7.2459289488551E-16,0.));
#21155=CARTESIAN_POINT('Ctrl Pts',(-5.91624311178355,8.95268515702394E-6,
46.0633751911966));
#21156=CARTESIAN_POINT('Ctrl Pts',(-5.91626844413286,0.482775674933225,
46.0406548784336));
#21157=CARTESIAN_POINT('Ctrl Pts',(-5.73873369182433,1.9501676262938,45.9715945671664));
#21158=CARTESIAN_POINT('Ctrl Pts',(-4.53885955463525,4.17663170963269,45.8561942573948));
#21159=CARTESIAN_POINT('Ctrl Pts',(-1.9858849930876,5.83967116274058,45.7171742618825));
#21160=CARTESIAN_POINT('Ctrl Pts',(1.05166000220467,6.07778822718667,45.5781542663699));
#21161=CARTESIAN_POINT('Ctrl Pts',(3.83259228064817,4.83288060115294,45.4391342708575));
#21162=CARTESIAN_POINT('Ctrl Pts',(5.67834406774424,2.40871483224303,45.3001142753448));
#21163=CARTESIAN_POINT('Ctrl Pts',(6.13853845488877,-0.603194937442445,
45.1610942798325));
#21164=CARTESIAN_POINT('Ctrl Pts',(5.10088465258069,-3.46792073955065,45.0220742843197));
#21165=CARTESIAN_POINT('Ctrl Pts',(2.81857776262614,-5.48644856813047,44.8830542888075));
#21166=CARTESIAN_POINT('Ctrl Pts',(-0.151482674794658,-6.1662428993653,
44.7440342932947));
#21167=CARTESIAN_POINT('Ctrl Pts',(-3.08458023385813,-5.3414289544657,44.6050142977824));
#21168=CARTESIAN_POINT('Ctrl Pts',(-5.26501770087436,-3.21326735647927,
44.4659943022696));
#21169=CARTESIAN_POINT('Ctrl Pts',(-5.89138148615921,-1.17682672319444,
44.3687812670773));
#21170=CARTESIAN_POINT('Ctrl Pts',(-5.91720758821343,-0.0963716088886832,
44.317908230389));
#21171=CARTESIAN_POINT('Ctrl Pts',(-5.917134484543,-9.42401903047951E-5,
44.3133751922049));
#21172=CARTESIAN_POINT('Ctrl Pts',(-5.91674999906443,0.000105219438300132,
44.0616248077951));
#21173=CARTESIAN_POINT('Ctrl Pts',(-5.91675292974581,-0.164694264183333,
44.0693844018043));
#21174=CARTESIAN_POINT('Ctrl Pts',(-5.90986626711654,-0.329524092285221,
44.0771439958136));
#21175=CARTESIAN_POINT('Ctrl Pts',(-5.89610847089198,-0.493796984575521,
44.0849035898228));
#21176=CARTESIAN_POINT('Ctrl Pts',(-5.88235316316463,-0.658040163339901,
44.092661780284));
#21177=CARTESIAN_POINT('Ctrl Pts',(-5.86172922869553,-0.821726284461634,
44.1004199707452));
#21178=CARTESIAN_POINT('Ctrl Pts',(-5.83430709207036,-0.98427197355076,
44.1081781612064));
#21179=CARTESIAN_POINT('Ctrl Pts',(-5.80688388374666,-1.14682401517105,
44.1159366548694));
#21180=CARTESIAN_POINT('Ctrl Pts',(-5.7726619930524,-1.30823521555114,44.1236951485324));
#21181=CARTESIAN_POINT('Ctrl Pts',(-5.73176329488124,-1.46793054806834,
44.1314536421954));
#21182=CARTESIAN_POINT('Ctrl Pts',(-5.6908653830365,-1.62762281025159,44.139211986692));
#21183=CARTESIAN_POINT('Ctrl Pts',(-5.64329100328209,-1.78559895718424,
44.1469703311887));
#21184=CARTESIAN_POINT('Ctrl Pts',(-5.58921245617926,-1.94129716483352,
44.1547286756854));
#21185=CARTESIAN_POINT('Ctrl Pts',(-5.53512176998858,-2.09703032227937,
44.1624887617086));
#21186=CARTESIAN_POINT('Ctrl Pts',(-5.47452410735967,-2.25048421314287,
44.1702488477318));
#21187=CARTESIAN_POINT('Ctrl Pts',(-5.40764088713853,-2.40111444921886,
44.178008933755));
#21188=CARTESIAN_POINT('Ctrl Pts',(-5.38769799454131,-2.44602859375355,
44.18032279606));
#21189=CARTESIAN_POINT('Ctrl Pts',(-5.36719658841139,-2.49069182920989,
44.182636658365));
#21190=CARTESIAN_POINT('Ctrl Pts',(-5.34614335675952,-2.53509009139243,
44.18495052067));
#21191=CARTESIAN_POINT('Ctrl Pts',(-5.27528135562149,-2.684527942898,44.192738632063));
#21192=CARTESIAN_POINT('Ctrl Pts',(-5.1981370458312,-2.83101946154697,44.2005267434561));
#21193=CARTESIAN_POINT('Ctrl Pts',(-5.11498062512479,-2.97403829280964,
44.2083148548492));
#21194=CARTESIAN_POINT('Ctrl Pts',(-5.03184053073186,-3.11702904481811,
44.2161014371824));
#21195=CARTESIAN_POINT('Ctrl Pts',(-4.94269084112915,-3.25654819377814,
44.2238880195156));
#21196=CARTESIAN_POINT('Ctrl Pts',(-4.84784704410832,-3.39209516367543,
44.2316746018488));
#21197=CARTESIAN_POINT('Ctrl Pts',(-4.75299963071467,-3.52764730194843,
44.2394614810826));
#21198=CARTESIAN_POINT('Ctrl Pts',(-4.65245785540012,-3.65922669403395,
44.2472483603165));
#21199=CARTESIAN_POINT('Ctrl Pts',(-4.54658018845511,-3.78636225848076,
44.2550352395503));
#21200=CARTESIAN_POINT('Ctrl Pts',(-4.44070950937486,-3.91348943205387,
44.2628216048546));
#21201=CARTESIAN_POINT('Ctrl Pts',(-4.32950384798739,-4.03617311942931,
44.270607970159));
#21202=CARTESIAN_POINT('Ctrl Pts',(-4.21336165507873,-4.1539757011822,44.2783943354633));
#21203=CARTESIAN_POINT('Ctrl Pts',(-4.09718896558881,-4.27180921550076,
44.286182745309));
#21204=CARTESIAN_POINT('Ctrl Pts',(-3.97607737753084,-4.38475883408334,
44.2939711551547));
#21205=CARTESIAN_POINT('Ctrl Pts',(-3.85046249940051,-4.49242352224391,
44.3017595650005));
#21206=CARTESIAN_POINT('Ctrl Pts',(-3.73144892918354,-4.59443022013675,
44.309138678652));
#21207=CARTESIAN_POINT('Ctrl Pts',(-3.60839340594453,-4.69169299836114,
44.3165177923036));
#21208=CARTESIAN_POINT('Ctrl Pts',(-3.48169401885481,-4.78390398331432,
44.3238969059552));
#21209=CARTESIAN_POINT('Ctrl Pts',(-3.34797214023092,-4.8812258916592,44.3316850173481));
#21210=CARTESIAN_POINT('Ctrl Pts',(-3.21014325251378,-4.97295487987166,
44.339473128741));
#21211=CARTESIAN_POINT('Ctrl Pts',(-3.0686964490714,-5.05875801614948,44.3472612401339));
#21212=CARTESIAN_POINT('Ctrl Pts',(-2.92727741624261,-5.14454430647754,
44.355047822467));
#21213=CARTESIAN_POINT('Ctrl Pts',(-2.78224215800226,-5.22440690065538,
44.3628344048));
#21214=CARTESIAN_POINT('Ctrl Pts',(-2.63410720459904,-5.29805717194326,
44.370620987133));
#21215=CARTESIAN_POINT('Ctrl Pts',(-2.48596660284336,-5.37171025149943,
44.3784078663667));
#21216=CARTESIAN_POINT('Ctrl Pts',(-2.33472635377261,-5.43915038839738,
44.3861947456004));
#21217=CARTESIAN_POINT('Ctrl Pts',(-2.1809266203098,-5.50013542008959,44.393981624834));
#21218=CARTESIAN_POINT('Ctrl Pts',(-2.02713703754053,-5.56111642680494,
44.4017679901382));
#21219=CARTESIAN_POINT('Ctrl Pts',(-1.87078860551923,-5.61564306319405,
44.4095543554424));
#21220=CARTESIAN_POINT('Ctrl Pts',(-1.71244058554131,-5.66352167855752,
44.4173407207465));
#21221=CARTESIAN_POINT('Ctrl Pts',(-1.55405098658872,-5.71141286587316,
44.4251291305921));
#21222=CARTESIAN_POINT('Ctrl Pts',(-1.3936610560103,-5.75265244962214,44.4329175404376));
#21223=CARTESIAN_POINT('Ctrl Pts',(-1.23184518070523,-5.78709668255796,
44.4407059502832));
#21224=CARTESIAN_POINT('Ctrl Pts',(-1.07853304660958,-5.81973080358423,
44.4480850639356));
#21225=CARTESIAN_POINT('Ctrl Pts',(-0.92394123975902,-5.84626536760117,
44.4554641775879));
#21226=CARTESIAN_POINT('Ctrl Pts',(-0.768566628930374,-5.86662048366814,
44.4628432912403));
#21227=CARTESIAN_POINT('Ctrl Pts',(-0.604580162022182,-5.88810381063853,
44.4706314026333));
#21228=CARTESIAN_POINT('Ctrl Pts',(-0.439663086899155,-5.90271092879514,
44.4784195140262));
#21229=CARTESIAN_POINT('Ctrl Pts',(-0.274404173926619,-5.91038348263729,
44.4862076254191));
#21230=CARTESIAN_POINT('Ctrl Pts',(-0.10917770666087,-5.91805453010723,
44.4939942077521));
#21231=CARTESIAN_POINT('Ctrl Pts',(0.0563901455546477,-5.91879371501194,
44.5017807900851));
#21232=CARTESIAN_POINT('Ctrl Pts',(0.22170771650763,-5.91259471390869,44.5095673724182));
#21233=CARTESIAN_POINT('Ctrl Pts',(0.38703159098281,-5.90639547643891,44.5173542516518));
#21234=CARTESIAN_POINT('Ctrl Pts',(0.552104845660218,-5.89325753162055,
44.5251411308855));
#21235=CARTESIAN_POINT('Ctrl Pts',(0.716337292044847,-5.87322666398342,
44.5329280101192));
#21236=CARTESIAN_POINT('Ctrl Pts',(0.88055889918308,-5.85319711837197,44.5407143754233));
#21237=CARTESIAN_POINT('Ctrl Pts',(1.04393949188983,-5.8262755991296,44.5485007407275));
#21238=CARTESIAN_POINT('Ctrl Pts',(1.20589532073218,-5.79255962748216,44.5562871060316));
#21239=CARTESIAN_POINT('Ctrl Pts',(1.3678936758865,-5.7588348027052,44.5640755158772));
#21240=CARTESIAN_POINT('Ctrl Pts',(1.52846620619538,-5.71831202381455,44.5718639257228));
#21241=CARTESIAN_POINT('Ctrl Pts',(1.68703975565961,-5.67113987001943,44.5796523355683));
#21242=CARTESIAN_POINT('Ctrl Pts',(1.83727995448778,-5.62644670530641,44.5870314492207));
#21243=CARTESIAN_POINT('Ctrl Pts',(1.9857256200061,-5.57578513978001,44.594410562873));
#21244=CARTESIAN_POINT('Ctrl Pts',(2.13190221775661,-5.5193227389259,44.6017896765254));
#21245=CARTESIAN_POINT('Ctrl Pts',(2.28618085879148,-5.45973083018408,44.6095777879184));
#21246=CARTESIAN_POINT('Ctrl Pts',(2.437986867365,-5.39365552973634,44.6173658993113));
#21247=CARTESIAN_POINT('Ctrl Pts',(2.58677531145044,-5.3213272827905,44.6251540107043));
#21248=CARTESIAN_POINT('Ctrl Pts',(2.7355345435187,-5.24901323623505,44.6329405930374));
#21249=CARTESIAN_POINT('Ctrl Pts',(2.88127710600939,-5.17044883233235,44.6407271753705));
#21250=CARTESIAN_POINT('Ctrl Pts',(3.02348041795781,-5.08591159230336,44.6485137577035));
#21251=CARTESIAN_POINT('Ctrl Pts',(3.16568915208702,-5.00137112888812,44.6563006369373));
#21252=CARTESIAN_POINT('Ctrl Pts',(3.30435808897071,-4.91085753351266,44.664087516171));
#21253=CARTESIAN_POINT('Ctrl Pts',(3.43899087555306,-4.81469337760597,44.6718743954047));
#21254=CARTESIAN_POINT('Ctrl Pts',(3.57361477644938,-4.71853556847794,44.6796607607089));
#21255=CARTESIAN_POINT('Ctrl Pts',(3.70420280015421,-4.61672813094623,44.6874471260131));
#21256=CARTESIAN_POINT('Ctrl Pts',(3.83028900055894,-4.50963598693921,44.6952334913173));
#21257=CARTESIAN_POINT('Ctrl Pts',(3.9564083086395,-4.40251572270987,44.703021901163));
#21258=CARTESIAN_POINT('Ctrl Pts',(4.07802318640741,-4.2901081846857,44.7108103110086));
#21259=CARTESIAN_POINT('Ctrl Pts',(4.19470141802977,-4.17281806170351,44.7185987208542));
#21260=CARTESIAN_POINT('Ctrl Pts',(4.30524798002809,-4.06169176443491,44.7259778345063));
#21261=CARTESIAN_POINT('Ctrl Pts',(4.41136322794721,-3.94618304619205,44.7333569481584));
#21262=CARTESIAN_POINT('Ctrl Pts',(4.51271063148502,-3.82666608407137,44.7407360618105));
#21263=CARTESIAN_POINT('Ctrl Pts',(4.61967535724367,-3.70052472641955,44.7485241732034));
#21264=CARTESIAN_POINT('Ctrl Pts',(4.72136692477582,-3.5698731490814,44.7563122845964));
#21265=CARTESIAN_POINT('Ctrl Pts',(4.81741706994369,-3.43517442595208,44.7641003959894));
#21266=CARTESIAN_POINT('Ctrl Pts',(4.9134483573405,-3.30050214856813,44.7718869783224));
#21267=CARTESIAN_POINT('Ctrl Pts',(5.00384024695538,-3.1617845708287,44.7796735606555));
#21268=CARTESIAN_POINT('Ctrl Pts',(5.08826662445309,-3.01951541161438,44.7874601429886));
#21269=CARTESIAN_POINT('Ctrl Pts',(5.17269622110941,-2.87724082770931,44.7952470222223));
#21270=CARTESIAN_POINT('Ctrl Pts',(5.25115968403862,-2.73141466411298,44.803033901456));
#21271=CARTESIAN_POINT('Ctrl Pts',(5.3233754838391,-2.58255765096557,44.8108207806897));
#21272=CARTESIAN_POINT('Ctrl Pts',(5.39558651743858,-2.43371046229491,44.8186071459939));
#21273=CARTESIAN_POINT('Ctrl Pts',(5.46155057369599,-2.28183311193025,44.8263935112981));
#21274=CARTESIAN_POINT('Ctrl Pts',(5.52103308621654,-2.12746897119613,44.8341798766023));
#21275=CARTESIAN_POINT('Ctrl Pts',(5.58053121763691,-1.97306429757344,44.8419682864479));
#21276=CARTESIAN_POINT('Ctrl Pts',(5.63354428774699,-1.81617182644615,44.8497566962934));
#21277=CARTESIAN_POINT('Ctrl Pts',(5.67988637536829,-1.65735371161551,44.857545106139));
#21278=CARTESIAN_POINT('Ctrl Pts',(5.7237930955098,-1.50688179981352,44.8649242197912));
#21279=CARTESIAN_POINT('Ctrl Pts',(5.76171187287224,-1.3546816810388,44.8723033334434));
#21280=CARTESIAN_POINT('Ctrl Pts',(5.7935262120333,-1.20124293670474,44.8796824470956));
#21281=CARTESIAN_POINT('Ctrl Pts',(5.8271039056369,-1.03929963440678,44.8874705584886));
#21282=CARTESIAN_POINT('Ctrl Pts',(5.85389327048895,-0.875918670096511,
44.8952586698815));
#21283=CARTESIAN_POINT('Ctrl Pts',(5.87379247632503,-0.71168287008151,44.9030467812745));
#21284=CARTESIAN_POINT('Ctrl Pts',(5.89368777529901,-0.547479314902179,
44.9108333636076));
#21285=CARTESIAN_POINT('Ctrl Pts',(5.90669557601055,-0.382421575905723,
44.9186199459407));
#21286=CARTESIAN_POINT('Ctrl Pts',(5.91276572254066,-0.217099223509076,
44.9264065282737));
#21287=CARTESIAN_POINT('Ctrl Pts',(5.91883610052409,-0.0517705674081396,
44.9341934075075));
#21288=CARTESIAN_POINT('Ctrl Pts',(5.91796827932953,0.113822403126622,44.9419802867412));
#21289=CARTESIAN_POINT('Ctrl Pts',(5.91016417722504,0.279087729479209,44.9497671659749));
#21290=CARTESIAN_POINT('Ctrl Pts',(5.90236059018677,0.444342148415976,44.9575535312791));
#21291=CARTESIAN_POINT('Ctrl Pts',(5.88762165353856,0.609268647252071,44.9653398965833));
#21292=CARTESIAN_POINT('Ctrl Pts',(5.86600135717776,0.773277854389171,44.9731262618875));
#21293=CARTESIAN_POINT('Ctrl Pts',(5.84437538376618,0.937330127013461,44.9809146717331));
#21294=CARTESIAN_POINT('Ctrl Pts',(5.81586447993154,1.10046430939594,44.9887030815787));
#21295=CARTESIAN_POINT('Ctrl Pts',(5.78057433824521,1.26209781020368,44.9964914914244));
#21296=CARTESIAN_POINT('Ctrl Pts',(5.74713876263145,1.41523715393347,45.0038706050765));
#21297=CARTESIAN_POINT('Ctrl Pts',(5.7076182026209,1.56702923267224,45.0112497187287));
#21298=CARTESIAN_POINT('Ctrl Pts',(5.6621445939367,1.71698839828737,45.0186288323808));
#21299=CARTESIAN_POINT('Ctrl Pts',(5.61415054660697,1.87525926132885,45.0264169437738));
#21300=CARTESIAN_POINT('Ctrl Pts',(5.5595076846427,2.03154479234359,45.0342050551667));
#21301=CARTESIAN_POINT('Ctrl Pts',(5.49840543322243,2.18528447905761,45.0419931665597));
#21302=CARTESIAN_POINT('Ctrl Pts',(5.43731517816377,2.33899398166495,45.0497797488928));
#21303=CARTESIAN_POINT('Ctrl Pts',(5.36976818200352,2.4901583405325,45.0575663312259));
#21304=CARTESIAN_POINT('Ctrl Pts',(5.29600247296227,2.63823584405897,45.065352913559));
#21305=CARTESIAN_POINT('Ctrl Pts',(5.22223395125119,2.7863189937472,45.0731397927927));
#21306=CARTESIAN_POINT('Ctrl Pts',(5.14224638112126,2.9313147648196,45.0809266720264));
#21307=CARTESIAN_POINT('Ctrl Pts',(5.056324660924,3.07270426267022,45.0887135512601));
#21308=CARTESIAN_POINT('Ctrl Pts',(4.97040861151069,3.21408442889559,45.0964999165643));
#21309=CARTESIAN_POINT('Ctrl Pts',(4.87855936183501,3.3518585251756,45.1042862818685));
#21310=CARTESIAN_POINT('Ctrl Pts',(4.78110629781429,3.48553484152727,45.1120726471727));
#21311=CARTESIAN_POINT('Ctrl Pts',(4.68362764459801,3.61924625856495,45.1198610570183));
#21312=CARTESIAN_POINT('Ctrl Pts',(4.58054242356535,3.74885748610181,45.1276494668639));
#21313=CARTESIAN_POINT('Ctrl Pts',(4.47222217801387,3.87390750444314,45.1354378767095));
#21314=CARTESIAN_POINT('Ctrl Pts',(4.36959437354556,3.99238589937065,45.1428169903616));
#21315=CARTESIAN_POINT('Ctrl Pts',(4.26226778446086,4.10676995904151,45.1501961040138));
#21316=CARTESIAN_POINT('Ctrl Pts',(4.15059061772226,4.21669634744737,45.1575752176659));
#21317=CARTESIAN_POINT('Ctrl Pts',(4.03272358712737,4.33271556036083,45.1653633290588));
#21318=CARTESIAN_POINT('Ctrl Pts',(3.90996793348465,4.44381038052038,45.1731514404517));
#21319=CARTESIAN_POINT('Ctrl Pts',(3.7827581642049,4.54957923698898,45.1809395518445));
#21320=CARTESIAN_POINT('Ctrl Pts',(3.65557337034532,4.65532732758679,45.1887261341775));
#21321=CARTESIAN_POINT('Ctrl Pts',(3.52393645125614,4.75575133673834,45.1965127165105));
#21322=CARTESIAN_POINT('Ctrl Pts',(3.388315598884,4.85048945621567,45.2042992988435));
#21323=CARTESIAN_POINT('Ctrl Pts',(3.25268957531885,4.94523118803647,45.2120861780772));
#21324=CARTESIAN_POINT('Ctrl Pts',(3.11307957418037,5.03428641015035,45.2198730573108));
#21325=CARTESIAN_POINT('Ctrl Pts',(2.9699840286919,5.11733577477724,45.2276599365445));
#21326=CARTESIAN_POINT('Ctrl Pts',(2.82689792742734,5.20037965819372,45.2354463018486));
#21327=CARTESIAN_POINT('Ctrl Pts',(2.68032701860359,5.27741831704511,45.2432326671527));
#21328=CARTESIAN_POINT('Ctrl Pts',(2.53079579490881,5.34817755940955,45.2510190324567));
#21329=CARTESIAN_POINT('Ctrl Pts',(2.38122530735057,5.41895538171443,45.2588074423023));
#21330=CARTESIAN_POINT('Ctrl Pts',(2.22869323985966,5.48345035427393,45.2665958521478));
#21331=CARTESIAN_POINT('Ctrl Pts',(2.07374642116591,5.54143540458621,45.2743842619933));
#21332=CARTESIAN_POINT('Ctrl Pts',(1.92694236129699,5.59637322692623,45.2817633756459));
#21333=CARTESIAN_POINT('Ctrl Pts',(1.77797106576764,5.64546765576021,45.2891424892985));
#21334=CARTESIAN_POINT('Ctrl Pts',(1.62731213581907,5.68856623193542,45.296521602951));
#21335=CARTESIAN_POINT('Ctrl Pts',(1.46830272302965,5.73405360724083,45.3043097143441));
#21336=CARTESIAN_POINT('Ctrl Pts',(1.30735650189762,5.77287787120483,45.3120978257372));
#21337=CARTESIAN_POINT('Ctrl Pts',(1.14504714899589,5.80489427888884,45.3198859371303));
#21338=CARTESIAN_POINT('Ctrl Pts',(0.982769662705261,5.8369044007095,45.3276725194635));
#21339=CARTESIAN_POINT('Ctrl Pts',(0.819129891934903,5.86210927137328,45.3354591017967));
#21340=CARTESIAN_POINT('Ctrl Pts',(0.654712068535333,5.88041517835384,45.3432456841299));
#21341=CARTESIAN_POINT('Ctrl Pts',(0.490287975921632,5.89872178333446,45.3510325633637));
#21342=CARTESIAN_POINT('Ctrl Pts',(0.325086088431835,5.91012885897701,45.3588194425975));
#21343=CARTESIAN_POINT('Ctrl Pts',(0.159696878896288,5.91459444673688,45.3666063218314));
#21344=CARTESIAN_POINT('Ctrl Pts',(-0.0056814150471084,5.91905973977055,
45.3743926871357));
#21345=CARTESIAN_POINT('Ctrl Pts',(-0.171246686855606,5.91658445321134,
45.38217905244));
#21346=CARTESIAN_POINT('Ctrl Pts',(-0.336407184442936,5.90717874867141,
45.3899654177442));
#21347=CARTESIAN_POINT('Ctrl Pts',(-0.501611049823396,5.89777057438445,
45.39775382759));
#21348=CARTESIAN_POINT('Ctrl Pts',(-0.666409609270265,5.8814283620441,45.4055422374357));
#21349=CARTESIAN_POINT('Ctrl Pts',(-0.830214040501387,5.8582143362508,45.4133306472814));
#21350=CARTESIAN_POINT('Ctrl Pts',(-0.985410227993851,5.83622025298702,
45.420709760933));
#21351=CARTESIAN_POINT('Ctrl Pts',(-1.13971382907723,5.8080580705383,45.4280888745846));
#21352=CARTESIAN_POINT('Ctrl Pts',(-1.29263075311924,5.77382336918877,45.4354679882362));
#21353=CARTESIAN_POINT('Ctrl Pts',(-1.45402331251518,5.73769116141929,45.4432560996291));
#21354=CARTESIAN_POINT('Ctrl Pts',(-1.61392876009556,5.69478128607549,45.451044211022));
#21355=CARTESIAN_POINT('Ctrl Pts',(-1.7717740862838,5.64524110642523,45.4588323224149));
#21356=CARTESIAN_POINT('Ctrl Pts',(-1.92958842229475,5.59571065312537,45.466618904748));
#21357=CARTESIAN_POINT('Ctrl Pts',(-2.08534313927165,5.5395525885105,45.474405487081));
#21358=CARTESIAN_POINT('Ctrl Pts',(-2.2384803745134,5.47696413859159,45.4821920694141));
#21359=CARTESIAN_POINT('Ctrl Pts',(-2.39162344884292,5.4143733021894,45.4899789486478));
#21360=CARTESIAN_POINT('Ctrl Pts',(-2.54214854446916,5.34535170708692,45.4977658278815));
#21361=CARTESIAN_POINT('Ctrl Pts',(-2.68951707927402,5.27014501155266,45.5055527071151));
#21362=CARTESIAN_POINT('Ctrl Pts',(-2.83687588784108,5.19494327961667,45.5133390724193));
#21363=CARTESIAN_POINT('Ctrl Pts',(-2.98107826791173,5.11355740950706,45.5211254377235));
#21364=CARTESIAN_POINT('Ctrl Pts',(-3.12160945014501,5.02627943943285,45.5289118030276));
#21365=CARTESIAN_POINT('Ctrl Pts',(-3.26217753301292,4.93897855193608,45.5367002128732));
#21366=CARTESIAN_POINT('Ctrl Pts',(-3.39907221916424,4.84578263999627,45.5444886227188));
#21367=CARTESIAN_POINT('Ctrl Pts',(-3.53180622075539,4.74702805779928,45.5522770325643));
#21368=CARTESIAN_POINT('Ctrl Pts',(-3.6575647905649,4.65346322233621,45.5596561462167));
#21369=CARTESIAN_POINT('Ctrl Pts',(-3.77958852371299,4.55490908299573,45.567035259869));
#21370=CARTESIAN_POINT('Ctrl Pts',(-3.89748927691541,4.45168596138917,45.5744143735213));
#21371=CARTESIAN_POINT('Ctrl Pts',(-4.02192484499469,4.34274155325654,45.5822024849142));
#21372=CARTESIAN_POINT('Ctrl Pts',(-4.14181187106979,4.22855700725017,45.5899905963072));
#21373=CARTESIAN_POINT('Ctrl Pts',(-4.25671768613563,4.10953587440725,45.5977787077001));
#21374=CARTESIAN_POINT('Ctrl Pts',(-4.3716009414481,3.99053810928859,45.6055652900331));
#21375=CARTESIAN_POINT('Ctrl Pts',(-4.48150471530554,3.86670588176482,45.6133518723661));
#21376=CARTESIAN_POINT('Ctrl Pts',(-4.58603349561461,3.73847928168672,45.6211384546991));
#21377=CARTESIAN_POINT('Ctrl Pts',(-4.69056626158296,3.61024779235671,45.6289253339328));
#21378=CARTESIAN_POINT('Ctrl Pts',(-4.78972341895787,3.4776218403516,45.6367122131665));
#21379=CARTESIAN_POINT('Ctrl Pts',(-4.88314955806598,3.34107482048217,45.6444990924002));
#21380=CARTESIAN_POINT('Ctrl Pts',(-4.97656953110303,3.20453681263698,45.6522854577043));
#21381=CARTESIAN_POINT('Ctrl Pts',(-5.0642590624491,3.06407851859942,45.6600718230085));
#21382=CARTESIAN_POINT('Ctrl Pts',(-5.14590584277307,2.92020266759243,45.6678581883127));
#21383=CARTESIAN_POINT('Ctrl Pts',(-5.22757406188339,2.77628903770896,45.6756465981582));
#21384=CARTESIAN_POINT('Ctrl Pts',(-5.30319619991197,2.62895633482615,45.6834350080038));
#21385=CARTESIAN_POINT('Ctrl Pts',(-5.37250528198391,2.47873305492039,45.6912234178494));
#21386=CARTESIAN_POINT('Ctrl Pts',(-5.43817203603136,2.33640430262884,45.6986025315017));
#21387=CARTESIAN_POINT('Ctrl Pts',(-5.49817208583667,2.1914812062773,45.7059816451541));
#21388=CARTESIAN_POINT('Ctrl Pts',(-5.55231784707662,2.04443074901901,45.7133607588064));
#21389=CARTESIAN_POINT('Ctrl Pts',(-5.60936455460306,1.88950182688849,45.7211352203467));
#21390=CARTESIAN_POINT('Ctrl Pts',(-5.65993365776862,1.73215368485384,45.728909681887));
#21391=CARTESIAN_POINT('Ctrl Pts',(-5.70383841306928,1.57294561892497,45.7366841434273));
#21392=CARTESIAN_POINT('Ctrl Pts',(-5.74773600855045,1.41376351603831,45.7444573371382));
#21393=CARTESIAN_POINT('Ctrl Pts',(-5.78497133736338,1.25272240398576,45.752230530849));
#21394=CARTESIAN_POINT('Ctrl Pts',(-5.81540773362642,1.09039600796133,45.7600037245599));
#21395=CARTESIAN_POINT('Ctrl Pts',(-5.84583994428435,0.928091935019634,
45.7677758493032));
#21396=CARTESIAN_POINT('Ctrl Pts',(-5.86947503018122,0.764503247196753,
45.7755479740466));
#21397=CARTESIAN_POINT('Ctrl Pts',(-5.88622751631293,0.600213452615404,
45.7833200987899));
#21398=CARTESIAN_POINT('Ctrl Pts',(-5.90298054378356,0.435918349182701,
45.7910924746812));
#21399=CARTESIAN_POINT('Ctrl Pts',(-5.91285049410255,0.270922413718954,
45.7988648505726));
#21400=CARTESIAN_POINT('Ctrl Pts',(-5.91580373762763,0.105814462012333,
45.8066372264639));
#21401=CARTESIAN_POINT('Ctrl Pts',(-5.91643544246187,0.0704975332260584,
45.8082997535743));
#21402=CARTESIAN_POINT('Ctrl Pts',(-5.91675086918974,0.0351754882530035,
45.8099622806847));
#21403=CARTESIAN_POINT('Ctrl Pts',(-5.91674999820112,-0.000145900885215194,
45.8116248077951));
#21404=CARTESIAN_POINT('Origin',(0.,0.,0.));
#21405=CARTESIAN_POINT('',(-5.91674999948831,7.78145713578612E-5,47.8133751922472));
#21406=CARTESIAN_POINT('',(-5.91674999827337,0.000142940948123385,47.5616248068849));
#21407=CARTESIAN_POINT('',(-5.91675,-7.2459289488551E-16,0.));
#21408=CARTESIAN_POINT('Ctrl Pts',(-5.9167499994883,7.78154695080284E-5,
47.8133751922049));
#21409=CARTESIAN_POINT('Ctrl Pts',(-5.91674898459005,0.0772462657434625,
47.8097415263266));
#21410=CARTESIAN_POINT('Ctrl Pts',(-5.91523813879494,0.154410604020374,
47.8061078604484));
#21411=CARTESIAN_POINT('Ctrl Pts',(-5.91221879226667,0.231515690329624,
47.8024741945702));
#21412=CARTESIAN_POINT('Ctrl Pts',(-5.90574747158356,0.396773879521906,
47.7946862123254));
#21413=CARTESIAN_POINT('Ctrl Pts',(-5.89234171448409,0.561790118658018,
47.7868982300805));
#21414=CARTESIAN_POINT('Ctrl Pts',(-5.87204325230494,0.725974245796646,
47.7791102478357));
#21415=CARTESIAN_POINT('Ctrl Pts',(-5.85174878075666,0.890126094714365,
47.7713237966902));
#21416=CARTESIAN_POINT('Ctrl Pts',(-5.82456434711627,1.05344584110727,47.7635373455446));
#21417=CARTESIAN_POINT('Ctrl Pts',(-5.79058345830377,1.21534923989721,47.7557508943991));
#21418=CARTESIAN_POINT('Ctrl Pts',(-5.75660127282074,1.37725881672939,47.7479641461318));
#21419=CARTESIAN_POINT('Ctrl Pts',(-5.7158221749785,1.53775162427468,47.7401773978645));
#21420=CARTESIAN_POINT('Ctrl Pts',(-5.66839078491173,1.69625365792614,47.7323906495971));
#21421=CARTESIAN_POINT('Ctrl Pts',(-5.62096253184304,1.85474520863424,47.7246044163266));
#21422=CARTESIAN_POINT('Ctrl Pts',(-5.56688295871592,2.01124594280084,47.7168181830561));
#21423=CARTESIAN_POINT('Ctrl Pts',(-5.5063465964238,2.16519692465883,47.7090319497856));
#21424=CARTESIAN_POINT('Ctrl Pts',(-5.44579429801664,2.31918843390339,47.7012436667997));
#21425=CARTESIAN_POINT('Ctrl Pts',(-5.37878192919868,2.47062855130434,47.6934553838139));
#21426=CARTESIAN_POINT('Ctrl Pts',(-5.30555256273948,2.61897738946112,47.685667100828));
#21427=CARTESIAN_POINT('Ctrl Pts',(-5.23593359251548,2.76001224809471,47.6782628002379));
#21428=CARTESIAN_POINT('Ctrl Pts',(-5.16069600116256,2.89825306412585,47.6708584996478));
#21429=CARTESIAN_POINT('Ctrl Pts',(-5.08008754470556,3.03325585808838,47.6634541990577));
#21430=CARTESIAN_POINT('Ctrl Pts',(-4.9953021689467,3.17525414359971,47.6556662269843));
#21431=CARTESIAN_POINT('Ctrl Pts',(-4.90454421118265,3.31372072242619,47.6478782549109));
#21432=CARTESIAN_POINT('Ctrl Pts',(-4.80813280107613,3.44815741080882,47.6400902828376));
#21433=CARTESIAN_POINT('Ctrl Pts',(-4.71174034733736,3.58256766631073,47.6323038420318));
#21434=CARTESIAN_POINT('Ctrl Pts',(-4.60969684529718,3.71294935283312,47.624517401226));
#21435=CARTESIAN_POINT('Ctrl Pts',(-4.50236405122898,3.83883426481282,47.6167309604202));
#21436=CARTESIAN_POINT('Ctrl Pts',(-4.39502716369273,3.96472397780296,47.6089442226544));
#21437=CARTESIAN_POINT('Ctrl Pts',(-4.2824007847869,4.0861163273587,47.6011574848886));
#21438=CARTESIAN_POINT('Ctrl Pts',(-4.16488664625825,4.20257656519422,47.5933707471228));
#21439=CARTESIAN_POINT('Ctrl Pts',(-4.04738028086294,4.31902909960812,47.5855845244215));
#21440=CARTESIAN_POINT('Ctrl Pts',(-3.92498702990236,4.43054995028435,47.5777983017201));
#21441=CARTESIAN_POINT('Ctrl Pts',(-3.79814523366374,4.53674148993497,47.5700120790187));
#21442=CARTESIAN_POINT('Ctrl Pts',(-3.67127004663938,4.64296098424292,47.5622238066137));
#21443=CARTESIAN_POINT('Ctrl Pts',(-3.53994421822294,4.7438481574137,47.5544355342087));
#21444=CARTESIAN_POINT('Ctrl Pts',(-3.40463959049158,4.83904534194063,47.5466472618036));
#21445=CARTESIAN_POINT('Ctrl Pts',(-3.27600474816551,4.9295498208105,47.5392429090508));
#21446=CARTESIAN_POINT('Ctrl Pts',(-3.14377414026063,5.01491161890032,47.531838556298));
#21447=CARTESIAN_POINT('Ctrl Pts',(-3.00837782388234,5.09485951045492,47.5244342035451));
#21448=CARTESIAN_POINT('Ctrl Pts',(-2.86596645185795,5.17894960412437,47.516646221843));
#21449=CARTESIAN_POINT('Ctrl Pts',(-2.72000168091004,5.25707997556426,47.5088582401409));
#21450=CARTESIAN_POINT('Ctrl Pts',(-2.57100217162245,5.3289659781249,47.5010702584388));
#21451=CARTESIAN_POINT('Ctrl Pts',(-2.4220319558704,5.4008378477855,47.4932838078661));
#21452=CARTESIAN_POINT('Ctrl Pts',(-2.27002847986774,5.46646765932704,47.4854973572933));
#21453=CARTESIAN_POINT('Ctrl Pts',(-2.11553348056156,5.52561749084418,47.4777109067205));
#21454=CARTESIAN_POINT('Ctrl Pts',(-1.96103258672679,5.5847695791358,47.4699241590672));
#21455=CARTESIAN_POINT('Ctrl Pts',(-1.8040402763721,5.63744107473975,47.4621374114139));
#21456=CARTESIAN_POINT('Ctrl Pts',(-1.64511736981318,5.68344256608959,47.4543506637606));
#21457=CARTESIAN_POINT('Ctrl Pts',(-1.48620497447095,5.72944101488468,47.4465644311255));
#21458=CARTESIAN_POINT('Ctrl Pts',(-1.32536254545813,5.76877025349844,47.4387781984904));
#21459=CARTESIAN_POINT('Ctrl Pts',(-1.16316527660633,5.80129098578905,47.4309919658554));
#21460=CARTESIAN_POINT('Ctrl Pts',(-1.0009253101604,5.83382027899464,47.4232036835347));
#21461=CARTESIAN_POINT('Ctrl Pts',(-0.837330104342507,5.85953741969641,
47.4154154012141));
#21462=CARTESIAN_POINT('Ctrl Pts',(-0.672965139961038,5.87835423251247,
47.4076271188934));
#21463=CARTESIAN_POINT('Ctrl Pts',(-0.516703714051457,5.89624333687711,
47.4002228152732));
#21464=CARTESIAN_POINT('Ctrl Pts',(-0.35974686430779,5.90789609377089,47.3928185116529));
#21465=CARTESIAN_POINT('Ctrl Pts',(-0.202601995391641,5.91328022285122,
47.3854142080327));
#21466=CARTESIAN_POINT('Ctrl Pts',(-0.0373142810084133,5.91894334373941,
47.3776262323232));
#21467=CARTESIAN_POINT('Ctrl Pts',(0.12824058182807,5.91767296532762,47.3698382566137));
#21468=CARTESIAN_POINT('Ctrl Pts',(0.293470960870003,5.90946743434855,47.3620502809042));
#21469=CARTESIAN_POINT('Ctrl Pts',(0.458668853635842,5.90126351667538,47.3542638364042));
#21470=CARTESIAN_POINT('Ctrl Pts',(0.623542070940536,5.88612718292717,47.3464773919043));
#21471=CARTESIAN_POINT('Ctrl Pts',(0.787501085140527,5.86410884989378,47.3386909474043));
#21472=CARTESIAN_POINT('Ctrl Pts',(0.951466353570333,5.84208967696929,47.3309042058898));
#21473=CARTESIAN_POINT('Ctrl Pts',(1.11451703189257,5.81318801807413,47.3231174643753));
#21474=CARTESIAN_POINT('Ctrl Pts',(1.27607005762088,5.777506016487,47.3153307228608));
#21475=CARTESIAN_POINT('Ctrl Pts',(1.43761239767306,5.74182637503092,47.3075444963883));
#21476=CARTESIAN_POINT('Ctrl Pts',(1.59765697133325,5.6993673573832,47.2997582699158));
#21477=CARTESIAN_POINT('Ctrl Pts',(1.75563208481372,5.65028198811994,47.2919720434433));
#21478=CARTESIAN_POINT('Ctrl Pts',(1.91364878485282,5.6011836972544,47.284183767266));
#21479=CARTESIAN_POINT('Ctrl Pts',(2.06959463018358,5.54545566216622,47.2763954910886));
#21480=CARTESIAN_POINT('Ctrl Pts',(2.22291336491067,5.48330071531751,47.2686072149112));
#21481=CARTESIAN_POINT('Ctrl Pts',(2.36867387911287,5.42420984798806,47.2612028807808));
#21482=CARTESIAN_POINT('Ctrl Pts',(2.51205981894196,5.35931056493724,47.2537985466505));
#21483=CARTESIAN_POINT('Ctrl Pts',(2.65261022735003,5.28881740507819,47.2463942125201));
#21484=CARTESIAN_POINT('Ctrl Pts',(2.80044304389721,5.21467174810495,47.2386062339468));
#21485=CARTESIAN_POINT('Ctrl Pts',(2.94519157314257,5.1343106245189,47.2308182553735));
#21486=CARTESIAN_POINT('Ctrl Pts',(3.08633557248104,5.0480157781586,47.2230302768002));
#21487=CARTESIAN_POINT('Ctrl Pts',(3.22745182187502,4.96173789799741,47.2152438294006));
#21488=CARTESIAN_POINT('Ctrl Pts',(3.36496468291711,4.8695287893827,47.207457382001));
#21489=CARTESIAN_POINT('Ctrl Pts',(3.49838068508846,4.77171490605841,47.1996709346013));
#21490=CARTESIAN_POINT('Ctrl Pts',(3.63180177689697,4.67389729126887,47.1918841901594));
#21491=CARTESIAN_POINT('Ctrl Pts',(3.76112543705835,4.57047465966712,47.1840974457175));
#21492=CARTESIAN_POINT('Ctrl Pts',(3.88588863122912,4.46181578599837,47.1763107012756));
#21493=CARTESIAN_POINT('Ctrl Pts',(4.01064357328261,4.35316409927105,47.1685244718664));
#21494=CARTESIAN_POINT('Ctrl Pts',(4.13083841205318,4.23927707351932,47.1607382424572));
#21495=CARTESIAN_POINT('Ctrl Pts',(4.2460444500956,4.12056271525048,47.1529520130481));
#21496=CARTESIAN_POINT('Ctrl Pts',(4.36128081564456,4.00181710592449,47.1451637339466));
#21497=CARTESIAN_POINT('Ctrl Pts',(4.47152553215949,3.87824185291479,47.1373754548452));
#21498=CARTESIAN_POINT('Ctrl Pts',(4.57638729802127,3.75028130425033,47.1295871757438));
#21499=CARTESIAN_POINT('Ctrl Pts',(4.67607941433032,3.62862916730995,47.1221828561651));
#21500=CARTESIAN_POINT('Ctrl Pts',(4.77090638293935,3.5030139099496,47.1147785365864));
#21501=CARTESIAN_POINT('Ctrl Pts',(4.86056617987861,3.3738445390267,47.1073742170077));
#21502=CARTESIAN_POINT('Ctrl Pts',(4.95487173760899,3.23798220180973,47.0995862394378));
#21503=CARTESIAN_POINT('Ctrl Pts',(5.04349416322125,3.09813905595918,47.0917982618679));
#21504=CARTESIAN_POINT('Ctrl Pts',(5.12611154720542,2.95481149451318,47.084010284298));
#21505=CARTESIAN_POINT('Ctrl Pts',(5.20871268788547,2.811512112526,47.076223837913));
#21506=CARTESIAN_POINT('Ctrl Pts',(5.28531098318517,2.66472995853285,47.068437391528));
#21507=CARTESIAN_POINT('Ctrl Pts',(5.35562943055617,2.51498786578794,47.060650945143));
#21508=CARTESIAN_POINT('Ctrl Pts',(5.42595056041088,2.36524006073369,47.0528642017234));
#21509=CARTESIAN_POINT('Ctrl Pts',(5.48999122356693,2.21253237853772,47.0450774583037));
#21510=CARTESIAN_POINT('Ctrl Pts',(5.5475213980055,2.0574102413401,47.0372907148841));
#21511=CARTESIAN_POINT('Ctrl Pts',(5.60504776725328,1.90229836431174,47.0295044864993));
#21512=CARTESIAN_POINT('Ctrl Pts',(5.65606439849992,1.74477265153495,47.0217182581145));
#21513=CARTESIAN_POINT('Ctrl Pts',(5.70039019635951,1.58539653454536,47.0139320297296));
#21514=CARTESIAN_POINT('Ctrl Pts',(5.74472766283695,1.42597846232665,47.0061437516463));
#21515=CARTESIAN_POINT('Ctrl Pts',(5.78237068883484,1.26470932008741,46.9983554735629));
#21516=CARTESIAN_POINT('Ctrl Pts',(5.81318840786456,1.10216654692885,46.9905671954796));
#21517=CARTESIAN_POINT('Ctrl Pts',(5.84248684772252,0.947636951174592,46.9831628708181));
#21518=CARTESIAN_POINT('Ctrl Pts',(5.8656166809451,0.79195653557368,46.9757585461566));
#21519=CARTESIAN_POINT('Ctrl Pts',(5.88250850967426,0.63562897677016,46.9683542214951));
#21520=CARTESIAN_POINT('Ctrl Pts',(5.90027558389392,0.471201348218344,46.9605662437743));
#21521=CARTESIAN_POINT('Ctrl Pts',(5.91114740556107,0.305998913864915,46.9527782660534));
#21522=CARTESIAN_POINT('Ctrl Pts',(5.91507894643294,0.140611592572644,46.9449902883326));
#21523=CARTESIAN_POINT('Ctrl Pts',(5.91900971432966,-0.0247432121329748,
46.9372038417959));
#21524=CARTESIAN_POINT('Ctrl Pts',(5.91600291646002,-0.190282511983973,
46.9294173952592));
#21525=CARTESIAN_POINT('Ctrl Pts',(5.90606560879723,-0.355414669200131,
46.9216309487226));
#21526=CARTESIAN_POINT('Ctrl Pts',(5.89612792205001,-0.520553125811444,
46.9138442051517));
#21527=CARTESIAN_POINT('Ctrl Pts',(5.87925921172332,-0.685284089509624,
46.9060574615808));
#21528=CARTESIAN_POINT('Ctrl Pts',(5.85551859508534,-0.849018577599937,
46.8982707180099));
#21529=CARTESIAN_POINT('Ctrl Pts',(5.83177954871321,-1.01274223586728,46.8904844894744));
#21530=CARTESIAN_POINT('Ctrl Pts',(5.80116955157325,-1.17546923416822,46.8826982609389));
#21531=CARTESIAN_POINT('Ctrl Pts',(5.76379929884797,-1.33661819720503,46.8749120324034));
#21532=CARTESIAN_POINT('Ctrl Pts',(5.72641920854025,-1.49780958211737,46.8671237541717));
#21533=CARTESIAN_POINT('Ctrl Pts',(5.68227537693676,-1.65742178974595,46.85933547594));
#21534=CARTESIAN_POINT('Ctrl Pts',(5.63152930497246,-1.81488518913357,46.8515471977083));
#21535=CARTESIAN_POINT('Ctrl Pts',(5.5832849635749,-1.96458580050346,46.8441428737997));
#21536=CARTESIAN_POINT('Ctrl Pts',(5.52907374942506,-2.11234411743046,46.8367385498912));
#21537=CARTESIAN_POINT('Ctrl Pts',(5.4690758249451,-2.25768469532418,46.8293342259826));
#21538=CARTESIAN_POINT('Ctrl Pts',(5.40596911694961,-2.41055607360159,46.8215462481342));
#21539=CARTESIAN_POINT('Ctrl Pts',(5.33643752795683,-2.56080719631072,46.8137582702858));
#21540=CARTESIAN_POINT('Ctrl Pts',(5.26072389823664,-2.70789856328148,46.8059702924374));
#21541=CARTESIAN_POINT('Ctrl Pts',(5.18502515445198,-2.85496101085406,46.7981838457709));
#21542=CARTESIAN_POINT('Ctrl Pts',(5.10314694126047,-2.99886465828883,46.7903973991044));
#21543=CARTESIAN_POINT('Ctrl Pts',(5.01537865147266,-3.13909342722581,46.7826109524378));
#21544=CARTESIAN_POINT('Ctrl Pts',(4.92760701350867,-3.27932754559623,46.7748242087346));
#21545=CARTESIAN_POINT('Ctrl Pts',(4.83394501550904,-3.41588623199086,46.7670374650315));
#21546=CARTESIAN_POINT('Ctrl Pts',(4.73472648900826,-3.5482806592466,46.7592507213283));
#21547=CARTESIAN_POINT('Ctrl Pts',(4.6355145250644,-3.68066632960991,46.7514644926595));
#21548=CARTESIAN_POINT('Ctrl Pts',(4.53074695982799,-3.80888803635458,46.7436782639907));
#21549=CARTESIAN_POINT('Ctrl Pts',(4.42079926864124,-3.93248832024725,46.7358920353219));
#21550=CARTESIAN_POINT('Ctrl Pts',(4.31082263412062,-4.05612114146967,46.7281037569564));
#21551=CARTESIAN_POINT('Ctrl Pts',(4.19566335985543,-4.17512986865475,46.720315478591));
#21552=CARTESIAN_POINT('Ctrl Pts',(4.07573590682066,-4.28909167311132,46.7125272002255));
#21553=CARTESIAN_POINT('Ctrl Pts',(3.9617207692809,-4.39743526317843,46.7051228769737));
#21554=CARTESIAN_POINT('Ctrl Pts',(3.84339645293024,-4.50121737957754,46.6977185537218));
#21555=CARTESIAN_POINT('Ctrl Pts',(3.72114871939846,-4.60010682165308,46.69031423047));
#21556=CARTESIAN_POINT('Ctrl Pts',(3.5925667289145,-4.70412021259759,46.6825262527759));
#21557=CARTESIAN_POINT('Ctrl Pts',(3.45959794722756,-4.80275764836333,46.6747382750817));
#21558=CARTESIAN_POINT('Ctrl Pts',(3.32271382828637,-4.89566168947718,46.6669502973876));
#21559=CARTESIAN_POINT('Ctrl Pts',(3.18585662195332,-4.98854746484865,46.6591638508776));
#21560=CARTESIAN_POINT('Ctrl Pts',(3.04508587856359,-5.07570191539245,46.6513774043676));
#21561=CARTESIAN_POINT('Ctrl Pts',(2.90090271377241,-5.15681044907876,46.6435909578576));
#21562=CARTESIAN_POINT('Ctrl Pts',(2.75671404873331,-5.23792207686447,46.635804214313));
#21563=CARTESIAN_POINT('Ctrl Pts',(2.60911297836769,-5.31298716617101,46.6280174707684));
#21564=CARTESIAN_POINT('Ctrl Pts',(2.45862659111139,-5.38173632278468,46.6202307272238));
#21565=CARTESIAN_POINT('Ctrl Pts',(2.30815015740981,-5.45048093215322,46.6124444987143));
#21566=CARTESIAN_POINT('Ctrl Pts',(2.15478907944805,-5.51291031212031,46.6046582702049));
#21567=CARTESIAN_POINT('Ctrl Pts',(1.99909199397069,-5.56880254292988,46.5968720416954));
#21568=CARTESIAN_POINT('Ctrl Pts',(1.84335392179122,-5.62470948716975,46.5890837634891));
#21569=CARTESIAN_POINT('Ctrl Pts',(1.68527891360305,-5.67407573368967,46.5812954852828));
#21570=CARTESIAN_POINT('Ctrl Pts',(1.52543325888557,-5.71672842937162,46.5735072070765));
#21571=CARTESIAN_POINT('Ctrl Pts',(1.37346783180315,-5.75727839068888,46.5661028830368));
#21572=CARTESIAN_POINT('Ctrl Pts',(1.21990238946817,-5.79176073038744,46.5586985589971));
#21573=CARTESIAN_POINT('Ctrl Pts',(1.06523416428594,-5.82006930695314,46.5512942349575));
#21574=CARTESIAN_POINT('Ctrl Pts',(0.902551831972747,-5.84984468747975,
46.5435062571582));
#21575=CARTESIAN_POINT('Ctrl Pts',(0.738591207079472,-5.8728001851706,46.5357182793589));
#21576=CARTESIAN_POINT('Ctrl Pts',(0.573937319065931,-5.88884763907875,
46.5279303015596));
#21577=CARTESIAN_POINT('Ctrl Pts',(0.409315803407721,-5.90489193792093,
46.520143854943));
#21578=CARTESIAN_POINT('Ctrl Pts',(0.244001614438643,-5.91403087197179,
46.5123574083264));
#21579=CARTESIAN_POINT('Ctrl Pts',(0.0785853148167597,-5.91622809827302,
46.5045709617098));
#21580=CARTESIAN_POINT('Ctrl Pts',(-0.0868372950723568,-5.91842540839359,
46.4967842180574));
#21581=CARTESIAN_POINT('Ctrl Pts',(-0.252361703950604,-5.91368047267539,
46.4889974744051));
#21582=CARTESIAN_POINT('Ctrl Pts',(-0.417396179871646,-5.90200906399919,
46.4812107307527));
#21583=CARTESIAN_POINT('Ctrl Pts',(-0.58241973999981,-5.89033842729914,
46.473424502135));
#21584=CARTESIAN_POINT('Ctrl Pts',(-0.74695311324624,-5.87174225709385,
46.4656382735173));
#21585=CARTESIAN_POINT('Ctrl Pts',(-0.910408372800225,-5.84628832313591,
46.4578520448996));
#21586=CARTESIAN_POINT('Ctrl Pts',(-1.07390666136105,-5.82082768852177,
46.4500637665854));
#21587=CARTESIAN_POINT('Ctrl Pts',(-1.23632595286218,-5.78850573009129,
46.4422754882712));
#21588=CARTESIAN_POINT('Ctrl Pts',(-1.39708630805294,-5.74944174771351,
46.4344872099569));
#21589=CARTESIAN_POINT('Ctrl Pts',(-1.54992132863309,-5.71230358299892,
46.427082886453));
#21590=CARTESIAN_POINT('Ctrl Pts',(-1.7012567847426,-5.66907219451902,46.419678562949));
#21591=CARTESIAN_POINT('Ctrl Pts',(-1.85060530178236,-5.61989239928266,
46.4122742394451));
#21592=CARTESIAN_POINT('Ctrl Pts',(-2.00769229647846,-5.56816435814387,
46.4044862616998));
#21593=CARTESIAN_POINT('Ctrl Pts',(-2.16263717236233,-5.50983660796316,
46.3966982839546));
#21594=CARTESIAN_POINT('Ctrl Pts',(-2.31488407594503,-5.44511177823157,
46.3889103062093));
#21595=CARTESIAN_POINT('Ctrl Pts',(-2.46710104647754,-5.38039967395797,
46.3811238596475));
#21596=CARTESIAN_POINT('Ctrl Pts',(-2.61662080920446,-5.30929312460174,
46.3733374130856));
#21597=CARTESIAN_POINT('Ctrl Pts',(-2.76290745608669,-5.23204290422017,
46.3655509665237));
#21598=CARTESIAN_POINT('Ctrl Pts',(-2.9091996834718,-5.15478973691838,46.3577642229266));
#21599=CARTESIAN_POINT('Ctrl Pts',(-3.0522582638074,-5.07139257533503,46.3499774793295));
#21600=CARTESIAN_POINT('Ctrl Pts',(-3.19157120857266,-4.98214851074414,
46.3421907357324));
#21601=CARTESIAN_POINT('Ctrl Pts',(-3.33087493882796,-4.89291034898104,
46.3344045071702));
#21602=CARTESIAN_POINT('Ctrl Pts',(-3.46643326025359,-4.79782623059214,
46.326618278608));
#21603=CARTESIAN_POINT('Ctrl Pts',(-3.59776241442733,-4.69723707852116,
46.3188320500458));
#21604=CARTESIAN_POINT('Ctrl Pts',(-3.72912614053044,-4.59662144671625,
46.3110437717868));
#21605=CARTESIAN_POINT('Ctrl Pts',(-3.85625821970206,-4.49049807834508,
46.3032554935278));
#21606=CARTESIAN_POINT('Ctrl Pts',(-3.97870657235139,-4.37924931622166,
46.2954672152689));
#21607=CARTESIAN_POINT('Ctrl Pts',(-4.09511834130026,-4.27348500896921,
46.2880628914901));
#21608=CARTESIAN_POINT('Ctrl Pts',(-4.2072968706866,-4.16308866564848,46.2806585677113));
#21609=CARTESIAN_POINT('Ctrl Pts',(-4.31488356651933,-4.0484207254041,46.2732542439325));
#21610=CARTESIAN_POINT('Ctrl Pts',(-4.42804485175323,-3.92781128208266,
46.2654662661662));
#21611=CARTESIAN_POINT('Ctrl Pts',(-4.53616629937832,-3.80243268057,46.2576782883999));
#21612=CARTESIAN_POINT('Ctrl Pts',(-4.63885686417549,-3.67272889772604,
46.2498903106336));
#21613=CARTESIAN_POINT('Ctrl Pts',(-4.74152723912757,-3.54305061575734,
46.2421038640504));
#21614=CARTESIAN_POINT('Ctrl Pts',(-4.83876866350964,-3.40904909957154,
46.2343174174673));
#21615=CARTESIAN_POINT('Ctrl Pts',(-4.9302306493656,-3.27120104954679,46.2265309708841));
#21616=CARTESIAN_POINT('Ctrl Pts',(-5.02169612429075,-3.13334774092878,
46.2187442272656));
#21617=CARTESIAN_POINT('Ctrl Pts',(-5.10738153956141,-2.99164786892421,
46.210957483647));
#21618=CARTESIAN_POINT('Ctrl Pts',(-5.18697957900952,-2.84660735076656,
46.2031707400284));
#21619=CARTESIAN_POINT('Ctrl Pts',(-5.26657235364277,-2.70157642595418,
46.1953845114447));
#21620=CARTESIAN_POINT('Ctrl Pts',(-5.34007840453294,-2.55320557737503,
46.1875982828609));
#21621=CARTESIAN_POINT('Ctrl Pts',(-5.40723618222366,-2.40202569348276,
46.1798120542772));
#21622=CARTESIAN_POINT('Ctrl Pts',(-5.47441163895776,-2.2508060120299,46.1720237759968));
#21623=CARTESIAN_POINT('Ctrl Pts',(-5.53523535156062,-2.09677610908315,
46.1642354977164));
#21624=CARTESIAN_POINT('Ctrl Pts',(-5.58949341081284,-1.94048807596951,
46.156447219436));
#21625=CARTESIAN_POINT('Ctrl Pts',(-5.64107660006892,-1.79190489216843,
46.149042895764));
#21626=CARTESIAN_POINT('Ctrl Pts',(-5.68672581629164,-1.64128111112891,
46.141638572092));
#21627=CARTESIAN_POINT('Ctrl Pts',(-5.72629874571322,-1.48910484430855,
46.13423424842));
#21628=CARTESIAN_POINT('Ctrl Pts',(-5.76840197275352,-1.32719840963888,
46.1263564914483));
#21629=CARTESIAN_POINT('Ctrl Pts',(-5.80364017635744,-1.16348277679236,
46.1184787344766));
#21630=CARTESIAN_POINT('Ctrl Pts',(-5.83188064495595,-0.998548299026231,
46.1106009775049));
#21631=CARTESIAN_POINT('Ctrl Pts',(-5.8601159255073,-0.833644121318528,
46.1027246677533));
#21632=CARTESIAN_POINT('Ctrl Pts',(-5.88135598412391,-0.667521844660853,
46.0948483580017));
#21633=CARTESIAN_POINT('Ctrl Pts',(-5.8955193839581,-0.500781145685749,
46.0869720482502));
#21634=CARTESIAN_POINT('Ctrl Pts',(-5.90966355881241,-0.334266775601957,
46.0791064295684));
#21635=CARTESIAN_POINT('Ctrl Pts',(-5.916750252318,-0.167135962851299,46.0712408108866));
#21636=CARTESIAN_POINT('Ctrl Pts',(-5.91674999999326,8.93202511665269E-6,
46.0633751922049));
#21637=CARTESIAN_POINT('Ctrl Pts',(-5.9167499982011,-0.000145901520597427,
45.811624807825));
#21638=CARTESIAN_POINT('Ctrl Pts',(-5.91674574497461,-0.172627159573382,
45.8197432531791));
#21639=CARTESIAN_POINT('Ctrl Pts',(-5.90919506021176,-0.345071345143527,
45.8278616985332));
#21640=CARTESIAN_POINT('Ctrl Pts',(-5.89413362177757,-0.516835961530533,
45.8359801438873));
#21641=CARTESIAN_POINT('Ctrl Pts',(-5.88403693874417,-0.631981197863106,
45.8414224772887));
#21642=CARTESIAN_POINT('Ctrl Pts',(-5.8705660667189,-0.746821081022063,
45.8468648106901));
#21643=CARTESIAN_POINT('Ctrl Pts',(-5.85374480608386,-0.861163345565901,
45.8523071440916));
#21644=CARTESIAN_POINT('Ctrl Pts',(-5.82967317321384,-1.02478990562834,
45.8600952554845));
#21645=CARTESIAN_POINT('Ctrl Pts',(-5.79873229853884,-1.18743575353866,
45.8678833668775));
#21646=CARTESIAN_POINT('Ctrl Pts',(-5.7610266728846,-1.34851853410037,45.8756714782704));
#21647=CARTESIAN_POINT('Ctrl Pts',(-5.7233284500727,-1.50956968886598,45.8834580606035));
#21648=CARTESIAN_POINT('Ctrl Pts',(-5.6788681990981,-1.66905807767523,45.8912446429365));
#21649=CARTESIAN_POINT('Ctrl Pts',(-5.62780125897437,-1.82641275509849,
45.8990312252695));
#21650=CARTESIAN_POINT('Ctrl Pts',(-5.57673237167957,-1.98377343242065,
45.9068181045032));
#21651=CARTESIAN_POINT('Ctrl Pts',(-5.51905638603465,-2.13899993042873,
45.9146049837369));
#21652=CARTESIAN_POINT('Ctrl Pts',(-5.45497836904886,-2.29153694181636,
45.9223918629706));
#21653=CARTESIAN_POINT('Ctrl Pts',(-5.3909045811751,-2.44406388584953,45.9301782282748));
#21654=CARTESIAN_POINT('Ctrl Pts',(-5.32042973137928,-2.59390140390795,
45.9379645935789));
#21655=CARTESIAN_POINT('Ctrl Pts',(-5.2438069038857,-2.74051449864085,45.9457509588831));
#21656=CARTESIAN_POINT('Ctrl Pts',(-5.16716395679363,-2.88716609099508,
45.9535393687286));
#21657=CARTESIAN_POINT('Ctrl Pts',(-5.08436995260354,-3.03059128393218,
45.9613277785742));
#21658=CARTESIAN_POINT('Ctrl Pts',(-4.99572420636531,-3.17027920165334,
45.9691161884198));
#21659=CARTESIAN_POINT('Ctrl Pts',(-4.91173696773099,-3.30262624567786,
45.9764953020721));
#21660=CARTESIAN_POINT('Ctrl Pts',(-4.82249734826175,-3.43161849408526,
45.9838744157243));
#21661=CARTESIAN_POINT('Ctrl Pts',(-4.72829602237616,-3.55684513119166,
45.9912535293766));
#21662=CARTESIAN_POINT('Ctrl Pts',(-4.62887345566512,-3.68901263058366,
45.9990416407696));
#21663=CARTESIAN_POINT('Ctrl Pts',(-4.52388805820152,-3.81703245673406,
46.0068297521625));
#21664=CARTESIAN_POINT('Ctrl Pts',(-4.41371020502661,-3.94044322234745,
46.0146178635555));
#21665=CARTESIAN_POINT('Ctrl Pts',(-4.30355398335264,-4.06382975840822,
46.0224044458885));
#21666=CARTESIAN_POINT('Ctrl Pts',(-4.18820755273805,-4.18260880128283,
46.0301910282216));
#21667=CARTESIAN_POINT('Ctrl Pts',(-4.0680804803437,-4.2963533104188,46.0379776105546));
#21668=CARTESIAN_POINT('Ctrl Pts',(-3.94794882753073,-4.41010215660767,
46.0457644897883));
#21669=CARTESIAN_POINT('Ctrl Pts',(-3.82303639748256,-4.51881586238337,
46.053551369022));
#21670=CARTESIAN_POINT('Ctrl Pts',(-3.69378894281856,-4.62210491101309,
46.0613382482558));
#21671=CARTESIAN_POINT('Ctrl Pts',(-3.56455001841176,-4.7253871426254,46.0691246135599));
#21672=CARTESIAN_POINT('Ctrl Pts',(-3.43097689164286,-4.82324523415024,
46.0769109788641));
#21673=CARTESIAN_POINT('Ctrl Pts',(-3.29354776314487,-4.91533047661939,
46.0846973441683));
#21674=CARTESIAN_POINT('Ctrl Pts',(-3.15608254854857,-5.0074398988032,46.0924857540139));
#21675=CARTESIAN_POINT('Ctrl Pts',(-3.01475957356343,-5.0937732633865,46.1002741638595));
#21676=CARTESIAN_POINT('Ctrl Pts',(-2.87008609456459,-5.17402516154367,
46.1080625737051));
#21677=CARTESIAN_POINT('Ctrl Pts',(-2.73301549027402,-5.250059665255,46.1154416873573));
#21678=CARTESIAN_POINT('Ctrl Pts',(-2.5929377030047,-5.32063532214679,46.1228208010096));
#21679=CARTESIAN_POINT('Ctrl Pts',(-2.45030452930873,-5.38553045448163,
46.1301999146618));
#21680=CARTESIAN_POINT('Ctrl Pts',(-2.29976571158208,-5.45402249069423,
46.1379880260548));
#21681=CARTESIAN_POINT('Ctrl Pts',(-2.14632643833284,-5.51621090595828,
46.1457761374478));
#21682=CARTESIAN_POINT('Ctrl Pts',(-1.99053268829148,-5.5718677460384,46.1535642488408));
#21683=CARTESIAN_POINT('Ctrl Pts',(-1.83476952563732,-5.62751365886812,
46.1613508311738));
#21684=CARTESIAN_POINT('Ctrl Pts',(-1.67665310925573,-5.67663044777479,
46.1691374135069));
#21685=CARTESIAN_POINT('Ctrl Pts',(-1.51674740067902,-5.71903907007405,
46.1769239958399));
#21686=CARTESIAN_POINT('Ctrl Pts',(-1.35683559493295,-5.76144930940471,
46.1847108750737));
#21687=CARTESIAN_POINT('Ctrl Pts',(-1.19513466829972,-5.79715078458653,
46.1924977543074));
#21688=CARTESIAN_POINT('Ctrl Pts',(-1.03222240487017,-5.82601471585715,
46.2002846335411));
#21689=CARTESIAN_POINT('Ctrl Pts',(-0.869320893555808,-5.85487674212499,
46.2080709988453));
#21690=CARTESIAN_POINT('Ctrl Pts',(-0.70520852010587,-5.8769020719177,46.2158573641495));
#21691=CARTESIAN_POINT('Ctrl Pts',(-0.540472038079021,-5.89201328397643,
46.2236437294537));
#21692=CARTESIAN_POINT('Ctrl Pts',(-0.375692299597308,-5.90712846393258,
46.2314321392993));
#21693=CARTESIAN_POINT('Ctrl Pts',(-0.210288443300414,-5.91532586725346,
46.2392205491449));
#21694=CARTESIAN_POINT('Ctrl Pts',(-0.0448520209422557,-5.91657999681551,
46.2470089589905));
#21695=CARTESIAN_POINT('Ctrl Pts',(0.111890393360747,-5.91776821941246,
46.2543880726427));
#21696=CARTESIAN_POINT('Ctrl Pts',(0.268661778863087,-5.91272416162945,
46.2617671862948));
#21697=CARTESIAN_POINT('Ctrl Pts',(0.424959344252692,-5.90146931858773,
46.2691462999469));
#21698=CARTESIAN_POINT('Ctrl Pts',(0.589919921780186,-5.88959066005894,
46.2769344113398));
#21699=CARTESIAN_POINT('Ctrl Pts',(0.754411580958356,-5.87078896788286,
46.2847225227327));
#21700=CARTESIAN_POINT('Ctrl Pts',(0.917845824056466,-5.8451252857199,46.2925106341257));
#21701=CARTESIAN_POINT('Ctrl Pts',(1.08124797968991,-5.81946664217356,46.3002972164587));
#21702=CARTESIAN_POINT('Ctrl Pts',(1.24359281801192,-5.78694874630574,46.3080837987917));
#21703=CARTESIAN_POINT('Ctrl Pts',(1.4042994511938,-5.74768419573282,46.3158703811247));
#21704=CARTESIAN_POINT('Ctrl Pts',(1.56501221208391,-5.70841814801131,46.3236572603584));
#21705=CARTESIAN_POINT('Ctrl Pts',(1.72408633151957,-5.66240500282972,46.331444139592));
#21706=CARTESIAN_POINT('Ctrl Pts',(1.88095283132228,-5.60980810802301,46.3392310188257));
#21707=CARTESIAN_POINT('Ctrl Pts',(2.03780897802685,-5.5572146845809,46.3470173841298));
#21708=CARTESIAN_POINT('Ctrl Pts',(2.19245749373133,-5.49803848276105,46.354803749434));
#21709=CARTESIAN_POINT('Ctrl Pts',(2.34434609568193,-5.43249224078239,46.3625901147381));
#21710=CARTESIAN_POINT('Ctrl Pts',(2.49627458049495,-5.36692878769167,46.3703785245837));
#21711=CARTESIAN_POINT('Ctrl Pts',(2.64544140911902,-5.29499207705749,46.3781669344292));
#21712=CARTESIAN_POINT('Ctrl Pts',(2.79131492773295,-5.21694273849304,46.3859553442748));
#21713=CARTESIAN_POINT('Ctrl Pts',(2.92952250721046,-5.14299504555116,46.3933344579272));
#21714=CARTESIAN_POINT('Ctrl Pts',(3.06477378425196,-5.06356078410268,46.4007135715797));
#21715=CARTESIAN_POINT('Ctrl Pts',(3.19663753035329,-4.97889938259821,46.4080926852321));
#21716=CARTESIAN_POINT('Ctrl Pts',(3.33581000982796,-4.88954550398078,46.4158807966251));
#21717=CARTESIAN_POINT('Ctrl Pts',(3.47125849796741,-4.79433669856308,46.4236689080181));
#21718=CARTESIAN_POINT('Ctrl Pts',(3.6024954269207,-4.69360812824371,46.431457019411));
#21719=CARTESIAN_POINT('Ctrl Pts',(3.73370658979074,-4.59289933422321,46.4392436017441));
#21720=CARTESIAN_POINT('Ctrl Pts',(3.86070759000126,-4.48667313205314,46.4470301840772));
#21721=CARTESIAN_POINT('Ctrl Pts',(3.98304220736054,-4.37530631349218,46.4548167664102));
#21722=CARTESIAN_POINT('Ctrl Pts',(4.1053814893116,-4.26393524853917,46.462603645644));
#21723=CARTESIAN_POINT('Ctrl Pts',(4.22305379344426,-4.14742338715017,46.4703905248777));
#21724=CARTESIAN_POINT('Ctrl Pts',(4.33563763839668,-4.02618638801262,46.4781774041114));
#21725=CARTESIAN_POINT('Ctrl Pts',(4.44821405288046,-3.90495739044687,46.4859637694156));
#21726=CARTESIAN_POINT('Ctrl Pts',(4.55570246288126,-3.77900411344552,46.4937501347198));
#21727=CARTESIAN_POINT('Ctrl Pts',(4.65771967777217,-3.64877759883963,46.501536500024));
#21728=CARTESIAN_POINT('Ctrl Pts',(4.75976368031205,-3.51851688939553,46.5093249098696));
#21729=CARTESIAN_POINT('Ctrl Pts',(4.85633341835975,-3.38398095073037,46.5171133197152));
#21730=CARTESIAN_POINT('Ctrl Pts',(4.9470867289568,-3.24565300959291,46.5249017295608));
#21731=CARTESIAN_POINT('Ctrl Pts',(5.03307077531267,-3.11459447272162,46.532280843213));
#21732=CARTESIAN_POINT('Ctrl Pts',(5.11383385716742,-2.98013245414141,46.5396599568651));
#21733=CARTESIAN_POINT('Ctrl Pts',(5.18912142264732,-2.84270107881969,46.5470390705172));
#21734=CARTESIAN_POINT('Ctrl Pts',(5.26858190721559,-2.69765237644318,46.5548271819105));
#21735=CARTESIAN_POINT('Ctrl Pts',(5.34197106653847,-2.54924401797225,46.5626152933037));
#21736=CARTESIAN_POINT('Ctrl Pts',(5.40902110942795,-2.39800358637405,46.570403404697));
#21737=CARTESIAN_POINT('Ctrl Pts',(5.47605798821034,-2.24679284819814,46.5781899870303));
#21738=CARTESIAN_POINT('Ctrl Pts',(5.53675810443455,-2.09275143826518,46.5859765693637));
#21739=CARTESIAN_POINT('Ctrl Pts',(5.59090111120075,-1.93642849784706,46.593763151697));
#21740=CARTESIAN_POINT('Ctrl Pts',(5.64504618242775,-1.78009959687001,46.601550030931));
#21741=CARTESIAN_POINT('Ctrl Pts',(5.69263353560257,-1.62148929195939,46.609336910165));
#21742=CARTESIAN_POINT('Ctrl Pts',(5.73349192409416,-1.46116423404319,46.617123789399));
#21743=CARTESIAN_POINT('Ctrl Pts',(5.77434761595574,-1.30084975748813,46.6249101547034));
#21744=CARTESIAN_POINT('Ctrl Pts',(5.80847515306132,-1.13882106408848,46.6326965200079));
#21745=CARTESIAN_POINT('Ctrl Pts',(5.83575384129191,-0.975657555880504,
46.6404828853124));
#21746=CARTESIAN_POINT('Ctrl Pts',(5.86303969235206,-0.81245120424876,46.6482712951582));
#21747=CARTESIAN_POINT('Ctrl Pts',(5.88347304638301,-0.648109757425478,
46.6560597050041));
#21748=CARTESIAN_POINT('Ctrl Pts',(5.8969846349975,-0.483221250674439,46.66384811485));
#21749=CARTESIAN_POINT('Ctrl Pts',(5.90978616316074,-0.326997957974139,
46.6712272285008));
#21750=CARTESIAN_POINT('Ctrl Pts',(5.9163746975525,-0.170283883823899,46.6786063421515));
#21751=CARTESIAN_POINT('Ctrl Pts',(5.91673441105521,-0.0135820298596808,
46.6859854558023));
#21752=CARTESIAN_POINT('Ctrl Pts',(5.9171140621842,0.15180524452064,46.6937735671945));
#21753=CARTESIAN_POINT('Ctrl Pts',(5.91055496608031,0.317237973511844,46.7015616785868));
#21754=CARTESIAN_POINT('Ctrl Pts',(5.89707438348461,0.482124753720084,46.709349789979));
#21755=CARTESIAN_POINT('Ctrl Pts',(5.8835964475663,0.646979161283371,46.7171363723114));
#21756=CARTESIAN_POINT('Ctrl Pts',(5.86319976261266,0.811287515665438,46.7249229546437));
#21757=CARTESIAN_POINT('Ctrl Pts',(5.83595356553042,0.974462181653458,46.732709536976));
#21758=CARTESIAN_POINT('Ctrl Pts',(5.80870632955674,1.13764306945519,46.740496416209));
#21759=CARTESIAN_POINT('Ctrl Pts',(5.77460910758077,1.29968986656213,46.748283295442));
#21760=CARTESIAN_POINT('Ctrl Pts',(5.73378262981295,1.46002305343281,46.7560701746749));
#21761=CARTESIAN_POINT('Ctrl Pts',(5.69295884656904,1.62034565840597,46.7638565399784));
#21762=CARTESIAN_POINT('Ctrl Pts',(5.64540677526719,1.7789545698254,46.7716429052819));
#21763=CARTESIAN_POINT('Ctrl Pts',(5.59129763801248,1.93528325721484,46.7794292705853));
#21764=CARTESIAN_POINT('Ctrl Pts',(5.53717429279703,2.09165299334327,46.7872176804302));
#21765=CARTESIAN_POINT('Ctrl Pts',(5.47649054395599,2.24574100624698,46.7950060902751));
#21766=CARTESIAN_POINT('Ctrl Pts',(5.40946690214381,2.39699778829907,46.80279450012));
#21767=CARTESIAN_POINT('Ctrl Pts',(5.34596548395855,2.5403057302543,46.8101736137758));
#21768=CARTESIAN_POINT('Ctrl Pts',(5.27677348696139,2.68107212328657,46.8175527274316));
#21769=CARTESIAN_POINT('Ctrl Pts',(5.20211766672,2.81884769792547,46.8249318410874));
#21770=CARTESIAN_POINT('Ctrl Pts',(5.12332394278771,2.96425967729436,46.8327199524816));
#21771=CARTESIAN_POINT('Ctrl Pts',(5.0384153994314,3.10639183003049,46.8405080638757));
#21772=CARTESIAN_POINT('Ctrl Pts',(4.94769014194066,3.24473308946102,46.8482961752698));
#21773=CARTESIAN_POINT('Ctrl Pts',(4.85698269677268,3.38304718799686,46.8560827576041));
#21774=CARTESIAN_POINT('Ctrl Pts',(4.76046099124113,3.51757161124834,46.8638693399383));
#21775=CARTESIAN_POINT('Ctrl Pts',(4.65846696926244,3.64782346869895,46.8716559222726));
#21776=CARTESIAN_POINT('Ctrl Pts',(4.55646905827439,3.77808029262389,46.8794428015074));
#21777=CARTESIAN_POINT('Ctrl Pts',(4.44899860719475,3.90406397076062,46.8872296807423));
#21778=CARTESIAN_POINT('Ctrl Pts',(4.33643889456204,4.02532337536123,46.8950165599772));
#21779=CARTESIAN_POINT('Ctrl Pts',(4.22388661080532,4.14657477691121,46.9028029252826));
#21780=CARTESIAN_POINT('Ctrl Pts',(4.10624595514678,4.26310229476014,46.9105892905879));
#21781=CARTESIAN_POINT('Ctrl Pts',(3.98393832978329,4.37449036425771,46.9183756558933));
#21782=CARTESIAN_POINT('Ctrl Pts',(3.86159858892146,4.48590768200002,46.92616406574));
#21783=CARTESIAN_POINT('Ctrl Pts',(3.73458966473574,4.59218263805356,46.9339524755868));
#21784=CARTESIAN_POINT('Ctrl Pts',(3.60336809649189,4.69293819730075,46.9417408854335));
#21785=CARTESIAN_POINT('Ctrl Pts',(3.47904247881391,4.78839885445902,46.9491199990799));
#21786=CARTESIAN_POINT('Ctrl Pts',(3.3509358006243,4.87890514593129,46.9564991127262));
#21787=CARTESIAN_POINT('Ctrl Pts',(3.21946212751893,4.96417104580123,46.9638782263726));
#21788=CARTESIAN_POINT('Ctrl Pts',(3.08070134129333,5.05416292801406,46.9716663377643));
#21789=CARTESIAN_POINT('Ctrl Pts',(2.93814017727367,5.13834917435367,46.979454449156));
#21790=CARTESIAN_POINT('Ctrl Pts',(2.79228492083751,5.21642362959178,46.9872425605476));
#21791=CARTESIAN_POINT('Ctrl Pts',(2.64645830053852,5.29448275627153,46.9950291428794));
#21792=CARTESIAN_POINT('Ctrl Pts',(2.49733915979091,5.36643233539255,47.0028157252111));
#21793=CARTESIAN_POINT('Ctrl Pts',(2.34545879920438,5.43201192779754,47.0106023075429));
#21794=CARTESIAN_POINT('Ctrl Pts',(2.19357264745324,5.49759402073791,47.0183891867753));
#21795=CARTESIAN_POINT('Ctrl Pts',(2.03892535696227,5.55680551066272,47.0261760660077));
#21796=CARTESIAN_POINT('Ctrl Pts',(1.88206932878776,5.60943362596764,47.0339629452402));
#21797=CARTESIAN_POINT('Ctrl Pts',(1.7252236530201,5.66205826784748,47.0417493105431));
#21798=CARTESIAN_POINT('Ctrl Pts',(1.56616983428111,5.70810030307102,47.049535675846));
#21799=CARTESIAN_POINT('Ctrl Pts',(1.40547673624174,5.74739642850424,47.0573220411489));
#21800=CARTESIAN_POINT('Ctrl Pts',(1.24474144345755,5.78670287230213,47.0651104509932));
#21801=CARTESIAN_POINT('Ctrl Pts',(1.08236632138698,5.81925978896817,47.0728988608376));
#21802=CARTESIAN_POINT('Ctrl Pts',(0.918932654476083,5.84495451984338,47.0806872706819));
#21803=CARTESIAN_POINT('Ctrl Pts',(0.764087746737819,5.869298942305,47.0880663843405));
#21804=CARTESIAN_POINT('Ctrl Pts',(0.60829294670612,5.88748383046348,47.0954454979991));
#21805=CARTESIAN_POINT('Ctrl Pts',(0.452048699719725,5.89945612201512,47.1028246116577));
#21806=CARTESIAN_POINT('Ctrl Pts',(0.287144395986138,5.91209199463443,47.1106127230507));
#21807=CARTESIAN_POINT('Ctrl Pts',(0.121680514692252,5.91781157111677,47.1184008344436));
#21808=CARTESIAN_POINT('Ctrl Pts',(-0.0437518879576071,5.91658823434588,
47.1261889458366));
#21809=CARTESIAN_POINT('Ctrl Pts',(-0.209151810839005,5.91536513775584,
47.1339755281696));
#21810=CARTESIAN_POINT('Ctrl Pts',(-0.374519948085462,5.90720185010354,
47.1417621105027));
#21811=CARTESIAN_POINT('Ctrl Pts',(-0.539265149226785,5.89212386676735,
47.1495486928358));
#21812=CARTESIAN_POINT('Ctrl Pts',(-0.704016632065692,5.87704530851104,
47.1573355720695));
#21813=CARTESIAN_POINT('Ctrl Pts',(-0.868144812725076,5.85505155218487,
47.1651224513032));
#21814=CARTESIAN_POINT('Ctrl Pts',(-1.03106281778922,5.82622004633129,47.1729093305369));
#21815=CARTESIAN_POINT('Ctrl Pts',(-1.19397007035901,5.79739044334046,47.180695695841));
#21816=CARTESIAN_POINT('Ctrl Pts',(-1.35566699252405,5.76172404971993,47.1884820611452));
#21817=CARTESIAN_POINT('Ctrl Pts',(-1.51557592213154,5.71934962970049,47.1962684264494));
#21818=CARTESIAN_POINT('Ctrl Pts',(-1.67552684057655,5.67696408301889,47.2040568362949));
#21819=CARTESIAN_POINT('Ctrl Pts',(-1.83368851875553,5.62786707033558,47.2118452461405));
#21820=CARTESIAN_POINT('Ctrl Pts',(-1.98949661765231,5.57223777048773,47.219633655986));
#21821=CARTESIAN_POINT('Ctrl Pts',(-2.13711669575537,5.51953189931348,47.2270127696383));
#21822=CARTESIAN_POINT('Ctrl Pts',(-2.28262395754884,5.46096273850716,47.2343918832905));
#21823=CARTESIAN_POINT('Ctrl Pts',(-2.42555356368133,5.3967231235457,47.2417709969428));
#21824=CARTESIAN_POINT('Ctrl Pts',(-2.5764052441222,5.32892293763579,47.2495591083406));
#21825=CARTESIAN_POINT('Ctrl Pts',(-2.72443930242105,5.25478167256802,47.2573472197384));
#21826=CARTESIAN_POINT('Ctrl Pts',(-2.86912398406555,5.17455873737654,47.2651353311363));
#21827=CARTESIAN_POINT('Ctrl Pts',(-3.01378025939573,5.09435155255949,47.2729219134742));
#21828=CARTESIAN_POINT('Ctrl Pts',(-3.15508819088794,5.00806523491198,47.2807084958122));
#21829=CARTESIAN_POINT('Ctrl Pts',(-3.29254087370797,4.91600499973936,47.2884950781501));
#21830=CARTESIAN_POINT('Ctrl Pts',(-3.42999879756825,4.82394125433043,47.2962819573887));
#21831=CARTESIAN_POINT('Ctrl Pts',(-3.56360091093889,4.72610332538268,47.3040688366274));
#21832=CARTESIAN_POINT('Ctrl Pts',(-3.69286892099062,4.62284000316706,47.311855715866));
#21833=CARTESIAN_POINT('Ctrl Pts',(-3.82212839942829,4.5195834962711,47.319642081175));
#21834=CARTESIAN_POINT('Ctrl Pts',(-3.94705409737575,4.41090251220354,47.3274284464841));
#21835=CARTESIAN_POINT('Ctrl Pts',(-4.06720036185885,4.29718649571964,47.3352148117932));
#21836=CARTESIAN_POINT('Ctrl Pts',(-4.18737817431023,4.18344061971995,47.3430032216436));
#21837=CARTESIAN_POINT('Ctrl Pts',(-4.30277381202874,4.06465728785799,47.350791631494));
#21838=CARTESIAN_POINT('Ctrl Pts',(-4.41297744151611,3.94126384084724,47.3585800413444));
#21839=CARTESIAN_POINT('Ctrl Pts',(-4.51738965399641,3.82435496163977,47.3659591549723));
#21840=CARTESIAN_POINT('Ctrl Pts',(-4.61714134975592,3.70330823982444,47.3733382686001));
#21841=CARTESIAN_POINT('Ctrl Pts',(-4.71191660204499,3.57851540416871,47.3807173822279));
#21842=CARTESIAN_POINT('Ctrl Pts',(-4.81194490595416,3.44680575012756,47.3885054936042));
#21843=CARTESIAN_POINT('Ctrl Pts',(-4.90646519569752,3.31087589954584,47.3962936049805));
#21844=CARTESIAN_POINT('Ctrl Pts',(-4.99513463593049,3.17120805552515,47.4040817163568));
#21845=CARTESIAN_POINT('Ctrl Pts',(-5.08378666746387,3.03156763285201,47.4118682986732));
#21846=CARTESIAN_POINT('Ctrl Pts',(-5.1665899703572,2.88819095065933,47.4196548809895));
#21847=CARTESIAN_POINT('Ctrl Pts',(-5.24324544567091,2.74158854661878,47.4274414633059));
#21848=CARTESIAN_POINT('Ctrl Pts',(-5.31990384384115,2.59498055266058,47.4352283425229));
#21849=CARTESIAN_POINT('Ctrl Pts',(-5.39041379381665,2.44514687205506,47.4430152217399));
#21850=CARTESIAN_POINT('Ctrl Pts',(-5.45452216931258,2.29262261765377,47.4508021009569));
#21851=CARTESIAN_POINT('Ctrl Pts',(-5.51862631369322,2.14010842976407,47.4585884662445));
#21852=CARTESIAN_POINT('Ctrl Pts',(-5.57632960537021,1.98490431807098,47.466374831532));
#21853=CARTESIAN_POINT('Ctrl Pts',(-5.62742703039951,1.82756547899902,47.4741611968196));
#21854=CARTESIAN_POINT('Ctrl Pts',(-5.67853787257673,1.67018532593765,47.4819496066488));
#21855=CARTESIAN_POINT('Ctrl Pts',(-5.72303928147326,1.51066962893358,47.489738016478));
#21856=CARTESIAN_POINT('Ctrl Pts',(-5.76077582780725,1.34958972441691,47.4975264263072));
#21857=CARTESIAN_POINT('Ctrl Pts',(-5.79652924519047,1.19697488236795,47.5049055400425));
#21858=CARTESIAN_POINT('Ctrl Pts',(-5.82621046646223,1.04295626177493,47.5122846537778));
#21859=CARTESIAN_POINT('Ctrl Pts',(-5.84972948598496,0.888028999131292,
47.5196637675131));
#21860=CARTESIAN_POINT('Ctrl Pts',(-5.87556177675534,0.717863482962543,
47.5277686722033));
#21861=CARTESIAN_POINT('Ctrl Pts',(-5.89396637127144,0.546559387938223,
47.5358735768934));
#21862=CARTESIAN_POINT('Ctrl Pts',(-5.90487006217366,0.374753400712039,
47.5439784815836));
#21863=CARTESIAN_POINT('Ctrl Pts',(-5.91278338067241,0.250065759700836,
47.5498605900174));
#21864=CARTESIAN_POINT('Ctrl Pts',(-5.91674697913699,0.125113954375808,
47.5557426984511));
#21865=CARTESIAN_POINT('Ctrl Pts',(-5.91674999827337,0.000142940948123385,
47.5616248068849));
#21866=CARTESIAN_POINT('Origin',(0.,0.,-3.23514056400928));
#21867=CARTESIAN_POINT('',(-4.76403455895385,1.22194835553447,1.41535621473006));
#21868=CARTESIAN_POINT('',(-4.76403458704967,1.22194824599671,1.06992377601457));
#21869=CARTESIAN_POINT('',(-4.76403458704967,1.22194824599672,-3.23514056400928));
#21870=CARTESIAN_POINT('',(-2.8553491342286,-4.00451799648347,2.16840434497101E-18));
#21871=CARTESIAN_POINT('Ctrl Pts',(-4.76403455895385,1.22194835553447,1.41535621473006));
#21872=CARTESIAN_POINT('Ctrl Pts',(-4.70800458999606,1.44039351914803,1.40248102012867));
#21873=CARTESIAN_POINT('Ctrl Pts',(-4.63700314305273,1.65477845756619,1.38953413322633));
#21874=CARTESIAN_POINT('Ctrl Pts',(-4.53470696246686,1.90462138753004,1.37415813085186));
#21875=CARTESIAN_POINT('Ctrl Pts',(-4.51734827967389,1.94543425658411,1.37163740433799));
#21876=CARTESIAN_POINT('Ctrl Pts',(-4.48332579221817,2.02251461500581,1.36686209249771));
#21877=CARTESIAN_POINT('Ctrl Pts',(-4.46676799018909,2.05882473359429,1.36460659436931));
#21878=CARTESIAN_POINT('Ctrl Pts',(-4.39436976654198,2.21260337620139,1.35501920397534));
#21879=CARTESIAN_POINT('Ctrl Pts',(-4.33432290960145,2.32803458784841,1.34773327110701));
#21880=CARTESIAN_POINT('Ctrl Pts',(-4.18113760089329,2.59599006489001,1.33044134998623));
#21881=CARTESIAN_POINT('Ctrl Pts',(-4.08412679119583,2.74608509668859,1.32044467337898));
#21882=CARTESIAN_POINT('Ctrl Pts',(-3.94196421486327,2.94178662712893,1.3068095633645));
#21883=CARTESIAN_POINT('Ctrl Pts',(-3.90377401407975,2.99227986154057,1.30323425584314));
#21884=CARTESIAN_POINT('Ctrl Pts',(-3.82025735868806,3.09838040828677,1.29559038274552));
#21885=CARTESIAN_POINT('Ctrl Pts',(-3.77466746673069,3.15376168985781,1.29152035466386));
#21886=CARTESIAN_POINT('Ctrl Pts',(-3.61460481143815,3.33975654501333,1.27756165950139));
#21887=CARTESIAN_POINT('Ctrl Pts',(-3.49443546192976,3.46529380119033,1.26762995378764));
#21888=CARTESIAN_POINT('Ctrl Pts',(-3.28103729949359,3.66581203918653,1.25086736292124));
#21889=CARTESIAN_POINT('Ctrl Pts',(-3.1912562490297,3.74423125195052,1.24404822497318));
#21890=CARTESIAN_POINT('Ctrl Pts',(-3.06518498035832,3.84651640082668,1.23480436463534));
#21891=CARTESIAN_POINT('Ctrl Pts',(-3.03129780311374,3.87327782015248,1.23235080372801));
#21892=CARTESIAN_POINT('Ctrl Pts',(-2.96477228891903,3.92440656182911,1.22759642534413));
#21893=CARTESIAN_POINT('Ctrl Pts',(-2.9321749923349,3.94882152596272,1.22529519661884));
#21894=CARTESIAN_POINT('Ctrl Pts',(-2.79208576872101,4.05105537801711,1.21551518142562));
#21895=CARTESIAN_POINT('Ctrl Pts',(-2.68177020542182,4.12491235949855,1.20808331305876));
#21896=CARTESIAN_POINT('Ctrl Pts',(-2.45204274421959,4.2656008941963,1.19299175042516));
#21897=CARTESIAN_POINT('Ctrl Pts',(-2.33255928461634,4.33209318646586,1.18533827960573));
#21898=CARTESIAN_POINT('Ctrl Pts',(-2.13833567289214,4.42981069090453,1.17310919377991));
#21899=CARTESIAN_POINT('Ctrl Pts',(-2.06532668337509,4.46431715818869,1.16855816212231));
#21900=CARTESIAN_POINT('Ctrl Pts',(-1.92938341482113,4.52451966249412,1.16015281534676));
#21901=CARTESIAN_POINT('Ctrl Pts',(-1.86670200509481,4.55073862400259,1.15630340995557));
#21902=CARTESIAN_POINT('Ctrl Pts',(-1.7025417419909,4.6154425868246,1.1462812007209));
#21903=CARTESIAN_POINT('Ctrl Pts',(-1.60029717189643,4.65188210785799,1.14009623174922));
#21904=CARTESIAN_POINT('Ctrl Pts',(-1.41032909081309,4.71258111216489,1.12869998971155));
#21905=CARTESIAN_POINT('Ctrl Pts',(-1.3229755827362,4.73784596503927,1.12349580990551));
#21906=CARTESIAN_POINT('Ctrl Pts',(-1.11494925858713,4.79181032440926,1.1111934385348));
#21907=CARTESIAN_POINT('Ctrl Pts',(-0.993790475945812,4.81839590232615,
1.10409881184008));
#21908=CARTESIAN_POINT('Ctrl Pts',(-0.832058031315079,4.84752406127705,
1.09474836862278));
#21909=CARTESIAN_POINT('Ctrl Pts',(-0.79227343934583,4.85418509642126,1.09245790434709));
#21910=CARTESIAN_POINT('Ctrl Pts',(-0.70921897981244,4.86704240413971,1.08769850294539));
#21911=CARTESIAN_POINT('Ctrl Pts',(-0.665939352632694,4.8731527950463,1.08523061740399));
#21912=CARTESIAN_POINT('Ctrl Pts',(-0.569007689189142,4.88552253571552,
1.07972410819372));
#21913=CARTESIAN_POINT('Ctrl Pts',(-0.515322334762011,4.89147658294237,
1.07668845170441));
#21914=CARTESIAN_POINT('Ctrl Pts',(-0.324104999640068,4.90950077418687,
1.06590772639198));
#21915=CARTESIAN_POINT('Ctrl Pts',(-0.18617567718527,4.91666357473129,1.05818794873214));
#21916=CARTESIAN_POINT('Ctrl Pts',(0.0696233275322052,4.91916683216118,
1.04384335123138));
#21917=CARTESIAN_POINT('Ctrl Pts',(0.187376707626406,4.91608982794185,1.03722941185142));
#21918=CARTESIAN_POINT('Ctrl Pts',(0.373250962939735,4.90454442225307,1.02672394956429));
#21919=CARTESIAN_POINT('Ctrl Pts',(0.441500390548411,4.89887227198899,1.02285279364985));
#21920=CARTESIAN_POINT('Ctrl Pts',(0.587500701242777,4.88366245920214,1.01453356174002));
#21921=CARTESIAN_POINT('Ctrl Pts',(0.665187208179159,4.8736887328254,1.01008363000141));
#21922=CARTESIAN_POINT('Ctrl Pts',(0.832459861589463,4.8481394882327,1.00044440941763));
#21923=CARTESIAN_POINT('Ctrl Pts',(0.921919570274004,4.83192611678681,0.995252988755495));
#21924=CARTESIAN_POINT('Ctrl Pts',(1.16936495129481,4.77995761069626,0.980790344560267));
#21925=CARTESIAN_POINT('Ctrl Pts',(1.32611175780708,4.73886453699499,0.971507779099062));
#21926=CARTESIAN_POINT('Ctrl Pts',(1.52923323236656,4.6747444305644,0.959362192624918));
#21927=CARTESIAN_POINT('Ctrl Pts',(1.57767903108842,4.65861768445817,0.956456788706344));
#21928=CARTESIAN_POINT('Ctrl Pts',(1.65758129799825,4.6306302617227,0.951653830300278));
#21929=CARTESIAN_POINT('Ctrl Pts',(1.68918250879534,4.6191963428178,0.949751679951918));
#21930=CARTESIAN_POINT('Ctrl Pts',(1.78387064679191,4.58383472440289,0.944041783846336));
#21931=CARTESIAN_POINT('Ctrl Pts',(1.84658506085465,4.55893178806036,0.940245321199586));
#21932=CARTESIAN_POINT('Ctrl Pts',(2.01218282940812,4.48919753266307,0.93015388892282));
#21933=CARTESIAN_POINT('Ctrl Pts',(2.11407766251384,4.44212224904136,0.923873921626289));
#21934=CARTESIAN_POINT('Ctrl Pts',(2.34194827429732,4.32722847802811,0.909575184603036));
#21935=CARTESIAN_POINT('Ctrl Pts',(2.4667538503199,4.2573175520126,0.901557789427352));
#21936=CARTESIAN_POINT('Ctrl Pts',(2.64212712942223,4.14877684306496,0.889931669827502));
#21937=CARTESIAN_POINT('Ctrl Pts',(2.69527157592141,4.11444966985275,0.886358710261123));
#21938=CARTESIAN_POINT('Ctrl Pts',(2.80726530176578,4.03900926546058,0.878714432627161));
#21939=CARTESIAN_POINT('Ctrl Pts',(2.86590656927715,3.99761350015156,0.874641627471378));
#21940=CARTESIAN_POINT('Ctrl Pts',(2.95578878974989,3.93116979732131,0.868283265482476));
#21941=CARTESIAN_POINT('Ctrl Pts',(2.98766568027562,3.90699847750105,0.866004827442259));
#21942=CARTESIAN_POINT('Ctrl Pts',(3.1648082201486,3.76924067396294,0.853209122484264));
#21943=CARTESIAN_POINT('Ctrl Pts',(3.30389020817152,3.6479439271942,0.84264291284247));
#21944=CARTESIAN_POINT('Ctrl Pts',(3.49264722396826,3.46365466272917,0.827556885825742));
#21945=CARTESIAN_POINT('Ctrl Pts',(3.54811236656066,3.4068148032227,0.823023055605946));
#21946=CARTESIAN_POINT('Ctrl Pts',(3.62627891112114,3.32273040893692,0.816493249232355));
#21947=CARTESIAN_POINT('Ctrl Pts',(3.65009999875253,3.29654457727735,0.814483556612904));
#21948=CARTESIAN_POINT('Ctrl Pts',(3.70214958748059,3.23807203690915,0.810049707746506));
#21949=CARTESIAN_POINT('Ctrl Pts',(3.73024274954224,3.20566859974127,0.807627819375163));
#21950=CARTESIAN_POINT('Ctrl Pts',(3.77538619953825,3.15220177867906,0.803683841414471));
#21951=CARTESIAN_POINT('Ctrl Pts',(3.79269239028166,3.13135776501974,0.802158917798039));
#21952=CARTESIAN_POINT('Ctrl Pts',(3.86066637610091,3.04809793389413,0.796114856427663));
#21953=CARTESIAN_POINT('Ctrl Pts',(3.90997302083059,2.98458657226352,0.791608110070563));
#21954=CARTESIAN_POINT('Ctrl Pts',(4.02309178955499,2.83126247167256,0.780931632574437));
#21955=CARTESIAN_POINT('Ctrl Pts',(4.08548662973932,2.74045865314341,0.774766370665049));
#21956=CARTESIAN_POINT('Ctrl Pts',(4.20013243126663,2.56098479366827,0.762814316050396));
#21957=CARTESIAN_POINT('Ctrl Pts',(4.25275332125629,2.47261892936278,0.757032639913442));
#21958=CARTESIAN_POINT('Ctrl Pts',(4.33532968791823,2.32350458598782,0.747411870026766));
#21959=CARTESIAN_POINT('Ctrl Pts',(4.36686990759476,2.26367050146169,0.743586333707472));
#21960=CARTESIAN_POINT('Ctrl Pts',(4.43432676579941,2.1290398462895,0.735047442657509));
#21961=CARTESIAN_POINT('Ctrl Pts',(4.46960488461165,2.05394656017347,0.730330602418138));
#21962=CARTESIAN_POINT('Ctrl Pts',(4.54363744908731,1.88540937436285,0.719836914730252));
#21963=CARTESIAN_POINT('Ctrl Pts',(4.58144269902896,1.79158932299904,0.71405651546578));
#21964=CARTESIAN_POINT('Ctrl Pts',(4.67356443828738,1.54094312972681,0.698774043179428));
#21965=CARTESIAN_POINT('Ctrl Pts',(4.72288402861999,1.38241729777547,0.689267197930461));
#21966=CARTESIAN_POINT('Ctrl Pts',(4.77299690510432,1.1869991856083,0.677790897478523));
#21967=CARTESIAN_POINT('Ctrl Pts',(4.78151662810783,1.15220019699886,0.675756637819336));
#21968=CARTESIAN_POINT('Ctrl Pts',(4.79922305390596,1.07629681946347,0.67134147583945));
#21969=CARTESIAN_POINT('Ctrl Pts',(4.80826354195133,1.03516111357796,0.668962561024106));
#21970=CARTESIAN_POINT('Ctrl Pts',(4.82709104058373,0.94391799637511,0.663710637263908));
#21971=CARTESIAN_POINT('Ctrl Pts',(4.83662847959172,0.893764014389616,0.660840171746807));
#21972=CARTESIAN_POINT('Ctrl Pts',(4.8659840072216,0.725128821764615,0.651228679364703));
#21973=CARTESIAN_POINT('Ctrl Pts',(4.88224223726022,0.606071875210853,0.644507959084496));
#21974=CARTESIAN_POINT('Ctrl Pts',(4.8989175476528,0.438333912222894,0.635061534370354));
#21975=CARTESIAN_POINT('Ctrl Pts',(4.90299727991083,0.390060776575174,0.632345676530746));
#21976=CARTESIAN_POINT('Ctrl Pts',(4.91350445818342,0.239207114951488,0.623858992564783));
#21977=CARTESIAN_POINT('Ctrl Pts',(4.91743008254092,0.136481191992652,0.618079906910746));
#21978=CARTESIAN_POINT('Ctrl Pts',(4.91859788618268,-0.0339022982125286,
0.608462805207919));
#21979=CARTESIAN_POINT('Ctrl Pts',(4.91766703455457,-0.101515191490959,
0.604638334234605));
#21980=CARTESIAN_POINT('Ctrl Pts',(4.91249170121569,-0.251961745133505,
0.596102261461636));
#21981=CARTESIAN_POINT('Ctrl Pts',(4.90754534292472,-0.334750513753387,
0.591387176854443));
#21982=CARTESIAN_POINT('Ctrl Pts',(4.89193099862737,-0.518083088487674,
0.580898301712649));
#21983=CARTESIAN_POINT('Ctrl Pts',(4.8802512632039,-0.618503289527568,0.575120963629649));
#21984=CARTESIAN_POINT('Ctrl Pts',(4.84122182036858,-0.882803168354224,
0.559831221571236));
#21985=CARTESIAN_POINT('Ctrl Pts',(4.80864971356233,-1.04578149136887,0.550313978955285));
#21986=CARTESIAN_POINT('Ctrl Pts',(4.75911102118852,-1.24150179945074,0.538829159195305));
#21987=CARTESIAN_POINT('Ctrl Pts',(4.74994898948943,-1.27610699534426,0.536796572194886));
#21988=CARTESIAN_POINT('Ctrl Pts',(4.72917785234302,-1.35123518461451,0.532381129816443));
#21989=CARTESIAN_POINT('Ctrl Pts',(4.7174238988848,-1.39171530736654,0.530000275641919));
#21990=CARTESIAN_POINT('Ctrl Pts',(4.69026905621618,-1.48093604635368,0.524742963330227));
#21991=CARTESIAN_POINT('Ctrl Pts',(4.67462575583941,-1.52959782333168,0.521869056859459));
#21992=CARTESIAN_POINT('Ctrl Pts',(4.61958074967787,-1.6920889190974,0.512235723518684));
#21993=CARTESIAN_POINT('Ctrl Pts',(4.57675681652586,-1.80471284968568,0.505496692101554));
#21994=CARTESIAN_POINT('Ctrl Pts',(4.4784101881611,-2.03726804454011,0.491346642355479));
#21995=CARTESIAN_POINT('Ctrl Pts',(4.42210257272034,-2.15676311186973,0.483938811092049));
#21996=CARTESIAN_POINT('Ctrl Pts',(4.33187517835345,-2.32981204292907,0.472936981507766));
#21997=CARTESIAN_POINT('Ctrl Pts',(4.30162036882072,-2.38521043338096,0.469372014032746));
#21998=CARTESIAN_POINT('Ctrl Pts',(4.25129151571578,-2.47329188882621,0.463628789000986));
#21999=CARTESIAN_POINT('Ctrl Pts',(4.23188670723431,-2.50634937533143,0.461455933981613));
#22000=CARTESIAN_POINT('Ctrl Pts',(4.1661067037804,-2.61546813496452,0.454223616716428));
#22001=CARTESIAN_POINT('Ctrl Pts',(4.11805203383028,-2.69049545619224,0.449152393739429));
#22002=CARTESIAN_POINT('Ctrl Pts',(3.9976919724941,-2.86762716283573,0.436930591734692));
#22003=CARTESIAN_POINT('Ctrl Pts',(3.92347685323226,-2.96835909051039,0.429771484919504));
#22004=CARTESIAN_POINT('Ctrl Pts',(3.77446042501811,-3.15525238391744,0.416089089147852));
#22005=CARTESIAN_POINT('Ctrl Pts',(3.70034154221736,-3.2418578022171,0.409570143745308));
#22006=CARTESIAN_POINT('Ctrl Pts',(3.59486287702776,-3.3567707773681,0.400690987727624));
#22007=CARTESIAN_POINT('Ctrl Pts',(3.56604898498235,-3.38736532533066,0.398303584216129));
#22008=CARTESIAN_POINT('Ctrl Pts',(3.52758504865158,-3.4271714896889,0.395167716502782));
#22009=CARTESIAN_POINT('Ctrl Pts',(3.51828483542188,-3.43671827677309,0.39441334647493));
#22010=CARTESIAN_POINT('Ctrl Pts',(3.50720905887663,-3.44799562411524,0.393519403773952));
#22011=CARTESIAN_POINT('Ctrl Pts',(3.50547087311366,-3.4497627692854,0.393379241384583));
#22012=CARTESIAN_POINT('Ctrl Pts',(3.50154773318927,-3.45374524486064,0.39306318043343));
#22013=CARTESIAN_POINT('Ctrl Pts',(3.49936201069401,-3.45595981781253,0.392887293943682));
#22014=CARTESIAN_POINT('Ctrl Pts',(3.49529564620845,-3.46007204346587,0.392560444902864));
#22015=CARTESIAN_POINT('Ctrl Pts',(3.4934155570471,-3.46197024050948,0.392409473979546));
#22016=CARTESIAN_POINT('Ctrl Pts',(3.4898060579431,-3.46560856984013,0.392119914366113));
#22017=CARTESIAN_POINT('Ctrl Pts',(3.48807689098957,-3.46734894176531,0.391981322084046));
#22018=CARTESIAN_POINT('Ctrl Pts',(3.48467787356313,-3.4707648689987,0.391709134410787));
#22019=CARTESIAN_POINT('Ctrl Pts',(3.48300811507393,-3.47244051478418,0.391575537707908));
#22020=CARTESIAN_POINT('Ctrl Pts',(3.4796623408941,-3.47579324435343,0.391308072399589));
#22021=CARTESIAN_POINT('Ctrl Pts',(3.47798632009024,-3.47747032214568,0.391174203910555));
#22022=CARTESIAN_POINT('Ctrl Pts',(3.47457233874385,-3.48088151952984,0.390901751935026));
#22023=CARTESIAN_POINT('Ctrl Pts',(3.47283429109789,-3.4826155510985,0.390763169734242));
#22024=CARTESIAN_POINT('Ctrl Pts',(3.4692417279892,-3.48619444925671,0.390476970149689));
#22025=CARTESIAN_POINT('Ctrl Pts',(3.46738703753967,-3.48803913928207,0.390329355266043));
#22026=CARTESIAN_POINT('Ctrl Pts',(3.46350156233611,-3.49189750266945,0.390020397528303));
#22027=CARTESIAN_POINT('Ctrl Pts',(3.46147049097223,-3.49391088632748,0.389859058671085));
#22028=CARTESIAN_POINT('Ctrl Pts',(3.45716175431413,-3.4981746552999,0.389517138197447));
#22029=CARTESIAN_POINT('Ctrl Pts',(3.45488364502583,-3.50042459050742,0.389336562628139));
#22030=CARTESIAN_POINT('Ctrl Pts',(3.44999300849109,-3.50524531782098,0.388949338658751));
#22031=CARTESIAN_POINT('Ctrl Pts',(3.4473798009595,-3.50781541770806,0.388742699290535));
#22032=CARTESIAN_POINT('Ctrl Pts',(3.44170577658994,-3.51338337868411,0.388294597423941));
#22033=CARTESIAN_POINT('Ctrl Pts',(3.4386439100999,-3.51638016684864,0.388053148464375));
#22034=CARTESIAN_POINT('Ctrl Pts',(3.39615462748598,-3.55785779711908,0.384707521223595));
#22035=CARTESIAN_POINT('Ctrl Pts',(3.35608700325326,-3.59567774704789,0.381611414952683));
#22036=CARTESIAN_POINT('Ctrl Pts',(3.20803239819903,-3.730795788619,0.370361704603109));
#22037=CARTESIAN_POINT('Ctrl Pts',(3.09638189732583,-3.82396762409812,0.362235442278122));
#22038=CARTESIAN_POINT('Ctrl Pts',(2.89234687366823,-3.97943089669666,0.347846628514966));
#22039=CARTESIAN_POINT('Ctrl Pts',(2.8016665598546,-4.04378594179957,0.341599942079325));
#22040=CARTESIAN_POINT('Ctrl Pts',(2.66451101283828,-4.13429444620673,0.332328067910208));
#22041=CARTESIAN_POINT('Ctrl Pts',(2.61966587564448,-4.1628548065556,0.329323306095288));
#22042=CARTESIAN_POINT('Ctrl Pts',(2.51655861475035,-4.22619435072219,0.322470893460467));
#22043=CARTESIAN_POINT('Ctrl Pts',(2.45802225513673,-4.26050612127827,0.318620301091709));
#22044=CARTESIAN_POINT('Ctrl Pts',(2.33119038067773,-4.33136600754815,0.310355522240256));
#22045=CARTESIAN_POINT('Ctrl Pts',(2.26270331285743,-4.36753404505853,0.305939760305673));
#22046=CARTESIAN_POINT('Ctrl Pts',(2.04696815636872,-4.47502703512429,0.292170303537145));
#22047=CARTESIAN_POINT('Ctrl Pts',(1.89699652614637,-4.54063316588837,0.282793734797807));
#22048=CARTESIAN_POINT('Ctrl Pts',(1.67696400021694,-4.62408049431107,0.269346058299386));
#22049=CARTESIAN_POINT('Ctrl Pts',(1.6093434487895,-4.64804717326741,0.265254487534897));
#22050=CARTESIAN_POINT('Ctrl Pts',(1.50912331455892,-4.68111871561968,0.25925777296061));
#22051=CARTESIAN_POINT('Ctrl Pts',(1.47691570451368,-4.6913799305283,0.257340843342974));
#22052=CARTESIAN_POINT('Ctrl Pts',(1.40993169889658,-4.71196258281475,0.253375818361156));
#22053=CARTESIAN_POINT('Ctrl Pts',(1.37514185940846,-4.72223291226185,0.251328168260566));
#22054=CARTESIAN_POINT('Ctrl Pts',(1.32431137831679,-4.73662923991965,0.248350921459366));
#22055=CARTESIAN_POINT('Ctrl Pts',(1.30835865813774,-4.74106051505588,0.247418608939291));
#22056=CARTESIAN_POINT('Ctrl Pts',(1.22630414057961,-4.76340756320277,0.242632996103116));
#22057=CARTESIAN_POINT('Ctrl Pts',(1.15985534548363,-4.78002187760958,0.238790169932708));
#22058=CARTESIAN_POINT('Ctrl Pts',(0.876893333134046,-4.84452337805585,
0.222520662097336));
#22059=CARTESIAN_POINT('Ctrl Pts',(0.657622635982413,-4.87912696044817,
0.210134065576976));
#22060=CARTESIAN_POINT('Ctrl Pts',(0.36920778394442,-4.90484142278869,0.193805420862475));
#22061=CARTESIAN_POINT('Ctrl Pts',(0.301530401692974,-4.90946667701105,
0.189972417139949));
#22062=CARTESIAN_POINT('Ctrl Pts',(0.22249308080866,-4.91322781521364,0.185489744185811));
#22063=CARTESIAN_POINT('Ctrl Pts',(0.211204815300942,-4.91372600584816,
0.184849374109209));
#22064=CARTESIAN_POINT('Ctrl Pts',(0.184504539836169,-4.9148122050559,0.183334320200665));
#22065=CARTESIAN_POINT('Ctrl Pts',(0.169091294900664,-4.91536662605794,
0.182459427987104));
#22066=CARTESIAN_POINT('Ctrl Pts',(0.0616604243043279,-4.91872505271733,
0.176359092274275));
#22067=CARTESIAN_POINT('Ctrl Pts',(-0.0304166115604183,-4.91901744999519,
0.17111840040058));
#22068=CARTESIAN_POINT('Ctrl Pts',(-0.249210191133736,-4.91356859160635,
0.158627210766751));
#22069=CARTESIAN_POINT('Ctrl Pts',(-0.375803584891369,-4.90551050793662,
0.151368589394854));
#22070=CARTESIAN_POINT('Ctrl Pts',(-0.61074667165503,-4.88140701142047,
0.137849933703064));
#22071=CARTESIAN_POINT('Ctrl Pts',(-0.719148645031559,-4.86661807870668,
0.131593773414491));
#22072=CARTESIAN_POINT('Ctrl Pts',(-0.868949575330054,-4.8410663525139,
0.12294221769599));
#22073=CARTESIAN_POINT('Ctrl Pts',(-0.910836712257016,-4.83336045969209,
0.120522507688562));
#22074=CARTESIAN_POINT('Ctrl Pts',(-0.991361723899217,-4.81746245629585,
0.115872036592666));
#22075=CARTESIAN_POINT('Ctrl Pts',(-1.03001141151743,-4.80934705763011,
0.113640555909532));
#22076=CARTESIAN_POINT('Ctrl Pts',(-1.28868875145496,-4.75177040217614,
0.0986950052671175));
#22077=CARTESIAN_POINT('Ctrl Pts',(-1.50518972358113,-4.68769099446982,
0.0861225413595998));
#22078=CARTESIAN_POINT('Ctrl Pts',(-1.81125436013622,-4.57370287505729,
0.0677891040393032));
#22079=CARTESIAN_POINT('Ctrl Pts',(-1.90486781891452,-4.53551304514553,
0.0621040996125177));
#22080=CARTESIAN_POINT('Ctrl Pts',(-2.05706093635756,-4.46788193455122,
0.0527025580373686));
#22081=CARTESIAN_POINT('Ctrl Pts',(-2.11634755714247,-4.44010603164832,
0.0489992994415321));
#22082=CARTESIAN_POINT('Ctrl Pts',(-2.23227254641777,-4.38294549566522,
0.041670234120012));
#22083=CARTESIAN_POINT('Ctrl Pts',(-2.28892885677717,-4.35362567505692,
0.0380455713974877));
#22084=CARTESIAN_POINT('Ctrl Pts',(-2.52146244390851,-4.22749472134931,
0.0229824627520859));
#22085=CARTESIAN_POINT('Ctrl Pts',(-2.69189827355834,-4.12106367661615,
0.0114832924308145));
#22086=CARTESIAN_POINT('Ctrl Pts',(-2.8553491342286,-4.00451799648347,2.16840434497101E-18));
#22087=CARTESIAN_POINT('',(2.85706463458462,-4.00329423553975,0.));
#22088=CARTESIAN_POINT('Origin',(0.,0.,0.));
#22089=CARTESIAN_POINT('Ctrl Pts',(2.85706463458456,-4.0032942355398,0.));
#22090=CARTESIAN_POINT('Ctrl Pts',(2.97498500626953,-3.91913701305856,0.00820407285754789));
#22091=CARTESIAN_POINT('Ctrl Pts',(3.08919334481163,-3.82975975962187,0.0164081457150967));
#22092=CARTESIAN_POINT('Ctrl Pts',(3.19923812022538,-3.73551315251289,0.0246122185726447));
#22093=CARTESIAN_POINT('Ctrl Pts',(3.30927402805244,-3.64127413994854,0.0328156303326808));
#22094=CARTESIAN_POINT('Ctrl Pts',(3.41514679505572,-3.54216676932236,0.0410190420927171));
#22095=CARTESIAN_POINT('Ctrl Pts',(3.51643872130203,-3.43858136181591,0.0492224538527535));
#22096=CARTESIAN_POINT('Ctrl Pts',(3.61774645859056,-3.33497978526902,0.0574271461145484));
#22097=CARTESIAN_POINT('Ctrl Pts',(3.71447169625567,-3.22689900641972,0.0656318383763429));
#22098=CARTESIAN_POINT('Ctrl Pts',(3.80623385628371,-3.11476594526452,0.0738365306381379));
#22099=CARTESIAN_POINT('Ctrl Pts',(3.89799542774863,-3.00263360333156,0.0820411702749799));
#22100=CARTESIAN_POINT('Ctrl Pts',(3.98479378129704,-2.88644928568954,0.0902458099118233));
#22101=CARTESIAN_POINT('Ctrl Pts',(4.06628890577333,-2.76667265813734,0.0984504495486656));
#22102=CARTESIAN_POINT('Ctrl Pts',(4.14780581620183,-2.64686401090421,0.106657282517786));
#22103=CARTESIAN_POINT('Ctrl Pts',(4.22401648141588,-2.52346140481058,0.114864115486905));
#22104=CARTESIAN_POINT('Ctrl Pts',(4.29462408636437,-2.39695369569772,0.123070948456026));
#22105=CARTESIAN_POINT('Ctrl Pts',(4.34036337126301,-2.31500257792212,0.12838729747486));
#22106=CARTESIAN_POINT('Ctrl Pts',(4.38375228545424,-2.23174901418395,0.133703646493694));
#22107=CARTESIAN_POINT('Ctrl Pts',(4.42472038127204,-2.14733150911911,0.139019995512528));
#22108=CARTESIAN_POINT('Ctrl Pts',(4.48738131754991,-2.01821445351738,0.147151381666807));
#22109=CARTESIAN_POINT('Ctrl Pts',(4.54440167627658,-1.8863219557833,0.155282767821084));
#22110=CARTESIAN_POINT('Ctrl Pts',(4.59555177087547,-1.75216636872852,0.163414153975364));
#22111=CARTESIAN_POINT('Ctrl Pts',(4.64668895824192,-1.6180446345407,0.171543488252865));
#22112=CARTESIAN_POINT('Ctrl Pts',(4.6919587153246,-1.48166126644035,0.179672822530368));
#22113=CARTESIAN_POINT('Ctrl Pts',(4.73117981574852,-1.34354777122133,0.187802156807869));
#22114=CARTESIAN_POINT('Ctrl Pts',(4.77040064845697,-1.20543521873771,0.195931435596143));
#22115=CARTESIAN_POINT('Ctrl Pts',(4.80357280941589,-1.06559288723808,0.204060714384417));
#22116=CARTESIAN_POINT('Ctrl Pts',(4.83056506717866,-0.924567030697748,
0.21218999317269));
#22117=CARTESIAN_POINT('Ctrl Pts',(4.857555278148,-0.783551867994089,0.220318655526632));
#22118=CARTESIAN_POINT('Ctrl Pts',(4.87836645982945,-0.641353692644201,
0.228447317880575));
#22119=CARTESIAN_POINT('Ctrl Pts',(4.8929186014829,-0.498528456321814,0.236575980234517));
#22120=CARTESIAN_POINT('Ctrl Pts',(4.907474371369,-0.355667609901753,0.244706669278334));
#22121=CARTESIAN_POINT('Ctrl Pts',(4.91576794811031,-0.212179727344983,
0.252837358322151));
#22122=CARTESIAN_POINT('Ctrl Pts',(4.9177711962389,-0.0686259713447046,
0.260968047365969));
#22123=CARTESIAN_POINT('Ctrl Pts',(4.9191732643376,0.0318469250800603,0.266658695252324));
#22124=CARTESIAN_POINT('Ctrl Pts',(4.91749506144905,0.132351984443032,0.27234934313868));
#22125=CARTESIAN_POINT('Ctrl Pts',(4.91274213444373,0.232696761819521,0.278039991025036));
#22126=CARTESIAN_POINT('Ctrl Pts',(4.90591850659579,0.376758603403428,0.286209875255664));
#22127=CARTESIAN_POINT('Ctrl Pts',(4.89275270583794,0.520543405431197,0.294379759486292));
#22128=CARTESIAN_POINT('Ctrl Pts',(4.87329139158351,0.663486303715512,0.30254964371692));
#22129=CARTESIAN_POINT('Ctrl Pts',(4.85383357489287,0.806403512475477,0.31071805966586));
#22130=CARTESIAN_POINT('Ctrl Pts',(4.82808254692009,0.948478790263434,0.318886475614799));
#22131=CARTESIAN_POINT('Ctrl Pts',(4.79613665314498,1.08915392248261,0.327054891563739));
#22132=CARTESIAN_POINT('Ctrl Pts',(4.76418902515154,1.22983669140763,0.335223750944214));
#22133=CARTESIAN_POINT('Ctrl Pts',(4.72604592905617,1.36911883791727,0.34339261032469));
#22134=CARTESIAN_POINT('Ctrl Pts',(4.68185662625592,1.50645331613149,0.351561469705165));
#22135=CARTESIAN_POINT('Ctrl Pts',(4.63766962985419,1.64378062636571,0.35972990272351));
#22136=CARTESIAN_POINT('Ctrl Pts',(4.5874371611,1.77916015569849,0.367898335741856));
#22137=CARTESIAN_POINT('Ctrl Pts',(4.53135804752916,1.91206101042637,0.376066768760201));
#22138=CARTESIAN_POINT('Ctrl Pts',(4.47526545410476,2.04499381081007,0.384237165241838));
#22139=CARTESIAN_POINT('Ctrl Pts',(4.41332353671453,2.17544643965099,0.392407561723476));
#22140=CARTESIAN_POINT('Ctrl Pts',(4.34577911951618,2.30290835833239,0.400577958205113));
#22141=CARTESIAN_POINT('Ctrl Pts',(4.30036031189514,2.38861741621942,0.406071967649259));
#22142=CARTESIAN_POINT('Ctrl Pts',(4.25240926499502,2.47297462776637,0.411565977093405));
#22143=CARTESIAN_POINT('Ctrl Pts',(4.2020126881557,2.5558310646595,0.41705998653755));
#22144=CARTESIAN_POINT('Ctrl Pts',(4.12724913271787,2.67874897300851,0.425210375024508));
#22145=CARTESIAN_POINT('Ctrl Pts',(4.04707367061566,2.79840842495914,0.433360763511466));
#22146=CARTESIAN_POINT('Ctrl Pts',(3.96179514680109,2.91433736504258,0.441511151998423));
#22147=CARTESIAN_POINT('Ctrl Pts',(3.8765348031365,3.03024159074984,0.449659802940235));
#22148=CARTESIAN_POINT('Ctrl Pts',(3.7861737667134,3.14241662086398,0.457808453882048));
#22149=CARTESIAN_POINT('Ctrl Pts',(3.6910631515518,3.25042087640301,0.46595710482386));
#22150=CARTESIAN_POINT('Ctrl Pts',(3.59594979774117,3.35842824185514,0.474105990400838));
#22151=CARTESIAN_POINT('Ctrl Pts',(3.4960868103159,3.46226433786603,0.482254875977814));
#22152=CARTESIAN_POINT('Ctrl Pts',(3.39186471754661,3.56152169730334,0.490403761554792));
#22153=CARTESIAN_POINT('Ctrl Pts',(3.28764897207037,3.66077301180784,0.498552150851533));
#22154=CARTESIAN_POINT('Ctrl Pts',(3.17907489601818,3.75544591673984,0.506700540148273));
#22155=CARTESIAN_POINT('Ctrl Pts',(3.06656885309214,3.84517080657611,0.514848929445014));
#22156=CARTESIAN_POINT('Ctrl Pts',(2.95403465952901,3.93491814687588,0.52299935758646));
#22157=CARTESIAN_POINT('Ctrl Pts',(2.83756679555529,4.01971478857669,0.531149785727906));
#22158=CARTESIAN_POINT('Ctrl Pts',(2.71762405879757,4.09923194483364,0.539300213869352));
#22159=CARTESIAN_POINT('Ctrl Pts',(2.63531299150039,4.1538008347629,0.544893469929588));
#22160=CARTESIAN_POINT('Ctrl Pts',(2.55136612578541,4.20588424380603,0.550486725989824));
#22161=CARTESIAN_POINT('Ctrl Pts',(2.46593947468516,4.25538782835236,0.55607998205006));
#22162=CARTESIAN_POINT('Ctrl Pts',(2.34133909001987,4.32759205967059,0.56423811358935));
#22163=CARTESIAN_POINT('Ctrl Pts',(2.21354229625245,4.39433327040732,0.572396245128639));
#22164=CARTESIAN_POINT('Ctrl Pts',(2.08304736530668,4.45534473822048,0.580554376667929));
#22165=CARTESIAN_POINT('Ctrl Pts',(1.95257870163044,4.51634392506105,0.588710866060368));
#22166=CARTESIAN_POINT('Ctrl Pts',(1.81941328694919,4.57161552832907,0.596867355452807));
#22167=CARTESIAN_POINT('Ctrl Pts',(1.68407187559563,4.6209398373413,0.605023844845245));
#22168=CARTESIAN_POINT('Ctrl Pts',(1.54872546381792,4.67026596872603,0.61318063559339));
#22169=CARTESIAN_POINT('Ctrl Pts',(1.41120320734963,4.71364424822052,0.621337426341534));
#22170=CARTESIAN_POINT('Ctrl Pts',(1.2720441076259,4.75090379304341,0.629494217089679));
#22171=CARTESIAN_POINT('Ctrl Pts',(1.13289314689424,4.78816115866895,0.637650530771966));
#22172=CARTESIAN_POINT('Ctrl Pts',(0.992105857661266,4.81930042003483,0.645806844454254));
#22173=CARTESIAN_POINT('Ctrl Pts',(0.850234559639156,4.84420109575307,0.653963158136542));
#22174=CARTESIAN_POINT('Ctrl Pts',(0.708328534722006,4.86910786659529,0.662121468300521));
#22175=CARTESIAN_POINT('Ctrl Pts',(0.565338300220735,4.88777294231582,0.6702797784645));
#22176=CARTESIAN_POINT('Ctrl Pts',(0.421825098856181,4.90012720737686,0.678438088628479));
#22177=CARTESIAN_POINT('Ctrl Pts',(0.324125086081751,4.90853766608593,0.683992051606518));
#22178=CARTESIAN_POINT('Ctrl Pts',(0.226182877781484,4.91402443261673,0.689546014584557));
#22179=CARTESIAN_POINT('Ctrl Pts',(0.128176613847126,4.91657948355996,0.695099977562596));
#22180=CARTESIAN_POINT('Ctrl Pts',(-0.0157489469344976,4.92033166352343,
0.703256162729597));
#22181=CARTESIAN_POINT('Ctrl Pts',(-0.159866312834054,4.91776039312803,
0.711412347896599));
#22182=CARTESIAN_POINT('Ctrl Pts',(-0.303610595441317,4.90886989732217,
0.7195685330636));
#22183=CARTESIAN_POINT('Ctrl Pts',(-0.447325607793905,4.89998121186362,
0.727723057408949));
#22184=CARTESIAN_POINT('Ctrl Pts',(-0.590667354579191,4.88477588866314,
0.735877581754297));
#22185=CARTESIAN_POINT('Ctrl Pts',(-0.733073701145311,4.86331019072289,
0.744032106099646));
#22186=CARTESIAN_POINT('Ctrl Pts',(-0.875485160104212,4.84184372216334,
0.752186923192701));
#22187=CARTESIAN_POINT('Ctrl Pts',(-1.01696082017052,4.81411647531375,0.760341740285757));
#22188=CARTESIAN_POINT('Ctrl Pts',(-1.15694589139997,4.78023631914498,0.768496557378813));
#22189=CARTESIAN_POINT('Ctrl Pts',(-1.29692276993108,4.74635814582979,0.776650897207));
#22190=CARTESIAN_POINT('Ctrl Pts',(-1.43540890909048,4.70632786328913,0.784805237035187));
#22191=CARTESIAN_POINT('Ctrl Pts',(-1.5718619475062,4.66030396867865,0.792959576863375));
#22192=CARTESIAN_POINT('Ctrl Pts',(-1.7083486942186,4.61426870468342,0.801115931076213));
#22193=CARTESIAN_POINT('Ctrl Pts',(-1.84280101926073,4.56223697680967,0.809272285289051));
#22194=CARTESIAN_POINT('Ctrl Pts',(-1.97469331186278,4.50441665330644,0.81742863950189));
#22195=CARTESIAN_POINT('Ctrl Pts',(-2.06466235906657,4.46497508085386,0.822992417359629));
#22196=CARTESIAN_POINT('Ctrl Pts',(-2.15344054255843,4.42284101055005,0.828556195217366));
#22197=CARTESIAN_POINT('Ctrl Pts',(-2.24086673186674,4.37809311830081,0.834119973075105));
#22198=CARTESIAN_POINT('Ctrl Pts',(-2.36902428234712,4.31249743918915,0.842275883189753));
#22199=CARTESIAN_POINT('Ctrl Pts',(-2.49432372899232,4.24125833080194,0.850431793304401));
#22200=CARTESIAN_POINT('Ctrl Pts',(-2.61627114275892,4.16464984963525,0.858587703419049));
#22201=CARTESIAN_POINT('Ctrl Pts',(-2.73819360076062,4.08805704590842,0.866741944478412));
#22202=CARTESIAN_POINT('Ctrl Pts',(-2.85676511109277,4.00609723939499,0.874896185537775));
#22203=CARTESIAN_POINT('Ctrl Pts',(-2.97151906855203,3.91908885938194,0.883050426597138));
#22204=CARTESIAN_POINT('Ctrl Pts',(-3.08627700950265,3.83207745901877,0.891204950717317));
#22205=CARTESIAN_POINT('Ctrl Pts',(-3.19721686341115,3.74001733367732,0.899359474837495));
#22206=CARTESIAN_POINT('Ctrl Pts',(-3.30390317391488,3.64326870816512,0.907513998957674));
#22207=CARTESIAN_POINT('Ctrl Pts',(-3.41058317786913,3.54652580175589,0.915668041039345));
#22208=CARTESIAN_POINT('Ctrl Pts',(-3.51300989412653,3.44509517520259,0.923822083121016));
#22209=CARTESIAN_POINT('Ctrl Pts',(-3.61078301066148,3.33937555725894,0.931976125202687));
#22210=CARTESIAN_POINT('Ctrl Pts',(-3.70858022337767,3.23362988471903,0.940132176847752));
#22211=CARTESIAN_POINT('Ctrl Pts',(-3.80172131710608,3.1235933543099,0.948288228492817));
#22212=CARTESIAN_POINT('Ctrl Pts',(-3.88984431783294,3.00970002583693,0.956444280137883));
#22213=CARTESIAN_POINT('Ctrl Pts',(-3.94997448168419,2.93198564427755,0.962009509621126));
#22214=CARTESIAN_POINT('Ctrl Pts',(-4.00776906322076,2.85247629359635,0.96757473910437));
#22215=CARTESIAN_POINT('Ctrl Pts',(-4.06312416161374,2.771318298177,0.973139968587613));
#22216=CARTESIAN_POINT('Ctrl Pts',(-4.14425959693511,2.65236287258256,0.981297072989826));
#22217=CARTESIAN_POINT('Ctrl Pts',(-4.22018261436947,2.52981973419644,0.98945417739204));
#22218=CARTESIAN_POINT('Ctrl Pts',(-4.29059067049875,2.40416612585924,0.997611281794252));
#22219=CARTESIAN_POINT('Ctrl Pts',(-4.36098272190655,2.27854108031892,1.00576653197422));
#22220=CARTESIAN_POINT('Ctrl Pts',(-4.42586215023802,2.14980726757971,1.01392178215418));
#22221=CARTESIAN_POINT('Ctrl Pts',(-4.48497167286734,2.01846777434706,1.02207703233415));
#22222=CARTESIAN_POINT('Ctrl Pts',(-4.54408319317163,1.88712384234366,1.03023255813027));
#22223=CARTESIAN_POINT('Ctrl Pts',(-4.59742427684112,1.75317435724535,1.03838808392639));
#22224=CARTESIAN_POINT('Ctrl Pts',(-4.64478500472299,1.61714418726361,1.04654360972251));
#22225=CARTESIAN_POINT('Ctrl Pts',(-4.69004273227576,1.48715428534852,1.05433699848653));
#22226=CARTESIAN_POINT('Ctrl Pts',(-4.72983964623876,1.35526476022636,1.06213038725054));
#22227=CARTESIAN_POINT('Ctrl Pts',(-4.76403458704967,1.22194824599671,1.06992377601457));
#22228=CARTESIAN_POINT('Origin',(0.,0.,-3.23514056400928));
#22229=CARTESIAN_POINT('',(-4.76403458654079,1.22194824798069,3.16499504358801));
#22230=CARTESIAN_POINT('',(-4.76390408110233,1.22191513442789,2.81993486269365));
#22231=CARTESIAN_POINT('',(-4.76403458704967,1.22194824599672,-3.23514056400928));
#22232=CARTESIAN_POINT('Ctrl Pts',(-4.76403458654079,1.22194824798069,3.16499504358802));
#22233=CARTESIAN_POINT('Ctrl Pts',(-4.74301709350956,1.30388957723802,3.16023305192965));
#22234=CARTESIAN_POINT('Ctrl Pts',(-4.71988804094678,1.38527880975492,3.15548845562783));
#22235=CARTESIAN_POINT('Ctrl Pts',(-4.63323274031351,1.66277434585329,3.13919596261171));
#22236=CARTESIAN_POINT('Ctrl Pts',(-4.55948977731996,1.85545571252533,3.12767309666291));
#22237=CARTESIAN_POINT('Ctrl Pts',(-4.44758466376989,2.10051907133321,3.11248323439081));
#22238=CARTESIAN_POINT('Ctrl Pts',(-4.42018300993925,2.15758470528142,3.10890733213118));
#22239=CARTESIAN_POINT('Ctrl Pts',(-4.3595942934519,2.2777627037162,3.1012864053832));
#22240=CARTESIAN_POINT('Ctrl Pts',(-4.3261207992843,2.34071442323075,3.09724003174466));
#22241=CARTESIAN_POINT('Ctrl Pts',(-4.21449690232407,2.54006000019183,3.08424088263224));
#22242=CARTESIAN_POINT('Ctrl Pts',(-4.13117329665404,2.67344254936908,3.07525509982565));
#22243=CARTESIAN_POINT('Ctrl Pts',(-3.98696109472604,2.88140951109765,3.06076799622857));
#22244=CARTESIAN_POINT('Ctrl Pts',(-3.93002125736954,2.95859976963131,3.05527793768984));
#22245=CARTESIAN_POINT('Ctrl Pts',(-3.84233520324323,3.07046925216586,3.04716206094201));
#22246=CARTESIAN_POINT('Ctrl Pts',(-3.81329739265491,3.10645848015262,3.04452565423422));
#22247=CARTESIAN_POINT('Ctrl Pts',(-3.76265531339808,3.16744360635762,3.04001630630863));
#22248=CARTESIAN_POINT('Ctrl Pts',(-3.74129881898546,3.19264109802267,3.0381405632103));
#22249=CARTESIAN_POINT('Ctrl Pts',(-3.69317444865286,3.24827465476587,3.03397210519915));
#22250=CARTESIAN_POINT('Ctrl Pts',(-3.66628084413627,3.27859887039511,3.03168176438035));
#22251=CARTESIAN_POINT('Ctrl Pts',(-3.57115509424977,3.38322480984051,3.02370705803337));
#22252=CARTESIAN_POINT('Ctrl Pts',(-3.5010139442892,3.45575760080483,3.01804794337373));
#22253=CARTESIAN_POINT('Ctrl Pts',(-3.2782655063435,3.67235366980646,3.00063409780202));
#22254=CARTESIAN_POINT('Ctrl Pts',(-3.11863526189354,3.80884747525298,2.98890623589892));
#22255=CARTESIAN_POINT('Ctrl Pts',(-2.90012562277155,3.97271482868649,2.97350625357134));
#22256=CARTESIAN_POINT('Ctrl Pts',(-2.84874425899097,4.00971916423845,2.96992940156971));
#22257=CARTESIAN_POINT('Ctrl Pts',(-2.73796859246272,4.0862944476954,2.9623038988482));
#22258=CARTESIAN_POINT('Ctrl Pts',(-2.67839847365179,4.12558550823075,2.9582538863873));
#22259=CARTESIAN_POINT('Ctrl Pts',(-2.48593565236306,4.24660357031631,2.94531834486757));
#22260=CARTESIAN_POINT('Ctrl Pts',(-2.35000172649193,4.32330993403215,2.93640050832401));
#22261=CARTESIAN_POINT('Ctrl Pts',(-2.12446260129611,4.43679520551466,2.92194750379035));
#22262=CARTESIAN_POINT('Ctrl Pts',(-2.03701267716492,4.47761906952178,2.91642355302585));
#22263=CARTESIAN_POINT('Ctrl Pts',(-1.90584188975182,4.53421437203681,2.90826640044368));
#22264=CARTESIAN_POINT('Ctrl Pts',(-1.86300749683615,4.55198159030713,2.90562252230479));
#22265=CARTESIAN_POINT('Ctrl Pts',(-1.789210963365,4.58137538532291,2.90110371742155));
#22266=CARTESIAN_POINT('Ctrl Pts',(-1.75837110911383,4.59330026910624,2.89922596806594));
#22267=CARTESIAN_POINT('Ctrl Pts',(-1.68955156410859,4.61911612708915,2.89506067331083));
#22268=CARTESIAN_POINT('Ctrl Pts',(-1.6515161313528,4.63285147510859,2.89277548146293));
#22269=CARTESIAN_POINT('Ctrl Pts',(-1.49684309994213,4.68656006741641,2.88354136197221));
#22270=CARTESIAN_POINT('Ctrl Pts',(-1.3788899561019,4.72261026288304,2.87663262815581));
#22271=CARTESIAN_POINT('Ctrl Pts',(-1.08133037657761,4.8014538781398,2.85938607387253));
#22272=CARTESIAN_POINT('Ctrl Pts',(-0.900438154972333,4.83864079645118,
2.849059325029));
#22273=CARTESIAN_POINT('Ctrl Pts',(-0.655490517643015,4.87478135477,2.83510151755098));
#22274=CARTESIAN_POINT('Ctrl Pts',(-0.592923652246619,4.88278634707422,
2.83153916415954));
#22275=CARTESIAN_POINT('Ctrl Pts',(-0.460320253923246,4.89716569442741,
2.82398821542964));
#22276=CARTESIAN_POINT('Ctrl Pts',(-0.39026597483526,4.90324575079728,2.81999847135481));
#22277=CARTESIAN_POINT('Ctrl Pts',(-0.144186528182758,4.91929594826984,
2.80597134883063));
#22278=CARTESIAN_POINT('Ctrl Pts',(0.0322206753293376,4.92130295271656,
2.79588874217486));
#22279=CARTESIAN_POINT('Ctrl Pts',(0.294936679940447,4.910163528698,2.7808363032379));
#22280=CARTESIAN_POINT('Ctrl Pts',(0.381410029446808,4.90420432353481,2.77587686003766));
#22281=CARTESIAN_POINT('Ctrl Pts',(0.511595013780203,4.89176855960307,2.76841243604769));
#22282=CARTESIAN_POINT('Ctrl Pts',(0.555450862294444,4.88698306576289,2.76589827290617));
#22283=CARTESIAN_POINT('Ctrl Pts',(0.631935092946077,4.87759432519969,2.76151637530628));
#22284=CARTESIAN_POINT('Ctrl Pts',(0.664592636502008,4.87325199652507,2.75964627224388));
#22285=CARTESIAN_POINT('Ctrl Pts',(0.717334627583887,4.86569909000665,2.75662843285732));
#22286=CARTESIAN_POINT('Ctrl Pts',(0.737446953119855,4.86269149755914,2.75547816584134));
#22287=CARTESIAN_POINT('Ctrl Pts',(0.822324901901064,4.84946016344697,2.75062481418638));
#22288=CARTESIAN_POINT('Ctrl Pts',(0.886901865066519,4.83806649000429,2.74693467162407));
#22289=CARTESIAN_POINT('Ctrl Pts',(1.11416335338782,4.79326623990264,2.73392305257977));
#22290=CARTESIAN_POINT('Ctrl Pts',(1.27536359542131,4.75291587480413,2.72464455043326));
#22291=CARTESIAN_POINT('Ctrl Pts',(1.51043444693336,4.68125201074298,2.71085722985321));
#22292=CARTESIAN_POINT('Ctrl Pts',(1.58607870036148,4.65616653542828,2.70638068074325));
#22293=CARTESIAN_POINT('Ctrl Pts',(1.72974064343552,4.60461743233548,2.69778342555605));
#22294=CARTESIAN_POINT('Ctrl Pts',(1.79784452502545,4.5784559944235,2.69366572863656));
#22295=CARTESIAN_POINT('Ctrl Pts',(1.93105867348263,4.5238523325872,2.6855169715415));
#22296=CARTESIAN_POINT('Ctrl Pts',(1.99618483007456,4.49549479986849,2.68148745396551));
#22297=CARTESIAN_POINT('Ctrl Pts',(2.18020214811072,4.41058169327061,2.66996133168117));
#22298=CARTESIAN_POINT('Ctrl Pts',(2.29746691519527,4.35065021975536,2.66244421100876));
#22299=CARTESIAN_POINT('Ctrl Pts',(2.51431108253571,4.22861160825194,2.64820622752174));
#22300=CARTESIAN_POINT('Ctrl Pts',(2.61435069249071,4.16750367848983,2.64149334373158));
#22301=CARTESIAN_POINT('Ctrl Pts',(2.76963977100701,4.06485351755627,2.63085807101604));
#22302=CARTESIAN_POINT('Ctrl Pts',(2.82636187669348,4.02562011270546,2.62692563133518));
#22303=CARTESIAN_POINT('Ctrl Pts',(2.90956359762636,3.96544572155702,2.62109198688894));
#22304=CARTESIAN_POINT('Ctrl Pts',(2.93668276386117,3.9454042232414,2.619180034864));
#22305=CARTESIAN_POINT('Ctrl Pts',(3.00381171141163,3.89471922236461,2.61442135421752));
#22306=CARTESIAN_POINT('Ctrl Pts',(3.0435606852841,3.8637366704063,2.61157948549453));
#22307=CARTESIAN_POINT('Ctrl Pts',(3.20851296260857,3.73103844583217,2.59966497236366));
#22308=CARTESIAN_POINT('Ctrl Pts',(3.32914970354058,3.62380551229913,2.59064915558177));
#22309=CARTESIAN_POINT('Ctrl Pts',(3.51272530632261,3.44370910479892,2.57623487544521));
#22310=CARTESIAN_POINT('Ctrl Pts',(3.57917360483278,3.37459442848034,2.57085690809602));
#22311=CARTESIAN_POINT('Ctrl Pts',(3.69547914704709,3.24631970904161,2.56111239529661));
#22312=CARTESIAN_POINT('Ctrl Pts',(3.74604138963816,3.18784119723681,2.55675309506328));
#22313=CARTESIAN_POINT('Ctrl Pts',(3.83845391152409,3.075724057186,2.54853543458689));
#22314=CARTESIAN_POINT('Ctrl Pts',(3.88061060478513,3.02236134551574,2.54468080638743));
#22315=CARTESIAN_POINT('Ctrl Pts',(3.99483259654115,2.87144595538523,2.53392610208056));
#22316=CARTESIAN_POINT('Ctrl Pts',(4.06441597733861,2.772077107505,2.52700873797852));
#22317=CARTESIAN_POINT('Ctrl Pts',(4.1392598474208,2.65631061448967,2.51912578009965));
#22318=CARTESIAN_POINT('Ctrl Pts',(4.14819439027773,2.64233636479901,2.51817707129355));
#22319=CARTESIAN_POINT('Ctrl Pts',(4.23232773351966,2.50926749725801,2.50917009856783));
#22320=CARTESIAN_POINT('Ctrl Pts',(4.30244881299908,2.38703913574604,2.50109945833231));
#22321=CARTESIAN_POINT('Ctrl Pts',(4.3942314456236,2.20983270358182,2.48970874282804));
#22322=CARTESIAN_POINT('Ctrl Pts',(4.42029994069726,2.1572155959279,2.48636404050036));
#22323=CARTESIAN_POINT('Ctrl Pts',(4.46114803688123,2.07091591345386,2.48094336559317));
#22324=CARTESIAN_POINT('Ctrl Pts',(4.4765027698302,2.0375125808251,2.47886115985932));
#22325=CARTESIAN_POINT('Ctrl Pts',(4.51677639130249,1.94724627757795,2.47327538730181));
#22326=CARTESIAN_POINT('Ctrl Pts',(4.5409955736983,1.89007840409149,2.46978011695905));
#22327=CARTESIAN_POINT('Ctrl Pts',(4.62897814776777,1.67094016382996,2.45651070977139));
#22328=CARTESIAN_POINT('Ctrl Pts',(4.6852098140499,1.50608407077768,2.44678825836016));
#22329=CARTESIAN_POINT('Ctrl Pts',(4.75404268059528,1.2627262848341,2.43259833525474));
#22330=CARTESIAN_POINT('Ctrl Pts',(4.77367402998435,1.18635390185786,2.42816844932864));
#22331=CARTESIAN_POINT('Ctrl Pts',(4.80782650739566,1.03886954455042,2.41964039386002));
#22332=CARTESIAN_POINT('Ctrl Pts',(4.82262638804753,0.967843074402873,2.41554507975477));
#22333=CARTESIAN_POINT('Ctrl Pts',(4.84729339854263,0.834788026932954,2.40788518667186));
#22334=CARTESIAN_POINT('Ctrl Pts',(4.85755405593428,0.77284722098763,2.40432409187291));
#22335=CARTESIAN_POINT('Ctrl Pts',(4.88456636428003,0.58788347840877,2.3936978757305));
#22336=CARTESIAN_POINT('Ctrl Pts',(4.89784874304496,0.464405641996751,2.38661306471273));
#22337=CARTESIAN_POINT('Ctrl Pts',(4.91708768542803,0.187229677655368,2.37072046283848));
#22338=CARTESIAN_POINT('Ctrl Pts',(4.92053708834936,0.0334852921816912,
2.36191159773346));
#22339=CARTESIAN_POINT('Ctrl Pts',(4.91612791451401,-0.146920002736653,
2.35161537595174));
#22340=CARTESIAN_POINT('Ctrl Pts',(4.91525575959535,-0.173666309192137,
2.35009002250873));
#22341=CARTESIAN_POINT('Ctrl Pts',(4.91243195062716,-0.242909670607889,
2.34614465167375));
#22342=CARTESIAN_POINT('Ctrl Pts',(4.91014711883086,-0.285391143376713,
2.34372764056872));
#22343=CARTESIAN_POINT('Ctrl Pts',(4.90456153063559,-0.369000202396119,
2.33897997016327));
#22344=CARTESIAN_POINT('Ctrl Pts',(4.90129383182566,-0.410126539747637,
2.33664919109031));
#22345=CARTESIAN_POINT('Ctrl Pts',(4.8843041383983,-0.594536683360004,2.32620725617069));
#22346=CARTESIAN_POINT('Ctrl Pts',(4.86481343458624,-0.737219074917836,
2.31815132841014));
#22347=CARTESIAN_POINT('Ctrl Pts',(4.81163968367875,-1.0300051071471,2.30148054433339));
#22348=CARTESIAN_POINT('Ctrl Pts',(4.77711888570422,-1.17979716536796,2.29287322705982));
#22349=CARTESIAN_POINT('Ctrl Pts',(4.71627412891487,-1.39681414389121,2.28017403837439));
#22350=CARTESIAN_POINT('Ctrl Pts',(4.69539462386937,-1.46546940659489,2.27612258382524));
#22351=CARTESIAN_POINT('Ctrl Pts',(4.6505359573117,-1.60215409512627,2.26797811397907));
#22352=CARTESIAN_POINT('Ctrl Pts',(4.62654738959398,-1.67016212507325,2.26388597779004));
#22353=CARTESIAN_POINT('Ctrl Pts',(4.54311787112304,-1.89107682197355,2.25045161456738));
#22354=CARTESIAN_POINT('Ctrl Pts',(4.47752269422252,-2.04153884509821,2.24107251947132));
#22355=CARTESIAN_POINT('Ctrl Pts',(4.34644566913616,-2.30534924827536,2.22420933300337));
#22356=CARTESIAN_POINT('Ctrl Pts',(4.28372572544921,-2.41990073701189,2.21673694207674));
#22357=CARTESIAN_POINT('Ctrl Pts',(4.19499847312478,-2.56766802886009,2.20692605885642));
#22358=CARTESIAN_POINT('Ctrl Pts',(4.17301810061789,-2.60323861409947,2.20455086887021));
#22359=CARTESIAN_POINT('Ctrl Pts',(4.13126288140205,-2.66892253452215,2.20014170945751));
#22360=CARTESIAN_POINT('Ctrl Pts',(4.11160560827748,-2.69910723163804,2.19810618492831));
#22361=CARTESIAN_POINT('Ctrl Pts',(4.00080258020134,-2.86523090508467,2.18684227917305));
#22362=CARTESIAN_POINT('Ctrl Pts',(3.903245854618,-2.9967720194161,2.17769022058223));
#22363=CARTESIAN_POINT('Ctrl Pts',(3.7346182800269,-3.20190381884043,2.16281209800813));
#22364=CARTESIAN_POINT('Ctrl Pts',(3.66749544585424,-3.2785726618406,2.15710156045378));
#22365=CARTESIAN_POINT('Ctrl Pts',(3.54126453605472,-3.41402456395137,2.14669108346902));
#22366=CARTESIAN_POINT('Ctrl Pts',(3.48295082773672,-3.47349557987469,2.14199878192741));
#22367=CARTESIAN_POINT('Ctrl Pts',(3.37462703763881,-3.5784973484031,2.13347222010209));
#22368=CARTESIAN_POINT('Ctrl Pts',(3.32513415870264,-3.6245321914051,2.12964384225648));
#22369=CARTESIAN_POINT('Ctrl Pts',(3.1985561824308,-3.73749100751741,2.12001065796144));
#22370=CARTESIAN_POINT('Ctrl Pts',(3.12030739495271,-3.80306219254956,2.11419598515099));
#22371=CARTESIAN_POINT('Ctrl Pts',(2.91665808345992,-3.96319806339806,2.09939842738159));
#22372=CARTESIAN_POINT('Ctrl Pts',(2.78866402178021,-4.05427995477066,2.09040127960862));
#22373=CARTESIAN_POINT('Ctrl Pts',(2.62385733423668,-4.16005569269729,2.07920541802012));
#22374=CARTESIAN_POINT('Ctrl Pts',(2.59093326715756,-4.18064056138376,2.07698745578791));
#22375=CARTESIAN_POINT('Ctrl Pts',(2.53556915187042,-4.21435020671714,2.07328989063368));
#22376=CARTESIAN_POINT('Ctrl Pts',(2.51326263294801,-4.2276908042218,2.07180867508287));
#22377=CARTESIAN_POINT('Ctrl Pts',(2.4548578533147,-4.26199465519438,2.06795325304509));
#22378=CARTESIAN_POINT('Ctrl Pts',(2.41859639468662,-4.28267638924241,2.06558202924274));
#22379=CARTESIAN_POINT('Ctrl Pts',(2.35052290613656,-4.320361770975,2.0611742765807));
#22380=CARTESIAN_POINT('Ctrl Pts',(2.31877863224819,-4.33748192554988,2.05913621807361));
#22381=CARTESIAN_POINT('Ctrl Pts',(2.14291473093149,-4.42984547855592,2.04793129421538));
#22382=CARTESIAN_POINT('Ctrl Pts',(1.99531925365292,-4.49825709304091,2.03883959554162));
#22383=CARTESIAN_POINT('Ctrl Pts',(1.70687352482483,-4.61495841972039,2.02140597009712));
#22384=CARTESIAN_POINT('Ctrl Pts',(1.56668845659874,-4.66441260250427,2.01307618624738));
#22385=CARTESIAN_POINT('Ctrl Pts',(1.35766839859157,-4.72766245922706,2.00076424789439));
#22386=CARTESIAN_POINT('Ctrl Pts',(1.29043298642667,-4.74645534801112,1.99682032972415));
#22387=CARTESIAN_POINT('Ctrl Pts',(1.15032507023243,-4.78241960034736,1.98862664329116));
#22388=CARTESIAN_POINT('Ctrl Pts',(1.07741450888023,-4.79937108350826,1.98437640506048));
#22389=CARTESIAN_POINT('Ctrl Pts',(0.85144200595235,-4.8465000180749,1.97123553793859));
#22390=CARTESIAN_POINT('Ctrl Pts',(0.697310659739751,-4.87106485097146,
1.96231446791112));
#22391=CARTESIAN_POINT('Ctrl Pts',(0.414742367297822,-4.9024112987271,1.94603961614529));
#22392=CARTESIAN_POINT('Ctrl Pts',(0.286703932307502,-4.91156280329857,
1.93869551810289));
#22393=CARTESIAN_POINT('Ctrl Pts',(0.116712562192694,-4.91704233864545,
1.92901450604185));
#22394=CARTESIAN_POINT('Ctrl Pts',(0.0749558047788633,-4.91785612476596,
1.92664214058223));
#22395=CARTESIAN_POINT('Ctrl Pts',(-0.00285776153617473,-4.91838130328029,
1.92223399107222));
#22396=CARTESIAN_POINT('Ctrl Pts',(-0.0389108048909155,-4.91822821714893,
1.92019667001157));
#22397=CARTESIAN_POINT('Ctrl Pts',(-0.239094154068225,-4.91517686468076,
1.90890350944235));
#22398=CARTESIAN_POINT('Ctrl Pts',(-0.403003010553682,-4.90445914633421,
1.89972439242493));
#22399=CARTESIAN_POINT('Ctrl Pts',(-0.66698314074775,-4.87387286348184,
1.88483491075393));
#22400=CARTESIAN_POINT('Ctrl Pts',(-0.767509013794877,-4.85905679071307,
1.87914038210205));
#22401=CARTESIAN_POINT('Ctrl Pts',(-0.949351925815127,-4.82647162024694,
1.86875296343087));
#22402=CARTESIAN_POINT('Ctrl Pts',(-1.03081475002244,-4.80973160439563,
1.86406764314558));
#22403=CARTESIAN_POINT('Ctrl Pts',(-1.17766279317997,-4.77565315806183,
1.85554729392236));
#22404=CARTESIAN_POINT('Ctrl Pts',(-1.2431897163529,-4.75901585769912,1.85171809976792));
#22405=CARTESIAN_POINT('Ctrl Pts',(-1.40700111609575,-4.71380988307916,
1.84206872178752));
#22406=CARTESIAN_POINT('Ctrl Pts',(-1.50477514033721,-4.68351439890763,
1.83623857782591));
#22407=CARTESIAN_POINT('Ctrl Pts',(-1.74963478407155,-4.59918442467976,
1.82144609153528));
#22408=CARTESIAN_POINT('Ctrl Pts',(-1.89521624740806,-4.5411313947083,1.81246978068025));
#22409=CARTESIAN_POINT('Ctrl Pts',(-2.07307948328668,-4.46016019734977,
1.80129706795286));
#22410=CARTESIAN_POINT('Ctrl Pts',(-2.10818977692013,-4.44367228945547,
1.79908143267296));
#22411=CARTESIAN_POINT('Ctrl Pts',(-2.16647951283241,-4.4154528883642,1.79538718523775));
#22412=CARTESIAN_POINT('Ctrl Pts',(-2.18976761399989,-4.40394998780079,
1.79390696352673));
#22413=CARTESIAN_POINT('Ctrl Pts',(-2.25022607114907,-4.37348907042819,
1.79005356745911));
#22414=CARTESIAN_POINT('Ctrl Pts',(-2.28724844388295,-4.35424145299417,
1.7876833752413));
#22415=CARTESIAN_POINT('Ctrl Pts',(-2.35581707396321,-4.31747733564131,
1.78327597814895));
#22416=CARTESIAN_POINT('Ctrl Pts',(-2.38742415044154,-4.30008030054506,
1.78123725029596));
#22417=CARTESIAN_POINT('Ctrl Pts',(-2.56195069180883,-4.20150064974658,
1.76993084478788));
#22418=CARTESIAN_POINT('Ctrl Pts',(-2.70092375277152,-4.11353999126039,
1.76074003648322));
#22419=CARTESIAN_POINT('Ctrl Pts',(-2.91812563713238,-3.96030516646903,
1.74584664913128));
#22420=CARTESIAN_POINT('Ctrl Pts',(-2.99918876353861,-3.89927439259758,
1.74016005178832));
#22421=CARTESIAN_POINT('Ctrl Pts',(-3.14310871835743,-3.78377518228253,
1.72978406090607));
#22422=CARTESIAN_POINT('Ctrl Pts',(-3.20658254161264,-3.73013608663222,
1.72510220339709));
#22423=CARTESIAN_POINT('Ctrl Pts',(-3.31918199949125,-3.62998409654493,
1.71658491825991));
#22424=CARTESIAN_POINT('Ctrl Pts',(-3.36876527755951,-3.58401646978838,
1.71275530171298));
#22425=CARTESIAN_POINT('Ctrl Pts',(-3.49107947195766,-3.46584012182361,
1.70309773334288));
#22426=CARTESIAN_POINT('Ctrl Pts',(-3.56253012367266,-3.39235351037586,
1.69725977399651));
#22427=CARTESIAN_POINT('Ctrl Pts',(-3.73714164171898,-3.20116140870804,
1.68246980303553));
#22428=CARTESIAN_POINT('Ctrl Pts',(-3.83707797472328,-3.08066459589637,
1.6735039705784));
#22429=CARTESIAN_POINT('Ctrl Pts',(-3.95439717399389,-2.92462458050187,
1.66234290045868));
#22430=CARTESIAN_POINT('Ctrl Pts',(-3.97732704932659,-2.89336404739846,
1.66012843706927));
#22431=CARTESIAN_POINT('Ctrl Pts',(-4.01499346437601,-2.84071904928267,
1.65643586047409));
#22432=CARTESIAN_POINT('Ctrl Pts',(-4.029934510683,-2.81948312373489,1.65495613926022));
#22433=CARTESIAN_POINT('Ctrl Pts',(-4.06843999476172,-2.763823307445,1.65110376300936));
#22434=CARTESIAN_POINT('Ctrl Pts',(-4.09173600409548,-2.72921596675235,
1.64873408984005));
#22435=CARTESIAN_POINT('Ctrl Pts',(-4.13761963713916,-2.65914538759537,
1.6439894133055));
#22436=CARTESIAN_POINT('Ctrl Pts',(-4.16019847406307,-2.62368046175027,
1.64161468523822));
#22437=CARTESIAN_POINT('Ctrl Pts',(-4.25014989913843,-2.47831114270315,
1.63197774372176));
#22438=CARTESIAN_POINT('Ctrl Pts',(-4.31364462548109,-2.36606657393467,
1.62475799913469));
#22439=CARTESIAN_POINT('Ctrl Pts',(-4.43714725584738,-2.12620644888387,
1.60964378140722));
#22440=CARTESIAN_POINT('Ctrl Pts',(-4.49622605156831,-1.99824434527271,
1.60175545542597));
#22441=CARTESIAN_POINT('Ctrl Pts',(-4.57985149395893,-1.79455660558094,
1.58936809433175));
#22442=CARTESIAN_POINT('Ctrl Pts',(-4.60819363628214,-1.72047212347358,
1.58489674910551));
#22443=CARTESIAN_POINT('Ctrl Pts',(-4.65756116513055,-1.58144293426877,
1.57655461338746));
#22444=CARTESIAN_POINT('Ctrl Pts',(-4.67905016543438,-1.51668295008528,
1.57268817140172));
#22445=CARTESIAN_POINT('Ctrl Pts',(-4.73266379286164,-1.34311023628735,
1.56236798506226));
#22446=CARTESIAN_POINT('Ctrl Pts',(-4.76238240630405,-1.23359838359574,
1.55590023624027));
#22447=CARTESIAN_POINT('Ctrl Pts',(-4.82635302771853,-0.960876598899115,
1.53988805560355));
#22448=CARTESIAN_POINT('Ctrl Pts',(-4.85614386666074,-0.796764811521365,
1.53033243503737));
#22449=CARTESIAN_POINT('Ctrl Pts',(-4.88525327202945,-0.571916225477431,
1.51738961257693));
#22450=CARTESIAN_POINT('Ctrl Pts',(-4.89187083435975,-0.512237800708074,
1.5139690165124));
#22451=CARTESIAN_POINT('Ctrl Pts',(-4.90077480004421,-0.415860374213651,
1.50847343897031));
#22452=CARTESIAN_POINT('Ctrl Pts',(-4.90374522095142,-0.379231247794851,
1.50639175857398));
#22453=CARTESIAN_POINT('Ctrl Pts',(-4.91052864611597,-0.282079192584326,
1.50088759076744));
#22454=CARTESIAN_POINT('Ctrl Pts',(-4.91363331244746,-0.221513109777117,
1.49747283964233));
#22455=CARTESIAN_POINT('Ctrl Pts',(-4.91716328222741,-0.113672950447315,
1.49140879962172));
#22456=CARTESIAN_POINT('Ctrl Pts',(-4.91802852094442,-0.0664212655845766,
1.48875724195036));
#22457=CARTESIAN_POINT('Ctrl Pts',(-4.91909383189297,0.206973859853138,
1.47342823072295));
#22458=CARTESIAN_POINT('Ctrl Pts',(-4.9043773698152,0.43290146778546,1.46079749396125));
#22459=CARTESIAN_POINT('Ctrl Pts',(-4.86504527327222,0.724694209471723,
1.44419241451101));
#22460=CARTESIAN_POINT('Ctrl Pts',(-4.85451335329151,0.792178751017915,
1.44033263029991));
#22461=CARTESIAN_POINT('Ctrl Pts',(-4.82922543572822,0.934668491773237,
1.43213313249681));
#22462=CARTESIAN_POINT('Ctrl Pts',(-4.81411930489155,1.00959329766838,1.42779205454876));
#22463=CARTESIAN_POINT('Ctrl Pts',(-4.78685401679215,1.13024159751727,1.42074840497709));
#22464=CARTESIAN_POINT('Ctrl Pts',(-4.77577284560566,1.17618406196278,1.41805356987303));
#22465=CARTESIAN_POINT('Ctrl Pts',(-4.76403455895385,1.22194835553447,1.41535621473006));
#22466=CARTESIAN_POINT('',(-4.91824999841653,0.000124803163104314,1.13985943599073));
#22467=CARTESIAN_POINT('Ctrl Pts',(-4.76403458704967,1.22194824599671,1.06992377601457));
#22468=CARTESIAN_POINT('Ctrl Pts',(-4.79982437332077,1.08241387519401,1.07808064693106));
#22469=CARTESIAN_POINT('Ctrl Pts',(-4.82947700993754,0.941316516416591,
1.08623751784756));
#22470=CARTESIAN_POINT('Ctrl Pts',(-4.85288018637509,0.799210209637021,
1.09439438876406));
#22471=CARTESIAN_POINT('Ctrl Pts',(-4.86987080685369,0.69604155077785,1.10031624720942));
#22472=CARTESIAN_POINT('Ctrl Pts',(-4.88356857401184,0.592341382594322,
1.10623810565479));
#22473=CARTESIAN_POINT('Ctrl Pts',(-4.89394752758848,0.488324338642415,
1.11215996410015));
#22474=CARTESIAN_POINT('Ctrl Pts',(-4.9091406584297,0.336059994572651,1.12082861932818));
#22475=CARTESIAN_POINT('Ctrl Pts',(-4.91722391166533,0.183081205296633,
1.12949727455621));
#22476=CARTESIAN_POINT('Ctrl Pts',(-4.91815834240437,0.030026347401424,
1.13816592978423));
#22477=CARTESIAN_POINT('Ctrl Pts',(-4.91821919245222,0.0200594284671798,
1.13873043185307));
#22478=CARTESIAN_POINT('Ctrl Pts',(-4.91824974548893,0.0100921881469089,
1.1392949339219));
#22479=CARTESIAN_POINT('Ctrl Pts',(-4.91824999841653,0.000124803163104037,
1.13985943599073));
#22480=CARTESIAN_POINT('Ctrl Pts',(-4.91833174648596,0.000124732719183029,
1.13985944009773));
#22481=CARTESIAN_POINT('Ctrl Pts',(-4.91765570671746,-0.655079802589096,
1.17696627993604));
#22482=CARTESIAN_POINT('Ctrl Pts',(-4.62138190515468,-2.12911601537738,
1.26041311827852));
#22483=CARTESIAN_POINT('Ctrl Pts',(-3.19184455084248,-4.01249957439954,
1.39019995512517));
#22484=CARTESIAN_POINT('Ctrl Pts',(-0.881775035232405,-5.05079265228957,
1.52921995063769));
#22485=CARTESIAN_POINT('Ctrl Pts',(1.64345394850212,-4.85665391387348,1.66823994615021));
#22486=CARTESIAN_POINT('Ctrl Pts',(3.76766821220293,-3.47745696095566,1.80725994166273));
#22487=CARTESIAN_POINT('Ctrl Pts',(4.97254391099345,-1.24973472203359,1.94627993717524));
#22488=CARTESIAN_POINT('Ctrl Pts',(4.964082610191,1.28293170371797,2.08529993268776));
#22489=CARTESIAN_POINT('Ctrl Pts',(3.74434891334654,3.50255353564616,2.22431992820028));
#22490=CARTESIAN_POINT('Ctrl Pts',(1.61096675357468,4.86752668456681,2.36333992371279));
#22491=CARTESIAN_POINT('Ctrl Pts',(-0.915503054237605,5.04478782126033,
2.50235991922531));
#22492=CARTESIAN_POINT('Ctrl Pts',(-3.21858343365825,3.99108389232243,2.64137991473783));
#22493=CARTESIAN_POINT('Ctrl Pts',(-4.37427005395998,2.44717777195728,2.74723822922728));
#22494=CARTESIAN_POINT('Ctrl Pts',(-4.70630282514833,1.44739632623978,2.80675654521255));
#22495=CARTESIAN_POINT('Ctrl Pts',(-4.76390408110233,1.22191513442789,2.81993486269365));
#22496=CARTESIAN_POINT('Origin',(0.,0.,-3.23514056400928));
#22497=CARTESIAN_POINT('',(-4.76403458685474,1.2219482467567,4.91544887818065));
#22498=CARTESIAN_POINT('',(-4.76403458704967,1.22194824599672,4.56992379268636));
#22499=CARTESIAN_POINT('',(-4.76403458704967,1.22194824599672,-3.23514056400928));
#22500=CARTESIAN_POINT('',(-4.9182499295104,6.30366423602885E-5,3.23536498942701));
#22501=CARTESIAN_POINT('Ctrl Pts',(-4.76403458685474,1.2219482467567,4.91544887818065));
#22502=CARTESIAN_POINT('Ctrl Pts',(-4.75872459594536,1.24265041676701,4.91424056353588));
#22503=CARTESIAN_POINT('Ctrl Pts',(-4.7532796218485,1.2633181343046,4.91303135304027));
#22504=CARTESIAN_POINT('Ctrl Pts',(-4.72876826565284,1.35395449739011,4.90771518220076));
#22505=CARTESIAN_POINT('Ctrl Pts',(-4.70829069555103,1.42353105069983,4.90359920941263));
#22506=CARTESIAN_POINT('Ctrl Pts',(-4.6623696245796,1.56770561514134,4.89499009065993));
#22507=CARTESIAN_POINT('Ctrl Pts',(-4.6366563561763,1.6421964179618,4.89049633022066));
#22508=CARTESIAN_POINT('Ctrl Pts',(-4.54856994431292,1.87879088058015,4.87607157451927));
#22509=CARTESIAN_POINT('Ctrl Pts',(-4.47939718397532,2.03822090576412,4.86611494218855));
#22510=CARTESIAN_POINT('Ctrl Pts',(-4.37409820714046,2.24952076452407,4.85263459154936));
#22511=CARTESIAN_POINT('Ctrl Pts',(-4.34519811752483,2.3048497240378,4.84907763227268));
#22512=CARTESIAN_POINT('Ctrl Pts',(-4.29761244002972,2.39187421693469,4.84344495094849));
#22513=CARTESIAN_POINT('Ctrl Pts',(-4.2796110891683,2.42393562680431,4.84136169040704));
#22514=CARTESIAN_POINT('Ctrl Pts',(-4.23207676064545,2.50641642624834,4.83598038759172));
#22515=CARTESIAN_POINT('Ctrl Pts',(-4.20200178483422,2.55651679646058,4.83268922961721));
#22516=CARTESIAN_POINT('Ctrl Pts',(-4.08767929391668,2.73949109802989,4.82056045222598));
#22517=CARTESIAN_POINT('Ctrl Pts',(-3.99796342003959,2.86883644190503,4.81176760623206));
#22518=CARTESIAN_POINT('Ctrl Pts',(-3.8347620686523,3.08156761558349,4.79673519417109));
#22519=CARTESIAN_POINT('Ctrl Pts',(-3.76437088201348,3.16717074972329,4.7905146411889));
#22520=CARTESIAN_POINT('Ctrl Pts',(-3.64915301124015,3.29801510378949,4.78068783321623));
#22521=CARTESIAN_POINT('Ctrl Pts',(-3.60623642412226,3.34488864815362,4.77709908410771));
#22522=CARTESIAN_POINT('Ctrl Pts',(-3.51319832431968,3.44263245718539,4.76946050996563));
#22523=CARTESIAN_POINT('Ctrl Pts',(-3.46285283556264,3.4932693543772,4.76540937641193));
#22524=CARTESIAN_POINT('Ctrl Pts',(-3.38291046196225,3.57024742224037,4.75909693694634));
#22525=CARTESIAN_POINT('Ctrl Pts',(-3.35406735414445,3.59735764269452,4.75684272799668));
#22526=CARTESIAN_POINT('Ctrl Pts',(-3.2485332245896,3.69417860351414,4.74867715516679));
#22527=CARTESIAN_POINT('Ctrl Pts',(-3.16997127781414,3.76180880463615,4.74275224075534));
#22528=CARTESIAN_POINT('Ctrl Pts',(-2.96966958500406,3.92350560322718,4.72801888073511));
#22529=CARTESIAN_POINT('Ctrl Pts',(-2.84554122766178,4.01444011788983,4.71920885604956));
#22530=CARTESIAN_POINT('Ctrl Pts',(-2.68228811155339,4.12265492714235,4.7080594509058));
#22531=CARTESIAN_POINT('Ctrl Pts',(-2.64692312568772,4.14544945484009,4.70566930382531));
#22532=CARTESIAN_POINT('Ctrl Pts',(-2.57594553464963,4.18991948466762,4.70092420292556));
#22533=CARTESIAN_POINT('Ctrl Pts',(-2.54034108764055,4.21160158325861,4.69856935021158));
#22534=CARTESIAN_POINT('Ctrl Pts',(-2.39717878842673,4.29630734648363,4.68919112793594));
#22535=CARTESIAN_POINT('Ctrl Pts',(-2.28751671115773,4.35568489642668,4.68220753902574));
#22536=CARTESIAN_POINT('Ctrl Pts',(-2.01428863032469,4.49045918857676,4.66513920511973));
#22537=CARTESIAN_POINT('Ctrl Pts',(-1.84861307337425,4.56116334286902,4.65506370180859));
#22538=CARTESIAN_POINT('Ctrl Pts',(-1.62010387772569,4.64418255103284,4.64135803783539));
#22539=CARTESIAN_POINT('Ctrl Pts',(-1.56036172513567,4.66459422901658,4.63779245300159));
#22540=CARTESIAN_POINT('Ctrl Pts',(-1.43169370043139,4.70580677472967,4.63014360619616));
#22541=CARTESIAN_POINT('Ctrl Pts',(-1.36267055697254,4.72625571084432,4.62605876483782));
#22542=CARTESIAN_POINT('Ctrl Pts',(-1.25440772076163,4.75576102763703,4.61967519978006));
#22543=CARTESIAN_POINT('Ctrl Pts',(-1.21546318501877,4.76586308056965,4.61738360773929));
#22544=CARTESIAN_POINT('Ctrl Pts',(-0.988537323067819,4.82176428219472,
4.60405640644271));
#22545=CARTESIAN_POINT('Ctrl Pts',(-0.798108964009134,4.85691650677823,
4.59296669097047));
#22546=CARTESIAN_POINT('Ctrl Pts',(-0.53378563045816,4.88974101300825,4.57774110135792));
#22547=CARTESIAN_POINT('Ctrl Pts',(-0.461271769975431,4.89711372229049,
4.57358226558045));
#22548=CARTESIAN_POINT('Ctrl Pts',(-0.350905677897745,4.90586175915028,
4.5672876304617));
#22549=CARTESIAN_POINT('Ctrl Pts',(-0.313157440626722,4.90841592282859,
4.5651410326665));
#22550=CARTESIAN_POINT('Ctrl Pts',(-0.227774763906893,4.91320418843766,
4.5603012985693));
#22551=CARTESIAN_POINT('Ctrl Pts',(-0.18012976332546,4.91518159204907,4.55761103880365));
#22552=CARTESIAN_POINT('Ctrl Pts',(-0.100548251299887,4.91732573805084,
4.55312851284391));
#22553=CARTESIAN_POINT('Ctrl Pts',(-0.068625578846102,4.91787483677015,
4.5513333916646));
#22554=CARTESIAN_POINT('Ctrl Pts',(0.0696330396414139,4.91890654373806,
4.54356682893646));
#22555=CARTESIAN_POINT('Ctrl Pts',(0.175964038255935,4.91625133711796,4.53761418222368));
#22556=CARTESIAN_POINT('Ctrl Pts',(0.432424076969489,4.90151575348922,4.52322229368798));
#22557=CARTESIAN_POINT('Ctrl Pts',(0.582245202030491,4.88598372858046,4.51478431965105));
#22558=CARTESIAN_POINT('Ctrl Pts',(0.793875437770638,4.85417063662485,4.50272143348942));
#22559=CARTESIAN_POINT('Ctrl Pts',(0.856445676047387,4.84352263083819,4.49913726753732));
#22560=CARTESIAN_POINT('Ctrl Pts',(0.98903877649286,4.81830866884365,4.49149708041534));
#22561=CARTESIAN_POINT('Ctrl Pts',(1.05898542167039,4.80342022390529,4.48743969915181));
#22562=CARTESIAN_POINT('Ctrl Pts',(1.16722617395881,4.77790147430067,4.48111404260705));
#22563=CARTESIAN_POINT('Ctrl Pts',(1.2057584487559,4.76832318308021,4.47885287061183));
#22564=CARTESIAN_POINT('Ctrl Pts',(1.29636491228674,4.74463187222538,4.47351313541038));
#22565=CARTESIAN_POINT('Ctrl Pts',(1.34833114519228,4.73012649551498,4.4704327344894));
#22566=CARTESIAN_POINT('Ctrl Pts',(1.55988243012506,4.66730646384806,4.45781850907384));
#22567=CARTESIAN_POINT('Ctrl Pts',(1.71719981406809,4.61174670253243,4.44826023765811));
#22568=CARTESIAN_POINT('Ctrl Pts',(1.92707851291203,4.52539252908285,4.4353043517684));
#22569=CARTESIAN_POINT('Ctrl Pts',(1.9823409680333,4.50145904659843,4.43187353070182));
#22570=CARTESIAN_POINT('Ctrl Pts',(2.07059769413016,4.4612956247345,4.42636777805977));
#22571=CARTESIAN_POINT('Ctrl Pts',(2.10387336477974,4.44570021112109,4.42428608475689));
#22572=CARTESIAN_POINT('Ctrl Pts',(2.19142474032359,4.40346407723899,4.41879212189009));
#22573=CARTESIAN_POINT('Ctrl Pts',(2.24538939989332,4.37619296257873,4.41538751833949));
#22574=CARTESIAN_POINT('Ctrl Pts',(2.42112530356607,4.28327793584752,4.40421512931147));
#22575=CARTESIAN_POINT('Ctrl Pts',(2.5406311086166,4.21349161532133,4.39647894513423));
#22576=CARTESIAN_POINT('Ctrl Pts',(2.76587536648273,4.06888739876674,4.38147773302931));
#22577=CARTESIAN_POINT('Ctrl Pts',(2.87191445202687,3.99474880295986,4.37422076756146));
#22578=CARTESIAN_POINT('Ctrl Pts',(3.02510246806257,3.87839031171318,4.36337587367283));
#22579=CARTESIAN_POINT('Ctrl Pts',(3.07455997233645,3.83930165809705,4.35981543981702));
#22580=CARTESIAN_POINT('Ctrl Pts',(3.17896670856479,3.75347246871542,4.35216352217035));
#22581=CARTESIAN_POINT('Ctrl Pts',(3.23366658720266,3.70645182724409,4.34807039495645));
#22582=CARTESIAN_POINT('Ctrl Pts',(3.39469505095068,3.56175109452141,4.33575400803965));
#22583=CARTESIAN_POINT('Ctrl Pts',(3.49777597657197,3.46057620717562,4.32750467224476));
#22584=CARTESIAN_POINT('Ctrl Pts',(3.68100057617198,3.26417693829627,4.31213094519123));
#22585=CARTESIAN_POINT('Ctrl Pts',(3.76227353610605,3.17016000416697,4.30501611070408));
#22586=CARTESIAN_POINT('Ctrl Pts',(3.87327501412115,3.03146444890006,4.2948824047719));
#22587=CARTESIAN_POINT('Ctrl Pts',(3.90596900099565,2.98922101838279,4.29184150831157));
#22588=CARTESIAN_POINT('Ctrl Pts',(3.95786830416947,2.91985699975271,4.2869249632931));
#22589=CARTESIAN_POINT('Ctrl Pts',(3.97749799501755,2.89305999545952,4.28504391622395));
#22590=CARTESIAN_POINT('Ctrl Pts',(4.03259562347711,2.81622392818115,4.27970051187964));
#22591=CARTESIAN_POINT('Ctrl Pts',(4.06740118006355,2.76571734853234,4.27624707206658));
#22592=CARTESIAN_POINT('Ctrl Pts',(4.15303689988456,2.6363364744895,4.26752781027166));
#22593=CARTESIAN_POINT('Ctrl Pts',(4.20257151141741,2.55663418841706,4.26227254211923));
#22594=CARTESIAN_POINT('Ctrl Pts',(4.33107060792832,2.33603998398586,4.2479706180758));
#22595=CARTESIAN_POINT('Ctrl Pts',(4.4054239406777,2.19259994381565,4.23892856344424));
#22596=CARTESIAN_POINT('Ctrl Pts',(4.50264309492157,1.98005292636655,4.22576117908536));
#22597=CARTESIAN_POINT('Ctrl Pts',(4.53124746908644,1.91368770871106,4.22168164208227));
#22598=CARTESIAN_POINT('Ctrl Pts',(4.58526700920266,1.78034754263775,4.21353757447278));
#22599=CARTESIAN_POINT('Ctrl Pts',(4.61070203475962,1.71339940042234,4.20947421460826));
#22600=CARTESIAN_POINT('Ctrl Pts',(4.68265471689841,1.51079138660646,4.19724410686154));
#22601=CARTESIAN_POINT('Ctrl Pts',(4.72471015860723,1.37362980795743,4.18905146336735));
#22602=CARTESIAN_POINT('Ctrl Pts',(4.80000625094332,1.0833361021509,4.17188671262462));
#22603=CARTESIAN_POINT('Ctrl Pts',(4.83204710631703,0.930053026692105,4.162921061449));
#22604=CARTESIAN_POINT('Ctrl Pts',(4.86313320006653,0.735370774443273,4.15170256864813));
#22605=CARTESIAN_POINT('Ctrl Pts',(4.86904369420111,0.695160601056541,4.14939464323175));
#22606=CARTESIAN_POINT('Ctrl Pts',(4.88021927933939,0.61197777537219,4.14464130973067));
#22607=CARTESIAN_POINT('Ctrl Pts',(4.88541672773209,0.568999531865461,4.14219676494567));
#22608=CARTESIAN_POINT('Ctrl Pts',(4.89298572745047,0.498627447645299,4.13820796911974));
#22609=CARTESIAN_POINT('Ctrl Pts',(4.89569614480389,0.4712726698626,4.1366608787722));
#22610=CARTESIAN_POINT('Ctrl Pts',(4.90560661652142,0.361915546742582,4.1304868905296));
#22611=CARTESIAN_POINT('Ctrl Pts',(4.91097682293429,0.279760500850208,4.12587283548614));
#22612=CARTESIAN_POINT('Ctrl Pts',(4.92180884448031,0.0102456745276687,
4.11075951620191));
#22613=CARTESIAN_POINT('Ctrl Pts',(4.91862515605703,-0.177292957268644,
4.1002744607054));
#22614=CARTESIAN_POINT('Ctrl Pts',(4.89951080706604,-0.43471631507129,4.08572582500054));
#22615=CARTESIAN_POINT('Ctrl Pts',(4.89275355067037,-0.505120742950989,
4.08173142681248));
#22616=CARTESIAN_POINT('Ctrl Pts',(4.8758993826123,-0.648204475541511,4.07357264459773));
#22617=CARTESIAN_POINT('Ctrl Pts',(4.86568955496173,-0.720852839267989,
4.06940848234307));
#22618=CARTESIAN_POINT('Ctrl Pts',(4.84087089033953,-0.872718008786922,
4.06065140771536));
#22619=CARTESIAN_POINT('Ctrl Pts',(4.82593318999009,-0.951859425678025,
4.05605767065837));
#22620=CARTESIAN_POINT('Ctrl Pts',(4.77271398448199,-1.20019521482268,4.04154347315174));
#22621=CARTESIAN_POINT('Ctrl Pts',(4.72742259732521,-1.36775103513162,4.03159914680417));
#22622=CARTESIAN_POINT('Ctrl Pts',(4.65483336419233,-1.58910351958976,4.01830168312997));
#22623=CARTESIAN_POINT('Ctrl Pts',(4.63526714857286,-1.64530308056132,4.01491182393494));
#22624=CARTESIAN_POINT('Ctrl Pts',(4.6019741903225,-1.73561726265998,4.00944671881719));
#22625=CARTESIAN_POINT('Ctrl Pts',(4.58887641333137,-1.76995678843787,4.00736496267961));
#22626=CARTESIAN_POINT('Ctrl Pts',(4.55294396323284,-1.86108304824452,4.00182903385924));
#22627=CARTESIAN_POINT('Ctrl Pts',(4.52943209988179,-1.91759584691068,3.99838281584693));
#22628=CARTESIAN_POINT('Ctrl Pts',(4.44043422417028,-2.12073361694215,3.98591929696027));
#22629=CARTESIAN_POINT('Ctrl Pts',(4.36883254475307,-2.26456836102405,3.97694600280763));
#22630=CARTESIAN_POINT('Ctrl Pts',(4.23349771611146,-2.50603047032997,3.96142327232429));
#22631=CARTESIAN_POINT('Ctrl Pts',(4.17309654259622,-2.60537068136046,3.95489460859878));
#22632=CARTESIAN_POINT('Ctrl Pts',(4.07165587579385,-2.75961562900759,3.94448005816727));
#22633=CARTESIAN_POINT('Ctrl Pts',(4.03289065707146,-2.81596392026291,3.94061379251168));
#22634=CARTESIAN_POINT('Ctrl Pts',(3.94704970304482,-2.93533064973419,3.93228076635458));
#22635=CARTESIAN_POINT('Ctrl Pts',(3.89961176273528,-2.99806525550416,3.92781202836162));
#22636=CARTESIAN_POINT('Ctrl Pts',(3.79370548613805,-3.13135314884162,3.91811371451174));
#22637=CARTESIAN_POINT('Ctrl Pts',(3.73472840705243,-3.20146487632408,3.91288191374618));
#22638=CARTESIAN_POINT('Ctrl Pts',(3.54903384808436,-3.41009890181161,3.8969050235269));
#22639=CARTESIAN_POINT('Ctrl Pts',(3.41631438007157,-3.54305132670593,3.88614208952505));
#22640=CARTESIAN_POINT('Ctrl Pts',(3.249759756662,-3.69181702036267,3.87343923193496));
#22641=CARTESIAN_POINT('Ctrl Pts',(3.22294161704689,-3.71525217968172,3.87141715764175));
#22642=CARTESIAN_POINT('Ctrl Pts',(3.1635815241555,-3.76599782031712,3.86699363645047));
#22643=CARTESIAN_POINT('Ctrl Pts',(3.13093539749032,-3.79318220438637,3.86459431065765));
#22644=CARTESIAN_POINT('Ctrl Pts',(3.07720222389468,-3.83675937573761,3.86069468497912));
#22645=CARTESIAN_POINT('Ctrl Pts',(3.0563267977331,-3.85340921131592,3.85919155674783));
#22646=CARTESIAN_POINT('Ctrl Pts',(2.91449444688216,-3.96465431163737,3.84905433380022));
#22647=CARTESIAN_POINT('Ctrl Pts',(2.78929963979749,-4.05371062399757,3.84047044368215));
#22648=CARTESIAN_POINT('Ctrl Pts',(2.55548430174767,-4.20406541552771,3.8248886739725));
#22649=CARTESIAN_POINT('Ctrl Pts',(2.44830981143169,-4.26736974701756,3.81790499852495));
#22650=CARTESIAN_POINT('Ctrl Pts',(2.28361493079192,-4.35640087299042,3.80734943345926));
#22651=CARTESIAN_POINT('Ctrl Pts',(2.22781225303845,-4.38519990167338,3.80380240947643));
#22652=CARTESIAN_POINT('Ctrl Pts',(2.10640079285942,-4.44494303554768,3.79614091265941));
#22653=CARTESIAN_POINT('Ctrl Pts',(2.04062794003601,-4.47552011889162,3.7920246219592));
#22654=CARTESIAN_POINT('Ctrl Pts',(1.90202636957154,-4.53626376090469,3.78341452554515));
#22655=CARTESIAN_POINT('Ctrl Pts',(1.8290998713085,-4.56615666707342,3.77892010396938));
#22656=CARTESIAN_POINT('Ctrl Pts',(1.59317665170389,-4.6563035042683,3.76448966422596));
#22657=CARTESIAN_POINT('Ctrl Pts',(1.42769390468811,-4.70967771342347,3.75452798434467));
#22658=CARTESIAN_POINT('Ctrl Pts',(1.19947362647151,-4.77015014843758,3.74104701920025));
#22659=CARTESIAN_POINT('Ctrl Pts',(1.13891390480475,-4.7849707074876,3.7374943714763));
#22660=CARTESIAN_POINT('Ctrl Pts',(1.04271321101288,-4.80658369181909,3.73189501697629));
#22661=CARTESIAN_POINT('Ctrl Pts',(1.00725118997585,-4.81413987218877,3.72984065571702));
#22662=CARTESIAN_POINT('Ctrl Pts',(0.970002510167214,-4.82164714812114,
3.72769261597097));
#22663=CARTESIAN_POINT('Ctrl Pts',(0.968296452116267,-4.82199005303189,
3.72759425257099));
#22664=CARTESIAN_POINT('Ctrl Pts',(0.964872259605189,-4.82267639958138,
3.72739687080567));
#22665=CARTESIAN_POINT('Ctrl Pts',(0.96315412288769,-4.82301982869689,3.7272978525937));
#22666=CARTESIAN_POINT('Ctrl Pts',(0.959683258237725,-4.82371167254044,
3.72709786438853));
#22667=CARTESIAN_POINT('Ctrl Pts',(0.95793052317704,-4.82406005028074,3.72699689481607));
#22668=CARTESIAN_POINT('Ctrl Pts',(0.954370305283553,-4.82476567073531,
3.72679184507216));
#22669=CARTESIAN_POINT('Ctrl Pts',(0.952562810769049,-4.8251228532191,3.72668776556913));
#22670=CARTESIAN_POINT('Ctrl Pts',(0.949983901192228,-4.82563097095457,
3.72653929826264));
#22671=CARTESIAN_POINT('Ctrl Pts',(0.949212650487708,-4.825782736978,3.72649490159276));
#22672=CARTESIAN_POINT('Ctrl Pts',(0.947595669092285,-4.82610052249641,
3.72640182936266));
#22673=CARTESIAN_POINT('Ctrl Pts',(0.946749931063116,-4.82626650459287,
3.72635315420136));
#22674=CARTESIAN_POINT('Ctrl Pts',(0.94496613573125,-4.82661610017683,3.72625050083226));
#22675=CARTESIAN_POINT('Ctrl Pts',(0.944028068413828,-4.82679966253133,
3.72619652316565));
#22676=CARTESIAN_POINT('Ctrl Pts',(0.942037567456653,-4.82718856414173,
3.72608199965397));
#22677=CARTESIAN_POINT('Ctrl Pts',(0.940985120014875,-4.8273938327209,3.72602145455115));
#22678=CARTESIAN_POINT('Ctrl Pts',(0.938738268407798,-4.82783129432263,
3.72589221374912));
#22679=CARTESIAN_POINT('Ctrl Pts',(0.937543844976476,-4.82806338833307,
3.72582351908098));
#22680=CARTESIAN_POINT('Ctrl Pts',(0.934978146894434,-4.82856095314098,
3.725675978963));
#22681=CARTESIAN_POINT('Ctrl Pts',(0.933606844957965,-4.82882628310621,
3.72559713496593));
#22682=CARTESIAN_POINT('Ctrl Pts',(0.930642864549843,-4.82939846688434,
3.72542674564744));
#22683=CARTESIAN_POINT('Ctrl Pts',(0.929050146822228,-4.8297051170827,3.7253352024035));
#22684=CARTESIAN_POINT('Ctrl Pts',(0.925586111278989,-4.8303702801614,3.72513613920447));
#22685=CARTESIAN_POINT('Ctrl Pts',(0.92371473607239,-4.83072849363597,3.72502862226533));
#22686=CARTESIAN_POINT('Ctrl Pts',(0.919619450999208,-4.8315099350758,3.72479338370328));
#22687=CARTESIAN_POINT('Ctrl Pts',(0.917395455888481,-4.83193271527192,
3.72466566652282));
#22688=CARTESIAN_POINT('Ctrl Pts',(0.912499109984687,-4.83286000549962,
3.724384554076));
#22689=CARTESIAN_POINT('Ctrl Pts',(0.909826630682355,-4.83336383490782,
3.7242311654405));
#22690=CARTESIAN_POINT('Ctrl Pts',(0.903909079774386,-4.83447435990249,
3.72389162331597));
#22691=CARTESIAN_POINT('Ctrl Pts',(0.900663811902359,-4.83508000543997,
3.72370547983367));
#22692=CARTESIAN_POINT('Ctrl Pts',(0.893440045184302,-4.83642060999115,
3.7232912803804));
#22693=CARTESIAN_POINT('Ctrl Pts',(0.889461243491172,-4.83715392844322,
3.72306323962401));
#22694=CARTESIAN_POINT('Ctrl Pts',(0.880563966309822,-4.83878240432233,
3.72255351454369));
#22695=CARTESIAN_POINT('Ctrl Pts',(0.87564502048999,-4.83967497393235,3.72227185341808));
#22696=CARTESIAN_POINT('Ctrl Pts',(0.86670625790034,-4.8412828873707,3.7217602719084));
#22697=CARTESIAN_POINT('Ctrl Pts',(0.86268689618551,-4.84200072823426,3.72153033062378));
#22698=CARTESIAN_POINT('Ctrl Pts',(0.798137042833475,-4.85344613072382,
3.71783900884012));
#22699=CARTESIAN_POINT('Ctrl Pts',(0.737411155880095,-4.86304297367625,
3.71438708377863));
#22700=CARTESIAN_POINT('Ctrl Pts',(0.480725322272015,-4.89868977554014,
3.6998515943665));
#22701=CARTESIAN_POINT('Ctrl Pts',(0.283469359160044,-4.91405159390131,
3.68881022822731));
#22702=CARTESIAN_POINT('Ctrl Pts',(0.00839591566748247,-4.91885248625896,
3.6733308756948));
#22703=CARTESIAN_POINT('Ctrl Pts',(-0.0690544227738577,-4.91837489142199,
3.66896449092164));
#22704=CARTESIAN_POINT('Ctrl Pts',(-0.183900738185932,-4.91495336645558,
3.66246769931661));
#22705=CARTESIAN_POINT('Ctrl Pts',(-0.221326823564799,-4.91341027087016,
3.66034706972902));
#22706=CARTESIAN_POINT('Ctrl Pts',(-0.321931021373896,-4.90811050686905,
3.65463581360591));
#22707=CARTESIAN_POINT('Ctrl Pts',(-0.385059977705378,-4.90356166839823,
3.65104043461192));
#22708=CARTESIAN_POINT('Ctrl Pts',(-0.609256774538074,-4.88305064654247,
3.63822399337025));
#22709=CARTESIAN_POINT('Ctrl Pts',(-0.76960278397842,-4.86035882704391,
3.62896620172699));
#22710=CARTESIAN_POINT('Ctrl Pts',(-1.05394210998029,-4.80569423780498,
3.61239131063181));
#22711=CARTESIAN_POINT('Ctrl Pts',(-1.17836301359127,-4.77670935673205,
3.60508399821852));
#22712=CARTESIAN_POINT('Ctrl Pts',(-1.33625636113991,-4.73338143529562,
3.59576934348538));
#22713=CARTESIAN_POINT('Ctrl Pts',(-1.37089167386659,-4.72346662190017,
3.59372359640799));
#22714=CARTESIAN_POINT('Ctrl Pts',(-1.4366942234486,-4.70384503844337,3.58983360870883));
#22715=CARTESIAN_POINT('Ctrl Pts',(-1.46787987238688,-4.69420676407748,
3.587988603152));
#22716=CARTESIAN_POINT('Ctrl Pts',(-1.50319612931055,-4.68290552671892,
3.5858961801963));
#22717=CARTESIAN_POINT('Ctrl Pts',(-1.50742297930052,-4.6815466180397,3.5856456975208));
#22718=CARTESIAN_POINT('Ctrl Pts',(-1.5176041777283,-4.67825820144726,3.58504223382688));
#22719=CARTESIAN_POINT('Ctrl Pts',(-1.52355669728959,-4.67632304593745,
3.58468930915814));
#22720=CARTESIAN_POINT('Ctrl Pts',(-1.53820535320386,-4.67152985056228,
3.58382051190248));
#22721=CARTESIAN_POINT('Ctrl Pts',(-1.54689724169928,-4.6686588842402,3.58330476214194));
#22722=CARTESIAN_POINT('Ctrl Pts',(-1.56833470707311,-4.66151156220546,
3.58203206556754));
#22723=CARTESIAN_POINT('Ctrl Pts',(-1.58107087309591,-4.65720717743159,
3.58127536602299));
#22724=CARTESIAN_POINT('Ctrl Pts',(-1.66297735298287,-4.62915090010136,
3.57640475112087));
#22725=CARTESIAN_POINT('Ctrl Pts',(-1.73162864758464,-4.60391073840025,
3.57230259169348));
#22726=CARTESIAN_POINT('Ctrl Pts',(-1.98613986995693,-4.50383932125865,
3.55697457632233));
#22727=CARTESIAN_POINT('Ctrl Pts',(-2.16793271914314,-4.4192065961505,3.54577534641404));
#22728=CARTESIAN_POINT('Ctrl Pts',(-2.35942627133897,-4.31539064729117,
3.5335010348647));
#22729=CARTESIAN_POINT('Ctrl Pts',(-2.37475260157293,-4.30697560334112,
3.53251526588411));
#22730=CARTESIAN_POINT('Ctrl Pts',(-2.44597846741211,-4.26737270682715,
3.52791790792911));
#22731=CARTESIAN_POINT('Ctrl Pts',(-2.50131021555066,-4.2351773958208,3.52429962307845));
#22732=CARTESIAN_POINT('Ctrl Pts',(-2.60970034299327,-4.16924433607679,
3.51711141238546));
#22733=CARTESIAN_POINT('Ctrl Pts',(-2.66277171809153,-4.13555085622148,
3.51354245357445));
#22734=CARTESIAN_POINT('Ctrl Pts',(-2.78098869205118,-4.05727911630663,
3.50547546513415));
#22735=CARTESIAN_POINT('Ctrl Pts',(-2.84573628082022,-4.01213120185137,
3.50097420268059));
#22736=CARTESIAN_POINT('Ctrl Pts',(-3.0501972384755,-3.86212222932367,3.48648476843722));
#22737=CARTESIAN_POINT('Ctrl Pts',(-3.18542117878974,-3.75137083161058,
3.47647067850075));
#22738=CARTESIAN_POINT('Ctrl Pts',(-3.3599518158474,-3.59217165425268,3.46298303081007));
#22739=CARTESIAN_POINT('Ctrl Pts',(-3.40465464284856,-3.54983102307576,
3.45947483811983));
#22740=CARTESIAN_POINT('Ctrl Pts',(-3.47438135519179,-3.4812597911473,3.45392144346955));
#22741=CARTESIAN_POINT('Ctrl Pts',(-3.4999301834248,-3.45557293175301,3.45186885591697));
#22742=CARTESIAN_POINT('Ctrl Pts',(-3.52760551450541,-3.42712625443474,
3.44962538291886));
#22743=CARTESIAN_POINT('Ctrl Pts',(-3.53001520191382,-3.42464417189484,
3.44942987231861));
#22744=CARTESIAN_POINT('Ctrl Pts',(-3.53756184542947,-3.41685437388873,
3.44881702995062));
#22745=CARTESIAN_POINT('Ctrl Pts',(-3.54268946971256,-3.4115376216713,3.44839983829968));
#22746=CARTESIAN_POINT('Ctrl Pts',(-3.55177159807441,-3.40207795016494,
3.44765946862222));
#22747=CARTESIAN_POINT('Ctrl Pts',(-3.55573087681693,-3.39793963979141,
3.44733622409126));
#22748=CARTESIAN_POINT('Ctrl Pts',(-3.56946438282923,-3.38353484068672,
3.44621327288334));
#22749=CARTESIAN_POINT('Ctrl Pts',(-3.57920146545026,-3.37323299965227,
3.44541406672986));
#22750=CARTESIAN_POINT('Ctrl Pts',(-3.61569469454993,-3.33428722416805,
3.44240691732782));
#22751=CARTESIAN_POINT('Ctrl Pts',(-3.64215274872672,-3.30536575916747,
3.44020254019076));
#22752=CARTESIAN_POINT('Ctrl Pts',(-3.73884428593209,-3.19710087927719,
3.43204860182555));
#22753=CARTESIAN_POINT('Ctrl Pts',(-3.80685411662903,-3.11581009805803,
3.42611687921128));
#22754=CARTESIAN_POINT('Ctrl Pts',(-3.96539681605747,-2.91336003330408,
3.41171056897874));
#22755=CARTESIAN_POINT('Ctrl Pts',(-4.05306975121028,-2.79010096314221,
3.4032372695488));
#22756=CARTESIAN_POINT('Ctrl Pts',(-4.16992940750641,-2.60864930448966,
3.39107185359933));
#22757=CARTESIAN_POINT('Ctrl Pts',(-4.20385808749572,-2.55361303305983,
3.38742067851559));
#22758=CARTESIAN_POINT('Ctrl Pts',(-4.26873482159039,-2.44357658411996,
3.38018919424736));
#22759=CARTESIAN_POINT('Ctrl Pts',(-4.29972893994066,-2.38861768245894,
3.37660997175069));
#22760=CARTESIAN_POINT('Ctrl Pts',(-4.36453759260036,-2.26834771398919,
3.36884244273321));
#22761=CARTESIAN_POINT('Ctrl Pts',(-4.39796195580901,-2.20284367027197,
3.36465228744954));
#22762=CARTESIAN_POINT('Ctrl Pts',(-4.49008613053705,-2.01184002191021,
3.35254486497715));
#22763=CARTESIAN_POINT('Ctrl Pts',(-4.54496847876638,-1.88457817892604,
3.34461111667337));
#22764=CARTESIAN_POINT('Ctrl Pts',(-4.62957081483979,-1.66311969328401,
3.33104556415695));
#22765=CARTESIAN_POINT('Ctrl Pts',(-4.66196237549322,-1.57003191234261,
3.32541395110656));
#22766=CARTESIAN_POINT('Ctrl Pts',(-4.70228757943409,-1.44185923300022,
3.31777033962583));
#22767=CARTESIAN_POINT('Ctrl Pts',(-4.7126656506422,-1.40756848105479,3.31573607428392));
#22768=CARTESIAN_POINT('Ctrl Pts',(-4.73179061504625,-1.34179290536352,
3.31185575524484));
#22769=CARTESIAN_POINT('Ctrl Pts',(-4.74060021149583,-1.3103283126574,3.31000896841078));
#22770=CARTESIAN_POINT('Ctrl Pts',(-4.77333912063673,-1.18874332971476,
3.30290402456549));
#22771=CARTESIAN_POINT('Ctrl Pts',(-4.79501756953323,-1.09803639803183,
3.29766930353714));
#22772=CARTESIAN_POINT('Ctrl Pts',(-4.85988451067937,-0.787859223582681,
3.27990175104639));
#22773=CARTESIAN_POINT('Ctrl Pts',(-4.89067947295103,-0.566085447524859,
3.26741014941425));
#22774=CARTESIAN_POINT('Ctrl Pts',(-4.9104406730498,-0.283411757147819,
3.2514320293728));
#22775=CARTESIAN_POINT('Ctrl Pts',(-4.91352005195395,-0.223764240752992,
3.24805821858464));
#22776=CARTESIAN_POINT('Ctrl Pts',(-4.9173380535753,-0.109381565021347,
3.24157883723314));
#22777=CARTESIAN_POINT('Ctrl Pts',(-4.91825070131855,-0.0546609832033692,
3.23847490589605));
#22778=CARTESIAN_POINT('Ctrl Pts',(-4.91824999959565,6.30663975847573E-5,
3.23536510923081));
#22779=CARTESIAN_POINT('Ctrl Pts',(-4.91824999959594,6.30435251926018E-5,
3.23536511053057));
#22780=CARTESIAN_POINT('Ctrl Pts',(-4.91824924063888,0.0592719879222192,
3.23200045131605));
#22781=CARTESIAN_POINT('Ctrl Pts',(-4.91717929112431,0.118475757485024,
3.22862943975445));
#22782=CARTESIAN_POINT('Ctrl Pts',(-4.91075122842712,0.296325476698879,
3.21847981779956));
#22783=CARTESIAN_POINT('Ctrl Pts',(-4.90216465842163,0.414810448163661,
3.21168634978811));
#22784=CARTESIAN_POINT('Ctrl Pts',(-4.87903381457549,0.627046359997565,
3.19946506954886));
#22785=CARTESIAN_POINT('Ctrl Pts',(-4.86605052775946,0.720909495938399,
3.19404174490195));
#22786=CARTESIAN_POINT('Ctrl Pts',(-4.84275082537018,0.859687092662535,
3.18600725543108));
#22787=CARTESIAN_POINT('Ctrl Pts',(-4.83450163814727,0.904926193268071,
3.1833856758173));
#22788=CARTESIAN_POINT('Ctrl Pts',(-4.81925221365533,0.982383634793772,
3.178895072711));
#22789=CARTESIAN_POINT('Ctrl Pts',(-4.81256020691428,1.01465944351237,3.17702328853145));
#22790=CARTESIAN_POINT('Ctrl Pts',(-4.79687704643086,1.08665159974418,3.17284818000448));
#22791=CARTESIAN_POINT('Ctrl Pts',(-4.78771606600824,1.12632855372567,3.17054728649361));
#22792=CARTESIAN_POINT('Ctrl Pts',(-4.77349677576707,1.18460233696871,3.16716463815977));
#22793=CARTESIAN_POINT('Ctrl Pts',(-4.76882042408035,1.20328960543859,3.1660793840661));
#22794=CARTESIAN_POINT('Ctrl Pts',(-4.76403458654079,1.22194824798069,3.16499504358802));
#22795=CARTESIAN_POINT('',(-4.91824999837926,-0.000126263188378294,2.88985943599073));
#22796=CARTESIAN_POINT('Ctrl Pts',(-4.76390408110233,1.22191513442789,2.81993486269365));
#22797=CARTESIAN_POINT('Ctrl Pts',(-4.86578211211368,0.823111680033963,
2.84324305302354));
#22798=CARTESIAN_POINT('Ctrl Pts',(-4.91787088034465,0.411440562533145,
2.86655124335343));
#22799=CARTESIAN_POINT('Ctrl Pts',(-4.91829688918831,-0.000126223649022064,
2.88985943368333));
#22800=CARTESIAN_POINT('Ctrl Pts',(-4.91824999837926,-0.000126263188378294,
2.88985943599073));
#22801=CARTESIAN_POINT('Ctrl Pts',(-4.91824608066218,-0.152730614993021,
2.89850193437823));
#22802=CARTESIAN_POINT('Ctrl Pts',(-4.91113527331487,-0.305300222186573,
2.90714443276572));
#22803=CARTESIAN_POINT('Ctrl Pts',(-4.89695320922365,-0.457200534967113,
2.91578693115321));
#22804=CARTESIAN_POINT('Ctrl Pts',(-4.89496601075217,-0.47848488874189,
2.91699792268976));
#22805=CARTESIAN_POINT('Ctrl Pts',(-4.89284006026767,-0.499756107960711,
2.91820891422632));
#22806=CARTESIAN_POINT('Ctrl Pts',(-4.89057553724052,-0.521012453828678,
2.91941990576287));
#22807=CARTESIAN_POINT('Ctrl Pts',(-4.87532347766989,-0.664178608266125,
2.92757619953141));
#22808=CARTESIAN_POINT('Ctrl Pts',(-4.85377769937605,-0.806701370795169,
2.93573249329995));
#22809=CARTESIAN_POINT('Ctrl Pts',(-4.82601684941236,-0.9480213244901,2.9438887870685));
#22810=CARTESIAN_POINT('Ctrl Pts',(-4.79826165753946,-1.08931247499177,
2.95204341845816));
#22811=CARTESIAN_POINT('Ctrl Pts',(-4.76429398550897,-1.22940097754245,
2.96019804984783));
#22812=CARTESIAN_POINT('Ctrl Pts',(-4.72424370144954,-1.36773700389158,
2.96835268123749));
#22813=CARTESIAN_POINT('Ctrl Pts',(-4.68419199654067,-1.50607793793789,
2.97650760192607));
#22814=CARTESIAN_POINT('Ctrl Pts',(-4.63805733725252,-1.64266594889159,
2.98466252261464));
#22815=CARTESIAN_POINT('Ctrl Pts',(-4.58601977931309,-1.77696529123365,
2.99281744330322));
#22816=CARTESIAN_POINT('Ctrl Pts',(-4.53398528081815,-1.91125673771359,
3.00097188453949));
#22817=CARTESIAN_POINT('Ctrl Pts',(-4.47604869978663,-2.04325947306684,
3.00912632577575));
#22818=CARTESIAN_POINT('Ctrl Pts',(-4.41243864038556,-2.17245674464014,
3.01728076701202));
#22819=CARTESIAN_POINT('Ctrl Pts',(-4.34881290177494,-2.30168586197986,
3.02543721823215));
#22820=CARTESIAN_POINT('Ctrl Pts',(-4.27951103805168,-2.42810783325788,
3.03359366945228));
#22821=CARTESIAN_POINT('Ctrl Pts',(-4.20480838597866,-2.55122901749402,
3.04175012067241));
#22822=CARTESIAN_POINT('Ctrl Pts',(-4.15385604408756,-2.63520612538982,
3.0473133808734));
#22823=CARTESIAN_POINT('Ctrl Pts',(-4.10039212815736,-2.71764813930332,
3.05287664107439));
#22824=CARTESIAN_POINT('Ctrl Pts',(-4.04451583520027,-2.79840574636958,
3.05843990127538));
#22825=CARTESIAN_POINT('Ctrl Pts',(-3.96259562287657,-2.91680444405521,
3.06659619498704));
#22826=CARTESIAN_POINT('Ctrl Pts',(-3.87545751923364,-3.03162564854714,
3.07475248869871));
#22827=CARTESIAN_POINT('Ctrl Pts',(-3.78343835069359,-3.14241583960509,
3.08290878241037));
#22828=CARTESIAN_POINT('Ctrl Pts',(-3.69143793709251,-3.25318344989748,
3.09106341374241));
#22829=CARTESIAN_POINT('Ctrl Pts',(-3.59455865692401,-3.35992142848364,
3.09921804507445));
#22830=CARTESIAN_POINT('Ctrl Pts',(-3.49317771874209,-3.46220919179992,
3.10737267640649));
#22831=CARTESIAN_POINT('Ctrl Pts',(-3.39179318391245,-3.56450058393495,
3.11552759703686));
#22832=CARTESIAN_POINT('Ctrl Pts',(-3.28590690439984,-3.66234120456008,
3.12368251766722));
#22833=CARTESIAN_POINT('Ctrl Pts',(-3.17593341234408,-3.75534685786234,
3.13183743829759));
#22834=CARTESIAN_POINT('Ctrl Pts',(-3.06596638596307,-3.84834704308047,
3.13999187947547));
#22835=CARTESIAN_POINT('Ctrl Pts',(-2.95191288393539,-3.93651261429531,
3.14814632065335));
#22836=CARTESIAN_POINT('Ctrl Pts',(-2.83422097248897,-4.01949928991207,
3.15630076183123));
#22837=CARTESIAN_POINT('Ctrl Pts',(-2.71650005122249,-4.10250642087277,
3.16445721299322));
#22838=CARTESIAN_POINT('Ctrl Pts',(-2.59513920195962,-4.18033191228843,
3.1726136641552));
#22839=CARTESIAN_POINT('Ctrl Pts',(-2.47061645917429,-4.25267414389547,
3.18077011531719));
#22840=CARTESIAN_POINT('Ctrl Pts',(-2.38568338701886,-4.30201651975012,
3.18633337580742));
#22841=CARTESIAN_POINT('Ctrl Pts',(-2.29927996119546,-4.34880887999953,
3.19189663629766));
#22842=CARTESIAN_POINT('Ctrl Pts',(-2.21156474753462,-4.39296761084829,
3.19745989678789));
#22843=CARTESIAN_POINT('Ctrl Pts',(-2.08296551174435,-4.45770870653298,
3.20561619052175));
#22844=CARTESIAN_POINT('Ctrl Pts',(-1.9514974155078,-4.51681114213254,3.21377248425562));
#22845=CARTESIAN_POINT('Ctrl Pts',(-1.81767327651818,-4.57003795633381,
3.22192877798948));
#22846=CARTESIAN_POINT('Ctrl Pts',(-1.68387641296691,-4.62325392208351,
3.23008340934398));
#22847=CARTESIAN_POINT('Ctrl Pts',(-1.54772477539994,-4.67059653185506,
3.23823804069848));
#22848=CARTESIAN_POINT('Ctrl Pts',(-1.40975087116384,-4.71187707222427,
3.24639267205298));
#22849=CARTESIAN_POINT('Ctrl Pts',(-1.27177207208402,-4.75315907708632,
3.254547592706));
#22850=CARTESIAN_POINT('Ctrl Pts',(-1.13197119649336,-4.78837848268315,
3.26270251335902));
#22851=CARTESIAN_POINT('Ctrl Pts',(-0.990896104083167,-4.81739638948393,
3.27085743401204));
#22852=CARTESIAN_POINT('Ctrl Pts',(-0.849829305904202,-4.84641259023423,
3.27901187521262));
#22853=CARTESIAN_POINT('Ctrl Pts',(-0.707488768775562,-4.86922795512995,
3.28716631641319));
#22854=CARTESIAN_POINT('Ctrl Pts',(-0.56443268956342,-4.88575468085046,
3.29532075761377));
#22855=CARTESIAN_POINT('Ctrl Pts',(-0.421341348532618,-4.90228548023501,
3.30347720879832));
#22856=CARTESIAN_POINT('Ctrl Pts',(-0.277534445550442,-4.91252450437559,
3.31163365998288));
#22857=CARTESIAN_POINT('Ctrl Pts',(-0.133576068908297,-4.91643575126483,
3.31979011116743));
#22858=CARTESIAN_POINT('Ctrl Pts',(-0.0353865604216701,-4.91910349050017,
3.32535337154509));
#22859=CARTESIAN_POINT('Ctrl Pts',(0.0628733040636802,-4.91882851520191,
3.33091663192276));
#22860=CARTESIAN_POINT('Ctrl Pts',(0.161024281146841,-4.91561331304458,
3.33647989230043));
#22861=CARTESIAN_POINT('Ctrl Pts',(0.304923387878341,-4.91089950649726,
3.34463618602925));
#22862=CARTESIAN_POINT('Ctrl Pts',(0.44864230126929,-4.89986174722436,3.35279247975807));
#22863=CARTESIAN_POINT('Ctrl Pts',(0.591617343619236,-4.8825374531312,3.36094877348689));
#22864=CARTESIAN_POINT('Ctrl Pts',(0.734563245433805,-4.86521668999838,
3.3691034048363));
#22865=CARTESIAN_POINT('Ctrl Pts',(0.876765246643208,-4.84161198837913,
3.37725803618572));
#22866=CARTESIAN_POINT('Ctrl Pts',(1.01766547679114,-4.81181255244294,3.38541266753513));
#22867=CARTESIAN_POINT('Ctrl Pts',(1.15857070559862,-4.78201205932441,3.39356758818305));
#22868=CARTESIAN_POINT('Ctrl Pts',(1.29817374275832,-4.74601645769387,3.40172250883096));
#22869=CARTESIAN_POINT('Ctrl Pts',(1.43592708279439,-4.70396603680315,3.40987742947888));
#22870=CARTESIAN_POINT('Ctrl Pts',(1.57367232389534,-4.66191808818376,3.41803187067437));
#22871=CARTESIAN_POINT('Ctrl Pts',(1.70956776563309,-4.61381613110507,3.42618631186987));
#22872=CARTESIAN_POINT('Ctrl Pts',(1.84308128461627,-4.55985026517288,3.43434075306536));
#22873=CARTESIAN_POINT('Ctrl Pts',(1.97662771327811,-4.50587109722215,3.44249720424486));
#22874=CARTESIAN_POINT('Ctrl Pts',(2.10779073549564,-4.44602525745084,3.45065365542437));
#22875=CARTESIAN_POINT('Ctrl Pts',(2.23605785082372,-4.3805511468615,3.45881010660388));
#22876=CARTESIAN_POINT('Ctrl Pts',(2.32354484093858,-4.33589330255544,3.4643733670069));
#22877=CARTESIAN_POINT('Ctrl Pts',(2.40968502205557,-4.28861808848679,3.46993662740992));
#22878=CARTESIAN_POINT('Ctrl Pts',(2.49432220988917,-4.23881348678538,3.47549988781293));
#22879=CARTESIAN_POINT('Ctrl Pts',(2.61840875523016,-4.16579498126317,3.48365618154046));
#22880=CARTESIAN_POINT('Ctrl Pts',(2.7393100219383,-4.08731032099381,3.49181247526798));
#22881=CARTESIAN_POINT('Ctrl Pts',(2.85654901377855,-4.00366217285884,3.49996876899551));
#22882=CARTESIAN_POINT('Ctrl Pts',(2.97376411049001,-3.92003107351662,3.5081234003436));
#22883=CARTESIAN_POINT('Ctrl Pts',(3.08731814915654,-3.83123878003184,3.51627803169169));
#22884=CARTESIAN_POINT('Ctrl Pts',(3.19676402067485,-3.73763064769899,3.52443266303979));
#22885=CARTESIAN_POINT('Ctrl Pts',(3.3062137749589,-3.64401919446929,3.53258758368635));
#22886=CARTESIAN_POINT('Ctrl Pts',(3.41155481370656,-3.54559177517056,3.54074250433291));
#22887=CARTESIAN_POINT('Ctrl Pts',(3.51237358098929,-3.44273363623567,3.54889742497948));
#22888=CARTESIAN_POINT('Ctrl Pts',(3.61318642083169,-3.33988154464193,3.55705186617359));
#22889=CARTESIAN_POINT('Ctrl Pts',(3.70947728754711,-3.23259949423101,3.56520630736769));
#22890=CARTESIAN_POINT('Ctrl Pts',(3.80086997320993,-3.12130910184351,3.5733607485618));
#22891=CARTESIAN_POINT('Ctrl Pts',(3.89228518620883,-3.00999127754444,3.58151719973992));
#22892=CARTESIAN_POINT('Ctrl Pts',(3.9787995929389,-2.89466339558759,3.58967365091805));
#22893=CARTESIAN_POINT('Ctrl Pts',(4.06007733465013,-2.77578008840043,3.59783010209617));
#22894=CARTESIAN_POINT('Ctrl Pts',(4.11551434184627,-2.69469350039641,3.60339336250593));
#22895=CARTESIAN_POINT('Ctrl Pts',(4.16851600626716,-2.61195354475019,3.60895662291568));
#22896=CARTESIAN_POINT('Ctrl Pts',(4.21898731285054,-2.52771222976552,3.61451988332544));
#22897=CARTESIAN_POINT('Ctrl Pts',(4.29298327405157,-2.40420607355315,3.62267617705545));
#22898=CARTESIAN_POINT('Ctrl Pts',(4.36156610255951,-2.27742534222545,3.63083247078547));
#22899=CARTESIAN_POINT('Ctrl Pts',(4.42446187416758,-2.14786409871237,3.63898876451548));
#22900=CARTESIAN_POINT('Ctrl Pts',(4.48734482664008,-2.01832926179393,3.6471433958661));
#22901=CARTESIAN_POINT('Ctrl Pts',(4.54454288850908,-1.88601534411718,3.65529802721671));
#22902=CARTESIAN_POINT('Ctrl Pts',(4.59582880990886,-1.75143958288938,3.66345265856733));
#22903=CARTESIAN_POINT('Ctrl Pts',(4.64711655075822,-1.61685904737255,3.67160757921645));
#22904=CARTESIAN_POINT('Ctrl Pts',(4.69249160875898,-1.48001681910063,3.67976249986557));
#22905=CARTESIAN_POINT('Ctrl Pts',(4.73177528819497,-1.34144909874636,3.68791742051469));
#22906=CARTESIAN_POINT('Ctrl Pts',(4.77105665802468,-1.20288952520729,3.69607186171138));
#22907=CARTESIAN_POINT('Ctrl Pts',(4.8042472754084,-1.06260498477754,3.70422630290806));
#22908=CARTESIAN_POINT('Ctrl Pts',(4.83121864536603,-0.92114573394641,3.71238074410475));
#22909=CARTESIAN_POINT('Ctrl Pts',(4.85819666348274,-0.779651614897389,
3.72053719528544));
#22910=CARTESIAN_POINT('Ctrl Pts',(4.87895230800256,-0.636982535690397,
3.72869364646614));
#22911=CARTESIAN_POINT('Ctrl Pts',(4.89340831385697,-0.493698426547547,
3.73685009764683));
#22912=CARTESIAN_POINT('Ctrl Pts',(4.90326830358628,-0.395968814457495,
3.74241335804388));
#22913=CARTESIAN_POINT('Ctrl Pts',(4.91019865819268,-0.297953270626755,
3.74797661844093));
#22914=CARTESIAN_POINT('Ctrl Pts',(4.91418871620659,-0.19983073839571,3.75353987883798));
#22915=CARTESIAN_POINT('Ctrl Pts',(4.92003853858251,-0.0559733351636417,
3.7616961725661));
#22916=CARTESIAN_POINT('Ctrl Pts',(4.91956821809947,0.0881680433193258,
3.76985246629422));
#22917=CARTESIAN_POINT('Ctrl Pts',(4.91277374208493,0.232028493036589,3.77800876002234));
#22918=CARTESIAN_POINT('Ctrl Pts',(4.9059806508902,0.375859621758297,3.78616339137103));
#22919=CARTESIAN_POINT('Ctrl Pts',(4.89286599134167,0.519409601861859,3.79431802271972));
#22920=CARTESIAN_POINT('Ctrl Pts',(4.87347782343726,0.662115523881759,3.80247265406841));
#22921=CARTESIAN_POINT('Ctrl Pts',(4.85408896770682,0.804826508620698,3.81062757471558));
#22922=CARTESIAN_POINT('Ctrl Pts',(4.82842619959451,0.9466930432584,3.81878249536277));
#22923=CARTESIAN_POINT('Ctrl Pts',(4.79658928665563,1.08715880976077,3.82693741600994));
#22924=CARTESIAN_POINT('Ctrl Pts',(4.76475424550513,1.22761631785595,3.83509185720468));
#22925=CARTESIAN_POINT('Ctrl Pts',(4.72674586065017,1.36667289640204,3.84324629839941));
#22926=CARTESIAN_POINT('Ctrl Pts',(4.68271470376923,1.5037839158614,3.85140073959414));
#22927=CARTESIAN_POINT('Ctrl Pts',(4.63867269367109,1.6409287317454,3.85955719077288));
#22928=CARTESIAN_POINT('Ctrl Pts',(4.58860504723008,1.77612671143222,3.86771364195163));
#22929=CARTESIAN_POINT('Ctrl Pts',(4.53271194629992,1.90884925396689,3.87587009313038));
#22930=CARTESIAN_POINT('Ctrl Pts',(4.49458900917956,1.99937515178435,3.88143335353708));
#22931=CARTESIAN_POINT('Ctrl Pts',(4.4537569969221,2.08874977601324,3.88699661394379));
#22932=CARTESIAN_POINT('Ctrl Pts',(4.4102922031268,2.17681091175577,3.89255987435049));
#22933=CARTESIAN_POINT('Ctrl Pts',(4.34656848732789,2.3059173056205,3.90071616807966));
#22934=CARTESIAN_POINT('Ctrl Pts',(4.27715977948955,2.4322477828378,3.90887246180882));
#22935=CARTESIAN_POINT('Ctrl Pts',(4.20233295759496,2.55530443900746,3.91702875553799));
#22936=CARTESIAN_POINT('Ctrl Pts',(4.12752138656948,2.67833601431827,3.92518338688774));
#22937=CARTESIAN_POINT('Ctrl Pts',(4.0472940782565,2.7980948139492,3.9333380182375));
#22938=CARTESIAN_POINT('Ctrl Pts',(3.96196267552736,2.91410961019452,3.94149264958725));
#22939=CARTESIAN_POINT('Ctrl Pts',(3.87662824553121,3.03012852224896,3.9496475702355));
#22940=CARTESIAN_POINT('Ctrl Pts',(3.78618955403156,3.14240289333373,3.95780249088375));
#22941=CARTESIAN_POINT('Ctrl Pts',(3.69100048784357,3.25049203371405,3.965957411532));
#22942=CARTESIAN_POINT('Ctrl Pts',(3.59581701810863,3.35857481920695,3.97411185272781));
#22943=CARTESIAN_POINT('Ctrl Pts',(3.49588395433114,3.46247261574569,3.98226629392362));
#22944=CARTESIAN_POINT('Ctrl Pts',(3.39159419425969,3.56177931432647,3.99042073511942));
#22945=CARTESIAN_POINT('Ctrl Pts',(3.28727872785898,3.66111049096425,3.99857718629924));
#22946=CARTESIAN_POINT('Ctrl Pts',(3.17860466161559,3.75584807729086,4.00673363747906));
#22947=CARTESIAN_POINT('Ctrl Pts',(3.06600077847207,3.8456237841095,4.01489008865887));
#22948=CARTESIAN_POINT('Ctrl Pts',(2.98919718946959,3.9068569875872,4.02045334906025));
#22949=CARTESIAN_POINT('Ctrl Pts',(2.9105661194372,3.9657826313092,4.02601660946162));
#22950=CARTESIAN_POINT('Ctrl Pts',(2.83025220084745,4.02229481044069,4.031579869863));
#22951=CARTESIAN_POINT('Ctrl Pts',(2.71250399866715,4.10514729243719,4.03973616359172));
#22952=CARTESIAN_POINT('Ctrl Pts',(2.59109313482248,4.18284130981275,4.04789245732045));
#22953=CARTESIAN_POINT('Ctrl Pts',(2.46649225777634,4.25506745009164,4.05604875104917));
#22954=CARTESIAN_POINT('Ctrl Pts',(2.34191677632543,4.32727886956063,4.06420338239847));
#22955=CARTESIAN_POINT('Ctrl Pts',(2.21415286808394,4.39402446744359,4.07235801374778));
#22956=CARTESIAN_POINT('Ctrl Pts',(2.08369971566118,4.4550396807945,4.08051264509708));
#22957=CARTESIAN_POINT('Ctrl Pts',(1.95324193520567,4.51605705875699,4.08866756574487));
#22958=CARTESIAN_POINT('Ctrl Pts',(1.82009502119072,4.57134350021133,4.09682248639267));
#22959=CARTESIAN_POINT('Ctrl Pts',(1.68478062872527,4.62068147523415,4.10497740704047));
#22960=CARTESIAN_POINT('Ctrl Pts',(1.54947419180213,4.67001654952823,4.11313184823582));
#22961=CARTESIAN_POINT('Ctrl Pts',(1.41200084611465,4.71340374331629,4.12128628943118));
#22962=CARTESIAN_POINT('Ctrl Pts',(1.27289994556292,4.75067456168973,4.12944073062653));
#22963=CARTESIAN_POINT('Ctrl Pts',(1.1337647581018,4.78795456692801,4.1375971818059));
#22964=CARTESIAN_POINT('Ctrl Pts',(0.993001537475622,4.81911509730807,4.14575363298527));
#22965=CARTESIAN_POINT('Ctrl Pts',(0.851163041547939,4.84403804064366,4.15391008416463));
#22966=CARTESIAN_POINT('Ctrl Pts',(0.75441943691503,4.86103720127757,4.15947334456826));
#22967=CARTESIAN_POINT('Ctrl Pts',(0.657175864064126,4.87513557740796,4.16503660497188));
#22968=CARTESIAN_POINT('Ctrl Pts',(0.559610002962579,4.88630941581519,4.17059986537551));
#22969=CARTESIAN_POINT('Ctrl Pts',(0.416568735195624,4.90269137558625,4.17875615910436));
#22970=CARTESIAN_POINT('Ctrl Pts',(0.272780852319435,4.91279102578247,4.18691245283321));
#22971=CARTESIAN_POINT('Ctrl Pts',(0.128809443601766,4.91656294475511,4.19506874656206));
#22972=CARTESIAN_POINT('Ctrl Pts',(-0.015132621505391,4.92033409495204,
4.20322337791149));
#22973=CARTESIAN_POINT('Ctrl Pts',(-0.159257803496844,4.91778007801928,
4.21137800926093));
#22974=CARTESIAN_POINT('Ctrl Pts',(-0.303001184225554,4.90890755106041,
4.21953264061036));
#22975=CARTESIAN_POINT('Ctrl Pts',(-0.44674966447892,4.90003470933456,4.22768756125829));
#22976=CARTESIAN_POINT('Ctrl Pts',(-0.590115982131058,4.88484292590067,
4.23584248190621));
#22977=CARTESIAN_POINT('Ctrl Pts',(-0.732538001433465,4.86339090953584,
4.24399740255414));
#22978=CARTESIAN_POINT('Ctrl Pts',(-0.874951647314697,4.84194015439993,
4.25215184374962));
#22979=CARTESIAN_POINT('Ctrl Pts',(-1.01642077512721,4.81422995346369,4.26030628494511));
#22980=CARTESIAN_POINT('Ctrl Pts',(-1.15639118110785,4.78037053990127,4.26846072614059));
#22981=CARTESIAN_POINT('Ctrl Pts',(-1.29639608832175,4.74650278034945,4.27661717732008));
#22982=CARTESIAN_POINT('Ctrl Pts',(-1.43490121004777,4.70648285792434,4.28477362849958));
#22983=CARTESIAN_POINT('Ctrl Pts',(-1.5713646904547,4.66047165768575,4.29293007967907));
#22984=CARTESIAN_POINT('Ctrl Pts',(-1.66444216499551,4.62908885617704,4.29849334008206));
#22985=CARTESIAN_POINT('Ctrl Pts',(-1.75657009904651,4.59491985801175,4.30405660048505));
#22986=CARTESIAN_POINT('Ctrl Pts',(-1.84758112035478,4.55802885754452,4.30961986088805));
#22987=CARTESIAN_POINT('Ctrl Pts',(-1.98101234028353,4.50394297732938,4.3177761546169));
#22988=CARTESIAN_POINT('Ctrl Pts',(-2.11209194922994,4.44398387197782,4.32593244834574));
#22989=CARTESIAN_POINT('Ctrl Pts',(-2.24030381501284,4.37838119388193,4.33408874207459));
#22990=CARTESIAN_POINT('Ctrl Pts',(-2.36848954922497,4.31279188663135,4.34224337342402));
#22991=CARTESIAN_POINT('Ctrl Pts',(-2.49380840855865,4.24156145365597,4.35039800477345));
#22992=CARTESIAN_POINT('Ctrl Pts',(-2.61576758348047,4.1649661477271,4.35855263612289));
#22993=CARTESIAN_POINT('Ctrl Pts',(-2.73773108509767,4.08836812445814,4.36670755677081));
#22994=CARTESIAN_POINT('Ctrl Pts',(-2.85633437841711,4.00640502218146,4.37486247741874));
#22995=CARTESIAN_POINT('Ctrl Pts',(-2.9711120122765,3.91939746300452,4.38301739806667));
#22996=CARTESIAN_POINT('Ctrl Pts',(-3.08588289801159,3.83239501926519,4.39117183926214));
#22997=CARTESIAN_POINT('Ctrl Pts',(-3.19682830814788,3.74034891489571,4.39932628045761));
#22998=CARTESIAN_POINT('Ctrl Pts',(-3.30351441882262,3.64362121345387,4.40748072165309));
#22999=CARTESIAN_POINT('Ctrl Pts',(-3.41022682650205,3.54686966965053,4.41563717283259));
#23000=CARTESIAN_POINT('Ctrl Pts',(-3.51267758864691,3.44543444760598,4.42379362401209));
#23001=CARTESIAN_POINT('Ctrl Pts',(-3.6104679682363,3.33971617249724,4.43195007519159));
#23002=CARTESIAN_POINT('Ctrl Pts',(-3.67716772951608,3.2676090414863,4.43751333559458));
#23003=CARTESIAN_POINT('Ctrl Pts',(-3.74170013640878,3.19351015398629,4.44307659599756));
#23004=CARTESIAN_POINT('Ctrl Pts',(-3.80394896442723,3.11755598803502,4.44863985640055));
#23005=CARTESIAN_POINT('Ctrl Pts',(-3.89521127194652,3.00620043852392,4.45679608998549));
#23006=CARTESIAN_POINT('Ctrl Pts',(-3.98159762459806,2.89081391760571,4.46495232357044));
#23007=CARTESIAN_POINT('Ctrl Pts',(-4.06276479474703,2.7718451048109,4.47310855715538));
#23008=CARTESIAN_POINT('Ctrl Pts',(-4.14392472648238,2.65288690154543,4.48126406337491));
#23009=CARTESIAN_POINT('Ctrl Pts',(-4.21986621201662,2.53034731756149,4.48941956959444));
#23010=CARTESIAN_POINT('Ctrl Pts',(-4.29028870489178,2.40470494888209,4.49757507581397));
#23011=CARTESIAN_POINT('Ctrl Pts',(-4.36070101043729,2.27908075564884,4.5057294022566));
#23012=CARTESIAN_POINT('Ctrl Pts',(-4.42559575425122,2.15035496606688,4.51388372869923));
#23013=CARTESIAN_POINT('Ctrl Pts',(-4.48471780196106,2.01903177272512,4.52203805514186));
#23014=CARTESIAN_POINT('Ctrl Pts',(-4.54384996796169,1.88768610441323,4.53019377713572));
#23015=CARTESIAN_POINT('Ctrl Pts',(-4.59720732361368,1.75374244818986,4.53834949912957));
#23016=CARTESIAN_POINT('Ctrl Pts',(-4.64458218845451,1.61772660149702,4.54650522112343));
#23017=CARTESIAN_POINT('Ctrl Pts',(-4.6899266988647,1.48754001422048,4.55431141164441));
#23018=CARTESIAN_POINT('Ctrl Pts',(-4.72979074132213,1.3554554268238,4.56211760216538));
#23019=CARTESIAN_POINT('Ctrl Pts',(-4.76403458704967,1.22194824599672,4.56992379268636));
#23020=CARTESIAN_POINT('Origin',(0.,0.,-3.23514056400928));
#23021=CARTESIAN_POINT('',(-4.76403458034885,1.22194827212136,6.66505438904205));
#23022=CARTESIAN_POINT('',(-4.76403458747083,1.22194824435476,6.31969203503535));
#23023=CARTESIAN_POINT('',(-4.76403458704967,1.22194824599672,-3.23514056400928));
#23024=CARTESIAN_POINT('Ctrl Pts',(-4.76403458034885,1.22194827212136,6.66505438904205));
#23025=CARTESIAN_POINT('Ctrl Pts',(-4.75505291261507,1.25696528278306,6.66298850631862));
#23026=CARTESIAN_POINT('Ctrl Pts',(-4.74568433605323,1.29188650858914,6.66092426077554));
#23027=CARTESIAN_POINT('Ctrl Pts',(-4.72449276544513,1.36753389112058,6.65644513873832));
#23028=CARTESIAN_POINT('Ctrl Pts',(-4.71252769295444,1.40821291880656,6.6540317517054));
#23029=CARTESIAN_POINT('Ctrl Pts',(-4.68968816954983,1.48230985312338,6.64962908124611));
#23030=CARTESIAN_POINT('Ctrl Pts',(-4.67897876636642,1.51577550090678,6.64763839000519));
#23031=CARTESIAN_POINT('Ctrl Pts',(-4.65012316235656,1.60272490653033,6.64245950934314));
#23032=CARTESIAN_POINT('Ctrl Pts',(-4.63141271811348,1.6560159708516,6.6392778831609));
#23033=CARTESIAN_POINT('Ctrl Pts',(-4.55420902715638,1.86435572332271,6.62678545022193));
#23034=CARTESIAN_POINT('Ctrl Pts',(-4.48881326221942,2.01672959488548,6.61752663069273));
#23035=CARTESIAN_POINT('Ctrl Pts',(-4.37846410109284,2.24175049097104,6.6034728686409));
#23036=CARTESIAN_POINT('Ctrl Pts',(-4.33910929904637,2.31700743735292,6.5987057137598));
#23037=CARTESIAN_POINT('Ctrl Pts',(-4.26698211854503,2.44664491726981,6.5903540301376));
#23038=CARTESIAN_POINT('Ctrl Pts',(-4.23506843588337,2.50148015991019,6.58677612860693));
#23039=CARTESIAN_POINT('Ctrl Pts',(-4.19016792796188,2.57530645830695,6.58189167470789));
#23040=CARTESIAN_POINT('Ctrl Pts',(-4.17809541004328,2.59484669257407,6.58059231133437));
#23041=CARTESIAN_POINT('Ctrl Pts',(-4.12745358626396,2.67554437873976,6.5751982836492));
#23042=CARTESIAN_POINT('Ctrl Pts',(-4.08767517773607,2.73593170727836,6.57109478331718));
#23043=CARTESIAN_POINT('Ctrl Pts',(-3.95523792012639,2.92764460434511,6.55783802478645));
#23044=CARTESIAN_POINT('Ctrl Pts',(-3.85747061087693,3.05531165048024,6.54864997535199));
#23045=CARTESIAN_POINT('Ctrl Pts',(-3.69277304997032,3.24984320941998,6.5340590108467));
#23046=CARTESIAN_POINT('Ctrl Pts',(-3.62986294409184,3.31996217299349,6.52866743971978));
#23047=CARTESIAN_POINT('Ctrl Pts',(-3.54417482744182,3.41012019448496,6.52156590829522));
#23048=CARTESIAN_POINT('Ctrl Pts',(-3.52317027865099,3.43181674178445,6.51984344301824));
#23049=CARTESIAN_POINT('Ctrl Pts',(-3.47075695006869,3.48496844323916,6.5155910619581));
#23050=CARTESIAN_POINT('Ctrl Pts',(-3.43911884753746,3.5161940318753,6.51306391684743));
#23051=CARTESIAN_POINT('Ctrl Pts',(-3.40480624655665,3.54915303496321,6.5103665230686));
#23052=CARTESIAN_POINT('Ctrl Pts',(-3.40254884346799,3.55131724998179,6.5101892614159));
#23053=CARTESIAN_POINT('Ctrl Pts',(-3.3711902837044,3.58132394715409,6.50772959715056));
#23054=CARTESIAN_POINT('Ctrl Pts',(-3.34175020300759,3.60881015874752,6.50545349185294));
#23055=CARTESIAN_POINT('Ctrl Pts',(-3.21999529407643,3.71971687890301,6.49616462279559));
#23056=CARTESIAN_POINT('Ctrl Pts',(-3.12486774972677,3.79998231490071,6.48919307074476));
#23057=CARTESIAN_POINT('Ctrl Pts',(-2.93079217792192,3.95151573038195,6.47539790114408));
#23058=CARTESIAN_POINT('Ctrl Pts',(-2.83203510991717,4.02288407463644,6.46857903313706));
#23059=CARTESIAN_POINT('Ctrl Pts',(-2.67210110888603,4.12965230280731,6.45777664631409));
#23060=CARTESIAN_POINT('Ctrl Pts',(-2.61263679817657,4.16752700209775,6.45381027575064));
#23061=CARTESIAN_POINT('Ctrl Pts',(-2.49930083493202,4.23633499212036,6.44633190318421));
#23062=CARTESIAN_POINT('Ctrl Pts',(-2.44561716792784,4.2675514517855,6.44282276636853));
#23063=CARTESIAN_POINT('Ctrl Pts',(-2.3368380924093,4.32807848562137,6.43577180011353));
#23064=CARTESIAN_POINT('Ctrl Pts',(-2.28174705272022,4.35737374228495,6.43223053360669));
#23065=CARTESIAN_POINT('Ctrl Pts',(-2.04752053710706,4.47626589059256,6.41728968137762));
#23066=CARTESIAN_POINT('Ctrl Pts',(-1.8635582535988,4.55592420511864,6.40582588817387));
#23067=CARTESIAN_POINT('Ctrl Pts',(-1.60647653706328,4.64906094520833,6.39017784295997));
#23068=CARTESIAN_POINT('Ctrl Pts',(-1.53714954813042,4.67244110882362,6.3859946935986));
#23069=CARTESIAN_POINT('Ctrl Pts',(-1.45744423016982,4.69735527515177,6.3812316035804));
#23070=CARTESIAN_POINT('Ctrl Pts',(-1.44755214990964,4.70041307109342,6.38064127473213));
#23071=CARTESIAN_POINT('Ctrl Pts',(-1.43142391771011,4.70534281668329,6.37968013307018));
#23072=CARTESIAN_POINT('Ctrl Pts',(-1.4251935818189,4.707233657808,6.37930916943893));
#23073=CARTESIAN_POINT('Ctrl Pts',(-1.41493713736025,4.71032415108176,6.37869902655022));
#23074=CARTESIAN_POINT('Ctrl Pts',(-1.41091321697408,4.71153102559629,6.3784597855265));
#23075=CARTESIAN_POINT('Ctrl Pts',(-1.40421970740588,4.71352923282481,6.37806205416633));
#23076=CARTESIAN_POINT('Ctrl Pts',(-1.40155098502394,4.71432345642007,6.37790353803809));
#23077=CARTESIAN_POINT('Ctrl Pts',(-1.39706969128375,4.71565296773759,6.37763746140108));
#23078=CARTESIAN_POINT('Ctrl Pts',(-1.39525748384109,4.71618947755765,6.37752988968853));
#23079=CARTESIAN_POINT('Ctrl Pts',(-1.38940424563578,4.7179186785217,6.37718253527371));
#23080=CARTESIAN_POINT('Ctrl Pts',(-1.38536198918495,4.71910722212408,6.37694279147449));
#23081=CARTESIAN_POINT('Ctrl Pts',(-1.37775302904576,4.72133386368881,6.3764917735986));
#23082=CARTESIAN_POINT('Ctrl Pts',(-1.37418666733051,4.72237311791691,6.37628048844328));
#23083=CARTESIAN_POINT('Ctrl Pts',(-1.36739265981452,4.72434457496952,6.37587819476449));
#23084=CARTESIAN_POINT('Ctrl Pts',(-1.36416522986907,4.72527751299334,6.37568717897338));
#23085=CARTESIAN_POINT('Ctrl Pts',(-1.35792813542062,4.72707351798856,6.37531821094751));
#23086=CARTESIAN_POINT('Ctrl Pts',(-1.35491859785934,4.7279370193174,6.37514025431216));
#23087=CARTESIAN_POINT('Ctrl Pts',(-1.34899897616601,4.7296293702954,6.37479037744119));
#23088=CARTESIAN_POINT('Ctrl Pts',(-1.34608894767503,4.73045840939594,6.37461845526892));
#23089=CARTESIAN_POINT('Ctrl Pts',(-1.34023266555534,4.732120966313,6.37427262028375));
#23090=CARTESIAN_POINT('Ctrl Pts',(-1.33728639481368,4.73295441937781,6.37409870824192));
#23091=CARTESIAN_POINT('Ctrl Pts',(-1.33116322699456,4.73468039204758,6.37373742975056));
#23092=CARTESIAN_POINT('Ctrl Pts',(-1.32798620575799,4.73557246688148,6.37355006832861));
#23093=CARTESIAN_POINT('Ctrl Pts',(-1.28986941822881,4.74623389369983,6.37130324390293));
#23094=CARTESIAN_POINT('Ctrl Pts',(-1.25482350222769,4.75561954983394,6.36924857836905));
#23095=CARTESIAN_POINT('Ctrl Pts',(-1.15875382208113,4.78021206934293,6.36364480665791));
#23096=CARTESIAN_POINT('Ctrl Pts',(-1.09753708320753,4.79463766543657,6.36010444669954));
#23097=CARTESIAN_POINT('Ctrl Pts',(-0.871528752343353,4.8433406150259,6.34711399386901));
#23098=CARTESIAN_POINT('Ctrl Pts',(-0.705285391828655,4.87032685390479,
6.33771099634563));
#23099=CARTESIAN_POINT('Ctrl Pts',(-0.458089588479042,4.89752975584298,
6.32375995828713));
#23100=CARTESIAN_POINT('Ctrl Pts',(-0.377990319456553,4.90436203183482,
6.3192448107855));
#23101=CARTESIAN_POINT('Ctrl Pts',(-0.235976477483957,4.91297561879717,
6.31123149464127));
#23102=CARTESIAN_POINT('Ctrl Pts',(-0.174127975481252,4.91555629390999,
6.3077389642151));
#23103=CARTESIAN_POINT('Ctrl Pts',(-0.0906651904439789,4.91746163501598,
6.30301775753363));
#23104=CARTESIAN_POINT('Ctrl Pts',(-0.0690797546309547,4.91781222615031,
6.30179601839482));
#23105=CARTESIAN_POINT('Ctrl Pts',(-0.0375893330700961,4.91811632554639,
6.30001243295995));
#23106=CARTESIAN_POINT('Ctrl Pts',(-0.0276856480126512,4.91818204767071,
6.29945132216187));
#23107=CARTESIAN_POINT('Ctrl Pts',(0.060659982620095,4.91850146177112,6.29444428451768));
#23108=CARTESIAN_POINT('Ctrl Pts',(0.139096678902155,4.91690839582929,6.28998694593467));
#23109=CARTESIAN_POINT('Ctrl Pts',(0.415322610096975,4.9046830776884,6.27423594043361));
#23110=CARTESIAN_POINT('Ctrl Pts',(0.612473311370285,4.88398239220987,6.2628888263114));
#23111=CARTESIAN_POINT('Ctrl Pts',(0.868519580157669,4.84134707518105,6.24804302721082));
#23112=CARTESIAN_POINT('Ctrl Pts',(0.929009381230061,4.83010449364666,6.24452846921355));
#23113=CARTESIAN_POINT('Ctrl Pts',(0.99272249287965,4.81702164391451,6.24082178848324));
#23114=CARTESIAN_POINT('Ctrl Pts',(0.996171586210946,4.81630954535316,6.24062111343635));
#23115=CARTESIAN_POINT('Ctrl Pts',(1.00231462985883,4.81503437367392,6.2402636737355));
#23116=CARTESIAN_POINT('Ctrl Pts',(1.00500887742851,4.81447274301061,6.24010689731957));
#23117=CARTESIAN_POINT('Ctrl Pts',(1.00982492309684,4.81346459305426,6.23982663993378));
#23118=CARTESIAN_POINT('Ctrl Pts',(1.01194689963991,4.81301893162801,6.23970315176186));
#23119=CARTESIAN_POINT('Ctrl Pts',(1.01575287342502,4.81221696574699,6.23948165449011));
#23120=CARTESIAN_POINT('Ctrl Pts',(1.01743697940885,4.81186118027409,6.23938364093418));
#23121=CARTESIAN_POINT('Ctrl Pts',(1.02046693005426,4.81121940886602,6.23920729473771));
#23122=CARTESIAN_POINT('Ctrl Pts',(1.02181284199485,4.81093374216684,6.23912895930726));
#23123=CARTESIAN_POINT('Ctrl Pts',(1.02424101873759,4.81041730233331,6.23898762984015));
#23124=CARTESIAN_POINT('Ctrl Pts',(1.02532332577159,4.81018672867091,6.23892463403583));
#23125=CARTESIAN_POINT('Ctrl Pts',(1.02728067224731,4.80976904680777,6.23881070420938));
#23126=CARTESIAN_POINT('Ctrl Pts',(1.02815573855833,4.80958206505233,6.23875976905424));
#23127=CARTESIAN_POINT('Ctrl Pts',(1.0312575981321,4.80891838303017,6.23857921566115));
#23128=CARTESIAN_POINT('Ctrl Pts',(1.03348411195619,4.80844037487127,6.23844960928702));
#23129=CARTESIAN_POINT('Ctrl Pts',(1.03776957209151,4.80751721943354,6.2382001410315));
#23130=CARTESIAN_POINT('Ctrl Pts',(1.03982856589221,4.80707229542779,6.23808027711206));
#23131=CARTESIAN_POINT('Ctrl Pts',(1.04380143369296,4.80621113411409,6.23784898934926));
#23132=CARTESIAN_POINT('Ctrl Pts',(1.0457153460761,4.80579507611878,6.23773756383627));
#23133=CARTESIAN_POINT('Ctrl Pts',(1.04941790323329,4.80498787502239,6.23752199897226));
#23134=CARTESIAN_POINT('Ctrl Pts',(1.05120657906983,4.80459687620753,6.23741785825338));
#23135=CARTESIAN_POINT('Ctrl Pts',(1.05467635076287,4.80383636485059,6.23721583462095));
#23136=CARTESIAN_POINT('Ctrl Pts',(1.05635747175302,4.80346696845043,6.2371179505881));
#23137=CARTESIAN_POINT('Ctrl Pts',(1.05962803824502,4.80274651971525,6.23692751542934));
#23138=CARTESIAN_POINT('Ctrl Pts',(1.06121750402719,4.80239556067814,6.23683496339089));
#23139=CARTESIAN_POINT('Ctrl Pts',(1.06431922715129,4.80170907539325,6.23665435073376));
#23140=CARTESIAN_POINT('Ctrl Pts',(1.06583150075843,4.8013736236614,6.23656628937612));
#23141=CARTESIAN_POINT('Ctrl Pts',(1.06879219197714,4.80071541699266,6.23639388126694));
#23142=CARTESIAN_POINT('Ctrl Pts',(1.07024062246942,4.800392720872,6.23630953392497));
#23143=CARTESIAN_POINT('Ctrl Pts',(1.07308617863345,4.79975740693362,6.23614382350653));
#23144=CARTESIAN_POINT('Ctrl Pts',(1.07448331426839,4.79944483451463,6.23606245996961));
#23145=CARTESIAN_POINT('Ctrl Pts',(1.07723834989331,4.79882720432505,6.23590201473469));
#23146=CARTESIAN_POINT('Ctrl Pts',(1.07859625726497,4.79852218013702,6.23582293269291));
#23147=CARTESIAN_POINT('Ctrl Pts',(1.08128476850906,4.79791706602453,6.2356663558697));
#23148=CARTESIAN_POINT('Ctrl Pts',(1.0826153773714,4.79761699885891,6.23558886085435));
#23149=CARTESIAN_POINT('Ctrl Pts',(1.08526148481792,4.7970191151694,6.23543474818395));
#23150=CARTESIAN_POINT('Ctrl Pts',(1.08657698606536,4.79672131096697,6.23535813040358));
#23151=CARTESIAN_POINT('Ctrl Pts',(1.08920582483537,4.79612505545591,6.23520501832044));
#23152=CARTESIAN_POINT('Ctrl Pts',(1.09051916260437,4.79582660575023,6.23512852400704));
#23153=CARTESIAN_POINT('Ctrl Pts',(1.09315802586402,4.79522579670934,6.23497482304469));
#23154=CARTESIAN_POINT('Ctrl Pts',(1.09448354891775,4.79492342713498,6.23489761651428));
#23155=CARTESIAN_POINT('Ctrl Pts',(1.13163389226899,4.78643272832944,6.23273372039523));
#23156=CARTESIAN_POINT('Ctrl Pts',(1.167365992197,4.7778436778543,6.23065186505073));
#23157=CARTESIAN_POINT('Ctrl Pts',(1.26108226973158,4.75420265967878,6.22518900332407));
#23158=CARTESIAN_POINT('Ctrl Pts',(1.3188935781906,4.73849040072027,6.2218154483081));
#23159=CARTESIAN_POINT('Ctrl Pts',(1.54600360218853,4.67228682817117,6.20851912784474));
#23160=CARTESIAN_POINT('Ctrl Pts',(1.71281707632494,4.61374572264444,6.19865240601285));
#23161=CARTESIAN_POINT('Ctrl Pts',(1.949312425594,4.51615252936203,6.18429830060129));
#23162=CARTESIAN_POINT('Ctrl Pts',(2.02176505733343,4.48418537735761,6.17984973597581));
#23163=CARTESIAN_POINT('Ctrl Pts',(2.15920419261345,4.41953689463318,6.17129398964628));
#23164=CARTESIAN_POINT('Ctrl Pts',(2.2242996883834,4.38713572201046,6.16718972478682));
#23165=CARTESIAN_POINT('Ctrl Pts',(2.34414037810097,4.32413214865336,6.15952609099346));
#23166=CARTESIAN_POINT('Ctrl Pts',(2.39906509548357,4.29390259684177,6.15597027785549));
#23167=CARTESIAN_POINT('Ctrl Pts',(2.57346388113466,4.19352578333136,6.14453177441374));
#23168=CARTESIAN_POINT('Ctrl Pts',(2.69055640005642,4.11937862322729,6.13662254651122));
#23169=CARTESIAN_POINT('Ctrl Pts',(2.90104761213393,3.973280459457,6.12196146902832));
#23170=CARTESIAN_POINT('Ctrl Pts',(2.99529419151232,3.90272310855013,6.11521961735173));
#23171=CARTESIAN_POINT('Ctrl Pts',(3.12632222687714,3.79708496361556,6.10560355625454));
#23172=CARTESIAN_POINT('Ctrl Pts',(3.16523304397283,3.76471044376927,6.10271574716572));
#23173=CARTESIAN_POINT('Ctrl Pts',(3.23541406174684,3.70446120902258,6.09745073254636));
#23174=CARTESIAN_POINT('Ctrl Pts',(3.26684121389002,3.67677651442494,6.09507163172042));
#23175=CARTESIAN_POINT('Ctrl Pts',(3.32897585484533,3.6206154474906,6.09032693093945));
#23176=CARTESIAN_POINT('Ctrl Pts',(3.35968094526277,3.59214148680241,6.08796152479812));
#23177=CARTESIAN_POINT('Ctrl Pts',(3.48553005266798,3.47241162842158,6.07816883169562));
#23178=CARTESIAN_POINT('Ctrl Pts',(3.57735020373068,3.37774015181016,6.07078637853904));
#23179=CARTESIAN_POINT('Ctrl Pts',(3.74907740499654,3.18581287119434,6.05635853620959));
#23180=CARTESIAN_POINT('Ctrl Pts',(3.82927533135065,3.08895373242096,6.04931881081417));
#23181=CARTESIAN_POINT('Ctrl Pts',(3.92977793066721,2.95763442778058,6.04002203543174));
#23182=CARTESIAN_POINT('Ctrl Pts',(3.95349998667428,2.92584924857875,6.03779009309128));
#23183=CARTESIAN_POINT('Ctrl Pts',(4.01888434562909,2.83599351169465,6.03152822775744));
#23184=CARTESIAN_POINT('Ctrl Pts',(4.05966887959046,2.77729707007067,6.02749255185915));
#23185=CARTESIAN_POINT('Ctrl Pts',(4.13917549979702,2.65737716083884,6.01934613489417));
#23186=CARTESIAN_POINT('Ctrl Pts',(4.17785319833812,2.59614515805817,6.01523610089585));
#23187=CARTESIAN_POINT('Ctrl Pts',(4.2969355736181,2.39806482897949,6.00208646252366));
#23188=CARTESIAN_POINT('Ctrl Pts',(4.37207426185078,2.25817089607497,5.99301328546572));
#23189=CARTESIAN_POINT('Ctrl Pts',(4.48123260798426,2.02898765791976,5.9784817257964));
#23190=CARTESIAN_POINT('Ctrl Pts',(4.51964665389634,1.9419142271221,5.97303465029629));
#23191=CARTESIAN_POINT('Ctrl Pts',(4.57880891142312,1.79652796864221,5.96407262707049));
#23192=CARTESIAN_POINT('Ctrl Pts',(4.60102584087305,1.73884016898957,5.96055030402325));
#23193=CARTESIAN_POINT('Ctrl Pts',(4.63350930777968,1.64950887009522,5.95515245527998));
#23194=CARTESIAN_POINT('Ctrl Pts',(4.64455198390078,1.6181547890226,5.95326866549175));
#23195=CARTESIAN_POINT('Ctrl Pts',(4.67240361893244,1.53643940268731,5.94838669246539));
#23196=CARTESIAN_POINT('Ctrl Pts',(4.68871652131276,1.48591355539177,5.94539436083786));
#23197=CARTESIAN_POINT('Ctrl Pts',(4.75811188040225,1.25844321002308,5.93201661840089));
#23198=CARTESIAN_POINT('Ctrl Pts',(4.80201823956137,1.07885572934138,5.92170206957395));
#23199=CARTESIAN_POINT('Ctrl Pts',(4.85034696894252,0.818381051162789,5.90684014254788));
#23200=CARTESIAN_POINT('Ctrl Pts',(4.86304506213647,0.739192687172608,5.90233555704712));
#23201=CARTESIAN_POINT('Ctrl Pts',(4.88361905482338,0.587200844381081,5.89369669429945));
#23202=CARTESIAN_POINT('Ctrl Pts',(4.89181645729435,0.514462329409633,5.88956551909227));
#23203=CARTESIAN_POINT('Ctrl Pts',(4.90399320985336,0.379383758089831,5.88188943061856));
#23204=CARTESIAN_POINT('Ctrl Pts',(4.90841420571629,0.317098276177648,5.87834828382102));
#23205=CARTESIAN_POINT('Ctrl Pts',(4.92332524789386,0.0296048401421414,
5.86198551973232));
#23206=CARTESIAN_POINT('Ctrl Pts',(4.91950826643874,-0.196070324342683,
5.8490768039767));
#23207=CARTESIAN_POINT('Ctrl Pts',(4.89460045066212,-0.486203970079088,
5.83241752508645));
#23208=CARTESIAN_POINT('Ctrl Pts',(4.8876617575062,-0.551607208692117,5.82865910047377));
#23209=CARTESIAN_POINT('Ctrl Pts',(4.87319008772243,-0.666080810443444,
5.82208120485445));
#23210=CARTESIAN_POINT('Ctrl Pts',(4.8662218998351,-0.715213099881239,5.8192581089666));
#23211=CARTESIAN_POINT('Ctrl Pts',(4.85271582207133,-0.801076347845169,
5.81432797416755));
#23212=CARTESIAN_POINT('Ctrl Pts',(4.84650137656249,-0.837853565599088,
5.81221781562353));
#23213=CARTESIAN_POINT('Ctrl Pts',(4.82626970415786,-0.949817277586713,
5.80579408290496));
#23214=CARTESIAN_POINT('Ctrl Pts',(4.81091654357623,-1.02475087476453,5.80149472781692));
#23215=CARTESIAN_POINT('Ctrl Pts',(4.7506690329984,-1.28747874373157,5.78636774469862));
#23216=CARTESIAN_POINT('Ctrl Pts',(4.69647287657621,-1.47295629382967,5.7755862874365));
#23217=CARTESIAN_POINT('Ctrl Pts',(4.61802032372933,-1.69253655714347,5.76247879942884));
#23218=CARTESIAN_POINT('Ctrl Pts',(4.60406438065428,-1.73013955019648,5.76022192687771));
#23219=CARTESIAN_POINT('Ctrl Pts',(4.56382132221355,-1.83463431979489,5.75391289574751));
#23220=CARTESIAN_POINT('Ctrl Pts',(4.53652580362779,-1.90112640945508,5.74985498900001));
#23221=CARTESIAN_POINT('Ctrl Pts',(4.48250597255629,-2.02492416873906,5.74220820755223));
#23222=CARTESIAN_POINT('Ctrl Pts',(4.4561145790334,-2.0823593425554,5.73862250780528));
#23223=CARTESIAN_POINT('Ctrl Pts',(4.34369670265896,-2.31508199843801,5.72392774161848));
#23224=CARTESIAN_POINT('Ctrl Pts',(4.2483765231206,-2.48567911650042,5.71275747209068));
#23225=CARTESIAN_POINT('Ctrl Pts',(4.10032533005141,-2.71713776285327,5.69703075605458));
#23226=CARTESIAN_POINT('Ctrl Pts',(4.05586199582944,-2.78307186925759,5.69248214360016));
#23227=CARTESIAN_POINT('Ctrl Pts',(3.99423885287356,-2.86983676563528,5.68640996191761));
#23228=CARTESIAN_POINT('Ctrl Pts',(3.97847832544998,-2.89164612277454,5.68487614336304));
#23229=CARTESIAN_POINT('Ctrl Pts',(3.93725040500319,-2.94772200147618,5.68091357106846));
#23230=CARTESIAN_POINT('Ctrl Pts',(3.91151424203479,-2.98178841304458,5.67848782793685));
#23231=CARTESIAN_POINT('Ctrl Pts',(3.86357452505938,-3.04355628505292,5.67405768486157));
#23232=CARTESIAN_POINT('Ctrl Pts',(3.8415083913864,-3.07136065605109,5.6720514163767));
#23233=CARTESIAN_POINT('Ctrl Pts',(3.70744762645759,-3.2365784101876,5.66004738376139));
#23234=CARTESIAN_POINT('Ctrl Pts',(3.58839016664414,-3.36809520616232,5.65014111709629));
#23235=CARTESIAN_POINT('Ctrl Pts',(3.38561070118491,-3.56910942128526,5.63414062683164));
#23236=CARTESIAN_POINT('Ctrl Pts',(3.30623536207469,-3.64276121982292,5.62806939701597));
#23237=CARTESIAN_POINT('Ctrl Pts',(3.16657322201732,-3.76402460780622,5.61765921094442));
#23238=CARTESIAN_POINT('Ctrl Pts',(3.10748324938472,-3.81295356501981,5.6133326164611));
#23239=CARTESIAN_POINT('Ctrl Pts',(2.99374741149748,-3.90273105610842,5.60513657746522));
#23240=CARTESIAN_POINT('Ctrl Pts',(2.93934869717951,-3.94386388677907,5.60127062206718));
#23241=CARTESIAN_POINT('Ctrl Pts',(2.69841940681127,-4.11828483397017,5.58436774804399));
#23242=CARTESIAN_POINT('Ctrl Pts',(2.50355613317588,-4.23956849098936,5.57124124977485));
#23243=CARTESIAN_POINT('Ctrl Pts',(2.26012341648045,-4.36842752941848,5.55548437682585));
#23244=CARTESIAN_POINT('Ctrl Pts',(2.21899404375236,-4.38946265511874,5.55284364332822));
#23245=CARTESIAN_POINT('Ctrl Pts',(2.12391509053258,-4.43641173976063,5.54679044063224));
#23246=CARTESIAN_POINT('Ctrl Pts',(2.06977624111165,-4.46192681147799,5.5433809760215));
#23247=CARTESIAN_POINT('Ctrl Pts',(1.98166225238367,-4.50150511145434,5.53789645488314));
#23248=CARTESIAN_POINT('Ctrl Pts',(1.94797193671454,-4.51618632522818,5.53581476779011));
#23249=CARTESIAN_POINT('Ctrl Pts',(1.85807588661132,-4.55416717389434,5.53029929125383));
#23250=CARTESIAN_POINT('Ctrl Pts',(1.80159692573019,-4.57680382999001,5.52687331592428));
#23251=CARTESIAN_POINT('Ctrl Pts',(1.58448687803319,-4.65917935072152,5.5138229035384));
#23252=CARTESIAN_POINT('Ctrl Pts',(1.42119322624803,-4.71155613805953,5.50424980576285));
#23253=CARTESIAN_POINT('Ctrl Pts',(1.17769164561383,-4.77584562496961,5.49012177751472));
#23254=CARTESIAN_POINT('Ctrl Pts',(1.09939237966458,-4.79447549596105,5.48560135584779));
#23255=CARTESIAN_POINT('Ctrl Pts',(0.948940420264369,-4.826393281715,5.47693898370612));
#23256=CARTESIAN_POINT('Ctrl Pts',(0.876878241277379,-4.84000458844437,
5.47280018791893));
#23257=CARTESIAN_POINT('Ctrl Pts',(0.734753277355558,-4.86357118520218,
5.46464667886968));
#23258=CARTESIAN_POINT('Ctrl Pts',(0.664726309320707,-4.87363579183947,
5.4606337039462));
#23259=CARTESIAN_POINT('Ctrl Pts',(0.407986319430107,-4.90489919755143,
5.44592554294287));
#23260=CARTESIAN_POINT('Ctrl Pts',(0.220319240221392,-4.91690417492387,
5.43517694418905));
#23261=CARTESIAN_POINT('Ctrl Pts',(-0.0495503678360604,-4.91868364291584,
5.4197290236926));
#23262=CARTESIAN_POINT('Ctrl Pts',(-0.131531119113077,-4.91717436244273,
5.41503858489698));
#23263=CARTESIAN_POINT('Ctrl Pts',(-0.270156107836289,-4.9111528147168,
5.40712050533713));
#23264=CARTESIAN_POINT('Ctrl Pts',(-0.32682969755795,-4.90770707659288,
5.40388719174384));
#23265=CARTESIAN_POINT('Ctrl Pts',(-0.420143768930545,-4.90041001544262,
5.3985741293536));
#23266=CARTESIAN_POINT('Ctrl Pts',(-0.456822753742693,-4.89712692427873,
5.3964888308824));
#23267=CARTESIAN_POINT('Ctrl Pts',(-0.557681358024918,-4.88695617358912,
5.39076123885311));
#23268=CARTESIAN_POINT('Ctrl Pts',(-0.621767717142504,-4.87921655581746,
5.38712821212504));
#23269=CARTESIAN_POINT('Ctrl Pts',(-0.852372888648902,-4.84674938224515,
5.3740453911183));
#23270=CARTESIAN_POINT('Ctrl Pts',(-1.01774780099616,-4.81473872079946,
5.36464096454729));
#23271=CARTESIAN_POINT('Ctrl Pts',(-1.25828433468656,-4.75523043837684,
5.35073905539647));
#23272=CARTESIAN_POINT('Ctrl Pts',(-1.33493872436339,-4.73428288495452,
5.34627529266875));
#23273=CARTESIAN_POINT('Ctrl Pts',(-1.48082615357229,-4.69059081057421,
5.33769700630783));
#23274=CARTESIAN_POINT('Ctrl Pts',(-1.5501274412763,-4.66814663470203,5.33358544960583));
#23275=CARTESIAN_POINT('Ctrl Pts',(-1.67803223408347,-4.62356051569849,
5.32591861432572));
#23276=CARTESIAN_POINT('Ctrl Pts',(-1.73676087486603,-4.60182198450657,
5.32236694929157));
#23277=CARTESIAN_POINT('Ctrl Pts',(-1.98973951303468,-4.50264869695589,
5.30692128446282));
#23278=CARTESIAN_POINT('Ctrl Pts',(-2.1793533330118,-4.41399199375302,5.29495455365991));
#23279=CARTESIAN_POINT('Ctrl Pts',(-2.45571894078246,-4.26261249228675,
5.27692106358769));
#23280=CARTESIAN_POINT('Ctrl Pts',(-2.54702315555395,-4.20869269993568,
5.27086110702291));
#23281=CARTESIAN_POINT('Ctrl Pts',(-2.66962319805726,-4.13083929628305,
5.26260058795375));
#23282=CARTESIAN_POINT('Ctrl Pts',(-2.70247982285064,-4.10941895908117,
5.26037432882795));
#23283=CARTESIAN_POINT('Ctrl Pts',(-2.77294206864005,-4.06227165751999,
5.25557470930506));
#23284=CARTESIAN_POINT('Ctrl Pts',(-2.81045351558883,-4.03641051414627,
5.25300320723842));
#23285=CARTESIAN_POINT('Ctrl Pts',(-3.01141774141955,-3.89370195954318,
5.23911927566544));
#23286=CARTESIAN_POINT('Ctrl Pts',(-3.1679540036146,-3.76744219490056,5.22790741264078));
#23287=CARTESIAN_POINT('Ctrl Pts',(-3.37559018148979,-3.57785045328687,
5.21213385307693));
#23288=CARTESIAN_POINT('Ctrl Pts',(-3.43351761384499,-3.52229748541702,
5.20762591614298));
#23289=CARTESIAN_POINT('Ctrl Pts',(-3.54164927052531,-3.41339487964103,
5.19898207847478));
#23290=CARTESIAN_POINT('Ctrl Pts',(-3.59207193289128,-3.36029213380412,
5.1948492909109));
#23291=CARTESIAN_POINT('Ctrl Pts',(-3.68889407500936,-3.25365313396146,
5.18669727590681));
#23292=CARTESIAN_POINT('Ctrl Pts',(-3.73535990842118,-3.20020068316858,
5.18267973170018));
#23293=CARTESIAN_POINT('Ctrl Pts',(-3.90128992947281,-3.00078198566881,
5.16792644371664));
#23294=CARTESIAN_POINT('Ctrl Pts',(-4.01348390176428,-2.84898242511502,
5.15713686155798));
#23295=CARTESIAN_POINT('Ctrl Pts',(-4.17698230674647,-2.5988741862028,5.14003303230848));
#23296=CARTESIAN_POINT('Ctrl Pts',(-4.23416626724637,-2.50462864429724,
5.133729251485));
#23297=CARTESIAN_POINT('Ctrl Pts',(-4.30892413618677,-2.37153067945724,
5.12503858646369));
#23298=CARTESIAN_POINT('Ctrl Pts',(-4.32923216383696,-2.33425232183811,
5.12262684278592));
#23299=CARTESIAN_POINT('Ctrl Pts',(-4.36835795724081,-2.2601638083154,5.11787984671498));
#23300=CARTESIAN_POINT('Ctrl Pts',(-4.38719929067779,-2.22336999060224,
5.11554451737087));
#23301=CARTESIAN_POINT('Ctrl Pts',(-4.46893765753467,-2.05866366845608,
5.10517712080673));
#23302=CARTESIAN_POINT('Ctrl Pts',(-4.52672095034548,-1.92828893970501,
5.09719900934306));
#23303=CARTESIAN_POINT('Ctrl Pts',(-4.63577440227729,-1.65020191606282,
5.08046496221209));
#23304=CARTESIAN_POINT('Ctrl Pts',(-4.68583090679651,-1.50218460391411,
5.07171637600747));
#23305=CARTESIAN_POINT('Ctrl Pts',(-4.7484018406608,-1.28334248875194,5.05889066980605));
#23306=CARTESIAN_POINT('Ctrl Pts',(-4.7665438287729,-1.21422722656571,5.05485599977968));
#23307=CARTESIAN_POINT('Ctrl Pts',(-4.79795523529087,-1.08297823763899,
5.04721496956757));
#23308=CARTESIAN_POINT('Ctrl Pts',(-4.81153912878306,-1.02093457364158,
5.04361158263338));
#23309=CARTESIAN_POINT('Ctrl Pts',(-4.85218229897371,-0.816417616264684,
5.0317546831821));
#23310=CARTESIAN_POINT('Ctrl Pts',(-4.87414263729166,-0.673010697956814,
5.02347185655213));
#23311=CARTESIAN_POINT('Ctrl Pts',(-4.90155054759469,-0.419595530929521,
5.00888389166927));
#23312=CARTESIAN_POINT('Ctrl Pts',(-4.90970167726523,-0.309980230833086,
5.00259032852891));
#23313=CARTESIAN_POINT('Ctrl Pts',(-4.91689127836406,-0.133487742381665,
4.99250027109077));
#23314=CARTESIAN_POINT('Ctrl Pts',(-4.91825013655806,-0.0667425821893914,
4.9886945698553));
#23315=CARTESIAN_POINT('Ctrl Pts',(-4.91824992449483,0.0369214290317507,
4.98280585634637));
#23316=CARTESIAN_POINT('Ctrl Pts',(-4.91783432300853,0.0738317761361386,
4.98071375598035));
#23317=CARTESIAN_POINT('Ctrl Pts',(-4.91575794422724,0.166030384660693,
4.9754991923389));
#23318=CARTESIAN_POINT('Ctrl Pts',(-4.91357994119894,0.221301879863546,
4.97238242118607));
#23319=CARTESIAN_POINT('Ctrl Pts',(-4.90183918475955,0.429791417210259,
4.96063870870852));
#23320=CARTESIAN_POINT('Ctrl Pts',(-4.88603729618649,0.58257034637313,4.9520572789805));
#23321=CARTESIAN_POINT('Ctrl Pts',(-4.84452369037121,0.857483701056971,
4.93647307377018));
#23322=CARTESIAN_POINT('Ctrl Pts',(-4.82126240423902,0.979855279510011,
4.92948446112467));
#23323=CARTESIAN_POINT('Ctrl Pts',(-4.78410853719335,1.14157970064753,4.92012878523927));
#23324=CARTESIAN_POINT('Ctrl Pts',(-4.77432503429674,1.18182866914119,4.91779052029596));
#23325=CARTESIAN_POINT('Ctrl Pts',(-4.76403458685474,1.2219482467567,4.91544887818065));
#23326=CARTESIAN_POINT('',(-4.91824999923043,8.70047197037183E-5,4.63985943599073));
#23327=CARTESIAN_POINT('Ctrl Pts',(-4.76403458704967,1.22194824599672,4.56992379268636));
#23328=CARTESIAN_POINT('Ctrl Pts',(-4.7899691695387,1.12083655948854,4.5758358124286));
#23329=CARTESIAN_POINT('Ctrl Pts',(-4.81268096566489,1.01890921653989,4.58174783217083));
#23330=CARTESIAN_POINT('Ctrl Pts',(-4.83212549536711,0.916376701757057,
4.58765985191307));
#23331=CARTESIAN_POINT('Ctrl Pts',(-4.86073941546255,0.765493279524208,
4.59635978259268));
#23332=CARTESIAN_POINT('Ctrl Pts',(-4.88228416449266,0.613254030957627,
4.60505971327229));
#23333=CARTESIAN_POINT('Ctrl Pts',(-4.89666114209985,0.460318066068917,
4.6137596439519));
#23334=CARTESIAN_POINT('Ctrl Pts',(-4.91103811970703,0.307382101180202,
4.62245957463151));
#23335=CARTESIAN_POINT('Ctrl Pts',(-4.91824728090875,0.153749768058952,
4.63115950531112));
#23336=CARTESIAN_POINT('Ctrl Pts',(-4.91824999923044,8.70047197037183E-5,
4.63985943599073));
#23337=CARTESIAN_POINT('Ctrl Pts',(-4.91824999940249,7.66643645414756E-5,
4.6396755826554));
#23338=CARTESIAN_POINT('Ctrl Pts',(-4.91825071781255,-0.0460115057582501,
4.64226769254208));
#23339=CARTESIAN_POINT('Ctrl Pts',(-4.91760360853023,-0.0920972119024113,
4.64486297114107));
#23340=CARTESIAN_POINT('Ctrl Pts',(-4.91513167264574,-0.180054659700487,
4.64982563246288));
#23341=CARTESIAN_POINT('Ctrl Pts',(-4.91341918181897,-0.221925555652266,
4.6521921095278));
#23342=CARTESIAN_POINT('Ctrl Pts',(-4.90752604377101,-0.331651055084946,
4.65840690394181));
#23343=CARTESIAN_POINT('Ctrl Pts',(-4.90247328448707,-0.399449432917536,
4.66226038693857));
#23344=CARTESIAN_POINT('Ctrl Pts',(-4.88504433863517,-0.582126852888477,
4.67268765266898));
#23345=CARTESIAN_POINT('Ctrl Pts',(-4.87002313522901,-0.696709393471204,
4.67927629797717));
#23346=CARTESIAN_POINT('Ctrl Pts',(-4.82207872142587,-0.983609958476236,
4.69590673758689));
#23347=CARTESIAN_POINT('Ctrl Pts',(-4.7839469969302,-1.1548952765937,4.70596106603709));
#23348=CARTESIAN_POINT('Ctrl Pts',(-4.7246500966436,-1.3670717952216,4.71852538957432));
#23349=CARTESIAN_POINT('Ctrl Pts',(-4.71195765278293,-1.4101981998542,4.72108466930329));
#23350=CARTESIAN_POINT('Ctrl Pts',(-4.68834946590333,-1.4865341664381,4.7256221620174));
#23351=CARTESIAN_POINT('Ctrl Pts',(-4.67766761054332,-1.5198125891021,4.7276025475386));
#23352=CARTESIAN_POINT('Ctrl Pts',(-4.64903737890213,-1.60584537822008,
4.73272887479813));
#23353=CARTESIAN_POINT('Ctrl Pts',(-4.63054556330881,-1.65841364638349,
4.73586845427189));
#23354=CARTESIAN_POINT('Ctrl Pts',(-4.55355196671715,-1.86595389466506,
4.74831616700343));
#23355=CARTESIAN_POINT('Ctrl Pts',(-4.4881308045679,-2.01824230508286,4.75757113487215));
#23356=CARTESIAN_POINT('Ctrl Pts',(-4.37723969986203,-2.24418348030965,
4.77168352834208));
#23357=CARTESIAN_POINT('Ctrl Pts',(-4.33730848835138,-2.32041844946865,
4.77651383217334));
#23358=CARTESIAN_POINT('Ctrl Pts',(-4.26419444525155,-2.45151645150938,
4.78496384469718));
#23359=CARTESIAN_POINT('Ctrl Pts',(-4.23190066204659,-2.5068513833749,4.78857669519219));
#23360=CARTESIAN_POINT('Ctrl Pts',(-4.18390422587973,-2.58552077411517,
4.79378586781187));
#23361=CARTESIAN_POINT('Ctrl Pts',(-4.16906790196309,-2.6093763744932,4.79537532196427));
#23362=CARTESIAN_POINT('Ctrl Pts',(-4.11403149678931,-2.69620272713746,
4.80119750447677));
#23363=CARTESIAN_POINT('Ctrl Pts',(-4.07260276090377,-2.75838193053204,
4.80543921980069));
#23364=CARTESIAN_POINT('Ctrl Pts',(-3.9387313186842,-2.9497115712902,4.8187307104834));
#23365=CARTESIAN_POINT('Ctrl Pts',(-3.84144067351982,-3.07534311320507,
4.82781280115858));
#23366=CARTESIAN_POINT('Ctrl Pts',(-3.67901062875269,-3.26532886799321,
4.84212180059315));
#23367=CARTESIAN_POINT('Ctrl Pts',(-3.61786181878908,-3.33295181803246,
4.8473392476154));
#23368=CARTESIAN_POINT('Ctrl Pts',(-3.53468664292533,-3.41994536603993,
4.85421019418093));
#23369=CARTESIAN_POINT('Ctrl Pts',(-3.51431664932619,-3.4408740852958,4.85587583997594));
#23370=CARTESIAN_POINT('Ctrl Pts',(-3.46263853165682,-3.4930320349338,4.86005815932614));
#23371=CARTESIAN_POINT('Ctrl Pts',(-3.43109321637514,-3.5240229565949,4.86257193940952));
#23372=CARTESIAN_POINT('Ctrl Pts',(-3.39690004892525,-3.55672077546072,
4.86525391644256));
#23373=CARTESIAN_POINT('Ctrl Pts',(-3.39466404110137,-3.55885496544315,
4.86542910701477));
#23374=CARTESIAN_POINT('Ctrl Pts',(-3.36263357931177,-3.58936924999506,
4.86793591686767));
#23375=CARTESIAN_POINT('Ctrl Pts',(-3.33248593662625,-3.61737663601108,
4.8702609802002));
#23376=CARTESIAN_POINT('Ctrl Pts',(-3.22957562173448,-3.71060259262217,
4.87809127466346));
#23377=CARTESIAN_POINT('Ctrl Pts',(-3.1552214855713,-3.77403074327478,4.88357339091479));
#23378=CARTESIAN_POINT('Ctrl Pts',(-2.97216872199697,-3.92099152762595,
4.8967310516798));
#23379=CARTESIAN_POINT('Ctrl Pts',(-2.86177226081297,-4.00227695857349,
4.90439661345062));
#23380=CARTESIAN_POINT('Ctrl Pts',(-2.68708794782346,-4.11997066981224,
4.91622341307867));
#23381=CARTESIAN_POINT('Ctrl Pts',(-2.62513469412078,-4.15971966118694,
4.92036232552669));
#23382=CARTESIAN_POINT('Ctrl Pts',(-2.50716278720296,-4.23172452798077,
4.9281542972376));
#23383=CARTESIAN_POINT('Ctrl Pts',(-2.45135479397978,-4.26429563712494,
4.93180417842555));
#23384=CARTESIAN_POINT('Ctrl Pts',(-2.3410197219222,-4.32580838709126,4.93895711942695));
#23385=CARTESIAN_POINT('Ctrl Pts',(-2.28655727348435,-4.35484181949582,
4.94245877855016));
#23386=CARTESIAN_POINT('Ctrl Pts',(-2.0378694492351,-4.48146344043974,4.95832699843909));
#23387=CARTESIAN_POINT('Ctrl Pts',(-1.83785299614449,-4.56713481157362,
4.97077268987212));
#23388=CARTESIAN_POINT('Ctrl Pts',(-1.56955648417159,-4.66156359033867,
4.98704581548869));
#23389=CARTESIAN_POINT('Ctrl Pts',(-1.50583270558919,-4.68253677257851,
4.99087984154093));
#23390=CARTESIAN_POINT('Ctrl Pts',(-1.43368427021741,-4.70465756038691,
4.99518223531445));
#23391=CARTESIAN_POINT('Ctrl Pts',(-1.42566267161582,-4.70709457035336,
4.99566005051411));
#23392=CARTESIAN_POINT('Ctrl Pts',(-1.41249136114473,-4.71105933629108,
4.99644372672864));
#23393=CARTESIAN_POINT('Ctrl Pts',(-1.4073453130967,-4.71259918571027,4.99674968823818));
#23394=CARTESIAN_POINT('Ctrl Pts',(-1.39879911059558,-4.71514121485024,
4.9972574364198));
#23395=CARTESIAN_POINT('Ctrl Pts',(-1.395400378983,-4.71614815396453,4.99745926488267));
#23396=CARTESIAN_POINT('Ctrl Pts',(-1.38969267172222,-4.71783246108092,
4.99779804368089));
#23397=CARTESIAN_POINT('Ctrl Pts',(-1.38738428315576,-4.7185118102563,4.99793501203151));
#23398=CARTESIAN_POINT('Ctrl Pts',(-1.38089203534353,-4.72041727575545,
4.99832010230251));
#23399=CARTESIAN_POINT('Ctrl Pts',(-1.37670704092632,-4.72163952394104,
4.99856818800653));
#23400=CARTESIAN_POINT('Ctrl Pts',(-1.3688244946898,-4.72393028936543,4.99903518132851));
#23401=CARTESIAN_POINT('Ctrl Pts',(-1.3651273035362,-4.72500003399201,4.99925410068527));
#23402=CARTESIAN_POINT('Ctrl Pts',(-1.35807678337894,-4.72703106418668,
4.9996713540575));
#23403=CARTESIAN_POINT('Ctrl Pts',(-1.35472368022259,-4.72799312410791,
4.99986969572102));
#23404=CARTESIAN_POINT('Ctrl Pts',(-1.34823293533339,-4.72984795277611,
5.00025344583448));
#23405=CARTESIAN_POINT('Ctrl Pts',(-1.34509542348376,-4.73074116878585,
5.000438858813));
#23406=CARTESIAN_POINT('Ctrl Pts',(-1.33890756389329,-4.73249613259774,
5.0008043650079));
#23407=CARTESIAN_POINT('Ctrl Pts',(-1.33585726716918,-4.73335805443423,
5.00098445999174));
#23408=CARTESIAN_POINT('Ctrl Pts',(-1.32969142877049,-4.73509389949874,
5.00134833791924));
#23409=CARTESIAN_POINT('Ctrl Pts',(-1.32657585346998,-4.73596769814061,
5.00153211942631));
#23410=CARTESIAN_POINT('Ctrl Pts',(-1.28961658288973,-4.74629401504445,
5.00371126213087));
#23411=CARTESIAN_POINT('Ctrl Pts',(-1.25567331122557,-4.75538667006777,
5.00570228083981));
#23412=CARTESIAN_POINT('Ctrl Pts',(-1.16715127983303,-4.77808587448706,
5.0108687434756));
#23413=CARTESIAN_POINT('Ctrl Pts',(-1.11243134855468,-4.79112130282467,
5.01403768488064));
#23414=CARTESIAN_POINT('Ctrl Pts',(-0.895501291952956,-4.8388816873854,
5.02652748216524));
#23415=CARTESIAN_POINT('Ctrl Pts',(-0.73180162460796,-4.86632978590451,
5.03579563421216));
#23416=CARTESIAN_POINT('Ctrl Pts',(-0.482008635444411,-4.89532188683373,
5.04989636080355));
#23417=CARTESIAN_POINT('Ctrl Pts',(-0.396746889515972,-4.902968532215,5.05470134201408));
#23418=CARTESIAN_POINT('Ctrl Pts',(-0.247456298998478,-4.91243775123713,
5.06312259905793));
#23419=CARTESIAN_POINT('Ctrl Pts',(-0.183510403218548,-4.91524191719394,
5.06673213793642));
#23420=CARTESIAN_POINT('Ctrl Pts',(-0.0938489923399746,-4.91742160620816,
5.07180208835004));
#23421=CARTESIAN_POINT('Ctrl Pts',(-0.0681651160506288,-4.91784469011154,
5.07325540017648));
#23422=CARTESIAN_POINT('Ctrl Pts',(-0.0323896412794005,-4.9181536962559,
5.07528141278941));
#23423=CARTESIAN_POINT('Ctrl Pts',(-0.0222998710602266,-4.91820979464608,
5.07585299470894));
#23424=CARTESIAN_POINT('Ctrl Pts',(-0.00261464561696009,-4.91825866519176,
5.07696853707053));
#23425=CARTESIAN_POINT('Ctrl Pts',(0.00698075873364639,-4.91825440605936,
5.07751247593772));
#23426=CARTESIAN_POINT('Ctrl Pts',(0.0986877221735663,-4.91794532244331,
5.08271287886767));
#23427=CARTESIAN_POINT('Ctrl Pts',(0.180778817291399,-4.9156122966194,5.08738183166554));
#23428=CARTESIAN_POINT('Ctrl Pts',(0.4513360896731,-4.90113628722826,5.10282702063363));
#23429=CARTESIAN_POINT('Ctrl Pts',(0.639161405255672,-4.88019598024818,
5.11364713404883));
#23430=CARTESIAN_POINT('Ctrl Pts',(0.885087952496398,-4.83833429676218,
5.12791391497391));
#23431=CARTESIAN_POINT('Ctrl Pts',(0.944668490681234,-4.82705510415669,
5.13137747692948));
#23432=CARTESIAN_POINT('Ctrl Pts',(1.00726319369671,-4.81400195880645,5.13502102479273));
#23433=CARTESIAN_POINT('Ctrl Pts',(1.01050017046645,-4.81332353018949,5.13520945784415));
#23434=CARTESIAN_POINT('Ctrl Pts',(1.01628031092397,-4.81210599949933,5.13554595805206));
#23435=CARTESIAN_POINT('Ctrl Pts',(1.01882373561556,-4.81156814526674,5.13569403552057));
#23436=CARTESIAN_POINT('Ctrl Pts',(1.02338269366746,-4.81060029227805,5.13595947048108));
#23437=CARTESIAN_POINT('Ctrl Pts',(1.02539838513513,-4.81017104285608,5.13607683433701));
#23438=CARTESIAN_POINT('Ctrl Pts',(1.02902418418433,-4.80939653205173,5.13628795530469));
#23439=CARTESIAN_POINT('Ctrl Pts',(1.0306343890886,-4.80905172879,5.13638171639048));
#23440=CARTESIAN_POINT('Ctrl Pts',(1.03354011673042,-4.80842798072262,5.13655092012238));
#23441=CARTESIAN_POINT('Ctrl Pts',(1.03483570033424,-4.80814932089286,5.13662636528204));
#23442=CARTESIAN_POINT('Ctrl Pts',(1.03718039063906,-4.80764402298699,5.13676290598655));
#23443=CARTESIAN_POINT('Ctrl Pts',(1.0382295359943,-4.80741756508404,5.13682400314211));
#23444=CARTESIAN_POINT('Ctrl Pts',(1.04013304765276,-4.80700604013264,5.13693485664496));
#23445=CARTESIAN_POINT('Ctrl Pts',(1.04098743884944,-4.80682108870813,5.13698461403702));
#23446=CARTESIAN_POINT('Ctrl Pts',(1.04405923631298,-4.80615527440475,5.13716350990187));
#23447=CARTESIAN_POINT('Ctrl Pts',(1.04627635974414,-4.80567310474473,5.13729263642487));
#23448=CARTESIAN_POINT('Ctrl Pts',(1.0505489610052,-4.80474082241846,5.13754148504364));
#23449=CARTESIAN_POINT('Ctrl Pts',(1.05260448511337,-4.80429092458072,5.13766120911544));
#23450=CARTESIAN_POINT('Ctrl Pts',(1.05657597640264,-4.80341900292049,5.13789253703513));
#23451=CARTESIAN_POINT('Ctrl Pts',(1.05849198095969,-4.80299715154796,5.13800414250044));
#23452=CARTESIAN_POINT('Ctrl Pts',(1.06220404748173,-4.80217752775453,5.1382203738823));
#23453=CARTESIAN_POINT('Ctrl Pts',(1.06400013964827,-4.80177989389245,5.13832500112196));
#23454=CARTESIAN_POINT('Ctrl Pts',(1.06748995303853,-4.80100523572899,5.13852829820184));
#23455=CARTESIAN_POINT('Ctrl Pts',(1.06918369862117,-4.80062832262004,5.13862696912131));
#23456=CARTESIAN_POINT('Ctrl Pts',(1.07248473522235,-4.79989190168304,5.13881927964687));
#23457=CARTESIAN_POINT('Ctrl Pts',(1.07409204577864,-4.79953248268261,5.13891292012755));
#23458=CARTESIAN_POINT('Ctrl Pts',(1.07723483160756,-4.79882805034599,5.13909602058514));
#23459=CARTESIAN_POINT('Ctrl Pts',(1.07877032239213,-4.79848310726887,5.13918548126315));
#23460=CARTESIAN_POINT('Ctrl Pts',(1.08178313477067,-4.79780476941849,5.13936101762581));
#23461=CARTESIAN_POINT('Ctrl Pts',(1.08326046843861,-4.79747142916449,5.13944709386107));
#23462=CARTESIAN_POINT('Ctrl Pts',(1.08617002588369,-4.79681351461398,5.13961662168773));
#23463=CARTESIAN_POINT('Ctrl Pts',(1.08760225871064,-4.79648898111538,5.13970007369524));
#23464=CARTESIAN_POINT('Ctrl Pts',(1.09043443677156,-4.79584589649442,5.13986509976984));
#23465=CARTESIAN_POINT('Ctrl Pts',(1.0918343882915,-4.79552737374796,5.13994667412805));
#23466=CARTESIAN_POINT('Ctrl Pts',(1.09461501092848,-4.79489343427869,5.1401087025234));
#23467=CARTESIAN_POINT('Ctrl Pts',(1.09599568567718,-4.79457803411498,5.14018915672955));
#23468=CARTESIAN_POINT('Ctrl Pts',(1.13367760426103,-4.78595288154341,5.14238498530579));
#23469=CARTESIAN_POINT('Ctrl Pts',(1.16988357743715,-4.77723166266297,5.14449556909737));
#23470=CARTESIAN_POINT('Ctrl Pts',(1.25974105184251,-4.7545041629124,5.14973599144898));
#23471=CARTESIAN_POINT('Ctrl Pts',(1.31326132928385,-4.74000022571797,5.1528601936069));
#23472=CARTESIAN_POINT('Ctrl Pts',(1.54146534651177,-4.67399528431897,5.16621915149373));
#23473=CARTESIAN_POINT('Ctrl Pts',(1.71346086340778,-4.61371867093199,5.17638821372312));
#23474=CARTESIAN_POINT('Ctrl Pts',(1.95580633422812,-4.51336184161958,5.19110366824187));
#23475=CARTESIAN_POINT('Ctrl Pts',(2.02913328782687,-4.48087396279234,5.19560854448105));
#23476=CARTESIAN_POINT('Ctrl Pts',(2.16806216442214,-4.41521099962841,5.20426403964951));
#23477=CARTESIAN_POINT('Ctrl Pts',(2.23377922410107,-4.38232950968985,5.20841161548671));
#23478=CARTESIAN_POINT('Ctrl Pts',(2.35468420283209,-4.31840835530656,5.21615269141199));
#23479=CARTESIAN_POINT('Ctrl Pts',(2.41005740370888,-4.28775134751623,5.21974253088625));
#23480=CARTESIAN_POINT('Ctrl Pts',(2.57395707292246,-4.19283113526673,5.23050946215255));
#23481=CARTESIAN_POINT('Ctrl Pts',(2.68061839692196,-4.12545419101313,5.23770702656021));
#23482=CARTESIAN_POINT('Ctrl Pts',(2.91265791253478,-3.96607530909511,5.25381004483454));
#23483=CARTESIAN_POINT('Ctrl Pts',(3.03650381417749,-3.87207623235681,5.26271618314803));
#23484=CARTESIAN_POINT('Ctrl Pts',(3.17561059536704,-3.75570962719337,5.27306148475141));
#23485=CARTESIAN_POINT('Ctrl Pts',(3.19539708421455,-3.73888953312831,5.27454140320438));
#23486=CARTESIAN_POINT('Ctrl Pts',(3.24670150437148,-3.69457193901863,5.27840014716026));
#23487=CARTESIAN_POINT('Ctrl Pts',(3.2780037186468,-3.66682753208075,5.28077594915888));
#23488=CARTESIAN_POINT('Ctrl Pts',(3.34068355524541,-3.6098277546292,5.28557491134537));
#23489=CARTESIAN_POINT('Ctrl Pts',(3.37203999243243,-3.58055434001805,5.2879976011686));
#23490=CARTESIAN_POINT('Ctrl Pts',(3.48130004655076,-3.47584406399227,5.29652756602882));
#23491=CARTESIAN_POINT('Ctrl Pts',(3.55708834601077,-3.39824438951752,5.30260671780489));
#23492=CARTESIAN_POINT('Ctrl Pts',(3.73884696280387,-3.19939297347475,5.31770203876384));
#23493=CARTESIAN_POINT('Ctrl Pts',(3.84154508238719,-3.07532483653806,5.32670753791862));
#23494=CARTESIAN_POINT('Ctrl Pts',(3.98561326815726,-2.88277528455182,5.34023716497286));
#23495=CARTESIAN_POINT('Ctrl Pts',(4.03170075523626,-2.81795941812591,5.34472059484519));
#23496=CARTESIAN_POINT('Ctrl Pts',(4.1148306763227,-2.69483185219806,5.35312150052658));
#23497=CARTESIAN_POINT('Ctrl Pts',(4.15225562799454,-2.6368017106891,5.35703475806465));
#23498=CARTESIAN_POINT('Ctrl Pts',(4.25046600992333,-2.47724067152091,5.36768004891839));
#23499=CARTESIAN_POINT('Ctrl Pts',(4.308828819861,-2.37427383837306,5.3744278731477));
#23500=CARTESIAN_POINT('Ctrl Pts',(4.42712611589811,-2.14681161624436,5.38908681390839));
#23501=CARTESIAN_POINT('Ctrl Pts',(4.48564489804156,-2.02169126567489,5.39699818174306));
#23502=CARTESIAN_POINT('Ctrl Pts',(4.55968528609232,-1.84428507603931,5.40798574030637));
#23503=CARTESIAN_POINT('Ctrl Pts',(4.57972144943016,-1.79395341777754,5.41107777825666));
#23504=CARTESIAN_POINT('Ctrl Pts',(4.6144770087273,-1.70226636429126,5.41666142455238));
#23505=CARTESIAN_POINT('Ctrl Pts',(4.62948204368616,-1.66102525762501,5.41915530481924));
#23506=CARTESIAN_POINT('Ctrl Pts',(4.65743884866577,-1.580863209721,5.42396619766399));
#23507=CARTESIAN_POINT('Ctrl Pts',(4.67045962077837,-1.54197019729098,5.42628372901171));
#23508=CARTESIAN_POINT('Ctrl Pts',(4.71568777733272,-1.4010423317161,5.4346302823018));
#23509=CARTESIAN_POINT('Ctrl Pts',(4.74505030614714,-1.29812514640594,5.44063049662655));
#23510=CARTESIAN_POINT('Ctrl Pts',(4.7963620268681,-1.09314861159687,5.45247161324059));
#23511=CARTESIAN_POINT('Ctrl Pts',(4.81846585141105,-0.99118583831548,5.45830969925278));
#23512=CARTESIAN_POINT('Ctrl Pts',(4.85198060683616,-0.808739615205265,
5.46871529811053));
#23513=CARTESIAN_POINT('Ctrl Pts',(4.86467038157827,-0.728531048966778,
5.47327596689699));
#23514=CARTESIAN_POINT('Ctrl Pts',(4.88511342376834,-0.574734224607493,
5.48201409882638));
#23515=CARTESIAN_POINT('Ctrl Pts',(4.89320325069664,-0.50121289902779,5.48618833122787));
#23516=CARTESIAN_POINT('Ctrl Pts',(4.9058501854067,-0.356277557477541,5.49442239896876));
#23517=CARTESIAN_POINT('Ctrl Pts',(4.9105128869947,-0.284890797760436,5.49848050589524));
#23518=CARTESIAN_POINT('Ctrl Pts',(4.9229129325575,0.000587095606161998,
5.51473161378684));
#23519=CARTESIAN_POINT('Ctrl Pts',(4.91821652440404,0.214979093078194,5.5269979173557));
#23520=CARTESIAN_POINT('Ctrl Pts',(4.89370727608886,0.495303515500945,5.54309748253594));
#23521=CARTESIAN_POINT('Ctrl Pts',(4.88648504658181,0.562103608129633,5.54693742137544));
#23522=CARTESIAN_POINT('Ctrl Pts',(4.87145426625354,0.678716462703673,5.5536409194428));
#23523=CARTESIAN_POINT('Ctrl Pts',(4.86424405457737,0.728596297980341,5.55650827510348));
#23524=CARTESIAN_POINT('Ctrl Pts',(4.85030985991866,0.815533526851358,5.56150253721946));
#23525=CARTESIAN_POINT('Ctrl Pts',(4.84392455036782,0.852640397463089,5.56363271592947));
#23526=CARTESIAN_POINT('Ctrl Pts',(4.82614043672559,0.949332100474078,5.56918331031746));
#23527=CARTESIAN_POINT('Ctrl Pts',(4.81406420978863,1.00878583318358,5.57259652492391));
#23528=CARTESIAN_POINT('Ctrl Pts',(4.76411064517863,1.23333762715918,5.5855173980748));
#23529=CARTESIAN_POINT('Ctrl Pts',(4.7188136608917,1.39666386279084,5.59497979383111));
#23530=CARTESIAN_POINT('Ctrl Pts',(4.64031036490253,1.63183090218435,5.608891116679));
#23531=CARTESIAN_POINT('Ctrl Pts',(4.61365867496534,1.70572736751597,5.61330459176182));
#23532=CARTESIAN_POINT('Ctrl Pts',(4.55895610372849,1.84672314208421,5.62182493991813));
#23533=CARTESIAN_POINT('Ctrl Pts',(4.53116424692069,1.91390112715617,5.62592907411136));
#23534=CARTESIAN_POINT('Ctrl Pts',(4.47265493035265,2.04690339705705,5.63415495995136));
#23535=CARTESIAN_POINT('Ctrl Pts',(4.44194784495269,2.11271266842417,5.63827567657888));
#23536=CARTESIAN_POINT('Ctrl Pts',(4.33713186559064,2.32495131161454,5.65174215485226));
#23537=CARTESIAN_POINT('Ctrl Pts',(4.25715104676581,2.46835475091049,5.66112474415458));
#23538=CARTESIAN_POINT('Ctrl Pts',(4.10067057170046,2.71861367363788,5.67802108823279));
#23539=CARTESIAN_POINT('Ctrl Pts',(4.02677312587739,2.82691673024172,5.68552307983263));
#23540=CARTESIAN_POINT('Ctrl Pts',(3.92357405645862,2.96589229976798,5.69537615993432));
#23541=CARTESIAN_POINT('Ctrl Pts',(3.89807827817353,2.99932264100133,5.69776430892468));
#23542=CARTESIAN_POINT('Ctrl Pts',(3.84585334320688,3.06600963986201,5.70256244686095));
#23543=CARTESIAN_POINT('Ctrl Pts',(3.81911375722526,3.09925365464379,5.70497207875724));
#23544=CARTESIAN_POINT('Ctrl Pts',(3.71223769261212,3.22864358931082,5.71443192605509));
#23545=CARTESIAN_POINT('Ctrl Pts',(3.62887521221341,3.32206463822661,5.72144275414572));
#23546=CARTESIAN_POINT('Ctrl Pts',(3.4301198367567,3.52838266886259,5.73749204838565));
#23547=CARTESIAN_POINT('Ctrl Pts',(3.31255324410316,3.63898291012171,5.74652306265818));
#23548=CARTESIAN_POINT('Ctrl Pts',(3.13313603445137,3.79185664243156,5.75979728255143));
#23549=CARTESIAN_POINT('Ctrl Pts',(3.07541928292658,3.83881677989051,5.76399605292956));
#23550=CARTESIAN_POINT('Ctrl Pts',(2.9604104713672,3.92813252631501,5.77223683623686));
#23551=CARTESIAN_POINT('Ctrl Pts',(2.90321920843041,3.97058854243853,5.77627689576103));
#23552=CARTESIAN_POINT('Ctrl Pts',(2.69198906046289,4.12039123091393,5.79100296671283));
#23553=CARTESIAN_POINT('Ctrl Pts',(2.53276042401556,4.22013647686359,5.8017422662152));
#23554=CARTESIAN_POINT('Ctrl Pts',(2.29582635435419,4.35030892832668,5.81721703804273));
#23555=CARTESIAN_POINT('Ctrl Pts',(2.22243860698376,4.38825400235455,5.8219432578573));
#23556=CARTESIAN_POINT('Ctrl Pts',(2.12330064633558,4.43638808505068,5.82823226240219));
#23557=CARTESIAN_POINT('Ctrl Pts',(2.09837038633469,4.44823410001496,5.82980583840515));
#23558=CARTESIAN_POINT('Ctrl Pts',(2.03388954079763,4.47821049672092,5.83385475101351));
#23559=CARTESIAN_POINT('Ctrl Pts',(1.99419549028122,4.4960271710339,5.83632701749922));
#23560=CARTESIAN_POINT('Ctrl Pts',(1.92150771139633,4.52750105349003,5.84081527783571));
#23561=CARTESIAN_POINT('Ctrl Pts',(1.88859175906055,4.54133007726786,5.84283330581411));
#23562=CARTESIAN_POINT('Ctrl Pts',(1.69094306188053,4.62184793158595,5.8548745658535));
#23563=CARTESIAN_POINT('Ctrl Pts',(1.52284290624634,4.67992711911205,5.86480554975824));
#23564=CARTESIAN_POINT('Ctrl Pts',(1.24742190864058,4.75867047507026,5.88085779967603));
#23565=CARTESIAN_POINT('Ctrl Pts',(1.14191522597249,4.78508468191166,5.88695590495483));
#23566=CARTESIAN_POINT('Ctrl Pts',(0.960260456342191,4.82421242982289,5.89741471569399));
#23567=CARTESIAN_POINT('Ctrl Pts',(0.884529656508206,4.83867056237916,5.90176291363321));
#23568=CARTESIAN_POINT('Ctrl Pts',(0.740416114672127,4.86268752164608,5.91002737442573));
#23569=CARTESIAN_POINT('Ctrl Pts',(0.672110545568175,4.87259820078722,5.91394022762721));
#23570=CARTESIAN_POINT('Ctrl Pts',(0.384347508419882,4.90818455296475,5.93041967681783));
#23571=CARTESIAN_POINT('Ctrl Pts',(0.163499881675224,4.92049425296194,5.9430678768831));
#23572=CARTESIAN_POINT('Ctrl Pts',(-0.106809308814562,4.91733813536378,
5.95853572053028));
#23573=CARTESIAN_POINT('Ctrl Pts',(-0.15618595415305,4.91601754945549,5.96135998741251));
#23574=CARTESIAN_POINT('Ctrl Pts',(-0.267807488811053,4.91134878875579,
5.96773899379231));
#23575=CARTESIAN_POINT('Ctrl Pts',(-0.330025932074981,4.90756057482039,
5.97129078963232));
#23576=CARTESIAN_POINT('Ctrl Pts',(-0.4291627244893,4.8996306672596,5.97693843781409));
#23577=CARTESIAN_POINT('Ctrl Pts',(-0.466134766404531,4.89625160118804,
5.97904172325503));
#23578=CARTESIAN_POINT('Ctrl Pts',(-0.56298322292073,4.88629318028304,5.98454466314392));
#23579=CARTESIAN_POINT('Ctrl Pts',(-0.622783252270197,4.87903190233572,
5.98793681733293));
#23580=CARTESIAN_POINT('Ctrl Pts',(-0.856468986073093,4.84628994653024,
6.00119949172932));
#23581=CARTESIAN_POINT('Ctrl Pts',(-1.02907137683812,4.81259577104911,6.01101467141172));
#23582=CARTESIAN_POINT('Ctrl Pts',(-1.27697363917176,4.75025295472467,6.02535573714729));
#23583=CARTESIAN_POINT('Ctrl Pts',(-1.35396049165321,4.72888524251669,6.02984370265032));
#23584=CARTESIAN_POINT('Ctrl Pts',(-1.50055251039084,4.68432519472137,6.03847416766882));
#23585=CARTESIAN_POINT('Ctrl Pts',(-1.5702265023191,4.66143206880253,6.04261368065903));
#23586=CARTESIAN_POINT('Ctrl Pts',(-1.70726982245865,4.61298175562244,6.05084141680459));
#23587=CARTESIAN_POINT('Ctrl Pts',(-1.77464148875063,4.5874849697979,6.05492824434737));
#23588=CARTESIAN_POINT('Ctrl Pts',(-2.03190448665103,4.48360831109142,6.07070942973382));
#23589=CARTESIAN_POINT('Ctrl Pts',(-2.21737322889601,4.39484166271974,6.08246941738451));
#23590=CARTESIAN_POINT('Ctrl Pts',(-2.48480885623965,4.24559520460927,6.09999460791644));
#23591=CARTESIAN_POINT('Ctrl Pts',(-2.57134166005497,4.19375203665733,6.10575812723543));
#23592=CARTESIAN_POINT('Ctrl Pts',(-2.68924137135573,4.11809462524778,6.11372526748306));
#23593=CARTESIAN_POINT('Ctrl Pts',(-2.72200831559824,4.09650989141345,6.11595208378754));
#23594=CARTESIAN_POINT('Ctrl Pts',(-2.79342048699943,4.04823301884738,6.12083133500346));
#23595=CARTESIAN_POINT('Ctrl Pts',(-2.83194874426976,4.02137476166968,6.12348148806722));
#23596=CARTESIAN_POINT('Ctrl Pts',(-3.09993907534417,3.82879550972027,6.14206623140382));
#23597=CARTESIAN_POINT('Ctrl Pts',(-3.31510475331593,3.64408834780691,6.15780892499917));
#23598=CARTESIAN_POINT('Ctrl Pts',(-3.5641127845189,3.38992304519,6.17785458421856));
#23599=CARTESIAN_POINT('Ctrl Pts',(-3.61387695694162,3.33682054815876,6.1819629344182));
#23600=CARTESIAN_POINT('Ctrl Pts',(-3.7049673719628,3.23519070744461,6.18968905856347));
#23601=CARTESIAN_POINT('Ctrl Pts',(-3.74656434335059,3.18692605013148,6.19330349523909));
#23602=CARTESIAN_POINT('Ctrl Pts',(-3.91241054430925,2.98675994809304,6.20808313574593));
#23603=CARTESIAN_POINT('Ctrl Pts',(-4.02845213660913,2.82829677702066,6.21931023561548));
#23604=CARTESIAN_POINT('Ctrl Pts',(-4.17763573896722,2.59669500594495,6.23507898491558));
#23605=CARTESIAN_POINT('Ctrl Pts',(-4.21894014309601,2.52903331629471,6.23961309832852));
#23606=CARTESIAN_POINT('Ctrl Pts',(-4.27205226486006,2.43710412728897,6.24567073837196));
#23607=CARTESIAN_POINT('Ctrl Pts',(-4.28532167382844,2.41369535009285,6.24720451947806));
#23608=CARTESIAN_POINT('Ctrl Pts',(-4.31919595224799,2.35277725310244,6.25117276906155));
#23609=CARTESIAN_POINT('Ctrl Pts',(-4.33950466325037,2.3151055723415,6.25360418693083));
#23610=CARTESIAN_POINT('Ctrl Pts',(-4.37872693927959,2.24002019399494,6.25840360754624));
#23611=CARTESIAN_POINT('Ctrl Pts',(-4.39765898921972,2.20262015427534,6.26077162518407));
#23612=CARTESIAN_POINT('Ctrl Pts',(-4.47597181659911,2.0428783860973,6.27080172231748));
#23613=CARTESIAN_POINT('Ctrl Pts',(-4.53074358810137,1.91834281447384,6.2784154865502));
#23614=CARTESIAN_POINT('Ctrl Pts',(-4.62286227527088,1.68285105610479,6.29258130479891));
#23615=CARTESIAN_POINT('Ctrl Pts',(-4.66154638638726,1.57252291758111,6.2991273701076));
#23616=CARTESIAN_POINT('Ctrl Pts',(-4.70844494961317,1.42176335221978,6.30800104716982));
#23617=CARTESIAN_POINT('Ctrl Pts',(-4.72013626914036,1.38245377839685,6.31030826681332));
#23618=CARTESIAN_POINT('Ctrl Pts',(-4.74274893536813,1.3027904344289,6.314973309344));
#23619=CARTESIAN_POINT('Ctrl Pts',(-4.75364979408675,1.2624356505064,6.31733098714234));
#23620=CARTESIAN_POINT('Ctrl Pts',(-4.76403458747083,1.22194824435476,6.31969203503535));
#23621=CARTESIAN_POINT('Origin',(0.,0.,-3.23514056400928));
#23622=CARTESIAN_POINT('',(-4.76403458704967,1.22194824599671,8.41520471722259));
#23623=CARTESIAN_POINT('',(-4.76403458713635,1.22194824565879,8.07015829796832));
#23624=CARTESIAN_POINT('',(-4.76403458704967,1.22194824599672,-3.23514056400928));
#23625=CARTESIAN_POINT('',(-4.91824999926051,-8.5287480579431E-5,6.73514056400926));
#23626=CARTESIAN_POINT('Ctrl Pts',(-4.91824999926051,-8.5287480579431E-5,
6.73514056400926));
#23627=CARTESIAN_POINT('Ctrl Pts',(-4.9182473175325,-0.154731769320271,
6.74389616606202));
#23628=CARTESIAN_POINT('Ctrl Pts',(-4.91094555559967,-0.309347709470215,
6.75265176811478));
#23629=CARTESIAN_POINT('Ctrl Pts',(-4.89638425253901,-0.463254049078936,
6.76140737016754));
#23630=CARTESIAN_POINT('Ctrl Pts',(-4.88182294947835,-0.617160388687658,
6.7701629722203));
#23631=CARTESIAN_POINT('Ctrl Pts',(-4.86000215205804,-0.770356766869605,
6.77891857427307));
#23632=CARTESIAN_POINT('Ctrl Pts',(-4.83102301718729,-0.922171171695713,
6.78767417632583));
#23633=CARTESIAN_POINT('Ctrl Pts',(-4.80402699906593,-1.06359652624984,
6.79583061000592));
#23634=CARTESIAN_POINT('Ctrl Pts',(-4.77081145334733,-1.20386205789481,
6.80398704368602));
#23635=CARTESIAN_POINT('Ctrl Pts',(-4.73150086408182,-1.34241671462069,
6.81214347736611));
#23636=CARTESIAN_POINT('Ctrl Pts',(-4.69219827562945,-1.48094317156785,
6.820298250982));
#23637=CARTESIAN_POINT('Ctrl Pts',(-4.64680320966298,-1.61775912652929,
6.8284530245979));
#23638=CARTESIAN_POINT('Ctrl Pts',(-4.59549040688103,-1.75232730469067,
6.83660779821379));
#23639=CARTESIAN_POINT('Ctrl Pts',(-4.54417578438562,-1.88690025506309,
6.84476286102362));
#23640=CARTESIAN_POINT('Ctrl Pts',(-4.48694312085571,-2.01922495513687,
6.85291792383345));
#23641=CARTESIAN_POINT('Ctrl Pts',(-4.42401601323758,-2.14878230100619,
6.86107298664328));
#23642=CARTESIAN_POINT('Ctrl Pts',(-4.36109259628959,-2.27833204834689,
6.86922757115928));
#23643=CARTESIAN_POINT('Ctrl Pts',(-4.29247555048242,-2.40511446560006,
6.87738215567528));
#23644=CARTESIAN_POINT('Ctrl Pts',(-4.21843529101728,-2.52863337753814,
6.88553674019129));
#23645=CARTESIAN_POINT('Ctrl Pts',(-4.14437682765308,-2.65218265843794,
6.89369332963319));
#23646=CARTESIAN_POINT('Ctrl Pts',(-4.06489265817825,-2.7724665434294,6.90184991907509));
#23647=CARTESIAN_POINT('Ctrl Pts',(-3.98029786645074,-2.88901574187951,
6.91000650851699));
#23648=CARTESIAN_POINT('Ctrl Pts',(-3.92286118202748,-2.9681482675878,6.91554452621498));
#23649=CARTESIAN_POINT('Ctrl Pts',(-3.86306947491248,-3.04555970926984,
6.92108254391297));
#23650=CARTESIAN_POINT('Ctrl Pts',(-3.80103237900352,-3.12111132711841,
6.92662056161096));
#23651=CARTESIAN_POINT('Ctrl Pts',(-3.70966368246236,-3.23238431214869,
6.93477699529105));
#23652=CARTESIAN_POINT('Ctrl Pts',(-3.61338837694744,-3.33966318888148,
6.94293342897114));
#23653=CARTESIAN_POINT('Ctrl Pts',(-3.51257941745858,-3.4425236235277,6.95108986265124));
#23654=CARTESIAN_POINT('Ctrl Pts',(-3.41179097543487,-3.54536312317576,
6.95924463626714));
#23655=CARTESIAN_POINT('Ctrl Pts',(-3.30647095430475,-3.64378573589915,
6.96739940988304));
#23656=CARTESIAN_POINT('Ctrl Pts',(-3.19702984908185,-3.73740327053152,
6.97555418349894));
#23657=CARTESIAN_POINT('Ctrl Pts',(-3.08758486273307,-3.83102412513618,
6.98370924630877));
#23658=CARTESIAN_POINT('Ctrl Pts',(-2.97401875168829,-3.91983934031082,
6.9918643091186));
#23659=CARTESIAN_POINT('Ctrl Pts',(-2.85677621914406,-4.00350005573036,
7.00001937192843));
#23660=CARTESIAN_POINT('Ctrl Pts',(-2.73954056286551,-4.08715586445526,
7.00817395644444));
#23661=CARTESIAN_POINT('Ctrl Pts',(-2.61862918942034,-4.16565758463701,
7.01632854096045));
#23662=CARTESIAN_POINT('Ctrl Pts',(-2.49451694429524,-4.23869888965045,
7.02448312547646));
#23663=CARTESIAN_POINT('Ctrl Pts',(-2.37037418432866,-4.31175815295512,
7.03263971491836));
#23664=CARTESIAN_POINT('Ctrl Pts',(-2.24302926852906,-4.37935414844116,
7.04079630436027));
#23665=CARTESIAN_POINT('Ctrl Pts',(-2.11298340441212,-4.44122552852014,
7.04895289380217));
#23666=CARTESIAN_POINT('Ctrl Pts',(-2.02468714993508,-4.48323387040317,
7.05449091150014));
#23667=CARTESIAN_POINT('Ctrl Pts',(-1.9351463235655,-4.52260416321385,7.0600289291981));
#23668=CARTESIAN_POINT('Ctrl Pts',(-1.84452357534784,-4.55926702908329,
7.06556694689607));
#23669=CARTESIAN_POINT('Ctrl Pts',(-1.71105371734862,-4.61326437078482,
7.07372338057616));
#23670=CARTESIAN_POINT('Ctrl Pts',(-1.5751861762655,-4.66140690006042,7.08187981425625));
#23671=CARTESIAN_POINT('Ctrl Pts',(-1.43745146864538,-4.70350043454758,
7.09003624793634));
#23672=CARTESIAN_POINT('Ctrl Pts',(-1.29974479392128,-4.74558540181376,
7.09819102155223));
#23673=CARTESIAN_POINT('Ctrl Pts',(-1.16017203060442,-4.78162373260446,
7.10634579516812));
#23674=CARTESIAN_POINT('Ctrl Pts',(-1.01927936807949,-4.81147094268556,
7.11450056878401));
#23675=CARTESIAN_POINT('Ctrl Pts',(-0.878381709057261,-4.84131921124268,
7.12265563159384));
#23676=CARTESIAN_POINT('Ctrl Pts',(-0.736164383736719,-4.86497584673957,
7.13081069440368));
#23677=CARTESIAN_POINT('Ctrl Pts',(-0.593184803227397,-4.88234726865266,
7.13896575721351));
#23678=CARTESIAN_POINT('Ctrl Pts',(-0.450213608459839,-4.89971767173314,
7.14712034172952));
#23679=CARTESIAN_POINT('Ctrl Pts',(-0.306480580255943,-4.91080355930208,
7.15527492624552));
#23680=CARTESIAN_POINT('Ctrl Pts',(-0.16254924873632,-4.91556312178323,
7.16342951076152));
#23681=CARTESIAN_POINT('Ctrl Pts',(-0.0185825295579952,-4.9203238544736,
7.17158610020342));
#23682=CARTESIAN_POINT('Ctrl Pts',(0.125582255771689,-4.91875514271468,
7.17974268964532));
#23683=CARTESIAN_POINT('Ctrl Pts',(0.26937994759,-4.91086728657336,7.18789927908722));
#23684=CARTESIAN_POINT('Ctrl Pts',(0.367013176268963,-4.90551172868718,
7.19343729678522));
#23685=CARTESIAN_POINT('Ctrl Pts',(0.464477156232307,-4.89724419261147,
7.19897531448322));
#23686=CARTESIAN_POINT('Ctrl Pts',(0.561595867944282,-4.88608157357283,
7.20451333218122));
#23687=CARTESIAN_POINT('Ctrl Pts',(0.704633029320816,-4.86964118517939,
7.21266976586132));
#23688=CARTESIAN_POINT('Ctrl Pts',(0.846974502216946,-4.84691241621129,
7.22082619954141));
#23689=CARTESIAN_POINT('Ctrl Pts',(0.988061524253188,-4.81797856852752,
7.2289826332215));
#23690=CARTESIAN_POINT('Ctrl Pts',(1.12911983110287,-4.78905060969746,7.23713740683739));
#23691=CARTESIAN_POINT('Ctrl Pts',(1.26892386882529,-4.7539201587667,7.24529218045329));
#23692=CARTESIAN_POINT('Ctrl Pts',(1.40692488970152,-4.71272165709353,7.25344695406918));
#23693=CARTESIAN_POINT('Ctrl Pts',(1.54493080452828,-4.67152169439182,7.261602016879));
#23694=CARTESIAN_POINT('Ctrl Pts',(1.68113325285886,-4.62425334247315,7.26975707968883));
#23695=CARTESIAN_POINT('Ctrl Pts',(1.81499798705176,-4.57110111127484,7.27791214249866));
#23696=CARTESIAN_POINT('Ctrl Pts',(1.948854870088,-4.51795199745092,7.28606672701467));
#23697=CARTESIAN_POINT('Ctrl Pts',(2.0803740026185,-4.45891981912179,7.29422131153067));
#23698=CARTESIAN_POINT('Ctrl Pts',(2.20904053280529,-4.39423747502605,7.30237589604668));
#23699=CARTESIAN_POINT('Ctrl Pts',(2.33773869757232,-4.32953922781392,7.31053248548858));
#23700=CARTESIAN_POINT('Ctrl Pts',(2.46358255932365,-4.25918818912044,7.31868907493048));
#23701=CARTESIAN_POINT('Ctrl Pts',(2.58608076637406,-4.18346379598177,7.32684566437237));
#23702=CARTESIAN_POINT('Ctrl Pts',(2.66925244535202,-4.13204977884158,7.33238368207036));
#23703=CARTESIAN_POINT('Ctrl Pts',(2.75088231011637,-4.07815966173679,7.33792169976835));
#23704=CARTESIAN_POINT('Ctrl Pts',(2.83082387716705,-4.02189249470456,7.34345971746633));
#23705=CARTESIAN_POINT('Ctrl Pts',(2.94856241205253,-3.93902179235354,7.35161615114642));
#23706=CARTESIAN_POINT('Ctrl Pts',(3.06268146398457,-3.8509619613798,7.3597725848265));
#23707=CARTESIAN_POINT('Ctrl Pts',(3.17273022551003,-3.75805348267358,7.36792901850659));
#23708=CARTESIAN_POINT('Ctrl Pts',(3.28275658901019,-3.66516391346193,7.37608379212248));
#23709=CARTESIAN_POINT('Ctrl Pts',(3.38871405921516,-3.56742788093614,7.38423856573838));
#23710=CARTESIAN_POINT('Ctrl Pts',(3.49018508971363,-3.4652259813814,7.39239333935427));
#23711=CARTESIAN_POINT('Ctrl Pts',(3.59165971869407,-3.36302045742576,7.4005484021641));
#23712=CARTESIAN_POINT('Ctrl Pts',(3.68864735118197,-3.25634898434736,7.40870346497392));
#23713=CARTESIAN_POINT('Ctrl Pts',(3.78076712818884,-3.14562918744513,7.41685852778374));
#23714=CARTESIAN_POINT('Ctrl Pts',(3.8728815023777,-3.03491588425068,7.42501311229975));
#23715=CARTESIAN_POINT('Ctrl Pts',(3.96012837896673,-2.92015499010418,7.43316769681575));
#23716=CARTESIAN_POINT('Ctrl Pts',(4.04216708177416,-2.80179734197915,7.44132228133175));
#23717=CARTESIAN_POINT('Ctrl Pts',(4.12422595501689,-2.6834105938659,7.44947887077365));
#23718=CARTESIAN_POINT('Ctrl Pts',(4.2010739048446,-2.56142559973553,7.45763546021554));
#23719=CARTESIAN_POINT('Ctrl Pts',(4.27241315665875,-2.43632281960114,7.46579204965743));
#23720=CARTESIAN_POINT('Ctrl Pts',(4.32084982763793,-2.35138273338132,7.47133006735544));
#23721=CARTESIAN_POINT('Ctrl Pts',(4.36674794282232,-2.2650059855518,7.47686808505345));
#23722=CARTESIAN_POINT('Ctrl Pts',(4.41002626073745,-2.17734963708314,7.48240610275146));
#23723=CARTESIAN_POINT('Ctrl Pts',(4.47376688944432,-2.04824871471139,7.49056253643155));
#23724=CARTESIAN_POINT('Ctrl Pts',(4.5318465054285,-1.91632278832777,7.49871897011165));
#23725=CARTESIAN_POINT('Ctrl Pts',(4.58403214243955,-1.78208652415674,7.50687540379174));
#23726=CARTESIAN_POINT('Ctrl Pts',(4.63620715820228,-1.64787758084979,7.51503017740764));
#23727=CARTESIAN_POINT('Ctrl Pts',(4.68249046693005,-1.51135954951569,7.52318495102354));
#23728=CARTESIAN_POINT('Ctrl Pts',(4.72269750227204,-1.37306640936752,7.53133972463944));
#23729=CARTESIAN_POINT('Ctrl Pts',(4.76290596348202,-1.23476836490948,7.53949478744927));
#23730=CARTESIAN_POINT('Ctrl Pts',(4.7970376231031,-1.09469540593501,7.5476498502591));
#23731=CARTESIAN_POINT('Ctrl Pts',(4.82495784683387,-0.953396475122647,
7.55580491306893));
#23732=CARTESIAN_POINT('Ctrl Pts',(4.8528764330456,-0.812105831481982,7.56395949758493));
#23733=CARTESIAN_POINT('Ctrl Pts',(4.87458424826237,-0.669589688331877,
7.57211408210094));
#23734=CARTESIAN_POINT('Ctrl Pts',(4.88999783325884,-0.526406927408665,
7.58026866661694));
#23735=CARTESIAN_POINT('Ctrl Pts',(4.90541520791444,-0.383188962873989,
7.58842525605885));
#23736=CARTESIAN_POINT('Ctrl Pts',(4.91453522398999,-0.239304385894645,
7.59658184550075));
#23737=CARTESIAN_POINT('Ctrl Pts',(4.91732626782645,-0.0953175652439695,
7.60473843494265));
#23738=CARTESIAN_POINT('Ctrl Pts',(4.91922128170108,0.00244407480408897,
7.61027645264062));
#23739=CARTESIAN_POINT('Ctrl Pts',(4.91819978220986,0.100252745594403,7.6158144703386));
#23740=CARTESIAN_POINT('Ctrl Pts',(4.91426557286648,0.197931659517309,7.62135248803658));
#23741=CARTESIAN_POINT('Ctrl Pts',(4.90847124006675,0.341793890879735,7.62950892171667));
#23742=CARTESIAN_POINT('Ctrl Pts',(4.89635426123467,0.485428394634977,7.63766535539676));
#23743=CARTESIAN_POINT('Ctrl Pts',(4.87795629785876,0.628271771353843,7.64582178907685));
#23744=CARTESIAN_POINT('Ctrl Pts',(4.85956207898706,0.771086075418557,7.65397656269274));
#23745=CARTESIAN_POINT('Ctrl Pts',(4.83488946854167,0.913109241979222,7.66213133630864));
#23746=CARTESIAN_POINT('Ctrl Pts',(4.80403186908258,1.05378406864922,7.67028610992454));
#23747=CARTESIAN_POINT('Ctrl Pts',(4.77317317531592,1.19446388409125,7.67844117273436));
#23748=CARTESIAN_POINT('Ctrl Pts',(4.73612912166717,1.33379493631443,7.6865962355442));
#23749=CARTESIAN_POINT('Ctrl Pts',(4.69304411621821,1.47123077242479,7.69475129835402));
#23750=CARTESIAN_POINT('Ctrl Pts',(4.64996163770159,1.60865854793365,7.70290588287003));
#23751=CARTESIAN_POINT('Ctrl Pts',(4.60083901722313,1.74419101067667,7.71106046738603));
#23752=CARTESIAN_POINT('Ctrl Pts',(4.5458703560629,1.87729746400739,7.71921505190204));
#23753=CARTESIAN_POINT('Ctrl Pts',(4.49088818003972,2.01043664353947,7.72737164134394));
#23754=CARTESIAN_POINT('Ctrl Pts',(4.43005721879998,2.1411483122626,7.73552823078584));
#23755=CARTESIAN_POINT('Ctrl Pts',(4.36361972559094,2.26892175998504,7.74368482022774));
#23756=CARTESIAN_POINT('Ctrl Pts',(4.31851116449161,2.35567512913047,7.74922283792573));
#23757=CARTESIAN_POINT('Ctrl Pts',(4.27081904526634,2.44107443420284,7.75476085562373));
#23758=CARTESIAN_POINT('Ctrl Pts',(4.22063128929397,2.52496625370176,7.76029887332172));
#23759=CARTESIAN_POINT('Ctrl Pts',(4.14671438879556,2.6485227497911,7.76845530700181));
#23760=CARTESIAN_POINT('Ctrl Pts',(4.06735438141007,2.76885429624838,7.77661174068191));
#23761=CARTESIAN_POINT('Ctrl Pts',(3.98285740119603,2.88548609149966,7.784768174362));
#23762=CARTESIAN_POINT('Ctrl Pts',(3.89837761849953,3.00209414889262,7.79292294797789));
#23763=CARTESIAN_POINT('Ctrl Pts',(3.80876314492887,3.11500368645602,7.80107772159379));
#23764=CARTESIAN_POINT('Ctrl Pts',(3.7143625846748,3.22377009913361,7.80923249520969));
#23765=CARTESIAN_POINT('Ctrl Pts',(3.61995867667985,3.33254036901041,7.81738755801952));
#23766=CARTESIAN_POINT('Ctrl Pts',(3.52076855886865,3.43716696483075,7.82554262082935));
#23767=CARTESIAN_POINT('Ctrl Pts',(3.41718048160865,3.53723912375356,7.83369768363918));
#23768=CARTESIAN_POINT('Ctrl Pts',(3.31359847978159,3.63730541345177,7.84185226815519));
#23769=CARTESIAN_POINT('Ctrl Pts',(3.20561927588551,3.73281756883447,7.85000685267119));
#23770=CARTESIAN_POINT('Ctrl Pts',(3.0936672186751,3.82340243795955,7.8581614371872));
#23771=CARTESIAN_POINT('Ctrl Pts',(2.98168763638626,3.91400957872206,7.86631802662911));
#23772=CARTESIAN_POINT('Ctrl Pts',(2.86573350906554,3.99968680173407,7.87447461607101));
#23773=CARTESIAN_POINT('Ctrl Pts',(2.74626190658445,4.08010154321472,7.88263120551291));
#23774=CARTESIAN_POINT('Ctrl Pts',(2.66514517836632,4.13470013061083,7.88816922321089));
#23775=CARTESIAN_POINT('Ctrl Pts',(2.58240760078612,4.18687361812252,7.89370724090886));
#23776=CARTESIAN_POINT('Ctrl Pts',(2.49819978186957,4.23652934751629,7.89924525860684));
#23777=CARTESIAN_POINT('Ctrl Pts',(2.3741778794859,4.30966267531056,7.90740169228692));
#23778=CARTESIAN_POINT('Ctrl Pts',(2.24691919032533,4.37735992693958,7.915558125967));
#23779=CARTESIAN_POINT('Ctrl Pts',(2.1169196995089,4.43935063363226,7.92371455964709));
#23780=CARTESIAN_POINT('Ctrl Pts',(1.98694666725375,4.5013287234685,7.93186933326297));
#23781=CARTESIAN_POINT('Ctrl Pts',(1.85423424804504,4.55760244143561,7.94002410687886));
#23782=CARTESIAN_POINT('Ctrl Pts',(1.71930127391744,4.60794815422286,7.94817888049475));
#23783=CARTESIAN_POINT('Ctrl Pts',(1.58436351464194,4.65829565242753,7.95633394330457));
#23784=CARTESIAN_POINT('Ctrl Pts',(1.44720535506439,4.70271460430195,7.9644890061144));
#23785=CARTESIAN_POINT('Ctrl Pts',(1.30836425012304,4.74103006228604,7.97264406892422));
#23786=CARTESIAN_POINT('Ctrl Pts',(1.16953128820214,4.77934327307138,7.98079865344022));
#23787=CARTESIAN_POINT('Ctrl Pts',(1.02901590122402,4.81155361802777,7.98895323795622));
#23788=CARTESIAN_POINT('Ctrl Pts',(0.887369248564386,4.83753644732546,7.99710782247221));
#23789=CARTESIAN_POINT('Ctrl Pts',(0.745687769968309,4.86352566488822,8.00526441191411));
#23790=CARTESIAN_POINT('Ctrl Pts',(0.60287479915392,4.88328424664097,8.01342100135601));
#23791=CARTESIAN_POINT('Ctrl Pts',(0.459490809848882,4.89673883908101,8.0215775907979));
#23792=CARTESIAN_POINT('Ctrl Pts',(0.362138469628618,4.90587400171036,8.02711560849592));
#23793=CARTESIAN_POINT('Ctrl Pts',(0.264523077887973,4.91210415728261,8.03265362619394));
#23794=CARTESIAN_POINT('Ctrl Pts',(0.16682121793857,4.91541999667836,8.03819164389196));
#23795=CARTESIAN_POINT('Ctrl Pts',(0.0229251914986702,4.9203035896172,8.04634807757206));
#23796=CARTESIAN_POINT('Ctrl Pts',(-0.121212320760765,4.9188650470535,8.05450451125216));
#23797=CARTESIAN_POINT('Ctrl Pts',(-0.265026381185507,4.91110416095767,
8.06266094493225));
#23798=CARTESIAN_POINT('Ctrl Pts',(-0.40881117139462,4.90334485442095,8.07081571854815));
#23799=CARTESIAN_POINT('Ctrl Pts',(-0.552272307158635,4.88926578941549,
8.07897049216404));
#23800=CARTESIAN_POINT('Ctrl Pts',(-0.694847196162797,4.86891881596774,
8.08712526577994));
#23801=CARTESIAN_POINT('Ctrl Pts',(-0.837427141321202,4.84857112095228,
8.09528032858977));
#23802=CARTESIAN_POINT('Ctrl Pts',(-0.979120445041749,4.82195511627215,
8.10343539139961));
#23803=CARTESIAN_POINT('Ctrl Pts',(-1.1193714547929,4.78917431387654,8.11159045420944));
#23804=CARTESIAN_POINT('Ctrl Pts',(-1.25961423883288,4.75639543407252,8.11974503872545));
#23805=CARTESIAN_POINT('Ctrl Pts',(-1.39841457249709,4.71745255700106,8.12789962324147));
#23806=CARTESIAN_POINT('Ctrl Pts',(-1.53522883328251,4.67249991888261,8.13605420775748));
#23807=CARTESIAN_POINT('Ctrl Pts',(-1.6720767318888,4.6275362284895,8.14421079719938));
#23808=CARTESIAN_POINT('Ctrl Pts',(-1.80693726375302,4.57655992879013,8.15236738664128));
#23809=CARTESIAN_POINT('Ctrl Pts',(-1.93928316919885,4.51977475679508,8.16052397608318));
#23810=CARTESIAN_POINT('Ctrl Pts',(-2.02914106530028,4.48121975905606,8.16606199378115));
#23811=CARTESIAN_POINT('Ctrl Pts',(-2.11784009512883,4.43998795518557,8.17160001147911));
#23812=CARTESIAN_POINT('Ctrl Pts',(-2.20522074303678,4.39615565431665,8.17713802917708));
#23813=CARTESIAN_POINT('Ctrl Pts',(-2.33391561157184,4.33159911539219,8.18529446285716));
#23814=CARTESIAN_POINT('Ctrl Pts',(-2.4597978017508,4.26137542963897,8.19345089653725));
#23815=CARTESIAN_POINT('Ctrl Pts',(-2.58237112939528,4.18575470047705,8.20160733021734));
#23816=CARTESIAN_POINT('Ctrl Pts',(-2.70491950991187,4.11014936226549,8.20976210383322));
#23817=CARTESIAN_POINT('Ctrl Pts',(-2.82416008676265,4.02914934758439,8.21791687744911));
#23818=CARTESIAN_POINT('Ctrl Pts',(-2.93962364167508,3.943069351128,8.22607165106499));
#23819=CARTESIAN_POINT('Ctrl Pts',(-3.05509129128864,3.85698630200394,8.23422671387482));
#23820=CARTESIAN_POINT('Ctrl Pts',(-3.16678138042917,3.76582310760995,8.24238177668464));
#23821=CARTESIAN_POINT('Ctrl Pts',(-3.2742555016918,3.66993650791686,8.25053683949447));
#23822=CARTESIAN_POINT('Ctrl Pts',(-3.38172331960527,3.57405553196566,8.25869142401047));
#23823=CARTESIAN_POINT('Ctrl Pts',(-3.48497541525943,3.47345192843738,8.26684600852648));
#23824=CARTESIAN_POINT('Ctrl Pts',(-3.58360821337217,3.3685212238535,8.27500059304248));
#23825=CARTESIAN_POINT('Ctrl Pts',(-3.68226526182543,3.26356472049513,8.28315718248438));
#23826=CARTESIAN_POINT('Ctrl Pts',(-3.77630051385871,3.15427923398948,8.29131377192628));
#23827=CARTESIAN_POINT('Ctrl Pts',(-3.86534844568513,3.04109593007843,8.29947036136818));
#23828=CARTESIAN_POINT('Ctrl Pts',(-3.92580864488223,2.96424872026801,8.3050083790662));
#23829=CARTESIAN_POINT('Ctrl Pts',(-3.98397053870476,2.8856053883823,8.31054639676421));
#23830=CARTESIAN_POINT('Ctrl Pts',(-4.03973056180145,2.80530926112387,8.31608441446223));
#23831=CARTESIAN_POINT('Ctrl Pts',(-4.12289735951155,2.68554654579954,8.32434443969226));
#23832=CARTESIAN_POINT('Ctrl Pts',(-4.20075037613452,2.56206019082026,8.33260446492229));
#23833=CARTESIAN_POINT('Ctrl Pts',(-4.27297159049031,2.43534327136087,8.34086449015232));
#23834=CARTESIAN_POINT('Ctrl Pts',(-4.34427488904071,2.31023689617466,8.34901953227206));
#23835=CARTESIAN_POINT('Ctrl Pts',(-4.41008855441688,2.18198190344048,8.35717457439181));
#23836=CARTESIAN_POINT('Ctrl Pts',(-4.47015167695163,2.05107948347852,8.36532961651156));
#23837=CARTESIAN_POINT('Ctrl Pts',(-4.53137462429007,1.91764932491212,8.37364213329673));
#23838=CARTESIAN_POINT('Ctrl Pts',(-4.5866224854162,1.78146875710113,8.3819546500819));
#23839=CARTESIAN_POINT('Ctrl Pts',(-4.63566945407151,1.64309213834414,8.39026716686708));
#23840=CARTESIAN_POINT('Ctrl Pts',(-4.68471642272683,1.50471551958715,8.39857968365225));
#23841=CARTESIAN_POINT('Ctrl Pts',(-4.72756237674539,1.36414319731729,8.40689220043742));
#23842=CARTESIAN_POINT('Ctrl Pts',(-4.76403458704967,1.22194824599671,8.41520471722259));
#23843=CARTESIAN_POINT('Ctrl Pts',(-4.91824999943065,-7.48357700250612E-5,
6.73532637328698));
#23844=CARTESIAN_POINT('Ctrl Pts',(-4.91825068197842,0.044782597342662,
6.73280315748358));
#23845=CARTESIAN_POINT('Ctrl Pts',(-4.91763767400033,0.0896377529279913,
6.73027690885947));
#23846=CARTESIAN_POINT('Ctrl Pts',(-4.91529202496372,0.175392823737547,
6.72543828609909));
#23847=CARTESIAN_POINT('Ctrl Pts',(-4.91366219255074,0.216291843413273,
6.72312674364904));
#23848=CARTESIAN_POINT('Ctrl Pts',(-4.90800307853509,0.324373432807522,
6.71700549422386));
#23849=CARTESIAN_POINT('Ctrl Pts',(-4.9031050174068,0.391501465204401,6.713190634307));
#23850=CARTESIAN_POINT('Ctrl Pts',(-4.88631051071312,0.570865805284201,
6.70295469375948));
#23851=CARTESIAN_POINT('Ctrl Pts',(-4.87192610393772,0.682827722773605,
6.69651966464271));
#23852=CARTESIAN_POINT('Ctrl Pts',(-4.83016420314059,0.938054762448882,
6.68173546027204));
#23853=CARTESIAN_POINT('Ctrl Pts',(-4.80024346688583,1.08077994976788,6.67338283263945));
#23854=CARTESIAN_POINT('Ctrl Pts',(-4.76403458034885,1.22194827212136,6.66505438904205));
#23855=CARTESIAN_POINT('Ctrl Pts',(-4.76403458747083,1.22194824435476,6.31969203503535));
#23856=CARTESIAN_POINT('Ctrl Pts',(-4.77178283058391,1.1917400106154,6.32145364669194));
#23857=CARTESIAN_POINT('Ctrl Pts',(-4.77924378711755,1.16145794762219,6.32321713004904));
#23858=CARTESIAN_POINT('Ctrl Pts',(-4.80103637042951,1.06923991961347,6.32858121421732));
#23859=CARTESIAN_POINT('Ctrl Pts',(-4.81445539466772,1.00709650795569,6.33218747631128));
#23860=CARTESIAN_POINT('Ctrl Pts',(-4.87091265910445,0.718648100760694,
6.34889799567108));
#23861=CARTESIAN_POINT('Ctrl Pts',(-4.89922231388978,0.489758247256351,
6.36209293286357));
#23862=CARTESIAN_POINT('Ctrl Pts',(-4.91596178877969,0.173225970591947,
6.38022198480445));
#23863=CARTESIAN_POINT('Ctrl Pts',(-4.91825032080293,0.0866118245555618,
6.38516859458936));
#23864=CARTESIAN_POINT('Ctrl Pts',(-4.91824985906285,-0.0380692441522994,
6.39225712131835));
#23865=CARTESIAN_POINT('Ctrl Pts',(-4.91780813497978,-0.076119322468207,
6.39441593126176));
#23866=CARTESIAN_POINT('Ctrl Pts',(-4.91579114373851,-0.162991404124876,
6.39933325600049));
#23867=CARTESIAN_POINT('Ctrl Pts',(-4.91393004110767,-0.211802730676662,
6.40208857352072));
#23868=CARTESIAN_POINT('Ctrl Pts',(-4.90795465352176,-0.324425840632596,
6.40843776971936));
#23869=CARTESIAN_POINT('Ctrl Pts',(-4.90332242625457,-0.388201355869752,
6.41202710696751));
#23870=CARTESIAN_POINT('Ctrl Pts',(-4.87692525221264,-0.674299447633779,
6.42813920866103));
#23871=CARTESIAN_POINT('Ctrl Pts',(-4.84127308265718,-0.895071847565557,
6.44061271800409));
#23872=CARTESIAN_POINT('Ctrl Pts',(-4.77626862988934,-1.17496066822926,
6.45680897234867));
#23873=CARTESIAN_POINT('Ctrl Pts',(-4.7605837988785,-1.23697873026874,6.4604214837415));
#23874=CARTESIAN_POINT('Ctrl Pts',(-4.72457726150975,-1.36850069337734,
6.46814080145536));
#23875=CARTESIAN_POINT('Ctrl Pts',(-4.70392126793976,-1.43789741908723,
6.47224907536894));
#23876=CARTESIAN_POINT('Ctrl Pts',(-4.66937855276934,-1.54522336114714,
6.478662937225));
#23877=CARTESIAN_POINT('Ctrl Pts',(-4.65654380800173,-1.58348067361957,
6.48096127111801));
#23878=CARTESIAN_POINT('Ctrl Pts',(-4.57902831121979,-1.80543951935753,
6.49436778766183));
#23879=CARTESIAN_POINT('Ctrl Pts',(-4.50395269367732,-1.98532649315502,
6.50553107493504));
#23880=CARTESIAN_POINT('Ctrl Pts',(-4.38645067987844,-2.22565220641557,
6.5208227379221));
#23881=CARTESIAN_POINT('Ctrl Pts',(-4.35304405580042,-2.29030236888245,
6.52497480778277));
#23882=CARTESIAN_POINT('Ctrl Pts',(-4.30000015922807,-2.38759916720453,
6.53127510341335));
#23883=CARTESIAN_POINT('Ctrl Pts',(-4.28139788170872,-2.42079808984258,
6.53343407288476));
#23884=CARTESIAN_POINT('Ctrl Pts',(-4.23804790655977,-2.49610051731637,
6.53835102910746));
#23885=CARTESIAN_POINT('Ctrl Pts',(-4.21305465290573,-2.53805800197352,
6.54110582230903));
#23886=CARTESIAN_POINT('Ctrl Pts',(-4.15391546406366,-2.63405672965554,
6.54745341383125));
#23887=CARTESIAN_POINT('Ctrl Pts',(-4.11933253421103,-2.68781846700604,
6.55104167402111));
#23888=CARTESIAN_POINT('Ctrl Pts',(-3.95919476207011,-2.92641110212529,
6.56715590881812));
#23889=CARTESIAN_POINT('Ctrl Pts',(-3.82218185833917,-3.10322895657413,
6.5796325671518));
#23890=CARTESIAN_POINT('Ctrl Pts',(-3.63109643789519,-3.31789283219575,
6.59583186933676));
#23891=CARTESIAN_POINT('Ctrl Pts',(-3.58764089355813,-3.3648338584015,6.59944420412304));
#23892=CARTESIAN_POINT('Ctrl Pts',(-3.49307026046255,-3.46307453662107,
6.60716360002116));
#23893=CARTESIAN_POINT('Ctrl Pts',(-3.4417127417228,-3.51411985128582,6.61127213081374));
#23894=CARTESIAN_POINT('Ctrl Pts',(-3.36000320386708,-3.59182268156121,
6.6176865357552));
#23895=CARTESIAN_POINT('Ctrl Pts',(-3.33041781073134,-3.61927187240741,
6.61998515559381));
#23896=CARTESIAN_POINT('Ctrl Pts',(-3.15611492101516,-3.7770421803878,6.633391518541));
#23897=CARTESIAN_POINT('Ctrl Pts',(-3.00409750124454,-3.89903914432749,
6.64455435374067));
#23898=CARTESIAN_POINT('Ctrl Pts',(-2.78590797394217,-4.05378744601438,
6.65984499410598));
#23899=CARTESIAN_POINT('Ctrl Pts',(-2.72563892459175,-4.09455352036824,
6.66399650542669));
#23900=CARTESIAN_POINT('Ctrl Pts',(-2.63250292993435,-4.15458293517651,
6.67029616093516));
#23901=CARTESIAN_POINT('Ctrl Pts',(-2.60028012236711,-4.17482627031082,
6.67245504574602));
#23902=CARTESIAN_POINT('Ctrl Pts',(-2.52617107903467,-4.22019288809571,
6.67737219548491));
#23903=CARTESIAN_POINT('Ctrl Pts',(-2.48413904789124,-4.24507027067345,
6.68012726489912));
#23904=CARTESIAN_POINT('Ctrl Pts',(-2.38625013356782,-4.30105570045904,
6.68647570174519));
#23905=CARTESIAN_POINT('Ctrl Pts',(-2.33014324305514,-4.33170894759047,
6.69006452930829));
#23906=CARTESIAN_POINT('Ctrl Pts',(-2.07535229382865,-4.46452736069087,
6.70617764021293));
#23907=CARTESIAN_POINT('Ctrl Pts',(-1.87044581954264,-4.55417645095849,
6.71865263951328));
#23908=CARTESIAN_POINT('Ctrl Pts',(-1.59994815344273,-4.65117622857774,
6.73485033595483));
#23909=CARTESIAN_POINT('Ctrl Pts',(-1.53932371869043,-4.67159039092748,
6.73846276378926));
#23910=CARTESIAN_POINT('Ctrl Pts',(-1.40926726626786,-4.71257790642061,
6.74618211845602));
#23911=CARTESIAN_POINT('Ctrl Pts',(-1.33974418774053,-4.73281207088394,
6.75029051386871));
#23912=CARTESIAN_POINT('Ctrl Pts',(-1.23081467734926,-4.7619225869941,6.75670463259733));
#23913=CARTESIAN_POINT('Ctrl Pts',(-1.19170238672114,-4.771860946282,6.75900310174045));
#23914=CARTESIAN_POINT('Ctrl Pts',(-0.963142482804232,-4.82695225004833,
6.77240966312414));
#23915=CARTESIAN_POINT('Ctrl Pts',(-0.771269805782495,-4.86130161291053,
6.78357285535616));
#23916=CARTESIAN_POINT('Ctrl Pts',(-0.505617272158434,-4.89273212417459,
6.79886408140672));
#23917=CARTESIAN_POINT('Ctrl Pts',(-0.433184010815897,-4.89967634230047,
6.80301581710834));
#23918=CARTESIAN_POINT('Ctrl Pts',(-0.322672362076679,-4.90780130331323,
6.80931572976934));
#23919=CARTESIAN_POINT('Ctrl Pts',(-0.284690448949799,-4.91015096458474,
6.81147464858849));
#23920=CARTESIAN_POINT('Ctrl Pts',(-0.19790886319272,-4.9145091536491,6.81639172056273));
#23921=CARTESIAN_POINT('Ctrl Pts',(-0.149098890094445,-4.91623206727721,
6.81914667899317));
#23922=CARTESIAN_POINT('Ctrl Pts',(-0.0363604621139229,-4.91853100351121,
6.8254947761769));
#23923=CARTESIAN_POINT('Ctrl Pts',(0.02756980110591,-4.91858814327327,6.82908337575979));
#23924=CARTESIAN_POINT('Ctrl Pts',(0.314859149471245,-4.91324340934329,
6.84519693820587));
#23925=CARTESIAN_POINT('Ctrl Pts',(0.53769045165593,-4.89387219634178,6.85767260407866));
#23926=CARTESIAN_POINT('Ctrl Pts',(0.821628175002489,-4.84955683112862,
6.87387094568142));
#23927=CARTESIAN_POINT('Ctrl Pts',(0.884627108629116,-4.83846143763935,
6.8774833361316));
#23928=CARTESIAN_POINT('Ctrl Pts',(1.01843579026431,-4.81219424265948,6.88520270735362));
#23929=CARTESIAN_POINT('Ctrl Pts',(1.08916311691707,-4.79668098040192,6.88931115714788));
#23930=CARTESIAN_POINT('Ctrl Pts',(1.19873895105736,-4.77009816529883,6.89572539084788));
#23931=CARTESIAN_POINT('Ctrl Pts',(1.23783755790536,-4.7601018617538,6.89802392052561));
#23932=CARTESIAN_POINT('Ctrl Pts',(1.46488165059817,-4.69906718937616,6.91143043352738));
#23933=CARTESIAN_POINT('Ctrl Pts',(1.64978505091154,-4.63738277533979,6.92259351401493));
#23934=CARTESIAN_POINT('Ctrl Pts',(1.89806798841607,-4.5378204130107,6.93788451726422));
#23935=CARTESIAN_POINT('Ctrl Pts',(1.96498631693775,-4.50924662724441,6.94203614417355));
#23936=CARTESIAN_POINT('Ctrl Pts',(2.06590227474172,-4.46348281677045,6.94833593215241));
#23937=CARTESIAN_POINT('Ctrl Pts',(2.10037469255156,-4.44736520604732,6.9504948344821));
#23938=CARTESIAN_POINT('Ctrl Pts',(2.1786553176585,-4.40965182755431,6.95541194415692));
#23939=CARTESIAN_POINT('Ctrl Pts',(2.22233583897437,-4.38780032945321,6.9581669563948));
#23940=CARTESIAN_POINT('Ctrl Pts',(2.32242274327858,-4.33585310759225,6.96451521825342));
#23941=CARTESIAN_POINT('Ctrl Pts',(2.37858231812219,-4.30530089847534,6.96810392836518));
#23942=CARTESIAN_POINT('Ctrl Pts',(2.62825926812963,-4.16309352426808,6.98421727188625));
#23943=CARTESIAN_POINT('Ctrl Pts',(2.81462700601331,-4.03942672935072,6.99669261458354));
#23944=CARTESIAN_POINT('Ctrl Pts',(3.04270679528162,-3.86460990480026,7.01289064339163));
#23945=CARTESIAN_POINT('Ctrl Pts',(3.09270892510015,-3.82471250572877,7.01650305196705));
#23946=CARTESIAN_POINT('Ctrl Pts',(3.19761919515084,-3.73760034042959,7.02422241516076));
#23947=CARTESIAN_POINT('Ctrl Pts',(3.25229154497666,-3.69012525037815,7.02833083858715));
#23948=CARTESIAN_POINT('Ctrl Pts',(3.33577377972258,-3.61433601491832,7.03474501654138));
#23949=CARTESIAN_POINT('Ctrl Pts',(3.36531697440985,-3.58684445921951,7.03704351686796));
#23950=CARTESIAN_POINT('Ctrl Pts',(3.53544619155861,-3.42457754102047,7.05045005859609));
#23951=CARTESIAN_POINT('Ctrl Pts',(3.66826527567222,-3.28191102770945,7.06161319859044));
#23952=CARTESIAN_POINT('Ctrl Pts',(3.83860093819687,-3.07564938708435,7.07690431196482));
#23953=CARTESIAN_POINT('Ctrl Pts',(3.88367821962874,-3.0185294404834,7.08105598848666));
#23954=CARTESIAN_POINT('Ctrl Pts',(3.9503770514992,-2.93004304153632,7.08735583332418));
#23955=CARTESIAN_POINT('Ctrl Pts',(3.97292882179493,-2.89939092084906,7.08951474317347));
#23956=CARTESIAN_POINT('Ctrl Pts',(4.02360660282389,-2.82880860014699,7.09443183565475));
#23957=CARTESIAN_POINT('Ctrl Pts',(4.05149810912533,-2.78871499820808,7.09718682335397));
#23958=CARTESIAN_POINT('Ctrl Pts',(4.11450790945524,-2.69519834457089,7.10353501011303));
#23959=CARTESIAN_POINT('Ctrl Pts',(4.14919102093863,-2.6414926512652,7.10712366981832));
#23960=CARTESIAN_POINT('Ctrl Pts',(4.30033764449198,-2.3971215668924,7.12323711317747));
#23961=CARTESIAN_POINT('Ctrl Pts',(4.40477389066716,-2.19933209126232,7.13571260325617));
#23962=CARTESIAN_POINT('Ctrl Pts',(4.5213488951806,-1.93666685498963,7.15191077471157));
#23963=CARTESIAN_POINT('Ctrl Pts',(4.54615291529909,-1.87770282484303,7.15552317502115));
#23964=CARTESIAN_POINT('Ctrl Pts',(4.59656596951498,-1.75100146772376,7.16324254187564));
#23965=CARTESIAN_POINT('Ctrl Pts',(4.6218433579639,-1.68314843716951,7.16735097732638));
#23966=CARTESIAN_POINT('Ctrl Pts',(4.65886271020273,-1.57664511050129,7.17376518070197));
#23967=CARTESIAN_POINT('Ctrl Pts',(4.67164226754552,-1.53836603437918,7.17606369441338));
#23968=CARTESIAN_POINT('Ctrl Pts',(4.74334300352038,-1.31446113729494,7.18947022427023));
#23969=CARTESIAN_POINT('Ctrl Pts',(4.79166765767429,-1.12562471879695,7.20063333837024));
#23970=CARTESIAN_POINT('Ctrl Pts',(4.84249076595225,-0.862994459733448,
7.2159244020139));
#23971=CARTESIAN_POINT('Ctrl Pts',(4.85472691289473,-0.791266730478749,
7.22007605517951));
#23972=CARTESIAN_POINT('Ctrl Pts',(4.87093260873582,-0.681649903374358,
7.22637587324951));
#23973=CARTESIAN_POINT('Ctrl Pts',(4.87606079811396,-0.643942717480421,
7.22853477955875));
#23974=CARTESIAN_POINT('Ctrl Pts',(4.88677026056715,-0.557713753790923,
7.23345188013408));
#23975=CARTESIAN_POINT('Ctrl Pts',(4.89206741692258,-0.50916075844421,7.23620687938527));
#23976=CARTESIAN_POINT('Ctrl Pts',(4.90262645512341,-0.396892113144574,
7.24255510149858));
#23977=CARTESIAN_POINT('Ctrl Pts',(4.90737094656236,-0.333136611869135,
7.24614378493346));
#23978=CARTESIAN_POINT('Ctrl Pts',(4.92310448246431,-0.0462315612044295,
7.26225718129194));
#23979=CARTESIAN_POINT('Ctrl Pts',(4.92012375211529,0.177415835946856,7.27473260198826));
#23980=CARTESIAN_POINT('Ctrl Pts',(4.89674708081442,0.463834425980844,7.29093070628994));
#23981=CARTESIAN_POINT('Ctrl Pts',(4.89030077242132,0.527477574863849,7.29454311049082));
#23982=CARTESIAN_POINT('Ctrl Pts',(4.87391548083669,0.662851962028703,7.30226247562188));
#23983=CARTESIAN_POINT('Ctrl Pts',(4.86362993746052,0.734526040634645,7.30637090541187));
#23984=CARTESIAN_POINT('Ctrl Pts',(4.84515319410033,0.845755327414831,7.31278509681974));
#23985=CARTESIAN_POINT('Ctrl Pts',(4.83805068678152,0.885481267418061,7.31508360422993));
#23986=CARTESIAN_POINT('Ctrl Pts',(4.79382776815947,1.1163898714064,7.32849013993213));
#23987=CARTESIAN_POINT('Ctrl Pts',(4.74586681008939,1.30531921586182,7.339653266482));
#23988=CARTESIAN_POINT('Ctrl Pts',(4.6647767160168,1.56023539026103,7.3549443536397));
#23989=CARTESIAN_POINT('Ctrl Pts',(4.64118623628629,1.62906930027749,7.35909601764795));
#23990=CARTESIAN_POINT('Ctrl Pts',(4.60294471798695,1.73306981825063,7.3653958481442));
#23991=CARTESIAN_POINT('Ctrl Pts',(4.58939804413654,1.76863131402072,7.36755475609683));
#23992=CARTESIAN_POINT('Ctrl Pts',(4.55752595544476,1.84946623835404,7.37247185291465));
#23993=CARTESIAN_POINT('Ctrl Pts',(4.53893614759754,1.8946310797409,7.37522684680306));
#23994=CARTESIAN_POINT('Ctrl Pts',(4.49446774063554,1.99825654285989,7.38157505250386));
#23995=CARTESIAN_POINT('Ctrl Pts',(4.4681158035053,2.05650449806004,7.38516372492274));
#23996=CARTESIAN_POINT('Ctrl Pts',(4.34459761442576,2.31593759231043,7.40127714310026));
#23997=CARTESIAN_POINT('Ctrl Pts',(4.23492756844381,2.51087292893292,7.41375259600591));
#23998=CARTESIAN_POINT('Ctrl Pts',(4.07730338704221,2.75115819865284,7.42995073148231));
#23999=CARTESIAN_POINT('Ctrl Pts',(4.04117966895238,2.80395098312828,7.43356313387674));
#24000=CARTESIAN_POINT('Ctrl Pts',(3.96199412911397,2.91496610020577,7.44128249980783));
#24001=CARTESIAN_POINT('Ctrl Pts',(3.91865538660908,2.97297235784486,7.44539093222567));
#24002=CARTESIAN_POINT('Ctrl Pts',(3.84919097806788,3.06178711974118,7.45180512918924));
#24003=CARTESIAN_POINT('Ctrl Pts',(3.82393945699752,3.09326664808159,7.4541036395246));
#24004=CARTESIAN_POINT('Ctrl Pts',(3.67458349587361,3.27483543226568,7.46751017257027));
#24005=CARTESIAN_POINT('Ctrl Pts',(3.54203969687229,3.4177572735651,7.47867329339827));
#24006=CARTESIAN_POINT('Ctrl Pts',(3.34882296625803,3.6027574177494,7.49396436966288));
#24007=CARTESIAN_POINT('Ctrl Pts',(3.29516212942431,3.65190128467041,7.49811602860376));
#24008=CARTESIAN_POINT('Ctrl Pts',(3.21180463970207,3.72490832466444,7.50441585329254));
#24009=CARTESIAN_POINT('Ctrl Pts',(3.18288859267893,3.74964682844187,7.50657476047713));
#24010=CARTESIAN_POINT('Ctrl Pts',(3.11621195223415,3.80536348782805,7.51149185905104));
#24011=CARTESIAN_POINT('Ctrl Pts',(3.07827119880927,3.83611974672936,7.51424685544575));
#24012=CARTESIAN_POINT('Ctrl Pts',(2.98962586473817,3.90581703147857,7.52059506881696));
#24013=CARTESIAN_POINT('Ctrl Pts',(2.93860749021198,3.94434476362664,7.52418374638418));
#24014=CARTESIAN_POINT('Ctrl Pts',(2.70597695217865,4.11300182049617,7.54029715436445));
#24015=CARTESIAN_POINT('Ctrl Pts',(2.51637810379095,4.23165871643153,7.55277259221695));
#24016=CARTESIAN_POINT('Ctrl Pts',(2.26296817405587,4.36717865322322,7.56897071312374));
#24017=CARTESIAN_POINT('Ctrl Pts',(2.20598148821953,4.39623929150023,7.57258311636243));
#24018=CARTESIAN_POINT('Ctrl Pts',(2.08331757197039,4.45580663132141,7.58030248191965));
#24019=CARTESIAN_POINT('Ctrl Pts',(2.01750063482169,4.485991068307,7.58441091310937));
#24020=CARTESIAN_POINT('Ctrl Pts',(1.91399845690158,4.53071975047165,7.59082510747651));
#24021=CARTESIAN_POINT('Ctrl Pts',(1.87675951482418,4.54627157663472,7.5931236164448));
#24022=CARTESIAN_POINT('Ctrl Pts',(1.65871446616653,4.63419651230902,7.60653015074433));
#24023=CARTESIAN_POINT('Ctrl Pts',(1.47392943744713,4.69623700712047,7.61769327425889));
#24024=CARTESIAN_POINT('Ctrl Pts',(1.21573224659156,4.7661799568481,7.6329843556193));
#24025=CARTESIAN_POINT('Ctrl Pts',(1.14509462496572,4.78364241535902,7.63713601692109));
#24026=CARTESIAN_POINT('Ctrl Pts',(1.03683686822607,4.80786959794581,7.64344307169396));
#24027=CARTESIAN_POINT('Ctrl Pts',(0.99948247674698,4.81577362446879,7.64560917348137));
#24028=CARTESIAN_POINT('Ctrl Pts',(0.927939186921827,4.8300435829962,7.64973741796102));
#24029=CARTESIAN_POINT('Ctrl Pts',(0.893767593379231,4.83648339884518,7.65170070792163));
#24030=CARTESIAN_POINT('Ctrl Pts',(0.85560335904116,4.84325736068748,7.65388558077693));
#24031=CARTESIAN_POINT('Ctrl Pts',(0.85167548729847,4.84394961103328,7.65411035631631));
#24032=CARTESIAN_POINT('Ctrl Pts',(0.841213707107986,4.84578028281944,7.65470880054106));
#24033=CARTESIAN_POINT('Ctrl Pts',(0.834678326720705,4.84691026752705,7.65508239480081));
#24034=CARTESIAN_POINT('Ctrl Pts',(0.817317607904486,4.84987582801172,7.65607418497732));
#24035=CARTESIAN_POINT('Ctrl Pts',(0.806488364786014,4.85168838008895,7.6566921890241));
#24036=CARTESIAN_POINT('Ctrl Pts',(0.724373839009992,4.8651498316236,7.66137369467279));
#24037=CARTESIAN_POINT('Ctrl Pts',(0.652845340211353,4.87526342165295,7.66542547178192));
#24038=CARTESIAN_POINT('Ctrl Pts',(0.3784903304552,4.9079087320114,7.68091165053709));
#24039=CARTESIAN_POINT('Ctrl Pts',(0.174558611429953,4.91938525749718,7.6923169665087));
#24040=CARTESIAN_POINT('Ctrl Pts',(-0.0930765618389588,4.91778026207772,
7.70739970893978));
#24041=CARTESIAN_POINT('Ctrl Pts',(-0.156645318064476,4.91616599474898,
7.71098981375896));
#24042=CARTESIAN_POINT('Ctrl Pts',(-0.284131261217925,4.91045338619682,
7.71821205787909));
#24043=CARTESIAN_POINT('Ctrl Pts',(-0.348035527932679,4.90633816485267,
7.72184362564228));
#24044=CARTESIAN_POINT('Ctrl Pts',(-0.484321578294143,4.8948857227741,7.72961775328187));
#24045=CARTESIAN_POINT('Ctrl Pts',(-0.556657849699929,4.88718789516025,
7.73376173588517));
#24046=CARTESIAN_POINT('Ctrl Pts',(-0.759828367297922,4.8609977000814,7.74545535619367));
#24047=CARTESIAN_POINT('Ctrl Pts',(-0.890126085322538,4.83883384570765,
7.75301992334525));
#24048=CARTESIAN_POINT('Ctrl Pts',(-1.12306673609224,4.7894821599995,7.76664820089394));
#24049=CARTESIAN_POINT('Ctrl Pts',(-1.2260248762179,4.76416641732152,7.77270903999833));
#24050=CARTESIAN_POINT('Ctrl Pts',(-1.36761361164759,4.72445779511306,7.78107714959033));
#24051=CARTESIAN_POINT('Ctrl Pts',(-1.40700199835899,4.71287745300862,7.78340858655596));
#24052=CARTESIAN_POINT('Ctrl Pts',(-1.47808680716164,4.69100763089798,7.78762061087861));
#24053=CARTESIAN_POINT('Ctrl Pts',(-1.50983230982812,4.68088662826973,7.78950337733068));
#24054=CARTESIAN_POINT('Ctrl Pts',(-1.54921060694038,4.66788988251512,7.79184263322448));
#24055=CARTESIAN_POINT('Ctrl Pts',(-1.55694215998566,4.66531677067464,7.79230210687444));
#24056=CARTESIAN_POINT('Ctrl Pts',(-1.57440098300788,4.65945812523704,7.79334011271191));
#24057=CARTESIAN_POINT('Ctrl Pts',(-1.58412443661279,4.65616132088417,7.79391853676024));
#24058=CARTESIAN_POINT('Ctrl Pts',(-1.60284438574317,4.64974876532318,7.79503283002394));
#24059=CARTESIAN_POINT('Ctrl Pts',(-1.61184229527788,4.64663729175639,7.79556873317469));
#24060=CARTESIAN_POINT('Ctrl Pts',(-1.68756493844513,4.62020601693896,7.80008151295579));
#24061=CARTESIAN_POINT('Ctrl Pts',(-1.75378926871329,4.59547629552562,7.80404696352562));
#24062=CARTESIAN_POINT('Ctrl Pts',(-2.01266330356796,4.4923953958986,7.81966617551992));
#24063=CARTESIAN_POINT('Ctrl Pts',(-2.20079311862945,4.40328724624318,7.83128755476275));
#24064=CARTESIAN_POINT('Ctrl Pts',(-2.41927666459205,4.28229262630039,7.84536297369916));
#24065=CARTESIAN_POINT('Ctrl Pts',(-2.45557791612058,4.26158031538454,7.8477213545114));
#24066=CARTESIAN_POINT('Ctrl Pts',(-2.54989189255759,4.20616260388858,7.85390339851401));
#24067=CARTESIAN_POINT('Ctrl Pts',(-2.60746050539538,4.17071961307367,7.85773208944402));
#24068=CARTESIAN_POINT('Ctrl Pts',(-2.72097051952861,4.09756649022808,7.86539931504959));
#24069=CARTESIAN_POINT('Ctrl Pts',(-2.77690329354805,4.05986941713503,7.86923699637247));
#24070=CARTESIAN_POINT('Ctrl Pts',(-2.87630836174342,3.98985772875539,7.87616937621111));
#24071=CARTESIAN_POINT('Ctrl Pts',(-2.92005596430082,3.95795245097997,7.87926084872527));
#24072=CARTESIAN_POINT('Ctrl Pts',(-3.10763152500895,3.81634999236261,7.89269505717952));
#24073=CARTESIAN_POINT('Ctrl Pts',(-3.24587337153958,3.69948742128846,7.90306746712873));
#24074=CARTESIAN_POINT('Ctrl Pts',(-3.41518489999616,3.53954829161749,7.91635078105455));
#24075=CARTESIAN_POINT('Ctrl Pts',(-3.45243742265772,3.50322222261266,7.91931212149051));
#24076=CARTESIAN_POINT('Ctrl Pts',(-3.51546145991991,3.43978372627169,7.92438607435672));
#24077=CARTESIAN_POINT('Ctrl Pts',(-3.54151260918142,3.41295617141851,7.92650250108592));
#24078=CARTESIAN_POINT('Ctrl Pts',(-3.57662920391338,3.37595793762689,7.92938335719712));
#24079=CARTESIAN_POINT('Ctrl Pts',(-3.5859617582813,3.36604318581503,7.93015174584316));
#24080=CARTESIAN_POINT('Ctrl Pts',(-3.60081466876786,3.35013182020227,7.93137924529148));
#24081=CARTESIAN_POINT('Ctrl Pts',(-3.60636148561714,3.344160033093,7.93183868955648));
#24082=CARTESIAN_POINT('Ctrl Pts',(-3.66481626328689,3.28091216233567,7.93669167442809));
#24083=CARTESIAN_POINT('Ctrl Pts',(-3.71637029823852,3.22239892947686,7.94106884369432));
#24084=CARTESIAN_POINT('Ctrl Pts',(-3.90811626378505,2.9940443597575,7.95778826929178));
#24085=CARTESIAN_POINT('Ctrl Pts',(-4.03823391256918,2.81608596980777,7.9700873078123));
#24086=CARTESIAN_POINT('Ctrl Pts',(-4.19188774783474,2.57327948826339,7.98628413891051));
#24087=CARTESIAN_POINT('Ctrl Pts',(-4.22662242456887,2.51582053535723,7.99007616922156));
#24088=CARTESIAN_POINT('Ctrl Pts',(-4.29191806672198,2.40263583924494,7.9974750697209));
#24089=CARTESIAN_POINT('Ctrl Pts',(-4.32259680498291,2.34699305863723,8.00108025677559));
#24090=CARTESIAN_POINT('Ctrl Pts',(-4.38736284553651,2.22394544153685,8.00898780776939));
#24091=CARTESIAN_POINT('Ctrl Pts',(-4.42099287813049,2.15631813023155,8.01329240851244));
#24092=CARTESIAN_POINT('Ctrl Pts',(-4.51615926623172,1.95335247217197,8.02609452662168));
#24093=CARTESIAN_POINT('Ctrl Pts',(-4.57313180781293,1.81596958664167,8.03461102999183));
#24094=CARTESIAN_POINT('Ctrl Pts',(-4.64817323254806,1.60897027349304,8.04720508761879));
#24095=CARTESIAN_POINT('Ctrl Pts',(-4.67108231578293,1.5411975475882,8.05129135760475));
#24096=CARTESIAN_POINT('Ctrl Pts',(-4.70577863845991,1.43066236506373,8.05788921025566));
#24097=CARTESIAN_POINT('Ctrl Pts',(-4.71848002125068,1.38819802177408,8.0604081695738));
#24098=CARTESIAN_POINT('Ctrl Pts',(-4.73983902255868,1.31310627375847,8.06483255285959));
#24099=CARTESIAN_POINT('Ctrl Pts',(-4.74873789707925,1.2805508395401,8.06674071604243));
#24100=CARTESIAN_POINT('Ctrl Pts',(-4.75956918758595,1.23925950449858,8.0691499986643));
#24101=CARTESIAN_POINT('Ctrl Pts',(-4.76181370441031,1.23060684651069,8.06965426408417));
#24102=CARTESIAN_POINT('Ctrl Pts',(-4.76403458713635,1.22194824565879,8.07015829796832));
#24103=CARTESIAN_POINT('Origin',(0.,0.,-3.23514056400928));
#24104=CARTESIAN_POINT('',(-4.76403458704821,1.22194824600244,10.1653249229632));
#24105=CARTESIAN_POINT('',(-4.76374494423105,1.22187361077196,9.81992259791717));
#24106=CARTESIAN_POINT('',(-4.76403458704967,1.22194824599672,-3.23514056400928));
#24107=CARTESIAN_POINT('',(-4.91824999837441,0.000126452135718109,8.48514056400927));
#24108=CARTESIAN_POINT('Ctrl Pts',(-4.76403458704821,1.22194824600244,10.1653249229632));
#24109=CARTESIAN_POINT('Ctrl Pts',(-4.76379686960342,1.22287503986022,10.1652702466491));
#24110=CARTESIAN_POINT('Ctrl Pts',(-4.76355888131435,1.22380176589749,10.1652155692027));
#24111=CARTESIAN_POINT('Ctrl Pts',(-4.72137445563459,1.38786911408632,10.1555345787607));
#24112=CARTESIAN_POINT('Ctrl Pts',(-4.67107487714302,1.54874686609432,10.1458780018919));
#24113=CARTESIAN_POINT('Ctrl Pts',(-4.59083775675595,1.76559678829643,10.1326750074967));
#24114=CARTESIAN_POINT('Ctrl Pts',(-4.56792959485441,1.82404569052493,10.12909764159));
#24115=CARTESIAN_POINT('Ctrl Pts',(-4.52983613972323,1.91601670895238,10.1234442094655));
#24116=CARTESIAN_POINT('Ctrl Pts',(-4.5153828869176,1.94983407238386,10.1213604786415));
#24117=CARTESIAN_POINT('Ctrl Pts',(-4.47710686609372,2.03668275729377,10.1159953495209));
#24118=CARTESIAN_POINT('Ctrl Pts',(-4.45272068633773,2.08945953606607,10.1127207221413));
#24119=CARTESIAN_POINT('Ctrl Pts',(-4.36174400915149,2.27752193488876,10.1009760808265));
#24120=CARTESIAN_POINT('Ctrl Pts',(-4.28987640509362,2.41016138859182,10.0925469864519));
#24121=CARTESIAN_POINT('Ctrl Pts',(-4.14862070490562,2.64446826013169,10.0772106915698));
#24122=CARTESIAN_POINT('Ctrl Pts',(-4.0812956305547,2.74723344088206,10.0703171379118));
#24123=CARTESIAN_POINT('Ctrl Pts',(-3.97388873739136,2.89850378996609,10.0598568339744));
#24124=CARTESIAN_POINT('Ctrl Pts',(-3.93660756454765,2.94893823176713,10.0563141078044));
#24125=CARTESIAN_POINT('Ctrl Pts',(-3.85407027465479,3.05624037300058,10.0486490059244));
#24126=CARTESIAN_POINT('Ctrl Pts',(-3.8084975719434,3.11284580055319,10.0445247538165));
#24127=CARTESIAN_POINT('Ctrl Pts',(-3.71073577283674,3.22891290696235,10.0358901827421));
#24128=CARTESIAN_POINT('Ctrl Pts',(-3.65833223703798,3.28816721094897,10.0313792131835));
#24129=CARTESIAN_POINT('Ctrl Pts',(-3.48480347951792,3.47509602234596,10.0168054996788));
#24130=CARTESIAN_POINT('Ctrl Pts',(-3.35824921395468,3.59754218673306,10.006716469207));
#24131=CARTESIAN_POINT('Ctrl Pts',(-3.17975157962301,3.75260178478131,9.99321831354768));
#24132=CARTESIAN_POINT('Ctrl Pts',(-3.13336924390907,3.79141630137753,9.98977269901734));
#24133=CARTESIAN_POINT('Ctrl Pts',(-3.05767059483008,3.85242572894921,9.9842521917851));
#24134=CARTESIAN_POINT('Ctrl Pts',(-3.02880105558526,3.87516421195266,9.98217044645512));
#24135=CARTESIAN_POINT('Ctrl Pts',(-2.95197167751795,3.93429414144715,9.97669093754206));
#24136=CARTESIAN_POINT('Ctrl Pts',(-2.90359380173349,3.97013228247349,9.97330074030465));
#24137=CARTESIAN_POINT('Ctrl Pts',(-2.78066560570278,4.05774793137651,9.96481632029374));
#24138=CARTESIAN_POINT('Ctrl Pts',(-2.70531717305857,4.10836690848389,9.95973195871955));
#24139=CARTESIAN_POINT('Ctrl Pts',(-2.49171174242977,4.24344096399808,9.94557327542539));
#24140=CARTESIAN_POINT('Ctrl Pts',(-2.35062077042142,4.32319324756917,9.93650494876144));
#24141=CARTESIAN_POINT('Ctrl Pts',(-2.14027416845257,4.42874622856134,9.92324995664961));
#24142=CARTESIAN_POINT('Ctrl Pts',(-2.07396703265842,4.46018242401888,9.91910864883493));
#24143=CARTESIAN_POINT('Ctrl Pts',(-1.94243041748114,4.51897627139127,9.91095448332424));
#24144=CARTESIAN_POINT('Ctrl Pts',(-1.87726467116537,4.54643373078613,9.90694338686368));
#24145=CARTESIAN_POINT('Ctrl Pts',(-1.66178531833791,4.63180264343459,9.89376297661376));
#24146=CARTESIAN_POINT('Ctrl Pts',(-1.50921829070979,4.68373623425784,9.88455750945212));
#24147=CARTESIAN_POINT('Ctrl Pts',(-1.21893522283393,4.76688901259839,9.86727257949013));
#24148=CARTESIAN_POINT('Ctrl Pts',(-1.08188386701515,4.79985019243221,9.85920517059126));
#24149=CARTESIAN_POINT('Ctrl Pts',(-0.902948178720308,4.83483028412233,
9.84882814445847));
#24150=CARTESIAN_POINT('Ctrl Pts',(-0.86219127418395,4.8422645066816,9.84647502193498));
#24151=CARTESIAN_POINT('Ctrl Pts',(-0.779592497046392,4.85625492379467,
9.84172959527507));
#24152=CARTESIAN_POINT('Ctrl Pts',(-0.737750069124316,4.86278739384556,
9.8393377143324));
#24153=CARTESIAN_POINT('Ctrl Pts',(-0.587648426827218,4.88423937604565,
9.83079066061389));
#24154=CARTESIAN_POINT('Ctrl Pts',(-0.478982327106876,4.89609041575107,
9.82466437227494));
#24155=CARTESIAN_POINT('Ctrl Pts',(-0.330168538068199,4.9073178262427,9.81630216199654));
#24156=CARTESIAN_POINT('Ctrl Pts',(-0.290291022566702,4.90983814755577,
9.81406410772107));
#24157=CARTESIAN_POINT('Ctrl Pts',(-0.0986536452562509,4.91960703995444,
9.80331377585089));
#24158=CARTESIAN_POINT('Ctrl Pts',(0.0533552664461227,4.92030673605178,
9.79479868821307));
#24159=CARTESIAN_POINT('Ctrl Pts',(0.268532306588229,4.91132341200776,9.78265922315142));
#24160=CARTESIAN_POINT('Ctrl Pts',(0.33185605757132,4.90745134519767,9.77907658964663));
#24161=CARTESIAN_POINT('Ctrl Pts',(0.466398097436955,4.89660844019906,9.77143581988103));
#24162=CARTESIAN_POINT('Ctrl Pts',(0.537574988305485,4.8893061240547,9.76737630607454));
#24163=CARTESIAN_POINT('Ctrl Pts',(0.767508788425144,4.86063460104369,9.75419596892673));
#24164=CARTESIAN_POINT('Ctrl Pts',(0.925386064185252,4.83306299749805,9.74504012016212));
#24165=CARTESIAN_POINT('Ctrl Pts',(1.2156461660436,4.76762618650111,9.72800752022895));
#24166=CARTESIAN_POINT('Ctrl Pts',(1.34833465840257,4.73181247639205,9.7201423867171));
#24167=CARTESIAN_POINT('Ctrl Pts',(1.51903665017495,4.67797417520116,9.70995452050717));
#24168=CARTESIAN_POINT('Ctrl Pts',(1.55856274125989,4.66495412251792,9.70759072700317));
#24169=CARTESIAN_POINT('Ctrl Pts',(1.6377799961365,4.63774041399282,9.70284589577237));
#24170=CARTESIAN_POINT('Ctrl Pts',(1.6774635113954,4.62353497732534,9.70046518518342));
#24171=CARTESIAN_POINT('Ctrl Pts',(1.76485036628183,4.5909800755694,9.69520829968754));
#24172=CARTESIAN_POINT('Ctrl Pts',(1.81246023038522,4.5723935578756,9.69233467556155));
#24173=CARTESIAN_POINT('Ctrl Pts',(1.97125812018535,4.50753007351493,9.68270283866493));
#24174=CARTESIAN_POINT('Ctrl Pts',(2.08103441066348,4.45791228447537,9.67596501276302));
#24175=CARTESIAN_POINT('Ctrl Pts',(2.30752289452494,4.34535088683849,9.6617912982349));
#24176=CARTESIAN_POINT('Ctrl Pts',(2.42373462353738,4.28161722855317,9.65435853704751));
#24177=CARTESIAN_POINT('Ctrl Pts',(2.5912268385222,4.18075346230769,9.64333613268098));
#24178=CARTESIAN_POINT('Ctrl Pts',(2.64459302378546,4.14720190886849,9.63977583477576));
#24179=CARTESIAN_POINT('Ctrl Pts',(2.75761229834963,4.07307744539168,9.63212383175679));
#24180=CARTESIAN_POINT('Ctrl Pts',(2.81704740274419,4.03219905661168,9.62803048150884));
#24181=CARTESIAN_POINT('Ctrl Pts',(2.9388209033491,3.94443848725308,9.61949101454432));
#24182=CARTESIAN_POINT('Ctrl Pts',(3.00098668885025,3.89735063949391,9.61504438220197));
#24183=CARTESIAN_POINT('Ctrl Pts',(3.19312877377477,3.74448754513546,9.60101693677749));
#24184=CARTESIAN_POINT('Ctrl Pts',(3.31883438164156,3.63353773855162,9.59141218229546));
#24185=CARTESIAN_POINT('Ctrl Pts',(3.48716765548531,3.46892681650276,9.57796187969366));
#24186=CARTESIAN_POINT('Ctrl Pts',(3.53471622064002,3.42046384557414,9.5740911050927));
#24187=CARTESIAN_POINT('Ctrl Pts',(3.60658289763835,3.34411561798373,9.56813452784262));
#24188=CARTESIAN_POINT('Ctrl Pts',(3.63161496112999,3.31691457348638,9.56603922599912));
#24189=CARTESIAN_POINT('Ctrl Pts',(3.69288285178246,3.24881283710017,9.56085917029369));
#24190=CARTESIAN_POINT('Ctrl Pts',(3.72874823813457,3.207585585262,9.55777985300247));
#24191=CARTESIAN_POINT('Ctrl Pts',(3.86219353239414,3.048926709225,9.54611960073225));
#24192=CARTESIAN_POINT('Ctrl Pts',(3.95497424984526,2.92757105254055,9.53758432389728));
#24193=CARTESIAN_POINT('Ctrl Pts',(4.11281148504426,2.69989441241424,9.52205654350608));
#24194=CARTESIAN_POINT('Ctrl Pts',(4.17976045802128,2.59504337713921,9.51507770187174));
#24195=CARTESIAN_POINT('Ctrl Pts',(4.27460809724857,2.43328937455458,9.50450715953463));
#24196=CARTESIAN_POINT('Ctrl Pts',(4.30550067155555,2.37820003893879,9.50094008003325));
#24197=CARTESIAN_POINT('Ctrl Pts',(4.36929557217262,2.25911810590922,9.49329206617317));
#24198=CARTESIAN_POINT('Ctrl Pts',(4.40187185366961,2.19496752498877,9.4892095707269));
#24199=CARTESIAN_POINT('Ctrl Pts',(4.45043430535197,2.09390366526493,9.48283094233865));
#24200=CARTESIAN_POINT('Ctrl Pts',(4.46739491706761,2.05746948839183,9.48054193859886));
#24201=CARTESIAN_POINT('Ctrl Pts',(4.56382874449322,1.8434980235541,9.46715853316292));
#24202=CARTESIAN_POINT('Ctrl Pts',(4.63315972021679,1.6615799132947,9.45600931320434));
#24203=CARTESIAN_POINT('Ctrl Pts',(4.71431345957692,1.40363547551885,9.4405524479604));
#24204=CARTESIAN_POINT('Ctrl Pts',(4.73541343816889,1.33071549279272,9.43622170977432));
#24205=CARTESIAN_POINT('Ctrl Pts',(4.76438994797274,1.22113616544467,9.42977999246851));
#24206=CARTESIAN_POINT('Ctrl Pts',(4.77354873962446,1.18482808786651,9.42765652133304));
#24207=CARTESIAN_POINT('Ctrl Pts',(4.79421222192891,1.09878035466701,9.42265047384854));
#24208=CARTESIAN_POINT('Ctrl Pts',(4.80535886023037,1.0489592024184,9.41977195675482));
#24209=CARTESIAN_POINT('Ctrl Pts',(4.8464905393913,0.8506766230049,9.4083763568927));
#24210=CARTESIAN_POINT('Ctrl Pts',(4.87038693639682,0.7010371380656,9.39990800673258));
#24211=CARTESIAN_POINT('Ctrl Pts',(4.88961768096841,0.53031677156654,9.39028027568745));
#24212=CARTESIAN_POINT('Ctrl Pts',(4.89176947319828,0.510086624099066,9.38913998010303));
#24213=CARTESIAN_POINT('Ctrl Pts',(4.90584185316167,0.369496168752397,9.38121806222294));
#24214=CARTESIAN_POINT('Ctrl Pts',(4.91344445156743,0.248746447774333,9.37442629238887));
#24215=CARTESIAN_POINT('Ctrl Pts',(4.91835528027675,0.0598821449223939,
9.36376973764994));
#24216=CARTESIAN_POINT('Ctrl Pts',(4.91871311481507,-0.00810509747336468,
9.3599270785901));
#24217=CARTESIAN_POINT('Ctrl Pts',(4.91646504737613,-0.153420773411911,
9.35169152091769));
#24218=CARTESIAN_POINT('Ctrl Pts',(4.91344405681667,-0.230724510835193,
9.34729689970407));
#24219=CARTESIAN_POINT('Ctrl Pts',(4.90239795447109,-0.406809796795339,
9.33724816159998));
#24220=CARTESIAN_POINT('Ctrl Pts',(4.89320803648174,-0.505484654148446,
9.33158907696805));
#24221=CARTESIAN_POINT('Ctrl Pts',(4.85824986835514,-0.788075728287074,
9.31529934921482));
#24222=CARTESIAN_POINT('Ctrl Pts',(4.82503975880103,-0.970900296213722,
9.30465420832144));
#24223=CARTESIAN_POINT('Ctrl Pts',(4.77333716600311,-1.18561077336241,9.29209405504729));
#24224=CARTESIAN_POINT('Ctrl Pts',(4.76473470897244,-1.21972283727005,9.29009701520104));
#24225=CARTESIAN_POINT('Ctrl Pts',(4.74472702463483,-1.29561727175221,9.2856519460565));
#24226=CARTESIAN_POINT('Ctrl Pts',(4.73313436642068,-1.3373472927828,9.28320634162732));
#24227=CARTESIAN_POINT('Ctrl Pts',(4.71327999300418,-1.40532252077077,9.27921545059115));
#24228=CARTESIAN_POINT('Ctrl Pts',(4.70534660956014,-1.43166091473649,9.27766732444666));
#24229=CARTESIAN_POINT('Ctrl Pts',(4.65108945065757,-1.60646771172044,9.26737600368524));
#24230=CARTESIAN_POINT('Ctrl Pts',(4.5979663373299,-1.75273435792148,9.2586827538543));
#24231=CARTESIAN_POINT('Ctrl Pts',(4.49120130920548,-2.00824017091746,9.24315915279642));
#24232=CARTESIAN_POINT('Ctrl Pts',(4.44027057061565,-2.11846985443216,9.23634479207004));
#24233=CARTESIAN_POINT('Ctrl Pts',(4.35700930345676,-2.28244642931361,9.22597494628348));
#24234=CARTESIAN_POINT('Ctrl Pts',(4.32764382451953,-2.33764637967326,9.22244282289246));
#24235=CARTESIAN_POINT('Ctrl Pts',(4.26171453812721,-2.45607509110152,9.21476756203614));
#24236=CARTESIAN_POINT('Ctrl Pts',(4.22477854412438,-2.5190795427007,9.21062239753048));
#24237=CARTESIAN_POINT('Ctrl Pts',(4.14454916263361,-2.64920184584863,9.20192360513128));
#24238=CARTESIAN_POINT('Ctrl Pts',(4.10099606986845,-2.7161349819613,9.19736923545529));
#24239=CARTESIAN_POINT('Ctrl Pts',(3.96186183938436,-2.91897817504703,9.1833132734703));
#24240=CARTESIAN_POINT('Ctrl Pts',(3.86100947263396,-3.051129064422,9.17378998380648));
#24241=CARTESIAN_POINT('Ctrl Pts',(3.71151622078594,-3.22770587482084,9.16057585216328));
#24242=CARTESIAN_POINT('Ctrl Pts',(3.6683820313404,-3.27664634849965,9.15685750750201));
#24243=CARTESIAN_POINT('Ctrl Pts',(3.59937732546918,-3.35186869541264,9.15105939842205));
#24244=CARTESIAN_POINT('Ctrl Pts',(3.57416336947065,-3.378741945967,9.14897109346012));
#24245=CARTESIAN_POINT('Ctrl Pts',(3.50967140968571,-3.44594817282243,9.14370486038983));
#24246=CARTESIAN_POINT('Ctrl Pts',(3.46999849901174,-3.48589482642406,9.14053300034068));
#24247=CARTESIAN_POINT('Ctrl Pts',(3.37172487137077,-3.58150601801696,9.13282313638277));
#24248=CARTESIAN_POINT('Ctrl Pts',(3.31242098542295,-3.63642425064118,9.12829285936765));
#24249=CARTESIAN_POINT('Ctrl Pts',(3.10803220043903,-3.81654765738064,9.11302768590466));
#24250=CARTESIAN_POINT('Ctrl Pts',(2.95699421758855,-3.93472797984795,9.10230903105011));
#24251=CARTESIAN_POINT('Ctrl Pts',(2.74728643826898,-4.07990504647664,9.08793228076171));
#24252=CARTESIAN_POINT('Ctrl Pts',(2.69443077468446,-4.11500311712939,9.08434934050108));
#24253=CARTESIAN_POINT('Ctrl Pts',(2.58056377755479,-4.18748026047541,9.07670868913933));
#24254=CARTESIAN_POINT('Ctrl Pts',(2.51938587796649,-4.22457039007471,9.07264960399454));
#24255=CARTESIAN_POINT('Ctrl Pts',(2.31973212503026,-4.3397340932608,9.0595391116142));
#24256=CARTESIAN_POINT('Ctrl Pts',(2.17827523823209,-4.41243300006857,9.05045337362229));
#24257=CARTESIAN_POINT('Ctrl Pts',(1.90714666265894,-4.53555365342887,9.03340776031207));
#24258=CARTESIAN_POINT('Ctrl Pts',(1.77836975984092,-4.58757637019983,9.02545929719546));
#24259=CARTESIAN_POINT('Ctrl Pts',(1.60842579967038,-4.64799687394563,9.01519340198725));
#24260=CARTESIAN_POINT('Ctrl Pts',(1.5691124717664,-4.66141551460841,9.01283391216292));
#24261=CARTESIAN_POINT('Ctrl Pts',(1.48950075017981,-4.687467727895,9.00808889272457));
#24262=CARTESIAN_POINT('Ctrl Pts',(1.44920012969174,-4.70008353377655,9.00570372866885));
#24263=CARTESIAN_POINT('Ctrl Pts',(1.35963656085164,-4.72685924453157,9.00043418042529));
#24264=CARTESIAN_POINT('Ctrl Pts',(1.31030458450458,-4.74077123014954,8.99755236758017));
#24265=CARTESIAN_POINT('Ctrl Pts',(1.14355802989694,-4.78499336532816,8.98786588846651));
#24266=CARTESIAN_POINT('Ctrl Pts',(1.02524230931461,-4.81173200576692,8.98108183534108));
#24267=CARTESIAN_POINT('Ctrl Pts',(0.77741366775612,-4.85818300742241,8.96695111412338));
#24268=CARTESIAN_POINT('Ctrl Pts',(0.647858156546125,-4.87715012594922,
8.95960791547125));
#24269=CARTESIAN_POINT('Ctrl Pts',(0.449287006469579,-4.89816876755121,
8.94835113327228));
#24270=CARTESIAN_POINT('Ctrl Pts',(0.380728321367008,-4.90397409206418,
8.94446462303749));
#24271=CARTESIAN_POINT('Ctrl Pts',(0.252993107993749,-4.91209546442165,
8.93721560062547));
#24272=CARTESIAN_POINT('Ctrl Pts',(0.193852650364851,-4.91478467727583,
8.9338562559431));
#24273=CARTESIAN_POINT('Ctrl Pts',(0.0602279577463912,-4.91844514999225,
8.92625505543547));
#24274=CARTESIAN_POINT('Ctrl Pts',(-0.0142587363162196,-4.91879320934879,
8.92201016832599));
#24275=CARTESIAN_POINT('Ctrl Pts',(-0.232898185613029,-4.91484836499791,
8.90952316325364));
#24276=CARTESIAN_POINT('Ctrl Pts',(-0.376887746122749,-4.90590779622597,
8.90126317323262));
#24277=CARTESIAN_POINT('Ctrl Pts',(-0.608333217285808,-4.88128627954514,
8.88794769081639));
#24278=CARTESIAN_POINT('Ctrl Pts',(-0.69612303946579,-4.86954187079948,
8.88288854422808));
#24279=CARTESIAN_POINT('Ctrl Pts',(-0.822761046317827,-4.84910558664577,
8.87559057875893));
#24280=CARTESIAN_POINT('Ctrl Pts',(-0.861895873358112,-4.84230278827586,
8.87333535806386));
#24281=CARTESIAN_POINT('Ctrl Pts',(-0.937738991330432,-4.8281704090436,
8.86896672169268));
#24282=CARTESIAN_POINT('Ctrl Pts',(-0.974454414857338,-4.82089437205882,
8.8668525822506));
#24283=CARTESIAN_POINT('Ctrl Pts',(-1.01444164373047,-4.81249446639752,
8.86454879001763));
#24284=CARTESIAN_POINT('Ctrl Pts',(-1.01779910481413,-4.81178551266636,
8.86435534630946));
#24285=CARTESIAN_POINT('Ctrl Pts',(-1.02509046355174,-4.81023791333416,
8.86393522294324));
#24286=CARTESIAN_POINT('Ctrl Pts',(-1.02902408054916,-4.80939795432142,
8.86370855533334));
#24287=CARTESIAN_POINT('Ctrl Pts',(-1.0376559299184,-4.80754369046655,8.86321112238485));
#24288=CARTESIAN_POINT('Ctrl Pts',(-1.04235371571048,-4.80652732188719,
8.86294037534294));
#24289=CARTESIAN_POINT('Ctrl Pts',(-1.10521165810498,-4.79283148309207,
8.85931730671267));
#24290=CARTESIAN_POINT('Ctrl Pts',(-1.16313882040914,-4.77910395441256,
8.8559739986206));
#24291=CARTESIAN_POINT('Ctrl Pts',(-1.39546955289134,-4.71957194859762,
8.8425194767058));
#24292=CARTESIAN_POINT('Ctrl Pts',(-1.56754243727073,-4.66524439092781,
8.83244572881302));
#24293=CARTESIAN_POINT('Ctrl Pts',(-1.80989581021524,-4.57380118784936,
8.81788812726857));
#24294=CARTESIAN_POINT('Ctrl Pts',(-1.88287053067865,-4.54424675062605,
8.81345557348258));
#24295=CARTESIAN_POINT('Ctrl Pts',(-2.00224869747087,-4.49252968777582,
8.80610924268411));
#24296=CARTESIAN_POINT('Ctrl Pts',(-2.0490703190493,-4.47136820339269,8.80320318619195));
#24297=CARTESIAN_POINT('Ctrl Pts',(-2.16399586378667,-4.41724220346222,
8.79600461437046));
#24298=CARTESIAN_POINT('Ctrl Pts',(-2.23168673167228,-4.38343255111028,
8.79170666911089));
#24299=CARTESIAN_POINT('Ctrl Pts',(-2.3760935202413,-4.30709322380119,8.78240432795874));
#24300=CARTESIAN_POINT('Ctrl Pts',(-2.45250641415723,-4.26404555934227,
8.77739788200632));
#24301=CARTESIAN_POINT('Ctrl Pts',(-2.67304584173115,-4.13191322621563,
8.76269560726573));
#24302=CARTESIAN_POINT('Ctrl Pts',(-2.81376957642028,-4.03739793114908,
8.7529838023842));
#24303=CARTESIAN_POINT('Ctrl Pts',(-2.99032344619345,-3.90509566256631,
8.74040324934802));
#24304=CARTESIAN_POINT('Ctrl Pts',(-3.03082928388353,-3.87374242616237,
8.73748849438426));
#24305=CARTESIAN_POINT('Ctrl Pts',(-3.09805012838817,-3.82001074145402,
8.73260633175094));
#24306=CARTESIAN_POINT('Ctrl Pts',(-3.12503001080965,-3.79797105276432,
8.73063461283748));
#24307=CARTESIAN_POINT('Ctrl Pts',(-3.15839488539357,-3.77011925510705,
8.72817969360587));
#24308=CARTESIAN_POINT('Ctrl Pts',(-3.16500144492923,-3.76457478393626,
8.7276927653901));
#24309=CARTESIAN_POINT('Ctrl Pts',(-3.17709761395905,-3.75436887875197,
8.7267996626337));
#24310=CARTESIAN_POINT('Ctrl Pts',(-3.18259163201268,-3.7497127130559,8.72639342219237));
#24311=CARTESIAN_POINT('Ctrl Pts',(-3.1959067632568,-3.73837782969405,8.72540738492953));
#24312=CARTESIAN_POINT('Ctrl Pts',(-3.20371719853828,-3.73168660921981,
8.72482774167346));
#24313=CARTESIAN_POINT('Ctrl Pts',(-3.22578974253956,-3.7126566296321,8.72318599332096));
#24314=CARTESIAN_POINT('Ctrl Pts',(-3.24000197548396,-3.70026024963596,
8.72212454007649));
#24315=CARTESIAN_POINT('Ctrl Pts',(-3.3115807945471,-3.63709825733186,8.716755333729));
#24316=CARTESIAN_POINT('Ctrl Pts',(-3.36782737576097,-3.58507879932278,
8.71245980224359));
#24317=CARTESIAN_POINT('Ctrl Pts',(-3.56773108643695,-3.39134072243121,
8.69685919985536));
#24318=CARTESIAN_POINT('Ctrl Pts',(-3.70384552709633,-3.24213265198416,
8.68557681518277));
#24319=CARTESIAN_POINT('Ctrl Pts',(-3.87347026614292,-3.03152174189137,
8.67033112404397));
#24320=CARTESIAN_POINT('Ctrl Pts',(-3.91540710032853,-2.97716023660427,
8.66645268296599));
#24321=CARTESIAN_POINT('Ctrl Pts',(-3.96012541627941,-2.91661337612306,
8.66218946709337));
#24322=CARTESIAN_POINT('Ctrl Pts',(-3.96404812423363,-2.91127967860756,
8.66181438487778));
#24323=CARTESIAN_POINT('Ctrl Pts',(-3.97149017706006,-2.90111780747741,
8.66110066374459));
#24324=CARTESIAN_POINT('Ctrl Pts',(-3.97501151818084,-2.89629110926061,
8.66076204140052));
#24325=CARTESIAN_POINT('Ctrl Pts',(-3.98378491041336,-2.8842192922372,8.65991607690125));
#24326=CARTESIAN_POINT('Ctrl Pts',(-3.98902599704824,-2.87696623767165,
8.65940864941668));
#24327=CARTESIAN_POINT('Ctrl Pts',(-4.04368087443625,-2.80089376474113,
8.65409538453157));
#24328=CARTESIAN_POINT('Ctrl Pts',(-4.09132792552962,-2.73082340198061,
8.64927628126284));
#24329=CARTESIAN_POINT('Ctrl Pts',(-4.1952015255127,-2.56924026783685,8.63832208188501));
#24330=CARTESIAN_POINT('Ctrl Pts',(-4.2502886706651,-2.47704608638311,8.63218221578728));
#24331=CARTESIAN_POINT('Ctrl Pts',(-4.36272849798232,-2.27405560456766,
8.6188997409065));
#24332=CARTESIAN_POINT('Ctrl Pts',(-4.41897411213275,-2.16272905236547,
8.61175950152938));
#24333=CARTESIAN_POINT('Ctrl Pts',(-4.49239050723868,-2.00256420936867,
8.60171152332366));
#24334=CARTESIAN_POINT('Ctrl Pts',(-4.51311571000412,-1.95540853947422,
8.59878003938712));
#24335=CARTESIAN_POINT('Ctrl Pts',(-4.54659222573431,-1.87587112165083,
8.59388355267721));
#24336=CARTESIAN_POINT('Ctrl Pts',(-4.55974727004699,-1.84366433781596,
8.59191417461849));
#24337=CARTESIAN_POINT('Ctrl Pts',(-4.59539094156781,-1.75368421923288,
8.58644662141081));
#24338=CARTESIAN_POINT('Ctrl Pts',(-4.61713065241062,-1.6956211016924,8.58295709963222));
#24339=CARTESIAN_POINT('Ctrl Pts',(-4.67130923271195,-1.54214354480996,
8.57381280496334));
#24340=CARTESIAN_POINT('Ctrl Pts',(-4.70192352877415,-1.44611617359454,
8.5681705738051));
#24341=CARTESIAN_POINT('Ctrl Pts',(-4.77359076766381,-1.19489250333297,
8.55353498666965));
#24342=CARTESIAN_POINT('Ctrl Pts',(-4.81003494102768,-1.0385084848992,8.54454372832498));
#24343=CARTESIAN_POINT('Ctrl Pts',(-4.85008662028798,-0.818436494833083,
8.53193411522017));
#24344=CARTESIAN_POINT('Ctrl Pts',(-4.86020445934079,-0.756036392071409,
8.52836400066404));
#24345=CARTESIAN_POINT('Ctrl Pts',(-4.87801276479547,-0.6309955321278,8.52121380370745));
#24346=CARTESIAN_POINT('Ctrl Pts',(-4.88570595530992,-0.568367050155467,
8.51763441550896));
#24347=CARTESIAN_POINT('Ctrl Pts',(-4.89819102465612,-0.447563356708912,
8.51072956049755));
#24348=CARTESIAN_POINT('Ctrl Pts',(-4.90315642882732,-0.389416525542466,
8.50740577200676));
#24349=CARTESIAN_POINT('Ctrl Pts',(-4.91452940169788,-0.220911331953344,
8.49777044851229));
#24350=CARTESIAN_POINT('Ctrl Pts',(-4.91825281349053,-0.110408334943236,
8.49144711962447));
#24351=CARTESIAN_POINT('Ctrl Pts',(-4.91824999840495,0.00012525870399141,
8.48511971591668));
#24352=CARTESIAN_POINT('Ctrl Pts',(-4.76403458704967,1.22194824599671,8.41520471722259));
#24353=CARTESIAN_POINT('Ctrl Pts',(-4.79982248259297,1.0824212466131,8.42336126929135));
#24354=CARTESIAN_POINT('Ctrl Pts',(-4.82947364947956,0.941332311715187,
8.43151782136011));
#24355=CARTESIAN_POINT('Ctrl Pts',(-4.85287602958132,0.799235449673663,
8.43967437342887));
#24356=CARTESIAN_POINT('Ctrl Pts',(-4.86756266525287,0.71005969772877,8.44479318220169));
#24357=CARTESIAN_POINT('Ctrl Pts',(-4.87978926605988,0.620487210156302,
8.44991199097452));
#24358=CARTESIAN_POINT('Ctrl Pts',(-4.88953849541565,0.530656540851442,
8.45503079974735));
#24359=CARTESIAN_POINT('Ctrl Pts',(-4.90598317603319,0.379133111412091,
8.46366503865378));
#24360=CARTESIAN_POINT('Ctrl Pts',(-4.91538074332051,0.226839147476468,
8.47229927756021));
#24361=CARTESIAN_POINT('Ctrl Pts',(-4.9176871206407,0.0744072979253948,
8.48093351646665));
#24362=CARTESIAN_POINT('Ctrl Pts',(-4.91806171606027,0.0496497389009686,
8.48233586564752));
#24363=CARTESIAN_POINT('Ctrl Pts',(-4.91824936172107,0.0248885507464108,
8.4837382148284));
#24364=CARTESIAN_POINT('Ctrl Pts',(-4.91824999837441,0.000126452135718109,
8.48514056400927));
#24365=CARTESIAN_POINT('',(-4.91787035223228,-3.97720175591356E-5,8.1398455264357));
#24366=CARTESIAN_POINT('Ctrl Pts',(-4.76403458713635,1.22194824565879,8.07015829796832));
#24367=CARTESIAN_POINT('Ctrl Pts',(-4.7829881060944,1.14805377411723,8.07445983792208));
#24368=CARTESIAN_POINT('Ctrl Pts',(-4.80022027915519,1.07372647371595,8.07874466348763));
#24369=CARTESIAN_POINT('Ctrl Pts',(-4.86183194194516,0.776733074723372,
8.09575746200658));
#24370=CARTESIAN_POINT('Ctrl Pts',(-4.89249982611999,0.551514877477385,
8.10843153398002));
#24371=CARTESIAN_POINT('Ctrl Pts',(-4.91127259025011,0.268034296101974,
8.12444404401394));
#24372=CARTESIAN_POINT('Ctrl Pts',(-4.91405238549001,0.21102112114891,8.12766659502292));
#24373=CARTESIAN_POINT('Ctrl Pts',(-4.91744686864092,0.102646600721967,
8.13380112341401));
#24374=CARTESIAN_POINT('Ctrl Pts',(-4.91825054455029,0.0512986358838704,
8.13671144365306));
#24375=CARTESIAN_POINT('Ctrl Pts',(-4.91824999972317,-5.2182147148742E-5,
8.13962702323731));
#24376=CARTESIAN_POINT('Ctrl Pts',(-4.91784618449604,-3.89820090755666E-5,
8.13985943599073));
#24377=CARTESIAN_POINT('Ctrl Pts',(-4.91794771965564,-0.366944504507531,
8.16063286907332));
#24378=CARTESIAN_POINT('Ctrl Pts',(-4.78704988297834,-1.55224723866423,
8.22774630066009));
#24379=CARTESIAN_POINT('Ctrl Pts',(-3.84485907817879,-3.39191518737209,
8.34119973075105));
#24380=CARTESIAN_POINT('Ctrl Pts',(-1.75217326669541,-4.81849756800367,
8.48021972626356));
#24381=CARTESIAN_POINT('Ctrl Pts',(0.768055611337776,-5.06933137082908,
8.61923972177608));
#24382=CARTESIAN_POINT('Ctrl Pts',(3.10087331400732,-4.08321131707098,8.75825971728859));
#24383=CARTESIAN_POINT('Ctrl Pts',(4.67705529414154,-2.10075789774117,8.89727971280111));
#24384=CARTESIAN_POINT('Ctrl Pts',(5.11200164370846,0.394295782505144,9.03629970831364));
#24385=CARTESIAN_POINT('Ctrl Pts',(4.29958227865011,2.79313841377351,9.17531970382614));
#24386=CARTESIAN_POINT('Ctrl Pts',(2.43803345405823,4.51043488438445,9.31433969933867));
#24387=CARTESIAN_POINT('Ctrl Pts',(-0.0184133290357824,5.12715232060577,
9.45335969485118));
#24388=CARTESIAN_POINT('Ctrl Pts',(-2.47036712544234,4.49280716645095,9.5923796903637));
#24389=CARTESIAN_POINT('Ctrl Pts',(-4.09563866263082,2.97172585056254,9.71456732471902));
#24390=CARTESIAN_POINT('Ctrl Pts',(-4.63391221881488,1.72658135255771,9.79041496057018));
#24391=CARTESIAN_POINT('Ctrl Pts',(-4.76374494423105,1.22187361077196,9.81992259791717));
#24392=CARTESIAN_POINT('Origin',(0.,0.,-3.23514056400928));
#24393=CARTESIAN_POINT('',(-4.76403457734943,1.22194828381523,11.9150196727617));
#24394=CARTESIAN_POINT('',(-4.76403460025573,1.22194819451,11.5699436565254));
#24395=CARTESIAN_POINT('',(-4.76403458704967,1.22194824599672,-3.23514056400928));
#24396=CARTESIAN_POINT('Ctrl Pts',(-4.76403457734944,1.22194828381523,11.9150196727617));
#24397=CARTESIAN_POINT('Ctrl Pts',(-4.7244905674948,1.37611931770409,11.9060746123167));
#24398=CARTESIAN_POINT('Ctrl Pts',(-4.67747937823696,1.52830606459855,11.8971783354818));
#24399=CARTESIAN_POINT('Ctrl Pts',(-4.60398021861279,1.73081177289111,11.8850980175744));
#24400=CARTESIAN_POINT('Ctrl Pts',(-4.58389655736411,1.78332149431695,11.8819432183635));
#24401=CARTESIAN_POINT('Ctrl Pts',(-4.53123569457204,1.91423427479359,11.8740121046384));
#24402=CARTESIAN_POINT('Ctrl Pts',(-4.49752056546728,1.99215920738576,11.8692307682782));
#24403=CARTESIAN_POINT('Ctrl Pts',(-4.43562557068445,2.12562490050214,11.860918742926));
#24404=CARTESIAN_POINT('Ctrl Pts',(-4.40837645993941,2.18157564673165,11.8573957671926));
#24405=CARTESIAN_POINT('Ctrl Pts',(-4.33998825313583,2.31548095496047,11.8488642653837));
#24406=CARTESIAN_POINT('Ctrl Pts',(-4.29780126794634,2.392875691752,11.8438491696215));
#24407=CARTESIAN_POINT('Ctrl Pts',(-4.16496665594137,2.62171252167947,11.8287537188025));
#24408=CARTESIAN_POINT('Ctrl Pts',(-4.06822584951849,2.76945148479429,11.8186415546403));
#24409=CARTESIAN_POINT('Ctrl Pts',(-3.92877394929637,2.95929213479102,11.8051718261099));
#24410=CARTESIAN_POINT('Ctrl Pts',(-3.89293631351057,3.00628036340595,11.8017969201398));
#24411=CARTESIAN_POINT('Ctrl Pts',(-3.83346821661113,3.08140438852422,11.7963378933445));
#24412=CARTESIAN_POINT('Ctrl Pts',(-3.81035401818076,3.10994113480862,11.7942489473734));
#24413=CARTESIAN_POINT('Ctrl Pts',(-3.76373841711918,3.16619272151378,11.7901020555366));
#24414=CARTESIAN_POINT('Ctrl Pts',(-3.74024528769188,3.193911151498,11.7880445167892));
#24415=CARTESIAN_POINT('Ctrl Pts',(-3.67450264140116,3.26975753757497,11.7823730628181));
#24416=CARTESIAN_POINT('Ctrl Pts',(-3.63161692229767,3.31732462927569,11.7787683406521));
#24417=CARTESIAN_POINT('Ctrl Pts',(-3.47030442281233,3.48936749830215,11.7655185374147));
#24418=CARTESIAN_POINT('Ctrl Pts',(-3.3463083419578,3.60845108683862,11.7559215004634));
#24419=CARTESIAN_POINT('Ctrl Pts',(-3.15691230812849,3.77216879101442,11.7418745563128));
#24420=CARTESIAN_POINT('Ctrl Pts',(-3.09626749269752,3.82210415470926,11.7374611812107));
#24421=CARTESIAN_POINT('Ctrl Pts',(-2.97951976547875,3.91363226063336,11.7291039663979));
#24422=CARTESIAN_POINT('Ctrl Pts',(-2.92367608697119,3.95552442793255,11.7251635355641));
#24423=CARTESIAN_POINT('Ctrl Pts',(-2.81069941748672,4.03657605552683,11.7172941763925));
#24424=CARTESIAN_POINT('Ctrl Pts',(-2.75359303278346,4.07574566582514,11.7133662917186));
#24425=CARTESIAN_POINT('Ctrl Pts',(-2.57174881594076,4.1949070333938,11.7010037259994));
#24426=CARTESIAN_POINT('Ctrl Pts',(-2.44421331635595,4.27047506302232,11.6925395973986));
#24427=CARTESIAN_POINT('Ctrl Pts',(-2.21836016760169,4.390862739709,11.6778912930164));
#24428=CARTESIAN_POINT('Ctrl Pts',(-2.12161647647625,4.43841650664979,11.6717193035401));
#24429=CARTESIAN_POINT('Ctrl Pts',(-1.97897522108829,4.50280074747896,11.6627802138757));
#24430=CARTESIAN_POINT('Ctrl Pts',(-1.93426603593116,4.52218668965104,11.6600008187116));
#24431=CARTESIAN_POINT('Ctrl Pts',(-1.85392462957113,4.55561330381255,11.6550488779386));
#24432=CARTESIAN_POINT('Ctrl Pts',(-1.81840253394566,4.56990824545826,11.6528740641586));
#24433=CARTESIAN_POINT('Ctrl Pts',(-1.74951436905888,4.59670008705208,11.6486862822818));
#24434=CARTESIAN_POINT('Ctrl Pts',(-1.71617230597098,4.6092520939032,11.6466727668808));
#24435=CARTESIAN_POINT('Ctrl Pts',(-1.6072407171445,4.64891479299054,11.6401325628829));
#24436=CARTESIAN_POINT('Ctrl Pts',(-1.5311225431248,4.67453692599931,11.6356216086757));
#24437=CARTESIAN_POINT('Ctrl Pts',(-1.31035813489288,4.7428772149839,11.6226586322734));
#24438=CARTESIAN_POINT('Ctrl Pts',(-1.16433115678242,4.78082165324332,11.614228115212));
#24439=CARTESIAN_POINT('Ctrl Pts',(-0.93619494143326,4.82902765031254,11.6011399787944));
#24440=CARTESIAN_POINT('Ctrl Pts',(-0.855183149266913,4.84403040958246,
11.5965087092486));
#24441=CARTESIAN_POINT('Ctrl Pts',(-0.716853764278619,4.86606954711842,
11.5886111462403));
#24442=CARTESIAN_POINT('Ctrl Pts',(-0.659719143635766,4.87414430708519,
11.5853522521962));
#24443=CARTESIAN_POINT('Ctrl Pts',(-0.533470063845456,4.88972640514343,
11.5781522650352));
#24444=CARTESIAN_POINT('Ctrl Pts',(-0.464311872666966,4.8967774060811,11.5742088613727));
#24445=CARTESIAN_POINT('Ctrl Pts',(-0.177320180609664,4.91990295387174,
11.5578353192441));
#24446=CARTESIAN_POINT('Ctrl Pts',(0.0413123148125404,4.92292376582453,
11.5453276418417));
#24447=CARTESIAN_POINT('Ctrl Pts',(0.324647561748035,4.90795823283804,11.529096159069));
#24448=CARTESIAN_POINT('Ctrl Pts',(0.38980410966039,4.90321352849762,11.5253630825652));
#24449=CARTESIAN_POINT('Ctrl Pts',(0.493199458271979,4.89361021623511,11.5194435126087));
#24450=CARTESIAN_POINT('Ctrl Pts',(0.531508874276635,4.88959763234913,11.5172512075485));
#24451=CARTESIAN_POINT('Ctrl Pts',(0.590002087466434,4.88277540042378,11.5139066451562));
#24452=CARTESIAN_POINT('Ctrl Pts',(0.610221985699057,4.88028966447644,11.5127510116306));
#24453=CARTESIAN_POINT('Ctrl Pts',(0.63597067456829,4.87696172030142,11.5112802220076));
#24454=CARTESIAN_POINT('Ctrl Pts',(0.641514193277487,4.87623562393877,11.5109636201346));
#24455=CARTESIAN_POINT('Ctrl Pts',(0.652094264631559,4.87483148005618,11.5103594520851));
#24456=CARTESIAN_POINT('Ctrl Pts',(0.657131026752012,4.87415507577591,11.5100718664993));
#24457=CARTESIAN_POINT('Ctrl Pts',(0.668800865182612,4.8725694750713,11.5094056211974));
#24458=CARTESIAN_POINT('Ctrl Pts',(0.675433154306773,4.8716545383418,11.5090270289994));
#24459=CARTESIAN_POINT('Ctrl Pts',(0.740437120809957,4.86255182215224,11.5053168125755));
#24460=CARTESIAN_POINT('Ctrl Pts',(0.798659547235146,4.85332879616948,11.5019969126584));
#24461=CARTESIAN_POINT('Ctrl Pts',(1.031819681583,4.8120844523055,11.4886868846752));
#24462=CARTESIAN_POINT('Ctrl Pts',(1.20512849217673,4.77163227574737,11.4787548336228));
#24463=CARTESIAN_POINT('Ctrl Pts',(1.45202900179808,4.69969022421419,11.4643264813003));
#24464=CARTESIAN_POINT('Ctrl Pts',(1.52764374349726,4.67565833467376,11.4598695648807));
#24465=CARTESIAN_POINT('Ctrl Pts',(1.67144881163996,4.62609322113823,11.4513014330926));
#24466=CARTESIAN_POINT('Ctrl Pts',(1.73971860354431,4.60085412063183,11.4471931620788));
#24467=CARTESIAN_POINT('Ctrl Pts',(1.86566830250704,4.551086660596,11.4395277860474));
#24468=CARTESIAN_POINT('Ctrl Pts',(1.92348832946062,4.52695267769817,11.4359742686168));
#24469=CARTESIAN_POINT('Ctrl Pts',(2.09235392855577,4.45264904144882,11.4254870840906));
#24470=CARTESIAN_POINT('Ctrl Pts',(2.20201350561321,4.39945046082844,11.4185346720033));
#24471=CARTESIAN_POINT('Ctrl Pts',(2.44785964546724,4.26868783988599,11.4026082874923));
#24472=CARTESIAN_POINT('Ctrl Pts',(2.58254435506734,4.18857703776568,11.3936314581767));
#24473=CARTESIAN_POINT('Ctrl Pts',(2.73554869453851,4.08738007028649,11.3831648563363));
#24474=CARTESIAN_POINT('Ctrl Pts',(2.75779911215781,4.0724005901083,11.3816359254806));
#24475=CARTESIAN_POINT('Ctrl Pts',(2.81507242078053,4.03315825661325,11.3776832830877));
#24476=CARTESIAN_POINT('Ctrl Pts',(2.84990476634391,4.008620852083,11.3752625796703));
#24477=CARTESIAN_POINT('Ctrl Pts',(2.91778310031388,3.95947245216452,11.3705143891019));
#24478=CARTESIAN_POINT('Ctrl Pts',(2.95084739502148,3.93489263105812,11.3681867522965));
#24479=CARTESIAN_POINT('Ctrl Pts',(3.09876989239596,3.82201469904843,11.3576950358432));
#24480=CARTESIAN_POINT('Ctrl Pts',(3.21000253829246,3.7290824419785,11.349587046979));
#24481=CARTESIAN_POINT('Ctrl Pts',(3.43000513533123,3.52812761538154,11.3328943125461));
#24482=CARTESIAN_POINT('Ctrl Pts',(3.53815548318082,3.41966002863199,11.3243172389735));
#24483=CARTESIAN_POINT('Ctrl Pts',(3.68926887629328,3.25324741581559,11.3116516610141));
#24484=CARTESIAN_POINT('Ctrl Pts',(3.73630116590786,3.19912129059041,11.3076032248845));
#24485=CARTESIAN_POINT('Ctrl Pts',(3.82261214581019,3.09529146283879,11.2999590334696));
#24486=CARTESIAN_POINT('Ctrl Pts',(3.86214677326821,3.04581927373262,11.2963663719308));
#24487=CARTESIAN_POINT('Ctrl Pts',(3.99611483504287,2.87137289363798,11.2838600351471));
#24488=CARTESIAN_POINT('Ctrl Pts',(4.08552499571757,2.74266301803783,11.2749105775543));
#24489=CARTESIAN_POINT('Ctrl Pts',(4.22321707792243,2.52273625988765,11.260058370783));
#24490=CARTESIAN_POINT('Ctrl Pts',(4.27504645325742,2.43387318521027,11.2541690979252));
#24491=CARTESIAN_POINT('Ctrl Pts',(4.35477380844231,2.28676309161599,11.2446129607616));
#24492=CARTESIAN_POINT('Ctrl Pts',(4.38437846665882,2.22947661269929,11.2409377476548));
#24493=CARTESIAN_POINT('Ctrl Pts',(4.42910704578718,2.1385859134006,11.2351841247694));
#24494=CARTESIAN_POINT('Ctrl Pts',(4.44499415426079,2.10536598870881,11.2330974433948));
#24495=CARTESIAN_POINT('Ctrl Pts',(4.48387562960427,2.02166252704719,11.2278795893127));
#24496=CARTESIAN_POINT('Ctrl Pts',(4.50639177829064,1.97096252655223,11.2247541579613));
#24497=CARTESIAN_POINT('Ctrl Pts',(4.59889822442862,1.7527870313095,11.211428263852));
#24498=CARTESIAN_POINT('Ctrl Pts',(4.66044645631806,1.5818871130622,11.20129258381));
#24499=CARTESIAN_POINT('Ctrl Pts',(4.74342535230206,1.30416198834911,11.1850310731285));
#24500=CARTESIAN_POINT('Ctrl Pts',(4.7710037379179,1.19935210770026,11.1789413851554));
#24501=CARTESIAN_POINT('Ctrl Pts',(4.8102037499395,1.02749072581088,11.1689943713321));
#24502=CARTESIAN_POINT('Ctrl Pts',(4.82393581494914,0.960958076300132,11.1651530049468));
#24503=CARTESIAN_POINT('Ctrl Pts',(4.8509747700032,0.814711677053215,11.1567215550321));
#24504=CARTESIAN_POINT('Ctrl Pts',(4.86370399427486,0.734911267762847,11.1521287224107));
#24505=CARTESIAN_POINT('Ctrl Pts',(4.89263884105355,0.519525776076575,11.1397440487492));
#24506=CARTESIAN_POINT('Ctrl Pts',(4.90517415958433,0.383520178632083,11.1319346787192));
#24507=CARTESIAN_POINT('Ctrl Pts',(4.91841971519391,0.120290824076351,11.1168470553203));
#24508=CARTESIAN_POINT('Ctrl Pts',(4.91988585020692,-0.00678998865839053,
11.1095754556349));
#24509=CARTESIAN_POINT('Ctrl Pts',(4.91526297003377,-0.176674280481472,
11.0998993840201));
#24510=CARTESIAN_POINT('Ctrl Pts',(4.91353471336303,-0.219546221357184,
11.0974614982575));
#24511=CARTESIAN_POINT('Ctrl Pts',(4.90935805768069,-0.297722042531042,
11.0930255902301));
#24512=CARTESIAN_POINT('Ctrl Pts',(4.90708919011208,-0.333032523742834,
11.0910256249111));
#24513=CARTESIAN_POINT('Ctrl Pts',(4.89850406295982,-0.44735087531657,11.084557444096));
#24514=CARTESIAN_POINT('Ctrl Pts',(4.89065896730684,-0.526231849482437,
11.0801046133913));
#24515=CARTESIAN_POINT('Ctrl Pts',(4.86220525429989,-0.755827612450618,
11.067126451132));
#24516=CARTESIAN_POINT('Ctrl Pts',(4.83650816569251,-0.905816814448504,
11.0586239157759));
#24517=CARTESIAN_POINT('Ctrl Pts',(4.78224613211133,-1.15304369469664,11.0444170325476));
#24518=CARTESIAN_POINT('Ctrl Pts',(4.75755516543369,-1.25102211025607,11.038735926388));
#24519=CARTESIAN_POINT('Ctrl Pts',(4.71135253285143,-1.41311758381988,11.0292216053931));
#24520=CARTESIAN_POINT('Ctrl Pts',(4.69150458321728,-1.47767675950514,11.0254011956502));
#24521=CARTESIAN_POINT('Ctrl Pts',(4.64406846125941,-1.6213670055684,11.0168200298761));
#24522=CARTESIAN_POINT('Ctrl Pts',(4.61577476468717,-1.70024289988798,11.0120555059813));
#24523=CARTESIAN_POINT('Ctrl Pts',(4.52026759711774,-1.94650745030007,10.9969964375777));
#24524=CARTESIAN_POINT('Ctrl Pts',(4.44585535547024,-2.1109428269787,10.9866641765529));
#24525=CARTESIAN_POINT('Ctrl Pts',(4.34205925707084,-2.31034195054938,10.9738057362076));
#24526=CARTESIAN_POINT('Ctrl Pts',(4.32100347477446,-2.34948665008068,10.9712653168886));
#24527=CARTESIAN_POINT('Ctrl Pts',(4.27100898910727,-2.43948523756618,10.9653891660272));
#24528=CARTESIAN_POINT('Ctrl Pts',(4.24168745156505,-2.49011921183023,10.9620564843368));
#24529=CARTESIAN_POINT('Ctrl Pts',(4.19247985484302,-2.57170128544579,10.9566475643527));
#24530=CARTESIAN_POINT('Ctrl Pts',(4.17313798447193,-2.60297027159792,10.9545651666386));
#24531=CARTESIAN_POINT('Ctrl Pts',(4.12006834574893,-2.68665298707303,10.9489654428427));
#24532=CARTESIAN_POINT('Ctrl Pts',(4.08569187845162,-2.73864737811433,10.9454565087779));
#24533=CARTESIAN_POINT('Ctrl Pts',(3.95289981190829,-2.93142780059339,10.9323027001105));
#24534=CARTESIAN_POINT('Ctrl Pts',(3.8481198567885,-3.06767989436164,10.9227077378722));
#24535=CARTESIAN_POINT('Ctrl Pts',(3.68473539528482,-3.25856213738321,10.9086112330787));
#24536=CARTESIAN_POINT('Ctrl Pts',(3.63158786517697,-3.31769069646575,10.9041453211765));
#24537=CARTESIAN_POINT('Ctrl Pts',(3.52702876075377,-3.42849224601403,10.8955638468174));
#24538=CARTESIAN_POINT('Ctrl Pts',(3.4758557319513,-3.48036172382289,10.8914512583837));
#24539=CARTESIAN_POINT('Ctrl Pts',(3.37860040705878,-3.5746555178347,10.88378395934));
#24540=CARTESIAN_POINT('Ctrl Pts',(3.33282328770755,-3.61737357862419,10.8802328704035));
#24541=CARTESIAN_POINT('Ctrl Pts',(3.19601789929503,-3.74023516176712,10.869780737857));
#24542=CARTESIAN_POINT('Ctrl Pts',(3.10282724385609,-3.81789889429667,10.8628611758776));
#24543=CARTESIAN_POINT('Ctrl Pts',(2.85784266244473,-4.00716605671408,10.8451552767022));
#24544=CARTESIAN_POINT('Ctrl Pts',(2.70233291258256,-4.113640972227,10.8343565145569));
#24545=CARTESIAN_POINT('Ctrl Pts',(2.50595032105009,-4.23214857629367,10.8213030755625));
#24546=CARTESIAN_POINT('Ctrl Pts',(2.47053499452362,-4.25291964211589,10.8189713262023));
#24547=CARTESIAN_POINT('Ctrl Pts',(2.39770089289377,-4.29441997553446,10.8142233269937));
#24548=CARTESIAN_POINT('Ctrl Pts',(2.36026338174731,-4.31510942202753,10.8118077012397));
#24549=CARTESIAN_POINT('Ctrl Pts',(2.2149870038767,-4.39293853385853,10.8025184267318));
#24550=CARTESIAN_POINT('Ctrl Pts',(2.10530466229432,-4.44654576889522,10.7956816005542));
#24551=CARTESIAN_POINT('Ctrl Pts',(1.83672874274556,-4.56564467935578,10.7792217846967));
#24552=CARTESIAN_POINT('Ctrl Pts',(1.67617834340497,-4.62699784631384,10.7696072668492));
#24553=CARTESIAN_POINT('Ctrl Pts',(1.44449707614652,-4.70188859843657,10.7558881807876));
#24554=CARTESIAN_POINT('Ctrl Pts',(1.3757708247917,-4.72245515349356,10.7518379672928));
#24555=CARTESIAN_POINT('Ctrl Pts',(1.24559462598124,-4.75832785546681,10.7441933146452));
#24556=CARTESIAN_POINT('Ctrl Pts',(1.18425080404157,-4.77396479615308,10.7406019845797));
#24557=CARTESIAN_POINT('Ctrl Pts',(0.969320674726666,-4.82435423259623,
10.728049944093));
#24558=CARTESIAN_POINT('Ctrl Pts',(0.814382911509027,-4.85291207845091,
10.7190529601176));
#24559=CARTESIAN_POINT('Ctrl Pts',(0.556874565091969,-4.88769453288823,
10.7041793239958));
#24560=CARTESIAN_POINT('Ctrl Pts',(0.455000721114591,-4.8982284151843,10.6983162460567));
#24561=CARTESIAN_POINT('Ctrl Pts',(0.288713442575388,-4.91018994115737,
10.688794999373));
#24562=CARTESIAN_POINT('Ctrl Pts',(0.224469721518231,-4.91354599033202,
10.6851285386314));
#24563=CARTESIAN_POINT('Ctrl Pts',(0.12338053489275,-4.91684002280076,10.6793839206464));
#24564=CARTESIAN_POINT('Ctrl Pts',(0.0865704821135372,-4.91762586655673,
10.6772975462724));
#24565=CARTESIAN_POINT('Ctrl Pts',(-0.00581759150620979,-4.9185605415174,
10.6720741144194));
#24566=CARTESIAN_POINT('Ctrl Pts',(-0.06139579123391,-4.91818079250148,
10.6689428374763));
#24567=CARTESIAN_POINT('Ctrl Pts',(-0.298272090618897,-4.91254627786168,
10.6556190098578));
#24568=CARTESIAN_POINT('Ctrl Pts',(-0.479211637011975,-4.89820723622012,
10.6454909880087));
#24569=CARTESIAN_POINT('Ctrl Pts',(-0.738001355605268,-4.86321920916054,
10.6308402635684));
#24570=CARTESIAN_POINT('Ctrl Pts',(-0.816784611373685,-4.85060922136111,
10.6263586715613));
#24571=CARTESIAN_POINT('Ctrl Pts',(-0.966997531568134,-4.82280276826103,
10.617753933895));
#24572=CARTESIAN_POINT('Ctrl Pts',(-1.03846407717233,-4.80792085678421,
10.6136338140703));
#24573=CARTESIAN_POINT('Ctrl Pts',(-1.17873252734246,-4.7754384428343,10.605484583352));
#24574=CARTESIAN_POINT('Ctrl Pts',(-1.2475372695405,-4.75792741617651,10.6014570378615));
#24575=CARTESIAN_POINT('Ctrl Pts',(-1.48337123395864,-4.69243948446795,
10.5875370479908));
#24576=CARTESIAN_POINT('Ctrl Pts',(-1.64822055199276,-4.63710535859989,
10.5776008996415));
#24577=CARTESIAN_POINT('Ctrl Pts',(-1.92885623999235,-4.5260460572966,10.5603236948443));
#24578=CARTESIAN_POINT('Ctrl Pts',(-2.04603519113683,-4.47429546022447,
10.5529955488369));
#24579=CARTESIAN_POINT('Ctrl Pts',(-2.19786767535073,-4.40002722195041,
10.5433766098407));
#24580=CARTESIAN_POINT('Ctrl Pts',(-2.23444760751868,-4.38156431197187,
10.541049558764));
#24581=CARTESIAN_POINT('Ctrl Pts',(-2.30881995330094,-4.34285290155752,
10.5363007261591));
#24582=CARTESIAN_POINT('Ctrl Pts',(-2.34658692964247,-4.32256298282666,
10.5338796145433));
#24583=CARTESIAN_POINT('Ctrl Pts',(-2.56752679638586,-4.20011622683668,
10.5196424860244));
#24584=CARTESIAN_POINT('Ctrl Pts',(-2.74428038348977,-4.08681993558374,
10.5079431263938));
#24585=CARTESIAN_POINT('Ctrl Pts',(-2.97721662631528,-3.91556703001333,
10.4917225570818));
#24586=CARTESIAN_POINT('Ctrl Pts',(-3.04002299989872,-3.86700711280358,
10.4872629864342));
#24587=CARTESIAN_POINT('Ctrl Pts',(-3.15812504082092,-3.77103821131222,
10.4786909180222));
#24588=CARTESIAN_POINT('Ctrl Pts',(-3.2135971153543,-3.72387921164953,10.4745813733624));
#24589=CARTESIAN_POINT('Ctrl Pts',(-3.32116695431864,-3.62823569170451,
10.4664340651944));
#24590=CARTESIAN_POINT('Ctrl Pts',(-3.373300068129,-3.579817127543,10.4623977669007));
#24591=CARTESIAN_POINT('Ctrl Pts',(-3.56085064125861,-3.39789373459276,
10.447536985881));
#24592=CARTESIAN_POINT('Ctrl Pts',(-3.68954307446087,-3.25769999598795,
10.4366578778787));
#24593=CARTESIAN_POINT('Ctrl Pts',(-3.86011207468373,-3.0487781751467,10.4212202614789));
#24594=CARTESIAN_POINT('Ctrl Pts',(-3.90892776621562,-2.98593325997835,
10.4166687028537));
#24595=CARTESIAN_POINT('Ctrl Pts',(-3.97218966995185,-2.90027875892196,
10.4105929666145));
#24596=CARTESIAN_POINT('Ctrl Pts',(-3.98800381045214,-2.87849496639993,
10.409058531442));
#24597=CARTESIAN_POINT('Ctrl Pts',(-4.02844140873953,-2.82181971638326,
10.4050947068313));
#24598=CARTESIAN_POINT('Ctrl Pts',(-4.05279083571904,-2.78673522127334,
10.4026683283143));
#24599=CARTESIAN_POINT('Ctrl Pts',(-4.09967943092282,-2.71725999456605,
10.3979192632281));
#24600=CARTESIAN_POINT('Ctrl Pts',(-4.12225039424235,-2.68289490055045,
10.3955963812893));
#24601=CARTESIAN_POINT('Ctrl Pts',(-4.22313405006362,-2.52501671304363,
10.3850318629094));
#24602=CARTESIAN_POINT('Ctrl Pts',(-4.2963452864242,-2.39833041056331,10.3768475983938));
#24603=CARTESIAN_POINT('Ctrl Pts',(-4.43230731972234,-2.13679484452241,
10.3603341294461));
#24604=CARTESIAN_POINT('Ctrl Pts',(-4.49480701624097,-2.00198640737134,
10.3520128972845));
#24605=CARTESIAN_POINT('Ctrl Pts',(-4.57859906874176,-1.79746240085071,
10.3395619395194));
#24606=CARTESIAN_POINT('Ctrl Pts',(-4.60460035147513,-1.72976760222191,
10.3354685899248));
#24607=CARTESIAN_POINT('Ctrl Pts',(-4.65031093746895,-1.60241539284799,
10.3278094892047));
#24608=CARTESIAN_POINT('Ctrl Pts',(-4.67039235411379,-1.54290701494473,
10.3242472064281));
#24609=CARTESIAN_POINT('Ctrl Pts',(-4.72696197406515,-1.36403444774561,
10.3135823071809));
#24610=CARTESIAN_POINT('Ctrl Pts',(-4.7600518413802,-1.24364998951344,10.3064597189482));
#24611=CARTESIAN_POINT('Ctrl Pts',(-4.82352072643319,-0.972807890322336,
10.2905475216113));
#24612=CARTESIAN_POINT('Ctrl Pts',(-4.85151036882933,-0.821921397181798,
10.2817571973669));
#24613=CARTESIAN_POINT('Ctrl Pts',(-4.87603128716218,-0.643592335528763,
10.2714871104685));
#24614=CARTESIAN_POINT('Ctrl Pts',(-4.87944453888547,-0.617181666680833,
10.2699692291038));
#24615=CARTESIAN_POINT('Ctrl Pts',(-4.88773665754798,-0.548645342023595,
10.266039056218));
#24616=CARTESIAN_POINT('Ctrl Pts',(-4.89228552337227,-0.506481744906349,
10.2636297671248));
#24617=CARTESIAN_POINT('Ctrl Pts',(-4.8996543684323,-0.428767407664563,
10.2592070075046));
#24618=CARTESIAN_POINT('Ctrl Pts',(-4.90263407618996,-0.393234747177966,
10.2571917698034));
#24619=CARTESIAN_POINT('Ctrl Pts',(-4.91134152187288,-0.273818284863138,
10.2504369324928));
#24620=CARTESIAN_POINT('Ctrl Pts',(-4.91530472988333,-0.189820123855565,
10.245714926708));
#24621=CARTESIAN_POINT('Ctrl Pts',(-4.91786999539248,-0.0705540499605967,
10.2390244879591));
#24622=CARTESIAN_POINT('Ctrl Pts',(-4.91824910538206,-0.0353399245040969,
10.2370508736839));
#24623=CARTESIAN_POINT('Ctrl Pts',(-4.91825477204957,0.188114146117957,
10.2245303756001));
#24624=CARTESIAN_POINT('Ctrl Pts',(-4.90745272922607,0.376196211149348,
10.2139997504658));
#24625=CARTESIAN_POINT('Ctrl Pts',(-4.87779411797335,0.633494626895945,
10.1994022806027));
#24626=CARTESIAN_POINT('Ctrl Pts',(-4.86817435285551,0.703611554061901,
10.1954053538392));
#24627=CARTESIAN_POINT('Ctrl Pts',(-4.84551871392882,0.845874047925768,
10.1872476796469));
#24628=CARTESIAN_POINT('Ctrl Pts',(-4.83237603175276,0.917984874495307,
10.1830871854366));
#24629=CARTESIAN_POINT('Ctrl Pts',(-4.80164031852491,1.06758784650079,10.1743958106042));
#24630=CARTESIAN_POINT('Ctrl Pts',(-4.7837709210378,1.14500179752884,10.1698643878674));
#24631=CARTESIAN_POINT('Ctrl Pts',(-4.76403458704821,1.22194824600244,10.1653249229632));
#24632=CARTESIAN_POINT('',(-4.91847990603042,0.000102917318248914,9.88985943599074));
#24633=CARTESIAN_POINT('Ctrl Pts',(-4.76374494423105,1.22187361077196,9.81992259791717));
#24634=CARTESIAN_POINT('Ctrl Pts',(-4.83780683195621,0.933967707338634,
9.83675495907435));
#24635=CARTESIAN_POINT('Ctrl Pts',(-4.90451732111342,0.526079169820603,
9.86006723843221));
#24636=CARTESIAN_POINT('Ctrl Pts',(-4.91858617934998,0.114510461609331,
9.88337951779007));
#24637=CARTESIAN_POINT('Ctrl Pts',(-4.91847990603042,0.000102917318248914,
9.88985943599074));
#24638=CARTESIAN_POINT('Ctrl Pts',(-4.91824999876294,0.000110310282362309,
9.88999175175149));
#24639=CARTESIAN_POINT('Ctrl Pts',(-4.91825453779905,-0.202265332865951,
9.90134365005785));
#24640=CARTESIAN_POINT('Ctrl Pts',(-4.90576812281614,-0.404447615577542,
9.91264566029797));
#24641=CARTESIAN_POINT('Ctrl Pts',(-4.87289744207536,-0.669508609740337,
9.92767551990786));
#24642=CARTESIAN_POINT('Ctrl Pts',(-4.86366606934858,-0.733569026504508,
9.93132374267188));
#24643=CARTESIAN_POINT('Ctrl Pts',(-4.84285675483651,-0.860215179119433,
9.9385757723957));
#24644=CARTESIAN_POINT('Ctrl Pts',(-4.8313227855427,-0.92279560612633,9.94217860732116));
#24645=CARTESIAN_POINT('Ctrl Pts',(-4.79975029445116,-1.07722585063687,
9.95112425534546));
#24646=CARTESIAN_POINT('Ctrl Pts',(-4.77828661142264,-1.16875795308923,
9.95647522580859));
#24647=CARTESIAN_POINT('Ctrl Pts',(-4.69310277752286,-1.49026986293166,
9.97545931182569));
#24648=CARTESIAN_POINT('Ctrl Pts',(-4.61528813011351,-1.71616818121476,
9.98915931489593));
#24649=CARTESIAN_POINT('Ctrl Pts',(-4.5054544861416,-1.97273965245129,10.0050442085078));
#24650=CARTESIAN_POINT('Ctrl Pts',(-4.48906419700856,-2.00975733533123,
10.0073437676501));
#24651=CARTESIAN_POINT('Ctrl Pts',(-4.45467149444764,-2.08491322213457,
10.0120261686412));
#24652=CARTESIAN_POINT('Ctrl Pts',(-4.43663178725853,-2.12303078303241,
10.0144082690615));
#24653=CARTESIAN_POINT('Ctrl Pts',(-4.36071909717125,-2.27823847923328,
10.0241486493368));
#24654=CARTESIAN_POINT('Ctrl Pts',(-4.29868279070856,-2.39323392314751,
10.0314630305708));
#24655=CARTESIAN_POINT('Ctrl Pts',(-4.17292731400944,-2.60564207440643,
10.045291497569));
#24656=CARTESIAN_POINT('Ctrl Pts',(-4.11018565601439,-2.70352855235342,
10.0518004780026));
#24657=CARTESIAN_POINT('Ctrl Pts',(-3.99377011426145,-2.8717214089548,10.0632938232787));
#24658=CARTESIAN_POINT('Ctrl Pts',(-3.9415580828843,-2.94297522860048,10.0682666269201));
#24659=CARTESIAN_POINT('Ctrl Pts',(-3.88111108590409,-3.02097121720359,
10.0738406735553));
#24660=CARTESIAN_POINT('Ctrl Pts',(-3.87474005314753,-3.02913847097678,
10.0744259906496));
#24661=CARTESIAN_POINT('Ctrl Pts',(-3.8636049146689,-3.04332039020862,10.0754452394634));
#24662=CARTESIAN_POINT('Ctrl Pts',(-3.85885244369161,-3.04934415108085,
10.0758790756252));
#24663=CARTESIAN_POINT('Ctrl Pts',(-3.84398846546855,-3.0680938596647,10.0772323079428));
#24664=CARTESIAN_POINT('Ctrl Pts',(-3.83382797033259,-3.08078080141492,
10.078152097182));
#24665=CARTESIAN_POINT('Ctrl Pts',(-3.80124348828779,-3.12105670885988,
10.0810854215126));
#24666=CARTESIAN_POINT('Ctrl Pts',(-3.77858323860506,-3.14845290996315,
10.0831008577279));
#24667=CARTESIAN_POINT('Ctrl Pts',(-3.70427897573426,-3.23632893135392,
10.0896327616442));
#24668=CARTESIAN_POINT('Ctrl Pts',(-3.65146495520528,-3.29580205117316,
10.0941584660166));
#24669=CARTESIAN_POINT('Ctrl Pts',(-3.47466138870684,-3.48542925322802,
10.1089468804662));
#24670=CARTESIAN_POINT('Ctrl Pts',(-3.34497641622151,-3.61007213664745,
10.1192465150454));
#24671=CARTESIAN_POINT('Ctrl Pts',(-3.16356840353964,-3.76624138507315,
10.1329349241729));
#24672=CARTESIAN_POINT('Ctrl Pts',(-3.11767055738278,-3.80432248800459,
10.1363410267463));
#24673=CARTESIAN_POINT('Ctrl Pts',(-3.03500724895677,-3.87040673228028,
10.1423710496987));
#24674=CARTESIAN_POINT('Ctrl Pts',(-2.99851821360445,-3.89874413937888,
10.1449979812391));
#24675=CARTESIAN_POINT('Ctrl Pts',(-2.93061991554279,-3.9499568561393,10.1498199417267));
#24676=CARTESIAN_POINT('Ctrl Pts',(-2.89932872405437,-3.97298190691566,
10.1520166365853));
#24677=CARTESIAN_POINT('Ctrl Pts',(-2.80524481460706,-4.04050830936632,
10.1585516564845));
#24678=CARTESIAN_POINT('Ctrl Pts',(-2.74167669366778,-4.08390927848074,
10.1628763192199));
#24679=CARTESIAN_POINT('Ctrl Pts',(-2.54722356455809,-4.21008442479594,
10.1758816517908));
#24680=CARTESIAN_POINT('Ctrl Pts',(-2.41342358950316,-4.28818672538865,
10.1845367222657));
#24681=CARTESIAN_POINT('Ctrl Pts',(-2.20837238548503,-4.39523862388356,
10.197519351947));
#24682=CARTESIAN_POINT('Ctrl Pts',(-2.1397662946987,-4.42904405154125,10.201817743285));
#24683=CARTESIAN_POINT('Ctrl Pts',(-2.00970074295045,-4.48940574839535,
10.2098982595506));
#24684=CARTESIAN_POINT('Ctrl Pts',(-1.94843297421072,-4.51633367543774,
10.2136769085086));
#24685=CARTESIAN_POINT('Ctrl Pts',(-1.83631583245147,-4.56290435431281,
10.2205491921026));
#24686=CARTESIAN_POINT('Ctrl Pts',(-1.78565280542158,-4.58296803071386,
10.223639198762));
#24687=CARTESIAN_POINT('Ctrl Pts',(-1.62300713282659,-4.64427283973423,
10.2335150634465));
#24688=CARTESIAN_POINT('Ctrl Pts',(-1.50985359894462,-4.68228190871158,
10.2403208171079));
#24689=CARTESIAN_POINT('Ctrl Pts',(-1.2640779129937,-4.75500308051646,10.2549761087533));
#24690=CARTESIAN_POINT('Ctrl Pts',(-1.13115839664881,-4.788363804184,10.2628252112486));
#24691=CARTESIAN_POINT('Ctrl Pts',(-0.944139328405097,-4.82707988484651,
10.27374100434));
#24692=CARTESIAN_POINT('Ctrl Pts',(-0.891081463195211,-4.83715548450801,
10.276823444333));
#24693=CARTESIAN_POINT('Ctrl Pts',(-0.833708393484895,-4.84707449891059,
10.2801389545071));
#24694=CARTESIAN_POINT('Ctrl Pts',(-0.829547700261919,-4.84778830977509,
10.2803792953215));
#24695=CARTESIAN_POINT('Ctrl Pts',(-0.821788863246662,-4.84910913898542,
10.2808272932941));
#24696=CARTESIAN_POINT('Ctrl Pts',(-0.818190953500681,-4.84971751148334,
10.2810349624566));
#24697=CARTESIAN_POINT('Ctrl Pts',(-0.811411481920297,-4.85085609691034,
10.2814261260442));
#24698=CARTESIAN_POINT('Ctrl Pts',(-0.808230069436244,-4.85138718520848,
10.2816096284923));
#24699=CARTESIAN_POINT('Ctrl Pts',(-0.769567965604294,-4.85780214789214,
10.2838389129152));
#24700=CARTESIAN_POINT('Ctrl Pts',(-0.734024013661139,-4.86329984154134,
10.2858809559073));
#24701=CARTESIAN_POINT('Ctrl Pts',(-0.655752472887715,-4.87452869285757,
10.2903597697187));
#24702=CARTESIAN_POINT('Ctrl Pts',(-0.613003267108175,-4.88008896808139,
10.2927943215402));
#24703=CARTESIAN_POINT('Ctrl Pts',(-0.449352733539945,-4.89919022053326,
10.3020806558717));
#24704=CARTESIAN_POINT('Ctrl Pts',(-0.328036348878668,-4.90880590896388,
10.3088959458809));
#24705=CARTESIAN_POINT('Ctrl Pts',(-0.0867202898605512,-4.91894624303943,
10.3224272000269));
#24706=CARTESIAN_POINT('Ctrl Pts',(0.0331902186420285,-4.91959863579707,
10.3291386278264));
#24707=CARTESIAN_POINT('Ctrl Pts',(0.223430798605837,-4.91367748938978,
10.3398314847085));
#24708=CARTESIAN_POINT('Ctrl Pts',(0.29380181124556,-4.90997231768317,10.343796389656));
#24709=CARTESIAN_POINT('Ctrl Pts',(0.413754207979656,-4.90106853611265,
10.3505814568448));
#24710=CARTESIAN_POINT('Ctrl Pts',(0.46338079400134,-4.89662572868215,10.3533963369673));
#24711=CARTESIAN_POINT('Ctrl Pts',(0.575773910052433,-4.88483982553145,
10.3597926947478));
#24712=CARTESIAN_POINT('Ctrl Pts',(0.638483498859213,-4.87703951468597,
10.363376687218));
#24713=CARTESIAN_POINT('Ctrl Pts',(0.822879047335149,-4.85048548965462,
10.3739667208791));
#24714=CARTESIAN_POINT('Ctrl Pts',(0.944030009033002,-4.82836888850827,
10.3809919480464));
#24715=CARTESIAN_POINT('Ctrl Pts',(1.21197480950682,-4.76898347484425,10.3966897109753));
#24716=CARTESIAN_POINT('Ctrl Pts',(1.35813765337885,-4.72943428217761,10.4053632815479));
#24717=CARTESIAN_POINT('Ctrl Pts',(1.55766824051209,-4.665430379579,10.4173226980138));
#24718=CARTESIAN_POINT('Ctrl Pts',(1.61277289979163,-4.64666920102113,10.4206380535241));
#24719=CARTESIAN_POINT('Ctrl Pts',(1.70250237364478,-4.61433099151768,10.4260525627033));
#24720=CARTESIAN_POINT('Ctrl Pts',(1.73732873664354,-4.60133173431402,10.428157679161));
#24721=CARTESIAN_POINT('Ctrl Pts',(1.8324179779233,-4.56460530719894,10.4339173634115));
#24722=CARTESIAN_POINT('Ctrl Pts',(1.89236490333903,-4.54008066931748,10.4375626405245));
#24723=CARTESIAN_POINT('Ctrl Pts',(2.10478604920366,-4.44823950749769,10.4505636540001));
#24724=CARTESIAN_POINT('Ctrl Pts',(2.25430134203274,-4.37436680089563,10.4598749871749));
#24725=CARTESIAN_POINT('Ctrl Pts',(2.47002588358666,-4.25377855135578,10.4737394150351));
#24726=CARTESIAN_POINT('Ctrl Pts',(2.53929903148868,-4.21279243460511,10.4782603026381));
#24727=CARTESIAN_POINT('Ctrl Pts',(2.66995074349636,-4.13109731453634,10.4869395049358));
#24728=CARTESIAN_POINT('Ctrl Pts',(2.73148206263846,-4.09067324154082,10.4910947228509));
#24729=CARTESIAN_POINT('Ctrl Pts',(2.84412235436368,-4.01299727011866,10.4988391936614));
#24730=CARTESIAN_POINT('Ctrl Pts',(2.89546525157868,-3.97611115574936,10.5024247248457));
#24731=CARTESIAN_POINT('Ctrl Pts',(3.04502524018541,-3.86422985722543,10.5130421194359));
#24732=CARTESIAN_POINT('Ctrl Pts',(3.14114242521811,-3.78651221195174,10.5200933546459));
#24733=CARTESIAN_POINT('Ctrl Pts',(3.31919911108462,-3.63109087774792,10.5336121436552));
#24734=CARTESIAN_POINT('Ctrl Pts',(3.40159205396748,-3.55402239581124,10.5400728038296));
#24735=CARTESIAN_POINT('Ctrl Pts',(3.51051459684917,-3.44487810903477,10.5488907039106));
#24736=CARTESIAN_POINT('Ctrl Pts',(3.53939543843366,-3.41519807267941,10.5512569083409));
#24737=CARTESIAN_POINT('Ctrl Pts',(3.58657143394745,-3.36547536937454,10.555167859758));
#24738=CARTESIAN_POINT('Ctrl Pts',(3.60508166634326,-3.3456397448249,10.5567144196348));
#24739=CARTESIAN_POINT('Ctrl Pts',(3.65251935714299,-3.29395453875242,10.5607086133711));
#24740=CARTESIAN_POINT('Ctrl Pts',(3.68119487640266,-3.26187653002807,10.5631531902242));
#24741=CARTESIAN_POINT('Ctrl Pts',(3.73683420692254,-3.19796700492586,10.5679541535831));
#24742=CARTESIAN_POINT('Ctrl Pts',(3.76382129218169,-3.1661604798308,10.5703106636474));
#24743=CARTESIAN_POINT('Ctrl Pts',(3.87968173354682,-3.02603428565132,10.580562089299));
#24744=CARTESIAN_POINT('Ctrl Pts',(3.96430884837542,-2.91428723382091,10.5884051439988));
#24745=CARTESIAN_POINT('Ctrl Pts',(4.12900310119292,-2.67634044089566,10.6046165962002));
#24746=CARTESIAN_POINT('Ctrl Pts',(4.20832358431271,-2.54979934754399,10.6129778650592));
#24747=CARTESIAN_POINT('Ctrl Pts',(4.3183107628147,-2.35518411303656,10.6255671417043));
#24748=CARTESIAN_POINT('Ctrl Pts',(4.35338596557883,-2.28970096610409,10.6297591356357));
#24749=CARTESIAN_POINT('Ctrl Pts',(4.4191990525009,-2.15984880739337,10.6379978962051));
#24750=CARTESIAN_POINT('Ctrl Pts',(4.45004651880877,-2.09555552506387,10.6420427708163));
#24751=CARTESIAN_POINT('Ctrl Pts',(4.55754573015877,-1.85841498352604,10.65684946934));
#24752=CARTESIAN_POINT('Ctrl Pts',(4.62561103308836,-1.68185913012717,10.667665442533));
#24753=CARTESIAN_POINT('Ctrl Pts',(4.70825651854234,-1.42413495691479,10.6831578845587));
#24754=CARTESIAN_POINT('Ctrl Pts',(4.73123337113465,-1.34583458717698,10.6878257955512));
#24755=CARTESIAN_POINT('Ctrl Pts',(4.7593084965076,-1.24053055285824,10.6940446954036));
#24756=CARTESIAN_POINT('Ctrl Pts',(4.76614393052881,-1.2140038968994,10.6956063131025));
#24757=CARTESIAN_POINT('Ctrl Pts',(4.78320989659181,-1.14540843955969,10.6996310272541));
#24758=CARTESIAN_POINT('Ctrl Pts',(4.79310725979743,-1.10325892822445,10.7020910593208));
#24759=CARTESIAN_POINT('Ctrl Pts',(4.81139511192857,-1.02048063529088,10.7068944564715));
#24760=CARTESIAN_POINT('Ctrl Pts',(4.81983063366231,-0.979865480218618,
10.7092380709465));
#24761=CARTESIAN_POINT('Ctrl Pts',(4.85530129297295,-0.797526290371632,
10.7197120598799));
#24762=CARTESIAN_POINT('Ctrl Pts',(4.87660643751717,-0.654759059181606,
10.7277868246346));
#24763=CARTESIAN_POINT('Ctrl Pts',(4.90762437728455,-0.357987799616617,
10.7445028265277));
#24764=CARTESIAN_POINT('Ctrl Pts',(4.91643121418963,-0.204048114438797,
10.7531364784312));
#24765=CARTESIAN_POINT('Ctrl Pts',(4.91872977752001,0.0222614244504118,
10.7658886621944));
#24766=CARTESIAN_POINT('Ctrl Pts',(4.91787265926533,0.0944803843395491,
10.7699664682051));
#24767=CARTESIAN_POINT('Ctrl Pts',(4.91294825881184,0.239724842675599,10.7781946786687));
#24768=CARTESIAN_POINT('Ctrl Pts',(4.90884178898662,0.312731058954474,10.7823443341099));
#24769=CARTESIAN_POINT('Ctrl Pts',(4.89095861970288,0.540114485856213,10.795321887893));
#24770=CARTESIAN_POINT('Ctrl Pts',(4.87151250100734,0.693948696867291,10.8041810658028));
#24771=CARTESIAN_POINT('Ctrl Pts',(4.82807097118783,0.942549789180452,10.8186277644665));
#24772=CARTESIAN_POINT('Ctrl Pts',(4.80845895023498,1.03797498600089,10.8242040387665));
#24773=CARTESIAN_POINT('Ctrl Pts',(4.77157645023075,1.19380798303528,10.8333480793429));
#24774=CARTESIAN_POINT('Ctrl Pts',(4.75595943213808,1.25457934709739,10.8369235192983));
#24775=CARTESIAN_POINT('Ctrl Pts',(4.72925621012607,1.35081359723044,10.8425950121735));
#24776=CARTESIAN_POINT('Ctrl Pts',(4.71892367477497,1.38647793731166,10.8446986458065));
#24777=CARTESIAN_POINT('Ctrl Pts',(4.6908799310336,1.47932825172955,10.850181054024));
#24778=CARTESIAN_POINT('Ctrl Pts',(4.67252675702473,1.53631391227947,10.8535524730919));
#24779=CARTESIAN_POINT('Ctrl Pts',(4.595727323005,1.7606512537303,10.8668803902101));
#24780=CARTESIAN_POINT('Ctrl Pts',(4.52929271328128,1.92512612168283,10.8767800299091));
#24781=CARTESIAN_POINT('Ctrl Pts',(4.42037760088476,2.15772514150769,10.8911897421422));
#24782=CARTESIAN_POINT('Ctrl Pts',(4.38488688494591,2.22896450595652,10.89566067467));
#24783=CARTESIAN_POINT('Ctrl Pts',(4.31346974260532,2.36400459036397,10.9042659388265));
#24784=CARTESIAN_POINT('Ctrl Pts',(4.27781648405565,2.42792604654686,10.9083973407692));
#24785=CARTESIAN_POINT('Ctrl Pts',(4.20420579608915,2.55324162265044,10.9166242060046));
#24786=CARTESIAN_POINT('Ctrl Pts',(4.16629678512446,2.61464339716152,10.9207183542512));
#24787=CARTESIAN_POINT('Ctrl Pts',(4.0314524699551,2.82266962737561,10.9348200258843));
#24788=CARTESIAN_POINT('Ctrl Pts',(3.92801832070811,2.96491879635683,10.944871924919));
#24789=CARTESIAN_POINT('Ctrl Pts',(3.76228534837853,3.16890746826185,10.9599175803453));
#24790=CARTESIAN_POINT('Ctrl Pts',(3.7055909517281,3.23502108474885,10.9649008954576));
#24791=CARTESIAN_POINT('Ctrl Pts',(3.60764257044835,3.34328725541346,10.973234175767));
#24792=CARTESIAN_POINT('Ctrl Pts',(3.56733178262398,3.38626618270303,10.9765904807856));
#24793=CARTESIAN_POINT('Ctrl Pts',(3.50036134701894,3.45514595677104,10.9820445555773));
#24794=CARTESIAN_POINT('Ctrl Pts',(3.47416355286357,3.48148686456857,10.9841485424768));
#24795=CARTESIAN_POINT('Ctrl Pts',(3.40213225590443,3.5522888790613,10.9898558574977));
#24796=CARTESIAN_POINT('Ctrl Pts',(3.35572725656295,3.59615835251417,10.9934502588543));
#24797=CARTESIAN_POINT('Ctrl Pts',(3.18443279412108,3.75188986628587,11.0064569032389));
#24798=CARTESIAN_POINT('Ctrl Pts',(3.054699027469,3.85825142891675,11.0158231975103));
#24799=CARTESIAN_POINT('Ctrl Pts',(2.85489817870372,4.0056512170232,11.0297517671742));
#24800=CARTESIAN_POINT('Ctrl Pts',(2.78884201183321,4.05191872506418,11.0342814331302));
#24801=CARTESIAN_POINT('Ctrl Pts',(2.66030115574118,4.13731928837812,11.0429736360396));
#24802=CARTESIAN_POINT('Ctrl Pts',(2.5980154189877,4.17671268442128,11.0471330467238));
#24803=CARTESIAN_POINT('Ctrl Pts',(2.48073143703083,4.24725153423737,11.054879440332));
#24804=CARTESIAN_POINT('Ctrl Pts',(2.42597231029193,4.27876527716147,11.0584626682572));
#24805=CARTESIAN_POINT('Ctrl Pts',(2.26294008323037,4.36845393780467,11.0690399301249));
#24806=CARTESIAN_POINT('Ctrl Pts',(2.15307700464381,4.42363497717238,11.0760530643338));
#24807=CARTESIAN_POINT('Ctrl Pts',(1.90027975062149,4.53895724255116,11.0919458666604));
#24808=CARTESIAN_POINT('Ctrl Pts',(1.75633458444715,4.59657318369448,11.1008275454499));
#24809=CARTESIAN_POINT('Ctrl Pts',(1.5842273423605,4.65619431914305,11.1112206220899));
#24810=CARTESIAN_POINT('Ctrl Pts',(1.55847140683504,4.664878207896,11.112770032296));
#24811=CARTESIAN_POINT('Ctrl Pts',(1.49171422786373,4.68677151313694,11.1167700075476));
#24812=CARTESIAN_POINT('Ctrl Pts',(1.45060882249536,4.69965665296393,11.1192175141761));
#24813=CARTESIAN_POINT('Ctrl Pts',(1.36942029670281,4.72393979450627,11.1240188883864));
#24814=CARTESIAN_POINT('Ctrl Pts',(1.32935103975748,4.73537168474138,11.1263729035258));
#24815=CARTESIAN_POINT('Ctrl Pts',(1.1531158100579,4.78323895126235,11.1366694928455));
#24816=CARTESIAN_POINT('Ctrl Pts',(1.01556359198251,4.81432055593229,11.1445594611984));
#24817=CARTESIAN_POINT('Ctrl Pts',(0.722232394343318,4.86746954773252,11.1612596406445));
#24818=CARTESIAN_POINT('Ctrl Pts',(0.566346945827341,4.88805991800792,11.1700626349582));
#24819=CARTESIAN_POINT('Ctrl Pts',(0.337829955120684,4.90716434514307,11.1829836385668));
#24820=CARTESIAN_POINT('Ctrl Pts',(0.265791838299751,4.91159297257837,11.1870586830919));
#24821=CARTESIAN_POINT('Ctrl Pts',(0.120570360926469,4.91731630109065,11.1952873492919));
#24822=CARTESIAN_POINT('Ctrl Pts',(0.0474031804538423,4.91856580576221,
11.1994402529787));
#24823=CARTESIAN_POINT('Ctrl Pts',(-0.179580576738728,4.91737674624483,
11.212355479898));
#24824=CARTESIAN_POINT('Ctrl Pts',(-0.333273012809801,4.90935549042928,
11.2211484141319));
#24825=CARTESIAN_POINT('Ctrl Pts',(-0.624127961619186,4.88045303890979,
11.2378801883569));
#24826=CARTESIAN_POINT('Ctrl Pts',(-0.761282733999841,4.86094710743022,
11.2458087761434));
#24827=CARTESIAN_POINT('Ctrl Pts',(-0.938972266765734,4.82797050046806,
11.2560962169342));
#24828=CARTESIAN_POINT('Ctrl Pts',(-0.980411596812561,4.81972626069503,
11.2584963228103));
#24829=CARTESIAN_POINT('Ctrl Pts',(-1.0632584020914,4.8021314197854,11.263294195181));
#24830=CARTESIAN_POINT('Ctrl Pts',(-1.10466139503448,4.79277663379129,11.2656917110484));
#24831=CARTESIAN_POINT('Ctrl Pts',(-1.26962935098017,4.75325173665569,11.2752543594274));
#24832=CARTESIAN_POINT('Ctrl Pts',(-1.39212547193389,4.71882910417538,11.2823784165381));
#24833=CARTESIAN_POINT('Ctrl Pts',(-1.66524233102293,4.63051849031779,11.2984589052828));
#24834=CARTESIAN_POINT('Ctrl Pts',(-1.81484510571672,4.57395562108618,11.3074081005433));
#24835=CARTESIAN_POINT('Ctrl Pts',(-2.02964932608798,4.48054028778274,11.3205992118557));
#24836=CARTESIAN_POINT('Ctrl Pts',(-2.09718952433785,4.44932731821316,11.3247977771892));
#24837=CARTESIAN_POINT('Ctrl Pts',(-2.22795273842943,4.38525737579467,11.3330384974887));
#24838=CARTESIAN_POINT('Ctrl Pts',(-2.29122154266443,4.35253481793322,11.3370787008989));
#24839=CARTESIAN_POINT('Ctrl Pts',(-2.51875745094776,4.22851712706546,11.3518150964457));
#24840=CARTESIAN_POINT('Ctrl Pts',(-2.6784662105056,4.12920248928634,11.3625647005813));
#24841=CARTESIAN_POINT('Ctrl Pts',(-2.8995403429102,3.97349390074871,11.3780432902847));
#24842=CARTESIAN_POINT('Ctrl Pts',(-2.96577752162708,3.92430271529468,11.382763090999));
#24843=CARTESIAN_POINT('Ctrl Pts',(-3.05246605767687,3.85647437199492,11.3890443829365));
#24844=CARTESIAN_POINT('Ctrl Pts',(-3.07404252703777,3.83929761387948,11.3906166475733));
#24845=CARTESIAN_POINT('Ctrl Pts',(-3.12926427750536,3.79457230357593,11.3946629082647));
#24846=CARTESIAN_POINT('Ctrl Pts',(-3.16269093105303,3.76675722858857,11.3971338348229));
#24847=CARTESIAN_POINT('Ctrl Pts',(-3.22289155969841,3.71529655936839,11.4016214305927));
#24848=CARTESIAN_POINT('Ctrl Pts',(-3.24978513776297,3.69179564939717,11.4036401256431));
#24849=CARTESIAN_POINT('Ctrl Pts',(-3.40891153078802,3.54965703426927,11.4156782168946));
#24850=CARTESIAN_POINT('Ctrl Pts',(-3.53489477033996,3.42421720426567,11.4256054723474));
#24851=CARTESIAN_POINT('Ctrl Pts',(-3.72659081949087,3.21146750948727,11.4416530757779));
#24852=CARTESIAN_POINT('Ctrl Pts',(-3.79666723299588,3.12830949722579,11.44775029539));
#24853=CARTESIAN_POINT('Ctrl Pts',(-3.91163141969075,2.98232579894194,11.4582088664809));
#24854=CARTESIAN_POINT('Ctrl Pts',(-3.95790174523656,2.92064053281702,11.4625577215321));
#24855=CARTESIAN_POINT('Ctrl Pts',(-4.04280236092864,2.80173061052302,11.4708225852292));
#24856=CARTESIAN_POINT('Ctrl Pts',(-4.08171541248564,2.74473031292967,11.4747351791655));
#24857=CARTESIAN_POINT('Ctrl Pts',(-4.24019973466902,2.5017531242543,11.491222555841));
#24858=CARTESIAN_POINT('Ctrl Pts',(-4.34835849498808,2.30864422782793,11.5038790772387));
#24859=CARTESIAN_POINT('Ctrl Pts',(-4.46431287622472,2.06434684620571,11.5193521263622));
#24860=CARTESIAN_POINT('Ctrl Pts',(-4.48479716282679,2.01945829355026,11.5221733657652));
#24861=CARTESIAN_POINT('Ctrl Pts',(-4.52960675793347,1.91721821393183,11.528547176138));
#24862=CARTESIAN_POINT('Ctrl Pts',(-4.55352502141188,1.85969703877645,11.5320968015898));
#24863=CARTESIAN_POINT('Ctrl Pts',(-4.58863643128285,1.77051535587367,11.5375394989834));
#24864=CARTESIAN_POINT('Ctrl Pts',(-4.60060866329848,1.73916902174103,11.5394409567526));
#24865=CARTESIAN_POINT('Ctrl Pts',(-4.63105907937749,1.65692680613651,11.5443999699896));
#24866=CARTESIAN_POINT('Ctrl Pts',(-4.64901924671663,1.60584394675804,11.5474513627748));
#24867=CARTESIAN_POINT('Ctrl Pts',(-4.70267021721186,1.44479754551616,11.5569987762822));
#24868=CARTESIAN_POINT('Ctrl Pts',(-4.73532314901596,1.33388612096574,11.5634697876258));
#24869=CARTESIAN_POINT('Ctrl Pts',(-4.76403460025573,1.22194819451,11.5699436565254));
#24870=CARTESIAN_POINT('Origin',(0.,0.,-3.23514056400928));
#24871=CARTESIAN_POINT('',(-4.76403458702644,1.22194824608729,13.6654522135017));
#24872=CARTESIAN_POINT('',(-4.76403458795361,1.2219482424725,13.3199864568809));
#24873=CARTESIAN_POINT('',(-4.76403458704967,1.22194824599672,-3.23514056400928));
#24874=CARTESIAN_POINT('',(-4.91824987725453,7.97280680624427E-5,11.9853488470161));
#24875=CARTESIAN_POINT('Ctrl Pts',(-4.76403458702644,1.22194824608729,13.6654522135017));
#24876=CARTESIAN_POINT('Ctrl Pts',(-4.74749192885731,1.28644344539825,13.6616823062681));
#24877=CARTESIAN_POINT('Ctrl Pts',(-4.72964128849383,1.35059602842922,13.6579039764822));
#24878=CARTESIAN_POINT('Ctrl Pts',(-4.69919306528571,1.45200268377938,13.6518820798644));
#24879=CARTESIAN_POINT('Ctrl Pts',(-4.68744182409409,1.48950205793768,13.6496443602594));
#24880=CARTESIAN_POINT('Ctrl Pts',(-4.6434992367366,1.62405449416783,13.6415748319803));
#24881=CARTESIAN_POINT('Ctrl Pts',(-4.60873278690012,1.72023835122265,13.6357297656318));
#24882=CARTESIAN_POINT('Ctrl Pts',(-4.51090312638626,1.96658149489708,13.6205600978903));
#24883=CARTESIAN_POINT('Ctrl Pts',(-4.4433355123608,2.11481917321635,13.6112319379519));
#24884=CARTESIAN_POINT('Ctrl Pts',(-4.35198178344643,2.29144862239404,13.5999189376336));
#24885=CARTESIAN_POINT('Ctrl Pts',(-4.33507169156301,2.32328123492653,13.5978721073683));
#24886=CARTESIAN_POINT('Ctrl Pts',(-4.29781068710802,2.39160019774105,13.5934635259008));
#24887=CARTESIAN_POINT('Ctrl Pts',(-4.27734166387624,2.42801905918483,13.5911036349509));
#24888=CARTESIAN_POINT('Ctrl Pts',(-4.19183988926921,2.57570783617989,13.5814827167307));
#24889=CARTESIAN_POINT('Ctrl Pts',(-4.1229090377552,2.68466278955151,13.5742644366832));
#24890=CARTESIAN_POINT('Ctrl Pts',(-3.96478163196837,2.91412539207323,13.5586525581168));
#24891=CARTESIAN_POINT('Ctrl Pts',(-3.87419582731745,3.03351715070708,13.5502656369448));
#24892=CARTESIAN_POINT('Ctrl Pts',(-3.72929977990374,3.20739233238047,13.5375263805228));
#24893=CARTESIAN_POINT('Ctrl Pts',(-3.67893017903384,3.26504440652756,13.5332087834669));
#24894=CARTESIAN_POINT('Ctrl Pts',(-3.5806066494643,3.3724184769856,13.5249734352092));
#24895=CARTESIAN_POINT('Ctrl Pts',(-3.53291052514645,3.42235203319116,13.5210589017055));
#24896=CARTESIAN_POINT('Ctrl Pts',(-3.39356557741864,3.56221541485905,13.509838407936));
#24897=CARTESIAN_POINT('Ctrl Pts',(-3.29942630375064,3.6495823514634,13.502512343544));
#24898=CARTESIAN_POINT('Ctrl Pts',(-3.07913823650141,3.83852593340706,13.48591173545));
#24899=CARTESIAN_POINT('Ctrl Pts',(-2.95117266312915,3.93776000823887,13.4766355023107));
#24900=CARTESIAN_POINT('Ctrl Pts',(-2.77680396093254,4.05969673197617,13.4645030830632));
#24901=CARTESIAN_POINT('Ctrl Pts',(-2.73460852932787,4.08823850441202,13.4616044135441));
#24902=CARTESIAN_POINT('Ctrl Pts',(-2.66383415509746,4.13452554071916,13.4568069408464));
#24903=CARTESIAN_POINT('Ctrl Pts',(-2.63550333433586,4.15264205639874,13.4549035835955));
#24904=CARTESIAN_POINT('Ctrl Pts',(-2.54954786919555,4.20637343198898,13.4491772771134));
#24905=CARTESIAN_POINT('Ctrl Pts',(-2.49137087827708,4.24108984875067,13.4453657170116));
#24906=CARTESIAN_POINT('Ctrl Pts',(-2.33420051716059,4.33052901406561,13.4352096473382));
#24907=CARTESIAN_POINT('Ctrl Pts',(-2.23400566223528,4.38305743858922,13.4288803637976));
#24908=CARTESIAN_POINT('Ctrl Pts',(-2.00385315194508,4.49377408594179,13.4145700730411));
#24909=CARTESIAN_POINT('Ctrl Pts',(-1.8730018093682,4.54986774438346,13.4065905002074));
#24910=CARTESIAN_POINT('Ctrl Pts',(-1.68083098074824,4.62255114599162,13.3950083199938));
#24911=CARTESIAN_POINT('Ctrl Pts',(-1.62133349472312,4.64375381287817,13.3914411017798));
#24912=CARTESIAN_POINT('Ctrl Pts',(-1.49323006352035,4.68664291922593,13.3837931639312));
#24913=CARTESIAN_POINT('Ctrl Pts',(-1.4245232187835,4.70798166017359,13.379710884901));
#24914=CARTESIAN_POINT('Ctrl Pts',(-1.3167466528588,4.73887919072883,13.3733327120224));
#24915=CARTESIAN_POINT('Ctrl Pts',(-1.27798555888444,4.74947898389579,13.3710439471497));
#24916=CARTESIAN_POINT('Ctrl Pts',(-1.05082889829543,4.80861619264809,13.357658845234));
#24917=CARTESIAN_POINT('Ctrl Pts',(-0.859817066022298,4.84641565524565,
13.3465076622931));
#24918=CARTESIAN_POINT('Ctrl Pts',(-0.591882408590292,4.88309508910117,
13.331049422339));
#24919=CARTESIAN_POINT('Ctrl Pts',(-0.516464281686567,4.8916466849467,13.3267192545723));
#24920=CARTESIAN_POINT('Ctrl Pts',(-0.403585365849269,4.90180618895677,
13.3202781422558));
#24921=CARTESIAN_POINT('Ctrl Pts',(-0.366255447635611,4.90473669682284,
13.3181547095109));
#24922=CARTESIAN_POINT('Ctrl Pts',(-0.27795668760385,4.91065469496709,13.3131485036964));
#24923=CARTESIAN_POINT('Ctrl Pts',(-0.226967635776463,4.91327540780572,
13.3102697912342));
#24924=CARTESIAN_POINT('Ctrl Pts',(-0.140415964614919,4.91637371095197,
13.3053961082695));
#24925=CARTESIAN_POINT('Ctrl Pts',(-0.104872408415938,4.91726030488352,
13.3033983327393));
#24926=CARTESIAN_POINT('Ctrl Pts',(0.0610761293950787,4.91959956527556,
13.2940812658211));
#24927=CARTESIAN_POINT('Ctrl Pts',(0.191496361446129,4.9162505555357,13.2867872464725));
#24928=CARTESIAN_POINT('Ctrl Pts',(0.446495422878773,4.89953910154356,13.2724617233754));
#24929=CARTESIAN_POINT('Ctrl Pts',(0.571002444413348,4.88659361992049,13.2654368436197));
#24930=CARTESIAN_POINT('Ctrl Pts',(0.762398595181521,4.85927805447106,13.254532842792));
#24931=CARTESIAN_POINT('Ctrl Pts',(0.829710012372377,4.84823844164387,13.2506780241328));
#24932=CARTESIAN_POINT('Ctrl Pts',(0.972159468716897,4.82182207549118,13.2424690479482));
#24933=CARTESIAN_POINT('Ctrl Pts',(1.04721149933344,4.80608052825962,13.2381134273332));
#24934=CARTESIAN_POINT('Ctrl Pts',(1.22735954459834,4.76387570462259,13.2275765077693));
#24935=CARTESIAN_POINT('Ctrl Pts',(1.33200848961411,4.73568117491051,13.2213868525684));
#24936=CARTESIAN_POINT('Ctrl Pts',(1.6052055281734,4.65230361057469,13.2050433057154));
#24937=CARTESIAN_POINT('Ctrl Pts',(1.77185022306973,4.59142258506078,13.1948811535334));
#24938=CARTESIAN_POINT('Ctrl Pts',(1.96747457287629,4.50771411765555,13.1827782696507));
#24939=CARTESIAN_POINT('Ctrl Pts',(1.99995312058972,4.49339852621279,13.1807631771229));
#24940=CARTESIAN_POINT('Ctrl Pts',(2.07115662570032,4.46108915328266,13.1763343761193));
#24941=CARTESIAN_POINT('Ctrl Pts',(2.10980805224177,4.44294004476959,13.173922868979));
#24942=CARTESIAN_POINT('Ctrl Pts',(2.17242820236224,4.41253476556097,13.1699992674948));
#24943=CARTESIAN_POINT('Ctrl Pts',(2.19654107435516,4.40058117421988,13.1684843416449));
#24944=CARTESIAN_POINT('Ctrl Pts',(2.29152426996722,4.3525194823362,13.1624980852108));
#24945=CARTESIAN_POINT('Ctrl Pts',(2.36161269585703,4.31489222868149,13.1580389499542));
#24946=CARTESIAN_POINT('Ctrl Pts',(2.59173293086761,4.18406403501136,13.1432059270431));
#24947=CARTESIAN_POINT('Ctrl Pts',(2.74740947404174,4.08352931826245,13.1328484107231));
#24948=CARTESIAN_POINT('Ctrl Pts',(2.95545620293753,3.93188076414463,13.118344545202));
#24949=CARTESIAN_POINT('Ctrl Pts',(3.01292118538963,3.88802179553499,13.1142637510599));
#24950=CARTESIAN_POINT('Ctrl Pts',(3.12533421853084,3.7982356374216,13.106119618944));
#24951=CARTESIAN_POINT('Ctrl Pts',(3.18028764362498,3.75234303859302,13.1020574643793));
#24952=CARTESIAN_POINT('Ctrl Pts',(3.35099333965024,3.60333905172189,13.0891685015358));
#24953=CARTESIAN_POINT('Ctrl Pts',(3.46288227067792,3.4959482254365,13.0803096231098));
#24954=CARTESIAN_POINT('Ctrl Pts',(3.66800678810294,3.2795438821689,13.063241615592));
#24955=CARTESIAN_POINT('Ctrl Pts',(3.76191818507742,3.17138047154007,13.0550430351599));
#24956=CARTESIAN_POINT('Ctrl Pts',(3.87666621726056,3.02693701312246,13.0445438587821));
#24957=CARTESIAN_POINT('Ctrl Pts',(3.901946908681,2.99427771260203,13.0421981252545));
#24958=CARTESIAN_POINT('Ctrl Pts',(3.95239700468902,2.92737875823166,13.0374520257537));
#24959=CARTESIAN_POINT('Ctrl Pts',(3.97754005276687,2.89312351305757,13.0350521510918));
#24960=CARTESIAN_POINT('Ctrl Pts',(4.01776101058695,2.83681035728992,13.0311514458086));
#24961=CARTESIAN_POINT('Ctrl Pts',(4.03310850865928,2.8149480118026,13.0296477866961));
#24962=CARTESIAN_POINT('Ctrl Pts',(4.1354899661822,2.66655051408254,13.0195087346167));
#24963=CARTESIAN_POINT('Ctrl Pts',(4.21673445644975,2.53612303329006,13.0109235433458));
#24964=CARTESIAN_POINT('Ctrl Pts',(4.35249344802412,2.29356823095315,12.9953430469677));
#24965=CARTESIAN_POINT('Ctrl Pts',(4.40910351243269,2.18276432951868,12.9883619678482));
#24966=CARTESIAN_POINT('Ctrl Pts',(4.48787769374794,2.01297772182069,12.9778091183968));
#24967=CARTESIAN_POINT('Ctrl Pts',(4.51321019853709,1.95552016111104,12.9742621889819));
#24968=CARTESIAN_POINT('Ctrl Pts',(4.56541863483289,1.83068184306081,12.9666006158049));
#24969=CARTESIAN_POINT('Ctrl Pts',(4.59191801686957,1.76315968731107,12.9624841529034));
#24970=CARTESIAN_POINT('Ctrl Pts',(4.6440764643316,1.62109468921444,12.9538735269379));
#24971=CARTESIAN_POINT('Ctrl Pts',(4.66945625275408,1.54647092762302,12.9493787472607));
#24972=CARTESIAN_POINT('Ctrl Pts',(4.74502419619914,1.30542562236449,12.9349452274976));
#24973=CARTESIAN_POINT('Ctrl Pts',(4.78818893692642,1.13694206772998,12.9249808123392));
#24974=CARTESIAN_POINT('Ctrl Pts',(4.83458759626187,0.905443052705651,12.9114995120545));
#24975=CARTESIAN_POINT('Ctrl Pts',(4.84566905186505,0.844130275520592,12.9079491985528));
#24976=CARTESIAN_POINT('Ctrl Pts',(4.8614332198621,0.746325563740343,12.9023232632492));
#24977=CARTESIAN_POINT('Ctrl Pts',(4.86687647517669,0.70996353186131,12.9002401439926));
#24978=CARTESIAN_POINT('Ctrl Pts',(4.87992672603027,0.615567730797254,12.8948534607081));
#24979=CARTESIAN_POINT('Ctrl Pts',(4.88690645051748,0.557453090019006,12.8915568186201));
#24980=CARTESIAN_POINT('Ctrl Pts',(4.89736161935942,0.454983635883838,12.8857665460685));
#24981=CARTESIAN_POINT('Ctrl Pts',(4.90127558706457,0.410680641534235,12.8832704705766));
#24982=CARTESIAN_POINT('Ctrl Pts',(4.91802246773135,0.186466304784413,12.8706612384507));
#24983=CARTESIAN_POINT('Ctrl Pts',(4.92155243729071,0.00599995829114273,
12.860582500595));
#24984=CARTESIAN_POINT('Ctrl Pts',(4.91219488473717,-0.257951611378148,
12.8457330282399));
#24985=CARTESIAN_POINT('Ctrl Pts',(4.90709006754119,-0.341561794685724,
12.8410142512721));
#24986=CARTESIAN_POINT('Ctrl Pts',(4.89401672904728,-0.492285135535927,
12.8324639582707));
#24987=CARTESIAN_POINT('Ctrl Pts',(4.88679532867845,-0.559442292800807,
12.8286385052027));
#24988=CARTESIAN_POINT('Ctrl Pts',(4.86531875422939,-0.726686941079942,
12.8190644922807));
#24989=CARTESIAN_POINT('Ctrl Pts',(4.84935660262994,-0.826523222251747,
12.8133064074555));
#24990=CARTESIAN_POINT('Ctrl Pts',(4.80165815682912,-1.07538939964532,12.7988339658511));
#24991=CARTESIAN_POINT('Ctrl Pts',(4.76605277958366,-1.22357019038186,12.7901065841066));
#24992=CARTESIAN_POINT('Ctrl Pts',(4.70161958018936,-1.4457526491025,12.7768774393197));
#24993=CARTESIAN_POINT('Ctrl Pts',(4.67778410044732,-1.52110601934953,12.7723656677487));
#24994=CARTESIAN_POINT('Ctrl Pts',(4.64067093286858,-1.6292962990354,12.7658602060999));
#24995=CARTESIAN_POINT('Ctrl Pts',(4.62883825429193,-1.66261528688749,12.7638529339004));
#24996=CARTESIAN_POINT('Ctrl Pts',(4.60183688074375,-1.73612367217808,12.7594175770459));
#24997=CARTESIAN_POINT('Ctrl Pts',(4.58649884049838,-1.77624787853159,12.7569917875394));
#24998=CARTESIAN_POINT('Ctrl Pts',(4.49952794048236,-1.995122337446,12.7437176441949));
#24999=CARTESIAN_POINT('Ctrl Pts',(4.41796940105603,-2.16974947306241,12.7329671455295));
#25000=CARTESIAN_POINT('Ctrl Pts',(4.26993253241486,-2.44355201436016,12.7155139950434));
#25001=CARTESIAN_POINT('Ctrl Pts',(4.2097228480303,-2.54587967292014,12.7088480930045));
#25002=CARTESIAN_POINT('Ctrl Pts',(4.10936563073724,-2.70312812961401,12.6983253542854));
#25003=CARTESIAN_POINT('Ctrl Pts',(4.07168048033703,-2.75956618021655,12.6944895072439));
#25004=CARTESIAN_POINT('Ctrl Pts',(3.98832199442357,-2.87897891029431,12.6862366513769));
#25005=CARTESIAN_POINT('Ctrl Pts',(3.94229796858069,-2.94168632331191,12.6818177618071));
#25006=CARTESIAN_POINT('Ctrl Pts',(3.83999919904504,-3.07435278892578,12.6722754356151));
#25007=CARTESIAN_POINT('Ctrl Pts',(3.78325664268296,-3.14391600934878,12.6671500171384));
#25008=CARTESIAN_POINT('Ctrl Pts',(3.61833640537448,-3.33516463603254,12.6527060716879));
#25009=CARTESIAN_POINT('Ctrl Pts',(3.50597492077443,-3.45308871233971,12.6433751181095));
#25010=CARTESIAN_POINT('Ctrl Pts',(3.35064211424312,-3.60069889886854,12.631154725642));
#25011=CARTESIAN_POINT('Ctrl Pts',(3.31275596473747,-3.63558566699827,12.6282236560214));
#25012=CARTESIAN_POINT('Ctrl Pts',(3.24658032947463,-3.6946288219731,12.623191489593));
#25013=CARTESIAN_POINT('Ctrl Pts',(3.2185522060674,-3.71907081052029,12.621086705534));
#25014=CARTESIAN_POINT('Ctrl Pts',(3.13554260286828,-3.78981825227685,12.6149268125057));
#25015=CARTESIAN_POINT('Ctrl Pts',(3.07981988626181,-3.83523916666179,12.6108839731272));
#25016=CARTESIAN_POINT('Ctrl Pts',(2.92244037331296,-3.95788043731194,12.5996823954742));
#25017=CARTESIAN_POINT('Ctrl Pts',(2.81874315776881,-4.03238918151887,12.5925427107956));
#25018=CARTESIAN_POINT('Ctrl Pts',(2.60885187264373,-4.1711440777764,12.5784392148485));
#25019=CARTESIAN_POINT('Ctrl Pts',(2.50289203306217,-4.23557339000261,12.5714813480575));
#25020=CARTESIAN_POINT('Ctrl Pts',(2.33978305097612,-4.32649265170639,12.5609528563646));
#25021=CARTESIAN_POINT('Ctrl Pts',(2.28437404045716,-4.35600258589951,12.5574068526786));
#25022=CARTESIAN_POINT('Ctrl Pts',(2.16373385446374,-4.41731857350783,12.5497445250737));
#25023=CARTESIAN_POINT('Ctrl Pts',(2.09833290915234,-4.44875785021114,12.5456263695164));
#25024=CARTESIAN_POINT('Ctrl Pts',(1.96043738859697,-4.51132896922765,12.5370105387455));
#25025=CARTESIAN_POINT('Ctrl Pts',(1.88784079521458,-4.5421867842771,12.5325122395333));
#25026=CARTESIAN_POINT('Ctrl Pts',(1.65255721292173,-4.63558066923525,12.5180484002647));
#25027=CARTESIAN_POINT('Ctrl Pts',(1.48727781368162,-4.69122138437479,12.5080570534598));
#25028=CARTESIAN_POINT('Ctrl Pts',(1.25976308759379,-4.75457797612843,12.4945723732099));
#25029=CARTESIAN_POINT('Ctrl Pts',(1.19982256219548,-4.77005667889414,12.4910449594774));
#25030=CARTESIAN_POINT('Ctrl Pts',(1.10435164529871,-4.79279707934915,12.4854717228737));
#25031=CARTESIAN_POINT('Ctrl Pts',(1.0690061064841,-4.8008043477951,12.4834183982528));
#25032=CARTESIAN_POINT('Ctrl Pts',(1.03206036881866,-4.80874587155152,12.4812821856536));
#25033=CARTESIAN_POINT('Ctrl Pts',(1.03054575847516,-4.80907069003373,12.4811946274699));
#25034=CARTESIAN_POINT('Ctrl Pts',(1.0275309130035,-4.80971575444775,12.4810203756845));
#25035=CARTESIAN_POINT('Ctrl Pts',(1.02603068100881,-4.81003601414708,12.4809336819387));
#25036=CARTESIAN_POINT('Ctrl Pts',(1.02302498124307,-4.81067618106065,12.4807600247561));
#25037=CARTESIAN_POINT('Ctrl Pts',(1.02151951264981,-4.81099608361409,12.4806730613798));
#25038=CARTESIAN_POINT('Ctrl Pts',(1.01848616054647,-4.81163916375126,12.4804978728357));
#25039=CARTESIAN_POINT('Ctrl Pts',(1.01695827276544,-4.81196232038722,12.4804096479059));
#25040=CARTESIAN_POINT('Ctrl Pts',(1.01386422637074,-4.81261518870416,12.4802310220451));
#25041=CARTESIAN_POINT('Ctrl Pts',(1.01229806019504,-4.81294486373869,12.4801406215189));
#25042=CARTESIAN_POINT('Ctrl Pts',(1.00911215003705,-4.81361386796449,12.4799567633444));
#25043=CARTESIAN_POINT('Ctrl Pts',(1.0074923951227,-4.81395314424492,12.4798633062699));
#25044=CARTESIAN_POINT('Ctrl Pts',(1.00418396726489,-4.81464438955609,12.4796724533781));
#25045=CARTESIAN_POINT('Ctrl Pts',(1.00249527973445,-4.81499628786041,12.4795750583155));
#25046=CARTESIAN_POINT('Ctrl Pts',(0.999033141422483,-4.81571584763252,
12.4793754202129));
#25047=CARTESIAN_POINT('Ctrl Pts',(0.997259671934652,-4.81608341804172,
12.4792731781301));
#25048=CARTESIAN_POINT('Ctrl Pts',(0.993611208404693,-4.81683749923351,
12.4790628856171));
#25049=CARTESIAN_POINT('Ctrl Pts',(0.991736190854317,-4.81722389507111,
12.4789548363763));
#25050=CARTESIAN_POINT('Ctrl Pts',(0.987866570630245,-4.81801897532477,
12.4787318962226));
#25051=CARTESIAN_POINT('Ctrl Pts',(0.985871938743684,-4.81842751614692,
12.4786170067716));
#25052=CARTESIAN_POINT('Ctrl Pts',(0.983160138138206,-4.81898119322629,
12.4784608453657));
#25053=CARTESIAN_POINT('Ctrl Pts',(0.982443190469378,-4.81912740808886,
12.4784195627736));
#25054=CARTESIAN_POINT('Ctrl Pts',(0.980876210056647,-4.81944661507176,
12.4783293419559));
#25055=CARTESIAN_POINT('Ctrl Pts',(0.980026164088165,-4.81961954231709,
12.4782804043685));
#25056=CARTESIAN_POINT('Ctrl Pts',(0.97816224901603,-4.81999821030666,12.4781731083966));
#25057=CARTESIAN_POINT('Ctrl Pts',(0.977148360607587,-4.82020385607519,
12.4781147509397));
#25058=CARTESIAN_POINT('Ctrl Pts',(0.97491720136122,-4.82065566653902,12.4779863447503));
#25059=CARTESIAN_POINT('Ctrl Pts',(0.973699901940516,-4.82090169012053,
12.4779162973843));
#25060=CARTESIAN_POINT('Ctrl Pts',(0.971010559042593,-4.82144416243935,
12.4777615654374));
#25061=CARTESIAN_POINT('Ctrl Pts',(0.969538472613948,-4.82174039817744,
12.4776768828985));
#25062=CARTESIAN_POINT('Ctrl Pts',(0.966272314896894,-4.8223961081474,12.4774890269009));
#25063=CARTESIAN_POINT('Ctrl Pts',(0.964478178039828,-4.82275525550491,
12.4773858565377));
#25064=CARTESIAN_POINT('Ctrl Pts',(0.960479238258706,-4.82355343593039,
12.4771559471917));
#25065=CARTESIAN_POINT('Ctrl Pts',(0.958274333638604,-4.8239919587307,12.4770292129689));
#25066=CARTESIAN_POINT('Ctrl Pts',(0.953336206927131,-4.82497055962427,
12.4767454471985));
#25067=CARTESIAN_POINT('Ctrl Pts',(0.950602824633124,-4.82550982741635,
12.476588423069));
#25068=CARTESIAN_POINT('Ctrl Pts',(0.944451063516573,-4.82671807587247,
12.4762351294651));
#25069=CARTESIAN_POINT('Ctrl Pts',(0.941032428649438,-4.82738574837216,
12.4760388716879));
#25070=CARTESIAN_POINT('Ctrl Pts',(0.933301291381195,-4.82888714454379,
12.4755952031977));
#25071=CARTESIAN_POINT('Ctrl Pts',(0.928988374639183,-4.82971872421858,
12.4753478110885));
#25072=CARTESIAN_POINT('Ctrl Pts',(0.865270786774493,-4.84191569676271,
12.4716945667584));
#25073=CARTESIAN_POINT('Ctrl Pts',(0.805662146167855,-4.85219020093511,
12.4682979459368));
#25074=CARTESIAN_POINT('Ctrl Pts',(0.559009464096017,-4.89003412043751,
12.4543003172029));
#25075=CARTESIAN_POINT('Ctrl Pts',(0.370643022856385,-4.90790676089643,
12.4437392596268));
#25076=CARTESIAN_POINT('Ctrl Pts',(0.100342408565345,-4.91790049558818,
12.4285293816744));
#25077=CARTESIAN_POINT('Ctrl Pts',(0.0189066834802143,-4.91888770038409,
12.4239408807574));
#25078=CARTESIAN_POINT('Ctrl Pts',(-0.0876736691723155,-4.91753286074616,
12.4179166280193));
#25079=CARTESIAN_POINT('Ctrl Pts',(-0.112829152108404,-4.91702000038844,
12.4164933998463));
#25080=CARTESIAN_POINT('Ctrl Pts',(-0.180391203396617,-4.91512382793135,
12.4126667597681));
#25081=CARTESIAN_POINT('Ctrl Pts',(-0.222785502628914,-4.91338476168384,
12.4102611712456));
#25082=CARTESIAN_POINT('Ctrl Pts',(-0.332222403201716,-4.90747622692522,
12.4040380914457));
#25083=CARTESIAN_POINT('Ctrl Pts',(-0.39921132557982,-4.90248149802811,
12.4002158304595));
#25084=CARTESIAN_POINT('Ctrl Pts',(-0.570674863714475,-4.88615935420432,
12.390394935081));
#25085=CARTESIAN_POINT('Ctrl Pts',(-0.674926651024151,-4.87285304146652,
12.3843874288826));
#25086=CARTESIAN_POINT('Ctrl Pts',(-0.916141303239926,-4.83417542507247,
12.3704048357757));
#25087=CARTESIAN_POINT('Ctrl Pts',(-1.05261408047837,-4.8063053365427,12.3624303166353));
#25088=CARTESIAN_POINT('Ctrl Pts',(-1.2334267554739,-4.76130863294554,12.3518126371884));
#25089=CARTESIAN_POINT('Ctrl Pts',(-1.27896721060993,-4.74927830348323,
12.3491341119404));
#25090=CARTESIAN_POINT('Ctrl Pts',(-1.35785592567837,-4.72722141786824,
12.3444894413808));
#25091=CARTESIAN_POINT('Ctrl Pts',(-1.3912831187497,-4.7174915317498,12.3425201818188));
#25092=CARTESIAN_POINT('Ctrl Pts',(-1.42821352579923,-4.70631526832061,
12.3403417923546));
#25093=CARTESIAN_POINT('Ctrl Pts',(-1.43182125024315,-4.70521893087799,
12.3401289559409));
#25094=CARTESIAN_POINT('Ctrl Pts',(-1.43666410257372,-4.70374116952377,
12.3398432108308));
#25095=CARTESIAN_POINT('Ctrl Pts',(-1.43790034396326,-4.7033634065771,12.33977026455));
#25096=CARTESIAN_POINT('Ctrl Pts',(-1.44077493814102,-4.70248376671346,
12.3396006359168));
#25097=CARTESIAN_POINT('Ctrl Pts',(-1.44241317806771,-4.70198152083979,
12.3395039573316));
#25098=CARTESIAN_POINT('Ctrl Pts',(-1.4462810280311,-4.70079351725624,12.339275684959));
#25099=CARTESIAN_POINT('Ctrl Pts',(-1.44851041371257,-4.70010702913194,
12.3391440985326));
#25100=CARTESIAN_POINT('Ctrl Pts',(-1.45386623397875,-4.69845365473027,
12.3388279468481));
#25101=CARTESIAN_POINT('Ctrl Pts',(-1.45699219436929,-4.69748523334786,
12.3386433967852));
#25102=CARTESIAN_POINT('Ctrl Pts',(-1.46464670555598,-4.6951054929536,12.3381914239928));
#25103=CARTESIAN_POINT('Ctrl Pts',(-1.46917418737869,-4.69369074069278,
12.3379240343906));
#25104=CARTESIAN_POINT('Ctrl Pts',(-1.48047711262466,-4.69014083443975,
12.3372563401194));
#25105=CARTESIAN_POINT('Ctrl Pts',(-1.48724999382016,-4.68799754521871,
12.336856111036));
#25106=CARTESIAN_POINT('Ctrl Pts',(-1.50443382134391,-4.68251870821666,
12.3358402907139));
#25107=CARTESIAN_POINT('Ctrl Pts',(-1.51483834221053,-4.67916310607729,
12.3352248752226));
#25108=CARTESIAN_POINT('Ctrl Pts',(-1.5916787829674,-4.65409784462052,12.3306769121839));
#25109=CARTESIAN_POINT('Ctrl Pts',(-1.65765679325125,-4.63100876370727,
12.3267554908878));
#25110=CARTESIAN_POINT('Ctrl Pts',(-1.91862173391321,-4.53339191868338,
12.3111365036432));
#25111=CARTESIAN_POINT('Ctrl Pts',(-2.10926747445009,-4.44789178569794,
12.2994723947233));
#25112=CARTESIAN_POINT('Ctrl Pts',(-2.35092203219417,-4.3204749469813,12.2840760735682));
#25113=CARTESIAN_POINT('Ctrl Pts',(-2.40734458242593,-4.28929249607858,
12.2804361716082));
#25114=CARTESIAN_POINT('Ctrl Pts',(-2.51881371244413,-4.22479563607489,
12.2731468599012));
#25115=CARTESIAN_POINT('Ctrl Pts',(-2.57385214466697,-4.1914920619834,12.2694981899941));
#25116=CARTESIAN_POINT('Ctrl Pts',(-2.68987632584927,-4.11813904582324,
12.2616946098737));
#25117=CARTESIAN_POINT('Ctrl Pts',(-2.75065628212739,-4.07779275108807,
12.2575383117097));
#25118=CARTESIAN_POINT('Ctrl Pts',(-2.92141966976215,-3.95888290034441,
12.2456589273973));
#25119=CARTESIAN_POINT('Ctrl Pts',(-3.02909274183899,-3.87711793944665,
12.2379201759736));
#25120=CARTESIAN_POINT('Ctrl Pts',(-3.2111578411961,-3.72664208839046,12.2244027498735));
#25121=CARTESIAN_POINT('Ctrl Pts',(-3.28705254872941,-3.65987456558176,
12.2186256206746));
#25122=CARTESIAN_POINT('Ctrl Pts',(-3.39046279915788,-3.56308737395465,
12.2105660014033));
#25123=CARTESIAN_POINT('Ctrl Pts',(-3.41974470013231,-3.53499305131765,
12.2082616629441));
#25124=CARTESIAN_POINT('Ctrl Pts',(-3.45218256253671,-3.50309046547008,
12.2056850005498));
#25125=CARTESIAN_POINT('Ctrl Pts',(-3.45568412320601,-3.49963633754612,
12.205406538103));
#25126=CARTESIAN_POINT('Ctrl Pts',(-3.46130201892822,-3.49407789025903,
12.2049592514128));
#25127=CARTESIAN_POINT('Ctrl Pts',(-3.4634216279619,-3.49197688944594,12.2047903721451));
#25128=CARTESIAN_POINT('Ctrl Pts',(-3.50010584028113,-3.45554847344008,
12.201865473296));
#25129=CARTESIAN_POINT('Ctrl Pts',(-3.53416075469713,-3.42071103463849,
12.1991179495173));
#25130=CARTESIAN_POINT('Ctrl Pts',(-3.63079654163704,-3.31887091832525,
12.191215479791));
#25131=CARTESIAN_POINT('Ctrl Pts',(-3.69202905576581,-3.25061677211752,
12.1860756386855));
#25132=CARTESIAN_POINT('Ctrl Pts',(-3.87536319405307,-3.03439180829279,
12.1701904957235));
#25133=CARTESIAN_POINT('Ctrl Pts',(-3.99074226239509,-2.88096314841509,
12.1594621702696));
#25134=CARTESIAN_POINT('Ctrl Pts',(-4.13096579999139,-2.66985078793095,
12.1451783330193));
#25135=CARTESIAN_POINT('Ctrl Pts',(-4.16409799853801,-2.61787498363122,
12.1416982144141));
#25136=CARTESIAN_POINT('Ctrl Pts',(-4.21350352823815,-2.53705853438356,
12.1363376528447));
#25137=CARTESIAN_POINT('Ctrl Pts',(-4.23047722361203,-2.50865311150036,
12.1344629215847));
#25138=CARTESIAN_POINT('Ctrl Pts',(-4.27952121560959,-2.42466471778734,
12.1289461525333));
#25139=CARTESIAN_POINT('Ctrl Pts',(-4.31079168558416,-2.36862317839646,
12.1252985561602));
#25140=CARTESIAN_POINT('Ctrl Pts',(-4.4164231085557,-2.17029094010327,12.1124994198052));
#25141=CARTESIAN_POINT('Ctrl Pts',(-4.48490615416431,-2.02498683376665,
12.103313244126));
#25142=CARTESIAN_POINT('Ctrl Pts',(-4.55221903231299,-1.86191759123798,
12.0932148872363));
#25143=CARTESIAN_POINT('Ctrl Pts',(-4.55820701822915,-1.84720979155811,
12.0923059573267));
#25144=CARTESIAN_POINT('Ctrl Pts',(-4.60202829792678,-1.73806454732453,
12.0855749718152));
#25145=CARTESIAN_POINT('Ctrl Pts',(-4.63699488322442,-1.64250164090664,
12.0797590196825));
#25146=CARTESIAN_POINT('Ctrl Pts',(-4.68175392539196,-1.50732102509259,
12.0716559901385));
#25147=CARTESIAN_POINT('Ctrl Pts',(-4.69405598062844,-1.46856222239915,
12.0693467976528));
#25148=CARTESIAN_POINT('Ctrl Pts',(-4.71546319001737,-1.39809789665345,
12.0651759736675));
#25149=CARTESIAN_POINT('Ctrl Pts',(-4.72473269007326,-1.36644497124293,
12.0633122071074));
#25150=CARTESIAN_POINT('Ctrl Pts',(-4.78602724535463,-1.14905620733739,
12.0505701575916));
#25151=CARTESIAN_POINT('Ctrl Pts',(-4.82740577608411,-0.960490658908029,
12.0398003807952));
#25152=CARTESIAN_POINT('Ctrl Pts',(-4.87707695667389,-0.647128576719021,
12.0220145408731));
#25153=CARTESIAN_POINT('Ctrl Pts',(-4.89188262449464,-0.523582719061208,
12.0150317542213));
#25154=CARTESIAN_POINT('Ctrl Pts',(-4.90758453802529,-0.330968325508063,
12.0041330333462));
#25155=CARTESIAN_POINT('Ctrl Pts',(-4.91173777046985,-0.262217397667348,
12.0002407800475));
#25156=CARTESIAN_POINT('Ctrl Pts',(-4.91698278804598,-0.128939089868967,
11.992683349764));
#25157=CARTESIAN_POINT('Ctrl Pts',(-4.91825104681945,-0.0644325092458331,
11.9890201256933));
#25158=CARTESIAN_POINT('Ctrl Pts',(-4.9182499993517,7.98561370042354E-5,
11.9853490513894));
#25159=CARTESIAN_POINT('Ctrl Pts',(-4.91824999935358,7.97400756539363E-5,
11.9853490579939));
#25160=CARTESIAN_POINT('Ctrl Pts',(-4.91824586312372,0.255196284351623,
11.9708316583857));
#25161=CARTESIAN_POINT('Ctrl Pts',(-4.89839170797622,0.509925348674778,
11.9561953390914));
#25162=CARTESIAN_POINT('Ctrl Pts',(-4.85195482658824,0.806045273478557,
11.939085497959));
#25163=CARTESIAN_POINT('Ctrl Pts',(-4.84444124173504,0.850037484604231,
11.9365418443026));
#25164=CARTESIAN_POINT('Ctrl Pts',(-4.83040234913672,0.92599125711354,11.9321491905602));
#25165=CARTESIAN_POINT('Ctrl Pts',(-4.82415588900359,0.95800138190684,11.9302976477932));
#25166=CARTESIAN_POINT('Ctrl Pts',(-4.81035161837271,1.02518005234567,11.926412434742));
#25167=CARTESIAN_POINT('Ctrl Pts',(-4.80272542381217,1.06033266985377,11.924379745439));
#25168=CARTESIAN_POINT('Ctrl Pts',(-4.78504506018961,1.1377221099375,11.9199017942449));
#25169=CARTESIAN_POINT('Ctrl Pts',(-4.77481742903138,1.17990896109132,11.9174588098249));
#25170=CARTESIAN_POINT('Ctrl Pts',(-4.76403457734943,1.22194828381523,11.9150196727617));
#25171=CARTESIAN_POINT('Ctrl Pts',(-4.76403460025573,1.22194819451,11.5699436565254));
#25172=CARTESIAN_POINT('Ctrl Pts',(-4.78098833517923,1.15585031888646,11.573766391097));
#25173=CARTESIAN_POINT('Ctrl Pts',(-4.79656778033866,1.08939451803579,11.5775899281936));
#25174=CARTESIAN_POINT('Ctrl Pts',(-4.82747975550792,0.943974298564324,
11.5859302393302));
#25175=CARTESIAN_POINT('Ctrl Pts',(-4.84226688445056,0.864927468062738,
11.5904471333619));
#25176=CARTESIAN_POINT('Ctrl Pts',(-4.86686164324608,0.71291982604495,11.5991204219165));
#25177=CARTESIAN_POINT('Ctrl Pts',(-4.87698231678454,0.64003144261876,11.6032737330627));
#25178=CARTESIAN_POINT('Ctrl Pts',(-4.89275288639956,0.504133468807987,
11.6110173433907));
#25179=CARTESIAN_POINT('Ctrl Pts',(-4.89882984601668,0.441188611407961,
11.6146039360536));
#25180=CARTESIAN_POINT('Ctrl Pts',(-4.91339697047539,0.252285496999654,
11.6253741599271));
#25181=CARTESIAN_POINT('Ctrl Pts',(-4.9182533146826,0.126100836882465,11.6325783485043));
#25182=CARTESIAN_POINT('Ctrl Pts',(-4.91824505553169,-0.188264015889626,
11.6505610645531));
#25183=CARTESIAN_POINT('Ctrl Pts',(-4.90744522725096,-0.376244584205871,
11.6613490122019));
#25184=CARTESIAN_POINT('Ctrl Pts',(-4.88180002559322,-0.598745212729988,
11.6740888745682));
#25185=CARTESIAN_POINT('Ctrl Pts',(-4.87730769301797,-0.634300423492197,
11.6761235414629));
#25186=CARTESIAN_POINT('Ctrl Pts',(-4.86653706601074,-0.712650395613172,
11.6806030201867));
#25187=CARTESIAN_POINT('Ctrl Pts',(-4.86008203348525,-0.755417955942893,
11.6830455462112));
#25188=CARTESIAN_POINT('Ctrl Pts',(-4.80969175839413,-1.06183157362575,
11.7005471002254));
#25189=CARTESIAN_POINT('Ctrl Pts',(-4.74489296991637,-1.32159540990317,
11.7154186912288));
#25190=CARTESIAN_POINT('Ctrl Pts',(-4.63369466279226,-1.65059275050297,
11.7349555154213));
#25191=CARTESIAN_POINT('Ctrl Pts',(-4.60623475035732,-1.72574154352134,
11.7394655261874));
#25192=CARTESIAN_POINT('Ctrl Pts',(-4.55172547928513,-1.86433076770848,
11.7478863131506));
#25193=CARTESIAN_POINT('Ctrl Pts',(-4.52515110206806,-1.92793708653123,
11.7517926779444));
#25194=CARTESIAN_POINT('Ctrl Pts',(-4.45019806079601,-2.09724330766243,
11.762311836897));
#25195=CARTESIAN_POINT('Ctrl Pts',(-4.39939505592838,-2.20182080367125,
11.7689395942986));
#25196=CARTESIAN_POINT('Ctrl Pts',(-4.24809266901591,-2.48708850108384,
11.7874000729362));
#25197=CARTESIAN_POINT('Ctrl Pts',(-4.13983601864805,-2.66339238904601,
11.7992580880018));
#25198=CARTESIAN_POINT('Ctrl Pts',(-4.00012025100349,-2.86173228450808,
11.8130584137562));
#25199=CARTESIAN_POINT('Ctrl Pts',(-3.97910994721514,-2.8908749122066,11.8150981909489));
#25200=CARTESIAN_POINT('Ctrl Pts',(-3.93220284564366,-2.95445770680338,
11.8195736280161));
#25201=CARTESIAN_POINT('Ctrl Pts',(-3.90616887642156,-2.98879312232786,
11.8220070625958));
#25202=CARTESIAN_POINT('Ctrl Pts',(-3.84731220176153,-3.06433461022059,
11.8274045304857));
#25203=CARTESIAN_POINT('Ctrl Pts',(-3.81427182960623,-3.10536443285343,
11.8303657975174));
#25204=CARTESIAN_POINT('Ctrl Pts',(-3.69826255434059,-3.24478028806058,
11.8405479629783));
#25205=CARTESIAN_POINT('Ctrl Pts',(-3.61209527463768,-3.34043604565295,
11.8477461484402));
#25206=CARTESIAN_POINT('Ctrl Pts',(-3.43613415240409,-3.52099397803826,
11.8618783329864));
#25207=CARTESIAN_POINT('Ctrl Pts',(-3.34669684877314,-3.60611094834908,
11.8688059895568));
#25208=CARTESIAN_POINT('Ctrl Pts',(-3.20676083151303,-3.72959287689251,
11.8793286289782));
#25209=CARTESIAN_POINT('Ctrl Pts',(-3.15856668220214,-3.77049525443292,
11.8828993261185));
#25210=CARTESIAN_POINT('Ctrl Pts',(-3.05255372544539,-3.85700919828873,
11.8906474310381));
#25211=CARTESIAN_POINT('Ctrl Pts',(-2.99447180271443,-3.90227403605745,
11.8948268513807));
#25212=CARTESIAN_POINT('Ctrl Pts',(-2.8707981671648,-3.99426873905427,11.903598033241));
#25213=CARTESIAN_POINT('Ctrl Pts',(-2.80503056586202,-4.04072619965047,
11.9081905427128));
#25214=CARTESIAN_POINT('Ctrl Pts',(-2.58471620400986,-4.18838188256451,
11.9233468428301));
#25215=CARTESIAN_POINT('Ctrl Pts',(-2.4256085924832,-4.28249035704451,11.9339394637194));
#25216=CARTESIAN_POINT('Ctrl Pts',(-2.21405030510433,-4.39204164750832,
11.9475296588114));
#25217=CARTESIAN_POINT('Ctrl Pts',(-2.16611580780215,-4.41587941283665,
11.9505771630055));
#25218=CARTESIAN_POINT('Ctrl Pts',(-2.0874745581742,-4.45339893724738,11.955521989465));
#25219=CARTESIAN_POINT('Ctrl Pts',(-2.05700030704158,-4.46755659030982,
11.9574246712789));
#25220=CARTESIAN_POINT('Ctrl Pts',(-1.96877752544967,-4.50744883454713,
11.9628960658759));
#25221=CARTESIAN_POINT('Ctrl Pts',(-1.91067463309062,-4.53238375841664,
11.9664551840295));
#25222=CARTESIAN_POINT('Ctrl Pts',(-1.70030090263576,-4.61790136053752,
11.979214730734));
#25223=CARTESIAN_POINT('Ctrl Pts',(-1.54550530741354,-4.67198565248014,
11.9883708900171));
#25224=CARTESIAN_POINT('Ctrl Pts',(-1.29012572899634,-4.74712871785957,
12.0033020623864));
#25225=CARTESIAN_POINT('Ctrl Pts',(-1.19107580359823,-4.77294390847587,
12.0090510865457));
#25226=CARTESIAN_POINT('Ctrl Pts',(-1.02969487315582,-4.80966760007122,
12.0183829845819));
#25227=CARTESIAN_POINT('Ctrl Pts',(-0.967832205204608,-4.82249672570205,
12.0219518969845));
#25228=CARTESIAN_POINT('Ctrl Pts',(-0.83330981147716,-4.84770132359213,
12.0297017826942));
#25229=CARTESIAN_POINT('Ctrl Pts',(-0.7605843570137,-4.8596424382312,12.0338847945671));
#25230=CARTESIAN_POINT('Ctrl Pts',(-0.607771056789594,-4.88121912619603,
12.0426670434425));
#25231=CARTESIAN_POINT('Ctrl Pts',(-0.527658800370901,-4.89052776546599,
12.047267044382));
#25232=CARTESIAN_POINT('Ctrl Pts',(-0.2736696191737,-4.91372629632837,12.0618422862466));
#25233=CARTESIAN_POINT('Ctrl Pts',(-0.0992640703909754,-4.92034021057034,
12.0718419787528));
#25234=CARTESIAN_POINT('Ctrl Pts',(0.134840340244993,-4.91676398581778,
12.0852069404104));
#25235=CARTESIAN_POINT('Ctrl Pts',(0.194536257817274,-4.91476406116013,
12.0886093805751));
#25236=CARTESIAN_POINT('Ctrl Pts',(0.291263699719364,-4.90975837487325,
12.0941084845825));
#25237=CARTESIAN_POINT('Ctrl Pts',(0.328323091291363,-4.90741946742565,
12.0962116520858));
#25238=CARTESIAN_POINT('Ctrl Pts',(0.428076507567132,-4.89998873894347,
12.1018644039));
#25239=CARTESIAN_POINT('Ctrl Pts',(0.490705256787886,-4.8941135697492,12.1054054407801));
#25240=CARTESIAN_POINT('Ctrl Pts',(0.650430182585883,-4.87603297592932,
12.114437512945));
#25241=CARTESIAN_POINT('Ctrl Pts',(0.747306182844398,-4.86212820348557,
12.1199170489853));
#25242=CARTESIAN_POINT('Ctrl Pts',(0.995513166931167,-4.81890875823923,
12.1340309761498));
#25243=CARTESIAN_POINT('Ctrl Pts',(1.1459954929802,-4.78535491654709,12.1426622720842));
#25244=CARTESIAN_POINT('Ctrl Pts',(1.36522866154184,-4.72553547851673,12.1554634954052));
#25245=CARTESIAN_POINT('Ctrl Pts',(1.43536552967434,-4.70470620639795,12.1595933574341));
#25246=CARTESIAN_POINT('Ctrl Pts',(1.57372652120927,-4.66023363504856,12.1678200857226));
#25247=CARTESIAN_POINT('Ctrl Pts',(1.64194683410348,-4.63663704932532,12.1719156523649));
#25248=CARTESIAN_POINT('Ctrl Pts',(1.85958908973308,-4.55595131851039,12.185119237694));
#25249=CARTESIAN_POINT('Ctrl Pts',(2.00675268876172,-4.49307316776388,12.1942619777953));
#25250=CARTESIAN_POINT('Ctrl Pts',(2.27439181097747,-4.36294344438658,12.2112979129175));
#25251=CARTESIAN_POINT('Ctrl Pts',(2.39561386256894,-4.29757704330211,12.2191795499294));
#25252=CARTESIAN_POINT('Ctrl Pts',(2.549891981026,-4.20582740307757,12.2293962081102));
#25253=CARTESIAN_POINT('Ctrl Pts',(2.58557525991751,-4.18398540784354,12.2317725510444));
#25254=CARTESIAN_POINT('Ctrl Pts',(2.65726345838225,-4.13883716163471,12.2365714648212));
#25255=CARTESIAN_POINT('Ctrl Pts',(2.69325095242651,-4.11550987157241,12.2389935703404));
#25256=CARTESIAN_POINT('Ctrl Pts',(2.75138682471223,-4.07673672157479,12.242932344316));
#25257=CARTESIAN_POINT('Ctrl Pts',(2.7737210177932,-4.06157401537206,12.2444518840647));
#25258=CARTESIAN_POINT('Ctrl Pts',(2.86147654458704,-4.0009352571259,12.2504503931676));
#25259=CARTESIAN_POINT('Ctrl Pts',(2.92591388801677,-3.95405602066236,12.2549170904686));
#25260=CARTESIAN_POINT('Ctrl Pts',(3.14000352353164,-3.79020203249851,12.2700237200506));
#25261=CARTESIAN_POINT('Ctrl Pts',(3.28400866277456,-3.66613415711815,12.2806463810935));
#25262=CARTESIAN_POINT('Ctrl Pts',(3.47208035656892,-3.48410654873394,12.295395632557));
#25263=CARTESIAN_POINT('Ctrl Pts',(3.52258306560186,-3.43303784337182,12.2994512630649));
#25264=CARTESIAN_POINT('Ctrl Pts',(3.62253383731474,-3.3274384592002,12.307684414492));
#25265=CARTESIAN_POINT('Ctrl Pts',(3.67191242947728,-3.27286679229285,12.3118614417936));
#25266=CARTESIAN_POINT('Ctrl Pts',(3.77265531652826,-3.15637811471549,12.3206252485247));
#25267=CARTESIAN_POINT('Ctrl Pts',(3.82376269945519,-3.09426721189536,12.3252127652597));
#25268=CARTESIAN_POINT('Ctrl Pts',(3.98671683084131,-2.8860229519787,12.3403235018235));
#25269=CARTESIAN_POINT('Ctrl Pts',(4.09188850663947,-2.73486527224022,12.3508753436892));
#25270=CARTESIAN_POINT('Ctrl Pts',(4.21667373355567,-2.53214663193979,12.3644554401123));
#25271=CARTESIAN_POINT('Ctrl Pts',(4.24424416456475,-2.48565796301862,12.367532457769));
#25272=CARTESIAN_POINT('Ctrl Pts',(4.28768432903433,-2.40957932072106,12.3725044562423));
#25273=CARTESIAN_POINT('Ctrl Pts',(4.3040268893569,-2.38026510502099,12.3744049727553));
#25274=CARTESIAN_POINT('Ctrl Pts',(4.34991074104524,-2.29594377058648,12.3798300078691));
#25275=CARTESIAN_POINT('Ctrl Pts',(4.37870643117465,-2.24053819078453,12.3833452321062));
#25276=CARTESIAN_POINT('Ctrl Pts',(4.42844543031621,-2.1402122705825,12.389637498959));
#25277=CARTESIAN_POINT('Ctrl Pts',(4.44977935230398,-2.09549546528303,12.392416683309));
#25278=CARTESIAN_POINT('Ctrl Pts',(4.56237464594534,-1.8500145001232,12.4075567080177));
#25279=CARTESIAN_POINT('Ctrl Pts',(4.6407283960526,-1.64361028202658,12.4198772819986));
#25280=CARTESIAN_POINT('Ctrl Pts',(4.72507273319894,-1.36661456342681,12.4362060421504));
#25281=CARTESIAN_POINT('Ctrl Pts',(4.74378704604622,-1.30016615049333,12.4401069882077));
#25282=CARTESIAN_POINT('Ctrl Pts',(4.7804195390905,-1.15875346003012,12.4483836219702));
#25283=CARTESIAN_POINT('Ctrl Pts',(4.79798677023111,-1.08371735632732,12.4527606428638));
#25284=CARTESIAN_POINT('Ctrl Pts',(4.83607943332904,-0.901856989705154,
12.4633418365647));
#25285=CARTESIAN_POINT('Ctrl Pts',(4.85483828423952,-0.794704454320485,
12.4695544239148));
#25286=CARTESIAN_POINT('Ctrl Pts',(4.89489172648632,-0.510780180795229,
12.4859610607633));
#25287=CARTESIAN_POINT('Ctrl Pts',(4.91016903207596,-0.333320255196364,
12.4961634956557));
#25288=CARTESIAN_POINT('Ctrl Pts',(4.91692035504379,-0.119785444310117,
12.5083148080151));
#25289=CARTESIAN_POINT('Ctrl Pts',(4.91765953992758,-0.0841369180339632,
12.5103390127729));
#25290=CARTESIAN_POINT('Ctrl Pts',(4.91844081732371,-0.00488619640901847,
12.5148276938987));
#25291=CARTESIAN_POINT('Ctrl Pts',(4.91829087786488,0.0387149766614358,
12.5172897548081));
#25292=CARTESIAN_POINT('Ctrl Pts',(4.91666364247416,0.135934692632118,12.5227694176435));
#25293=CARTESIAN_POINT('Ctrl Pts',(4.91488893389383,0.189542748932334,12.5257841141135));
#25294=CARTESIAN_POINT('Ctrl Pts',(4.90558340422741,0.377567595599534,12.5363515755941));
#25295=CARTESIAN_POINT('Ctrl Pts',(4.89341138872779,0.511694248772478,12.5438799646214));
#25296=CARTESIAN_POINT('Ctrl Pts',(4.85980570638349,0.765669813902728,12.5582434482152));
#25297=CARTESIAN_POINT('Ctrl Pts',(4.83939633156508,0.885553144829605,12.5650698065815));
#25298=CARTESIAN_POINT('Ctrl Pts',(4.80056665704078,1.0716533508382,12.5757930195174));
#25299=CARTESIAN_POINT('Ctrl Pts',(4.78516580992274,1.13845033494815,12.579667514265));
#25300=CARTESIAN_POINT('Ctrl Pts',(4.74913887420359,1.28102603885606,12.5880012263426));
#25301=CARTESIAN_POINT('Ctrl Pts',(4.72808371928204,1.35667678428075,12.5924623440499));
#25302=CARTESIAN_POINT('Ctrl Pts',(4.67880155679679,1.51863048567403,12.6021052957347));
#25303=CARTESIAN_POINT('Ctrl Pts',(4.64997746309202,1.60472175947004,12.6072891803258));
#25304=CARTESIAN_POINT('Ctrl Pts',(4.56291679509271,1.84266435625749,12.6217816929282));
#25305=CARTESIAN_POINT('Ctrl Pts',(4.49950766187454,1.99249912002729,12.6311021350282));
#25306=CARTESIAN_POINT('Ctrl Pts',(4.40634243916989,2.18540487858849,12.6433181384147));
#25307=CARTESIAN_POINT('Ctrl Pts',(4.38316042141994,2.23153601414809,12.6462560302448));
#25308=CARTESIAN_POINT('Ctrl Pts',(4.34352775000413,2.30740192031852,12.6511118941388));
#25309=CARTESIAN_POINT('Ctrl Pts',(4.32748778296205,2.33734602638833,12.6530345667343));
#25310=CARTESIAN_POINT('Ctrl Pts',(4.27799082788966,2.42749273023385,12.658843973673));
#25311=CARTESIAN_POINT('Ctrl Pts',(4.24357818988832,2.48716119392316,12.662718888001));
#25312=CARTESIAN_POINT('Ctrl Pts',(4.14766747263507,2.64567299747709,12.6731229881941));
#25313=CARTESIAN_POINT('Ctrl Pts',(4.08389500509627,2.74308820063897,12.6796360760718));
#25314=CARTESIAN_POINT('Ctrl Pts',(3.93687223313482,2.95116402587236,12.6939122493554));
#25315=CARTESIAN_POINT('Ctrl Pts',(3.85228473071804,3.0607570562648,12.7016733521907));
#25316=CARTESIAN_POINT('Ctrl Pts',(3.72224628283575,3.21529306839571,12.7130592062826));
#25317=CARTESIAN_POINT('Ctrl Pts',(3.68036327687757,3.26315076974412,12.7166511056339));
#25318=CARTESIAN_POINT('Ctrl Pts',(3.58846248043213,3.36414068772975,12.7243818166378));
#25319=CARTESIAN_POINT('Ctrl Pts',(3.53816648341238,3.41699916703725,12.728522350703));
#25320=CARTESIAN_POINT('Ctrl Pts',(3.38202900490992,3.57394665016725,12.7411181529036));
#25321=CARTESIAN_POINT('Ctrl Pts',(3.27263545404829,3.67438036903596,12.7496012959984));
#25322=CARTESIAN_POINT('Ctrl Pts',(3.04598311810229,3.86430604889635,12.7665280438839));
#25323=CARTESIAN_POINT('Ctrl Pts',(2.92890403246031,3.95378252491936,12.7749628617417));
#25324=CARTESIAN_POINT('Ctrl Pts',(2.77408223819932,4.06144754020602,12.7856947703326));
#25325=CARTESIAN_POINT('Ctrl Pts',(2.739882781973,4.08459677178946,12.7880401164099));
#25326=CARTESIAN_POINT('Ctrl Pts',(2.66905220012077,4.13125130064764,12.7928438028343));
#25327=CARTESIAN_POINT('Ctrl Pts',(2.63239242779999,4.15470662287336,12.7953013765048));
#25328=CARTESIAN_POINT('Ctrl Pts',(2.57197110734827,4.19224404633857,12.7993101648414));
#25329=CARTESIAN_POINT('Ctrl Pts',(2.54839391139228,4.20661788194225,12.8008642589004));
#25330=CARTESIAN_POINT('Ctrl Pts',(2.48814434605346,4.24265658527528,12.8048116434279));
#25331=CARTESIAN_POINT('Ctrl Pts',(2.45130923539939,4.26404505693337,12.8072026656876));
#25332=CARTESIAN_POINT('Ctrl Pts',(2.24530989914214,4.38010790126974,12.8204650456799));
#25333=CARTESIAN_POINT('Ctrl Pts',(2.07094160404649,4.46519454328312,12.8312931153747));
#25334=CARTESIAN_POINT('Ctrl Pts',(1.81733743792339,4.57088742324357,12.8467472920114));
#25335=CARTESIAN_POINT('Ctrl Pts',(1.74191113233369,4.60016006188954,12.8513073076284));
#25336=CARTESIAN_POINT('Ctrl Pts',(1.60112772581875,4.65083833598275,12.8597669537097));
#25337=CARTESIAN_POINT('Ctrl Pts',(1.53597723902097,4.67275946311942,12.863661813852));
#25338=CARTESIAN_POINT('Ctrl Pts',(1.36276118265149,4.72702716528049,12.8739730987878));
#25339=CARTESIAN_POINT('Ctrl Pts',(1.25400621760271,4.75703392323669,12.8804031565053));
#25340=CARTESIAN_POINT('Ctrl Pts',(0.95166791222481,4.82936322028765,12.8981719767938));
#25341=CARTESIAN_POINT('Ctrl Pts',(0.756409996755351,4.86377068043257,12.9095349950983));
#25342=CARTESIAN_POINT('Ctrl Pts',(0.514959687059944,4.89142304227158,12.9233773513371));
#25343=CARTESIAN_POINT('Ctrl Pts',(0.470241067282416,4.89592445407627,12.9259319539752));
#25344=CARTESIAN_POINT('Ctrl Pts',(0.386790045311462,4.90317077886525,12.9306795818137));
#25345=CARTESIAN_POINT('Ctrl Pts',(0.348074948250218,4.9060711458306,12.9328740395691));
#25346=CARTESIAN_POINT('Ctrl Pts',(0.262941891064752,4.91143613949402,12.9376862305218));
#25347=CARTESIAN_POINT('Ctrl Pts',(0.216515177281609,4.91370172298623,12.9403018732373));
#25348=CARTESIAN_POINT('Ctrl Pts',(0.0737877311793425,4.9186399002408,12.9483268148581));
#25349=CARTESIAN_POINT('Ctrl Pts',(-0.0225651832630477,4.91914160196261,
12.9537220050758));
#25350=CARTESIAN_POINT('Ctrl Pts',(-0.275919939155246,4.91301638971006,
12.9679192321155));
#25351=CARTESIAN_POINT('Ctrl Pts',(-0.432695325324775,4.90169724137416,
12.9767176553217));
#25352=CARTESIAN_POINT('Ctrl Pts',(-0.661138657531286,4.87415720550904,
12.989679896139));
#25353=CARTESIAN_POINT('Ctrl Pts',(-0.733414702123794,4.86380668811291,
12.9938013922589));
#25354=CARTESIAN_POINT('Ctrl Pts',(-0.863827360069615,4.84215749735272,
13.001284827541));
#25355=CARTESIAN_POINT('Ctrl Pts',(-0.922041595448284,4.83141036784889,
13.004642311391));
#25356=CARTESIAN_POINT('Ctrl Pts',(-0.994035189030095,4.81677079152845,
13.0088179688936));
#25357=CARTESIAN_POINT('Ctrl Pts',(-1.00801064715348,4.81386553085616,13.009629649949));
#25358=CARTESIAN_POINT('Ctrl Pts',(-1.0362006670346,4.80787716089409,13.0112691563902));
#25359=CARTESIAN_POINT('Ctrl Pts',(-1.05041459765812,4.80479175286518,13.0120969879372));
#25360=CARTESIAN_POINT('Ctrl Pts',(-1.14907691917501,4.78291646109989,13.0178513599189));
#25361=CARTESIAN_POINT('Ctrl Pts',(-1.23302979291403,4.7619644015857,13.0227899080874));
#25362=CARTESIAN_POINT('Ctrl Pts',(-1.4757361078947,4.69454342987918,13.0371934807508));
#25363=CARTESIAN_POINT('Ctrl Pts',(-1.63275248939524,4.64226825653443,13.0466744900902));
#25364=CARTESIAN_POINT('Ctrl Pts',(-1.83826272680442,4.56212889000835,13.0592602045832));
#25365=CARTESIAN_POINT('Ctrl Pts',(-1.88934804300358,4.54121062445764,13.0624033369308));
#25366=CARTESIAN_POINT('Ctrl Pts',(-1.95708127069116,4.51213459900771,13.0665871252505));
#25367=CARTESIAN_POINT('Ctrl Pts',(-1.97405045573635,4.50473645677946,13.067636662298));
#25368=CARTESIAN_POINT('Ctrl Pts',(-2.02417614545175,4.48254527616926,13.0707407622591));
#25369=CARTESIAN_POINT('Ctrl Pts',(-2.05721118955374,4.46748065218478,13.0727916730823));
#25370=CARTESIAN_POINT('Ctrl Pts',(-2.13477061799304,4.43106931551151,13.0776230553163));
#25371=CARTESIAN_POINT('Ctrl Pts',(-2.17914642094442,4.40941513214496,13.0804001698281));
#25372=CARTESIAN_POINT('Ctrl Pts',(-2.32158540530958,4.33723327304474,13.089368980715));
#25373=CARTESIAN_POINT('Ctrl Pts',(-2.41827694264989,4.28407377385376,13.0955429661045));
#25374=CARTESIAN_POINT('Ctrl Pts',(-2.63787070061991,4.15353946241633,13.1098557616424));
#25375=CARTESIAN_POINT('Ctrl Pts',(-2.75929616954299,4.07388460897361,13.1179932892749));
#25376=CARTESIAN_POINT('Ctrl Pts',(-2.93357466086628,3.94818756273855,13.1301052844369));
#25377=CARTESIAN_POINT('Ctrl Pts',(-2.98925522652132,3.90619999069877,13.1340440641749));
#25378=CARTESIAN_POINT('Ctrl Pts',(-3.079801238083,3.83485100305548,13.1405725543417));
#25379=CARTESIAN_POINT('Ctrl Pts',(-3.11518510151981,3.80616337320029,13.1431561186991));
#25380=CARTESIAN_POINT('Ctrl Pts',(-3.23755328563427,3.70410322917328,13.152208230679));
#25381=CARTESIAN_POINT('Ctrl Pts',(-3.3223845942299,3.6282078337653,13.1586962174754));
#25382=CARTESIAN_POINT('Ctrl Pts',(-3.52503218067891,3.43383489916485,13.1747472077926));
#25383=CARTESIAN_POINT('Ctrl Pts',(-3.63959159421848,3.31216651960875,13.1843213862007));
#25384=CARTESIAN_POINT('Ctrl Pts',(-3.78664593755876,3.13912492772573,13.1972846986788));
#25385=CARTESIAN_POINT('Ctrl Pts',(-3.82471060550807,3.09263345338399,13.2007076122421));
#25386=CARTESIAN_POINT('Ctrl Pts',(-3.86712709144033,3.03884550323575,13.2045968708277));
#25387=CARTESIAN_POINT('Ctrl Pts',(-3.87232299249328,3.03222172279014,13.2050746144678));
#25388=CARTESIAN_POINT('Ctrl Pts',(-3.88189708795891,3.01995183855786,13.2059573474881));
#25389=CARTESIAN_POINT('Ctrl Pts',(-3.8862800337432,3.01430947454687,13.2063624059064));
#25390=CARTESIAN_POINT('Ctrl Pts',(-3.89514852216803,3.00284117359959,13.2071839253731));
#25391=CARTESIAN_POINT('Ctrl Pts',(-3.89963331719153,2.99701470054644,13.2076003700913));
#25392=CARTESIAN_POINT('Ctrl Pts',(-3.91471447636118,2.97733067435723,13.2090041848999));
#25393=CARTESIAN_POINT('Ctrl Pts',(-3.9252501981295,2.96342677691314,13.2099906304472));
#25394=CARTESIAN_POINT('Ctrl Pts',(-3.97258539452435,2.90026360731435,13.2144495680702));
#25395=CARTESIAN_POINT('Ctrl Pts',(-4.00853342260501,2.85037254419387,13.2179105772898));
#25396=CARTESIAN_POINT('Ctrl Pts',(-4.10085440886187,2.71704137224539,13.2270220051929));
#25397=CARTESIAN_POINT('Ctrl Pts',(-4.15561681082883,2.63252157093875,13.2326597597566));
#25398=CARTESIAN_POINT('Ctrl Pts',(-4.29131487191327,2.40828834848544,13.2473426957897));
#25399=CARTESIAN_POINT('Ctrl Pts',(-4.36803373687612,2.26616779017128,13.256385706574));
#25400=CARTESIAN_POINT('Ctrl Pts',(-4.46755004179216,2.05791080258784,13.2693972741878));
#25401=CARTESIAN_POINT('Ctrl Pts',(-4.496145655261,1.99466146271686,13.2733181836867));
#25402=CARTESIAN_POINT('Ctrl Pts',(-4.54745197937491,1.87446505715379,13.2807200633776));
#25403=CARTESIAN_POINT('Ctrl Pts',(-4.57045526740873,1.81765709190626,13.2841981554568));
#25404=CARTESIAN_POINT('Ctrl Pts',(-4.65355990534784,1.60086460416551,13.2974025853318));
#25405=CARTESIAN_POINT('Ctrl Pts',(-4.70636995203586,1.43821686912942,13.3071734417914));
#25406=CARTESIAN_POINT('Ctrl Pts',(-4.75517464728987,1.2561084876741,13.3179663082455));
#25407=CARTESIAN_POINT('Ctrl Pts',(-4.75965068753344,1.23903984464184,13.3189764473691));
#25408=CARTESIAN_POINT('Ctrl Pts',(-4.76403458795361,1.2219482424725,13.3199864568809));
#25409=CARTESIAN_POINT('Origin',(0.,0.,-3.23514056400928));
#25410=CARTESIAN_POINT('',(-4.76403458688904,1.22194824662298,15.4150234826428));
#25411=CARTESIAN_POINT('',(-4.76403458707897,1.2219482458825,15.0697260295707));
#25412=CARTESIAN_POINT('',(-4.76403458704967,1.22194824599672,-3.23514056400928));
#25413=CARTESIAN_POINT('Ctrl Pts',(-4.76403458688904,1.22194824662298,15.4150234826428));
#25414=CARTESIAN_POINT('Ctrl Pts',(-4.75134449250892,1.27142337677261,15.4121081981807));
#25415=CARTESIAN_POINT('Ctrl Pts',(-4.73788412615466,1.32069912133302,15.4091978920613));
#25416=CARTESIAN_POINT('Ctrl Pts',(-4.71333760987541,1.40534867036559,15.4041898595337));
#25417=CARTESIAN_POINT('Ctrl Pts',(-4.70261496733127,1.44082227632375,15.4020887840589));
#25418=CARTESIAN_POINT('Ctrl Pts',(-4.67604786342768,1.52525646341863,15.3970824162182));
#25419=CARTESIAN_POINT('Ctrl Pts',(-4.65983392678187,1.57409617343573,15.3941813954399));
#25420=CARTESIAN_POINT('Ctrl Pts',(-4.58916078114956,1.77630900694187,15.3821289778244));
#25421=CARTESIAN_POINT('Ctrl Pts',(-4.52787191167994,1.92718631601876,15.373033575167));
#25422=CARTESIAN_POINT('Ctrl Pts',(-4.42133328548739,2.15616773840472,15.3588763536351));
#25423=CARTESIAN_POINT('Ctrl Pts',(-4.38122830216776,2.23653430829834,15.3538373511134));
#25424=CARTESIAN_POINT('Ctrl Pts',(-4.3087138104182,2.3724019380417,15.3451709440757));
#25425=CARTESIAN_POINT('Ctrl Pts',(-4.27737562109464,2.42844875297089,15.3415514531651));
#25426=CARTESIAN_POINT('Ctrl Pts',(-4.22654342092121,2.51532145543982,15.3358643859259));
#25427=CARTESIAN_POINT('Ctrl Pts',(-4.20778850548242,2.54657165322187,15.3338026587189));
#25428=CARTESIAN_POINT('Ctrl Pts',(-4.15588271862014,2.63091999060186,15.3281926142887));
#25429=CARTESIAN_POINT('Ctrl Pts',(-4.12206287757725,2.68359808744987,15.3246395381905));
#25430=CARTESIAN_POINT('Ctrl Pts',(-3.97715955366056,2.90009619811801,15.3098204784923));
#25431=CARTESIAN_POINT('Ctrl Pts',(-3.85724497471954,3.05777948854271,15.2984922811165));
#25432=CARTESIAN_POINT('Ctrl Pts',(-3.67460024539284,3.27005186364464,15.2824660862827));
#25433=CARTESIAN_POINT('Ctrl Pts',(-3.61949106206961,3.33094742861924,15.2777706203196));
#25434=CARTESIAN_POINT('Ctrl Pts',(-3.52951770356506,3.42549710679179,15.2703306319995));
#25435=CARTESIAN_POINT('Ctrl Pts',(-3.49563657051375,3.46006512791778,15.2675771154922));
#25436=CARTESIAN_POINT('Ctrl Pts',(-3.45915328737675,3.49620512999272,15.2646642483703));
#25437=CARTESIAN_POINT('Ctrl Pts',(-3.45705422393186,3.49828070191186,15.2644968369092));
#25438=CARTESIAN_POINT('Ctrl Pts',(-3.45148020888507,3.50378241960159,15.26405275832));
#25439=CARTESIAN_POINT('Ctrl Pts',(-3.44800202238222,3.50720528768666,15.2637761458504));
#25440=CARTESIAN_POINT('Ctrl Pts',(-3.41547338250635,3.53912142066376,15.2611938274844));
#25441=CARTESIAN_POINT('Ctrl Pts',(-3.3860752804669,3.56725848424321,15.2588944710153));
#25442=CARTESIAN_POINT('Ctrl Pts',(-3.28155310678575,3.66484077526313,15.250830570676));
#25443=CARTESIAN_POINT('Ctrl Pts',(-3.20461420031283,3.73230450963938,15.2450920018536));
#25444=CARTESIAN_POINT('Ctrl Pts',(-3.02202957411019,3.88259243773808,15.2318382194647));
#25445=CARTESIAN_POINT('Ctrl Pts',(-2.91498660155145,3.96358924898163,15.2243313616186));
#25446=CARTESIAN_POINT('Ctrl Pts',(-2.74498599449902,4.0816088740256,15.2127103994135));
#25447=CARTESIAN_POINT('Ctrl Pts',(-2.68429230960297,4.12177798693677,15.2086175984317));
#25448=CARTESIAN_POINT('Ctrl Pts',(-2.56843920373896,4.1948089200395,15.2008962711094));
#25449=CARTESIAN_POINT('Ctrl Pts',(-2.5134840488733,4.22796637189551,15.1972707782827));
#25450=CARTESIAN_POINT('Ctrl Pts',(-2.40222710354667,4.292157812925,15.1899974741594));
#25451=CARTESIAN_POINT('Ctrl Pts',(-2.34593419841334,4.32318243535292,15.1863503382714));
#25452=CARTESIAN_POINT('Ctrl Pts',(-2.10367866822939,4.45057111597126,15.1707841804805));
#25453=CARTESIAN_POINT('Ctrl Pts',(-1.91227227415226,4.53610623313886,15.1587938603834));
#25454=CARTESIAN_POINT('Ctrl Pts',(-1.65089821233089,4.63341601767566,15.1428352615917));
#25455=CARTESIAN_POINT('Ctrl Pts',(-1.58528889334641,4.65627191318991,15.1388639140763));
#25456=CARTESIAN_POINT('Ctrl Pts',(-1.50908177424914,4.68102219849805,15.1342948655925));
#25457=CARTESIAN_POINT('Ctrl Pts',(-1.49893569650502,4.68428099099336,15.1336874407614));
#25458=CARTESIAN_POINT('Ctrl Pts',(-1.48219143695011,4.68959906405419,15.1326864892855));
#25459=CARTESIAN_POINT('Ctrl Pts',(-1.47559937041334,4.69167745434099,15.132292804156));
#25460=CARTESIAN_POINT('Ctrl Pts',(-1.46460517174817,4.69511831460446,15.1316368607983));
#25461=CARTESIAN_POINT('Ctrl Pts',(-1.46020547023611,4.69648850546849,15.1313745338387));
#25462=CARTESIAN_POINT('Ctrl Pts',(-1.45277328326636,4.69879164426458,15.1309316896031));
#25463=CARTESIAN_POINT('Ctrl Pts',(-1.44974181049916,4.69972784442821,15.1307511420472));
#25464=CARTESIAN_POINT('Ctrl Pts',(-1.4118654054906,4.71138496054417,15.1284963361687));
#25465=CARTESIAN_POINT('Ctrl Pts',(-1.37690297716942,4.72172112657146,15.1264258325769));
#25466=CARTESIAN_POINT('Ctrl Pts',(-1.30754614861273,4.74138966315003,15.1223413459808));
#25467=CARTESIAN_POINT('Ctrl Pts',(-1.27315880040227,4.7507388445087,15.1203273214971));
#25468=CARTESIAN_POINT('Ctrl Pts',(-1.16096478362739,4.77993632938074,15.1137869526605));
#25469=CARTESIAN_POINT('Ctrl Pts',(-1.08277254747144,4.79825326460896,15.1092763339742));
#25470=CARTESIAN_POINT('Ctrl Pts',(-0.856563816594028,4.84543245616913,
15.0963147135238));
#25471=CARTESIAN_POINT('Ctrl Pts',(-0.707623868615375,4.86941328336244,
15.0878852022365));
#25472=CARTESIAN_POINT('Ctrl Pts',(-0.510448090398453,4.89192180765791,
15.0767457586803));
#25473=CARTESIAN_POINT('Ctrl Pts',(-0.463002097236165,4.89664020013576,
15.0740670574182));
#25474=CARTESIAN_POINT('Ctrl Pts',(-0.351138624602694,4.90612436334394,
15.0677506799311));
#25475=CARTESIAN_POINT('Ctrl Pts',(-0.286681255865129,4.91031244961213,
15.0641104202797));
#25476=CARTESIAN_POINT('Ctrl Pts',(-0.1889158644417,4.91473308812075,15.0585817495178));
#25477=CARTESIAN_POINT('Ctrl Pts',(-0.155656902375431,4.91589884394543,
15.0566996799156));
#25478=CARTESIAN_POINT('Ctrl Pts',(-0.0497141779749854,4.91853600533687,
15.0506991299016));
#25479=CARTESIAN_POINT('Ctrl Pts',(0.0229910128247335,4.91873349373449,
15.0465728768188));
#25480=CARTESIAN_POINT('Ctrl Pts',(0.309195103284661,4.91316499759241,15.0302849580215));
#25481=CARTESIAN_POINT('Ctrl Pts',(0.522217801307229,4.8951075966827,15.0180524220398));
#25482=CARTESIAN_POINT('Ctrl Pts',(0.796076162255547,4.85380933256637,15.0022104074079));
#25483=CARTESIAN_POINT('Ctrl Pts',(0.858576484478969,4.8431445161373,14.9985879502636));
#25484=CARTESIAN_POINT('Ctrl Pts',(0.925706404782001,4.83034937881088,14.994692816851));
#25485=CARTESIAN_POINT('Ctrl Pts',(0.93055796281134,4.82941708150651,14.9944112869345));
#25486=CARTESIAN_POINT('Ctrl Pts',(0.939231455464921,4.82773678882183,14.9939079348186));
#25487=CARTESIAN_POINT('Ctrl Pts',(0.943053920851509,4.82699156115675,14.9936860903007));
#25488=CARTESIAN_POINT('Ctrl Pts',(0.949913265567177,4.8256458048252,14.9932879708419));
#25489=CARTESIAN_POINT('Ctrl Pts',(0.952950469987507,4.8250469476986,14.993111681854));
#25490=CARTESIAN_POINT('Ctrl Pts',(0.958421962559012,4.82396274503491,14.9927940849062));
#25491=CARTESIAN_POINT('Ctrl Pts',(0.960856452080789,4.82347842353463,14.9926527680618));
#25492=CARTESIAN_POINT('Ctrl Pts',(0.965259253631101,4.82259905715617,14.9923971862347));
#25493=CARTESIAN_POINT('Ctrl Pts',(0.967227693368259,4.82220464953539,14.9922829155089));
#25494=CARTESIAN_POINT('Ctrl Pts',(1.00836722016818,4.81393549991612,14.9898946439239));
#25495=CARTESIAN_POINT('Ctrl Pts',(1.04744144416762,4.80558486720289,14.9876250519173));
#25496=CARTESIAN_POINT('Ctrl Pts',(1.12691124076052,4.78758588715078,14.983008701684));
#25497=CARTESIAN_POINT('Ctrl Pts',(1.16729513719841,4.77790013336824,14.9806626573088));
#25498=CARTESIAN_POINT('Ctrl Pts',(1.35837900780964,4.72950290273426,14.9695490535891));
#25499=CARTESIAN_POINT('Ctrl Pts',(1.50731022357342,4.68416569096008,14.9608463206792));
#25500=CARTESIAN_POINT('Ctrl Pts',(1.78653577408412,4.58446563994996,14.9442349258733));
#25501=CARTESIAN_POINT('Ctrl Pts',(1.91713019414159,4.53140667394269,14.9363368902122));
#25502=CARTESIAN_POINT('Ctrl Pts',(2.11059342679835,4.44294255977192,14.9243510297896));
#25503=CARTESIAN_POINT('Ctrl Pts',(2.17525886145283,4.41164277019152,14.9202950287322));
#25504=CARTESIAN_POINT('Ctrl Pts',(2.29550857448917,4.35015184351033,14.9126487942917));
#25505=CARTESIAN_POINT('Ctrl Pts',(2.3512413932859,4.32028291636005,14.9090617196259));
#25506=CARTESIAN_POINT('Ctrl Pts',(2.51455424576044,4.22866218964797,14.8984147557209));
#25507=CARTESIAN_POINT('Ctrl Pts',(2.62039053303689,4.16390679449838,14.8913354672254));
#25508=CARTESIAN_POINT('Ctrl Pts',(2.85075928074599,4.01069230160558,14.8755090150239));
#25509=CARTESIAN_POINT('Ctrl Pts',(2.97385038876209,3.92029276335414,14.8667612607164));
#25510=CARTESIAN_POINT('Ctrl Pts',(3.13500080183473,3.78997825287945,14.8549379330655));
#25511=CARTESIAN_POINT('Ctrl Pts',(3.17688886294378,3.75493574335113,14.8518287712587));
#25512=CARTESIAN_POINT('Ctrl Pts',(3.24614017156926,3.69501335112484,14.8466315121843));
#25513=CARTESIAN_POINT('Ctrl Pts',(3.27382169608558,3.67050966655902,14.8445386299097));
#25514=CARTESIAN_POINT('Ctrl Pts',(3.35158639971549,3.60009272357943,14.83861234241));
#25515=CARTESIAN_POINT('Ctrl Pts',(3.40099823848978,3.55345045945065,14.8347895704619));
#25516=CARTESIAN_POINT('Ctrl Pts',(3.56882243750937,3.38832475601191,14.8215671907573));
#25517=CARTESIAN_POINT('Ctrl Pts',(3.68213777208877,3.26482771307609,14.8122090675872));
#25518=CARTESIAN_POINT('Ctrl Pts',(3.83864222729527,3.07572558306742,14.7984351931569));
#25519=CARTESIAN_POINT('Ctrl Pts',(3.88691737220398,3.01448755211031,14.7940540133454));
#25520=CARTESIAN_POINT('Ctrl Pts',(3.97700759073066,2.8944421789207,14.7855980934248));
#25521=CARTESIAN_POINT('Ctrl Pts',(4.01902464973138,2.83581127907917,14.7815260493546));
#25522=CARTESIAN_POINT('Ctrl Pts',(4.09531859930095,2.72424703808877,14.7738748249614));
#25523=CARTESIAN_POINT('Ctrl Pts',(4.12989655562918,2.67153713894641,14.7702989384917));
#25524=CARTESIAN_POINT('Ctrl Pts',(4.2323031903402,2.50868910725879,14.7593620572437));
#25525=CARTESIAN_POINT('Ctrl Pts',(4.29680831724125,2.39652851182006,14.7519791613104));
#25526=CARTESIAN_POINT('Ctrl Pts',(4.42099862334972,2.15941873270447,14.7366660212109));
#25527=CARTESIAN_POINT('Ctrl Pts',(4.47998218011592,2.0342266189149,14.7287399443678));
#25528=CARTESIAN_POINT('Ctrl Pts',(4.55704840546019,1.85098567951177,14.7173914644622));
#25529=CARTESIAN_POINT('Ctrl Pts',(4.57945725407452,1.79482855427854,14.713946849728));
#25530=CARTESIAN_POINT('Ctrl Pts',(4.61381313348214,1.70389607406004,14.7084273408619));
#25531=CARTESIAN_POINT('Ctrl Pts',(4.62641535144787,1.66937548146195,14.7063456002465));
#25532=CARTESIAN_POINT('Ctrl Pts',(4.65864474379314,1.57792217908994,14.7008651257434));
#25533=CARTESIAN_POINT('Ctrl Pts',(4.67761524571174,1.52076460861603,14.697473964864));
#25534=CARTESIAN_POINT('Ctrl Pts',(4.74513746817459,1.30409089039796,14.6847183390208));
#25535=CARTESIAN_POINT('Ctrl Pts',(4.78661698991098,1.14248893977293,14.6754028564007));
#25536=CARTESIAN_POINT('Ctrl Pts',(4.83054896227543,0.926223646075818,14.6630254441948));
#25537=CARTESIAN_POINT('Ctrl Pts',(4.84041804934139,0.873181873656372,14.6599970701756));
#25538=CARTESIAN_POINT('Ctrl Pts',(4.85603198938666,0.78084104448554,14.6547320573465));
#25539=CARTESIAN_POINT('Ctrl Pts',(4.86217717232046,0.741614819769123,14.6524977115511));
#25540=CARTESIAN_POINT('Ctrl Pts',(4.87805758351715,0.631545966343782,14.6462313082988));
#25541=CARTESIAN_POINT('Ctrl Pts',(4.88672373667603,0.560559597487248,14.6421934984164));
#25542=CARTESIAN_POINT('Ctrl Pts',(4.90015435359788,0.426260617300041,14.6345518132589));
#25543=CARTESIAN_POINT('Ctrl Pts',(4.90524669378877,0.362995268065324,14.6309509389889));
#25544=CARTESIAN_POINT('Ctrl Pts',(4.91991983002028,0.122607504312978,14.6172565010753));
#25545=CARTESIAN_POINT('Ctrl Pts',(4.92114108316411,-0.054887424198698,
14.607114536424));
#25546=CARTESIAN_POINT('Ctrl Pts',(4.90699938991099,-0.354274608169366,
14.5899570621734));
#25547=CARTESIAN_POINT('Ctrl Pts',(4.89666765233485,-0.476235119059623,
14.582954921352));
#25548=CARTESIAN_POINT('Ctrl Pts',(4.87658845447658,-0.640239170016415,
14.5735475710963));
#25549=CARTESIAN_POINT('Ctrl Pts',(4.87082212334513,-0.682724723852563,
14.5711115024601));
#25550=CARTESIAN_POINT('Ctrl Pts',(4.85846037196939,-0.765652988007717,
14.5663607394535));
#25551=CARTESIAN_POINT('Ctrl Pts',(4.85191358511333,-0.8060994299673,14.5640457722358));
#25552=CARTESIAN_POINT('Ctrl Pts',(4.82423595635871,-0.964517263815048,
14.5549774387385));
#25553=CARTESIAN_POINT('Ctrl Pts',(4.79930125580401,-1.08178287533086,14.5482612072467));
#25554=CARTESIAN_POINT('Ctrl Pts',(4.74764075214014,-1.28747716029942,14.5363786954475));
#25555=CARTESIAN_POINT('Ctrl Pts',(4.72266188258935,-1.37628297699634,14.5312144532447));
#25556=CARTESIAN_POINT('Ctrl Pts',(4.67130997176311,-1.54093639258833,14.521538699467));
#25557=CARTESIAN_POINT('Ctrl Pts',(4.64554825003911,-1.6169425208653,14.5170311507592));
#25558=CARTESIAN_POINT('Ctrl Pts',(4.59274637455384,-1.76102935970212,14.5083878893918));
#25559=CARTESIAN_POINT('Ctrl Pts',(4.56602224225133,-1.82920321063417,14.504255288613));
#25560=CARTESIAN_POINT('Ctrl Pts',(4.51047413519662,-1.96209623616906,14.4961033183088));
#25561=CARTESIAN_POINT('Ctrl Pts',(4.48175394993675,-2.02683989049321,14.4920856302962));
#25562=CARTESIAN_POINT('Ctrl Pts',(4.37145646462214,-2.26166503923959,14.4773314762783));
#25563=CARTESIAN_POINT('Ctrl Pts',(4.28151307638783,-2.42763349735151,14.4665411653619));
#25564=CARTESIAN_POINT('Ctrl Pts',(4.12428176406584,-2.68172032387355,14.4494377290776));
#25565=CARTESIAN_POINT('Ctrl Pts',(4.06316829635748,-2.77344330358308,14.4431350604432));
#25566=CARTESIAN_POINT('Ctrl Pts',(3.97431598593088,-2.89755021344921,14.4344456209673));
#25567=CARTESIAN_POINT('Ctrl Pts',(3.94916066269556,-2.93174264066341,14.4320339986259));
#25568=CARTESIAN_POINT('Ctrl Pts',(3.89864010064452,-2.9985825326546,14.4272870171358));
#25569=CARTESIAN_POINT('Ctrl Pts',(3.87329956719775,-3.03124435677622,14.4249515820252));
#25570=CARTESIAN_POINT('Ctrl Pts',(3.75878426363892,-3.17506398316356,14.4145859530099));
#25571=CARTESIAN_POINT('Ctrl Pts',(3.66521417449634,-3.28263558788164,14.4066096849645));
#25572=CARTESIAN_POINT('Ctrl Pts',(3.4597856322612,-3.49905217645652,14.3898932799596));
#25573=CARTESIAN_POINT('Ctrl Pts',(3.34715347526959,-3.6069440766278,14.3811604917817));
#25574=CARTESIAN_POINT('Ctrl Pts',(3.1756513158615,-3.75626630357179,14.3683470296151));
#25575=CARTESIAN_POINT('Ctrl Pts',(3.12069587316908,-3.80204615116858,14.3643085513225));
#25576=CARTESIAN_POINT('Ctrl Pts',(3.00816898366336,-3.89170121455556,14.3561625797643));
#25577=CARTESIAN_POINT('Ctrl Pts',(2.95058809868431,-3.93553664516097,14.3520558245999));
#25578=CARTESIAN_POINT('Ctrl Pts',(2.75733673926691,-4.07603006696622,14.3384623951906));
#25579=CARTESIAN_POINT('Ctrl Pts',(2.61772477701156,-4.16706644472577,14.3289375410327));
#25580=CARTESIAN_POINT('Ctrl Pts',(2.3621257258463,-4.31581157348355,14.3120085078497));
#25581=CARTESIAN_POINT('Ctrl Pts',(2.24796863116282,-4.3763575134295,14.3046159265916));
#25582=CARTESIAN_POINT('Ctrl Pts',(2.09462667935548,-4.45010131085714,14.2949326978781));
#25583=CARTESIAN_POINT('Ctrl Pts',(2.05747253308808,-4.46740074727395,14.2926051349198));
#25584=CARTESIAN_POINT('Ctrl Pts',(1.98102911978013,-4.50183780292758,14.2878563980824));
#25585=CARTESIAN_POINT('Ctrl Pts',(1.9417232822473,-4.51893026389814,14.285435889093));
#25586=CARTESIAN_POINT('Ctrl Pts',(1.79025517599162,-4.58245622716335,14.2761784011427));
#25587=CARTESIAN_POINT('Ctrl Pts',(1.67661061729344,-4.62524551824978,14.269377716539));
#25588=CARTESIAN_POINT('Ctrl Pts',(1.39821166820359,-4.71845723479997,14.2529295952357));
#25589=CARTESIAN_POINT('Ctrl Pts',(1.23216788117661,-4.7645142409005,14.2432907464544));
#25590=CARTESIAN_POINT('Ctrl Pts',(0.994022976208555,-4.81728620218662,
14.22954702831));
#25591=CARTESIAN_POINT('Ctrl Pts',(0.923662793841521,-4.83127052836926,
14.2254968781382));
#25592=CARTESIAN_POINT('Ctrl Pts',(0.790681066175808,-4.85468984663343,
14.217852242124));
#25593=CARTESIAN_POINT('Ctrl Pts',(0.728133919774229,-4.8644640958365,14.2142608648231));
#25594=CARTESIAN_POINT('Ctrl Pts',(0.509433634148416,-4.89432779897977,
14.2017104175261));
#25595=CARTESIAN_POINT('Ctrl Pts',(0.352520395140321,-4.90812545059303,
14.1927150911721));
#25596=CARTESIAN_POINT('Ctrl Pts',(0.0928914124104607,-4.91843893486339,
14.1778422065908));
#25597=CARTESIAN_POINT('Ctrl Pts',(-0.00953775875027473,-4.91930681469287,
14.1719782192377));
#25598=CARTESIAN_POINT('Ctrl Pts',(-0.176232658199517,-4.91551253107512,
14.1624557606317));
#25599=CARTESIAN_POINT('Ctrl Pts',(-0.24051152815045,-4.91278696288025,
14.1587889954078));
#25600=CARTESIAN_POINT('Ctrl Pts',(-0.341465524313964,-4.90652013900496,
14.153044064287));
#25601=CARTESIAN_POINT('Ctrl Pts',(-0.378185470144098,-4.9038265033064,
14.1509576793653));
#25602=CARTESIAN_POINT('Ctrl Pts',(-0.470245499078712,-4.89603312990407,
14.1457344427815));
#25603=CARTESIAN_POINT('Ctrl Pts',(-0.525535858177351,-4.89040728429077,
14.1426033702849));
#25604=CARTESIAN_POINT('Ctrl Pts',(-0.699771565341797,-4.86968958182358,
14.1327367000703));
#25605=CARTESIAN_POINT('Ctrl Pts',(-0.818267044930069,-4.85118503882439,
14.1260260387463));
#25606=CARTESIAN_POINT('Ctrl Pts',(-1.08092201190979,-4.80026996932733,
14.1110370925674));
#25607=CARTESIAN_POINT('Ctrl Pts',(-1.224535363853,-4.76565804401943,14.1027622716073));
#25608=CARTESIAN_POINT('Ctrl Pts',(-1.4350219756809,-4.70478500022798,14.0904155433134));
#25609=CARTESIAN_POINT('Ctrl Pts',(-1.50322999118492,-4.68343777668757,
14.0863801046689));
#25610=CARTESIAN_POINT('Ctrl Pts',(-1.63111898051464,-4.64033035671548,
14.0787389178572));
#25611=CARTESIAN_POINT('Ctrl Pts',(-1.6908910222866,-4.61888540529683,14.0751361497508));
#25612=CARTESIAN_POINT('Ctrl Pts',(-1.88919159463853,-4.5433741146259,14.0630703354164));
#25613=CARTESIAN_POINT('Ctrl Pts',(-2.02567973927464,-4.48418485568739,
14.0545760199992));
#25614=CARTESIAN_POINT('Ctrl Pts',(-2.25581450273617,-4.37173069560083,
14.039915868712));
#25615=CARTESIAN_POINT('Ctrl Pts',(-2.35078270411255,-4.32140592306065,
14.0337623156356));
#25616=CARTESIAN_POINT('Ctrl Pts',(-2.4718918946353,-4.25205416570508,14.0257908032886));
#25617=CARTESIAN_POINT('Ctrl Pts',(-2.49960051909974,-4.23582476344418,
14.0239583660017));
#25618=CARTESIAN_POINT('Ctrl Pts',(-2.56820626010293,-4.19473362262961,
14.0194007353132));
#25619=CARTESIAN_POINT('Ctrl Pts',(-2.60890341005437,-4.16954393542025,
14.0166786647914));
#25620=CARTESIAN_POINT('Ctrl Pts',(-2.68105442388414,-4.12341573176651,
14.0118224184637));
#25621=CARTESIAN_POINT('Ctrl Pts',(-2.71264653822793,-4.10270141552781,
14.0096857753031));
#25622=CARTESIAN_POINT('Ctrl Pts',(-2.80417192856449,-4.04117067190184,
14.0034607422161));
#25623=CARTESIAN_POINT('Ctrl Pts',(-2.86344521181984,-3.99939024292269,
13.9993843895584));
#25624=CARTESIAN_POINT('Ctrl Pts',(-3.07821041810672,-3.84078421340153,
13.9844000891049));
#25625=CARTESIAN_POINT('Ctrl Pts',(-3.22765704651937,-3.71607759864433,
13.9735408567487));
#25626=CARTESIAN_POINT('Ctrl Pts',(-3.39857898786815,-3.5553419469705,13.960351819487));
#25627=CARTESIAN_POINT('Ctrl Pts',(-3.42749312580402,-3.5274759171243,13.9580923181677));
#25628=CARTESIAN_POINT('Ctrl Pts',(-3.50722629172008,-3.44872701203439,
13.9517783021545));
#25629=CARTESIAN_POINT('Ctrl Pts',(-3.55727508185132,-3.39707934848813,
13.9477180397646));
#25630=CARTESIAN_POINT('Ctrl Pts',(-3.64913066212785,-3.29803266101072,
13.9400705646552));
#25631=CARTESIAN_POINT('Ctrl Pts',(-3.69119151542172,-3.250888972088,13.936486546888));
#25632=CARTESIAN_POINT('Ctrl Pts',(-3.88119892905612,-3.02947710740625,
13.9198979898087));
#25633=CARTESIAN_POINT('Ctrl Pts',(-4.01778910762865,-2.84583988030193,
13.9068045571363));
#25634=CARTESIAN_POINT('Ctrl Pts',(-4.18806747750911,-2.58008719510037,
13.8887524405794));
#25635=CARTESIAN_POINT('Ctrl Pts',(-4.23307218809573,-2.5055656573129,13.8837821235464));
#25636=CARTESIAN_POINT('Ctrl Pts',(-4.2949440057624,-2.39668469936246,13.8766619844641));
#25637=CARTESIAN_POINT('Ctrl Pts',(-4.31342491676308,-2.36326196377785,
13.8744951841325));
#25638=CARTESIAN_POINT('Ctrl Pts',(-4.3542885155946,-2.28728358244348,13.8696130843376));
#25639=CARTESIAN_POINT('Ctrl Pts',(-4.37644020850545,-2.2446081708195,13.8669006772187));
#25640=CARTESIAN_POINT('Ctrl Pts',(-4.48547124543402,-2.0268068973371,13.8531873992869));
#25641=CARTESIAN_POINT('Ctrl Pts',(-4.56248031474317,-1.84693614833202,
13.8422764251408));
#25642=CARTESIAN_POINT('Ctrl Pts',(-4.65571196738907,-1.58744080420424,
13.8268078632914));
#25643=CARTESIAN_POINT('Ctrl Pts',(-4.68099178131023,-1.51127033133288,
13.8223001719689));
#25644=CARTESIAN_POINT('Ctrl Pts',(-4.7257520109773,-1.36448223827827,13.8136566988981));
#25645=CARTESIAN_POINT('Ctrl Pts',(-4.74554076291879,-1.29398089287288,
13.8095240295042));
#25646=CARTESIAN_POINT('Ctrl Pts',(-4.78135935675284,-1.15447006748005,
13.8013720427921));
#25647=CARTESIAN_POINT('Ctrl Pts',(-4.79748684961141,-1.08550366564466,
13.7973544076187));
#25648=CARTESIAN_POINT('Ctrl Pts',(-4.85109117423788,-0.831668844096764,
13.7826005696829));
#25649=CARTESIAN_POINT('Ctrl Pts',(-4.87941431400663,-0.645037090594373,
13.771810524382));
#25650=CARTESIAN_POINT('Ctrl Pts',(-4.90719367347956,-0.34752809249043,
13.7547069432821));
#25651=CARTESIAN_POINT('Ctrl Pts',(-4.9137481104115,-0.237498272426668,
13.7484038677095));
#25652=CARTESIAN_POINT('Ctrl Pts',(-4.91770023727319,-0.0849072196384362,
13.7397139808591));
#25653=CARTESIAN_POINT('Ctrl Pts',(-4.91824988907269,-0.042461084205414,
13.7373023151503));
#25654=CARTESIAN_POINT('Ctrl Pts',(-4.91825010801743,0.0413238316877421,
13.7325553282673));
#25655=CARTESIAN_POINT('Ctrl Pts',(-4.91772907888801,0.0826591704296608,
13.7302199307599));
#25656=CARTESIAN_POINT('Ctrl Pts',(-4.91311046343467,0.265815186267638,
13.7198896887542));
#25657=CARTESIAN_POINT('Ctrl Pts',(-4.90339839974557,0.407427507211956,
13.7119482571227));
#25658=CARTESIAN_POINT('Ctrl Pts',(-4.87072741108792,0.698593346091473,
13.6955342622679));
#25659=CARTESIAN_POINT('Ctrl Pts',(-4.84696531171142,0.847906089698089,
13.68706901625));
#25660=CARTESIAN_POINT('Ctrl Pts',(-4.80162648412878,1.06717652952238,13.674456396872));
#25661=CARTESIAN_POINT('Ctrl Pts',(-4.78530484911705,1.13813003537015,13.670346976507));
#25662=CARTESIAN_POINT('Ctrl Pts',(-4.7662939684885,1.21311403254434,13.6659684627439));
#25663=CARTESIAN_POINT('Ctrl Pts',(-4.76516734420597,1.2175319425333,13.6657103575944));
#25664=CARTESIAN_POINT('Ctrl Pts',(-4.76403458702644,1.22194824608729,13.6654522135017));
#25665=CARTESIAN_POINT('',(-4.9182499639856,0.000107902101101913,13.389740414873));
#25666=CARTESIAN_POINT('Ctrl Pts',(-4.76403458795361,1.2219482424725,13.3199864568809));
#25667=CARTESIAN_POINT('Ctrl Pts',(-4.79152982453573,1.11475200164307,13.3263211013333));
#25668=CARTESIAN_POINT('Ctrl Pts',(-4.81540061011838,1.00665267818612,13.3326514556104));
#25669=CARTESIAN_POINT('Ctrl Pts',(-4.84333424286708,0.856206246615081,
13.3413619657047));
#25670=CARTESIAN_POINT('Ctrl Pts',(-4.8505256393311,0.814479467250247,13.3437672638303));
#25671=CARTESIAN_POINT('Ctrl Pts',(-4.86234930437609,0.740152742923929,
13.348030828943));
#25672=CARTESIAN_POINT('Ctrl Pts',(-4.86719468058729,0.707589435507746,
13.349891635032));
#25673=CARTESIAN_POINT('Ctrl Pts',(-4.87790924393894,0.630256336248681,
13.3542969718298));
#25674=CARTESIAN_POINT('Ctrl Pts',(-4.88348959718709,0.585449439817111,
13.3568385040052));
#25675=CARTESIAN_POINT('Ctrl Pts',(-4.90829832212776,0.361101322043394,
13.3695249524841));
#25676=CARTESIAN_POINT('Ctrl Pts',(-4.91824603641982,0.180673647320878,
13.3796082680788));
#25677=CARTESIAN_POINT('Ctrl Pts',(-4.9182499988158,0.000107927761981499,
13.3897403530557));
#25678=CARTESIAN_POINT('Ctrl Pts',(-4.91824999881644,0.000107898724551486,
13.3897403546851));
#25679=CARTESIAN_POINT('Ctrl Pts',(-4.91825167684014,-0.0763799386656473,
13.3940323170261));
#25680=CARTESIAN_POINT('Ctrl Pts',(-4.91646906583336,-0.15285694645591,
13.3983302366743));
#25681=CARTESIAN_POINT('Ctrl Pts',(-4.91001074095604,-0.291254482407087,
13.4061352017772));
#25682=CARTESIAN_POINT('Ctrl Pts',(-4.90594467761584,-0.35318744316204,
13.4096377748873));
#25683=CARTESIAN_POINT('Ctrl Pts',(-4.89494492677524,-0.483074502355274,
13.4170111961256));
#25684=CARTESIAN_POINT('Ctrl Pts',(-4.8877655020059,-0.550994617529353,
13.4208829302558));
#25685=CARTESIAN_POINT('Ctrl Pts',(-4.86450147179037,-0.734446094391615,
13.4313920786582));
#25686=CARTESIAN_POINT('Ctrl Pts',(-4.84571793790796,-0.849589751411313,
13.4380446593507));
#25687=CARTESIAN_POINT('Ctrl Pts',(-4.79065510034131,-1.12508000809426,
13.4541086330826));
#25688=CARTESIAN_POINT('Ctrl Pts',(-4.75039660083467,-1.28448963101816,
13.463527966129));
#25689=CARTESIAN_POINT('Ctrl Pts',(-4.68788270764438,-1.48840065142926,
13.4756982410256));
#25690=CARTESIAN_POINT('Ctrl Pts',(-4.67283171583888,-1.53499987073122,
13.4784875724753));
#25691=CARTESIAN_POINT('Ctrl Pts',(-4.65053790541573,-1.60065460487296,
13.482426666588));
#25692=CARTESIAN_POINT('Ctrl Pts',(-4.64386874711576,-1.61990155255968,
13.48358254593));
#25693=CARTESIAN_POINT('Ctrl Pts',(-4.62347926261925,-1.67758399694161,
13.4870496256959));
#25694=CARTESIAN_POINT('Ctrl Pts',(-4.60939991912805,-1.71589072615071,
13.4893558539465));
#25695=CARTESIAN_POINT('Ctrl Pts',(-4.5261082748265,-1.93408243881794,13.5025270970803));
#25696=CARTESIAN_POINT('Ctrl Pts',(-4.4468452647102,-2.10995259746291,13.5132880098638));
#25697=CARTESIAN_POINT('Ctrl Pts',(-4.31644468592308,-2.35909164841149,
13.5290526275224));
#25698=CARTESIAN_POINT('Ctrl Pts',(-4.27331709678737,-2.43634335335123,
13.5340171366736));
#25699=CARTESIAN_POINT('Ctrl Pts',(-4.18920906058899,-2.57788976488181,
13.5432837659071));
#25700=CARTESIAN_POINT('Ctrl Pts',(-4.1487717313446,-2.6424763260761,13.5475809455948));
#25701=CARTESIAN_POINT('Ctrl Pts',(-4.09953687364169,-2.71719656609823,
13.5526420140313));
#25702=CARTESIAN_POINT('Ctrl Pts',(-4.09217809235758,-2.72826652227305,
13.5533941747566));
#25703=CARTESIAN_POINT('Ctrl Pts',(-4.04436873689368,-2.79955844896837,
13.5582535958301));
#25704=CARTESIAN_POINT('Ctrl Pts',(-4.0026351141331,-2.85890852711016,13.5623704663148));
#25705=CARTESIAN_POINT('Ctrl Pts',(-3.84429597690079,-3.07381871272004,
13.5775565338341));
#25706=CARTESIAN_POINT('Ctrl Pts',(-3.71981129866037,-3.2233484383157,13.588682511825));
#25707=CARTESIAN_POINT('Ctrl Pts',(-3.53527975622997,-3.42003676189591,
13.6041182160004));
#25708=CARTESIAN_POINT('Ctrl Pts',(-3.48249813626058,-3.47376758806334,
13.6084251910664));
#25709=CARTESIAN_POINT('Ctrl Pts',(-3.41728831465045,-3.53716953412255,
13.6136134101297));
#25710=CARTESIAN_POINT('Ctrl Pts',(-3.40602131359527,-3.54802008899062,
13.6145051864753));
#25711=CARTESIAN_POINT('Ctrl Pts',(-3.38485597629069,-3.56820939165594,
13.6161716619043));
#25712=CARTESIAN_POINT('Ctrl Pts',(-3.37497027398729,-3.5775611656746,13.6169464986052));
#25713=CARTESIAN_POINT('Ctrl Pts',(-3.33637466750735,-3.61376987147128,
13.6199578093061));
#25714=CARTESIAN_POINT('Ctrl Pts',(-3.30738174804376,-3.64032342379345,
13.6221904160358));
#25715=CARTESIAN_POINT('Ctrl Pts',(-3.24587957686131,-3.69530969391984,
13.6268631931859));
#25716=CARTESIAN_POINT('Ctrl Pts',(-3.21330784644957,-3.7236676414984,13.6293020715046));
#25717=CARTESIAN_POINT('Ctrl Pts',(-3.08799235205111,-3.82990229979522,
13.6385614161177));
#25718=CARTESIAN_POINT('Ctrl Pts',(-2.99275635837726,-3.90477379187308,
13.6453458424578));
#25719=CARTESIAN_POINT('Ctrl Pts',(-2.79778048407332,-4.04673024076732,
13.6588575155489));
#25720=CARTESIAN_POINT('Ctrl Pts',(-2.69815245378672,-4.11382721956924,
13.6655802357866));
#25721=CARTESIAN_POINT('Ctrl Pts',(-2.53629175635438,-4.21442492263593,
13.67628661483));
#25722=CARTESIAN_POINT('Ctrl Pts',(-2.47562131498319,-4.25034731283924,
13.6802536849865));
#25723=CARTESIAN_POINT('Ctrl Pts',(-2.36077563782384,-4.31505291208773,
13.6876894879155));
#25724=CARTESIAN_POINT('Ctrl Pts',(-2.3067933150796,-4.34415098126529,13.6911551754821));
#25725=CARTESIAN_POINT('Ctrl Pts',(-2.20147004863784,-4.39840648330201,
13.6978662588447));
#25726=CARTESIAN_POINT('Ctrl Pts',(-2.15020660081262,-4.4236931923424,13.7011101170813));
#25727=CARTESIAN_POINT('Ctrl Pts',(-1.89814084748495,-4.54261271615078,
13.7169587793334));
#25728=CARTESIAN_POINT('Ctrl Pts',(-1.69161061391552,-4.62349651050588,
13.7296472781057));
#25729=CARTESIAN_POINT('Ctrl Pts',(-1.41878230508698,-4.70960786143244,
13.7460133686137));
#25730=CARTESIAN_POINT('Ctrl Pts',(-1.35685119317719,-4.72782237097062,
13.7497018956835));
#25731=CARTESIAN_POINT('Ctrl Pts',(-1.28983706931227,-4.74610656846844,
13.7536614541681));
#25732=CARTESIAN_POINT('Ctrl Pts',(-1.28509297043751,-4.74739331444389,
13.7539415908372));
#25733=CARTESIAN_POINT('Ctrl Pts',(-1.27739115853274,-4.7494698927789,13.7543960998104));
#25734=CARTESIAN_POINT('Ctrl Pts',(-1.27443462499064,-4.75026407907514,
13.7545705077718));
#25735=CARTESIAN_POINT('Ctrl Pts',(-1.26959724492533,-4.7515586586024,13.7548557584355));
#25736=CARTESIAN_POINT('Ctrl Pts',(-1.26771684027733,-4.75206069651287,
13.7549666150422));
#25737=CARTESIAN_POINT('Ctrl Pts',(-1.26134542427597,-4.75375771156918,
13.7553421407173));
#25738=CARTESIAN_POINT('Ctrl Pts',(-1.25685301481277,-4.7549474401786,13.7556067642878));
#25739=CARTESIAN_POINT('Ctrl Pts',(-1.24851063560456,-4.75714411084994,
13.7560978782762));
#25740=CARTESIAN_POINT('Ctrl Pts',(-1.24466111765875,-4.75815275089392,
13.7563243838259));
#25741=CARTESIAN_POINT('Ctrl Pts',(-1.23744085063474,-4.76003522352121,
13.7567490074312));
#25742=CARTESIAN_POINT('Ctrl Pts',(-1.23407038991793,-4.76091015045831,
13.7569471356054));
#25743=CARTESIAN_POINT('Ctrl Pts',(-1.22767839732198,-4.76256218319146,
13.7573227117195));
#25744=CARTESIAN_POINT('Ctrl Pts',(-1.22465704994484,-4.76333999479953,
13.7575001663877));
#25745=CARTESIAN_POINT('Ctrl Pts',(-1.2188560312492,-4.76482751711196,13.7578407431331));
#25746=CARTESIAN_POINT('Ctrl Pts',(-1.21607647457035,-4.76553767173865,
13.7580038695869));
#25747=CARTESIAN_POINT('Ctrl Pts',(-1.17810901508679,-4.77520267514886,
13.7602312663522));
#25748=CARTESIAN_POINT('Ctrl Pts',(-1.14282330999256,-4.78377010052902,
13.7622914801498));
#25749=CARTESIAN_POINT('Ctrl Pts',(-1.06132250591924,-4.80260539293934,
13.7670260945994));
#25750=CARTESIAN_POINT('Ctrl Pts',(-1.01504754666644,-4.81259831828243,
13.7696972571044));
#25751=CARTESIAN_POINT('Ctrl Pts',(-0.778096397923194,-4.86019743631449,
13.7833069896748));
#25752=CARTESIAN_POINT('Ctrl Pts',(-0.585454902308647,-4.88714610008783,
13.7941546640719));
#25753=CARTESIAN_POINT('Ctrl Pts',(-0.310146395291452,-4.90914347106024,
13.8096463835072));
#25754=CARTESIAN_POINT('Ctrl Pts',(-0.228419649536216,-4.91362439589162,
13.8142427851226));
#25755=CARTESIAN_POINT('Ctrl Pts',(-0.0791857700927101,-4.91807523946254,
13.8226508858267));
#25756=CARTESIAN_POINT('Ctrl Pts',(-0.0117180612027642,-4.91869871070011,
13.8264576754604));
#25757=CARTESIAN_POINT('Ctrl Pts',(0.124214317225545,-4.91715803250257,
13.8341474528072));
#25758=CARTESIAN_POINT('Ctrl Pts',(0.192663803526632,-4.91495196630278,
13.8380298875709));
#25759=CARTESIAN_POINT('Ctrl Pts',(0.266391232003425,-4.91103323587466,
13.8422259323727));
#25760=CARTESIAN_POINT('Ctrl Pts',(0.271737637686643,-4.91074030962273,
13.8425302921144));
#25761=CARTESIAN_POINT('Ctrl Pts',(0.407452139301232,-4.90308228582337,
13.8502582950425));
#25762=CARTESIAN_POINT('Ctrl Pts',(0.537474600852064,-4.89053713533766,
13.8577121558279));
#25763=CARTESIAN_POINT('Ctrl Pts',(0.787850148485951,-4.8562735094596,13.8721702823118));
#25764=CARTESIAN_POINT('Ctrl Pts',(0.908199539499136,-4.83521188070644,
13.8791672957652));
#25765=CARTESIAN_POINT('Ctrl Pts',(1.07806004082689,-4.79891944565424,13.8890920948371));
#25766=CARTESIAN_POINT('Ctrl Pts',(1.12830789870454,-4.78735445175538,13.8920340634327));
#25767=CARTESIAN_POINT('Ctrl Pts',(1.21961214443693,-4.76482258068863,13.8973876523161));
#25768=CARTESIAN_POINT('Ctrl Pts',(1.26072609942754,-4.75410956609177,13.8998012603206));
#25769=CARTESIAN_POINT('Ctrl Pts',(1.34240134477714,-4.73169350138373,13.9045994178986));
#25770=CARTESIAN_POINT('Ctrl Pts',(1.38296111953067,-4.71999823707557,13.9069838328906));
#25771=CARTESIAN_POINT('Ctrl Pts',(1.52760397872074,-4.67626646246126,13.9155025597058));
#25772=CARTESIAN_POINT('Ctrl Pts',(1.63076795574651,-4.64129704871887,13.9216078980534));
#25773=CARTESIAN_POINT('Ctrl Pts',(1.8831769820695,-4.54628243089763,13.9367201673611));
#25774=CARTESIAN_POINT('Ctrl Pts',(2.03079746610144,-4.48228743133347,13.9457161475407));
#25775=CARTESIAN_POINT('Ctrl Pts',(2.24679134505054,-4.37578744044238,13.9592639295677));
#25776=CARTESIAN_POINT('Ctrl Pts',(2.31769074753595,-4.33865145698193,13.9637754762328));
#25777=CARTESIAN_POINT('Ctrl Pts',(2.44790634338457,-4.26634359762335,13.9721974292407));
#25778=CARTESIAN_POINT('Ctrl Pts',(2.50745034939835,-4.23162211926783,13.9761034130744));
#25779=CARTESIAN_POINT('Ctrl Pts',(2.66219535798669,-4.13697349897558,13.9864089269786));
#25780=CARTESIAN_POINT('Ctrl Pts',(2.75610371220013,-4.07501235200957,13.992821864936));
#25781=CARTESIAN_POINT('Ctrl Pts',(2.96457023488572,-3.92696034325726,14.0074375041001));
#25782=CARTESIAN_POINT('Ctrl Pts',(3.07765815487796,-3.83897309257753,14.0156442773939));
#25783=CARTESIAN_POINT('Ctrl Pts',(3.22859322960071,-3.71057777133043,14.0269712122641));
#25784=CARTESIAN_POINT('Ctrl Pts',(3.26984242678359,-3.67427982259964,14.0301076505254));
#25785=CARTESIAN_POINT('Ctrl Pts',(3.34323108869436,-3.60748537275188,14.0357590267355));
#25786=CARTESIAN_POINT('Ctrl Pts',(3.37558320074343,-3.57723118394673,14.0382763222217));
#25787=CARTESIAN_POINT('Ctrl Pts',(3.43299790162759,-3.5220670893688,14.0427885685707));
#25788=CARTESIAN_POINT('Ctrl Pts',(3.45820889755284,-3.49731645990656,14.0447858234373));
#25789=CARTESIAN_POINT('Ctrl Pts',(3.53756531648004,-3.41771195653865,14.0511286036384));
#25790=CARTESIAN_POINT('Ctrl Pts',(3.59068931290156,-3.36185571740985,14.0554596100534));
#25791=CARTESIAN_POINT('Ctrl Pts',(3.7679623734281,-3.16646762567048,14.0702613358484));
#25792=CARTESIAN_POINT('Ctrl Pts',(3.88546620096534,-3.02112726447142,14.0806924494521));
#25793=CARTESIAN_POINT('Ctrl Pts',(4.01807730624421,-2.83652639417858,14.0934686204313));
#25794=CARTESIAN_POINT('Ctrl Pts',(4.04132615609887,-2.80330342629285,14.0957501345275));
#25795=CARTESIAN_POINT('Ctrl Pts',(4.10503251732457,-2.7098261982146,14.1021234083423));
#25796=CARTESIAN_POINT('Ctrl Pts',(4.14457086811401,-2.64895869173633,14.1062210145287));
#25797=CARTESIAN_POINT('Ctrl Pts',(4.21633100668064,-2.53294523728996,14.1139438579367));
#25798=CARTESIAN_POINT('Ctrl Pts',(4.24885390645133,-2.47800304702044,14.1175658497177));
#25799=CARTESIAN_POINT('Ctrl Pts',(4.3341246529263,-2.32733527915788,14.1274096044594));
#25800=CARTESIAN_POINT('Ctrl Pts',(4.38476603186628,-2.23046013350441,14.1336445153872));
#25801=CARTESIAN_POINT('Ctrl Pts',(4.49116297592678,-2.00927325328605,14.1476792493686));
#25802=CARTESIAN_POINT('Ctrl Pts',(4.54506679379011,-1.8841687036833,14.1554814282547));
#25803=CARTESIAN_POINT('Ctrl Pts',(4.61295638002113,-1.70666898952153,14.1663430833198));
#25804=CARTESIAN_POINT('Ctrl Pts',(4.63137469552708,-1.65603565853215,14.1694182335561));
#25805=CARTESIAN_POINT('Ctrl Pts',(4.66322840388901,-1.56377620851263,14.1749760779869));
#25806=CARTESIAN_POINT('Ctrl Pts',(4.67694753568088,-1.52225391618948,14.1774610117201));
#25807=CARTESIAN_POINT('Ctrl Pts',(4.70249312506016,-1.44133038089155,14.1822696488373));
#25808=CARTESIAN_POINT('Ctrl Pts',(4.71438258399559,-1.40195283541347,14.1845938005728));
#25809=CARTESIAN_POINT('Ctrl Pts',(4.7556809245083,-1.25870389093789,14.193000727328));
#25810=CARTESIAN_POINT('Ctrl Pts',(4.78216222984586,-1.15401968430612,14.1990541949692));
#25811=CARTESIAN_POINT('Ctrl Pts',(4.82757093079337,-0.945925394577104,
14.2109896915945));
#25812=CARTESIAN_POINT('Ctrl Pts',(4.84667113820963,-0.842611869243496,
14.2168688388425));
#25813=CARTESIAN_POINT('Ctrl Pts',(4.87453826802848,-0.659194625513001,
14.2272764926467));
#25814=CARTESIAN_POINT('Ctrl Pts',(4.88467270559163,-0.579338656424719,
14.2317977431269));
#25815=CARTESIAN_POINT('Ctrl Pts',(4.90031603341352,-0.426034303383812,
14.2404774828004));
#25816=CARTESIAN_POINT('Ctrl Pts',(4.90614382516365,-0.352640120360553,
14.2446328739957));
#25817=CARTESIAN_POINT('Ctrl Pts',(4.91390970225144,-0.216033067373404,
14.2523774234397));
#25818=CARTESIAN_POINT('Ctrl Pts',(4.916280361264,-0.152859893171549,14.2559628585982));
#25819=CARTESIAN_POINT('Ctrl Pts',(4.9199760899503,0.0498357403372268,14.2674870649977));
#25820=CARTESIAN_POINT('Ctrl Pts',(4.91658265046109,0.189373944499596,14.2754527703436));
#25821=CARTESIAN_POINT('Ctrl Pts',(4.89868946124453,0.456606728287852,14.2907784952849));
#25822=CARTESIAN_POINT('Ctrl Pts',(4.88510979815556,0.584252151718793,14.2981296696833));
#25823=CARTESIAN_POINT('Ctrl Pts',(4.85758054794787,0.772622145415723,14.3089992894859));
#25824=CARTESIAN_POINT('Ctrl Pts',(4.84744567471641,0.8338491015791,14.3125353958361));
#25825=CARTESIAN_POINT('Ctrl Pts',(4.82940046101154,0.931371209801383,14.3181672661824));
#25826=CARTESIAN_POINT('Ctrl Pts',(4.82223300428199,0.967796485959617,14.3202703654164));
#25827=CARTESIAN_POINT('Ctrl Pts',(4.80230443987185,1.06335025786377,14.3257873640336));
#25828=CARTESIAN_POINT('Ctrl Pts',(4.78886373653931,1.12233058794211,14.3291936642752));
#25829=CARTESIAN_POINT('Ctrl Pts',(4.7330112354986,1.34811195991372,14.3422659123206));
#25830=CARTESIAN_POINT('Ctrl Pts',(4.68294354155497,1.51289178801349,14.3518793025374));
#25831=CARTESIAN_POINT('Ctrl Pts',(4.59676063163994,1.75086711670799,14.3660772891082));
#25832=CARTESIAN_POINT('Ctrl Pts',(4.56730259648165,1.82633260776676,14.3706271284036));
#25833=CARTESIAN_POINT('Ctrl Pts',(4.50744455649639,1.96915777886446,14.3793492147358));
#25834=CARTESIAN_POINT('Ctrl Pts',(4.47736382856672,2.03662754716905,14.3835182675823));
#25835=CARTESIAN_POINT('Ctrl Pts',(4.4151537895079,2.16811593788381,14.3917511419207));
#25836=CARTESIAN_POINT('Ctrl Pts',(4.38312283903101,2.23216122245357,14.3958132835056));
#25837=CARTESIAN_POINT('Ctrl Pts',(4.29749198320441,2.39442287078337,14.4062479162397));
#25838=CARTESIAN_POINT('Ctrl Pts',(4.24191857735035,2.49155063080567,14.4126323139129));
#25839=CARTESIAN_POINT('Ctrl Pts',(4.11393508689775,2.69851932422035,14.4265496039859));
#25840=CARTESIAN_POINT('Ctrl Pts',(4.04033193021224,2.80752317116742,14.4340826076938));
#25841=CARTESIAN_POINT('Ctrl Pts',(3.91918160854877,2.97229436234543,14.4457707064155));
#25842=CARTESIAN_POINT('Ctrl Pts',(3.87460714634799,3.03017126784096,14.4499373391271));
#25843=CARTESIAN_POINT('Ctrl Pts',(3.80518636244167,3.11627186704895,14.456222031481));
#25844=CARTESIAN_POINT('Ctrl Pts',(3.78127862387289,3.1452385642401,14.4583514554826));
#25845=CARTESIAN_POINT('Ctrl Pts',(3.72332042997619,3.21384479995823,14.4634309502287));
#25846=CARTESIAN_POINT('Ctrl Pts',(3.68896546622392,3.2532210658755,14.4663766007021));
#25847=CARTESIAN_POINT('Ctrl Pts',(3.54451708046733,3.41355095922362,14.4785177337017));
#25848=CARTESIAN_POINT('Ctrl Pts',(3.42905137901958,3.52952389101047,14.4876572778858));
#25849=CARTESIAN_POINT('Ctrl Pts',(3.24183141359206,3.69969090859694,14.5018398398606));
#25850=CARTESIAN_POINT('Ctrl Pts',(3.17401212538648,3.75803546698278,14.506859228625));
#25851=CARTESIAN_POINT('Ctrl Pts',(3.04422743507703,3.86366791659541,14.5162764161599));
#25852=CARTESIAN_POINT('Ctrl Pts',(2.98265577040692,3.91139550659128,14.5206693664105));
#25853=CARTESIAN_POINT('Ctrl Pts',(2.86466892410699,3.99844710003593,14.5289624882789));
#25854=CARTESIAN_POINT('Ctrl Pts',(2.80851181943608,4.03808970603537,14.5328589103162));
#25855=CARTESIAN_POINT('Ctrl Pts',(2.64790614046063,4.14649369033188,14.5438701153153));
#25856=CARTESIAN_POINT('Ctrl Pts',(2.54164079857574,4.21246700050306,14.5510036427974));
#25857=CARTESIAN_POINT('Ctrl Pts',(2.31910268857065,4.33913758507798,14.565648729108));
#25858=CARTESIAN_POINT('Ctrl Pts',(2.20268208430339,4.39937994741953,14.5731563332335));
#25859=CARTESIAN_POINT('Ctrl Pts',(2.01793802303975,4.48580289828152,14.584812487278));
#25860=CARTESIAN_POINT('Ctrl Pts',(1.95120111566569,4.51523154515605,14.5889725340172));
#25861=CARTESIAN_POINT('Ctrl Pts',(1.84914731351935,4.55754838781354,14.5952502862206));
#25862=CARTESIAN_POINT('Ctrl Pts',(1.81429686836374,4.57153366199735,14.5973793125899));
#25863=CARTESIAN_POINT('Ctrl Pts',(1.73053078028478,4.60403971244273,14.6024611196625));
#25864=CARTESIAN_POINT('Ctrl Pts',(1.68147320643391,4.62218199592597,14.6054094616593));
#25865=CARTESIAN_POINT('Ctrl Pts',(1.47781971552132,4.69382490516186,14.6175552550523));
#25866=CARTESIAN_POINT('Ctrl Pts',(1.32089082730505,4.74037883982954,14.6266968022821));
#25867=CARTESIAN_POINT('Ctrl Pts',(1.07507022033003,4.80014565813485,14.6408784934936));
#25868=CARTESIAN_POINT('Ctrl Pts',(0.98764783592732,4.81889259894746,14.6458949550466));
#25869=CARTESIAN_POINT('Ctrl Pts',(0.823209273332857,4.84949204305968,14.6553078253636));
#25870=CARTESIAN_POINT('Ctrl Pts',(0.746327949929668,4.86191741828524,14.6596993964142));
#25871=CARTESIAN_POINT('Ctrl Pts',(0.601083152989585,4.88186515645548,14.6679915998785));
#25872=CARTESIAN_POINT('Ctrl Pts',(0.532793539321853,4.88978928629886,14.6718884930598));
#25873=CARTESIAN_POINT('Ctrl Pts',(0.344236739056679,4.90767192429651,14.682651746766));
#25874=CARTESIAN_POINT('Ctrl Pts',(0.22373541332353,4.91463981411025,14.6895349031257));
#25875=CARTESIAN_POINT('Ctrl Pts',(-0.0310519859282602,4.91998210022382,
14.7041082395092));
#25876=CARTESIAN_POINT('Ctrl Pts',(-0.165264155542381,4.9173037174781,14.7117966986442));
#25877=CARTESIAN_POINT('Ctrl Pts',(-0.352663529595229,4.90588224790001,
14.722526950132));
#25878=CARTESIAN_POINT('Ctrl Pts',(-0.406072135881076,4.90175047141565,
14.7255842283075));
#25879=CARTESIAN_POINT('Ctrl Pts',(-0.502774701096095,4.89267803307819,
14.7311147426369));
#25880=CARTESIAN_POINT('Ctrl Pts',(-0.546090903859773,4.88803288852975,
14.7335901841687));
#25881=CARTESIAN_POINT('Ctrl Pts',(-0.630303713928392,4.87786867006708,
14.7383966394427));
#25882=CARTESIAN_POINT('Ctrl Pts',(-0.671203866723175,4.87240915232685,
14.740728026222));
#25883=CARTESIAN_POINT('Ctrl Pts',(-0.819163543775919,4.85076048682675,
14.7491601232085));
#25884=CARTESIAN_POINT('Ctrl Pts',(-0.925750667805225,4.83155175879844,
14.7552314364843));
#25885=CARTESIAN_POINT('Ctrl Pts',(-1.18850958994432,4.77518333471985,14.7702906094161));
#25886=CARTESIAN_POINT('Ctrl Pts',(-1.34365934212007,4.73386839907784,14.7792667500666));
#25887=CARTESIAN_POINT('Ctrl Pts',(-1.57395847276817,4.66030556117216,14.792864759978));
#25888=CARTESIAN_POINT('Ctrl Pts',(-1.65078012129937,4.63365060990808,14.7974474276197));
#25889=CARTESIAN_POINT('Ctrl Pts',(-1.79118794483762,4.58099794748697,14.8059252433829));
#25890=CARTESIAN_POINT('Ctrl Pts',(-1.85495852337486,4.55554883441805,14.8098154601947));
#25891=CARTESIAN_POINT('Ctrl Pts',(-2.02075323715779,4.48532600740488,14.8200430072974));
#25892=CARTESIAN_POINT('Ctrl Pts',(-2.12182466152272,4.43840654269116,14.8263934457869));
#25893=CARTESIAN_POINT('Ctrl Pts',(-2.35139336995664,4.32220094464652,14.841099348348));
#25894=CARTESIAN_POINT('Ctrl Pts',(-2.47857510630205,4.25054550676974,14.8494603765965));
#25895=CARTESIAN_POINT('Ctrl Pts',(-2.64933455226606,4.14406457181817,14.8609638328261));
#25896=CARTESIAN_POINT('Ctrl Pts',(-2.69578934792101,4.113996184883,14.8641227379261));
#25897=CARTESIAN_POINT('Ctrl Pts',(-2.77866896370851,4.05834471960723,14.8698083265298));
#25898=CARTESIAN_POINT('Ctrl Pts',(-2.81527276189438,4.03303885567056,14.8723374111537));
#25899=CARTESIAN_POINT('Ctrl Pts',(-2.88458969773298,3.9837133272001,14.8771589419322));
#25900=CARTESIAN_POINT('Ctrl Pts',(-2.91735865944358,3.95977879275916,14.8794521699746));
#25901=CARTESIAN_POINT('Ctrl Pts',(-3.04943741624175,3.86077855671869,14.888761734365));
#25902=CARTESIAN_POINT('Ctrl Pts',(-3.14617741650998,3.78236010702591,14.8957368326135));
#25903=CARTESIAN_POINT('Ctrl Pts',(-3.30825340242307,3.64045479427342,14.9078057880056));
#25904=CARTESIAN_POINT('Ctrl Pts',(-3.37499356530957,3.57866875468029,14.9128973185698));
#25905=CARTESIAN_POINT('Ctrl Pts',(-3.49730285280509,3.4589721361504,14.9224980931795));
#25906=CARTESIAN_POINT('Ctrl Pts',(-3.55324229872355,3.40148268983198,14.9270036457929));
#25907=CARTESIAN_POINT('Ctrl Pts',(-3.65769162020997,3.28874969963707,14.9356601422778));
#25908=CARTESIAN_POINT('Ctrl Pts',(-3.70641801954624,3.23373590035625,14.9398080407918));
#25909=CARTESIAN_POINT('Ctrl Pts',(-3.79478102427495,3.12934897288139,14.9475492571313));
#25910=CARTESIAN_POINT('Ctrl Pts',(-3.83473249579089,3.08026209778686,14.9511389117518));
#25911=CARTESIAN_POINT('Ctrl Pts',(-3.95094342764352,2.93171190368531,14.9618605913808));
#25912=CARTESIAN_POINT('Ctrl Pts',(-4.02435976481273,2.83009124924692,14.9690127335073));
#25913=CARTESIAN_POINT('Ctrl Pts',(-4.17898571671349,2.59786043251403,14.9849721445177));
#25914=CARTESIAN_POINT('Ctrl Pts',(-4.25811535831989,2.46601993104681,14.9937800304174));
#25915=CARTESIAN_POINT('Ctrl Pts',(-4.34357566735924,2.30721567785916,15.0040689149052));
#25916=CARTESIAN_POINT('Ctrl Pts',(-4.35601794539661,2.28363776280585,15.0055884258566));
#25917=CARTESIAN_POINT('Ctrl Pts',(-4.38781443155689,2.22217845140705,15.0095276572629));
#25918=CARTESIAN_POINT('Ctrl Pts',(-4.40687008704669,2.18414483210621,15.0119443343971));
#25919=CARTESIAN_POINT('Ctrl Pts',(-4.44124461332515,2.11325415963933,15.0164077075403));
#25920=CARTESIAN_POINT('Ctrl Pts',(-4.45669823462681,2.08046575050416,15.0184560912733));
#25921=CARTESIAN_POINT('Ctrl Pts',(-4.5402659828963,1.89795265494197,15.029779340586));
#25922=CARTESIAN_POINT('Ctrl Pts',(-4.6011988447425,1.74505300773222,15.0389769283129));
#25923=CARTESIAN_POINT('Ctrl Pts',(-4.68729486763718,1.49292959920582,15.0539037972743));
#25924=CARTESIAN_POINT('Ctrl Pts',(-4.71722674372294,1.39547253369909,15.0596171653545));
#25925=CARTESIAN_POINT('Ctrl Pts',(-4.75094897008291,1.27213976150744,15.0668064032774));
#25926=CARTESIAN_POINT('Ctrl Pts',(-4.75759111255687,1.24706955162331,15.0682656424916));
#25927=CARTESIAN_POINT('Ctrl Pts',(-4.76403458707897,1.2219482458825,15.0697260295707));
#25928=CARTESIAN_POINT('Origin',(0.,0.,-3.23514056400928));
#25929=CARTESIAN_POINT('',(-4.76403457365963,1.22194829820076,17.1653174600137));
#25930=CARTESIAN_POINT('',(-4.76403458706411,1.22194824594044,16.8201710428097));
#25931=CARTESIAN_POINT('',(-4.76403458704967,1.22194824599672,-3.23514056400928));
#25932=CARTESIAN_POINT('',(-4.91824987842825,-5.7598872651143E-5,15.4853473318374));
#25933=CARTESIAN_POINT('Ctrl Pts',(-4.76403457365963,1.22194829820076,17.1653174600137));
#25934=CARTESIAN_POINT('Ctrl Pts',(-4.7435882878598,1.3016626466693,17.1607000675729));
#25935=CARTESIAN_POINT('Ctrl Pts',(-4.72114095238727,1.38086506133652,17.156075181965));
#25936=CARTESIAN_POINT('Ctrl Pts',(-4.67543677500989,1.52794436177981,17.1473970567574));
#25937=CARTESIAN_POINT('Ctrl Pts',(-4.65266761493952,1.59593449705834,17.1433488446468));
#25938=CARTESIAN_POINT('Ctrl Pts',(-4.60401244775245,1.73131762648301,17.1352040831917));
#25939=CARTESIAN_POINT('Ctrl Pts',(-4.57811266782932,1.79868718250882,17.131108378121));
#25940=CARTESIAN_POINT('Ctrl Pts',(-4.49588483867522,1.99927958484134,17.1187747412416));
#25941=CARTESIAN_POINT('Ctrl Pts',(-4.43515439691572,2.13061116431127,17.1105106302183));
#25942=CARTESIAN_POINT('Ctrl Pts',(-4.31389815823793,2.36510340138688,17.0954005820732));
#25943=CARTESIAN_POINT('Ctrl Pts',(-4.25522810851253,2.46910214550434,17.08856454819));
#25944=CARTESIAN_POINT('Ctrl Pts',(-4.16364361053867,2.61846769925544,17.0785667469425));
#25945=CARTESIAN_POINT('Ctrl Pts',(-4.13364592803784,2.66557173095634,17.0753866464699));
#25946=CARTESIAN_POINT('Ctrl Pts',(-4.08255611344895,2.74285859806554,17.07012742685));
#25947=CARTESIAN_POINT('Ctrl Pts',(-4.06191581932615,2.77333330500112,17.0680431022528));
#25948=CARTESIAN_POINT('Ctrl Pts',(-4.00448435002738,2.85611223367364,17.0623502732961));
#25949=CARTESIAN_POINT('Ctrl Pts',(-3.9670120848231,2.90793522441979,17.0587507978996));
#25950=CARTESIAN_POINT('Ctrl Pts',(-3.86761470075161,3.03990035527551,17.0494689412395));
#25951=CARTESIAN_POINT('Ctrl Pts',(-3.80420582253675,3.11888696519914,17.0437988562822));
#25952=CARTESIAN_POINT('Ctrl Pts',(-3.63473477380734,3.31712818357754,17.0291878548076));
#25953=CARTESIAN_POINT('Ctrl Pts',(-3.52522779067636,3.43327895638431,17.0202489123287));
#25954=CARTESIAN_POINT('Ctrl Pts',(-3.36470360389514,3.58775025085969,17.0076907505431));
#25955=CARTESIAN_POINT('Ctrl Pts',(-3.31829503152825,3.63071620766254,17.0041190290465));
#25956=CARTESIAN_POINT('Ctrl Pts',(-3.21744103329441,3.72053946305271,16.9964734427018));
#25957=CARTESIAN_POINT('Ctrl Pts',(-3.16277155953977,3.76712311986316,16.9923980728256));
#25958=CARTESIAN_POINT('Ctrl Pts',(-3.07605618755443,3.83779434337348,16.9860344504823));
#25959=CARTESIAN_POINT('Ctrl Pts',(-3.04470249900674,3.86271585271366,16.9837533197907));
#25960=CARTESIAN_POINT('Ctrl Pts',(-2.86359398858533,4.00309489417528,16.9706871672441));
#25961=CARTESIAN_POINT('Ctrl Pts',(-2.707584131138,4.11022219394695,16.9598504667024));
#25962=CARTESIAN_POINT('Ctrl Pts',(-2.48067562118521,4.24749624362917,16.944687352597));
#25963=CARTESIAN_POINT('Ctrl Pts',(-2.41464844272446,4.2853761763514,16.9403427701605));
#25964=CARTESIAN_POINT('Ctrl Pts',(-2.31702584494433,4.33840965259396,16.934024869532));
#25965=CARTESIAN_POINT('Ctrl Pts',(-2.28610579611743,4.35478213119361,16.9320389401891));
#25966=CARTESIAN_POINT('Ctrl Pts',(-2.21615766620555,4.39087006168276,16.9275816717394));
#25967=CARTESIAN_POINT('Ctrl Pts',(-2.177036001686,4.41039782873514,16.9251129085179));
#25968=CARTESIAN_POINT('Ctrl Pts',(-2.0889894083395,4.45288970521857,16.9196038272885));
#25969=CARTESIAN_POINT('Ctrl Pts',(-2.03993581364031,4.47557431221357,16.9165664810994));
#25970=CARTESIAN_POINT('Ctrl Pts',(-1.86409303583123,4.55340031043252,16.9057728605231));
#25971=CARTESIAN_POINT('Ctrl Pts',(-1.73536463069232,4.60399902460852,16.8980419356125));
#25972=CARTESIAN_POINT('Ctrl Pts',(-1.49353161245578,4.68746957899087,16.883696015127));
#25973=CARTESIAN_POINT('Ctrl Pts',(-1.3810487454063,4.72183349901057,16.8770920234809));
#25974=CARTESIAN_POINT('Ctrl Pts',(-1.20129016207633,4.76977699789816,16.8665972404686));
#25975=CARTESIAN_POINT('Ctrl Pts',(-1.13477589568856,4.78603742053143,16.8627267293476));
#25976=CARTESIAN_POINT('Ctrl Pts',(-0.991467640299607,4.81791584412069,
16.854406290497));
#25977=CARTESIAN_POINT('Ctrl Pts',(-0.914595990783938,4.83309788160964,
16.8499544940678));
#25978=CARTESIAN_POINT('Ctrl Pts',(-0.687611191202474,4.87231761713459,
16.8368325999193));
#25979=CARTESIAN_POINT('Ctrl Pts',(-0.536709200484851,4.8912401825467,16.8281363531721));
#25980=CARTESIAN_POINT('Ctrl Pts',(-0.259547906279528,4.91301308622068,
16.812221618506));
#25981=CARTESIAN_POINT('Ctrl Pts',(-0.133586471180473,4.9180502160204,16.8050111867082));
#25982=CARTESIAN_POINT('Ctrl Pts',(0.0286577518124332,4.91829993419519,
16.7957804389627));
#25983=CARTESIAN_POINT('Ctrl Pts',(0.0648851788747955,4.91795541444086,
16.7937230485191));
#25984=CARTESIAN_POINT('Ctrl Pts',(0.142601995657612,4.91635743229706,16.7893190938912));
#25985=CARTESIAN_POINT('Ctrl Pts',(0.18408611491318,4.91497895048201,16.7869742880521));
#25986=CARTESIAN_POINT('Ctrl Pts',(0.25128220393893,4.9118941312388,16.7831817213911));
#25987=CARTESIAN_POINT('Ctrl Pts',(0.277006726870557,4.91051056259284,16.7817311457572));
#25988=CARTESIAN_POINT('Ctrl Pts',(0.453643593825276,4.89961787513667,16.771775928592));
#25989=CARTESIAN_POINT('Ctrl Pts',(0.604059421862266,4.88335547473123,16.7633217649779));
#25990=CARTESIAN_POINT('Ctrl Pts',(0.851708956657628,4.84496173910409,16.7492763997331));
#25991=CARTESIAN_POINT('Ctrl Pts',(0.949445586010876,4.82676032493256,16.7437007859473));
#25992=CARTESIAN_POINT('Ctrl Pts',(1.12230603337375,4.78911488208626,16.7337450089658));
#25993=CARTESIAN_POINT('Ctrl Pts',(1.19764800332343,4.77083129624926,16.7293733458068));
#25994=CARTESIAN_POINT('Ctrl Pts',(1.33889504060652,4.73299736503347,16.7211032083921));
#25995=CARTESIAN_POINT('Ctrl Pts',(1.40488401512382,4.71383121768918,16.7172083590564));
#25996=CARTESIAN_POINT('Ctrl Pts',(1.58677921657446,4.65684183093536,16.7063769534346));
#25997=CARTESIAN_POINT('Ctrl Pts',(1.70171256068583,4.61608252210859,16.6994230385123));
#25998=CARTESIAN_POINT('Ctrl Pts',(1.96775292364144,4.51044783243746,16.6830540132048));
#25999=CARTESIAN_POINT('Ctrl Pts',(2.11735888099621,4.44218221295468,16.6736332160375));
#26000=CARTESIAN_POINT('Ctrl Pts',(2.31096876311112,4.34183063695612,16.6611928660984));
#26001=CARTESIAN_POINT('Ctrl Pts',(2.35826316329169,4.31632538758996,16.6581338423023));
#26002=CARTESIAN_POINT('Ctrl Pts',(2.43408567861289,4.27381701620875,16.6532004235577));
#26003=CARTESIAN_POINT('Ctrl Pts',(2.4628757389652,4.25729116918938,16.6513205233435));
#26004=CARTESIAN_POINT('Ctrl Pts',(2.54398585504326,4.20963481331582,16.6460037671551));
#26005=CARTESIAN_POINT('Ctrl Pts',(2.59589841320415,4.17782250143452,16.6425756591444));
#26006=CARTESIAN_POINT('Ctrl Pts',(2.68730752117895,4.11944477087858,16.6364801888386));
#26007=CARTESIAN_POINT('Ctrl Pts',(2.72703403811147,4.09325449034184,16.6338105800471));
#26008=CARTESIAN_POINT('Ctrl Pts',(2.9525842303575,3.93981602122527,16.6185157831822));
#26009=CARTESIAN_POINT('Ctrl Pts',(3.12987152550727,3.80050087641063,16.6059362661294));
#26010=CARTESIAN_POINT('Ctrl Pts',(3.34768553528662,3.6037276353272,16.5893819934988));
#26011=CARTESIAN_POINT('Ctrl Pts',(3.39742467396146,3.55687457749323,16.5855205639085));
#26012=CARTESIAN_POINT('Ctrl Pts',(3.500637767178,3.45550954527971,16.5773241025328));
#26013=CARTESIAN_POINT('Ctrl Pts',(3.55385106149317,3.40075777402751,16.5729877385427));
#26014=CARTESIAN_POINT('Ctrl Pts',(3.71281058769227,3.2293954028356,16.5596776202371));
#26015=CARTESIAN_POINT('Ctrl Pts',(3.81425112626018,3.10892980361486,16.5506736484283));
#26016=CARTESIAN_POINT('Ctrl Pts',(3.98691091419381,2.88269056516686,16.5343820819906));
#26017=CARTESIAN_POINT('Ctrl Pts',(4.06013100732523,2.77861482064724,16.5271034824382));
#26018=CARTESIAN_POINT('Ctrl Pts',(4.14883680849413,2.64152195570325,16.517813771439));
#26019=CARTESIAN_POINT('Ctrl Pts',(4.16810533262779,2.61101188760507,16.5157646508863));
#26020=CARTESIAN_POINT('Ctrl Pts',(4.20892156697231,2.54477944597455,16.5113571641546));
#26021=CARTESIAN_POINT('Ctrl Pts',(4.23035412696273,2.50898927829548,16.5090006358365));
#26022=CARTESIAN_POINT('Ctrl Pts',(4.26438376551111,2.45048735718644,16.5051850200385));
#26023=CARTESIAN_POINT('Ctrl Pts',(4.27726072637742,2.42794107745536,16.5037231157302));
#26024=CARTESIAN_POINT('Ctrl Pts',(4.30891673555707,2.37148104417662,16.5000821332972));
#26025=CARTESIAN_POINT('Ctrl Pts',(4.32747452750783,2.337445189415,16.4979049400579));
#26026=CARTESIAN_POINT('Ctrl Pts',(4.41888705791368,2.16496950380238,16.486951248353));
#26027=CARTESIAN_POINT('Ctrl Pts',(4.48550950147534,2.02332903777803,16.4782073795908));
#26028=CARTESIAN_POINT('Ctrl Pts',(4.58441777519533,1.7840404206516,16.4636757489455));
#26029=CARTESIAN_POINT('Ctrl Pts',(4.62059686826783,1.6881264086129,16.4579128179635));
#26030=CARTESIAN_POINT('Ctrl Pts',(4.67562500319894,1.52718191597249,16.4483122508563));
#26031=CARTESIAN_POINT('Ctrl Pts',(4.69617571387768,1.462767002805,16.444488033603));
#26032=CARTESIAN_POINT('Ctrl Pts',(4.73900726484476,1.31829285946753,16.4359430998373));
#26033=CARTESIAN_POINT('Ctrl Pts',(4.76060021522881,1.23805140158652,16.431218850975));
#26034=CARTESIAN_POINT('Ctrl Pts',(4.80401732184332,1.05872030433921,16.4207003602173));
#26035=CARTESIAN_POINT('Ctrl Pts',(4.82482910460444,0.959424280793805,16.4149025206396));
#26036=CARTESIAN_POINT('Ctrl Pts',(4.87128567225963,0.69769805528553,16.399689803974));
#26037=CARTESIAN_POINT('Ctrl Pts',(4.89188283033444,0.534499647991539,16.3902705957283));
#26038=CARTESIAN_POINT('Ctrl Pts',(4.90698776454125,0.334598155320559,16.3788655219691));
#26039=CARTESIAN_POINT('Ctrl Pts',(4.90931034472373,0.298591395049708,16.3768166078053));
#26040=CARTESIAN_POINT('Ctrl Pts',(4.91346376696336,0.220901438333412,16.372409024554));
#26041=CARTESIAN_POINT('Ctrl Pts',(4.91516084216039,0.179213791346714,16.3700521953385));
#26042=CARTESIAN_POINT('Ctrl Pts',(4.91985951689027,0.0112235388383775,
16.3605775728024));
#26043=CARTESIAN_POINT('Ctrl Pts',(4.91852459017969,-0.115152817134032,
16.3535007286764));
#26044=CARTESIAN_POINT('Ctrl Pts',(4.9038677968834,-0.413484588303955,16.3367669739928));
#26045=CARTESIAN_POINT('Ctrl Pts',(4.88636740155251,-0.585065426077207,
16.3271183933113));
#26046=CARTESIAN_POINT('Ctrl Pts',(4.84895669978049,-0.82575776687166,16.3133918929845));
#26047=CARTESIAN_POINT('Ctrl Pts',(4.83648887165774,-0.895897431022879,
16.3093692487406));
#26048=CARTESIAN_POINT('Ctrl Pts',(4.80822870795427,-1.03701674010458,16.3012201523235));
#26049=CARTESIAN_POINT('Ctrl Pts',(4.79237693190637,-1.10796669787156,16.2970942599748));
#26050=CARTESIAN_POINT('Ctrl Pts',(4.75599208485935,-1.255383278971,16.2884546484954));
#26051=CARTESIAN_POINT('Ctrl Pts',(4.73517344310343,-1.33175830351492,16.2839402716194));
#26052=CARTESIAN_POINT('Ctrl Pts',(4.66202769413637,-1.57664434632021,16.269336817161));
#26053=CARTESIAN_POINT('Ctrl Pts',(4.60247506198401,-1.74285192690166,16.2592213224859));
#26054=CARTESIAN_POINT('Ctrl Pts',(4.51083855416828,-1.96090028637332,16.245719189578));
#26055=CARTESIAN_POINT('Ctrl Pts',(4.48654229213352,-2.01587022889027,16.2422953972963));
#26056=CARTESIAN_POINT('Ctrl Pts',(4.44577518726742,-2.10371491977322,16.2367966414425));
#26057=CARTESIAN_POINT('Ctrl Pts',(4.42993266430623,-2.13687391039157,16.2347149593188));
#26058=CARTESIAN_POINT('Ctrl Pts',(4.3869916370064,-2.22422069827699,16.2292140017611));
#26059=CARTESIAN_POINT('Ctrl Pts',(4.35926096315105,-2.27809071909811,16.2258024405227));
#26060=CARTESIAN_POINT('Ctrl Pts',(4.26508296230659,-2.45302236526538,16.2146366750122));
#26061=CARTESIAN_POINT('Ctrl Pts',(4.19453205498405,-2.5717994959412,16.2069138435397));
#26062=CARTESIAN_POINT('Ctrl Pts',(4.04837820845451,-2.79581062715771,16.1919234728479));
#26063=CARTESIAN_POINT('Ctrl Pts',(3.9734322173684,-2.90133745138393,16.1846639198916));
#26064=CARTESIAN_POINT('Ctrl Pts',(3.8559172536894,-3.05369582828456,16.1738165299351));
#26065=CARTESIAN_POINT('Ctrl Pts',(3.8164653572522,-3.10286128419825,16.1702562155462));
#26066=CARTESIAN_POINT('Ctrl Pts',(3.72986585881353,-3.20663157720159,16.1626042228905));
#26067=CARTESIAN_POINT('Ctrl Pts',(3.68243982414509,-3.26098484747825,16.158510899697));
#26068=CARTESIAN_POINT('Ctrl Pts',(3.53613864565559,-3.42139232428936,16.1461595840663));
#26069=CARTESIAN_POINT('Ctrl Pts',(3.4337537384426,-3.52413625334683,16.1378752065714));
#26070=CARTESIAN_POINT('Ctrl Pts',(3.24054661756337,-3.70159620424662,16.1228595923853));
#26071=CARTESIAN_POINT('Ctrl Pts',(3.15129741141974,-3.77786734671018,16.1161384551606));
#26072=CARTESIAN_POINT('Ctrl Pts',(3.01487609011523,-3.88625006958355,16.106194969443));
#26073=CARTESIAN_POINT('Ctrl Pts',(2.96973631982194,-3.92085242529157,16.1029557193361));
#26074=CARTESIAN_POINT('Ctrl Pts',(2.89443945789357,-3.97652554281347,16.0976394198877));
#26075=CARTESIAN_POINT('Ctrl Pts',(2.86462842573123,-3.99805442530318,16.0955568086521));
#26076=CARTESIAN_POINT('Ctrl Pts',(2.78345115854087,-4.05530477842046,16.0899434630986));
#26077=CARTESIAN_POINT('Ctrl Pts',(2.73164012147523,-4.09038379453623,16.0864212140372));
#26078=CARTESIAN_POINT('Ctrl Pts',(2.56205194291797,-4.2005450275659,16.075058118365));
#26079=CARTESIAN_POINT('Ctrl Pts',(2.44174233374725,-4.2716019761059,16.0672479771617));
#26080=CARTESIAN_POINT('Ctrl Pts',(2.20797088217651,-4.39656405884317,16.052390475707));
#26081=CARTESIAN_POINT('Ctrl Pts',(2.09515036031063,-4.45143295539299,16.0453523220755));
#26082=CARTESIAN_POINT('Ctrl Pts',(1.92278636543803,-4.52725429192827,16.0347360508165));
#26083=CARTESIAN_POINT('Ctrl Pts',(1.8647353205005,-4.55147238913325,16.031183282393));
#26084=CARTESIAN_POINT('Ctrl Pts',(1.73894397586434,-4.60114019700116,16.0235261849199));
#26085=CARTESIAN_POINT('Ctrl Pts',(1.67107423019433,-4.6262217863785,16.0194201141789));
#26086=CARTESIAN_POINT('Ctrl Pts',(1.46401687848547,-4.69758962382259,16.0069596016588));
#26087=CARTESIAN_POINT('Ctrl Pts',(1.32329034517427,-4.73915556268299,15.9985780448355));
#26088=CARTESIAN_POINT('Ctrl Pts',(1.03597241981382,-4.81022234858021,15.9816365264345));
#26089=CARTESIAN_POINT('Ctrl Pts',(0.889467350789513,-4.83945517934842,
15.9730847673));
#26090=CARTESIAN_POINT('Ctrl Pts',(0.70141699179698,-4.86814860996931,15.9622593411364));
#26091=CARTESIAN_POINT('Ctrl Pts',(0.660899351644574,-4.87381460365856,
15.9599359281631));
#26092=CARTESIAN_POINT('Ctrl Pts',(0.590544755488948,-4.88275952430427,
15.9559191038084));
#26093=CARTESIAN_POINT('Ctrl Pts',(0.560739917416643,-4.88627203971508,
15.95422279412));
#26094=CARTESIAN_POINT('Ctrl Pts',(0.487118180101782,-4.89426591007949,
15.9500435444097));
#26095=CARTESIAN_POINT('Ctrl Pts',(0.443269559174345,-4.89843189866882,
15.9475638632177));
#26096=CARTESIAN_POINT('Ctrl Pts',(0.313284914341319,-4.9090218544607,15.9402325057621));
#26097=CARTESIAN_POINT('Ctrl Pts',(0.227028880546364,-4.91376648383623,
15.9353924780907));
#26098=CARTESIAN_POINT('Ctrl Pts',(-0.0365325744302362,-4.92130905522521,
15.9206200951733));
#26099=CARTESIAN_POINT('Ctrl Pts',(-0.213900343096126,-4.91679398930186,
15.9106975143877));
#26100=CARTESIAN_POINT('Ctrl Pts',(-0.460607304799696,-4.89713703937088,
15.8967515953338));
#26101=CARTESIAN_POINT('Ctrl Pts',(-0.530451703672448,-4.89006453078622,
15.892787875185));
#26102=CARTESIAN_POINT('Ctrl Pts',(-0.658589957239961,-4.87431151112026,
15.8854787596094));
#26103=CARTESIAN_POINT('Ctrl Pts',(-0.716925410791389,-4.86607349977366,
15.8821370114024));
#26104=CARTESIAN_POINT('Ctrl Pts',(-0.847858006018463,-4.84517787668112,
15.8746003395477));
#26105=CARTESIAN_POINT('Ctrl Pts',(-0.920346955213649,-4.83193265534748,
15.8704024784265));
#26106=CARTESIAN_POINT('Ctrl Pts',(-1.12290585404446,-4.79019731283169,
15.8585964258754));
#26107=CARTESIAN_POINT('Ctrl Pts',(-1.25215603505651,-4.75804715886603,
15.8509732999942));
#26108=CARTESIAN_POINT('Ctrl Pts',(-1.47968191145142,-4.69153735138861,
15.8374065955496));
#26109=CARTESIAN_POINT('Ctrl Pts',(-1.57847415540036,-4.65922751077476,
15.8314653952655));
#26110=CARTESIAN_POINT('Ctrl Pts',(-1.71445520406705,-4.60993328013733,
15.823234635117));
#26111=CARTESIAN_POINT('Ctrl Pts',(-1.75256755089303,-4.59557923804063,
15.8209219108523));
#26112=CARTESIAN_POINT('Ctrl Pts',(-1.82736811057167,-4.56634164153953,
15.8163734182383));
#26113=CARTESIAN_POINT('Ctrl Pts',(-1.86406359717801,-4.55148515873302,
15.8141373284263));
#26114=CARTESIAN_POINT('Ctrl Pts',(-1.94702277317141,-4.51672684505237,
15.8090663729141));
#26115=CARTESIAN_POINT('Ctrl Pts',(-1.9931682454743,-4.49655417854281,15.8062344214535));
#26116=CARTESIAN_POINT('Ctrl Pts',(-2.14482728339731,-4.42746245754207,
15.7968755671675));
#26117=CARTESIAN_POINT('Ctrl Pts',(-2.24891555050614,-4.37550990738065,
15.7903679324805));
#26118=CARTESIAN_POINT('Ctrl Pts',(-2.46571693545719,-4.25751826434365,
15.7765368063815));
#26119=CARTESIAN_POINT('Ctrl Pts',(-2.57783869583992,-4.19058097097493,
15.7692160868953));
#26120=CARTESIAN_POINT('Ctrl Pts',(-2.74606615784336,-4.08083932879514,
15.7578982510804));
#26121=CARTESIAN_POINT('Ctrl Pts',(-2.80413702840918,-4.04115631341736,
15.7539271637776));
#26122=CARTESIAN_POINT('Ctrl Pts',(-2.91876646743411,-3.95916292443407,
15.7459484051873));
#26123=CARTESIAN_POINT('Ctrl Pts',(-2.97530464690947,-3.91685216198046,
15.7419415772266));
#26124=CARTESIAN_POINT('Ctrl Pts',(-3.19637668403009,-3.74386192769029,
15.7259737959945));
#26125=CARTESIAN_POINT('Ctrl Pts',(-3.35337317468545,-3.60391623962902,
15.7139433117501));
#26126=CARTESIAN_POINT('Ctrl Pts',(-3.5659548858786,-3.38846844618353,15.6966263948497));
#26127=CARTESIAN_POINT('Ctrl Pts',(-3.62910069246196,-3.32075008508508,
15.6913371069472));
#26128=CARTESIAN_POINT('Ctrl Pts',(-3.71401907751841,-3.22436550940211,
15.6840295361575));
#26129=CARTESIAN_POINT('Ctrl Pts',(-3.73744487410673,-3.19718258707085,
15.681991967582));
#26130=CARTESIAN_POINT('Ctrl Pts',(-3.77925657675769,-3.14757737940318,
15.6783168435665));
#26131=CARTESIAN_POINT('Ctrl Pts',(-3.79774562588185,-3.12524428041842,
15.6766776752659));
#26132=CARTESIAN_POINT('Ctrl Pts',(-3.84299504239359,-3.06959252811821,
15.6726287855334));
#26133=CARTESIAN_POINT('Ctrl Pts',(-3.86952076263997,-3.03608601609949,
15.6702222072373));
#26134=CARTESIAN_POINT('Ctrl Pts',(-3.94507841544602,-2.93804485393541,
15.6632621057545));
#26135=CARTESIAN_POINT('Ctrl Pts',(-3.99295627561725,-2.87263843868657,
15.658718981789));
#26136=CARTESIAN_POINT('Ctrl Pts',(-4.14693457146008,-2.65099512142812,
15.6435969156073));
#26137=CARTESIAN_POINT('Ctrl Pts',(-4.2456509195922,-2.48983708204874,15.6330335546013));
#26138=CARTESIAN_POINT('Ctrl Pts',(-4.36776085066296,-2.26201236352936,
15.618465678188));
#26139=CARTESIAN_POINT('Ctrl Pts',(-4.39935770089278,-2.19992873914243,
15.6145318228235));
#26140=CARTESIAN_POINT('Ctrl Pts',(-4.44531558208509,-2.10467484944113,
15.6085433777263));
#26141=CARTESIAN_POINT('Ctrl Pts',(-4.46064739747598,-2.07198253390992,
15.6064963644958));
#26142=CARTESIAN_POINT('Ctrl Pts',(-4.51144252121119,-1.96049372621244,
15.5995420269483));
#26143=CARTESIAN_POINT('Ctrl Pts',(-4.54518857288801,-1.88093324009851,
15.5946234704278));
#26144=CARTESIAN_POINT('Ctrl Pts',(-4.62129635660792,-1.68747214795738,
15.5827605665497));
#26145=CARTESIAN_POINT('Ctrl Pts',(-4.66156740531742,-1.57280998657092,
15.5758079286257));
#26146=CARTESIAN_POINT('Ctrl Pts',(-4.73468799479361,-1.33702366023405,
15.5616764419799));
#26147=CARTESIAN_POINT('Ctrl Pts',(-4.76723228708275,-1.21589455173432,
15.5545025313147));
#26148=CARTESIAN_POINT('Ctrl Pts',(-4.8040386929305,-1.05451724675543,15.5450850947102));
#26149=CARTESIAN_POINT('Ctrl Pts',(-4.81248539205324,-1.01527277102387,
15.5428058482511));
#26150=CARTESIAN_POINT('Ctrl Pts',(-4.82703502764815,-0.943407084268541,
15.5386537341665));
#26151=CARTESIAN_POINT('Ctrl Pts',(-4.83329002077137,-0.91081923959383,
15.5367788889788));
#26152=CARTESIAN_POINT('Ctrl Pts',(-4.84757269053403,-0.832113664071977,
15.5322667976335));
#26153=CARTESIAN_POINT('Ctrl Pts',(-4.85527270506987,-0.785939662971163,
15.5296328733288));
#26154=CARTESIAN_POINT('Ctrl Pts',(-4.89954812040739,-0.494886787815442,
15.513091253198));
#26155=CARTESIAN_POINT('Ctrl Pts',(-4.91824709472654,-0.247649462345353,
15.4992917658497));
#26156=CARTESIAN_POINT('Ctrl Pts',(-4.91824999966148,-5.77046521768598E-5,
15.4853475479531));
#26157=CARTESIAN_POINT('Ctrl Pts',(-4.91824999966286,-5.75870754615866E-5,
15.4853475413313));
#26158=CARTESIAN_POINT('Ctrl Pts',(-4.91825044579516,0.0380445423567261,
15.4832016524643));
#26159=CARTESIAN_POINT('Ctrl Pts',(-4.91780812100187,0.0761452482382754,
15.4810533571179));
#26160=CARTESIAN_POINT('Ctrl Pts',(-4.91608020393543,0.150517373830886,
15.4768534137325));
#26161=CARTESIAN_POINT('Ctrl Pts',(-4.91483575734356,0.186787336092719,
15.4748021578625));
#26162=CARTESIAN_POINT('Ctrl Pts',(-4.91004881726367,0.292235419018164,
15.4688279896373));
#26163=CARTESIAN_POINT('Ctrl Pts',(-4.90544620961724,0.361356150664063,
15.4648986567023));
#26164=CARTESIAN_POINT('Ctrl Pts',(-4.8773692316182,0.680998301980589,15.4466526714679));
#26165=CARTESIAN_POINT('Ctrl Pts',(-4.83615212048835,0.929579899055647,
15.4322266241013));
#26166=CARTESIAN_POINT('Ctrl Pts',(-4.77215806660131,1.18994245846746,15.4169086953599));
#26167=CARTESIAN_POINT('Ctrl Pts',(-4.76813656803685,1.20595576894076,15.4159658272421));
#26168=CARTESIAN_POINT('Ctrl Pts',(-4.76403458688904,1.22194824662298,15.4150234826428));
#26169=CARTESIAN_POINT('Ctrl Pts',(-4.76403458707897,1.2219482458825,15.0697260295707));
#26170=CARTESIAN_POINT('Ctrl Pts',(-4.7673671792485,1.20895540071595,15.0704813479208));
#26171=CARTESIAN_POINT('Ctrl Pts',(-4.77064662770679,1.19594888736934,15.0712369728154));
#26172=CARTESIAN_POINT('Ctrl Pts',(-4.79107250321357,1.1135174566575,15.0760230610723));
#26173=CARTESIAN_POINT('Ctrl Pts',(-4.80675611995235,1.04373957717661,15.0800618850286));
#26174=CARTESIAN_POINT('Ctrl Pts',(-4.83555882569426,0.901125677627058,
15.0883009312144));
#26175=CARTESIAN_POINT('Ctrl Pts',(-4.84856673912676,0.828285605891197,
15.0925008639847));
#26176=CARTESIAN_POINT('Ctrl Pts',(-4.88477809217167,0.595249235037764,
15.1059221267969));
#26177=CARTESIAN_POINT('Ctrl Pts',(-4.90171972039349,0.434190427839137,
15.1151779879791));
#26178=CARTESIAN_POINT('Ctrl Pts',(-4.91573024887108,0.181793679350151,
15.1296489402847));
#26179=CARTESIAN_POINT('Ctrl Pts',(-4.91825122801099,0.090872538481914,
15.1348540807445));
#26180=CARTESIAN_POINT('Ctrl Pts',(-4.91824918374074,-0.0604592894478811,
15.143493192483));
#26181=CARTESIAN_POINT('Ctrl Pts',(-4.91713599127383,-0.120847541397437,
15.1469340051527));
#26182=CARTESIAN_POINT('Ctrl Pts',(-4.91354321669377,-0.218298561487058,
15.1524708947497));
#26183=CARTESIAN_POINT('Ctrl Pts',(-4.91175551922442,-0.255380037915821,
15.1545737137732));
#26184=CARTESIAN_POINT('Ctrl Pts',(-4.90585243390948,-0.354482955583493,
15.1601843174804));
#26185=CARTESIAN_POINT('Ctrl Pts',(-4.9009808828241,-0.416452633304532,
15.163683848214));
#26186=CARTESIAN_POINT('Ctrl Pts',(-4.89015599235757,-0.527231673687728,
15.1699385341009));
#26187=CARTESIAN_POINT('Ctrl Pts',(-4.88464288816208,-0.576075306459741,
15.1726958606277));
#26188=CARTESIAN_POINT('Ctrl Pts',(-4.85024570391863,-0.84463418520304,
15.1878744642066));
#26189=CARTESIAN_POINT('Ctrl Pts',(-4.80726966967169,-1.06228403116591,
15.2002543327913));
#26190=CARTESIAN_POINT('Ctrl Pts',(-4.73186070209481,-1.34292123599112,
15.2166419593025));
#26191=CARTESIAN_POINT('Ctrl Pts',(-4.7125569356201,-1.40916646885443,15.220541099801));
#26192=CARTESIAN_POINT('Ctrl Pts',(-4.66873095703343,-1.54857526382148,
15.2288209528956));
#26193=CARTESIAN_POINT('Ctrl Pts',(-4.64386774934535,-1.62161223100499,
15.2332030337889));
#26194=CARTESIAN_POINT('Ctrl Pts',(-4.57988380257849,-1.79600836484919,
15.2437819088672));
#26195=CARTESIAN_POINT('Ctrl Pts',(-4.5391027516234,-1.89671492966034,15.249987034683));
#26196=CARTESIAN_POINT('Ctrl Pts',(-4.42297189926609,-2.15824492923478,
15.2663604701842));
#26197=CARTESIAN_POINT('Ctrl Pts',(-4.34218936948808,-2.3164831052719,15.2765370511216));
#26198=CARTESIAN_POINT('Ctrl Pts',(-4.23508158134163,-2.50090864033163,
15.2886677095506));
#26199=CARTESIAN_POINT('Ctrl Pts',(-4.21679879528527,-2.5316137123602,15.2906965105245));
#26200=CARTESIAN_POINT('Ctrl Pts',(-4.17555173856853,-2.59919949546296,
15.2951809884637));
#26201=CARTESIAN_POINT('Ctrl Pts',(-4.15243010350678,-2.63598077267938,
15.2976343079277));
#26202=CARTESIAN_POINT('Ctrl Pts',(-4.06477627685243,-2.77140222810852,
15.3067256094917));
#26203=CARTESIAN_POINT('Ctrl Pts',(-3.99719139061608,-2.86801987967851,
15.3133299542669));
#26204=CARTESIAN_POINT('Ctrl Pts',(-3.82029020601668,-3.10249728604743,
15.3297857502547));
#26205=CARTESIAN_POINT('Ctrl Pts',(-3.70692863390716,-3.23709527693757,
15.3396276142171));
#26206=CARTESIAN_POINT('Ctrl Pts',(-3.53724083509185,-3.41794012191709,
15.3536010014379));
#26207=CARTESIAN_POINT('Ctrl Pts',(-3.48672688122618,-3.46945570646042,
15.3576746710699));
#26208=CARTESIAN_POINT('Ctrl Pts',(-3.38271318222823,-3.5709652030561,15.3659035803204));
#26209=CARTESIAN_POINT('Ctrl Pts',(-3.32919354032112,-3.62091302792393,
15.3700581174756));
#26210=CARTESIAN_POINT('Ctrl Pts',(-3.21518148216237,-3.722650747756,15.378752555278));
#26211=CARTESIAN_POINT('Ctrl Pts',(-3.15450569920082,-3.7742037796569,15.3832930931403));
#26212=CARTESIAN_POINT('Ctrl Pts',(-2.95460073767163,-3.93586305381782,
15.3979834017141));
#26213=CARTESIAN_POINT('Ctrl Pts',(-2.81065602117549,-4.0399128899484,15.4081599051578));
#26214=CARTESIAN_POINT('Ctrl Pts',(-2.6112183019896,-4.16824703972006,15.4216976837862));
#26215=CARTESIAN_POINT('Ctrl Pts',(-2.56044948534168,-4.1996241451417,15.4250974312394));
#26216=CARTESIAN_POINT('Ctrl Pts',(-2.47718487449013,-4.24901365017875,
15.4305938947043));
#26217=CARTESIAN_POINT('Ctrl Pts',(-2.4450343811341,-4.2675952029147,15.4326970976503));
#26218=CARTESIAN_POINT('Ctrl Pts',(-2.3578198533458,-4.31669218837916,15.4383529135941));
#26219=CARTESIAN_POINT('Ctrl Pts',(-2.30237525024915,-4.346517486669,15.441896957845));
#26220=CARTESIAN_POINT('Ctrl Pts',(-2.15919220207879,-4.42003123344747,
15.4509406281462));
#26221=CARTESIAN_POINT('Ctrl Pts',(-2.07069265300085,-4.46217650934667,
15.4564287188405));
#26222=CARTESIAN_POINT('Ctrl Pts',(-1.84022477623791,-4.5635960396736,15.4705345015754));
#26223=CARTESIAN_POINT('Ctrl Pts',(-1.69662993561883,-4.61890486656072,
15.4791491452054));
#26224=CARTESIAN_POINT('Ctrl Pts',(-1.48124303189271,-4.69046437340751,
15.4919342909448));
#26225=CARTESIAN_POINT('Ctrl Pts',(-1.41129915791689,-4.71198169349157,
15.4960649485231));
#26226=CARTESIAN_POINT('Ctrl Pts',(-1.27147059754913,-4.75160534828729,
15.5042917464087));
#26227=CARTESIAN_POINT('Ctrl Pts',(-1.20161528881772,-4.76974961611879,
15.5083865791224));
#26228=CARTESIAN_POINT('Ctrl Pts',(-1.09237083612256,-4.79557257324288,
15.5147719883428));
#26229=CARTESIAN_POINT('Ctrl Pts',(-1.0532438879321,-4.80431760361842,15.5170553243316));
#26230=CARTESIAN_POINT('Ctrl Pts',(-0.845639032286988,-4.84806008755224,
15.5291527548139));
#26231=CARTESIAN_POINT('Ctrl Pts',(-0.675518662393738,-4.87467595624735,
15.5390090397132));
#26232=CARTESIAN_POINT('Ctrl Pts',(-0.41532894800091,-4.90149925482032,
15.5539739518092));
#26233=CARTESIAN_POINT('Ctrl Pts',(-0.326067346606616,-4.9082454545971,
15.5590874225721));
#26234=CARTESIAN_POINT('Ctrl Pts',(-0.20015466054073,-4.91431151804329,
15.566259597224));
#26235=CARTESIAN_POINT('Ctrl Pts',(-0.163619804365508,-4.9156635544516,
15.5683357904989));
#26236=CARTESIAN_POINT('Ctrl Pts',(-0.0850297787411345,-4.91769476640752,
15.5727896936212));
#26237=CARTESIAN_POINT('Ctrl Pts',(-0.0429739913079264,-4.91824208104107,
15.5751655642479));
#26238=CARTESIAN_POINT('Ctrl Pts',(0.130860436831612,-4.91827445918214,
15.5849657903678));
#26239=CARTESIAN_POINT('Ctrl Pts',(0.26258614695643,-4.91300288791975,15.5923452386219));
#26240=CARTESIAN_POINT('Ctrl Pts',(0.556500497176249,-4.88938504559556,
15.6088637019004));
#26241=CARTESIAN_POINT('Ctrl Pts',(0.718307034272635,-4.86824538256003,
15.617995528561));
#26242=CARTESIAN_POINT('Ctrl Pts',(0.950265436641775,-4.82612265793943,
15.6312774598904));
#26243=CARTESIAN_POINT('Ctrl Pts',(1.02147105341181,-4.81155494976111,15.6353805237688));
#26244=CARTESIAN_POINT('Ctrl Pts',(1.16314485910006,-4.77928367709257,15.6436064374179));
#26245=CARTESIAN_POINT('Ctrl Pts',(1.23359596254363,-4.76158579300629,15.6477282634757));
#26246=CARTESIAN_POINT('Ctrl Pts',(1.34278903712325,-4.73156951539523,15.6541707451116));
#26247=CARTESIAN_POINT('Ctrl Pts',(1.38181438432096,-4.7203200589366,15.6564841327815));
#26248=CARTESIAN_POINT('Ctrl Pts',(1.59824846751835,-4.65501662899941,15.6693764117313));
#26249=CARTESIAN_POINT('Ctrl Pts',(1.77262811341739,-4.59144494174076,15.6800043778367));
#26250=CARTESIAN_POINT('Ctrl Pts',(2.0143853402445,-4.48747961276533,15.6950525320857));
#26251=CARTESIAN_POINT('Ctrl Pts',(2.08503515713005,-4.45509261122537,15.6994888398838));
#26252=CARTESIAN_POINT('Ctrl Pts',(2.18672109186782,-4.40552925153686,15.7059222591322));
#26253=CARTESIAN_POINT('Ctrl Pts',(2.21838552095762,-4.38967001522657,15.7079325094514));
#26254=CARTESIAN_POINT('Ctrl Pts',(2.28909508573001,-4.35329437694503,15.7124356598538));
#26255=CARTESIAN_POINT('Ctrl Pts',(2.32804116160241,-4.33259190966291,15.7149259578911));
#26256=CARTESIAN_POINT('Ctrl Pts',(2.41455409409214,-4.2851010728453,15.7204871184703));
#26257=CARTESIAN_POINT('Ctrl Pts',(2.46196408668838,-4.25803893694308,15.7235549349799));
#26258=CARTESIAN_POINT('Ctrl Pts',(2.63003253349694,-4.15835807641385,15.734522543836));
#26259=CARTESIAN_POINT('Ctrl Pts',(2.74801020215947,-4.08135432525978,15.7423962010869));
#26260=CARTESIAN_POINT('Ctrl Pts',(2.95670166819914,-3.93198578830688,15.7567884762859));
#26261=CARTESIAN_POINT('Ctrl Pts',(3.04847089222512,-3.86127203462677,15.7632945543163));
#26262=CARTESIAN_POINT('Ctrl Pts',(3.19071832002026,-3.74342723460587,15.7737156669957));
#26263=CARTESIAN_POINT('Ctrl Pts',(3.2428492033759,-3.69835906323116,15.7776113691402));
#26264=CARTESIAN_POINT('Ctrl Pts',(3.35349425194547,-3.59856567043365,15.7860569344498));
#26265=CARTESIAN_POINT('Ctrl Pts',(3.41165303401627,-3.54347596879543,15.7906090578309));
#26266=CARTESIAN_POINT('Ctrl Pts',(3.58243005550648,-3.37360749458785,15.8043334953769));
#26267=CARTESIAN_POINT('Ctrl Pts',(3.6907908299207,-3.25470348638313,15.8135355739758));
#26268=CARTESIAN_POINT('Ctrl Pts',(3.86246463666822,-3.04670533583653,15.8289727572797));
#26269=CARTESIAN_POINT('Ctrl Pts',(3.92898810858171,-2.96042215141192,15.8352023341882));
#26270=CARTESIAN_POINT('Ctrl Pts',(4.01719555139649,-2.83779811045146,15.8438006088084));
#26271=CARTESIAN_POINT('Ctrl Pts',(4.04135843959987,-2.80328026305817,15.8461940105383));
#26272=CARTESIAN_POINT('Ctrl Pts',(4.08903458912901,-2.733274770066,15.8509919695881));
#26273=CARTESIAN_POINT('Ctrl Pts',(4.11253665094254,-2.6977837554911,15.8533962169968));
#26274=CARTESIAN_POINT('Ctrl Pts',(4.19486897770873,-2.56987520200002,15.8619709286034));
#26275=CARTESIAN_POINT('Ctrl Pts',(4.25106905789913,-2.47580222080044,15.8681123108124));
#26276=CARTESIAN_POINT('Ctrl Pts',(4.39529968355737,-2.21496251478525,15.8848132716383));
#26277=CARTESIAN_POINT('Ctrl Pts',(4.47695752579596,-2.04488839144273,15.8953578798361));
#26278=CARTESIAN_POINT('Ctrl Pts',(4.57591083515631,-1.8042616788985,15.9100200634002));
#26279=CARTESIAN_POINT('Ctrl Pts',(4.60171786414726,-1.73738675011734,15.9140678863104));
#26280=CARTESIAN_POINT('Ctrl Pts',(4.65110125234697,-1.60058794024769,15.9223035262967));
#26281=CARTESIAN_POINT('Ctrl Pts',(4.67458411911539,-1.53064945490793,15.9264909433591));
#26282=CARTESIAN_POINT('Ctrl Pts',(4.72047378807687,-1.38305413975603,15.9352867638508));
#26283=CARTESIAN_POINT('Ctrl Pts',(4.74255756535897,-1.3053195374849,15.9398959508243));
#26284=CARTESIAN_POINT('Ctrl Pts',(4.80534587506586,-1.06161605077907,15.9542780411933));
#26285=CARTESIAN_POINT('Ctrl Pts',(4.83932417531062,-0.894046472751399,
15.9640738624175));
#26286=CARTESIAN_POINT('Ctrl Pts',(4.8735909931958,-0.664142973584231,15.9773450401738));
#26287=CARTESIAN_POINT('Ctrl Pts',(4.88152441693511,-0.603070938608932,
15.9808539082257));
#26288=CARTESIAN_POINT('Ctrl Pts',(4.89239866330379,-0.504971558861152,
15.9864584760367));
#26289=CARTESIAN_POINT('Ctrl Pts',(4.89607053501034,-0.468032385667622,
15.9885613412932));
#26290=CARTESIAN_POINT('Ctrl Pts',(4.90466492962352,-0.370349364947041,
15.9941036103659));
#26291=CARTESIAN_POINT('Ctrl Pts',(4.90887726347913,-0.309549463126548,
15.9975352377085));
#26292=CARTESIAN_POINT('Ctrl Pts',(4.92007393286105,-0.0883972189620109,
16.0099800895553));
#26293=CARTESIAN_POINT('Ctrl Pts',(4.92033841521507,0.0721939115846496,
16.0189488196257));
#26294=CARTESIAN_POINT('Ctrl Pts',(4.9072628802798,0.348468797282983,16.0344585550179));
#26295=CARTESIAN_POINT('Ctrl Pts',(4.89767106532848,0.464195142065669,16.0409789490285));
#26296=CARTESIAN_POINT('Ctrl Pts',(4.87584682986917,0.648137322021266,16.0514275529925));
#26297=CARTESIAN_POINT('Ctrl Pts',(4.86625284933039,0.716622187511607,16.0553364248338));
#26298=CARTESIAN_POINT('Ctrl Pts',(4.84258948784879,0.863001978962626,16.0637401463363));
#26299=CARTESIAN_POINT('Ctrl Pts',(4.82807724816486,0.940805633373073,16.0682368995086));
#26300=CARTESIAN_POINT('Ctrl Pts',(4.75927755919565,1.2659235725187,16.0871685825962));
#26301=CARTESIAN_POINT('Ctrl Pts',(4.68781299996906,1.50920270665969,16.1017021244908));
#26302=CARTESIAN_POINT('Ctrl Pts',(4.57989217346329,1.79341993720486,16.1190363631025));
#26303=CARTESIAN_POINT('Ctrl Pts',(4.56111023762814,1.84066316217621,16.1219290363049));
#26304=CARTESIAN_POINT('Ctrl Pts',(4.52701154763958,1.92270490866688,16.126968888265));
#26305=CARTESIAN_POINT('Ctrl Pts',(4.51201765572754,1.95763235060485,16.1291193650016));
#26306=CARTESIAN_POINT('Ctrl Pts',(4.46414217061016,2.06568280218006,16.1357917419951));
#26307=CARTESIAN_POINT('Ctrl Pts',(4.42987634105798,2.13817834113984,16.1402977371673));
#26308=CARTESIAN_POINT('Ctrl Pts',(4.33651308950098,2.32381668509506,16.1519569010382));
#26309=CARTESIAN_POINT('Ctrl Pts',(4.27475685666113,2.43555408431862,16.1590949877117));
#26310=CARTESIAN_POINT('Ctrl Pts',(4.15208084351505,2.63844511184313,16.1723886385792));
#26311=CARTESIAN_POINT('Ctrl Pts',(4.09232529351868,2.73020901066254,16.1785356288839));
#26312=CARTESIAN_POINT('Ctrl Pts',(3.99294446486412,2.87222134831729,16.1883061347029));
#26313=CARTESIAN_POINT('Ctrl Pts',(3.95531564077455,2.9238226765734,16.1919127672559));
#26314=CARTESIAN_POINT('Ctrl Pts',(3.87281408773291,3.03245071618966,16.1996348579622));
#26315=CARTESIAN_POINT('Ctrl Pts',(3.82766259158011,3.08924670808085,16.2037518540514));
#26316=CARTESIAN_POINT('Ctrl Pts',(3.75536082003134,3.17617537883206,16.2101841428276));
#26317=CARTESIAN_POINT('Ctrl Pts',(3.72906607709961,3.20700656263263,16.2124921725685));
#26318=CARTESIAN_POINT('Ctrl Pts',(3.57852526645503,3.37916400938806,16.2255336669809));
#26319=CARTESIAN_POINT('Ctrl Pts',(3.44662999478166,3.51359263992373,16.2363179473873));
#26320=CARTESIAN_POINT('Ctrl Pts',(3.25092111880429,3.69141025697158,16.2514368860352));
#26321=CARTESIAN_POINT('Ctrl Pts',(3.19329766425957,3.74136980701012,16.2557896868606));
#26322=CARTESIAN_POINT('Ctrl Pts',(3.10739882921164,3.81241336888809,16.2621286920996));
#26323=CARTESIAN_POINT('Ctrl Pts',(3.0800216708668,3.83456512910313,16.2641275597924));
#26324=CARTESIAN_POINT('Ctrl Pts',(3.01747302870874,3.88407321297097,16.2686446926175));
#26325=CARTESIAN_POINT('Ctrl Pts',(2.98216290201278,3.91124950521013,16.2711601899426));
#26326=CARTESIAN_POINT('Ctrl Pts',(2.90209662525436,3.97115752468188,16.2767944459938));
#26327=CARTESIAN_POINT('Ctrl Pts',(2.8571463767045,4.00361980805408,16.2799100303992));
#26328=CARTESIAN_POINT('Ctrl Pts',(2.69131544716929,4.11916459078317,16.2912531348665));
#26329=CARTESIAN_POINT('Ctrl Pts',(2.56728351967133,4.19758874222412,16.2994528432359));
#26330=CARTESIAN_POINT('Ctrl Pts',(2.34376594762202,4.32529899085836,16.3138932853996));
#26331=CARTESIAN_POINT('Ctrl Pts',(2.24577168014551,4.37698061405129,16.3201173327044));
#26332=CARTESIAN_POINT('Ctrl Pts',(2.08437675005714,4.45525140051145,16.3302385459353));
#26333=CARTESIAN_POINT('Ctrl Pts',(2.02201684702941,4.48389776952965,16.3341187629346));
#26334=CARTESIAN_POINT('Ctrl Pts',(1.8843220364278,4.54369409019706,16.3426291220493));
#26335=CARTESIAN_POINT('Ctrl Pts',(1.80877082889211,4.57429485104697,16.3472620295794));
#26336=CARTESIAN_POINT('Ctrl Pts',(1.58235888337296,4.65951257839769,16.3610490374727));
#26337=CARTESIAN_POINT('Ctrl Pts',(1.42954923481427,4.70864154935364,16.37023178492));
#26338=CARTESIAN_POINT('Ctrl Pts',(1.17025626710656,4.7782170357044,16.385597916378));
#26339=CARTESIAN_POINT('Ctrl Pts',(1.06500290883647,4.80277284323968,16.3917767760565));
#26340=CARTESIAN_POINT('Ctrl Pts',(0.91864851863792,4.83186948335065,16.400268478949));
#26341=CARTESIAN_POINT('Ctrl Pts',(0.878171926498472,4.83938962410504,16.4026064539316));
#26342=CARTESIAN_POINT('Ctrl Pts',(0.804813406509809,4.85206820583883,16.4068227350261));
#26343=CARTESIAN_POINT('Ctrl Pts',(0.771964585679908,4.85740272158678,16.4087032539633));
#26344=CARTESIAN_POINT('Ctrl Pts',(0.693052811795507,4.86939696443003,16.4132060363756));
#26345=CARTESIAN_POINT('Ctrl Pts',(0.646944421803848,4.87573706904295,16.4158250411155));
#26346=CARTESIAN_POINT('Ctrl Pts',(0.504869292626538,4.89322214301878,16.4238686767958));
#26347=CARTESIAN_POINT('Ctrl Pts',(0.408658490960322,4.9021948525179,16.4292791304113));
#26348=CARTESIAN_POINT('Ctrl Pts',(0.156016665095246,4.9182667785227,16.443460878629));
#26349=CARTESIAN_POINT('Ctrl Pts',(-0.000596170775789447,4.9207406136419,
16.4522286612861));
#26350=CARTESIAN_POINT('Ctrl Pts',(-0.228838237714226,4.91344824948127,
16.4650928524501));
#26351=CARTESIAN_POINT('Ctrl Pts',(-0.300558463776009,4.90958298568872,
16.4691470686148));
#26352=CARTESIAN_POINT('Ctrl Pts',(-0.435830583027537,4.89931740790259,
16.4768258812867));
#26353=CARTESIAN_POINT('Ctrl Pts',(-0.499392842118374,4.89324698291994,
16.4804474715297));
#26354=CARTESIAN_POINT('Ctrl Pts',(-0.635825294570917,4.87753113609829,
16.4882548990247));
#26355=CARTESIAN_POINT('Ctrl Pts',(-0.708633967692077,4.86748616222254,
16.4924423925208));
#26356=CARTESIAN_POINT('Ctrl Pts',(-0.915856476843084,4.83414878672588,
16.504425014285));
#26357=CARTESIAN_POINT('Ctrl Pts',(-1.04956320196758,4.80689133539,16.5122360962206));
#26358=CARTESIAN_POINT('Ctrl Pts',(-1.27845798040773,4.75022212984519,16.5257307199666));
#26359=CARTESIAN_POINT('Ctrl Pts',(-1.3742074236622,4.7234118381211,16.5314132189931));
#26360=CARTESIAN_POINT('Ctrl Pts',(-1.50812317232462,4.68149776540023,16.5393980527388));
#26361=CARTESIAN_POINT('Ctrl Pts',(-1.54701351207227,4.66879064493385,16.5417213444778));
#26362=CARTESIAN_POINT('Ctrl Pts',(-1.61733021741208,4.64484011230029,16.5459281650604));
#26363=CARTESIAN_POINT('Ctrl Pts',(-1.64880918460329,4.63375927317048,16.5478138303745));
#26364=CARTESIAN_POINT('Ctrl Pts',(-1.72424316887052,4.60633990630413,16.5523414308717));
#26365=CARTESIAN_POINT('Ctrl Pts',(-1.76808215225237,4.58969142707244,16.5549800415298));
#26366=CARTESIAN_POINT('Ctrl Pts',(-1.90298793269132,4.53623926683041,16.5631334486788));
#26367=CARTESIAN_POINT('Ctrl Pts',(-1.99319548371995,4.49733273347707,16.5686336625195));
#26368=CARTESIAN_POINT('Ctrl Pts',(-2.22112832413141,4.39081944415703,16.5827279988945));
#26369=CARTESIAN_POINT('Ctrl Pts',(-2.35696414470608,4.31942423390621,16.5913191375308));
#26370=CARTESIAN_POINT('Ctrl Pts',(-2.55131572875492,4.20537173537503,16.6040130836264));
#26371=CARTESIAN_POINT('Ctrl Pts',(-2.61258326118298,4.16758586320101,16.6080760674647));
#26372=CARTESIAN_POINT('Ctrl Pts',(-2.72662504582345,4.09374891572072,16.6157657741928));
#26373=CARTESIAN_POINT('Ctrl Pts',(-2.77956911217855,4.05798715645921,16.6193894513888));
#26374=CARTESIAN_POINT('Ctrl Pts',(-2.89174462314117,3.97899123865249,16.6271889694607));
#26375=CARTESIAN_POINT('Ctrl Pts',(-2.95073629188274,3.93544323171193,16.6313664136608));
#26376=CARTESIAN_POINT('Ctrl Pts',(-3.11583855531148,3.80776386669652,16.6432816121659));
#26377=CARTESIAN_POINT('Ctrl Pts',(-3.21947860345625,3.72054737041113,16.6510350791738));
#26378=CARTESIAN_POINT('Ctrl Pts',(-3.39408055564127,3.56084914488801,16.664576788578));
#26379=CARTESIAN_POINT('Ctrl Pts',(-3.46664763810893,3.49024124729134,16.6703634733672));
#26380=CARTESIAN_POINT('Ctrl Pts',(-3.56536507833701,3.3880707126168,16.678447641838));
#26381=CARTESIAN_POINT('Ctrl Pts',(-3.59337878763188,3.35834486715548,16.6807670427508));
#26382=CARTESIAN_POINT('Ctrl Pts',(-3.64361961303344,3.30368499378094,16.6849714183618));
#26383=CARTESIAN_POINT('Ctrl Pts',(-3.66596911359085,3.2788670160264,16.6868585089227));
#26384=CARTESIAN_POINT('Ctrl Pts',(-3.71915048020074,3.21858829610938,16.6913929455595));
#26385=CARTESIAN_POINT('Ctrl Pts',(-3.74973039223268,3.18290951097868,16.6940369490131));
#26386=CARTESIAN_POINT('Ctrl Pts',(-3.84292225891082,3.07097155732226,16.7022207793294));
#26387=CARTESIAN_POINT('Ctrl Pts',(-3.90375430148599,2.99326249140501,16.7077459105216));
#26388=CARTESIAN_POINT('Ctrl Pts',(-4.05256254632287,2.79091021575616,16.7218170709338));
#26389=CARTESIAN_POINT('Ctrl Pts',(-4.1371523699694,2.66390926434112,16.7303602423759));
#26390=CARTESIAN_POINT('Ctrl Pts',(-4.25279560296228,2.47145680855265,16.7430078317623));
#26391=CARTESIAN_POINT('Ctrl Pts',(-4.28852688842939,2.40892220036228,16.7470730553598));
#26392=CARTESIAN_POINT('Ctrl Pts',(-4.35334480409,2.28946601436645,16.7547655542114));
#26393=CARTESIAN_POINT('Ctrl Pts',(-4.3827202092115,2.23271786570329,16.7583897737235));
#26394=CARTESIAN_POINT('Ctrl Pts',(-4.44339073612706,2.10969917772394,16.7661873305752));
#26395=CARTESIAN_POINT('Ctrl Pts',(-4.47432722370128,2.04326885194887,16.7703622578942));
#26396=CARTESIAN_POINT('Ctrl Pts',(-4.55807085702216,1.85241413428989,16.7822606351142));
#26397=CARTESIAN_POINT('Ctrl Pts',(-4.60724946439388,1.72647041144817,16.7899997377937));
#26398=CARTESIAN_POINT('Ctrl Pts',(-4.68417348698489,1.50266621206,16.8035435174551));
#26399=CARTESIAN_POINT('Ctrl Pts',(-4.71418893700768,1.40567066878571,16.8093465351146));
#26400=CARTESIAN_POINT('Ctrl Pts',(-4.74905764439672,1.2792622310191,16.8168082304702));
#26401=CARTESIAN_POINT('Ctrl Pts',(-4.75667563174419,1.25063875536686,16.8184911850632));
#26402=CARTESIAN_POINT('Ctrl Pts',(-4.76403458706411,1.22194824594044,16.8201710428097));
#26403=CARTESIAN_POINT('Origin',(0.,0.,-3.23514056400928));
#26404=CARTESIAN_POINT('',(-4.76403456361785,1.22194833735086,18.9152905258446));
#26405=CARTESIAN_POINT('',(-4.76403458707798,1.22194824588636,18.5697043142649));
#26406=CARTESIAN_POINT('',(-4.76403458704967,1.22194824599672,-3.23514056400928));
#26407=CARTESIAN_POINT('Ctrl Pts',(-4.76403456361784,1.22194833735086,18.9152905258446));
#26408=CARTESIAN_POINT('Ctrl Pts',(-4.74331547396517,1.30272626896624,18.9105214132134));
#26409=CARTESIAN_POINT('Ctrl Pts',(-4.72054074812226,1.38298175666518,18.9057455795195));
#26410=CARTESIAN_POINT('Ctrl Pts',(-4.67259489281969,1.53690982447573,18.8965178438601));
#26411=CARTESIAN_POINT('Ctrl Pts',(-4.6477009457191,1.61062437622381,18.8920680814749));
#26412=CARTESIAN_POINT('Ctrl Pts',(-4.60234199617997,1.73511486013049,18.8845088175739));
#26413=CARTESIAN_POINT('Ctrl Pts',(-4.58275874947153,1.78619645364731,18.8813941071591));
#26414=CARTESIAN_POINT('Ctrl Pts',(-4.56084535866196,1.84062174824491,18.8780640956766));
#26415=CARTESIAN_POINT('Ctrl Pts',(-4.55935896037133,1.84430059271013,18.8778389494523));
#26416=CARTESIAN_POINT('Ctrl Pts',(-4.55577765380504,1.85313355836085,18.8772982372327));
#26417=CARTESIAN_POINT('Ctrl Pts',(-4.55367844734684,1.85828593449496,18.8769827247596));
#26418=CARTESIAN_POINT('Ctrl Pts',(-4.54880708197402,1.8701845872421,18.8762538510388));
#26419=CARTESIAN_POINT('Ctrl Pts',(-4.54602864822168,1.87692828562131,18.8758405728594));
#26420=CARTESIAN_POINT('Ctrl Pts',(-4.52668380042765,1.92358634667714,18.8729799660891));
#26421=CARTESIAN_POINT('Ctrl Pts',(-4.50960680919958,1.96328733180964,18.8705395254828));
#26422=CARTESIAN_POINT('Ctrl Pts',(-4.4323985011956,2.13645868988737,18.859853968443));
#26423=CARTESIAN_POINT('Ctrl Pts',(-4.36684822964812,2.26743239048121,18.8516633598902));
#26424=CARTESIAN_POINT('Ctrl Pts',(-4.24397687663926,2.48778185527467,18.8375288983511));
#26425=CARTESIAN_POINT('Ctrl Pts',(-4.1894267834232,2.57858513362137,18.8315944357521));
#26426=CARTESIAN_POINT('Ctrl Pts',(-4.0864211867594,2.73813863991214,18.8209185600211));
#26427=CARTESIAN_POINT('Ctrl Pts',(-4.03905337544367,2.80754143841542,18.816185992228));
#26428=CARTESIAN_POINT('Ctrl Pts',(-3.98492200464019,2.88264688888495,18.8109547034095));
#26429=CARTESIAN_POINT('Ctrl Pts',(-3.97989429229864,2.88958438030849,18.8104704363744));
#26430=CARTESIAN_POINT('Ctrl Pts',(-3.97132223061989,2.90134773059473,18.8096474979743));
#26431=CARTESIAN_POINT('Ctrl Pts',(-3.96778714744651,2.90618032229719,18.8093089003546));
#26432=CARTESIAN_POINT('Ctrl Pts',(-3.96028652085849,2.91639476493261,18.808592113452));
#26433=CARTESIAN_POINT('Ctrl Pts',(-3.95631881224679,2.92177500981004,18.8082139076738));
#26434=CARTESIAN_POINT('Ctrl Pts',(-3.94637763523444,2.93519794726404,18.807268695356));
#26435=CARTESIAN_POINT('Ctrl Pts',(-3.94039054269775,2.94323050406777,18.8067015819093));
#26436=CARTESIAN_POINT('Ctrl Pts',(-3.92175019846475,2.96808041841473,18.8049424998919));
#26437=CARTESIAN_POINT('Ctrl Pts',(-3.90901353788586,2.98483486073109,18.803749873941));
#26438=CARTESIAN_POINT('Ctrl Pts',(-3.84500654484156,3.06792049441307,18.7978020625483));
#26439=CARTESIAN_POINT('Ctrl Pts',(-3.79215405127514,3.13301434695902,18.79303457245));
#26440=CARTESIAN_POINT('Ctrl Pts',(-3.61644844325143,3.33845227855855,18.7776223797244));
#26441=CARTESIAN_POINT('Ctrl Pts',(-3.48727028426456,3.47316972420027,18.7669363710144));
#26442=CARTESIAN_POINT('Ctrl Pts',(-3.30668401638911,3.64124275027415,18.7528282260749));
#26443=CARTESIAN_POINT('Ctrl Pts',(-3.26186191996734,3.68144874324259,18.749389119728));
#26444=CARTESIAN_POINT('Ctrl Pts',(-3.20734839953662,3.72857073295407,18.7452831735555));
#26445=CARTESIAN_POINT('Ctrl Pts',(-3.19835607152841,3.73628718212743,18.7446083207139));
#26446=CARTESIAN_POINT('Ctrl Pts',(-3.15849923618768,3.77023959109998,18.7416280449013));
#26447=CARTESIAN_POINT('Ctrl Pts',(-3.1273389504335,3.79612633309031,18.7393267383424));
#26448=CARTESIAN_POINT('Ctrl Pts',(-3.06391563619396,3.84750495440327,18.7347020173427));
#26449=CARTESIAN_POINT('Ctrl Pts',(-3.03164559625151,3.87298314280356,18.7323790773355));
#26450=CARTESIAN_POINT('Ctrl Pts',(-2.83739336582278,4.02243567776609,18.7185591414124));
#26451=CARTESIAN_POINT('Ctrl Pts',(-2.66814404746926,4.13664104667713,18.7071771348875));
#26452=CARTESIAN_POINT('Ctrl Pts',(-2.42070239545599,4.2820881300412,18.6910796324424));
#26453=CARTESIAN_POINT('Ctrl Pts',(-2.34805937958714,4.32234841519318,18.6864165131972));
#26454=CARTESIAN_POINT('Ctrl Pts',(-2.21036581048511,4.39416512528423,18.6776722299491));
#26455=CARTESIAN_POINT('Ctrl Pts',(-2.14557111528362,4.42616409519408,18.6735952422316));
#26456=CARTESIAN_POINT('Ctrl Pts',(-2.03375504054126,4.47835223370126,18.6666142786657));
#26457=CARTESIAN_POINT('Ctrl Pts',(-1.98708035219212,4.49925659514901,18.663716171536));
#26458=CARTESIAN_POINT('Ctrl Pts',(-1.84899445025305,4.55853374101028,18.6551847448496));
#26459=CARTESIAN_POINT('Ctrl Pts',(-1.75673991932869,4.59487484331288,18.6495385595352));
#26460=CARTESIAN_POINT('Ctrl Pts',(-1.51187559547353,4.68287925285433,18.6346799291894));
#26461=CARTESIAN_POINT('Ctrl Pts',(-1.35771565104458,4.72987671766496,18.6254498601078));
#26462=CARTESIAN_POINT('Ctrl Pts',(-1.1460382011886,4.78320543242144,18.6129692926602));
#26463=CARTESIAN_POINT('Ctrl Pts',(-1.09030700296731,4.7962160588261,18.6097015638274));
#26464=CARTESIAN_POINT('Ctrl Pts',(-1.03008590310075,4.80917094919228,18.6061925521158));
#26465=CARTESIAN_POINT('Ctrl Pts',(-1.02580940221503,4.81008495316844,18.6059434846124));
#26466=CARTESIAN_POINT('Ctrl Pts',(-1.01791645631458,4.81176088449988,18.60548401379));
#26467=CARTESIAN_POINT('Ctrl Pts',(-1.01430036120518,4.81252444138505,18.6052735964848));
#26468=CARTESIAN_POINT('Ctrl Pts',(-0.973546885426587,4.82108177197463,
18.6029031641354));
#26469=CARTESIAN_POINT('Ctrl Pts',(-0.936321102980405,4.8284496291812,18.6007470353921));
#26470=CARTESIAN_POINT('Ctrl Pts',(-0.873978816667656,4.8400405466355,18.5971527857277));
#26471=CARTESIAN_POINT('Ctrl Pts',(-0.84890835220697,4.84450060201537,18.595711964562));
#26472=CARTESIAN_POINT('Ctrl Pts',(-0.75974656572301,4.85964916895445,18.5906021171547));
#26473=CARTESIAN_POINT('Ctrl Pts',(-0.695478952343455,4.86926216912934,
18.5869450359429));
#26474=CARTESIAN_POINT('Ctrl Pts',(-0.46170684271573,4.89950642840237,18.5737031774756));
#26475=CARTESIAN_POINT('Ctrl Pts',(-0.291348085244922,4.9125811092282,18.5641647883729));
#26476=CARTESIAN_POINT('Ctrl Pts',(-0.0157370415834658,4.91934444192025,
18.5486954685866));
#26477=CARTESIAN_POINT('Ctrl Pts',(0.0892350633911437,4.91856016626208,
18.5427958008881));
#26478=CARTESIAN_POINT('Ctrl Pts',(0.260461738125204,4.91179737069259,18.5331257181379));
#26479=CARTESIAN_POINT('Ctrl Pts',(0.326762435415399,4.90783250641799,18.529370049241));
#26480=CARTESIAN_POINT('Ctrl Pts',(0.472998047124371,4.8961109909255,18.5210536235431));
#26481=CARTESIAN_POINT('Ctrl Pts',(0.552864285732227,4.88773678226556,18.5164898330699));
#26482=CARTESIAN_POINT('Ctrl Pts',(0.824786360210946,4.85247469201418,18.500864979913));
#26483=CARTESIAN_POINT('Ctrl Pts',(1.01543957466489,4.81618774613089,18.4897549361265));
#26484=CARTESIAN_POINT('Ctrl Pts',(1.24466147200319,4.75834083312858,18.4762344179359));
#26485=CARTESIAN_POINT('Ctrl Pts',(1.28573712979467,4.74740663127209,18.4738054610475));
#26486=CARTESIAN_POINT('Ctrl Pts',(1.3531652380119,4.72851818362406,18.4698094694641));
#26487=CARTESIAN_POINT('Ctrl Pts',(1.37960178212249,4.72087272733882,18.4682405394414));
#26488=CARTESIAN_POINT('Ctrl Pts',(1.44748601296393,4.70062166242236,18.4642068063837));
#26489=CARTESIAN_POINT('Ctrl Pts',(1.48883406622992,4.68768951107477,18.461745031288));
#26490=CARTESIAN_POINT('Ctrl Pts',(1.5634335450985,4.66327092548179,18.4572970454119));
#26491=CARTESIAN_POINT('Ctrl Pts',(1.59674276797096,4.65197084403027,18.4553087456745));
#26492=CARTESIAN_POINT('Ctrl Pts',(1.70303869251309,4.61463399606859,18.4489516084091));
#26493=CARTESIAN_POINT('Ctrl Pts',(1.77553287830717,4.58722911197688,18.4445974415642));
#26494=CARTESIAN_POINT('Ctrl Pts',(2.01205070919356,4.49137140570089,18.4302796294759));
#26495=CARTESIAN_POINT('Ctrl Pts',(2.1730122675289,4.41574260694886,18.4203507765915));
#26496=CARTESIAN_POINT('Ctrl Pts',(2.40802001438941,4.28935494795731,18.4053577676388));
#26497=CARTESIAN_POINT('Ctrl Pts',(2.48535059699469,4.24501571294973,18.4003396591303));
#26498=CARTESIAN_POINT('Ctrl Pts',(2.6188505417372,4.16357162525271,18.3915056740083));
#26499=CARTESIAN_POINT('Ctrl Pts',(2.67554303374626,4.1273691595809,18.3876978955025));
#26500=CARTESIAN_POINT('Ctrl Pts',(2.80870470490234,4.03843851125573,18.3786104040157));
#26501=CARTESIAN_POINT('Ctrl Pts',(2.8844575039534,3.98468472016957,18.3733239310374));
#26502=CARTESIAN_POINT('Ctrl Pts',(3.06187679492681,3.85107708833363,18.3606481070797));
#26503=CARTESIAN_POINT('Ctrl Pts',(3.16200656322906,3.76929680170268,18.3532500156859));
#26504=CARTESIAN_POINT('Ctrl Pts',(3.31872804282334,3.63065140726908,18.3412729665813));
#26505=CARTESIAN_POINT('Ctrl Pts',(3.37735521158827,3.57617915700307,18.3366955264814));
#26506=CARTESIAN_POINT('Ctrl Pts',(3.4539620199916,3.50143671904021,18.3305885758325));
#26507=CARTESIAN_POINT('Ctrl Pts',(3.47314083462827,3.48241374425074,18.3290487354499));
#26508=CARTESIAN_POINT('Ctrl Pts',(3.52230078270599,3.43284316368129,18.3250739371256));
#26509=CARTESIAN_POINT('Ctrl Pts',(3.55204178645288,3.40206028665405,18.3226419928334));
#26510=CARTESIAN_POINT('Ctrl Pts',(3.60566526651638,3.34508846188033,18.3182089382677));
#26511=CARTESIAN_POINT('Ctrl Pts',(3.6296736743275,3.31902212690641,18.3162059213692));
#26512=CARTESIAN_POINT('Ctrl Pts',(3.70718304469727,3.23302196203446,18.3096738867691));
#26513=CARTESIAN_POINT('Ctrl Pts',(3.75949794688644,3.17203602794524,18.3051607434742));
#26514=CARTESIAN_POINT('Ctrl Pts',(3.90592101805128,2.99263026832876,18.2921708848987));
#26515=CARTESIAN_POINT('Ctrl Pts',(3.99609099271128,2.87111680554166,18.2837160468752));
#26516=CARTESIAN_POINT('Ctrl Pts',(4.10717053216583,2.70603261900159,18.2725475403385));
#26517=CARTESIAN_POINT('Ctrl Pts',(4.13324426754204,2.66603715400445,18.2698652807778));
#26518=CARTESIAN_POINT('Ctrl Pts',(4.20082947598973,2.55899061532629,18.2627426117146));
#26519=CARTESIAN_POINT('Ctrl Pts',(4.24131742945594,2.49131040234965,18.2582965546766));
#26520=CARTESIAN_POINT('Ctrl Pts',(4.31382091614593,2.36321849553766,18.2499735081212));
#26521=CARTESIAN_POINT('Ctrl Pts',(4.34623819659401,2.30305578580205,18.2461006861971));
#26522=CARTESIAN_POINT('Ctrl Pts',(4.42995226050839,2.13962565086336,18.2356685670212));
#26523=CARTESIAN_POINT('Ctrl Pts',(4.47888849303855,2.03519833781208,18.2290945535841));
#26524=CARTESIAN_POINT('Ctrl Pts',(4.57932783599482,1.79965482994503,18.2144561737728));
#26525=CARTESIAN_POINT('Ctrl Pts',(4.62896087317258,1.6678495450905,18.2063895953891));
#26526=CARTESIAN_POINT('Ctrl Pts',(4.68984673460836,1.48239076888442,18.1952324246198));
#26527=CARTESIAN_POINT('Ctrl Pts',(4.70596263479696,1.43040572405521,18.1921258050919));
#26528=CARTESIAN_POINT('Ctrl Pts',(4.73352063901732,1.33599952324321,18.1865251339607));
#26529=CARTESIAN_POINT('Ctrl Pts',(4.74526343128659,1.29367205803261,18.1840287758328));
#26530=CARTESIAN_POINT('Ctrl Pts',(4.76531565313282,1.21744307507194,18.1795617109125));
#26531=CARTESIAN_POINT('Ctrl Pts',(4.77383411874656,1.18359990946682,18.1775887127222));
#26532=CARTESIAN_POINT('Ctrl Pts',(4.79963766521207,1.07627129349993,18.1713592553093));
#26533=CARTESIAN_POINT('Ctrl Pts',(4.81559158360528,1.00247669492993,18.1671167038135));
#26534=CARTESIAN_POINT('Ctrl Pts',(4.86546509040271,0.74300260833375,18.1522907914608));
#26535=CARTESIAN_POINT('Ctrl Pts',(4.89039143466943,0.555765186730222,18.141749493902));
#26536=CARTESIAN_POINT('Ctrl Pts',(4.90750993087085,0.327346215257011,18.1288740250851));
#26537=CARTESIAN_POINT('Ctrl Pts',(4.91002895502809,0.287097376274816,18.1266049962327));
#26538=CARTESIAN_POINT('Ctrl Pts',(4.91566931740542,0.174847546183887,18.1202728968596));
#26539=CARTESIAN_POINT('Ctrl Pts',(4.91770352577797,0.102802612872553,18.1162040803201));
#26540=CARTESIAN_POINT('Ctrl Pts',(4.91854814053675,-0.0323307908643089,
18.108553928296));
#26541=CARTESIAN_POINT('Ctrl Pts',(4.91772908478377,-0.0954024630838392,
18.1049758597525));
#26542=CARTESIAN_POINT('Ctrl Pts',(4.91144360896867,-0.29041258890819,18.0938830156863));
#26543=CARTESIAN_POINT('Ctrl Pts',(4.90187712319243,-0.422158403298321,
18.0863450969728));
#26544=CARTESIAN_POINT('Ctrl Pts',(4.87016907421694,-0.702190421400551,
18.0702208916673));
#26545=CARTESIAN_POINT('Ctrl Pts',(4.84652652849525,-0.850175949269935,
18.0616376116439));
#26546=CARTESIAN_POINT('Ctrl Pts',(4.81106144783633,-1.02152114834946,18.0516583772163));
#26547=CARTESIAN_POINT('Ctrl Pts',(4.80576589326066,-1.04615099265636,18.0502229965166));
#26548=CARTESIAN_POINT('Ctrl Pts',(4.79137211451767,-1.11068042316063,18.0464604968913));
#26549=CARTESIAN_POINT('Ctrl Pts',(4.78196467346111,-1.15050930574099,18.04413634206));
#26550=CARTESIAN_POINT('Ctrl Pts',(4.76167176661313,-1.23187181011136,18.039386944299));
#26551=CARTESIAN_POINT('Ctrl Pts',(4.75073731035936,-1.27338966353862,18.0369623998446));
#26552=CARTESIAN_POINT('Ctrl Pts',(4.70694968965091,-1.43122915536108,18.0277304060125));
#26553=CARTESIAN_POINT('Ctrl Pts',(4.67035597288275,-1.54646951223147,18.0209588269278));
#26554=CARTESIAN_POINT('Ctrl Pts',(4.5713079954746,-1.82266235687388,18.0045203401299));
#26555=CARTESIAN_POINT('Ctrl Pts',(4.50455618028888,-1.98189998903594,17.9948621162993));
#26556=CARTESIAN_POINT('Ctrl Pts',(4.39840505843221,-2.20189937047227,17.9810987840984));
#26557=CARTESIAN_POINT('Ctrl Pts',(4.36582559194621,-2.26580993034484,17.9770486861306));
#26558=CARTESIAN_POINT('Ctrl Pts',(4.30188458165883,-2.38473880885627,17.9694040638177));
#26559=CARTESIAN_POINT('Ctrl Pts',(4.27083545710979,-2.43990871305937,17.9658126475643));
#26560=CARTESIAN_POINT('Ctrl Pts',(4.13969760851285,-2.66274539497912,17.9511112104505));
#26561=CARTESIAN_POINT('Ctrl Pts',(4.03073247449989,-2.82497842561231,17.9399400865834));
#26562=CARTESIAN_POINT('Ctrl Pts',(3.84296214492703,-3.07147543978423,17.9222038630931));
#26563=CARTESIAN_POINT('Ctrl Pts',(3.77034326363936,-3.16019486555355,17.9156492440026));
#26564=CARTESIAN_POINT('Ctrl Pts',(3.66859948150952,-3.27599198151733,17.906880747125));
#26565=CARTESIAN_POINT('Ctrl Pts',(3.64215089276217,-3.30537177268705,17.9046367138011));
#26566=CARTESIAN_POINT('Ctrl Pts',(3.58485493361127,-3.36749483388145,17.8998519211714));
#26567=CARTESIAN_POINT('Ctrl Pts',(3.55390672259805,-3.4001402063459,17.8973127737319));
#26568=CARTESIAN_POINT('Ctrl Pts',(3.38477137782874,-3.57371824985804,17.8836595478276));
#26569=CARTESIAN_POINT('Ctrl Pts',(3.23864219654943,-3.70666125076684,17.8726437104261));
#26570=CARTESIAN_POINT('Ctrl Pts',(2.99748624658588,-3.90087966654925,17.8552760713994));
#26571=CARTESIAN_POINT('Ctrl Pts',(2.9076686646918,-3.96828028925259,17.8489682732907));
#26572=CARTESIAN_POINT('Ctrl Pts',(2.759741980571,-4.07156635191415,17.8387890463593));
#26573=CARTESIAN_POINT('Ctrl Pts',(2.70305491952036,-4.10941873285273,17.8349353588157));
#26574=CARTESIAN_POINT('Ctrl Pts',(2.57847922797815,-4.18891006080834,17.8265588309162));
#26575=CARTESIAN_POINT('Ctrl Pts',(2.51032891672712,-4.23010297089548,17.8220336571834));
#26576=CARTESIAN_POINT('Ctrl Pts',(2.20981143096148,-4.40192752907998,17.8023096676312));
#26577=CARTESIAN_POINT('Ctrl Pts',(1.96804312816243,-4.51520067131362,17.7870002676973));
#26578=CARTESIAN_POINT('Ctrl Pts',(1.67796740621951,-4.62336031206839,17.7693733263332));
#26579=CARTESIAN_POINT('Ctrl Pts',(1.63744705691092,-4.63786614560272,17.7669278800102));
#26580=CARTESIAN_POINT('Ctrl Pts',(1.56334019641478,-4.66330328921069,17.7624882526341));
#26581=CARTESIAN_POINT('Ctrl Pts',(1.52981644233962,-4.67440817830512,17.7604920822536));
#26582=CARTESIAN_POINT('Ctrl Pts',(1.42125980145311,-4.70907511160374,17.7540622424194));
#26583=CARTESIAN_POINT('Ctrl Pts',(1.34578002100625,-4.73119902290545,17.7496437052549));
#26584=CARTESIAN_POINT('Ctrl Pts',(1.09064828138368,-4.79938095386135,17.7348287658821));
#26585=CARTESIAN_POINT('Ctrl Pts',(0.908931080695871,-4.83708748441574,
17.7244695065817));
#26586=CARTESIAN_POINT('Ctrl Pts',(0.6415110163948,-4.87697254075507,17.7092703142488));
#26587=CARTESIAN_POINT('Ctrl Pts',(0.557192399668656,-4.88732380145958,
17.7044855069337));
#26588=CARTESIAN_POINT('Ctrl Pts',(0.405523652805788,-4.9019670964302,17.6958748820173));
#26589=CARTESIAN_POINT('Ctrl Pts',(0.338272845491704,-4.90706655697591,
17.6920555763784));
#26590=CARTESIAN_POINT('Ctrl Pts',(0.172236881465047,-4.91622713863244,
17.6826149510968));
#26591=CARTESIAN_POINT('Ctrl Pts',(0.0733940364577686,-4.91869573819681,
17.6769848701628));
#26592=CARTESIAN_POINT('Ctrl Pts',(-0.186919709866415,-4.91734843654965,
17.6621198124596));
#26593=CARTESIAN_POINT('Ctrl Pts',(-0.348245052206564,-4.90856187094722,
17.652866874697));
#26594=CARTESIAN_POINT('Ctrl Pts',(-0.588161850295145,-4.88360604887743,
17.6390758512608));
#26595=CARTESIAN_POINT('Ctrl Pts',(-0.667267735593434,-4.87342758288902,
17.6345243973836));
#26596=CARTESIAN_POINT('Ctrl Pts',(-0.783357993448415,-4.85561065178102,
17.6278484082831));
#26597=CARTESIAN_POINT('Ctrl Pts',(-0.820557540131678,-4.84946284958733,
17.6257098797528));
#26598=CARTESIAN_POINT('Ctrl Pts',(-0.906748443653881,-4.83419830280463,
17.6207575078797));
#26599=CARTESIAN_POINT('Ctrl Pts',(-0.955679237668195,-4.82476354321358,
17.6179472489411));
#26600=CARTESIAN_POINT('Ctrl Pts',(-1.19056360995287,-4.7757600391135,17.6044422090022));
#26601=CARTESIAN_POINT('Ctrl Pts',(-1.37426212397276,-4.72617502712813,
17.593829082158));
#26602=CARTESIAN_POINT('Ctrl Pts',(-1.65926931602333,-4.63121726488516,
17.5769773768778));
#26603=CARTESIAN_POINT('Ctrl Pts',(-1.76270571193812,-4.59284401591475,
17.5707792420145));
#26604=CARTESIAN_POINT('Ctrl Pts',(-1.92772432370149,-4.525228346797,17.560716817535));
#26605=CARTESIAN_POINT('Ctrl Pts',(-1.99014251309905,-4.49812686564716,
17.5568693643289));
#26606=CARTESIAN_POINT('Ctrl Pts',(-2.12484940903831,-4.43628532535048,
17.5484669222303));
#26607=CARTESIAN_POINT('Ctrl Pts',(-2.19689130411521,-4.40105451918029,
17.5439093998879));
#26608=CARTESIAN_POINT('Ctrl Pts',(-2.39074871964318,-4.30030560310476,
17.5314601469033));
#26609=CARTESIAN_POINT('Ctrl Pts',(-2.51071303830721,-4.23138595886653,
17.523549789167));
#26610=CARTESIAN_POINT('Ctrl Pts',(-2.73969921218768,-4.08666284233317,
17.5080429013634));
#26611=CARTESIAN_POINT('Ctrl Pts',(-2.84887643505824,-4.0113175666439,17.500453336624));
#26612=CARTESIAN_POINT('Ctrl Pts',(-2.98742940470873,-3.90718657077729,
17.4905904903077));
#26613=CARTESIAN_POINT('Ctrl Pts',(-3.01967781271314,-3.88231726084807,
17.4882778697887));
#26614=CARTESIAN_POINT('Ctrl Pts',(-3.08547956492844,-3.83025634968345,
17.4835258138457));
#26615=CARTESIAN_POINT('Ctrl Pts',(-3.11899113042396,-3.80301751728287,
17.4810871931756));
#26616=CARTESIAN_POINT('Ctrl Pts',(-3.26659537985682,-3.67977850965094,
17.4702502282586));
#26617=CARTESIAN_POINT('Ctrl Pts',(-3.37664721603989,-3.57905990043224,
17.4619086555512));
#26618=CARTESIAN_POINT('Ctrl Pts',(-3.55581846051312,-3.39945240288033,
17.4476952892152));
#26619=CARTESIAN_POINT('Ctrl Pts',(-3.62730180408219,-3.32307131481538,
17.441833947363));
#26620=CARTESIAN_POINT('Ctrl Pts',(-3.72253557251001,-3.21457527778905,
17.433718105896));
#26621=CARTESIAN_POINT('Ctrl Pts',(-3.74841219452511,-3.1843635631397,17.4314796364833));
#26622=CARTESIAN_POINT('Ctrl Pts',(-3.81981495270167,-3.09892228062133,
17.4252054426908));
#26623=CARTESIAN_POINT('Ctrl Pts',(-3.86450588523843,-3.04300832763046,
17.4211639666958));
#26624=CARTESIAN_POINT('Ctrl Pts',(-3.95185751092409,-2.92869126635205,
17.4130184227654));
#26625=CARTESIAN_POINT('Ctrl Pts',(-3.99448221434602,-2.87028256374707,
17.4089151258923));
#26626=CARTESIAN_POINT('Ctrl Pts',(-4.12768848864678,-2.67903291247003,
17.3956550985692));
#26627=CARTESIAN_POINT('Ctrl Pts',(-4.21304875382387,-2.54268532526417,
17.3864635392939));
#26628=CARTESIAN_POINT('Ctrl Pts',(-4.33756876230242,-2.32024684315445,
17.3718707430376));
#26629=CARTESIAN_POINT('Ctrl Pts',(-4.38119174835607,-2.23678501058983,
17.3664808507323));
#26630=CARTESIAN_POINT('Ctrl Pts',(-4.4492827431028,-2.0968649473384,17.3575964777399));
#26631=CARTESIAN_POINT('Ctrl Pts',(-4.47513550988072,-2.04110799178625,
17.3540947494371));
#26632=CARTESIAN_POINT('Ctrl Pts',(-4.51476971886499,-1.95125300532157,
17.3485179449188));
#26633=CARTESIAN_POINT('Ctrl Pts',(-4.52922523739406,-1.91745995938972,
17.3464356708467));
#26634=CARTESIAN_POINT('Ctrl Pts',(-4.56599999550418,-1.82875376661715,
17.3410078714906));
#26635=CARTESIAN_POINT('Ctrl Pts',(-4.58770773675193,-1.77359356809547,
17.3376695546362));
#26636=CARTESIAN_POINT('Ctrl Pts',(-4.66912518485959,-1.55520389979611,
17.3245684348376));
#26637=CARTESIAN_POINT('Ctrl Pts',(-4.7211625410511,-1.38924944582241,17.314860470125));
#26638=CARTESIAN_POINT('Ctrl Pts',(-4.78429915932931,-1.14286976385979,
17.3005925636965));
#26639=CARTESIAN_POINT('Ctrl Pts',(-4.8023725282632,-1.06437196637666,17.2960684497278));
#26640=CARTESIAN_POINT('Ctrl Pts',(-4.83320912146336,-0.913594176086029,
17.2874005955588));
#26641=CARTESIAN_POINT('Ctrl Pts',(-4.84629817455614,-0.841402738694301,
17.2832600223409));
#26642=CARTESIAN_POINT('Ctrl Pts',(-4.86882359396789,-0.699099860195667,
17.275106050713));
#26643=CARTESIAN_POINT('Ctrl Pts',(-4.878371930121,-0.629023815874242,17.2710944068513));
#26644=CARTESIAN_POINT('Ctrl Pts',(-4.90762283464867,-0.373225186314052,
17.2564529353761));
#26645=CARTESIAN_POINT('Ctrl Pts',(-4.91825449348514,-0.186627823734712,
17.245770479597));
#26646=CARTESIAN_POINT('Ctrl Pts',(-4.91824955815441,0.0184161788696644,
17.2340334398973));
#26647=CARTESIAN_POINT('Ctrl Pts',(-4.918147005371,0.0367138400748713,17.2329861343362));
#26648=CARTESIAN_POINT('Ctrl Pts',(-4.91683555630391,0.153957453619647,
17.2262762700073));
#26649=CARTESIAN_POINT('Ctrl Pts',(-4.91274285224247,0.252849349144806,
17.2206199253197));
#26650=CARTESIAN_POINT('Ctrl Pts',(-4.90276274421755,0.392115347569802,
17.2126747798129));
#26651=CARTESIAN_POINT('Ctrl Pts',(-4.89935277553649,0.432642360882363,
17.2103652473645));
#26652=CARTESIAN_POINT('Ctrl Pts',(-4.89127973198438,0.516174812108789,
17.2056123643494));
#26653=CARTESIAN_POINT('Ctrl Pts',(-4.88655116919175,0.559170441647649,
17.2031698603842));
#26654=CARTESIAN_POINT('Ctrl Pts',(-4.86682792173742,0.71906825582968,17.1940902140146));
#26655=CARTESIAN_POINT('Ctrl Pts',(-4.84819988177671,0.835482873806668,
17.1874866343439));
#26656=CARTESIAN_POINT('Ctrl Pts',(-4.80750001899003,1.04197008281173,17.1756954892456));
#26657=CARTESIAN_POINT('Ctrl Pts',(-4.78703320865461,1.13228305424205,17.1705112504368));
#26658=CARTESIAN_POINT('Ctrl Pts',(-4.76403457365963,1.22194829820076,17.1653174600137));
#26659=CARTESIAN_POINT('',(-4.91824992201636,-7.83730597753569E-6,16.8896169247543));
#26660=CARTESIAN_POINT('Ctrl Pts',(-4.76403458706411,1.22194824594044,16.8201710428097));
#26661=CARTESIAN_POINT('Ctrl Pts',(-4.76683376815824,1.21103502143015,16.820810022915));
#26662=CARTESIAN_POINT('Ctrl Pts',(-4.76959547071965,1.20011209781449,16.8214485515573));
#26663=CARTESIAN_POINT('Ctrl Pts',(-4.78039081463275,1.1567890969395,16.8239770185866));
#26664=CARTESIAN_POINT('Ctrl Pts',(-4.78813206739585,1.12431698757102,16.8258632257805));
#26665=CARTESIAN_POINT('Ctrl Pts',(-4.80595938298161,1.04601132814585,16.830393427176));
#26666=CARTESIAN_POINT('Ctrl Pts',(-4.81572122274099,1.00010721898561,16.8330340899698));
#26667=CARTESIAN_POINT('Ctrl Pts',(-4.8738428179346,0.706180720126455,16.8498689318998));
#26668=CARTESIAN_POINT('Ctrl Pts',(-4.90368400624962,0.454882822490331,
16.863950195434));
#26669=CARTESIAN_POINT('Ctrl Pts',(-4.91686092655596,0.134970651184922,
16.8819877004013));
#26670=CARTESIAN_POINT('Ctrl Pts',(-4.91825010759213,0.0674847396381241,
16.8857975340099));
#26671=CARTESIAN_POINT('Ctrl Pts',(-4.91824999999375,-7.84079902334413E-6,
16.8896167897774));
#26672=CARTESIAN_POINT('Ctrl Pts',(-4.91824999999374,-7.84493095884421E-6,
16.8896167900112));
#26673=CARTESIAN_POINT('Ctrl Pts',(-4.9182499406561,-0.0372086038747788,
16.8917218986356));
#26674=CARTESIAN_POINT('Ctrl Pts',(-4.91782781161351,-0.074408016725493,
16.8938296531246));
#26675=CARTESIAN_POINT('Ctrl Pts',(-4.91603513617609,-0.1533922633977,16.8983118618922));
#26676=CARTESIAN_POINT('Ctrl Pts',(-4.9145537589959,-0.195171630419358,
16.9006868621136));
#26677=CARTESIAN_POINT('Ctrl Pts',(-4.90029915421615,-0.490732554241179,
16.9175211677159));
#26678=CARTESIAN_POINT('Ctrl Pts',(-4.86840743386882,-0.743206820677955,
16.9320965060318));
#26679=CARTESIAN_POINT('Ctrl Pts',(-4.80771245688787,-1.03791829214628,
16.9492782213025));
#26680=CARTESIAN_POINT('Ctrl Pts',(-4.79761805181208,-1.08362102737906,
16.9519467852207));
#26681=CARTESIAN_POINT('Ctrl Pts',(-4.77921665046172,-1.16162959670902,
16.9565063199693));
#26682=CARTESIAN_POINT('Ctrl Pts',(-4.77123052301745,-1.19400772017509,
16.9584001692723));
#26683=CARTESIAN_POINT('Ctrl Pts',(-4.75269895615327,-1.26598368377879,
16.9626119081756));
#26684=CARTESIAN_POINT('Ctrl Pts',(-4.74198667733389,-1.30553607717061,
16.9649273551055));
#26685=CARTESIAN_POINT('Ctrl Pts',(-4.70373745743341,-1.44007540284274,
16.972815135504));
#26686=CARTESIAN_POINT('Ctrl Pts',(-4.67383033374763,-1.5343642451736,16.9783635396721));
#26687=CARTESIAN_POINT('Ctrl Pts',(-4.59589210317195,-1.75659305285647,
16.991563184021));
#26688=CARTESIAN_POINT('Ctrl Pts',(-4.54533292936468,-1.88355827876789,
16.9992047563436));
#26689=CARTESIAN_POINT('Ctrl Pts',(-4.45953232575029,-2.07536994975504,
17.011003276141));
#26690=CARTESIAN_POINT('Ctrl Pts',(-4.42800903348103,-2.14180411217169,
17.0151380531904));
#26691=CARTESIAN_POINT('Ctrl Pts',(-4.36635535599447,-2.26455277884726,
17.0228823151365));
#26692=CARTESIAN_POINT('Ctrl Pts',(-4.33659445330829,-2.32103572121766,
17.0264884724047));
#26693=CARTESIAN_POINT('Ctrl Pts',(-4.27101249070263,-2.43983597970989,
17.034172033163));
#26694=CARTESIAN_POINT('Ctrl Pts',(-4.23490783685697,-2.50197976732081,
17.0382507954912));
#26695=CARTESIAN_POINT('Ctrl Pts',(-4.11573940102004,-2.69711972231305,
17.0512601399769));
#26696=CARTESIAN_POINT('Ctrl Pts',(-4.02767305029983,-2.82694434760437,
17.0602234027118));
#26697=CARTESIAN_POINT('Ctrl Pts',(-3.87563938326855,-3.02950686859028,
17.0747218469415));
#26698=CARTESIAN_POINT('Ctrl Pts',(-3.81546241605834,-3.10495397510474,
17.0802456993313));
#26699=CARTESIAN_POINT('Ctrl Pts',(-3.72304455923327,-3.21407618460228,
17.0884108157213));
#26700=CARTESIAN_POINT('Ctrl Pts',(-3.6924818841511,-3.2491420556541,17.091062784323));
#26701=CARTESIAN_POINT('Ctrl Pts',(-3.63921215664185,-3.30853818230312,
17.0956013388401));
#26702=CARTESIAN_POINT('Ctrl Pts',(-3.61674716605781,-3.33308115549669,
17.0974907567837));
#26703=CARTESIAN_POINT('Ctrl Pts',(-3.5659185569494,-3.38749233372036,17.1017099586851));
#26704=CARTESIAN_POINT('Ctrl Pts',(-3.53742522617143,-3.41723605835062,
17.1040372356401));
#26705=CARTESIAN_POINT('Ctrl Pts',(-3.44025786187565,-3.51614972297263,
17.1118560223275));
#26706=CARTESIAN_POINT('Ctrl Pts',(-3.36990173456311,-3.58363582195775,
17.1173245850347));
#26707=CARTESIAN_POINT('Ctrl Pts',(-3.19585635448023,-3.7409204623283,17.1304732700751));
#26708=CARTESIAN_POINT('Ctrl Pts',(-3.09032675873492,-3.82855901390511,
17.1381433476802));
#26709=CARTESIAN_POINT('Ctrl Pts',(-2.92272617665242,-3.95629545377406,
17.1499754693926));
#26710=CARTESIAN_POINT('Ctrl Pts',(-2.86318442822054,-3.99959708141711,
17.1541151588609));
#26711=CARTESIAN_POINT('Ctrl Pts',(-2.75025028128185,-4.07791360674584,
17.1618632466984));
#26712=CARTESIAN_POINT('Ctrl Pts',(-2.69710440767758,-4.11325706668356,
17.1654682887335));
#26713=CARTESIAN_POINT('Ctrl Pts',(-2.5827538493258,-4.18613402094023,17.1731460026015));
#26714=CARTESIAN_POINT('Ctrl Pts',(-2.52138470493362,-4.22338187911524,
17.1772200161051));
#26715=CARTESIAN_POINT('Ctrl Pts',(-2.32215406245505,-4.33841384702664,
17.1903090314727));
#26716=CARTESIAN_POINT('Ctrl Pts',(-2.18134637949275,-4.41089118817675,
17.1993576022221));
#26717=CARTESIAN_POINT('Ctrl Pts',(-1.95014230137425,-4.51611516796321,
17.2138991803865));
#26718=CARTESIAN_POINT('Ctrl Pts',(-1.86185296493187,-4.55322466860793,
17.2193808066606));
#26719=CARTESIAN_POINT('Ctrl Pts',(-1.7293007192413,-4.60443812702757,17.2274944796773));
#26720=CARTESIAN_POINT('Ctrl Pts',(-1.68583069876612,-4.62053095975743,
17.2301371210996));
#26721=CARTESIAN_POINT('Ctrl Pts',(-1.61081791436717,-4.64710155229553,
17.2346639004896));
#26722=CARTESIAN_POINT('Ctrl Pts',(-1.57938453761665,-4.65787845487469,
17.236550844341));
#26723=CARTESIAN_POINT('Ctrl Pts',(-1.51395306982043,-4.67957306199701,
17.2404568802906));
#26724=CARTESIAN_POINT('Ctrl Pts',(-1.4799404065659,-4.69044074283164,17.2424751156509));
#26725=CARTESIAN_POINT('Ctrl Pts',(-1.36899914505102,-4.72456164860013,
17.2490238181737));
#26726=CARTESIAN_POINT('Ctrl Pts',(-1.29161781384732,-4.7463001480696,17.2535384293322));
#26727=CARTESIAN_POINT('Ctrl Pts',(-1.06690019192772,-4.80352648084476,
17.2665458857707));
#26728=CARTESIAN_POINT('Ctrl Pts',(-0.918412913925084,-4.83411423142414,
17.2750167009667));
#26729=CARTESIAN_POINT('Ctrl Pts',(-0.693717780619998,-4.86967244115822,
17.2877856464014));
#26730=CARTESIAN_POINT('Ctrl Pts',(-0.618420010849212,-4.87980640884685,
17.2920559518669));
#26731=CARTESIAN_POINT('Ctrl Pts',(-0.479811557003569,-4.89520127430561,
17.2999156178035));
#26732=CARTESIAN_POINT('Ctrl Pts',(-0.416575485034823,-4.90098759465092,
17.3035008947515));
#26733=CARTESIAN_POINT('Ctrl Pts',(-0.283783852069842,-4.91054984057586,
17.3110360203917));
#26734=CARTESIAN_POINT('Ctrl Pts',(-0.214224289609376,-4.91407578469857,
17.3149867284281));
#26735=CARTESIAN_POINT('Ctrl Pts',(0.0316490666192468,-4.9213084551853,
17.3289745817257));
#26736=CARTESIAN_POINT('Ctrl Pts',(0.208061245372728,-4.91701002417909,
17.3390577479166));
#26737=CARTESIAN_POINT('Ctrl Pts',(0.473134295322018,-4.89625837344953,
17.3542785133904));
#26738=CARTESIAN_POINT('Ctrl Pts',(0.562203186402082,-4.88683229051902,
17.3594038428411));
#26739=CARTESIAN_POINT('Ctrl Pts',(0.695508503642364,-4.869031778393,17.3670809849684));
#26740=CARTESIAN_POINT('Ctrl Pts',(0.739968372798642,-4.86247358796272,
17.3696424493637));
#26741=CARTESIAN_POINT('Ctrl Pts',(0.816961916429679,-4.8500359546179,17.3740778249231));
#26742=CARTESIAN_POINT('Ctrl Pts',(0.849537729134805,-4.84443610856278,
17.3759542768317));
#26743=CARTESIAN_POINT('Ctrl Pts',(0.924028911228534,-4.83085644665498,
17.380243488437));
#26744=CARTESIAN_POINT('Ctrl Pts',(0.965901988871422,-4.82265869019897,
17.3826533743843));
#26745=CARTESIAN_POINT('Ctrl Pts',(1.15754598477091,-4.78254320035006,17.3936901389126));
#26746=CARTESIAN_POINT('Ctrl Pts',(1.30588318341657,-4.74418615847176,17.4022556708684));
#26747=CARTESIAN_POINT('Ctrl Pts',(1.55149358910475,-4.66828166653712,17.4166582271282));
#26748=CARTESIAN_POINT('Ctrl Pts',(1.64979873095074,-4.63445250261479,17.4224834675145));
#26749=CARTESIAN_POINT('Ctrl Pts',(1.78412862038106,-4.58341022674273,17.4305624585805));
#26750=CARTESIAN_POINT('Ctrl Pts',(1.82112686985034,-4.56883586284299,17.4328003118664));
#26751=CARTESIAN_POINT('Ctrl Pts',(1.92449369557707,-4.52666247356809,17.4390912820081));
#26752=CARTESIAN_POINT('Ctrl Pts',(1.99043948193806,-4.49805509581903,17.443150255538));
#26753=CARTESIAN_POINT('Ctrl Pts',(2.12251660826238,-4.43728637121658,17.4513824667194));
#26754=CARTESIAN_POINT('Ctrl Pts',(2.18860126062016,-4.40506656505984,17.4555551712934));
#26755=CARTESIAN_POINT('Ctrl Pts',(2.35543568900626,-4.31904460113421,17.4662362924335));
#26756=CARTESIAN_POINT('Ctrl Pts',(2.45507863244366,-4.26319269916226,17.4727566710008));
#26757=CARTESIAN_POINT('Ctrl Pts',(2.65854114989443,-4.13964718219351,17.4863744119855));
#26758=CARTESIAN_POINT('Ctrl Pts',(2.76193070440002,-4.07139517776031,17.4934693498927));
#26759=CARTESIAN_POINT('Ctrl Pts',(2.90480001019544,-3.96913200708307,17.503508931808));
#26760=CARTESIAN_POINT('Ctrl Pts',(2.94648649402665,-3.93828508282532,17.5064679586548));
#26761=CARTESIAN_POINT('Ctrl Pts',(3.02155255881747,-3.88087899931883,17.5118477848604));
#26762=CARTESIAN_POINT('Ctrl Pts',(3.05508941652167,-3.85453374436886,17.514270603834));
#26763=CARTESIAN_POINT('Ctrl Pts',(3.12101101783324,-3.80134739514397,17.5190692926702));
#26764=CARTESIAN_POINT('Ctrl Pts',(3.1534025737818,-3.77452037383418,17.5214451056121));
#26765=CARTESIAN_POINT('Ctrl Pts',(3.3137768020608,-3.63819126262147,17.5333117882414));
#26766=CARTESIAN_POINT('Ctrl Pts',(3.43642015488624,-3.52258004292693,17.5427264075202));
#26767=CARTESIAN_POINT('Ctrl Pts',(3.63043402176212,-3.31989564739133,17.5584486293972));
#26768=CARTESIAN_POINT('Ctrl Pts',(3.70518304087935,-3.2362596602761,17.5647374046495));
#26769=CARTESIAN_POINT('Ctrl Pts',(3.82603544698187,-3.09135814463713,17.5753584560345));
#26770=CARTESIAN_POINT('Ctrl Pts',(3.87368404362773,-3.03143764009383,17.5796765181378));
#26771=CARTESIAN_POINT('Ctrl Pts',(3.96172553014344,-2.91525409557114,17.5879231331634));
#26772=CARTESIAN_POINT('Ctrl Pts',(4.00236673547217,-2.85920198433273,17.5918485108084));
#26773=CARTESIAN_POINT('Ctrl Pts',(4.16357885728932,-2.62668358152558,17.607930666373));
#26774=CARTESIAN_POINT('Ctrl Pts',(4.2737686847842,-2.44330806048286,17.6201624882223));
#26775=CARTESIAN_POINT('Ctrl Pts',(4.41900557269763,-2.16153706332632,17.6383032501186));
#26776=CARTESIAN_POINT('Ctrl Pts',(4.4634271657228,-2.06825314382132,17.6442072384528));
#26777=CARTESIAN_POINT('Ctrl Pts',(4.52066950472716,-1.93759612130531,17.6523202728613));
#26778=CARTESIAN_POINT('Ctrl Pts',(4.53602732433491,-1.90136468831857,17.6545536972916));
#26779=CARTESIAN_POINT('Ctrl Pts',(4.56865922260557,-1.82173472271906,17.6594250612977));
#26780=CARTESIAN_POINT('Ctrl Pts',(4.58575322658706,-1.77826654584235,17.6620608270097));
#26781=CARTESIAN_POINT('Ctrl Pts',(4.67110681286416,-1.55180208258173,17.6756908288605));
#26782=CARTESIAN_POINT('Ctrl Pts',(4.72904111056056,-1.36510076895345,17.6865919334457));
#26783=CARTESIAN_POINT('Ctrl Pts',(4.79531409463303,-1.09584082731927,17.702145695313));
#26784=CARTESIAN_POINT('Ctrl Pts',(4.81291427397403,-1.01575607806269,17.7067502313632));
#26785=CARTESIAN_POINT('Ctrl Pts',(4.84264007347487,-0.86229104156598,17.7155533783299));
#26786=CARTESIAN_POINT('Ctrl Pts',(4.85511936876258,-0.789002195977594,
17.7197486097811));
#26787=CARTESIAN_POINT('Ctrl Pts',(4.87629931738731,-0.644954579899805,
17.7279883213161));
#26788=CARTESIAN_POINT('Ctrl Pts',(4.88513226089707,-0.574233470319792,
17.7320308799801));
#26789=CARTESIAN_POINT('Ctrl Pts',(4.91143611162197,-0.318565151268578,
17.7466468501595));
#26790=CARTESIAN_POINT('Ctrl Pts',(4.91996296057207,-0.13285780833357,17.7572721194808));
#26791=CARTESIAN_POINT('Ctrl Pts',(4.91665743448756,0.174546046984221,17.7748699046814));
#26792=CARTESIAN_POINT('Ctrl Pts',(4.91083499096335,0.296119722934534,17.78183025779));
#26793=CARTESIAN_POINT('Ctrl Pts',(4.89711999655882,0.457159542235371,17.7910245076019));
#26794=CARTESIAN_POINT('Ctrl Pts',(4.89324494839363,0.496923583102964,17.7932925183525));
#26795=CARTESIAN_POINT('Ctrl Pts',(4.8839192052753,0.581883330872484,17.7981315823567));
#26796=CARTESIAN_POINT('Ctrl Pts',(4.87832465690898,0.627059505105819,17.800700969163));
#26797=CARTESIAN_POINT('Ctrl Pts',(4.84446634353182,0.872482049445226,17.8146571088486));
#26798=CARTESIAN_POINT('Ctrl Pts',(4.80449932921346,1.07091867939412,17.8259411428385));
#26799=CARTESIAN_POINT('Ctrl Pts',(4.73170926027818,1.34409326716187,17.8418007628503));
#26800=CARTESIAN_POINT('Ctrl Pts',(4.70908366565301,1.42133391690607,17.846321445072));
#26801=CARTESIAN_POINT('Ctrl Pts',(4.66215288266024,1.56809828555493,17.8550003432272));
#26802=CARTESIAN_POINT('Ctrl Pts',(4.63816140783909,1.63769970446574,17.8591554630706));
#26803=CARTESIAN_POINT('Ctrl Pts',(4.59068015969314,1.76602232320095,17.8668998894089));
#26804=CARTESIAN_POINT('Ctrl Pts',(4.56760247114469,1.82487992197727,17.8704854749731));
#26805=CARTESIAN_POINT('Ctrl Pts',(4.49607581716378,1.99743773762816,17.8811038852354));
#26806=CARTESIAN_POINT('Ctrl Pts',(4.44446930119099,2.10977422106515,17.8881560886962));
#26807=CARTESIAN_POINT('Ctrl Pts',(4.33066635607802,2.33474499407003,17.9025769022562));
#26808=CARTESIAN_POINT('Ctrl Pts',(4.26817112610533,2.44712495697199,17.9099414526203));
#26809=CARTESIAN_POINT('Ctrl Pts',(4.16377178777008,2.61866587745628,17.9214172275421));
#26810=CARTESIAN_POINT('Ctrl Pts',(4.12484134023941,2.67956910444376,17.9255397127467));
#26811=CARTESIAN_POINT('Ctrl Pts',(4.06368723121824,2.77074652813486,17.9317779096321));
#26812=CARTESIAN_POINT('Ctrl Pts',(4.04243603938053,2.80166042879257,17.9339046950502));
#26813=CARTESIAN_POINT('Ctrl Pts',(3.99055209179637,2.87531596733622,17.9390000711915));
#26814=CARTESIAN_POINT('Ctrl Pts',(3.95958351300881,2.91781534820298,17.9419641157484));
#26815=CARTESIAN_POINT('Ctrl Pts',(3.85164963431727,3.06105348419405,17.9520539573294));
#26816=CARTESIAN_POINT('Ctrl Pts',(3.77147373167813,3.15931000356964,17.9591486651954));
#26817=CARTESIAN_POINT('Ctrl Pts',(3.67885148202854,3.26426244049555,17.966990730186));
#26818=CARTESIAN_POINT('Ctrl Pts',(3.67007218314261,3.27413006424849,17.9677307086419));
#26819=CARTESIAN_POINT('Ctrl Pts',(3.59480914259729,3.3580399981993,17.974046507965));
#26820=CARTESIAN_POINT('Ctrl Pts',(3.52613253760364,3.43008374717459,17.9796255430893));
#26821=CARTESIAN_POINT('Ctrl Pts',(3.42767627175922,3.52728326266153,17.9874058734882));
#26822=CARTESIAN_POINT('Ctrl Pts',(3.39971208030225,3.55424388418456,17.9895924650558));
#26823=CARTESIAN_POINT('Ctrl Pts',(3.31968490090331,3.62959041573985,17.9957878358959));
#26824=CARTESIAN_POINT('Ctrl Pts',(3.26688866224574,3.67718271812721,17.9998024868162));
#26825=CARTESIAN_POINT('Ctrl Pts',(3.15658337492318,3.77236437169542,18.0080539049934));
#26826=CARTESIAN_POINT('Ctrl Pts',(3.09898499484218,3.81982242759822,18.0122906958888));
#26827=CARTESIAN_POINT('Ctrl Pts',(2.91522586072174,3.96433753227178,18.0255969663952));
#26828=CARTESIAN_POINT('Ctrl Pts',(2.78542134979614,4.05659225731117,18.0346990137211));
#26829=CARTESIAN_POINT('Ctrl Pts',(2.53883343977273,4.21442310591339,18.0514591181867));
#26830=CARTESIAN_POINT('Ctrl Pts',(2.42340241549888,4.28184057684926,18.0591068381778));
#26831=CARTESIAN_POINT('Ctrl Pts',(2.26994530141025,4.36327165692594,18.0689899881626));
#26832=CARTESIAN_POINT('Ctrl Pts',(2.23429288528658,4.38163515034634,18.0712667101102));
#26833=CARTESIAN_POINT('Ctrl Pts',(2.15793752984839,4.41978921011624,18.0760996048673));
#26834=CARTESIAN_POINT('Ctrl Pts',(2.1171779461716,4.43945814876808,18.0786542264437));
#26835=CARTESIAN_POINT('Ctrl Pts',(1.82178945993727,4.57700732524579,18.0970107340914));
#26836=CARTESIAN_POINT('Ctrl Pts',(1.55775593073986,4.67346891892216,18.1126164539261));
#26837=CARTESIAN_POINT('Ctrl Pts',(1.21518105367392,4.7663451239606,18.132605222575));
#26838=CARTESIAN_POINT('Ctrl Pts',(1.1429911810417,4.78416991990166,18.1368012423489));
#26839=CARTESIAN_POINT('Ctrl Pts',(1.00088054385737,4.81585903080965,18.1450411897316));
#26840=CARTESIAN_POINT('Ctrl Pts',(0.931007274864338,4.82985355512137,18.1490831887826));
#26841=CARTESIAN_POINT('Ctrl Pts',(0.675138795852732,4.87534114974747,18.1638618958698));
#26842=CARTESIAN_POINT('Ctrl Pts',(0.487678907423868,4.89764547904067,18.1746524893051));
#26843=CARTESIAN_POINT('Ctrl Pts',(0.217569672574943,4.91411929470162,18.1901427464503));
#26844=CARTESIAN_POINT('Ctrl Pts',(0.135621870931243,4.91706333516054,18.1948335576079));
#26845=CARTESIAN_POINT('Ctrl Pts',(0.0261654859623787,4.91825713912549,
18.2010800027011));
#26846=CARTESIAN_POINT('Ctrl Pts',(-0.00130966417450025,4.91832656650228,
18.2026463293252));
#26847=CARTESIAN_POINT('Ctrl Pts',(-0.0721610569434313,4.91791190180704,
18.2066805765205));
#26848=CARTESIAN_POINT('Ctrl Pts',(-0.115533158525906,4.91708418068861,
18.2091454304341));
#26849=CARTESIAN_POINT('Ctrl Pts',(-0.200277612567998,4.91434499723206,
18.2139497184883));
#26850=CARTESIAN_POINT('Ctrl Pts',(-0.241648012259479,4.91248451985136,
18.2162894408996));
#26851=CARTESIAN_POINT('Ctrl Pts',(-0.428192851919074,4.90173314014378,
18.2268254952407));
#26852=CARTESIAN_POINT('Ctrl Pts',(-0.572954456015661,4.88692756742573,
18.234965135289));
#26853=CARTESIAN_POINT('Ctrl Pts',(-0.8251215528175,4.84977680641163,18.2492443373602));
#26854=CARTESIAN_POINT('Ctrl Pts',(-0.932831791129876,4.83021586158297,
18.2553757115236));
#26855=CARTESIAN_POINT('Ctrl Pts',(-1.07974663329832,4.79843732273243,18.2638240311053));
#26856=CARTESIAN_POINT('Ctrl Pts',(-1.11958474696796,4.78929885288586,18.2661235377934));
#26857=CARTESIAN_POINT('Ctrl Pts',(-1.23011524343585,4.76248976315965,18.272530900512));
#26858=CARTESIAN_POINT('Ctrl Pts',(-1.30053531215792,4.7437432471703,18.2766445992081));
#26859=CARTESIAN_POINT('Ctrl Pts',(-1.43163980041649,4.70570310229431,18.2843724967017));
#26860=CARTESIAN_POINT('Ctrl Pts',(-1.49241678125781,4.68678207765478,18.2879833130826));
#26861=CARTESIAN_POINT('Ctrl Pts',(-1.67404645381293,4.62634601525868,18.2988666118654));
#26862=CARTESIAN_POINT('Ctrl Pts',(-1.79366451009108,4.58129631463873,18.3061601185073));
#26863=CARTESIAN_POINT('Ctrl Pts',(-2.02526796087638,4.48360878631622,18.320540452009));
#26864=CARTESIAN_POINT('Ctrl Pts',(-2.13729393060609,4.4313014779321,18.3276210574031));
#26865=CARTESIAN_POINT('Ctrl Pts',(-2.29331750090348,4.35115643869589,18.3376438546885));
#26866=CARTESIAN_POINT('Ctrl Pts',(-2.33902781134628,4.32675588354676,18.3406004004621));
#26867=CARTESIAN_POINT('Ctrl Pts',(-2.42162253848157,4.28097465134513,18.3459764118893));
#26868=CARTESIAN_POINT('Ctrl Pts',(-2.45863090798584,4.25982790719744,18.3483978925117));
#26869=CARTESIAN_POINT('Ctrl Pts',(-2.53162015050201,4.21685345518621,18.3531964877128));
#26870=CARTESIAN_POINT('Ctrl Pts',(-2.56760511129622,4.19503965350301,18.355573534135));
#26871=CARTESIAN_POINT('Ctrl Pts',(-2.69572357476784,4.11510909626707,18.3640867998924));
#26872=CARTESIAN_POINT('Ctrl Pts',(-2.78620115859185,4.05439663183011,18.3701939158534));
#26873=CARTESIAN_POINT('Ctrl Pts',(-3.0050329793175,3.8967684326096,18.3853058414909));
#26874=CARTESIAN_POINT('Ctrl Pts',(-3.1307909095399,3.79646877866635,18.3942996292456));
#26875=CARTESIAN_POINT('Ctrl Pts',(-3.3115468559155,3.63720557891296,18.4078520372935));
#26876=CARTESIAN_POINT('Ctrl Pts',(-3.37037875960248,3.58275785010503,18.4123705090721));
#26877=CARTESIAN_POINT('Ctrl Pts',(-3.47725622901403,3.47888176194091,18.4207977421602));
#26878=CARTESIAN_POINT('Ctrl Pts',(-3.52564438744697,3.42983391802385,18.4247020309548));
#26879=CARTESIAN_POINT('Ctrl Pts',(-3.64996375012111,3.29840805285166,18.4349797245579));
#26880=CARTESIAN_POINT('Ctrl Pts',(-3.72413812139249,3.21442464593867,18.4413663654025));
#26881=CARTESIAN_POINT('Ctrl Pts',(-3.88680478978675,3.0170508958023,18.4559859940373));
#26882=CARTESIAN_POINT('Ctrl Pts',(-3.97332244634148,2.90216405837288,18.4642234223075));
#26883=CARTESIAN_POINT('Ctrl Pts',(-4.08582384968827,2.73829394405004,18.4755854740975));
#26884=CARTESIAN_POINT('Ctrl Pts',(-4.11620112735012,2.69241501361351,18.4787264154735));
#26885=CARTESIAN_POINT('Ctrl Pts',(-4.16965373116222,2.60866560610713,18.4843846522103));
#26886=CARTESIAN_POINT('Ctrl Pts',(-4.19299889058817,2.57097429925913,18.4869043138299));
#26887=CARTESIAN_POINT('Ctrl Pts',(-4.23678707074901,2.49809407446726,18.4917227343884));
#26888=CARTESIAN_POINT('Ctrl Pts',(-4.25730911779791,2.46295712550303,18.494022203581));
#26889=CARTESIAN_POINT('Ctrl Pts',(-4.33845233361514,2.31998224504474,18.503293824949));
#26890=CARTESIAN_POINT('Ctrl Pts',(-4.39543153582698,2.21012863082383,18.5102254462793));
#26891=CARTESIAN_POINT('Ctrl Pts',(-4.48710867158797,2.01577597990305,18.5222647591752));
#26892=CARTESIAN_POINT('Ctrl Pts',(-4.5237077260229,1.93224361286819,18.5273701829613));
#26893=CARTESIAN_POINT('Ctrl Pts',(-4.58812028931384,1.77335235877483,18.5369886671671));
#26894=CARTESIAN_POINT('Ctrl Pts',(-4.61645121734951,1.69823566531507,18.5414979919757));
#26895=CARTESIAN_POINT('Ctrl Pts',(-4.66718204829661,1.55306119512076,18.5501600731409));
#26896=CARTESIAN_POINT('Ctrl Pts',(-4.68987399224164,1.48312815289078,18.5543097715015));
#26897=CARTESIAN_POINT('Ctrl Pts',(-4.72916248407022,1.35211241555791,18.5620517758427));
#26898=CARTESIAN_POINT('Ctrl Pts',(-4.74616410155201,1.29116691226652,18.5656404041838));
#26899=CARTESIAN_POINT('Ctrl Pts',(-4.76267050742994,1.22725719054281,18.5693926742232));
#26900=CARTESIAN_POINT('Ctrl Pts',(-4.76335365943198,1.2246029924092,18.5695484879206));
#26901=CARTESIAN_POINT('Ctrl Pts',(-4.76403458707798,1.22194824588636,18.5697043142649));
#26902=CARTESIAN_POINT('Origin',(0.,0.,-3.23514056400928));
#26903=CARTESIAN_POINT('',(-4.76403458704968,1.22194824599669,20.6652050067296));
#26904=CARTESIAN_POINT('',(-4.76403459893337,1.2219481996655,20.3200311864783));
#26905=CARTESIAN_POINT('',(-4.76403458704967,1.22194824599672,-3.23514056400928));
#26906=CARTESIAN_POINT('',(-4.91824999838119,-0.000126187989179228,18.9851405640093));
#26907=CARTESIAN_POINT('Ctrl Pts',(-4.91824999838119,-0.000126187989179228,
18.9851405640093));
#26908=CARTESIAN_POINT('Ctrl Pts',(-4.91824608488009,-0.152657161176494,
18.9937788711624));
#26909=CARTESIAN_POINT('Ctrl Pts',(-4.91114211048955,-0.305153403297447,
19.0024171783155));
#26910=CARTESIAN_POINT('Ctrl Pts',(-4.89697369991277,-0.456981011490179,
19.0110554854686));
#26911=CARTESIAN_POINT('Ctrl Pts',(-4.8948411352829,-0.479833411575278,
19.012355684118));
#26912=CARTESIAN_POINT('Ctrl Pts',(-4.89254862248211,-0.50267067097549,
19.0136558827675));
#26913=CARTESIAN_POINT('Ctrl Pts',(-4.89009638484907,-0.525490636820512,
19.0149560814169));
#26914=CARTESIAN_POINT('Ctrl Pts',(-4.87471295583977,-0.668645329433346,
19.023112515097));
#26915=CARTESIAN_POINT('Ctrl Pts',(-4.85303617925358,-0.81115080021202,
19.0312689487771));
#26916=CARTESIAN_POINT('Ctrl Pts',(-4.82514522750803,-0.95244768672954,
19.0394253824572));
#26917=CARTESIAN_POINT('Ctrl Pts',(-4.79725995235747,-1.09371581534719,
19.0475801560731));
#26918=CARTESIAN_POINT('Ctrl Pts',(-4.76316308993429,-1.23377552232594,
19.055734929689));
#26919=CARTESIAN_POINT('Ctrl Pts',(-4.72298502473125,-1.37207708189603,
19.0638897033048));
#26920=CARTESIAN_POINT('Ctrl Pts',(-4.68280553468754,-1.51038354607481,
19.0720447661147));
#26921=CARTESIAN_POINT('Ctrl Pts',(-4.63654450007743,-1.6469314157073,19.0801998289245));
#26922=CARTESIAN_POINT('Ctrl Pts',(-4.58438247970837,-1.78118509488568,
19.0883548917343));
#26923=CARTESIAN_POINT('Ctrl Pts',(-4.53222351863791,-1.91543090009581,
19.0965094762503));
#26924=CARTESIAN_POINT('Ctrl Pts',(-4.47416438629209,-2.04738247246663,
19.1046640607664));
#26925=CARTESIAN_POINT('Ctrl Pts',(-4.41043417222228,-2.17652325395205,
19.1128186452824));
#26926=CARTESIAN_POINT('Ctrl Pts',(-4.34668828913151,-2.30569578661922,
19.1209752347242));
#26927=CARTESIAN_POINT('Ctrl Pts',(-4.27726868611204,-2.43205584716965,
19.1291318241661));
#26928=CARTESIAN_POINT('Ctrl Pts',(-4.20245116332172,-2.55511003332458,
19.137288413608));
#26929=CARTESIAN_POINT('Ctrl Pts',(-4.15165287706674,-2.63865920122057,
19.142826431306));
#26930=CARTESIAN_POINT('Ctrl Pts',(-4.09836717013825,-2.72068488610154,
19.148364449004));
#26931=CARTESIAN_POINT('Ctrl Pts',(-4.04269200790494,-2.80103987685316,
19.153902466702));
#26932=CARTESIAN_POINT('Ctrl Pts',(-3.96069321462759,-2.91938730524201,
19.1620589003821));
#26933=CARTESIAN_POINT('Ctrl Pts',(-3.87347869980731,-3.03415367771113,
19.1702153340622));
#26934=CARTESIAN_POINT('Ctrl Pts',(-3.78138560526144,-3.14488568422153,
19.1783717677423));
#26935=CARTESIAN_POINT('Ctrl Pts',(-3.68931125425647,-3.25559515364702,
19.1865265413582));
#26936=CARTESIAN_POINT('Ctrl Pts',(-3.59236051820411,-3.36227163805237,
19.1946813149741));
#26937=CARTESIAN_POINT('Ctrl Pts',(-3.49091089889729,-3.46449479123004,
19.2028360885901));
#26938=CARTESIAN_POINT('Ctrl Pts',(-3.38945768186793,-3.5667215695622,19.2109911513999));
#26939=CARTESIAN_POINT('Ctrl Pts',(-3.28350549537999,-3.66449446050219,
19.2191462142097));
#26940=CARTESIAN_POINT('Ctrl Pts',(-3.17346914021325,-3.75742953075825,
19.2273012770195));
#26941=CARTESIAN_POINT('Ctrl Pts',(-3.06343923867039,-3.85035915037949,
19.2354558615355));
#26942=CARTESIAN_POINT('Ctrl Pts',(-2.94932590394392,-3.93845130177503,
19.2436104460516));
#26943=CARTESIAN_POINT('Ctrl Pts',(-2.83157744438321,-4.02136198805333,
19.2517650305676));
#26944=CARTESIAN_POINT('Ctrl Pts',(-2.71380003461238,-4.10429305915703,
19.2599216200095));
#26945=CARTESIAN_POINT('Ctrl Pts',(-2.59238598769989,-4.18203992660568,
19.2680782094514));
#26946=CARTESIAN_POINT('Ctrl Pts',(-2.46781355110926,-4.25430127511693,
19.2762347988933));
#26947=CARTESIAN_POINT('Ctrl Pts',(-2.38323354822555,-4.30336401509966,
19.2817728165912));
#26948=CARTESIAN_POINT('Ctrl Pts',(-2.29719817246742,-4.34989888010521,
19.2873108342892));
#26949=CARTESIAN_POINT('Ctrl Pts',(-2.20986388044963,-4.39382347078079,
19.2928488519872));
#26950=CARTESIAN_POINT('Ctrl Pts',(-2.08123728521461,-4.4585159348193,19.3010052856673));
#26951=CARTESIAN_POINT('Ctrl Pts',(-1.94974394926948,-4.51756840679982,
19.3091617193473));
#26952=CARTESIAN_POINT('Ctrl Pts',(-1.81589680404786,-4.57074412536392,
19.3173181530274));
#26953=CARTESIAN_POINT('Ctrl Pts',(-1.68207690049345,-4.62390902117027,
19.3254729266433));
#26954=CARTESIAN_POINT('Ctrl Pts',(-1.54590445416985,-4.67119942620531,
19.3336277002592));
#26955=CARTESIAN_POINT('Ctrl Pts',(-1.40791206646716,-4.71242683503905,
19.3417824738751));
#26956=CARTESIAN_POINT('Ctrl Pts',(-1.26991478512027,-4.75365570592641,
19.3499375366849));
#26957=CARTESIAN_POINT('Ctrl Pts',(-1.13009775278517,-4.78882105098862,
19.3580925994948));
#26958=CARTESIAN_POINT('Ctrl Pts',(-0.989008902720726,-4.8177841849588,
19.3662476623046));
#26959=CARTESIAN_POINT('Ctrl Pts',(-0.847928327506779,-4.84674562024334,
19.3744022468206));
#26960=CARTESIAN_POINT('Ctrl Pts',(-0.705576411790162,-4.86950550582432,
19.3825568313366));
#26961=CARTESIAN_POINT('Ctrl Pts',(-0.56251140560929,-4.88597625670239,
19.3907114158526));
#26962=CARTESIAN_POINT('Ctrl Pts',(-0.419411224768708,-4.90245105715954,
19.3988680052945));
#26963=CARTESIAN_POINT('Ctrl Pts',(-0.275597935685257,-4.91263359460003,
19.4070245947364));
#26964=CARTESIAN_POINT('Ctrl Pts',(-0.131635658229963,-4.91648808764776,
19.4151811841783));
#26965=CARTESIAN_POINT('Ctrl Pts',(-0.0338906820886804,-4.91910514357135,
19.4207192018763));
#26966=CARTESIAN_POINT('Ctrl Pts',(0.0639228656633244,-4.9188061130699,
19.4262572195743));
#26967=CARTESIAN_POINT('Ctrl Pts',(0.161628174145175,-4.91559349375256,
19.4317952372723));
#26968=CARTESIAN_POINT('Ctrl Pts',(0.30552927960976,-4.91086192411335,19.4399516709524));
#26969=CARTESIAN_POINT('Ctrl Pts',(0.449249364441852,-4.89980619885904,
19.4481081046325));
#26970=CARTESIAN_POINT('Ctrl Pts',(0.592224736858196,-4.88246381692207,
19.4562645383126));
#26971=CARTESIAN_POINT('Ctrl Pts',(0.735171009755496,-4.86512496464875,
19.4644193119285));
#26972=CARTESIAN_POINT('Ctrl Pts',(0.877372540617288,-4.84150204851488,
19.4725740855444));
#26973=CARTESIAN_POINT('Ctrl Pts',(1.0182714523604,-4.81168435288599,19.4807288591603));
#26974=CARTESIAN_POINT('Ctrl Pts',(1.15917536082229,-4.78186559982778,19.4888839219701));
#26975=CARTESIAN_POINT('Ctrl Pts',(1.2987762295882,-4.74585169328947,19.4970389847799));
#26976=CARTESIAN_POINT('Ctrl Pts',(1.43652655403386,-4.70378300116572,19.5051940475897));
#26977=CARTESIAN_POINT('Ctrl Pts',(1.5742687994334,-4.66171677636759,19.5133486321057));
#26978=CARTESIAN_POINT('Ctrl Pts',(1.71016039788062,-4.61359657508639,19.5215032166218));
#26979=CARTESIAN_POINT('Ctrl Pts',(1.84366923352164,-4.5596125734393,19.5296578011378));
#26980=CARTESIAN_POINT('Ctrl Pts',(1.97721089429562,-4.50561529902248,19.5378143905797));
#26981=CARTESIAN_POINT('Ctrl Pts',(2.10836831117959,-4.44575146869014,19.5459709800216));
#26982=CARTESIAN_POINT('Ctrl Pts',(2.23662899856581,-4.38025955683844,19.5541275694634));
#26983=CARTESIAN_POINT('Ctrl Pts',(2.32371318513178,-4.33579300994492,19.5596655871614));
#26984=CARTESIAN_POINT('Ctrl Pts',(2.40946242741656,-4.28873297392088,19.5652036048594));
#26985=CARTESIAN_POINT('Ctrl Pts',(2.49372265869397,-4.23916623453436,19.5707416225574));
#26986=CARTESIAN_POINT('Ctrl Pts',(2.61782175439267,-4.16616397188512,19.5788980562375));
#26987=CARTESIAN_POINT('Ctrl Pts',(2.73873619268232,-4.08769493048598,19.5870544899176));
#26988=CARTESIAN_POINT('Ctrl Pts',(2.85598892375259,-4.00406172903247,19.5952109235977));
#26989=CARTESIAN_POINT('Ctrl Pts',(2.97321779058655,-3.92044554929322,19.6033656972135));
#26990=CARTESIAN_POINT('Ctrl Pts',(3.08678616468886,-3.83166750048702,19.6115204708294));
#26991=CARTESIAN_POINT('Ctrl Pts',(3.19624687824738,-3.73807289332269,19.6196752444453));
#26992=CARTESIAN_POINT('Ctrl Pts',(3.30571147362727,-3.64447496699906,19.6278303072551));
#26993=CARTESIAN_POINT('Ctrl Pts',(3.41106786021718,-3.54606035513149,19.635985370065));
#26994=CARTESIAN_POINT('Ctrl Pts',(3.51190241865963,-3.44321426349169,19.6441404328748));
#26995=CARTESIAN_POINT('Ctrl Pts',(3.61273106316279,-3.34037420376746,19.6522950173908));
#26996=CARTESIAN_POINT('Ctrl Pts',(3.70903817649805,-3.23310342386507,19.6604496019068));
#26997=CARTESIAN_POINT('Ctrl Pts',(3.80044748254855,-3.12182350476295,19.6686041864228));
#26998=CARTESIAN_POINT('Ctrl Pts',(3.89187926293657,-3.01051622583752,19.6767607758647));
#26999=CARTESIAN_POINT('Ctrl Pts',(3.9784106171142,-2.89519809660406,19.6849173653066));
#27000=CARTESIAN_POINT('Ctrl Pts',(4.05970561433167,-2.77632371806025,19.6930739547485));
#27001=CARTESIAN_POINT('Ctrl Pts',(4.11490186229257,-2.69561248245065,19.6986119724465));
#27002=CARTESIAN_POINT('Ctrl Pts',(4.16768504855189,-2.61326252925448,19.7041499901445));
#27003=CARTESIAN_POINT('Ctrl Pts',(4.21796140497238,-2.52942377799043,19.7096880078425));
#27004=CARTESIAN_POINT('Ctrl Pts',(4.29200879686997,-2.40594544119271,19.7178444415226));
#27005=CARTESIAN_POINT('Ctrl Pts',(4.36064416866912,-2.27919025359464,19.7260008752027));
#27006=CARTESIAN_POINT('Ctrl Pts',(4.42359339549742,-2.14965218903235,19.7341573088828));
#27007=CARTESIAN_POINT('Ctrl Pts',(4.48652981038342,-2.0201404891181,19.7423120824987));
#27008=CARTESIAN_POINT('Ctrl Pts',(4.54378224285713,-1.88784734295421,19.7504668561146));
#27009=CARTESIAN_POINT('Ctrl Pts',(4.59512323347547,-1.75328991660646,19.7586216297305));
#27010=CARTESIAN_POINT('Ctrl Pts',(4.64646604480694,-1.61872771842889,19.7667766925403));
#27011=CARTESIAN_POINT('Ctrl Pts',(4.69189687200536,-1.481901390683,19.7749317553501));
#27012=CARTESIAN_POINT('Ctrl Pts',(4.73123680249645,-1.3433470814362,19.78308681816));
#27013=CARTESIAN_POINT('Ctrl Pts',(4.77057442570357,-1.20480089838923,19.791241402676));
#27014=CARTESIAN_POINT('Ctrl Pts',(4.80382177640447,-1.06452725877274,19.799395987192));
#27015=CARTESIAN_POINT('Ctrl Pts',(4.83085013715846,-0.923076386230346,
19.807550571708));
#27016=CARTESIAN_POINT('Ctrl Pts',(4.85788514323695,-0.781590735887049,
19.8157071611499));
#27017=CARTESIAN_POINT('Ctrl Pts',(4.8786980409756,-0.638927603040939,19.8238637505918));
#27018=CARTESIAN_POINT('Ctrl Pts',(4.89321133906314,-0.495646904321914,
19.8320203400337));
#27019=CARTESIAN_POINT('Ctrl Pts',(4.90306532303982,-0.398364694528591,
19.8375583577317));
#27020=CARTESIAN_POINT('Ctrl Pts',(4.91001632217392,-0.300797983227913,
19.8430963754297));
#27021=CARTESIAN_POINT('Ctrl Pts',(4.91405372330819,-0.203123280154853,
19.8486343931277));
#27022=CARTESIAN_POINT('Ctrl Pts',(4.92000003774551,-0.0592672505635319,
19.8567908268078));
#27023=CARTESIAN_POINT('Ctrl Pts',(4.91962617282005,0.0848769552514978,
19.8649472604878));
#27024=CARTESIAN_POINT('Ctrl Pts',(4.91292774772659,0.228744416583424,19.8731036941679));
#27025=CARTESIAN_POINT('Ctrl Pts',(4.90623068595148,0.372582596831178,19.8812584677838));
#27026=CARTESIAN_POINT('Ctrl Pts',(4.89321164750471,0.516143810896978,19.8894132413997));
#27027=CARTESIAN_POINT('Ctrl Pts',(4.8739183255403,0.658865098834713,19.8975680150156));
#27028=CARTESIAN_POINT('Ctrl Pts',(4.85462431937398,0.801591448118389,19.9057230778255));
#27029=CARTESIAN_POINT('Ctrl Pts',(4.8290556255634,0.943477479570301,19.9138781406353));
#27030=CARTESIAN_POINT('Ctrl Pts',(4.79731164903516,1.0839667912494,19.9220332034451));
#27031=CARTESIAN_POINT('Ctrl Pts',(4.76556953428877,1.22444786324089,19.9301877879611));
#27032=CARTESIAN_POINT('Ctrl Pts',(4.72765293609565,1.36353205314515,19.9383423724771));
#27033=CARTESIAN_POINT('Ctrl Pts',(4.68371207112699,1.50067461405839,19.9464969569931));
#27034=CARTESIAN_POINT('Ctrl Pts',(4.63976040264311,1.63785089351007,19.954653546435));
#27035=CARTESIAN_POINT('Ctrl Pts',(4.5897816096453,1.77308427118075,19.9628101358769));
#27036=CARTESIAN_POINT('Ctrl Pts',(4.53397552910476,1.90584599692084,19.9709667253188));
#27037=CARTESIAN_POINT('Ctrl Pts',(4.4960852976679,1.99598621937554,19.9765047430168));
#27038=CARTESIAN_POINT('Ctrl Pts',(4.45550977342207,2.08498737877925,19.9820427607148));
#27039=CARTESIAN_POINT('Ctrl Pts',(4.41232408519324,2.17268940019591,19.9875807784128));
#27040=CARTESIAN_POINT('Ctrl Pts',(4.34871988217752,2.30185759002574,19.9957372120929));
#27041=CARTESIAN_POINT('Ctrl Pts',(4.27942791172819,2.42825503729542,20.003893645773));
#27042=CARTESIAN_POINT('Ctrl Pts',(4.20471460494752,2.55138357630542,20.0120500794531));
#27043=CARTESIAN_POINT('Ctrl Pts',(4.13001650443106,2.67448705518656,20.020204853069));
#27044=CARTESIAN_POINT('Ctrl Pts',(4.04989944227893,2.79432266716495,20.0283596266849));
#27045=CARTESIAN_POINT('Ctrl Pts',(3.96467463882862,2.91041888234824,20.0365144003008));
#27046=CARTESIAN_POINT('Ctrl Pts',(3.8794468130386,3.02651921466863,20.0446694631106));
#27047=CARTESIAN_POINT('Ctrl Pts',(3.78911107848246,3.13887961288154,20.0528245259204));
#27048=CARTESIAN_POINT('Ctrl Pts',(3.69402092720471,3.24705904656408,20.0609795887303));
#27049=CARTESIAN_POINT('Ctrl Pts',(3.59893635295717,3.35523213553099,20.0691341732463));
#27050=CARTESIAN_POINT('Ctrl Pts',(3.49909814150301,3.45922449983493,20.0772887577623));
#27051=CARTESIAN_POINT('Ctrl Pts',(3.39489882765871,3.55862965373773,20.0854433422783));
#27052=CARTESIAN_POINT('Ctrl Pts',(3.29067389486332,3.65805924787609,20.0935999317202));
#27053=CARTESIAN_POINT('Ctrl Pts',(3.18208595918008,3.75289914670456,20.1017565211621));
#27054=CARTESIAN_POINT('Ctrl Pts',(3.06956347473226,3.84278065170127,20.109913110604));
#27055=CARTESIAN_POINT('Ctrl Pts',(2.99316493650366,3.90380681575401,20.115451128302));
#27056=CARTESIAN_POINT('Ctrl Pts',(2.91495334929489,3.96254800376763,20.1209891459999));
#27057=CARTESIAN_POINT('Ctrl Pts',(2.83507127093721,4.01889959456646,20.1265271636979));
#27058=CARTESIAN_POINT('Ctrl Pts',(2.71742035144111,4.10189463686951,20.134683597378));
#27059=CARTESIAN_POINT('Ctrl Pts',(2.59610049447723,4.17973539837199,20.1428400310581));
#27060=CARTESIAN_POINT('Ctrl Pts',(2.471583999316,4.25211189843648,20.1509964647382));
#27061=CARTESIAN_POINT('Ctrl Pts',(2.34709284677197,4.32447366784274,20.159151238354));
#27062=CARTESIAN_POINT('Ctrl Pts',(2.21940664308317,4.39137322638844,20.1673060119699));
#27063=CARTESIAN_POINT('Ctrl Pts',(2.08902427446046,4.45254541169598,20.1754607855858));
#27064=CARTESIAN_POINT('Ctrl Pts',(1.95863728206862,4.51371976636173,20.1836158483956));
#27065=CARTESIAN_POINT('Ctrl Pts',(1.82555423475462,4.56916619584048,20.1917709112055));
#27066=CARTESIAN_POINT('Ctrl Pts',(1.69029654645842,4.61866654431025,20.1999259740153));
#27067=CARTESIAN_POINT('Ctrl Pts',(1.55504679101553,4.66816398958828,20.2080805585313));
#27068=CARTESIAN_POINT('Ctrl Pts',(1.41762296433932,4.71171593743785,20.2162351430473));
#27069=CARTESIAN_POINT('Ctrl Pts',(1.27856423732369,4.74915324595205,20.2243897275633));
#27070=CARTESIAN_POINT('Ctrl Pts',(1.13947132065162,4.78659975898541,20.2325463170052));
#27071=CARTESIAN_POINT('Ctrl Pts',(0.99874302363769,4.81792854136317,20.2407029064471));
#27072=CARTESIAN_POINT('Ctrl Pts',(0.856931980002171,4.84302081805866,20.248859495889));
#27073=CARTESIAN_POINT('Ctrl Pts',(0.760647610778716,4.8600575309413,20.254397513587));
#27074=CARTESIAN_POINT('Ctrl Pts',(0.663864374974099,4.87422032763894,20.259935531285));
#27075=CARTESIAN_POINT('Ctrl Pts',(0.566757510333805,4.88548554260272,20.265473548983));
#27076=CARTESIAN_POINT('Ctrl Pts',(0.423737797413014,4.90207703503818,20.2736299826631));
#27077=CARTESIAN_POINT('Ctrl Pts',(0.279962296446916,4.91238708678347,20.2817864163432));
#27078=CARTESIAN_POINT('Ctrl Pts',(0.135994049873843,4.91636946139109,20.2899428500233));
#27079=CARTESIAN_POINT('Ctrl Pts',(-0.00794489510218649,4.9203510254732,
20.2980976236392));
#27080=CARTESIAN_POINT('Ctrl Pts',(-0.152076173126647,4.91800747237844,
20.3062523972551));
#27081=CARTESIAN_POINT('Ctrl Pts',(-0.295834837797911,4.90934464172613,
20.314407170871));
#27082=CARTESIAN_POINT('Ctrl Pts',(-0.439598600603923,4.90068150386259,
20.3225622336808));
#27083=CARTESIAN_POINT('Ctrl Pts',(-0.582989389381103,4.88569865639613,
20.3307172964906));
#27084=CARTESIAN_POINT('Ctrl Pts',(-0.725444965208518,4.86445399453563,
20.3388723593005));
#27085=CARTESIAN_POINT('Ctrl Pts',(-0.867892186027029,4.84321057867296,
20.3470269438165));
#27086=CARTESIAN_POINT('Ctrl Pts',(-1.00940397279177,4.81570613345958,20.3551815283325));
#27087=CARTESIAN_POINT('Ctrl Pts',(-1.14942594378057,4.78205008989493,20.3633361128485));
#27088=CARTESIAN_POINT('Ctrl Pts',(-1.2894823412537,4.74838577149136,20.3714927022904));
#27089=CARTESIAN_POINT('Ctrl Pts',(-1.4280478654554,4.70856691052756,20.3796492917323));
#27090=CARTESIAN_POINT('Ctrl Pts',(-1.56458040993998,4.66275360740111,20.3878058811742));
#27091=CARTESIAN_POINT('Ctrl Pts',(-1.65728087661094,4.63164809628951,20.3933438988722));
#27092=CARTESIAN_POINT('Ctrl Pts',(-1.74904442656629,4.59778025841011,20.3988819165702));
#27093=CARTESIAN_POINT('Ctrl Pts',(-1.83970585710855,4.56121315242124,20.4044199342682));
#27094=CARTESIAN_POINT('Ctrl Pts',(-1.97323268672267,4.50735684658475,20.4125763679483));
#27095=CARTESIAN_POINT('Ctrl Pts',(-2.10441792833817,4.44762306864213,20.4207328016284));
#27096=CARTESIAN_POINT('Ctrl Pts',(-2.23274504039072,4.38224059667091,20.4288892353084));
#27097=CARTESIAN_POINT('Ctrl Pts',(-2.36104603425822,4.31687143187597,20.4370440089243));
#27098=CARTESIAN_POINT('Ctrl Pts',(-2.4864897610612,4.24585601839497,20.4451987825402));
#27099=CARTESIAN_POINT('Ctrl Pts',(-2.60858292234846,4.16946977441161,20.4533535561561));
#27100=CARTESIAN_POINT('Ctrl Pts',(-2.73068041344344,4.09308082153164,20.4615086189659));
#27101=CARTESIAN_POINT('Ctrl Pts',(-2.84942681559945,4.01132083132036,20.4696636817758));
#27102=CARTESIAN_POINT('Ctrl Pts',(-2.96435611309558,3.92450963780863,20.4778187445856));
#27103=CARTESIAN_POINT('Ctrl Pts',(-3.07927866999684,3.83770353576704,20.4859733291016));
#27104=CARTESIAN_POINT('Ctrl Pts',(-3.19038430367418,3.74584702557344,20.4941279136176));
#27105=CARTESIAN_POINT('Ctrl Pts',(-3.29723855453186,3.64930143685181,20.5022824981336));
#27106=CARTESIAN_POINT('Ctrl Pts',(-3.40411907709664,3.55273211096101,20.5104390875755));
#27107=CARTESIAN_POINT('Ctrl Pts',(-3.50674587961742,3.45147162710822,20.5185956770174));
#27108=CARTESIAN_POINT('Ctrl Pts',(-3.60471952372578,3.34591993594739,20.5267522664593));
#27109=CARTESIAN_POINT('Ctrl Pts',(-3.67123994612487,3.27425430439049,20.5322902841573));
#27110=CARTESIAN_POINT('Ctrl Pts',(-3.7356160460338,3.20061126464044,20.5378283018553));
#27111=CARTESIAN_POINT('Ctrl Pts',(-3.7977329246787,3.12512522874066,20.5433663195533));
#27112=CARTESIAN_POINT('Ctrl Pts',(-3.88921846670772,3.01394963427154,20.5515226944698));
#27113=CARTESIAN_POINT('Ctrl Pts',(-3.97583588714361,2.89873325391861,20.5596790693863));
#27114=CARTESIAN_POINT('Ctrl Pts',(-4.05724106183668,2.77992410483566,20.5678354443027));
#27115=CARTESIAN_POINT('Ctrl Pts',(-4.13863917622222,2.66112526012382,20.5759911118131));
#27116=CARTESIAN_POINT('Ctrl Pts',(-4.21482575387104,2.53873454170662,20.5841467793236));
#27117=CARTESIAN_POINT('Ctrl Pts',(-4.28549929090363,2.41322997042647,20.592302446834));
#27118=CARTESIAN_POINT('Ctrl Pts',(-4.35616260189941,2.28774355890481,20.6004569342682));
#27119=CARTESIAN_POINT('Ctrl Pts',(-4.42131430129921,2.15914448593707,20.6086114217024));
#27120=CARTESIAN_POINT('Ctrl Pts',(-4.48069824727407,2.02793645841655,20.6167659091367));
#27121=CARTESIAN_POINT('Ctrl Pts',(-4.54009265283834,1.89670532057433,20.6249218328613));
#27122=CARTESIAN_POINT('Ctrl Pts',(-4.59371713419027,1.7628646137145,20.6330777565859));
#27123=CARTESIAN_POINT('Ctrl Pts',(-4.64136295801333,1.62693975133738,20.6412336803105));
#27124=CARTESIAN_POINT('Ctrl Pts',(-4.68804206038235,1.49377276929592,20.6492241224502));
#27125=CARTESIAN_POINT('Ctrl Pts',(-4.72898271456912,1.35860569723107,20.6572145645899));
#27126=CARTESIAN_POINT('Ctrl Pts',(-4.76403458704968,1.22194824599669,20.6652050067296));
#27127=CARTESIAN_POINT('Ctrl Pts',(-4.91824999834649,-0.000127533484696671,
18.9851165466282));
#27128=CARTESIAN_POINT('Ctrl Pts',(-4.91825426647613,0.164470247714909,
18.9758954921501));
#27129=CARTESIAN_POINT('Ctrl Pts',(-4.90999572994125,0.32896299265212,18.9666777222489));
#27130=CARTESIAN_POINT('Ctrl Pts',(-4.88721015483374,0.555255832527698,
18.9538611209249));
#27131=CARTESIAN_POINT('Ctrl Pts',(-4.87971668875726,0.617654490600012,
18.9503131614603));
#27132=CARTESIAN_POINT('Ctrl Pts',(-4.86152175443621,0.748010587004119,
18.942864965379));
#27133=CARTESIAN_POINT('Ctrl Pts',(-4.85058607000977,0.815921713384803,
18.9389639209489));
#27134=CARTESIAN_POINT('Ctrl Pts',(-4.8174742604682,0.997232330121885,18.9284851571659));
#27135=CARTESIAN_POINT('Ctrl Pts',(-4.79272528367052,1.11009124993719,18.9218945455044));
#27136=CARTESIAN_POINT('Ctrl Pts',(-4.76403456361785,1.22194833735085,18.9152905258446));
#27137=CARTESIAN_POINT('Ctrl Pts',(-4.76403458707798,1.22194824588636,18.5697043142649));
#27138=CARTESIAN_POINT('Ctrl Pts',(-4.79432870303326,1.10383995719103,18.5766369470779));
#27139=CARTESIAN_POINT('Ctrl Pts',(-4.82022010554556,0.984646307948852,
18.5835959345697));
#27140=CARTESIAN_POINT('Ctrl Pts',(-4.86407035578851,0.739094272467518,
18.5978640165473));
#27141=CARTESIAN_POINT('Ctrl Pts',(-4.88159586539937,0.612750051166033,
18.6051692734577));
#27142=CARTESIAN_POINT('Ctrl Pts',(-4.9013045904696,0.41422223185854,18.6165700499129));
#27143=CARTESIAN_POINT('Ctrl Pts',(-4.90684315277572,0.342428397819731,
18.6206767293436));
#27144=CARTESIAN_POINT('Ctrl Pts',(-4.9128661836028,0.233098512577472,18.6268982956844));
#27145=CARTESIAN_POINT('Ctrl Pts',(-4.91450054511261,0.195636143911848,
18.6290241526574));
#27146=CARTESIAN_POINT('Ctrl Pts',(-4.91740116217215,0.105482254621061,
18.6341254373705));
#27147=CARTESIAN_POINT('Ctrl Pts',(-4.91824916554378,0.0527819592354969,
18.6370962725309));
#27148=CARTESIAN_POINT('Ctrl Pts',(-4.91825239113532,-0.15109410892035,
18.648565606603));
#27149=CARTESIAN_POINT('Ctrl Pts',(-4.91128494426198,-0.302186809004692,
18.6570175820926));
#27150=CARTESIAN_POINT('Ctrl Pts',(-4.89557526009948,-0.472129117360551,
18.6665822613926));
#27151=CARTESIAN_POINT('Ctrl Pts',(-4.89366559728594,-0.491528281524528,
18.66767490211));
#27152=CARTESIAN_POINT('Ctrl Pts',(-4.87921125968558,-0.629917930384619,
18.6754766685217));
#27153=CARTESIAN_POINT('Ctrl Pts',(-4.86244355274141,-0.748425873823323,
18.6821961863013));
#27154=CARTESIAN_POINT('Ctrl Pts',(-4.82919812443932,-0.934240783413535,
18.6928442494526));
#27155=CARTESIAN_POINT('Ctrl Pts',(-4.81559225279241,-1.00201371157166,
18.6967515731883));
#27156=CARTESIAN_POINT('Ctrl Pts',(-4.78333204332524,-1.14682017470983,
18.705159734493));
#27157=CARTESIAN_POINT('Ctrl Pts',(-4.764234892022,-1.22373511563692,18.7096625148899));
#27158=CARTESIAN_POINT('Ctrl Pts',(-4.73063504211087,-1.3463157619462,18.7169034802174));
#27159=CARTESIAN_POINT('Ctrl Pts',(-4.71730889568343,-1.39228976071185,
18.7196339945461));
#27160=CARTESIAN_POINT('Ctrl Pts',(-4.65910698213442,-1.58264450302222,
18.731002471672));
#27161=CARTESIAN_POINT('Ctrl Pts',(-4.60825682523033,-1.72511165143439,
18.7396651084371));
#27162=CARTESIAN_POINT('Ctrl Pts',(-4.52035783396687,-1.93959951023446,
18.7529219600983));
#27163=CARTESIAN_POINT('Ctrl Pts',(-4.48796049259087,-2.01342793443834,
18.7575250466827));
#27164=CARTESIAN_POINT('Ctrl Pts',(-4.43858711514532,-2.11882213030958,
18.7641450405954));
#27165=CARTESIAN_POINT('Ctrl Pts',(-4.42305816029026,-2.15105075479417,
18.7661760726778));
#27166=CARTESIAN_POINT('Ctrl Pts',(-4.38792848024276,-2.22196929406308,
18.7706586022368));
#27167=CARTESIAN_POINT('Ctrl Pts',(-4.36816477377153,-2.26057524984079,
18.7731077697738));
#27168=CARTESIAN_POINT('Ctrl Pts',(-4.33505476251579,-2.32319556431184,
18.7770999383562));
#27169=CARTESIAN_POINT('Ctrl Pts',(-4.3220134108504,-2.34736820962317,18.7786458169949));
#27170=CARTESIAN_POINT('Ctrl Pts',(-4.26925953279816,-2.44321936162507,
18.7847977244603));
#27171=CARTESIAN_POINT('Ctrl Pts',(-4.22796066111486,-2.51401006552931,
18.7893909513149));
#27172=CARTESIAN_POINT('Ctrl Pts',(-4.08579176459759,-2.74428293837395,
18.8045541987433));
#27173=CARTESIAN_POINT('Ctrl Pts',(-3.97751579749123,-2.89899123883298,
18.815109304399));
#27174=CARTESIAN_POINT('Ctrl Pts',(-3.81647353870796,-3.10302923770986,
18.8297596072273));
#27175=CARTESIAN_POINT('Ctrl Pts',(-3.77111590287003,-3.15799705740185,
18.8337844537811));
#27176=CARTESIAN_POINT('Ctrl Pts',(-3.67602973029557,-3.26825874900703,
18.8420300401426));
#27177=CARTESIAN_POINT('Ctrl Pts',(-3.62620924565683,-3.32344943664825,
18.8462506684459));
#27178=CARTESIAN_POINT('Ctrl Pts',(-3.46224163338755,-3.49701328387295,
18.8598400613412));
#27179=CARTESIAN_POINT('Ctrl Pts',(-3.34340424706155,-3.61079851719021,
18.8692445836429));
#27180=CARTESIAN_POINT('Ctrl Pts',(-3.12769534767233,-3.79754120303279,
18.8855774755665));
#27181=CARTESIAN_POINT('Ctrl Pts',(-3.0334103812626,-3.87326984610622,18.8924955985524));
#27182=CARTESIAN_POINT('Ctrl Pts',(-2.90176331872345,-3.971249201631,18.9018392393749));
#27183=CARTESIAN_POINT('Ctrl Pts',(-2.86675735132641,-3.99659266451767,
18.9042947421531));
#27184=CARTESIAN_POINT('Ctrl Pts',(-2.79745069637361,-4.04538981668817,
18.9090973586495));
#27185=CARTESIAN_POINT('Ctrl Pts',(-2.76317777843545,-4.06887672208052,
18.9114446850763));
#27186=CARTESIAN_POINT('Ctrl Pts',(-2.70723318683238,-4.106182140402,18.9152360835218));
#27187=CARTESIAN_POINT('Ctrl Pts',(-2.68574374039819,-4.120269878116,18.9166830139671));
#27188=CARTESIAN_POINT('Ctrl Pts',(-2.53698201416529,-4.2161345852076,18.9266388551767));
#27189=CARTESIAN_POINT('Ctrl Pts',(-2.40610521177728,-4.29217042399064,
18.9350967906375));
#27190=CARTESIAN_POINT('Ctrl Pts',(-2.15667076220081,-4.4220858485639,18.950858366288));
#27191=CARTESIAN_POINT('Ctrl Pts',(-2.03907694281269,-4.4775257288273,18.9581500052383));
#27192=CARTESIAN_POINT('Ctrl Pts',(-1.86096931040973,-4.55302180645849,
18.9690559070836));
#27193=CARTESIAN_POINT('Ctrl Pts',(-1.80203782152275,-4.57666624571895,
18.972642362632));
#27194=CARTESIAN_POINT('Ctrl Pts',(-1.67429179087219,-4.62507040204111,
18.9803769290442));
#27195=CARTESIAN_POINT('Ctrl Pts',(-1.60534940486965,-4.64944968180691,
18.9845268337863));
#27196=CARTESIAN_POINT('Ctrl Pts',(-1.46042235444775,-4.69709062798457,
18.993206967944));
#27197=CARTESIAN_POINT('Ctrl Pts',(-1.38436554835867,-4.72006627853959,
18.9977378139438));
#27198=CARTESIAN_POINT('Ctrl Pts',(-1.13795636709494,-4.78803456660602,
19.0123432878017));
#27199=CARTESIAN_POINT('Ctrl Pts',(-0.965732514575637,-4.82572070531165,
19.0224442742439));
#27200=CARTESIAN_POINT('Ctrl Pts',(-0.73189540278334,-4.86386713407337,
19.0359703616864));
#27201=CARTESIAN_POINT('Ctrl Pts',(-0.671755195955901,-4.87253727159177,
19.0394320181174));
#27202=CARTESIAN_POINT('Ctrl Pts',(-0.574636582512346,-4.8847061131109,
19.0449895497474));
#27203=CARTESIAN_POINT('Ctrl Pts',(-0.537752730431801,-4.88890407504678,
19.0470922966295));
#27204=CARTESIAN_POINT('Ctrl Pts',(-0.439376127973308,-4.89897408978788,
19.0526811382177));
#27205=CARTESIAN_POINT('Ctrl Pts',(-0.377814255559296,-4.90410593696443,
19.0561591307644));
#27206=CARTESIAN_POINT('Ctrl Pts',(-0.221688612512808,-4.9141633361231,
19.0649508945403));
#27207=CARTESIAN_POINT('Ctrl Pts',(-0.127049114941793,-4.91752029420821,
19.0702539036086));
#27208=CARTESIAN_POINT('Ctrl Pts',(0.128110007983465,-4.91919976060268,
19.0845484213874));
#27209=CARTESIAN_POINT('Ctrl Pts',(0.288545404198044,-4.91240055445093,
19.0935356251746));
#27210=CARTESIAN_POINT('Ctrl Pts',(0.520877362957384,-4.89113205091828,
19.1066790941154));
#27211=CARTESIAN_POINT('Ctrl Pts',(0.593238207355761,-4.88288380296367,
19.1107904015576));
#27212=CARTESIAN_POINT('Ctrl Pts',(0.737208516714782,-4.86322536304217,
19.1190162359285));
#27213=CARTESIAN_POINT('Ctrl Pts',(0.808802228264358,-4.85183224348297,
19.1231296527065));
#27214=CARTESIAN_POINT('Ctrl Pts',(0.91991527541282,-4.83162242107554,19.1295543828845));
#27215=CARTESIAN_POINT('Ctrl Pts',(0.959622202801336,-4.82389308921639,
19.1318584369995));
#27216=CARTESIAN_POINT('Ctrl Pts',(1.18717597902908,-4.77667678782321,19.1451110964801));
#27217=CARTESIAN_POINT('Ctrl Pts',(1.37267792339923,-4.72670945843621,19.156112912456));
#27218=CARTESIAN_POINT('Ctrl Pts',(1.62424242056307,-4.6428848850602,19.171271782757));
#27219=CARTESIAN_POINT('Ctrl Pts',(1.6931778874436,-4.61819145541775,19.1754503712101));
#27220=CARTESIAN_POINT('Ctrl Pts',(1.79432833913429,-4.57938886658624,19.1816109367912));
#27221=CARTESIAN_POINT('Ctrl Pts',(1.82698441010816,-4.56645864854688,19.1836043907144));
#27222=CARTESIAN_POINT('Ctrl Pts',(1.90095871697168,-4.53624785186008,19.1881289700401));
#27223=CARTESIAN_POINT('Ctrl Pts',(1.94218511172701,-4.51875045484249,19.1906572438408));
#27224=CARTESIAN_POINT('Ctrl Pts',(2.03430189876892,-4.4781604816573,19.1963286959396));
#27225=CARTESIAN_POINT('Ctrl Pts',(2.0850493284833,-4.45475867932403,19.1994686338295));
#27226=CARTESIAN_POINT('Ctrl Pts',(2.27029906402286,-4.3654730044483,19.211009229151));
#27227=CARTESIAN_POINT('Ctrl Pts',(2.4021705511308,-4.29432057232326,19.2193811843846));
#27228=CARTESIAN_POINT('Ctrl Pts',(2.62338472373952,-4.16157987907467,19.2338548520061));
#27229=CARTESIAN_POINT('Ctrl Pts',(2.71431581368152,-4.10285068484597,19.239937484154));
#27230=CARTESIAN_POINT('Ctrl Pts',(2.85949994390126,-4.00214095390071,19.2499085564038));
#27231=CARTESIAN_POINT('Ctrl Pts',(2.91494352867892,-3.96194096733918,19.2537811969673));
#27232=CARTESIAN_POINT('Ctrl Pts',(3.03517632227392,-3.870874526165,19.2623326010502));
#27233=CARTESIAN_POINT('Ctrl Pts',(3.09956361540195,-3.81951175752819,19.26701442908));
#27234=CARTESIAN_POINT('Ctrl Pts',(3.23858366880941,-3.70278206802622,19.2773610906178));
#27235=CARTESIAN_POINT('Ctrl Pts',(3.31259003083972,-3.63672465910901,19.2830291351357));
#27236=CARTESIAN_POINT('Ctrl Pts',(3.5045930936445,-3.45461787963514,19.298172563015));
#27237=CARTESIAN_POINT('Ctrl Pts',(3.61881712636447,-3.33477447372053,19.3076541905599));
#27238=CARTESIAN_POINT('Ctrl Pts',(3.75403136367206,-3.17776258546909,19.3194478308024));
#27239=CARTESIAN_POINT('Ctrl Pts',(3.78087467785808,-3.14577705156483,19.3218195512954));
#27240=CARTESIAN_POINT('Ctrl Pts',(3.83451221282742,-3.08018602581176,19.3266189163718));
#27241=CARTESIAN_POINT('Ctrl Pts',(3.86127981128248,-3.04656333286735,19.3290460523197));
#27242=CARTESIAN_POINT('Ctrl Pts',(3.90419197598866,-2.991187305484,19.3329947391149));
#27243=CARTESIAN_POINT('Ctrl Pts',(3.92060340974476,-2.96964398473853,19.334519162483));
#27244=CARTESIAN_POINT('Ctrl Pts',(3.98484223628481,-2.88385679413459,19.3405459276595));
#27245=CARTESIAN_POINT('Ctrl Pts',(4.03127548615795,-2.81858399923418,19.3450359004127));
#27246=CARTESIAN_POINT('Ctrl Pts',(4.17122233247975,-2.61131880567306,19.359049186885));
#27247=CARTESIAN_POINT('Ctrl Pts',(4.25898122966773,-2.46559523781207,19.3685590201726));
#27248=CARTESIAN_POINT('Ctrl Pts',(4.37521519296654,-2.24779573884169,19.3824547186311));
#27249=CARTESIAN_POINT('Ctrl Pts',(4.40981659854938,-2.17913080129116,19.386791346997));
#27250=CARTESIAN_POINT('Ctrl Pts',(4.47278107941558,-2.04653356507111,19.3950948936077));
#27251=CARTESIAN_POINT('Ctrl Pts',(4.50141812470357,-1.98275185892781,19.3990587030837));
#27252=CARTESIAN_POINT('Ctrl Pts',(4.58172078126055,-1.79318299274071,19.4107605899651));
#27253=CARTESIAN_POINT('Ctrl Pts',(4.62954064815573,-1.66584006521686,19.4185220974666));
#27254=CARTESIAN_POINT('Ctrl Pts',(4.72685629629543,-1.36996812769256,19.4363425988618));
#27255=CARTESIAN_POINT('Ctrl Pts',(4.77272788172151,-1.20043844764767,19.4464028437742));
#27256=CARTESIAN_POINT('Ctrl Pts',(4.81804093246147,-0.988612762782616,
19.4587299222992));
#27257=CARTESIAN_POINT('Ctrl Pts',(4.82613738011974,-0.948299357519549,
19.4610649764219));
#27258=CARTESIAN_POINT('Ctrl Pts',(4.84180297542768,-0.864893530228911,
19.4658712360023));
#27259=CARTESIAN_POINT('Ctrl Pts',(4.84930456243093,-0.821792061921997,
19.4683415685301));
#27260=CARTESIAN_POINT('Ctrl Pts',(4.86476479252794,-0.725364078129904,
19.4738450608758));
#27261=CARTESIAN_POINT('Ctrl Pts',(4.87242363944781,-0.671995151214585,
19.4768752744007));
#27262=CARTESIAN_POINT('Ctrl Pts',(4.89635685603151,-0.483194833892426,
19.4875578036661));
#27263=CARTESIAN_POINT('Ctrl Pts',(4.90787364274382,-0.347223573507748,
19.4951852407297));
#27264=CARTESIAN_POINT('Ctrl Pts',(4.9188097554043,-0.0924847346240719,
19.5094815563517));
#27265=CARTESIAN_POINT('Ctrl Pts',(4.91960972675315,0.0261240352611648,
19.5161404403524));
#27266=CARTESIAN_POINT('Ctrl Pts',(4.91410453217042,0.213232477211713,19.5266986324756));
#27267=CARTESIAN_POINT('Ctrl Pts',(4.9106513707835,0.281770149642892,19.5305772269907));
#27268=CARTESIAN_POINT('Ctrl Pts',(4.90019267294761,0.428275214564888,19.5389004963521));
#27269=CARTESIAN_POINT('Ctrl Pts',(4.89275753682427,0.506193020379609,19.5433469751185));
#27270=CARTESIAN_POINT('Ctrl Pts',(4.87275435669971,0.673490396800174,19.5529440966326));
#27271=CARTESIAN_POINT('Ctrl Pts',(4.85957896867461,0.762768875663262,19.5580967183268));
#27272=CARTESIAN_POINT('Ctrl Pts',(4.81573103892388,1.01216885011612,19.5725804157951));
#27273=CARTESIAN_POINT('Ctrl Pts',(4.77954362239245,1.17120207407848,19.5819238252465));
#27274=CARTESIAN_POINT('Ctrl Pts',(4.72145928084235,1.37830296625863,19.5941901124877));
#27275=CARTESIAN_POINT('Ctrl Pts',(4.70659556462621,1.42823495549765,19.5971548968754));
#27276=CARTESIAN_POINT('Ctrl Pts',(4.67970196840458,1.51359555077219,19.602232433501));
#27277=CARTESIAN_POINT('Ctrl Pts',(4.66805609797243,1.54913985760844,19.6043490560377));
#27278=CARTESIAN_POINT('Ctrl Pts',(4.63169333064582,1.65598750128358,19.6107225584945));
#27279=CARTESIAN_POINT('Ctrl Pts',(4.60573968511436,1.72685838715588,19.6149655800664));
#27280=CARTESIAN_POINT('Ctrl Pts',(4.52656548317585,1.9285564901575,19.6271272528967));
#27281=CARTESIAN_POINT('Ctrl Pts',(4.4693279356573,2.05772524694976,19.6350230689612));
#27282=CARTESIAN_POINT('Ctrl Pts',(4.35533300492557,2.28770393681237,19.6494179884599));
#27283=CARTESIAN_POINT('Ctrl Pts',(4.30042770271129,2.38931705205794,19.6559042867065));
#27284=CARTESIAN_POINT('Ctrl Pts',(4.2071387682403,2.54831542005669,19.6663043605052));
#27285=CARTESIAN_POINT('Ctrl Pts',(4.17103554398776,2.60698876946897,19.6701989748279));
#27286=CARTESIAN_POINT('Ctrl Pts',(4.09026532004442,2.73227784730404,19.6786484604192));
#27287=CARTESIAN_POINT('Ctrl Pts',(4.04517721981732,2.79859851828699,19.6832056239085));
#27288=CARTESIAN_POINT('Ctrl Pts',(3.90488611654688,2.99447635750198,19.6969337609773));
#27289=CARTESIAN_POINT('Ctrl Pts',(3.80493356569033,3.12049738133075,19.7061344269571));
#27290=CARTESIAN_POINT('Ctrl Pts',(3.627198762198,3.32332340285735,19.7215708197155));
#27291=CARTESIAN_POINT('Ctrl Pts',(3.55270376558751,3.40284376000782,19.7278010753153));
#27292=CARTESIAN_POINT('Ctrl Pts',(3.44588222421833,3.5095364935912,19.7363948210824));
#27293=CARTESIAN_POINT('Ctrl Pts',(3.4157551803352,3.53886525715323,19.7387831016085));
#27294=CARTESIAN_POINT('Ctrl Pts',(3.3543098991227,3.59716665476884,19.743581233846));
#27295=CARTESIAN_POINT('Ctrl Pts',(3.32298328459847,3.62612534105932,19.7459907296958));
#27296=CARTESIAN_POINT('Ctrl Pts',(3.1464425344962,3.78511239205391,19.7593826341135));
#27297=CARTESIAN_POINT('Ctrl Pts',(2.99397369653049,3.90682730708985,19.7702632753973));
#27298=CARTESIAN_POINT('Ctrl Pts',(2.73779672420761,4.08750640222258,19.7878412051488));
#27299=CARTESIAN_POINT('Ctrl Pts',(2.63847195465235,4.15231317731388,19.7945000067143));
#27300=CARTESIAN_POINT('Ctrl Pts',(2.47774168652459,4.24908792361381,19.8050835317234));
#27301=CARTESIAN_POINT('Ctrl Pts',(2.4178365971761,4.28345866027102,19.8089875786432));
#27302=CARTESIAN_POINT('Ctrl Pts',(2.28748222242553,4.35464387717831,19.817405527634));
#27303=CARTESIAN_POINT('Ctrl Pts',(2.2168240648166,4.39103507942887,19.8219214578777));
#27304=CARTESIAN_POINT('Ctrl Pts',(2.0004569245974,4.49591703447775,19.8356201890093));
#27305=CARTESIAN_POINT('Ctrl Pts',(1.85223897866696,4.55898099758762,19.8448332815318));
#27306=CARTESIAN_POINT('Ctrl Pts',(1.59953284735159,4.65214124076494,19.8602499369504));
#27307=CARTESIAN_POINT('Ctrl Pts',(1.49665642634832,4.68625046031451,19.8664476008381));
#27308=CARTESIAN_POINT('Ctrl Pts',(1.35151408767178,4.72910564403863,19.8750637351172));
#27309=CARTESIAN_POINT('Ctrl Pts',(1.3101332551722,4.74073638085314,19.8775058862079));
#27310=CARTESIAN_POINT('Ctrl Pts',(1.22826956602362,4.76259171469625,19.8823065276988));
#27311=CARTESIAN_POINT('Ctrl Pts',(1.18779838140854,4.77284621815424,19.8846651217342));
#27312=CARTESIAN_POINT('Ctrl Pts',(1.12202251238696,4.78862391420492,19.8884788499442));
#27313=CARTESIAN_POINT('Ctrl Pts',(1.09679635259678,4.79446465005718,19.8899368428148));
#27314=CARTESIAN_POINT('Ctrl Pts',(0.998780478637364,4.81634468282167,19.8955861802687));
#27315=CARTESIAN_POINT('Ctrl Pts',(0.925675608253634,4.83092779384029,19.8997664283788));
#27316=CARTESIAN_POINT('Ctrl Pts',(0.658333081801188,4.87796631825089,19.9149796688525));
#27317=CARTESIAN_POINT('Ctrl Pts',(0.462526433117458,4.90041081634733,19.925988357735));
#27318=CARTESIAN_POINT('Ctrl Pts',(0.193718860918683,4.91496510686333,19.9411563286238));
#27319=CARTESIAN_POINT('Ctrl Pts',(0.121457143487274,4.91728146450245,19.945238271405));
#27320=CARTESIAN_POINT('Ctrl Pts',(0.00686639641869532,4.91842716653716,
19.9517264060405));
#27321=CARTESIAN_POINT('Ctrl Pts',(-0.0354419246901917,4.91830425822997,
19.9541251300483));
#27322=CARTESIAN_POINT('Ctrl Pts',(-0.145492786155172,4.91656445772501,
19.9603748387904));
#27323=CARTESIAN_POINT('Ctrl Pts',(-0.213212531446191,4.91409345748516,
19.9642307652372));
#27324=CARTESIAN_POINT('Ctrl Pts',(-0.38688485398336,4.90415960294977,19.974150018255));
#27325=CARTESIAN_POINT('Ctrl Pts',(-0.492685660863038,4.89466258774151,
19.9802224140866));
#27326=CARTESIAN_POINT('Ctrl Pts',(-0.717299590460411,4.86714365382385,
19.9931751076551));
#27327=CARTESIAN_POINT('Ctrl Pts',(-0.83592958645818,4.84817780437051,20.0000530840343));
#27328=CARTESIAN_POINT('Ctrl Pts',(-1.00854683223634,4.81405616478265,20.0100934607818));
#27329=CARTESIAN_POINT('Ctrl Pts',(-1.0631590083135,4.8022907552385,20.0132746103603));
#27330=CARTESIAN_POINT('Ctrl Pts',(-1.12486107586515,4.78789377919472,20.016871114548));
#27331=CARTESIAN_POINT('Ctrl Pts',(-1.13215893972855,4.78617335837082,20.0172965309918));
#27332=CARTESIAN_POINT('Ctrl Pts',(-1.17381060179265,4.7762536724149,20.0197247142577));
#27333=CARTESIAN_POINT('Ctrl Pts',(-1.20807911052451,4.76770126540984,20.0217228261442));
#27334=CARTESIAN_POINT('Ctrl Pts',(-1.24501400374092,4.75805961880605,20.0238781474693));
#27335=CARTESIAN_POINT('Ctrl Pts',(-1.24777446657012,4.75733644870801,20.0240392443418));
#27336=CARTESIAN_POINT('Ctrl Pts',(-1.25347037997348,4.7558389675686,20.0243716748096));
#27337=CARTESIAN_POINT('Ctrl Pts',(-1.25640574714266,4.7550643399938,20.0245430051136));
#27338=CARTESIAN_POINT('Ctrl Pts',(-1.2625548712552,4.75343552784848,20.0249019450786));
#27339=CARTESIAN_POINT('Ctrl Pts',(-1.26576848320394,4.75258080071179,20.025089549177));
#27340=CARTESIAN_POINT('Ctrl Pts',(-1.27259250431573,4.75075839754867,20.0254879613153));
#27341=CARTESIAN_POINT('Ctrl Pts',(-1.27620268261707,4.74978986343968,20.0256987608068));
#27342=CARTESIAN_POINT('Ctrl Pts',(-1.28396402195081,4.74769817347365,20.0261520026911));
#27343=CARTESIAN_POINT('Ctrl Pts',(-1.28811482175121,4.7465736865768,20.0263944322311));
#27344=CARTESIAN_POINT('Ctrl Pts',(-1.29325052438582,4.74517514837672,20.026694430635));
#27345=CARTESIAN_POINT('Ctrl Pts',(-1.29423682104021,4.74490623286286,20.0267520465109));
#27346=CARTESIAN_POINT('Ctrl Pts',(-1.29671403840483,4.74422998534715,20.0268967618399));
#27347=CARTESIAN_POINT('Ctrl Pts',(-1.29820485123214,4.74382225800069,20.0269838576877));
#27348=CARTESIAN_POINT('Ctrl Pts',(-1.30198118215206,4.74278754326246,20.0272044898995));
#27349=CARTESIAN_POINT('Ctrl Pts',(-1.3042664401492,4.74215960637262,20.0273380177192));
#27350=CARTESIAN_POINT('Ctrl Pts',(-1.31012133743681,4.74054626145924,20.0276801506956));
#27351=CARTESIAN_POINT('Ctrl Pts',(-1.31369032037994,4.73955847289722,20.0278887348446));
#27352=CARTESIAN_POINT('Ctrl Pts',(-1.32296552816608,4.73698008912057,20.0284308920981));
#27353=CARTESIAN_POINT('Ctrl Pts',(-1.32867000372478,4.73538321308394,20.0287644114725));
#27354=CARTESIAN_POINT('Ctrl Pts',(-1.39764886320229,4.71593923656379,20.0327983964666));
#27355=CARTESIAN_POINT('Ctrl Pts',(-1.46056254049221,4.69683536009163,20.0364884487407));
#27356=CARTESIAN_POINT('Ctrl Pts',(-1.73234654059603,4.60831842322037,20.052515612393));
#27357=CARTESIAN_POINT('Ctrl Pts',(-1.9368056692472,4.52619111309733,20.0648081656987));
#27358=CARTESIAN_POINT('Ctrl Pts',(-2.18741716397102,4.40542451548976,20.0804891615229));
#27359=CARTESIAN_POINT('Ctrl Pts',(-2.23930825192616,4.37927590823518,20.0837700930237));
#27360=CARTESIAN_POINT('Ctrl Pts',(-2.34594576678927,4.32314883098023,20.0905892351438));
#27361=CARTESIAN_POINT('Ctrl Pts',(-2.4006094166857,4.29303525228549,20.0941279004626));
#27362=CARTESIAN_POINT('Ctrl Pts',(-2.51663105814461,4.22621124387671,20.1017367869762));
#27363=CARTESIAN_POINT('Ctrl Pts',(-2.5777915798545,4.18918653092184,20.1058085437105));
#27364=CARTESIAN_POINT('Ctrl Pts',(-2.74385248774433,4.08364431442169,20.1170377892196));
#27365=CARTESIAN_POINT('Ctrl Pts',(-2.84697544566685,4.01243165993736,20.1242086071037));
#27366=CARTESIAN_POINT('Ctrl Pts',(-2.95642222677594,3.93050651774702,20.1320344171906));
#27367=CARTESIAN_POINT('Ctrl Pts',(-2.965554367429,3.92362092498309,20.1326890742104));
#27368=CARTESIAN_POINT('Ctrl Pts',(-3.05915880171828,3.85253012396034,20.1394164886881));
#27369=CARTESIAN_POINT('Ctrl Pts',(-3.14155717965971,3.78563862674755,20.1454834655101));
#27370=CARTESIAN_POINT('Ctrl Pts',(-3.25274580468659,3.68924287971734,20.1538575485699));
#27371=CARTESIAN_POINT('Ctrl Pts',(-3.28342597606756,3.66196425665762,20.1561888783821));
#27372=CARTESIAN_POINT('Ctrl Pts',(-3.34461570159707,3.60617142332149,20.1608785596103));
#27373=CARTESIAN_POINT('Ctrl Pts',(-3.37511082618469,3.5776463617704,20.1632366772715));
#27374=CARTESIAN_POINT('Ctrl Pts',(-3.41875128830562,3.53577054909075,20.1666456851509));
#27375=CARTESIAN_POINT('Ctrl Pts',(-3.43218921955439,3.52272776580468,20.1677002311345));
#27376=CARTESIAN_POINT('Ctrl Pts',(-3.46132935260226,3.49411948832873,20.16999809171));
#27377=CARTESIAN_POINT('Ctrl Pts',(-3.47700175729448,3.47852420871381,20.1712410694524));
#27378=CARTESIAN_POINT('Ctrl Pts',(-3.56437494627038,3.39040050653644,20.1782128622542));
#27379=CARTESIAN_POINT('Ctrl Pts',(-3.63391166545402,3.31576093242839,20.1839231048122));
#27380=CARTESIAN_POINT('Ctrl Pts',(-3.80576622150275,3.11939030161214,20.1985419915032));
#27381=CARTESIAN_POINT('Ctrl Pts',(-3.90459254113118,2.99476352706129,20.2074487818447));
#27382=CARTESIAN_POINT('Ctrl Pts',(-4.02644777760171,2.82478665607139,20.2192384447823));
#27383=CARTESIAN_POINT('Ctrl Pts',(-4.05506011657345,2.78355685329612,20.22207166518));
#27384=CARTESIAN_POINT('Ctrl Pts',(-4.09776891307631,2.71995796874464,20.2264046753747));
#27385=CARTESIAN_POINT('Ctrl Pts',(-4.11232437550277,2.69790096912222,20.2279007003425));
#27386=CARTESIAN_POINT('Ctrl Pts',(-4.16807613635892,2.611916563205,20.2337074769161));
#27387=CARTESIAN_POINT('Ctrl Pts',(-4.20796496005974,2.54715478901617,20.2380277707696));
#27388=CARTESIAN_POINT('Ctrl Pts',(-4.29074913079805,2.40549444999091,20.247371730651));
#27389=CARTESIAN_POINT('Ctrl Pts',(-4.33311385126951,2.32831608453999,20.2523974351221));
#27390=CARTESIAN_POINT('Ctrl Pts',(-4.44863512482891,2.10377863784714,20.2668379662034));
#27391=CARTESIAN_POINT('Ctrl Pts',(-4.5165012312343,1.95383108247484,20.2762672745679));
#27392=CARTESIAN_POINT('Ctrl Pts',(-4.59635539201891,1.750878122394,20.2887085913383));
#27393=CARTESIAN_POINT('Ctrl Pts',(-4.61516729231499,1.70067282216006,20.2917606471296));
#27394=CARTESIAN_POINT('Ctrl Pts',(-4.64462112157506,1.61797577883822,20.2967425556194));
#27395=CARTESIAN_POINT('Ctrl Pts',(-4.65575158392822,1.58566333095274,20.2986776402141));
#27396=CARTESIAN_POINT('Ctrl Pts',(-4.67952939376046,1.51422529478869,20.3029320526274));
#27397=CARTESIAN_POINT('Ctrl Pts',(-4.69202465932715,1.47505194165565,20.3052497211436));
#27398=CARTESIAN_POINT('Ctrl Pts',(-4.72563968281926,1.36491535679559,20.3117300454252));
#27399=CARTESIAN_POINT('Ctrl Pts',(-4.74564665006456,1.29363767442263,20.3158827199713));
#27400=CARTESIAN_POINT('Ctrl Pts',(-4.76403459893337,1.2219481996655,20.3200311864783));
#27401=CARTESIAN_POINT('Origin',(0.,0.,-3.23514056400928));
#27402=CARTESIAN_POINT('',(-4.76363197251292,1.22184512090322,22.4152102246214));
#27403=CARTESIAN_POINT('',(-4.76399535256163,1.22193798731013,22.0699206410069));
#27404=CARTESIAN_POINT('',(-4.76403458704967,1.22194824599672,-3.23514056400928));
#27405=CARTESIAN_POINT('',(-4.91798113867399,8.40603594123364E-5,20.7351405640093));
#27406=CARTESIAN_POINT('Ctrl Pts',(-4.91792389088375,8.40593809071227E-5,
20.7351405640093));
#27407=CARTESIAN_POINT('Ctrl Pts',(-4.91761499568841,-0.506908622338837,
20.7638467393807));
#27408=CARTESIAN_POINT('Ctrl Pts',(-4.71379420543462,-1.83214221616955,
20.8388683765138));
#27409=CARTESIAN_POINT('Ctrl Pts',(-3.54218620419026,-3.70656535167346,
20.9602054754087));
#27410=CARTESIAN_POINT('Ctrl Pts',(-1.33712299005241,-4.94952643399905,
21.0991518606938));
#27411=CARTESIAN_POINT('Ctrl Pts',(1.1938697653851,-4.98601893244312,21.2380982459789));
#27412=CARTESIAN_POINT('Ctrl Pts',(3.43385157575744,-3.80714764187707,21.377044631264));
#27413=CARTESIAN_POINT('Ctrl Pts',(4.83681713758415,-1.70026756393053,21.5159910165492));
#27414=CARTESIAN_POINT('Ctrl Pts',(5.0607874964779,0.821060123788163,21.6549374018343));
#27415=CARTESIAN_POINT('Ctrl Pts',(4.05116890385901,3.14225083718467,21.7938837871194));
#27416=CARTESIAN_POINT('Ctrl Pts',(2.05406028049099,4.69750424965121,21.9328301724046));
#27417=CARTESIAN_POINT('Ctrl Pts',(-0.443734465247909,5.10772058121166,
22.0717765576897));
#27418=CARTESIAN_POINT('Ctrl Pts',(-2.83336700616869,4.27290781783748,22.2107229429748));
#27419=CARTESIAN_POINT('Ctrl Pts',(-4.23316194614979,2.72698140687266,22.3252008319521));
#27420=CARTESIAN_POINT('Ctrl Pts',(-4.66782063352313,1.59563011253093,22.3933632591676));
#27421=CARTESIAN_POINT('Ctrl Pts',(-4.76363197251275,1.2218451209039,22.4152102246213));
#27422=CARTESIAN_POINT('Ctrl Pts',(-4.76403458704968,1.22194824599669,20.6652050067296));
#27423=CARTESIAN_POINT('Ctrl Pts',(-4.78905017617746,1.12441945767804,20.6709075727659));
#27424=CARTESIAN_POINT('Ctrl Pts',(-4.81106738250268,1.02613190791664,20.6766101388022));
#27425=CARTESIAN_POINT('Ctrl Pts',(-4.8300460831109,0.92727444563358,20.6823127048384));
#27426=CARTESIAN_POINT('Ctrl Pts',(-4.85934880158881,0.774640582730084,
20.6911173480336));
#27427=CARTESIAN_POINT('Ctrl Pts',(-4.88141421064647,0.620601429743954,
20.6999219912287));
#27428=CARTESIAN_POINT('Ctrl Pts',(-4.89613885764341,0.465840476101292,
20.7087266344239));
#27429=CARTESIAN_POINT('Ctrl Pts',(-4.91086350464035,0.311079522458631,
20.717531277619));
#27430=CARTESIAN_POINT('Ctrl Pts',(-4.91824734118169,0.155597140481115,
20.7263359208142));
#27431=CARTESIAN_POINT('Ctrl Pts',(-4.91824999928156,8.40649548998676E-5,
20.7351405640093));
#27432=CARTESIAN_POINT('',(-4.91801076244909,-0.000108722639682,20.3898594359907));
#27433=CARTESIAN_POINT('Ctrl Pts',(-4.76403459893337,1.2219481996655,20.3200311864783));
#27434=CARTESIAN_POINT('Ctrl Pts',(-4.78939679683197,1.1230680766562,20.3257530986544));
#27435=CARTESIAN_POINT('Ctrl Pts',(-4.81167893680868,1.02340456671475,20.3314672887943));
#27436=CARTESIAN_POINT('Ctrl Pts',(-4.85262058922403,0.809145605183855,
20.3436986279325));
#27437=CARTESIAN_POINT('Ctrl Pts',(-4.87035662702895,0.694455932341157,
20.3502142598379));
#27438=CARTESIAN_POINT('Ctrl Pts',(-4.89205212983886,0.511526776241396,
20.3606037104151));
#27439=CARTESIAN_POINT('Ctrl Pts',(-4.89867442481973,0.443646736066814,
20.3644580876923));
#27440=CARTESIAN_POINT('Ctrl Pts',(-4.90824927956457,0.318653304397231,
20.371561197904));
#27441=CARTESIAN_POINT('Ctrl Pts',(-4.91162140275056,0.261583703428601,
20.3748064943107));
#27442=CARTESIAN_POINT('Ctrl Pts',(-4.91683397047562,0.136310000200659,
20.3819382603392));
#27443=CARTESIAN_POINT('Ctrl Pts',(-4.91825161573311,0.0681001683324553,
20.3858266413289));
#27444=CARTESIAN_POINT('Ctrl Pts',(-4.91824999861809,-0.000116589767614233,
20.3897217550049));
#27445=CARTESIAN_POINT('Ctrl Pts',(-4.91801076244909,-0.000108722639682,
20.3898594359907));
#27446=CARTESIAN_POINT('Ctrl Pts',(-4.91822955624353,-0.271374287939473,
20.4052194041072));
#27447=CARTESIAN_POINT('Ctrl Pts',(-4.82960853223233,-1.36088848373683,
20.4669193707278));
#27448=CARTESIAN_POINT('Ctrl Pts',(-4.03599310824848,-3.16208627326169,
20.5749593358526));
#27449=CARTESIAN_POINT('Ctrl Pts',(-2.02999983921845,-4.70819823522251,
20.7139793313651));
#27450=CARTESIAN_POINT('Ctrl Pts',(0.471328207970822,-5.10547546167352,
20.8529993268776));
#27451=CARTESIAN_POINT('Ctrl Pts',(2.85764873209287,-4.25697940955172,20.9920193223901));
#27452=CARTESIAN_POINT('Ctrl Pts',(4.54668210701339,-2.36974930892355,21.1310393179027));
#27453=CARTESIAN_POINT('Ctrl Pts',(5.12629186064678,0.0957169203737284,
21.2700593134152));
#27454=CARTESIAN_POINT('Ctrl Pts',(4.45504898241472,2.53782752244213,21.4090793089277));
#27455=CARTESIAN_POINT('Ctrl Pts',(2.69674163414686,4.36068968490516,21.5480993044402));
#27456=CARTESIAN_POINT('Ctrl Pts',(0.28040964307056,5.11951173467278,21.6871192999527));
#27457=CARTESIAN_POINT('Ctrl Pts',(-2.20434434768312,4.62913555280215,21.8261392954652));
#27458=CARTESIAN_POINT('Ctrl Pts',(-3.99129943177484,3.14228185516009,21.9537397424833));
#27459=CARTESIAN_POINT('Ctrl Pts',(-4.61016782489247,1.81908628318109,22.0350001909972));
#27460=CARTESIAN_POINT('Ctrl Pts',(-4.76399535256163,1.22193798731013,22.0699206410069));
#27461=CARTESIAN_POINT('Origin',(0.,0.,-3.23514056400928));
#27462=CARTESIAN_POINT('',(-4.76403458701365,1.22194824613716,24.1649977190913));
#27463=CARTESIAN_POINT('',(-4.76403458704968,1.22194824599669,23.8199296610182));
#27464=CARTESIAN_POINT('',(-4.76403458704967,1.22194824599672,-3.23514056400928));
#27465=CARTESIAN_POINT('',(-4.91864051099776,-2.23298241357769E-5,22.4851265773791));
#27466=CARTESIAN_POINT('Ctrl Pts',(-4.76403458701365,1.22194824613716,24.1649977190913));
#27467=CARTESIAN_POINT('Ctrl Pts',(-4.75363281635131,1.2625018418874,24.1626119398973));
#27468=CARTESIAN_POINT('Ctrl Pts',(-4.74271348670068,1.30292162016342,24.1602303929971));
#27469=CARTESIAN_POINT('Ctrl Pts',(-4.72112396186882,1.37896855831405,24.1557448825383));
#27470=CARTESIAN_POINT('Ctrl Pts',(-4.71056339189361,1.41462302684786,24.1536402595871));
#27471=CARTESIAN_POINT('Ctrl Pts',(-4.67841977361937,1.51879268596693,24.1474832684845));
#27472=CARTESIAN_POINT('Ctrl Pts',(-4.65573882185894,1.58695904832956,24.1434431493272));
#27473=CARTESIAN_POINT('Ctrl Pts',(-4.58869297343085,1.77463391762388,24.1322545062445));
#27474=CARTESIAN_POINT('Ctrl Pts',(-4.54116335511359,1.89295122427059,24.1251249865935));
#27475=CARTESIAN_POINT('Ctrl Pts',(-4.43836439743762,2.12262151543145,24.1110205962885));
#27476=CARTESIAN_POINT('Ctrl Pts',(-4.3833642138382,2.23399155090376,24.1040515868379));
#27477=CARTESIAN_POINT('Ctrl Pts',(-4.2942992636445,2.39835741281224,24.0935113850455));
#27478=CARTESIAN_POINT('Ctrl Pts',(-4.26333539333574,2.45297689826029,24.0899649190951));
#27479=CARTESIAN_POINT('Ctrl Pts',(-4.19435753355469,2.56939882590294,24.0823029697932));
#27480=CARTESIAN_POINT('Ctrl Pts',(-4.15600446169644,2.63098312326885,24.0781856610526));
#27481=CARTESIAN_POINT('Ctrl Pts',(-4.07315478243788,2.7576818390502,24.0695724340903));
#27482=CARTESIAN_POINT('Ctrl Pts',(-4.02842584521631,2.82262006741788,24.0650758955646));
#27483=CARTESIAN_POINT('Ctrl Pts',(-3.88001568486795,3.02736687603185,24.0506272348809));
#27484=CARTESIAN_POINT('Ctrl Pts',(-3.77046851882402,3.16275812411159,24.0406493719329));
#27485=CARTESIAN_POINT('Ctrl Pts',(-3.61240899686483,3.33819423488402,24.0271664021113));
#27486=CARTESIAN_POINT('Ctrl Pts',(-3.56997135369261,3.38354018417156,24.0236275420042));
#27487=CARTESIAN_POINT('Ctrl Pts',(-3.50106217658194,3.45443167303,24.018013218801));
#27488=CARTESIAN_POINT('Ctrl Pts',(-3.47514349412997,3.48050460217875,24.0159303289431));
#27489=CARTESIAN_POINT('Ctrl Pts',(-3.40708780186065,3.54744714701854,24.0105342388606));
#27490=CARTESIAN_POINT('Ctrl Pts',(-3.36450710698333,3.58785738281828,24.007228026295));
#27491=CARTESIAN_POINT('Ctrl Pts',(-3.28824842792264,3.65767725505637,24.0014158383051));
#27492=CARTESIAN_POINT('Ctrl Pts',(-3.25487391797626,3.68740782044014,23.9989074307868));
#27493=CARTESIAN_POINT('Ctrl Pts',(-3.08472340505253,3.8348705229166,23.9862805043539));
#27494=CARTESIAN_POINT('Ctrl Pts',(-2.94194688341965,3.94546558139833,23.9761961129164));
#27495=CARTESIAN_POINT('Ctrl Pts',(-2.72468937698022,4.09539053348215,23.9613546417961));
#27496=CARTESIAN_POINT('Ctrl Pts',(-2.65476613328415,4.14105932982072,23.9566497862757));
#27497=CARTESIAN_POINT('Ctrl Pts',(-2.52677338651492,4.22008027152164,23.9481483585877));
#27498=CARTESIAN_POINT('Ctrl Pts',(-2.46912088535045,4.25406901290821,23.9443579139273));
#27499=CARTESIAN_POINT('Ctrl Pts',(-2.32298067850495,4.33625339992634,23.9348382281556));
#27500=CARTESIAN_POINT('Ctrl Pts',(-2.23367237938419,4.38292597379616,23.9290994079972));
#27501=CARTESIAN_POINT('Ctrl Pts',(-2.00697061889581,4.49267076134325,23.9147146020704));
#27502=CARTESIAN_POINT('Ctrl Pts',(-1.86798403862433,4.55221451091376,23.9060558570609));
#27503=CARTESIAN_POINT('Ctrl Pts',(-1.65123355061661,4.63347259059811,23.8928175669778));
#27504=CARTESIAN_POINT('Ctrl Pts',(-1.57530854822261,4.65983301047621,23.8882290463911));
#27505=CARTESIAN_POINT('Ctrl Pts',(-1.46498286364453,4.69513224505472,23.8816404530144));
#27506=CARTESIAN_POINT('Ctrl Pts',(-1.43107824495466,4.70557718933143,23.8796263111362));
#27507=CARTESIAN_POINT('Ctrl Pts',(-1.35609481771983,4.72779183585825,23.8751967505451));
#27508=CARTESIAN_POINT('Ctrl Pts',(-1.31496953878995,4.73939489460497,23.8727835443422));
#27509=CARTESIAN_POINT('Ctrl Pts',(-1.24767502016877,4.75743796427594,23.8688565960864));
#27510=CARTESIAN_POINT('Ctrl Pts',(-1.22159506721075,4.7642013435836,23.8673400220984));
#27511=CARTESIAN_POINT('Ctrl Pts',(-1.11817175512541,4.79011729165105,23.8613442359394));
#27512=CARTESIAN_POINT('Ctrl Pts',(-1.04042305655069,4.80760353522793,23.8568772516731));
#27513=CARTESIAN_POINT('Ctrl Pts',(-0.771537192694124,4.86124941311935,
23.8415133493799));
#27514=CARTESIAN_POINT('Ctrl Pts',(-0.578703172797429,4.88795632202422,
23.8306342908209));
#27515=CARTESIAN_POINT('Ctrl Pts',(-0.321709385304962,4.90812496302579,
23.816102948643));
#27516=CARTESIAN_POINT('Ctrl Pts',(-0.258532865706478,4.9118579204495,23.8125288830362));
#27517=CARTESIAN_POINT('Ctrl Pts',(-0.123602951670436,4.91722017990039,
23.8048844338932));
#27518=CARTESIAN_POINT('Ctrl Pts',(-0.0518503582946505,4.91850011356894,
23.8008125732088));
#27519=CARTESIAN_POINT('Ctrl Pts',(0.0598864713917693,4.91804791575499,
23.794456347513));
#27520=CARTESIAN_POINT('Ctrl Pts',(0.0998653794617415,4.91739855741258,
23.7921791006398));
#27521=CARTESIAN_POINT('Ctrl Pts',(0.321386503889912,4.91109789840972,23.7795426890686));
#27522=CARTESIAN_POINT('Ctrl Pts',(0.502514915989395,4.89588089161654,23.7691361681624));
#27523=CARTESIAN_POINT('Ctrl Pts',(0.761297277986533,4.85962540384258,23.7541911402653));
#27524=CARTESIAN_POINT('Ctrl Pts',(0.839930976755452,4.84665335834015,23.7496405674957));
#27525=CARTESIAN_POINT('Ctrl Pts',(0.953713289547652,4.82503053232281,23.7430513774998));
#27526=CARTESIAN_POINT('Ctrl Pts',(0.989136094779115,4.81789357476211,23.7409994147684));
#27527=CARTESIAN_POINT('Ctrl Pts',(1.06520524643603,4.80169291519703,23.7365932149715));
#27528=CARTESIAN_POINT('Ctrl Pts',(1.10582174120222,4.79250199762617,23.7342407882073));
#27529=CARTESIAN_POINT('Ctrl Pts',(1.17149689281986,4.77676130302535,23.7304332299061));
#27530=CARTESIAN_POINT('Ctrl Pts',(1.19662892648629,4.77052751149441,23.7289752823241));
#27531=CARTESIAN_POINT('Ctrl Pts',(1.37184094741916,4.72559592054621,23.7188005555667));
#27532=CARTESIAN_POINT('Ctrl Pts',(1.52006847974102,4.68002103336966,23.7101365849302));
#27533=CARTESIAN_POINT('Ctrl Pts',(1.7840260981573,4.58499693561589,23.6944121539718));
#27534=CARTESIAN_POINT('Ctrl Pts',(1.90048230307274,4.5379634727758,23.6873660977633));
#27535=CARTESIAN_POINT('Ctrl Pts',(2.07234468652241,4.46077581854696,23.6767441982816));
#27536=CARTESIAN_POINT('Ctrl Pts',(2.12918001775185,4.43392892917132,23.6731938069074));
#27537=CARTESIAN_POINT('Ctrl Pts',(2.25036205575529,4.37381965057869,23.6655349451547));
#27538=CARTESIAN_POINT('Ctrl Pts',(2.31452007068354,4.3402101787422,23.6614247018392));
#27539=CARTESIAN_POINT('Ctrl Pts',(2.53293709721332,4.21957074634783,23.6472282145625));
#27540=CARTESIAN_POINT('Ctrl Pts',(2.68322244101844,4.12563492453167,23.6370973052321));
#27541=CARTESIAN_POINT('Ctrl Pts',(2.83547195790068,4.01862697669044,23.6264448788333));
#27542=CARTESIAN_POINT('Ctrl Pts',(2.84281822078119,4.01343351327193,23.6259299073577));
#27543=CARTESIAN_POINT('Ctrl Pts',(2.9386852051657,3.94526477267804,23.6191969317627));
#27544=CARTESIAN_POINT('Ctrl Pts',(3.02511083142521,3.87939295830927,23.6129841521701));
#27545=CARTESIAN_POINT('Ctrl Pts',(3.14125222771581,3.78462940989133,23.6044530596793));
#27546=CARTESIAN_POINT('Ctrl Pts',(3.17289056748573,3.75814459969224,23.6021096300691));
#27547=CARTESIAN_POINT('Ctrl Pts',(3.23646205837304,3.70355311573759,23.5973632752029));
#27548=CARTESIAN_POINT('Ctrl Pts',(3.26837136175739,3.67542392582332,23.5949608627785));
#27549=CARTESIAN_POINT('Ctrl Pts',(3.31975080072493,3.62893283370501,23.5910551649576));
#27550=CARTESIAN_POINT('Ctrl Pts',(3.339442876036,3.61081987622443,23.5895490504008));
#27551=CARTESIAN_POINT('Ctrl Pts',(3.47124609185732,3.48758553047829,23.5794015412238));
#27552=CARTESIAN_POINT('Ctrl Pts',(3.57852518150923,3.37741919192519,23.5708103348311));
#27553=CARTESIAN_POINT('Ctrl Pts',(3.76283625345998,3.16948967793822,23.5552355975117));
#27554=CARTESIAN_POINT('Ctrl Pts',(3.84165295118343,3.073483943344,23.5482663935508));
#27555=CARTESIAN_POINT('Ctrl Pts',(3.9547215125295,2.92460291687742,23.5377259876296));
#27556=CARTESIAN_POINT('Ctrl Pts',(3.99173069379903,2.87388420528602,23.5341795139011));
#27557=CARTESIAN_POINT('Ctrl Pts',(4.06938876642955,2.7630636036435,23.5265175709376));
#27558=CARTESIAN_POINT('Ctrl Pts',(4.10969918976051,2.70274264674488,23.5224002764183));
#27559=CARTESIAN_POINT('Ctrl Pts',(4.19100506168466,2.57504864015972,23.5137870931857));
#27560=CARTESIAN_POINT('Ctrl Pts',(4.23174425468662,2.50753650371374,23.5092905842304));
#27561=CARTESIAN_POINT('Ctrl Pts',(4.35714970240799,2.28795039716937,23.4948421782815));
#27562=CARTESIAN_POINT('Ctrl Pts',(4.43537438191799,2.132351877021,23.4848645416041));
#27563=CARTESIAN_POINT('Ctrl Pts',(4.53009948837585,1.91604763835229,23.471381600174));
#27564=CARTESIAN_POINT('Ctrl Pts',(4.55393260056208,1.85869253245921,23.4678425476648));
#27565=CARTESIAN_POINT('Ctrl Pts',(4.5901345631387,1.76669160982141,23.4622280295423));
#27566=CARTESIAN_POINT('Ctrl Pts',(4.60321186606939,1.73233227490345,23.46014513598));
#27567=CARTESIAN_POINT('Ctrl Pts',(4.63616511915414,1.64274197553066,23.454749205338));
#27568=CARTESIAN_POINT('Ctrl Pts',(4.65543978121025,1.5872960579709,23.4514431548043));
#27569=CARTESIAN_POINT('Ctrl Pts',(4.68763389884376,1.4890496034675,23.445631338234));
#27570=CARTESIAN_POINT('Ctrl Pts',(4.70097081569815,1.44639334601556,23.4431231398826));
#27571=CARTESIAN_POINT('Ctrl Pts',(4.7652246568399,1.23060301940565,23.4304965113166));
#27572=CARTESIAN_POINT('Ctrl Pts',(4.80716615658716,1.05494221183952,23.4204122135255));
#27573=CARTESIAN_POINT('Ctrl Pts',(4.85425605322918,0.795207327790857,23.4055706064557));
#27574=CARTESIAN_POINT('Ctrl Pts',(4.86705781472965,0.712674206983198,23.4008655168694));
#27575=CARTESIAN_POINT('Ctrl Pts',(4.88632195994068,0.563488146704479,23.3923638794242));
#27576=CARTESIAN_POINT('Ctrl Pts',(4.8935364384407,0.496952896665293,23.3885734606663));
#27577=CARTESIAN_POINT('Ctrl Pts',(4.90820438091778,0.329940639013733,23.3790542855101));
#27578=CARTESIAN_POINT('Ctrl Pts',(4.9139324602483,0.229343531533057,23.3733159529812));
#27579=CARTESIAN_POINT('Ctrl Pts',(4.92051936296306,-0.0224000320528518,
23.3589333561474));
#27580=CARTESIAN_POINT('Ctrl Pts',(4.91750898769162,-0.173544246678037,
23.3502763392639));
#27581=CARTESIAN_POINT('Ctrl Pts',(4.90224722590296,-0.404490236563302,
23.3370398408738));
#27582=CARTESIAN_POINT('Ctrl Pts',(4.89498422490087,-0.48453057107198,23.3324514030228));
#27583=CARTESIAN_POINT('Ctrl Pts',(4.88169115623406,-0.599611490484468,
23.3258621569221));
#27584=CARTESIAN_POINT('Ctrl Pts',(4.87723747182906,-0.634820578031856,
23.3238472890544));
#27585=CARTESIAN_POINT('Ctrl Pts',(4.8665856149228,-0.712285944216729,23.3194183094497));
#27586=CARTESIAN_POINT('Ctrl Pts',(4.86021732393673,-0.754516026889388,
23.3170064016834));
#27587=CARTESIAN_POINT('Ctrl Pts',(4.84893936266278,-0.823222195517016,
23.3130820111139));
#27588=CARTESIAN_POINT('Ctrl Pts',(4.84436089359634,-0.849750121563693,
23.3115666967033));
#27589=CARTESIAN_POINT('Ctrl Pts',(4.82538841979017,-0.95453716599194,23.3055781944255));
#27590=CARTESIAN_POINT('Ctrl Pts',(4.80931385542178,-1.03248001900831,23.3011172095604));
#27591=CARTESIAN_POINT('Ctrl Pts',(4.74833253332805,-1.29570836995476,23.2859765806535));
#27592=CARTESIAN_POINT('Ctrl Pts',(4.69454966853988,-1.47875772149309,23.2753142299341));
#27593=CARTESIAN_POINT('Ctrl Pts',(4.60632854032987,-1.72509903637105,23.2605680546434));
#27594=CARTESIAN_POINT('Ctrl Pts',(4.58093203916142,-1.7914493593339,23.2565561602073));
#27595=CARTESIAN_POINT('Ctrl Pts',(4.52656720824242,-1.92475748393204,23.2484040448458));
#27596=CARTESIAN_POINT('Ctrl Pts',(4.49752840221002,-1.99166768470933,23.2442642583583));
#27597=CARTESIAN_POINT('Ctrl Pts',(4.43368498174905,-2.13024994013496,23.2355819738333));
#27598=CARTESIAN_POINT('Ctrl Pts',(4.39860502560117,-2.20177223577574,23.2310387574657));
#27599=CARTESIAN_POINT('Ctrl Pts',(4.28249288404842,-2.42464499236741,23.2166785295574));
#27600=CARTESIAN_POINT('Ctrl Pts',(4.19526652132877,-2.57262266417517,23.2068375171293));
#27601=CARTESIAN_POINT('Ctrl Pts',(4.06618769753098,-2.76751841958359,23.1934900134867));
#27602=CARTESIAN_POINT('Ctrl Pts',(4.03091451386379,-2.81864664509382,23.1899506528104));
#27603=CARTESIAN_POINT('Ctrl Pts',(3.97323641326655,-2.89895273549963,23.1843358224786));
#27604=CARTESIAN_POINT('Ctrl Pts',(3.95145650061225,-2.92857066242305,23.1822529229725));
#27605=CARTESIAN_POINT('Ctrl Pts',(3.89404838838512,-3.00483191117359,23.1768572476015));
#27606=CARTESIAN_POINT('Ctrl Pts',(3.85791368935393,-3.05108665115517,23.1735514565006));
#27607=CARTESIAN_POINT('Ctrl Pts',(3.79282483510735,-3.13139897259176,23.1677402345912));
#27608=CARTESIAN_POINT('Ctrl Pts',(3.76421825590976,-3.16572909572056,23.1652323711145));
#27609=CARTESIAN_POINT('Ctrl Pts',(3.61774591813145,-3.33671445362707,23.1526062195923));
#27610=CARTESIAN_POINT('Ctrl Pts',(3.49289063671655,-3.46719823189656,23.1425220718892));
#27611=CARTESIAN_POINT('Ctrl Pts',(3.30017937434332,-3.64759835310928,23.1276802471827));
#27612=CARTESIAN_POINT('Ctrl Pts',(3.23776745369198,-3.70310941466093,23.1229747827119));
#27613=CARTESIAN_POINT('Ctrl Pts',(3.12285485791498,-3.80018928904171,23.1144728092698));
#27614=CARTESIAN_POINT('Ctrl Pts',(3.07086110155305,-3.84232651648697,23.1106824319524));
#27615=CARTESIAN_POINT('Ctrl Pts',(2.93849395500464,-3.94519728383304,23.101164074049));
#27616=CARTESIAN_POINT('Ctrl Pts',(2.85708462695806,-4.00454683774597,23.0954265219999));
#27617=CARTESIAN_POINT('Ctrl Pts',(2.64918151914229,-4.14654498702786,23.0810474600151));
#27618=CARTESIAN_POINT('Ctrl Pts',(2.52059365296332,-4.22594431743793,23.0723932081582));
#27619=CARTESIAN_POINT('Ctrl Pts',(2.31831684224585,-4.33832301567438,23.0591596520405));
#27620=CARTESIAN_POINT('Ctrl Pts',(2.24713021611858,-4.37561945122382,23.0545714218355));
#27621=CARTESIAN_POINT('Ctrl Pts',(2.14321350561366,-4.4268589108072,23.0479811817797));
#27622=CARTESIAN_POINT('Ctrl Pts',(2.1111963325242,-4.44221724263565,23.0459651282934));
#27623=CARTESIAN_POINT('Ctrl Pts',(2.04034726338444,-4.47526386255296,23.0415370849775));
#27624=CARTESIAN_POINT('Ctrl Pts',(2.00144573507179,-4.49279630309929,23.0391272852502));
#27625=CARTESIAN_POINT('Ctrl Pts',(1.93767017584439,-4.52054643242715,23.0352070463384));
#27626=CARTESIAN_POINT('Ctrl Pts',(1.9129320222673,-4.53107016573018,23.033693776082));
#27627=CARTESIAN_POINT('Ctrl Pts',(1.8147959479843,-4.57187079203813,23.0277170828895));
#27628=CARTESIAN_POINT('Ctrl Pts',(1.74075538953395,-4.60057145273527,23.0232658226211));
#27629=CARTESIAN_POINT('Ctrl Pts',(1.48370490107368,-4.69311873618654,23.007956816658));
#27630=CARTESIAN_POINT('Ctrl Pts',(1.2976383096565,-4.74793401604108,22.9971170986894));
#27631=CARTESIAN_POINT('Ctrl Pts',(1.04696862063117,-4.8059412063301,22.9826144773261));
#27632=CARTESIAN_POINT('Ctrl Pts',(0.984841278992134,-4.81905610235706,
22.9790288368528));
#27633=CARTESIAN_POINT('Ctrl Pts',(0.860415936866699,-4.84281525631282,
22.971858305144));
#27634=CARTESIAN_POINT('Ctrl Pts',(0.798131820792461,-4.85346893238568,
22.9682741627323));
#27635=CARTESIAN_POINT('Ctrl Pts',(0.705729951494024,-4.86744744390977,
22.9629613243532));
#27636=CARTESIAN_POINT('Ctrl Pts',(0.675758631029433,-4.87169884588969,
22.9612387632728));
#27637=CARTESIAN_POINT('Ctrl Pts',(0.557159970118804,-4.88740643928316,
22.9544246404962));
#27638=CARTESIAN_POINT('Ctrl Pts',(0.468267178940948,-4.89672283928233,
22.9493217290823));
#27639=CARTESIAN_POINT('Ctrl Pts',(0.2139257255232,-4.91638973230299,22.9347315331563));
#27640=CARTESIAN_POINT('Ctrl Pts',(0.0481401655254922,-4.92080634360156,
22.9252307160508));
#27641=CARTESIAN_POINT('Ctrl Pts',(-0.167760106194562,-4.91564461031795,
22.9129164476526));
#27642=CARTESIAN_POINT('Ctrl Pts',(-0.21794760137163,-4.91367523468527,
22.9100583946967));
#27643=CARTESIAN_POINT('Ctrl Pts',(-0.304791773108721,-4.90893426256406,
22.9051238755183));
#27644=CARTESIAN_POINT('Ctrl Pts',(-0.341463338215585,-4.90651978849226,
22.9030440026842));
#27645=CARTESIAN_POINT('Ctrl Pts',(-0.418590724273965,-4.90057279488081,
22.89867524763));
#27646=CARTESIAN_POINT('Ctrl Pts',(-0.459036625533927,-4.89694979853538,
22.896387288996));
#27647=CARTESIAN_POINT('Ctrl Pts',(-0.536871489671071,-4.88900483651822,
22.8919857319605));
#27648=CARTESIAN_POINT('Ctrl Pts',(-0.574264778111661,-4.88475375777505,
22.8898717846808));
#27649=CARTESIAN_POINT('Ctrl Pts',(-0.757134858939948,-4.86183517300296,
22.8795283768062));
#27650=CARTESIAN_POINT('Ctrl Pts',(-0.901775472957081,-4.83709578108482,
22.8713287570633));
#27651=CARTESIAN_POINT('Ctrl Pts',(-1.15277484017265,-4.78251363791775,
22.856919624179));
#27652=CARTESIAN_POINT('Ctrl Pts',(-1.25963713659576,-4.75548529360846,
22.8507269206461));
#27653=CARTESIAN_POINT('Ctrl Pts',(-1.42964710344575,-4.70635216661582,
22.8407415713474));
#27654=CARTESIAN_POINT('Ctrl Pts',(-1.4934092709226,-4.68650938084254,22.8369660186691));
#27655=CARTESIAN_POINT('Ctrl Pts',(-1.6166334908108,-4.64539179256364,22.829602742714));
#27656=CARTESIAN_POINT('Ctrl Pts',(-1.6761290646742,-4.62425777839593,22.8260166909005));
#27657=CARTESIAN_POINT('Ctrl Pts',(-1.88808217620377,-4.54433981502277,
22.8131231209283));
#27658=CARTESIAN_POINT('Ctrl Pts',(-2.03799447773967,-4.4791133116889,22.803777682958));
#27659=CARTESIAN_POINT('Ctrl Pts',(-2.29152579983446,-4.35343471114599,
22.7875790851894));
#27660=CARTESIAN_POINT('Ctrl Pts',(-2.39669943443484,-4.29643067537482,
22.7807357706578));
#27661=CARTESIAN_POINT('Ctrl Pts',(-2.53645120613345,-4.21395541850418,
22.7714961598607));
#27662=CARTESIAN_POINT('Ctrl Pts',(-2.57292747797696,-4.19178353912988,
22.7690706409353));
#27663=CARTESIAN_POINT('Ctrl Pts',(-2.63730457530052,-4.15149537459055,
22.7647670691262));
#27664=CARTESIAN_POINT('Ctrl Pts',(-2.66531873635941,-4.13356569122878,
22.7628866298749));
#27665=CARTESIAN_POINT('Ctrl Pts',(-2.72970513775886,-4.09143025965455,
22.7585437853213));
#27666=CARTESIAN_POINT('Ctrl Pts',(-2.76594103862293,-4.06702125969586,
22.7560839473428));
#27667=CARTESIAN_POINT('Ctrl Pts',(-2.92534251259589,-3.95653043515634,
22.7451801263919));
#27668=CARTESIAN_POINT('Ctrl Pts',(-3.04485072135958,-3.86531324879298,
22.7367796378347));
#27669=CARTESIAN_POINT('Ctrl Pts',(-3.25457854607934,-3.68946293481423,
22.7214378998592));
#27670=CARTESIAN_POINT('Ctrl Pts',(-3.34614161669123,-3.60662640235896,
22.7145099320098));
#27671=CARTESIAN_POINT('Ctrl Pts',(-3.47940410689395,-3.47661721540432,
22.7040130174062));
#27672=CARTESIAN_POINT('Ctrl Pts',(-3.5234745644396,-3.4319450883633,22.7004684122164));
#27673=CARTESIAN_POINT('Ctrl Pts',(-3.61003285808672,-3.34077992829052,
22.6933505050603));
#27674=CARTESIAN_POINT('Ctrl Pts',(-3.65250658299013,-3.29428950127429,
22.6897778035394));
#27675=CARTESIAN_POINT('Ctrl Pts',(-3.83334312377685,-3.08855357988104,
22.6742021947446));
#27676=CARTESIAN_POINT('Ctrl Pts',(-3.96227107642496,-2.92131620382396,
22.6621260149102));
#27677=CARTESIAN_POINT('Ctrl Pts',(-4.13011525046187,-2.67195927118062,
22.6449263897562));
#27678=CARTESIAN_POINT('Ctrl Pts',(-4.17812756394652,-2.59624125284309,
22.6398030806088));
#27679=CARTESIAN_POINT('Ctrl Pts',(-4.24558769299956,-2.4831305166957,22.6323054232603));
#27680=CARTESIAN_POINT('Ctrl Pts',(-4.26666730757667,-2.44673295685174,
22.629915789141));
#27681=CARTESIAN_POINT('Ctrl Pts',(-4.30342916044187,-2.3813372136461,22.6256651581413));
#27682=CARTESIAN_POINT('Ctrl Pts',(-4.31929155749443,-2.35244339550757,
22.6238018171683));
#27683=CARTESIAN_POINT('Ctrl Pts',(-4.35569080675922,-2.28453159848305,
22.61945347387));
#27684=CARTESIAN_POINT('Ctrl Pts',(-4.37599585612377,-2.24539246989924,
22.6169711924386));
#27685=CARTESIAN_POINT('Ctrl Pts',(-4.45885387989294,-2.0802848570807,22.6065864823423));
#27686=CARTESIAN_POINT('Ctrl Pts',(-4.51651531885476,-1.95193566529595,
22.5987212159425));
#27687=CARTESIAN_POINT('Ctrl Pts',(-4.59309786003349,-1.75983309877459,
22.587131146069));
#27688=CARTESIAN_POINT('Ctrl Pts',(-4.61635581570514,-1.69788674781731,
22.5834209993106));
#27689=CARTESIAN_POINT('Ctrl Pts',(-4.66888749080919,-1.54890350032694,
22.574547255183));
#27690=CARTESIAN_POINT('Ctrl Pts',(-4.69698729231255,-1.46147957403543,
22.5693793727349));
#27691=CARTESIAN_POINT('Ctrl Pts',(-4.74013326567671,-1.3131077424678,22.5606524284325));
#27692=CARTESIAN_POINT('Ctrl Pts',(-4.75648980741909,-1.25256533697481,
22.5571035667272));
#27693=CARTESIAN_POINT('Ctrl Pts',(-4.78723653981814,-1.12945520095368,
22.5499059326125));
#27694=CARTESIAN_POINT('Ctrl Pts',(-4.80156835113523,-1.06688518485319,
22.5462574622833));
#27695=CARTESIAN_POINT('Ctrl Pts',(-4.84640628900657,-0.851876690113653,
22.5337472436324));
#27696=CARTESIAN_POINT('Ctrl Pts',(-4.87090836043322,-0.698282660932549,
22.5248535705399));
#27697=CARTESIAN_POINT('Ctrl Pts',(-4.90112114811131,-0.426700947045144,
22.509211331776));
#27698=CARTESIAN_POINT('Ctrl Pts',(-4.90993574011038,-0.309182287191449,
22.5024706214595));
#27699=CARTESIAN_POINT('Ctrl Pts',(-4.9158821497358,-0.156545822731047,
22.4937744193805));
#27700=CARTESIAN_POINT('Ctrl Pts',(-4.91687024323224,-0.121618032780329,
22.4917885365338));
#27701=CARTESIAN_POINT('Ctrl Pts',(-4.91799513852044,-0.0578028651488844,
22.4881688539813));
#27702=CARTESIAN_POINT('Ctrl Pts',(-4.91824979373262,-0.028919407406132,
22.4865339698279));
#27703=CARTESIAN_POINT('Ctrl Pts',(-4.91824999987475,-3.51006693910429E-5,
22.4849018564489));
#27704=CARTESIAN_POINT('Ctrl Pts',(-4.76363197251275,1.2218451209039,22.4152102246213));
#27705=CARTESIAN_POINT('Ctrl Pts',(-4.86586003699209,0.823026811626357,
22.4385203361033));
#27706=CARTESIAN_POINT('Ctrl Pts',(-4.91856347066883,0.411490142340121,
22.4618304475853));
#27707=CARTESIAN_POINT('Ctrl Pts',(-4.9186648078212,-2.15352476078406E-5,
22.4851405590673));
#27708=CARTESIAN_POINT('',(-4.9182499983453,0.000127579104957042,22.1398594359908));
#27709=CARTESIAN_POINT('Ctrl Pts',(-4.76399535256163,1.22193798731013,22.0699206410069));
#27710=CARTESIAN_POINT('Ctrl Pts',(-4.81429942686512,1.02666089548625,22.0813401895013));
#27711=CARTESIAN_POINT('Ctrl Pts',(-4.89251683443142,0.621776568813317,
22.1046531201869));
#27712=CARTESIAN_POINT('Ctrl Pts',(-4.91839361835249,0.210150187564921,
22.1279660508726));
#27713=CARTESIAN_POINT('Ctrl Pts',(-4.91818349699392,0.000127629067394636,
22.1398594330638));
#27714=CARTESIAN_POINT('Ctrl Pts',(-4.9182499983453,0.000127579104957042,
22.1398594359908));
#27715=CARTESIAN_POINT('Ctrl Pts',(-4.91825372288393,-0.143455589280298,
22.1479903075752));
#27716=CARTESIAN_POINT('Ctrl Pts',(-4.91196546422664,-0.287055776384316,
22.1561211791597));
#27717=CARTESIAN_POINT('Ctrl Pts',(-4.89940681158052,-0.430111563595313,
22.1642520507441));
#27718=CARTESIAN_POINT('Ctrl Pts',(-4.88684771079342,-0.573172455586439,
22.1723832124693));
#27719=CARTESIAN_POINT('Ctrl Pts',(-4.86801779513648,-0.715688571369777,
22.1805143741945));
#27720=CARTESIAN_POINT('Ctrl Pts',(-4.84299060350325,-0.857102722478036,
22.1886455359196));
#27721=CARTESIAN_POINT('Ctrl Pts',(-4.81796399284641,-0.998513590825499,
22.1967765088896));
#27722=CARTESIAN_POINT('Ctrl Pts',(-4.78674045548509,-1.13882221279591,
22.2049074818596));
#27723=CARTESIAN_POINT('Ctrl Pts',(-4.74944480663373,-1.27748075963587,
22.2130384548295));
#27724=CARTESIAN_POINT('Ctrl Pts',(-4.71214071757721,-1.4161706856479,22.2211712678822));
#27725=CARTESIAN_POINT('Ctrl Pts',(-4.66876186166881,-1.55320946412703,
22.229304080935));
#27726=CARTESIAN_POINT('Ctrl Pts',(-4.61948328533162,-1.68806316204158,
22.2374368939877));
#27727=CARTESIAN_POINT('Ctrl Pts',(-4.60784474256061,-1.71991271305675,
22.2393576899927));
#27728=CARTESIAN_POINT('Ctrl Pts',(-4.59587732787198,-1.75164045437253,
22.2412784859977));
#27729=CARTESIAN_POINT('Ctrl Pts',(-4.58358374572119,-1.78323949834577,
22.2431992820028));
#27730=CARTESIAN_POINT('Ctrl Pts',(-4.53138139485292,-1.91741880917317,
22.2513555757316));
#27731=CARTESIAN_POINT('Ctrl Pts',(-4.4732732995595,-2.04932941321032,22.2595118694605));
#27732=CARTESIAN_POINT('Ctrl Pts',(-4.40948182443103,-2.17845199683454,
22.2676681631893));
#27733=CARTESIAN_POINT('Ctrl Pts',(-4.34570335099645,-2.30754826326978,
22.2758227945388));
#27734=CARTESIAN_POINT('Ctrl Pts',(-4.27624395672583,-2.43385734304699,
22.2839774258882));
#27735=CARTESIAN_POINT('Ctrl Pts',(-4.20137293026017,-2.55688258693611,
22.2921320572376));
#27736=CARTESIAN_POINT('Ctrl Pts',(-4.12649924762621,-2.67991219534067,
22.3002869778855));
#27737=CARTESIAN_POINT('Ctrl Pts',(-4.04621371938924,-2.79965744692355,
22.3084418985335));
#27738=CARTESIAN_POINT('Ctrl Pts',(-3.96083038422565,-2.91564842357492,
22.3165968191814));
#27739=CARTESIAN_POINT('Ctrl Pts',(-3.87545206900655,-3.03163258076598,
22.3247512603768));
#27740=CARTESIAN_POINT('Ctrl Pts',(-3.78497674564009,-3.14386263566029,
22.3329057015723));
#27741=CARTESIAN_POINT('Ctrl Pts',(-3.6897603353316,-3.25189971098644,22.3410601427678));
#27742=CARTESIAN_POINT('Ctrl Pts',(-3.59452045517901,-3.35996341631582,
22.3492165939472));
#27743=CARTESIAN_POINT('Ctrl Pts',(-3.49453737409855,-3.46383182553087,
22.3573730451267));
#27744=CARTESIAN_POINT('Ctrl Pts',(-3.390206064975,-3.5631006019346,22.3655294963062));
#27745=CARTESIAN_POINT('Ctrl Pts',(-3.3190449401094,-3.63080873147178,22.3710927567092));
#27746=CARTESIAN_POINT('Ctrl Pts',(-3.2458617485111,-3.69637775720605,22.3766560171123));
#27747=CARTESIAN_POINT('Ctrl Pts',(-3.17079131872694,-3.75968954510687,
22.3822192775153));
#27748=CARTESIAN_POINT('Ctrl Pts',(-3.06073059330498,-3.85251093062657,
22.3903755712441));
#27749=CARTESIAN_POINT('Ctrl Pts',(-2.94657060164346,-3.94051351297408,
22.398531864973));
#27750=CARTESIAN_POINT('Ctrl Pts',(-2.82875515750392,-4.02334777534766,
22.4066881587018));
#27751=CARTESIAN_POINT('Ctrl Pts',(-2.71096372598283,-4.10616515481127,
22.4148427900512));
#27752=CARTESIAN_POINT('Ctrl Pts',(-2.58951860188466,-4.18381612337722,
22.4229974214006));
#27753=CARTESIAN_POINT('Ctrl Pts',(-2.46489394941216,-4.25599352450768,
22.43115205275));
#27754=CARTESIAN_POINT('Ctrl Pts',(-2.34026487568228,-4.32817348624603,
22.4393069733979));
#27755=CARTESIAN_POINT('Ctrl Pts',(-2.2124563355605,-4.39487932101967,22.4474618940458));
#27756=CARTESIAN_POINT('Ctrl Pts',(-2.08196898830354,-4.45584876249658,
22.4556168146937));
#27757=CARTESIAN_POINT('Ctrl Pts',(-1.95148931279198,-4.51681461939581,
22.4637712558892));
#27758=CARTESIAN_POINT('Ctrl Pts',(-1.81833144883585,-4.57204461692049,
22.4719256970847));
#27759=CARTESIAN_POINT('Ctrl Pts',(-1.6830179701643,-4.62132379027958,22.4800801382801));
#27760=CARTESIAN_POINT('Ctrl Pts',(-1.5476711381433,-4.67061511043665,22.4882365894596));
#27761=CARTESIAN_POINT('Ctrl Pts',(-1.41016794418998,-4.71395256061313,
22.4963930406391));
#27762=CARTESIAN_POINT('Ctrl Pts',(-1.27104871582113,-4.75117019527921,
22.5045494918186));
#27763=CARTESIAN_POINT('Ctrl Pts',(-1.1761598386047,-4.7765551805722,22.5101127522216));
#27764=CARTESIAN_POINT('Ctrl Pts',(-1.0805195132734,-4.79909414325774,22.5156760126247));
#27765=CARTESIAN_POINT('Ctrl Pts',(-0.984302665699794,-4.81874790010811,
22.5212392730278));
#27766=CARTESIAN_POINT('Ctrl Pts',(-0.843239186082988,-4.84756226473104,
22.5293955667566));
#27767=CARTESIAN_POINT('Ctrl Pts',(-0.700883169296038,-4.87018355294729,
22.5375518604854));
#27768=CARTESIAN_POINT('Ctrl Pts',(-0.557791584474612,-4.88651732942689,
22.5457081542143));
#27769=CARTESIAN_POINT('Ctrl Pts',(-0.414729163941527,-4.90284777682904,
22.5538627855637));
#27770=CARTESIAN_POINT('Ctrl Pts',(-0.270931806748138,-4.91289323106356,
22.5620174169132));
#27771=CARTESIAN_POINT('Ctrl Pts',(-0.126962853132465,-4.91661097672212,
22.5701720482626));
#27772=CARTESIAN_POINT('Ctrl Pts',(0.0170112080101646,-4.92032885427361,
22.5783269689105));
#27773=CARTESIAN_POINT('Ctrl Pts',(0.161156543326358,-4.9177185616535,22.5864818895584));
#27774=CARTESIAN_POINT('Ctrl Pts',(0.304908037492154,-4.90878947920693,
22.5946368102063));
#27775=CARTESIAN_POINT('Ctrl Pts',(0.44865108007284,-4.89986092172813,22.6027912514018));
#27776=CARTESIAN_POINT('Ctrl Pts',(0.591999993866124,-4.88461433935163,
22.6109456925973));
#27777=CARTESIAN_POINT('Ctrl Pts',(0.734393064423372,-4.86311113274484,
22.6191001337927));
#27778=CARTESIAN_POINT('Ctrl Pts',(0.876821233375318,-4.84160262582372,
22.6272565849722));
#27779=CARTESIAN_POINT('Ctrl Pts',(1.01829275721281,-4.81383446278952,22.6354130361517));
#27780=CARTESIAN_POINT('Ctrl Pts',(1.15825379764511,-4.77991958120016,22.6435694873312));
#27781=CARTESIAN_POINT('Ctrl Pts',(1.25371684855673,-4.75678730054672,22.6491327477342));
#27782=CARTESIAN_POINT('Ctrl Pts',(1.34847737014033,-4.7307965287713,22.6546960081373));
#27783=CARTESIAN_POINT('Ctrl Pts',(1.4423630223874,-4.70199659444256,22.6602592685403));
#27784=CARTESIAN_POINT('Ctrl Pts',(1.58000873752081,-4.6597730228787,22.6684155622691));
#27785=CARTESIAN_POINT('Ctrl Pts',(1.71582487225093,-4.61149325752146,22.676571855998));
#27786=CARTESIAN_POINT('Ctrl Pts',(1.84927720660251,-4.55734098742243,22.6847281497268));
#27787=CARTESIAN_POINT('Ctrl Pts',(1.9827023412946,-4.50319975439753,22.6928827810762));
#27788=CARTESIAN_POINT('Ctrl Pts',(2.11376432682064,-4.44318853014346,22.7010374124256));
#27789=CARTESIAN_POINT('Ctrl Pts',(2.24194810603734,-4.37753946325279,22.7091920437751));
#27790=CARTESIAN_POINT('Ctrl Pts',(2.3701364327771,-4.31188806735727,22.717346964423));
#27791=CARTESIAN_POINT('Ctrl Pts',(2.49544604932357,-4.24059857779578,22.7255018850709));
#27792=CARTESIAN_POINT('Ctrl Pts',(2.61738527654948,-4.16394973271797,22.7336568057188));
#27793=CARTESIAN_POINT('Ctrl Pts',(2.7393173345993,-4.08730539405764,22.7418112469143));
#27794=CARTESIAN_POINT('Ctrl Pts',(2.85787911693075,-4.00530250916809,22.7499656881097));
#27795=CARTESIAN_POINT('Ctrl Pts',(2.9726068308012,-3.91826386196413,22.7581201293052));
#27796=CARTESIAN_POINT('Ctrl Pts',(3.08736282384696,-3.8312037606487,22.7662765804847));
#27797=CARTESIAN_POINT('Ctrl Pts',(3.19828259312217,-3.73910561886982,22.7744330316642));
#27798=CARTESIAN_POINT('Ctrl Pts',(3.30493393014768,-3.64233369968467,22.7825894828436));
#27799=CARTESIAN_POINT('Ctrl Pts',(3.37767747352875,-3.57632859841125,22.7881527432467));
#27800=CARTESIAN_POINT('Ctrl Pts',(3.44843593242285,-3.50815003019972,22.7937160036498));
#27801=CARTESIAN_POINT('Ctrl Pts',(3.51708160490553,-3.43792379888432,22.7992792640529));
#27802=CARTESIAN_POINT('Ctrl Pts',(3.61772299635861,-3.33496515079369,22.8074355577817));
#27803=CARTESIAN_POINT('Ctrl Pts',(3.71385912080785,-3.22756494701395,22.8155918515106));
#27804=CARTESIAN_POINT('Ctrl Pts',(3.80510886101175,-3.11614017950891,22.8237481452394));
#27805=CARTESIAN_POINT('Ctrl Pts',(3.89634000310112,-3.00473812210237,22.8319027765889));
#27806=CARTESIAN_POINT('Ctrl Pts',(3.98268653584365,-2.88931339611125,22.8400574079384));
#27807=CARTESIAN_POINT('Ctrl Pts',(4.06380736289325,-2.77031636817793,22.8482120392878));
#27808=CARTESIAN_POINT('Ctrl Pts',(4.14493106783251,-2.65131511863683,22.8563669599358));
#27809=CARTESIAN_POINT('Ctrl Pts',(4.22082850451108,-2.52874158794351,22.8645218805837));
#27810=CARTESIAN_POINT('Ctrl Pts',(4.2912014032943,-2.40307585790899,22.8726768012316));
#27811=CARTESIAN_POINT('Ctrl Pts',(4.36157016464185,-2.27741751614301,22.8808312424271));
#27812=CARTESIAN_POINT('Ctrl Pts',(4.42641487521565,-2.14866763120932,22.8889856836225));
#27813=CARTESIAN_POINT('Ctrl Pts',(4.48548283279364,-2.01733160863889,22.897140124818));
#27814=CARTESIAN_POINT('Ctrl Pts',(4.54456535000215,-1.8859632131197,22.9052965759975));
#27815=CARTESIAN_POINT('Ctrl Pts',(4.59786813138542,-1.7520077114335,22.9134530271769));
#27816=CARTESIAN_POINT('Ctrl Pts',(4.64518606029957,-1.61599180929191,22.9216094783564));
#27817=CARTESIAN_POINT('Ctrl Pts',(4.67746014059345,-1.52321961389581,22.9271727387594));
#27818=CARTESIAN_POINT('Ctrl Pts',(4.70695095634588,-1.42948931754304,22.9327359991624));
#27819=CARTESIAN_POINT('Ctrl Pts',(4.73360660391814,-1.33497250227958,22.9382992595654));
#27820=CARTESIAN_POINT('Ctrl Pts',(4.77268643757363,-1.19640143931329,22.9464555532942));
#27821=CARTESIAN_POINT('Ctrl Pts',(4.80568463565858,-1.05608723077017,22.954611847023));
#27822=CARTESIAN_POINT('Ctrl Pts',(4.83246617905403,-0.914578422443352,
22.9627681407518));
#27823=CARTESIAN_POINT('Ctrl Pts',(4.85924226395468,-0.77309845581107,22.9709227721012));
#27824=CARTESIAN_POINT('Ctrl Pts',(4.87980415966228,-0.630424703735813,
22.9790774034506));
#27825=CARTESIAN_POINT('Ctrl Pts',(4.89406796062614,-0.487115858161732,
22.9872320348));
#27826=CARTESIAN_POINT('Ctrl Pts',(4.90833226762104,-0.34380192847831,22.9953869554479));
#27827=CARTESIAN_POINT('Ctrl Pts',(4.91629799589111,-0.199853192832361,
23.0035418760958));
#27828=CARTESIAN_POINT('Ctrl Pts',(4.91793306526228,-0.0558339332302211,
23.0116967967437));
#27829=CARTESIAN_POINT('Ctrl Pts',(4.91956803850278,0.0881768590439297,
23.0198512379392));
#27830=CARTESIAN_POINT('Ctrl Pts',(4.91487309462416,0.232257832325536,23.0280056791346));
#27831=CARTESIAN_POINT('Ctrl Pts',(4.90386828311162,0.375844282106113,23.0361601203301));
#27832=CARTESIAN_POINT('Ctrl Pts',(4.89286075902875,0.519466124436981,23.0443165715095));
#27833=CARTESIAN_POINT('Ctrl Pts',(4.8755402847948,0.662592865849866,23.052473022689));
#27834=CARTESIAN_POINT('Ctrl Pts',(4.85197888555946,0.804663878016858,23.0606294738685));
#27835=CARTESIAN_POINT('Ctrl Pts',(4.83590839160025,0.901566074699,23.0661927342716));
#27836=CARTESIAN_POINT('Ctrl Pts',(4.81693558990863,0.997977222729638,23.0717559946748));
#27837=CARTESIAN_POINT('Ctrl Pts',(4.79509703999832,1.09372182912263,23.0773192550779));
#27838=CARTESIAN_POINT('Ctrl Pts',(4.76307955119264,1.23409295614259,23.0854755488067));
#27839=CARTESIAN_POINT('Ctrl Pts',(4.72488802171999,1.37308347838278,23.0936318425356));
#27840=CARTESIAN_POINT('Ctrl Pts',(4.68066647623451,1.51014714539823,23.1017881362644));
#27841=CARTESIAN_POINT('Ctrl Pts',(4.6364539437873,1.64718287670805,23.1099427676138));
#27842=CARTESIAN_POINT('Ctrl Pts',(4.58621394982244,1.78229221795751,23.1180973989632));
#27843=CARTESIAN_POINT('Ctrl Pts',(4.53014025315144,1.91494447681311,23.1262520303126));
#27844=CARTESIAN_POINT('Ctrl Pts',(4.47406456717687,2.04760144171856,23.1344069509606));
#27845=CARTESIAN_POINT('Ctrl Pts',(4.41215489119676,2.17780084010838,23.1425618716085));
#27846=CARTESIAN_POINT('Ctrl Pts',(4.3446531622943,2.3050318787093,23.1507167922564));
#27847=CARTESIAN_POINT('Ctrl Pts',(4.27715540202295,2.43225543701207,23.1588712334519));
#27848=CARTESIAN_POINT('Ctrl Pts',(4.20406640426756,2.55651068948397,23.1670256746473));
#27849=CARTESIAN_POINT('Ctrl Pts',(4.12567407799985,2.67731142466095,23.1751801158427));
#27850=CARTESIAN_POINT('Ctrl Pts',(4.04726242884778,2.7981419359493,23.1833365670222));
#27851=CARTESIAN_POINT('Ctrl Pts',(3.96354502113518,2.91551594747252,23.1914930182017));
#27852=CARTESIAN_POINT('Ctrl Pts',(3.87485344714308,3.02897570569052,23.1996494693812));
#27853=CARTESIAN_POINT('Ctrl Pts',(3.81435969675836,3.10636306035582,23.2052127297842));
#27854=CARTESIAN_POINT('Ctrl Pts',(3.75155277972171,3.18193003621664,23.2107759901873));
#27855=CARTESIAN_POINT('Ctrl Pts',(3.68654879791111,3.2555400509163,23.2163392505904));
#27856=CARTESIAN_POINT('Ctrl Pts',(3.59124648761512,3.36345966239857,23.2244955443192));
#27857=CARTESIAN_POINT('Ctrl Pts',(3.49118424254412,3.46721179638804,23.232651838048));
#27858=CARTESIAN_POINT('Ctrl Pts',(3.38674998805847,3.56638578688369,23.2408081317769));
#27859=CARTESIAN_POINT('Ctrl Pts',(3.28233701889694,3.66553956417875,23.2489627631263));
#27860=CARTESIAN_POINT('Ctrl Pts',(3.1735540604992,3.76011682914599,23.2571173944757));
#27861=CARTESIAN_POINT('Ctrl Pts',(3.06082525747466,3.84974438186553,23.2652720258251));
#27862=CARTESIAN_POINT('Ctrl Pts',(2.94809245521654,3.93937511426505,23.273426946473));
#27863=CARTESIAN_POINT('Ctrl Pts',(2.83141378781708,4.02405557183889,23.281581867121));
#27864=CARTESIAN_POINT('Ctrl Pts',(2.71124617520242,4.10345308733392,23.2897367877689));
#27865=CARTESIAN_POINT('Ctrl Pts',(2.59108562760575,4.18284593480847,23.2978912289643));
#27866=CARTESIAN_POINT('Ctrl Pts',(2.46743682491781,4.25695627790285,23.3060456701598));
#27867=CARTESIAN_POINT('Ctrl Pts',(2.34078528370626,4.32549503734361,23.3142001113552));
#27868=CARTESIAN_POINT('Ctrl Pts',(2.21410252422082,4.39405069086828,23.3223565625347));
#27869=CARTESIAN_POINT('Ctrl Pts',(2.084415841582,4.45703185695303,23.3305130137142));
#27870=CARTESIAN_POINT('Ctrl Pts',(1.9522354842652,4.51419535205066,23.3386694648937));
#27871=CARTESIAN_POINT('Ctrl Pts',(1.86207939410505,4.55318478529557,23.3442327252968));
#27872=CARTESIAN_POINT('Ctrl Pts',(1.77076370792075,4.58946869529863,23.3497959856998));
#27873=CARTESIAN_POINT('Ctrl Pts',(1.67845574024884,4.62298273742459,23.3553592461029));
#27874=CARTESIAN_POINT('Ctrl Pts',(1.54312306780585,4.67211766044005,23.3635155398318));
#27875=CARTESIAN_POINT('Ctrl Pts',(1.40560602530865,4.71531512817721,23.3716718335606));
#27876=CARTESIAN_POINT('Ctrl Pts',(1.26644178220433,4.75240026458074,23.3798281272894));
#27877=CARTESIAN_POINT('Ctrl Pts',(1.1273059029359,4.78947784245703,23.3879827586388));
#27878=CARTESIAN_POINT('Ctrl Pts',(0.986523815983789,4.82044548815092,23.3961373899882));
#27879=CARTESIAN_POINT('Ctrl Pts',(0.844646557374703,4.8451785576607,23.4042920213376));
#27880=CARTESIAN_POINT('Ctrl Pts',(0.702764265444423,4.86991250461543,23.4124469419856));
#27881=CARTESIAN_POINT('Ctrl Pts',(0.559787053133157,4.88841137162501,23.4206018626335));
#27882=CARTESIAN_POINT('Ctrl Pts',(0.416275331412915,4.90060179069439,23.4287567832814));
#27883=CARTESIAN_POINT('Ctrl Pts',(0.272772047180556,4.91279149305219,23.4369112244768));
#27884=CARTESIAN_POINT('Ctrl Pts',(0.128734649953469,4.91867346210729,23.4450656656723));
#27885=CARTESIAN_POINT('Ctrl Pts',(-0.0152722056911815,4.91822628822966,
23.4532201068678));
#27886=CARTESIAN_POINT('Ctrl Pts',(-0.159314557511585,4.91777900412838,
23.4613765580473));
#27887=CARTESIAN_POINT('Ctrl Pts',(-0.303326017902509,4.91099946053709,
23.4695330092268));
#27888=CARTESIAN_POINT('Ctrl Pts',(-0.44674218654659,4.89791838246204,23.4776894604063));
#27889=CARTESIAN_POINT('Ctrl Pts',(-0.544561872414483,4.88899618798277,
23.4832527208093));
#27890=CARTESIAN_POINT('Ctrl Pts',(-0.642104633784729,4.8771434932435,23.4888159812124));
#27891=CARTESIAN_POINT('Ctrl Pts',(-0.739192769430403,4.86238389189108,
23.4943792416154));
#27892=CARTESIAN_POINT('Ctrl Pts',(-0.881533644123139,4.84074484657778,
23.5025355353443));
#27893=CARTESIAN_POINT('Ctrl Pts',(-1.02295032191188,4.8128471506273,23.5106918290731));
#27894=CARTESIAN_POINT('Ctrl Pts',(-1.16288746252878,4.77879438896396,23.518848122802));
#27895=CARTESIAN_POINT('Ctrl Pts',(-1.30279608178157,4.74474856778267,23.5270027541514));
#27896=CARTESIAN_POINT('Ctrl Pts',(-1.44122544047467,4.70455026261454,23.5351573855009));
#27897=CARTESIAN_POINT('Ctrl Pts',(-1.57763206797674,4.65835379942222,23.5433120168503));
#27898=CARTESIAN_POINT('Ctrl Pts',(-1.71404353472009,4.61215569733716,23.5514669374982));
#27899=CARTESIAN_POINT('Ctrl Pts',(-1.84843180851907,4.55995911520521,23.5596218581461));
#27900=CARTESIAN_POINT('Ctrl Pts',(-1.98026973172354,4.50196788661576,23.567776778794));
#27901=CARTESIAN_POINT('Ctrl Pts',(-2.11209990377826,4.44398006750581,23.5759312199895));
#27902=CARTESIAN_POINT('Ctrl Pts',(-2.24137971926182,4.380198419138,23.584085661185));
#27903=CARTESIAN_POINT('Ctrl Pts',(-2.36760316542589,4.31087442563169,23.5922401023805));
#27904=CARTESIAN_POINT('Ctrl Pts',(-2.49385772434203,4.24153334449001,23.60039655356));
#27905=CARTESIAN_POINT('Ctrl Pts',(-2.61705411498013,4.16664734934428,23.6085530047395));
#27906=CARTESIAN_POINT('Ctrl Pts',(-2.73671150297794,4.0865135766284,23.616709455919));
#27907=CARTESIAN_POINT('Ctrl Pts',(-2.81832606719533,4.03185683500354,23.622272716322));
#27908=CARTESIAN_POINT('Ctrl Pts',(-2.89829475799206,3.97475967955432,23.627835976725));
#27909=CARTESIAN_POINT('Ctrl Pts',(-2.97647284784729,3.91532788518763,23.633399237128));
#27910=CARTESIAN_POINT('Ctrl Pts',(-3.0910897123887,3.82819495655002,23.6415555308568));
#27911=CARTESIAN_POINT('Ctrl Pts',(-3.20189932385839,3.73600933835503,23.6497118245856));
#27912=CARTESIAN_POINT('Ctrl Pts',(-3.30846367824667,3.63912780102904,23.6578681183145));
#27913=CARTESIAN_POINT('Ctrl Pts',(-3.41500631316333,3.54226600966608,23.6660227496639));
#27914=CARTESIAN_POINT('Ctrl Pts',(-3.51730516965091,3.44071043351294,23.6741773810133));
#27915=CARTESIAN_POINT('Ctrl Pts',(-3.61495695327442,3.3348567118353,23.6823320123627));
#27916=CARTESIAN_POINT('Ctrl Pts',(-3.71261220125015,3.22899923482864,23.6904869330107));
#27917=CARTESIAN_POINT('Ctrl Pts',(-3.80561981680225,3.11884355058895,23.6986418536586));
#27918=CARTESIAN_POINT('Ctrl Pts',(-3.89361452591695,3.00482095740636,23.7067967743065));
#27919=CARTESIAN_POINT('Ctrl Pts',(-3.98160406155576,2.89080506795794,23.7149512155019));
#27920=CARTESIAN_POINT('Ctrl Pts',(-4.06458107667659,2.77292298992585,23.7231056566973));
#27921=CARTESIAN_POINT('Ctrl Pts',(-4.14222167116401,2.65163773721811,23.7312600978927));
#27922=CARTESIAN_POINT('Ctrl Pts',(-4.21988140324229,2.5303225889698,23.7394165490722));
#27923=CARTESIAN_POINT('Ctrl Pts',(-4.29220190557602,2.40560287169386,23.7475730002516));
#27924=CARTESIAN_POINT('Ctrl Pts',(-4.35890323685217,2.27796962979308,23.7557294514311));
#27925=CARTESIAN_POINT('Ctrl Pts',(-4.40439813003045,2.19091498492802,23.7612927118343));
#27926=CARTESIAN_POINT('Ctrl Pts',(-4.44727980599316,2.10250549146035,23.7668559722374));
#27927=CARTESIAN_POINT('Ctrl Pts',(-4.48747182549699,2.01290329570766,23.7724192326405));
#27928=CARTESIAN_POINT('Ctrl Pts',(-4.54616430584186,1.88205704369058,23.7805432720865));
#27929=CARTESIAN_POINT('Ctrl Pts',(-4.59914265290002,1.74861370798986,23.7886673115325));
#27930=CARTESIAN_POINT('Ctrl Pts',(-4.64619388201968,1.61309189855472,23.7967913509785));
#27931=CARTESIAN_POINT('Ctrl Pts',(-4.69086320095292,1.48443071283582,23.8045041209918));
#27932=CARTESIAN_POINT('Ctrl Pts',(-4.73019058037801,1.35389656612923,23.812216891005));
#27933=CARTESIAN_POINT('Ctrl Pts',(-4.76403458704968,1.22194824599669,23.8199296610182));
#27934=CARTESIAN_POINT('Origin',(0.,0.,-3.23514056400928));
#27935=CARTESIAN_POINT('',(-4.76403457790609,1.221948281645,25.9153493127618));
#27936=CARTESIAN_POINT('',(-4.76438990516231,1.22203958206317,25.569924562744));
#27937=CARTESIAN_POINT('',(-4.76403458704967,1.22194824599672,-3.23514056400928));
#27938=CARTESIAN_POINT('Ctrl Pts',(-4.76403457790609,1.221948281645,25.9153493127618));
#27939=CARTESIAN_POINT('Ctrl Pts',(-4.74875002836548,1.28153846529919,25.9118945228887));
#27940=CARTESIAN_POINT('Ctrl Pts',(-4.73234658248963,1.34084513057762,25.9084346143025));
#27941=CARTESIAN_POINT('Ctrl Pts',(-4.69614720705212,1.46276932404858,25.9012681232217));
#27942=CARTESIAN_POINT('Ctrl Pts',(-4.67620448887776,1.52532099721689,25.8975618007853));
#27943=CARTESIAN_POINT('Ctrl Pts',(-4.63222091208789,1.6542974654206,25.8898497389304));
#27944=CARTESIAN_POINT('Ctrl Pts',(-4.60798912151711,1.72064138763471,25.8858434768254));
#27945=CARTESIAN_POINT('Ctrl Pts',(-4.51839064989085,1.95046742754488,25.8718161362204));
#27946=CARTESIAN_POINT('Ctrl Pts',(-4.44568366032193,2.11094114988293,25.8617495733547));
#27947=CARTESIAN_POINT('Ctrl Pts',(-4.32332118104867,2.34650144285512,25.8465541938121));
#27948=CARTESIAN_POINT('Ctrl Pts',(-4.27995581230672,2.42469656592521,25.8414376007671));
#27949=CARTESIAN_POINT('Ctrl Pts',(-4.20461684436959,2.5522201961594,25.8329825919278));
#27950=CARTESIAN_POINT('Ctrl Pts',(-4.17384733280937,2.60223544202071,25.8296373223592));
#27951=CARTESIAN_POINT('Ctrl Pts',(-4.13451793790827,2.66367170302817,25.8254950832103));
#27952=CARTESIAN_POINT('Ctrl Pts',(-4.12679446771772,2.6756219732771,25.8246877781314));
#27953=CARTESIAN_POINT('Ctrl Pts',(-4.09767138862207,2.72025706171964,25.8216666892418));
#27954=CARTESIAN_POINT('Ctrl Pts',(-4.07593448720148,2.75271999618634,25.8194581497318));
#27955=CARTESIAN_POINT('Ctrl Pts',(-3.94719896339505,2.94011122106081,25.8066314063624));
#27956=CARTESIAN_POINT('Ctrl Pts',(-3.83176004896034,3.08905331441592,25.7961158073582));
#27957=CARTESIAN_POINT('Ctrl Pts',(-3.62416225441081,3.32730263217222,25.7784033607096));
#27958=CARTESIAN_POINT('Ctrl Pts',(-3.53654097633806,3.42028831921108,25.7712353389081));
#27959=CARTESIAN_POINT('Ctrl Pts',(-3.40607262686828,3.5483643478114,25.7609259341696));
#27960=CARTESIAN_POINT('Ctrl Pts',(-3.36609847511608,3.58630746988575,25.7578129616853));
#27961=CARTESIAN_POINT('Ctrl Pts',(-3.27323291417364,3.67153390265311,25.7506789193559));
#27962=CARTESIAN_POINT('Ctrl Pts',(-3.21993934609282,3.71836057433297,25.7466545508027));
#27963=CARTESIAN_POINT('Ctrl Pts',(-3.00536396947071,3.89882491348648,25.7307091999655));
#27964=CARTESIAN_POINT('Ctrl Pts',(-2.8366301860255,4.02325431635058,25.7187187283622));
#27965=CARTESIAN_POINT('Ctrl Pts',(-2.60205705991811,4.17412358660298,25.702760080165));
#27966=CARTESIAN_POINT('Ctrl Pts',(-2.54284161599757,4.21045903433922,25.6987888323481));
#27967=CARTESIAN_POINT('Ctrl Pts',(-2.43965848985968,4.270802744875,25.69197263239));
#27968=CARTESIAN_POINT('Ctrl Pts',(-2.39605708792969,4.29541617815705,25.6891233058648));
#27969=CARTESIAN_POINT('Ctrl Pts',(-2.33404859179352,4.32918261477363,25.6851169827759));
#27970=CARTESIAN_POINT('Ctrl Pts',(-2.31594860845906,4.33889236932821,25.6839530349122));
#27971=CARTESIAN_POINT('Ctrl Pts',(-2.28571799161006,4.35486655296985,25.6820180852886));
#27972=CARTESIAN_POINT('Ctrl Pts',(-2.27362125872273,4.3611943094973,25.6812461896));
#27973=CARTESIAN_POINT('Ctrl Pts',(-2.24860046154847,4.37415020140538,25.6796543017208));
#27974=CARTESIAN_POINT('Ctrl Pts',(-2.23567306398049,4.38077161847659,25.6788343969311));
#27975=CARTESIAN_POINT('Ctrl Pts',(-2.07692426712593,4.46119709626134,25.6687960404098));
#27976=CARTESIAN_POINT('Ctrl Pts',(-1.92753921805164,4.5277464388947,25.6596567720064));
#27977=CARTESIAN_POINT('Ctrl Pts',(-1.68000008054214,4.62354681230963,25.6447851253013));
#27978=CARTESIAN_POINT('Ctrl Pts',(-1.58376152517707,4.65739032174958,25.6390681400481));
#27979=CARTESIAN_POINT('Ctrl Pts',(-1.45989532629235,4.69666584648349,25.6317619024208));
#27980=CARTESIAN_POINT('Ctrl Pts',(-1.43317817093539,4.70488732700011,25.6301890667584));
#27981=CARTESIAN_POINT('Ctrl Pts',(-1.38406322686001,4.71954394419686,25.627302592721));
#27982=CARTESIAN_POINT('Ctrl Pts',(-1.36168698270088,4.72604851998848,25.6259894053175));
#27983=CARTESIAN_POINT('Ctrl Pts',(-1.28287441192812,4.74835244356736,25.6213699769613));
#27984=CARTESIAN_POINT('Ctrl Pts',(-1.2262030469283,4.76330176309321,25.6180586997349));
#27985=CARTESIAN_POINT('Ctrl Pts',(-1.09866510402713,4.79451801642506,25.6106240775847));
#27986=CARTESIAN_POINT('Ctrl Pts',(-1.02767782807547,4.81023348041227,25.6064977905989));
#27987=CARTESIAN_POINT('Ctrl Pts',(-0.806010885904746,4.85417608620273,
25.5936396372583));
#27988=CARTESIAN_POINT('Ctrl Pts',(-0.654343236654578,4.87693684089327,
25.5848773823583));
#27989=CARTESIAN_POINT('Ctrl Pts',(-0.404505680617832,4.90256426088584,
25.570500839929));
#27990=CARTESIAN_POINT('Ctrl Pts',(-0.306871944675769,4.90964264745801,
25.5648976325931));
#27991=CARTESIAN_POINT('Ctrl Pts',(-0.162462333983677,4.91578755680258,
25.5566441092165));
#27992=CARTESIAN_POINT('Ctrl Pts',(-0.115806625120437,4.91710790925397,
25.5539829125758));
#27993=CARTESIAN_POINT('Ctrl Pts',(-0.0502419764562126,4.91802968394553,
25.5502526000273));
#27994=CARTESIAN_POINT('Ctrl Pts',(-0.0313435736795576,4.91818643541423,
25.549178475921));
#27995=CARTESIAN_POINT('Ctrl Pts',(0.0198230901555402,4.91831590313559,
25.546273601232));
#27996=CARTESIAN_POINT('Ctrl Pts',(0.0520909331190609,4.91807999545365,
25.5444453970307));
#27997=CARTESIAN_POINT('Ctrl Pts',(0.138886448811547,4.91659111830121,25.5395371916102));
#27998=CARTESIAN_POINT('Ctrl Pts',(0.19339953504859,4.91474866004097,25.5364637871435));
#27999=CARTESIAN_POINT('Ctrl Pts',(0.41317027152132,4.9036585095395,25.5240881587301));
#28000=CARTESIAN_POINT('Ctrl Pts',(0.577943962168558,4.8869784044902,25.5148401042331));
#28001=CARTESIAN_POINT('Ctrl Pts',(0.826917085376503,4.84900463280085,25.5007188877127));
#28002=CARTESIAN_POINT('Ctrl Pts',(0.911912635931431,4.83374109364452,25.4958723068545));
#28003=CARTESIAN_POINT('Ctrl Pts',(1.00509993357753,4.81446102884588,25.490515783982));
#28004=CARTESIAN_POINT('Ctrl Pts',(1.01373328274043,4.81265059047086,25.4900191236602));
#28005=CARTESIAN_POINT('Ctrl Pts',(1.02946000951978,4.80930845472745,25.4891136357867));
#28006=CARTESIAN_POINT('Ctrl Pts',(1.03655495940822,4.80778426511544,25.4887048523722));
#28007=CARTESIAN_POINT('Ctrl Pts',(1.04991020668931,4.80488425503551,25.4879348320322));
#28008=CARTESIAN_POINT('Ctrl Pts',(1.05617123963045,4.80351188807435,25.4875736161116));
#28009=CARTESIAN_POINT('Ctrl Pts',(1.06841303567721,4.80080349545828,25.4868669053009));
#28010=CARTESIAN_POINT('Ctrl Pts',(1.07439402034343,4.79946852326035,25.4865214173269));
#28011=CARTESIAN_POINT('Ctrl Pts',(1.14802273977636,4.78288986253755,25.4822656718128));
#28012=CARTESIAN_POINT('Ctrl Pts',(1.2153427367887,4.76622843943874,25.4783471119655));
#28013=CARTESIAN_POINT('Ctrl Pts',(1.35547661561205,4.7283838193993,25.4701235798356));
#28014=CARTESIAN_POINT('Ctrl Pts',(1.42819841314884,4.70692888257124,25.4658177274077));
#28015=CARTESIAN_POINT('Ctrl Pts',(1.64552473023388,4.63731124179539,25.4528240196952));
#28016=CARTESIAN_POINT('Ctrl Pts',(1.78841427296511,4.58410085870939,25.4441082412064));
#28017=CARTESIAN_POINT('Ctrl Pts',(2.04694568047216,4.47389616161636,25.4280200953883));
#28018=CARTESIAN_POINT('Ctrl Pts',(2.16326663764913,4.41882467209778,25.4206568116731));
#28019=CARTESIAN_POINT('Ctrl Pts',(2.31431760536911,4.33991495424295,25.4109563830767));
#28020=CARTESIAN_POINT('Ctrl Pts',(2.35109248018979,4.32010323863895,25.4085836010601));
#28021=CARTESIAN_POINT('Ctrl Pts',(2.41912546407324,4.28232582355539,25.4041753017039));
#28022=CARTESIAN_POINT('Ctrl Pts',(2.45044702193469,4.2644802611968,25.402138244685));
#28023=CARTESIAN_POINT('Ctrl Pts',(2.62325523881742,4.1634896416304,25.3908480097775));
#28024=CARTESIAN_POINT('Ctrl Pts',(2.76070938764347,4.07364689674998,25.3816715192091));
#28025=CARTESIAN_POINT('Ctrl Pts',(2.97558899947648,3.91731789626265,25.3667830000934));
#28026=CARTESIAN_POINT('Ctrl Pts',(3.05588895172479,3.85500348781476,25.3610867758089));
#28027=CARTESIAN_POINT('Ctrl Pts',(3.19829199426285,3.73724870863627,25.3506969138183));
#28028=CARTESIAN_POINT('Ctrl Pts',(3.26102843752471,3.68263396164004,25.3460108530485));
#28029=CARTESIAN_POINT('Ctrl Pts',(3.37219251976504,3.58079183424249,25.3374898433669));
#28030=CARTESIAN_POINT('Ctrl Pts',(3.42108856480557,3.53410603214349,25.3336607342812));
#28031=CARTESIAN_POINT('Ctrl Pts',(3.54152979551226,3.41426662960101,25.3240130712444));
#28032=CARTESIAN_POINT('Ctrl Pts',(3.61178316939242,3.33986105120147,25.318184567119));
#28033=CARTESIAN_POINT('Ctrl Pts',(3.78362255592755,3.14609784889867,25.3033915434807));
#28034=CARTESIAN_POINT('Ctrl Pts',(3.88191994586096,3.02397562365284,25.2944130243293));
#28035=CARTESIAN_POINT('Ctrl Pts',(3.99707234477015,2.86602521527625,25.2832378579024));
#28036=CARTESIAN_POINT('Ctrl Pts',(4.01955324499409,2.83440992027006,25.2810219756092));
#28037=CARTESIAN_POINT('Ctrl Pts',(4.05645923102551,2.78118613031717,25.277327375925));
#28038=CARTESIAN_POINT('Ctrl Pts',(4.07109133322094,2.75972338296839,25.2758470486522));
#28039=CARTESIAN_POINT('Ctrl Pts',(4.10878334400893,2.70348360671294,25.2719934373972));
#28040=CARTESIAN_POINT('Ctrl Pts',(4.13157205269595,2.66852704834047,25.2696231356119));
#28041=CARTESIAN_POINT('Ctrl Pts',(4.17641621133642,2.59778697057288,25.2648784603831));
#28042=CARTESIAN_POINT('Ctrl Pts',(4.19846332812367,2.56200219596304,25.2625043567665));
#28043=CARTESIAN_POINT('Ctrl Pts',(4.30718214443455,2.38036726258589,25.2505708850209));
#28044=CARTESIAN_POINT('Ctrl Pts',(4.38672537253607,2.23038295384594,25.2410884138778));
#28045=CARTESIAN_POINT('Ctrl Pts',(4.50411876974339,1.97834348095936,25.2255075415065));
#28046=CARTESIAN_POINT('Ctrl Pts',(4.54661798150407,1.87861476664434,25.2194292235948));
#28047=CARTESIAN_POINT('Ctrl Pts',(4.61345190189181,1.70619559886004,25.2090210330939));
#28048=CARTESIAN_POINT('Ctrl Pts',(4.63944611601942,1.63419136756133,25.2047036356566));
#28049=CARTESIAN_POINT('Ctrl Pts',(4.6854196546457,1.49689140814331,25.1965134484897));
#28050=CARTESIAN_POINT('Ctrl Pts',(4.70574050472253,1.43172881185113,25.1926440787384));
#28051=CARTESIAN_POINT('Ctrl Pts',(4.78788540151665,1.1476416878596,25.1758381160438));
#28052=CARTESIAN_POINT('Ctrl Pts',(4.83583492567065,0.925000392210101,25.1628136794565));
#28053=CARTESIAN_POINT('Ctrl Pts',(4.87486173681126,0.653525841951685,25.147123065902));
#28054=CARTESIAN_POINT('Ctrl Pts',(4.880859272914,0.607112647828514,25.1444477424287));
#28055=CARTESIAN_POINT('Ctrl Pts',(4.89306669070323,0.50071665554164,25.138334007194));
#28056=CARTESIAN_POINT('Ctrl Pts',(4.89883768700977,0.440690651205942,25.1348985826877));
#28057=CARTESIAN_POINT('Ctrl Pts',(4.90634708071251,0.343935721916961,25.1293882428031));
#28058=CARTESIAN_POINT('Ctrl Pts',(4.90877991194379,0.307267429807165,25.1273065374152));
#28059=CARTESIAN_POINT('Ctrl Pts',(4.91412323350844,0.210288738032719,25.1218171109064));
#28060=CARTESIAN_POINT('Ctrl Pts',(4.91633449034602,0.149946046654312,25.1184170245335));
#28061=CARTESIAN_POINT('Ctrl Pts',(4.92064124695686,-0.0864771760380505,
25.10512705447));
#28062=CARTESIAN_POINT('Ctrl Pts',(4.91439132807231,-0.262577658666979,
25.0952922350161));
#28063=CARTESIAN_POINT('Ctrl Pts',(4.89166681725229,-0.516755903942656,
25.0809744088554));
#28064=CARTESIAN_POINT('Ctrl Pts',(4.88272257619821,-0.59536627711533,25.0765299464555));
#28065=CARTESIAN_POINT('Ctrl Pts',(4.86193164199094,-0.745710841696043,
25.0679802827223));
#28066=CARTESIAN_POINT('Ctrl Pts',(4.85038287242818,-0.817465461366168,
25.0638779847333));
#28067=CARTESIAN_POINT('Ctrl Pts',(4.82437083697558,-0.959012775985137,
25.0557317699744));
#28068=CARTESIAN_POINT('Ctrl Pts',(4.8099720023394,-1.02879961921618,25.0516892487404));
#28069=CARTESIAN_POINT('Ctrl Pts',(4.76535025269178,-1.22358200180145,25.040323634478));
#28070=CARTESIAN_POINT('Ctrl Pts',(4.73173455993439,-1.34774008211567,25.0329815499531));
#28071=CARTESIAN_POINT('Ctrl Pts',(4.65783751870718,-1.58360230434377,25.0188391334739));
#28072=CARTESIAN_POINT('Ctrl Pts',(4.61830060162211,-1.69544868890356,25.01204582796));
#28073=CARTESIAN_POINT('Ctrl Pts',(4.55611676870843,-1.85298713888958,25.0023690940653));
#28074=CARTESIAN_POINT('Ctrl Pts',(4.53674342472499,-1.89992644765093,24.9994719547882));
#28075=CARTESIAN_POINT('Ctrl Pts',(4.50003622043109,-1.98509909825754,24.9941925527533));
#28076=CARTESIAN_POINT('Ctrl Pts',(4.48293305672543,-2.02342671672803,24.9918083775204));
#28077=CARTESIAN_POINT('Ctrl Pts',(4.44782631327875,-2.09946903245329,24.9870635426189));
#28078=CARTESIAN_POINT('Ctrl Pts',(4.42982840700796,-2.13718260080019,24.9847030340324));
#28079=CARTESIAN_POINT('Ctrl Pts',(4.35215321764349,-2.29474847518332,24.9747992348253));
#28080=CARTESIAN_POINT('Ctrl Pts',(4.28807503532063,-2.41236843434848,24.9673024429398));
#28081=CARTESIAN_POINT('Ctrl Pts',(4.13508732614429,-2.66778563486339,24.9506230882706));
#28082=CARTESIAN_POINT('Ctrl Pts',(4.04392723399034,-2.80404690543407,24.9414476033246));
#28083=CARTESIAN_POINT('Ctrl Pts',(3.90352009856139,-2.99279340583187,24.9281916835003));
#28084=CARTESIAN_POINT('Ctrl Pts',(3.85966000459452,-3.04914840973011,24.9241595131294));
#28085=CARTESIAN_POINT('Ctrl Pts',(3.77447902277333,-3.15381179773572,24.9165189752553));
#28086=CARTESIAN_POINT('Ctrl Pts',(3.73341810534733,-3.20231320888572,24.9129135587893));
#28087=CARTESIAN_POINT('Ctrl Pts',(3.61824704873583,-3.33312710056247,24.9030028101423));
#28088=CARTESIAN_POINT('Ctrl Pts',(3.54227886064693,-3.41375277186777,24.8966837466174));
#28089=CARTESIAN_POINT('Ctrl Pts',(3.36856034709123,-3.58607378919437,24.8826912808268));
#28090=CARTESIAN_POINT('Ctrl Pts',(3.26965227216473,-3.67647902912972,24.8750166782366));
#28091=CARTESIAN_POINT('Ctrl Pts',(3.12634584575987,-3.79710326393923,24.8643112451312));
#28092=CARTESIAN_POINT('Ctrl Pts',(3.08495695275294,-3.83080568696026,24.8612650020019));
#28093=CARTESIAN_POINT('Ctrl Pts',(3.00895851107873,-3.89065963251992,24.855756576577));
#28094=CARTESIAN_POINT('Ctrl Pts',(2.9745358471372,-3.91703973043366,24.8532922029504));
#28095=CARTESIAN_POINT('Ctrl Pts',(2.91158814086704,-3.96397188945642,24.8488428471127));
#28096=CARTESIAN_POINT('Ctrl Pts',(2.88318314603763,-3.98467986355621,24.8468557601274));
#28097=CARTESIAN_POINT('Ctrl Pts',(2.79159276974941,-4.04995945218888,24.8405092529416));
#28098=CARTESIAN_POINT('Ctrl Pts',(2.72757692295855,-4.09334656566228,24.8361644375581));
#28099=CARTESIAN_POINT('Ctrl Pts',(2.50654684152594,-4.23566274040518,24.8214155989341));
#28100=CARTESIAN_POINT('Ctrl Pts',(2.34496968592233,-4.32720844884156,24.8110501117144));
#28101=CARTESIAN_POINT('Ctrl Pts',(2.14239529354691,-4.42729679290538,24.7983495532319));
#28102=CARTESIAN_POINT('Ctrl Pts',(2.10596437784323,-4.44474166874671,24.7960769229157));
#28103=CARTESIAN_POINT('Ctrl Pts',(2.00389342532524,-4.4920814859191,24.7897379815021));
#28104=CARTESIAN_POINT('Ctrl Pts',(1.93780492820308,-4.52098405640698,24.7856659250069));
#28105=CARTESIAN_POINT('Ctrl Pts',(1.81281120585003,-4.57240329238063,24.778014696421));
#28106=CARTESIAN_POINT('Ctrl Pts',(1.7540619178666,-4.59526093004211,24.7744388182871));
#28107=CARTESIAN_POINT('Ctrl Pts',(1.57346208256761,-4.66155895508438,24.7635011798637));
#28108=CARTESIAN_POINT('Ctrl Pts',(1.45032427299878,-4.70132679263998,24.7561175121078));
#28109=CARTESIAN_POINT('Ctrl Pts',(1.19267523494882,-4.77344836438742,24.740810752005));
#28110=CARTESIAN_POINT('Ctrl Pts',(1.05807532269833,-4.80507651287101,24.7328918541439));
#28111=CARTESIAN_POINT('Ctrl Pts',(0.862870866002943,-4.84234449709967,
24.7215465624031));
#28112=CARTESIAN_POINT('Ctrl Pts',(0.803214493592105,-4.85259651766762,
24.7180980576105));
#28113=CARTESIAN_POINT('Ctrl Pts',(0.707057953862087,-4.86729930449453,
24.7125746632872));
#28114=CARTESIAN_POINT('Ctrl Pts',(0.67067110686897,-4.87244638518387,24.7104929033638));
#28115=CARTESIAN_POINT('Ctrl Pts',(0.574580805407105,-4.88494197448149,
24.7050161767685));
#28116=CARTESIAN_POINT('Ctrl Pts',(0.514794283022248,-4.89160384448855,
24.7016287572397));
#28117=CARTESIAN_POINT('Ctrl Pts',(0.279298420002498,-4.91347916340054,
24.6883357899522));
#28118=CARTESIAN_POINT('Ctrl Pts',(0.102945798036454,-4.92033411843586,
24.6784857719044));
#28119=CARTESIAN_POINT('Ctrl Pts',(-0.152526876040929,-4.91652133513303,
24.6641506601392));
#28120=CARTESIAN_POINT('Ctrl Pts',(-0.231619298670093,-4.91343045456756,
24.6597042414346));
#28121=CARTESIAN_POINT('Ctrl Pts',(-0.383143685070682,-4.90384209845029,
24.6511516770548));
#28122=CARTESIAN_POINT('Ctrl Pts',(-0.455573966956382,-4.89764418974435,
24.647048441161));
#28123=CARTESIAN_POINT('Ctrl Pts',(-0.590176620624893,-4.88311435383984,
24.6393852481865));
#28124=CARTESIAN_POINT('Ctrl Pts',(-0.652378735392301,-4.87519395655599,
24.6358288387104));
#28125=CARTESIAN_POINT('Ctrl Pts',(-0.835703772958265,-4.84827918670137,
24.6252959527907));
#28126=CARTESIAN_POINT('Ctrl Pts',(-0.956286057888601,-4.82594324689242,
24.6183004296419));
#28127=CARTESIAN_POINT('Ctrl Pts',(-1.25257064314254,-4.75951980371715,
24.600933314225));
#28128=CARTESIAN_POINT('Ctrl Pts',(-1.42691394045778,-4.71018887179745,
24.5905524813566));
#28129=CARTESIAN_POINT('Ctrl Pts',(-1.63894829265869,-4.63733689092631,
24.5777867371998));
#28130=CARTESIAN_POINT('Ctrl Pts',(-1.67957034075495,-4.62277930188418,
24.5753347977912));
#28131=CARTESIAN_POINT('Ctrl Pts',(-1.75817123991425,-4.59343851471963,
24.5705807183892));
#28132=CARTESIAN_POINT('Ctrl Pts',(-1.79616829907697,-4.57871411871256,
24.5682781801633));
#28133=CARTESIAN_POINT('Ctrl Pts',(-1.93065715844491,-4.52466599697305,
24.5601044868722));
#28134=CARTESIAN_POINT('Ctrl Pts',(-2.02607804151243,-4.48275001099167,
24.5542604083466));
#28135=CARTESIAN_POINT('Ctrl Pts',(-2.13247163187994,-4.43192237124954,
24.5476523023696));
#28136=CARTESIAN_POINT('Ctrl Pts',(-2.14482222924629,-4.4259585143526,24.5468837865482));
#28137=CARTESIAN_POINT('Ctrl Pts',(-2.27586534939798,-4.36200308243287,
24.5387137211771));
#28138=CARTESIAN_POINT('Ctrl Pts',(-2.39219985749253,-4.29930384559869,
24.5313199721257));
#28139=CARTESIAN_POINT('Ctrl Pts',(-2.58229888333374,-4.18674160583593,
24.5189063024916));
#28140=CARTESIAN_POINT('Ctrl Pts',(-2.65748854877547,-4.13942352823295,
24.513904938638));
#28141=CARTESIAN_POINT('Ctrl Pts',(-2.78172617930073,-4.05645797336813,
24.5054655694754));
#28142=CARTESIAN_POINT('Ctrl Pts',(-2.83147138682824,-4.02189277756184,
24.5020371117377));
#28143=CARTESIAN_POINT('Ctrl Pts',(-2.94991368737741,-3.93630697754053,
24.493747661292));
#28144=CARTESIAN_POINT('Ctrl Pts',(-3.0179421690765,-3.88439547335493,24.4888804744478));
#28145=CARTESIAN_POINT('Ctrl Pts',(-3.28024928063424,-3.67318083455939,
24.4696735313068));
#28146=CARTESIAN_POINT('Ctrl Pts',(-3.46355705662923,-3.50086625062439,
24.4552473399512));
#28147=CARTESIAN_POINT('Ctrl Pts',(-3.66142136286597,-3.2840474043411,24.4385371770045));
#28148=CARTESIAN_POINT('Ctrl Pts',(-3.68954180614442,-3.25242295314027,
24.4361330310958));
#28149=CARTESIAN_POINT('Ctrl Pts',(-3.7443956145862,-3.18910694410987,24.4313868639297));
#28150=CARTESIAN_POINT('Ctrl Pts',(-3.77114337306935,-3.1574323949716,24.4290448278979));
#28151=CARTESIAN_POINT('Ctrl Pts',(-3.88669517477196,-3.0170333176635,24.4187926492465));
#28152=CARTESIAN_POINT('Ctrl Pts',(-3.9712222104939,-2.9048725363278,24.4109345388819));
#28153=CARTESIAN_POINT('Ctrl Pts',(-4.1419976834632,-2.65685469470588,24.3940649349396));
#28154=CARTESIAN_POINT('Ctrl Pts',(-4.22661283480377,-2.520072370854,24.3850605900295));
#28155=CARTESIAN_POINT('Ctrl Pts',(-4.3386601588022,-2.31737623043034,24.3720076862598));
#28156=CARTESIAN_POINT('Ctrl Pts',(-4.37159806093122,-2.25462520372215,
24.3680054278167));
#28157=CARTESIAN_POINT('Ctrl Pts',(-4.43576227975074,-2.12568772551956,
24.3598499253914));
#28158=CARTESIAN_POINT('Ctrl Pts',(-4.46689045451696,-2.05947197289073,
24.3556970001224));
#28159=CARTESIAN_POINT('Ctrl Pts',(-4.54747699290876,-1.87761805458317,
24.3443778734031));
#28160=CARTESIAN_POINT('Ctrl Pts',(-4.59399563410975,-1.76073850206107,
24.3371949085604));
#28161=CARTESIAN_POINT('Ctrl Pts',(-4.67437318127326,-1.53383094874207,
24.3234197317762));
#28162=CARTESIAN_POINT('Ctrl Pts',(-4.70895100423211,-1.42414274752008,
24.3168340540159));
#28163=CARTESIAN_POINT('Ctrl Pts',(-4.75789307223235,-1.24751842851091,
24.3063633027376));
#28164=CARTESIAN_POINT('Ctrl Pts',(-4.77475993704927,-1.18131978131719,
24.302468428636));
#28165=CARTESIAN_POINT('Ctrl Pts',(-4.79787435774482,-1.08199739384228,
24.2966750468482));
#28166=CARTESIAN_POINT('Ctrl Pts',(-4.80516917266076,-1.04912629159437,
24.2947660246127));
#28167=CARTESIAN_POINT('Ctrl Pts',(-4.82259739546037,-0.966595049042747,
24.2899941162226));
#28168=CARTESIAN_POINT('Ctrl Pts',(-4.8323018245132,-0.916848291746842,
24.2871361969917));
#28169=CARTESIAN_POINT('Ctrl Pts',(-4.86971990716506,-0.707900073762178,
24.2751901952639));
#28170=CARTESIAN_POINT('Ctrl Pts',(-4.89034807242049,-0.547531767085985,
24.2661587863224));
#28171=CARTESIAN_POINT('Ctrl Pts',(-4.91317675200177,-0.257886624354426,
24.2498734132655));
#28172=CARTESIAN_POINT('Ctrl Pts',(-4.91824897357135,-0.128987335353184,
24.2426359827897));
#28173=CARTESIAN_POINT('Ctrl Pts',(-4.91825054418017,0.0683528868924758,
24.2315070543874));
#28174=CARTESIAN_POINT('Ctrl Pts',(-4.91682452396337,0.13673695520985,24.2276419294321));
#28175=CARTESIAN_POINT('Ctrl Pts',(-4.91079728389466,0.281165252383581,
24.2194519491413));
#28176=CARTESIAN_POINT('Ctrl Pts',(-4.90585446576094,0.357177315883419,
24.215125832008));
#28177=CARTESIAN_POINT('Ctrl Pts',(-4.88981864771805,0.538595342356156,
24.2047551069089));
#28178=CARTESIAN_POINT('Ctrl Pts',(-4.87708007680103,0.643817457016504,
24.1987027752241));
#28179=CARTESIAN_POINT('Ctrl Pts',(-4.83789295986772,0.898293467968513,
24.1839719279346));
#28180=CARTESIAN_POINT('Ctrl Pts',(-4.80792540240429,1.04689689662642,24.1752892081604));
#28181=CARTESIAN_POINT('Ctrl Pts',(-4.76880303843594,1.20324303490926,24.1660979591495));
#28182=CARTESIAN_POINT('Ctrl Pts',(-4.76643256600081,1.21259919647824,24.1655477262546));
#28183=CARTESIAN_POINT('Ctrl Pts',(-4.76403458701365,1.22194824613716,24.1649977190913));
#28184=CARTESIAN_POINT('',(-4.91834666357043,-0.000109981193844847,23.8898594354524));
#28185=CARTESIAN_POINT('Ctrl Pts',(-4.76403458704968,1.22194824599669,23.8199296610182));
#28186=CARTESIAN_POINT('Ctrl Pts',(-4.79967280710214,1.08300478950659,23.8280513174643));
#28187=CARTESIAN_POINT('Ctrl Pts',(-4.8292303566121,0.942493438545646,23.8361729739104));
#28188=CARTESIAN_POINT('Ctrl Pts',(-4.85259123348966,0.800962785127571,
23.8442946303564));
#28189=CARTESIAN_POINT('Ctrl Pts',(-4.87595661619512,0.659404833386302,
23.8524178533013));
#28190=CARTESIAN_POINT('Ctrl Pts',(-4.89312288018924,0.516827521625683,
23.8605410762462));
#28191=CARTESIAN_POINT('Ctrl Pts',(-4.90402544113868,0.373788088580368,
23.8686642991911));
#28192=CARTESIAN_POINT('Ctrl Pts',(-4.9135077718429,0.249381794117097,23.8757293444318));
#28193=CARTESIAN_POINT('Ctrl Pts',(-4.91825278780639,0.124626196682925,
23.8827943896725));
#28194=CARTESIAN_POINT('Ctrl Pts',(-4.91824999877057,-0.000109969512879116,
23.8898594349132));
#28195=CARTESIAN_POINT('Ctrl Pts',(-4.91844317597977,-0.000109992856395721,
23.8898594359907));
#28196=CARTESIAN_POINT('Ctrl Pts',(-4.91856639306803,-0.127114903953705,
23.8970527000448));
#28197=CARTESIAN_POINT('Ctrl Pts',(-4.88269542365051,-1.07223352680412,
23.9505859626031));
#28198=CARTESIAN_POINT('Ctrl Pts',(-4.2981825700306,-2.79529185668768,24.0504592236655));
#28199=CARTESIAN_POINT('Ctrl Pts',(-2.43577373223791,-4.51165560462223,
24.189479219178));
#28200=CARTESIAN_POINT('Ctrl Pts',(0.0209816754386009,-5.12714245351884,
24.3284992146905));
#28201=CARTESIAN_POINT('Ctrl Pts',(2.47261740115848,-4.49156911968052,24.4675192102031));
#28202=CARTESIAN_POINT('Ctrl Pts',(4.32091643284836,-2.76002013574545,24.6065392057156));
#28203=CARTESIAN_POINT('Ctrl Pts',(5.11488031565789,-0.355006092729031,
24.7455592012281));
#28204=CARTESIAN_POINT('Ctrl Pts',(4.66077606687451,2.13663202817638,24.8845791967406));
#28205=CARTESIAN_POINT('Ctrl Pts',(3.06940843780244,4.1069163384864,25.0235991922531));
#28206=CARTESIAN_POINT('Ctrl Pts',(0.729082745657666,5.07508308497148,25.1626191877656));
#28207=CARTESIAN_POINT('Ctrl Pts',(-1.78914445815378,4.80489251463932,25.3016391832782));
#28208=CARTESIAN_POINT('Ctrl Pts',(-3.82211936364006,3.39601450889612,25.4374076416044));
#28209=CARTESIAN_POINT('Ctrl Pts',(-4.57494348751987,1.95876786470781,25.5268361014264));
#28210=CARTESIAN_POINT('Ctrl Pts',(-4.76438990516341,1.22203958205891,25.5699245627443));
#28211=CARTESIAN_POINT('Origin',(0.,0.,-3.23514056400928));
#28212=CARTESIAN_POINT('',(-4.76403458666814,1.22194824748421,27.665253726697));
#28213=CARTESIAN_POINT('',(-4.76403458719828,1.22194824541733,27.3196847251172));
#28214=CARTESIAN_POINT('',(-4.76403458704967,1.22194824599672,-3.23514056400928));
#28215=CARTESIAN_POINT('',(-4.91825002738015,0.00010786925271452,25.9850428854515));
#28216=CARTESIAN_POINT('Ctrl Pts',(-4.76403458666814,1.22194824748421,27.665253726697));
#28217=CARTESIAN_POINT('Ctrl Pts',(-4.76064996511665,1.23514394064655,27.6644742206369));
#28218=CARTESIAN_POINT('Ctrl Pts',(-4.7572104390177,1.24832588052699,27.6636945838257));
#28219=CARTESIAN_POINT('Ctrl Pts',(-4.71472557611052,1.40842257577462,27.6542144107116));
#28220=CARTESIAN_POINT('Ctrl Pts',(-4.66894380530174,1.55346573809053,27.645506153256));
#28221=CARTESIAN_POINT('Ctrl Pts',(-4.60181203668596,1.73618183649792,27.6344238022613));
#28222=CARTESIAN_POINT('Ctrl Pts',(-4.58658610954864,1.7760150072666,27.6320009900598));
#28223=CARTESIAN_POINT('Ctrl Pts',(-4.55564695658767,1.85390358612041,27.6272524850546));
#28224=CARTESIAN_POINT('Ctrl Pts',(-4.53997008276712,1.8919697126724,27.6249266255795));
#28225=CARTESIAN_POINT('Ctrl Pts',(-4.51383836417046,1.95322631117566,27.6211714560554));
#28226=CARTESIAN_POINT('Ctrl Pts',(-4.50367835575932,1.97654017861358,27.6197393329264));
#28227=CARTESIAN_POINT('Ctrl Pts',(-4.43219185283861,2.13716481521198,27.6098483184765));
#28228=CARTESIAN_POINT('Ctrl Pts',(-4.36477612579108,2.27167957594816,27.6014399966203));
#28229=CARTESIAN_POINT('Ctrl Pts',(-4.26230244143279,2.45468620632135,27.5896853908593));
#28230=CARTESIAN_POINT('Ctrl Pts',(-4.23236678175184,2.50594849424051,27.5863570348855));
#28231=CARTESIAN_POINT('Ctrl Pts',(-4.15183028490007,2.63829908330319,27.5776573184999));
#28232=CARTESIAN_POINT('Ctrl Pts',(-4.0997811906588,2.71847579392088,27.5722799167477));
#28233=CARTESIAN_POINT('Ctrl Pts',(-4.00714440926774,2.85245658919234,27.5630825130861));
#28234=CARTESIAN_POINT('Ctrl Pts',(-3.96772652645394,2.90703646133973,27.5592731077788));
#28235=CARTESIAN_POINT('Ctrl Pts',(-3.874814923407,3.03027471692886,27.550518062231));
#28236=CARTESIAN_POINT('Ctrl Pts',(-3.82059439056381,3.09835662658847,27.5455675823048));
#28237=CARTESIAN_POINT('Ctrl Pts',(-3.6436142650878,3.30886736111055,27.5298814541515));
#28238=CARTESIAN_POINT('Ctrl Pts',(-3.51448050112049,3.44571532237051,27.51910618738));
#28239=CARTESIAN_POINT('Ctrl Pts',(-3.32462576279781,3.62510758844716,27.504173950256));
#28240=CARTESIAN_POINT('Ctrl Pts',(-3.27030313309836,3.67418822170003,27.4999961848289));
#28241=CARTESIAN_POINT('Ctrl Pts',(-3.1885415628719,3.74480965037837,27.493852651144));
#28242=CARTESIAN_POINT('Ctrl Pts',(-3.16193685642271,3.76730035618366,27.49187536492));
#28243=CARTESIAN_POINT('Ctrl Pts',(-3.1011402483738,3.81759797281668,27.4874072372669));
#28244=CARTESIAN_POINT('Ctrl Pts',(-3.0668089789828,3.84523183566234,27.4849190976179));
#28245=CARTESIAN_POINT('Ctrl Pts',(-2.98904530750111,3.90612121022145,27.4793539751629));
#28246=CARTESIAN_POINT('Ctrl Pts',(-2.94542011511696,3.93912111763403,27.4762800610756));
#28247=CARTESIAN_POINT('Ctrl Pts',(-2.78608496067803,4.05552168112575,27.4652050227098));
#28248=CARTESIAN_POINT('Ctrl Pts',(-2.66731111347218,4.13460724979505,27.4572304922474));
#28249=CARTESIAN_POINT('Ctrl Pts',(-2.44801899439175,4.26723598243721,27.4428568356669));
#28250=CARTESIAN_POINT('Ctrl Pts',(-2.34876106128912,4.32266363918994,27.4364715963063));
#28251=CARTESIAN_POINT('Ctrl Pts',(-2.18697814426443,4.4057877925507,27.4262098583004));
#28252=CARTESIAN_POINT('Ctrl Pts',(-2.12564105470533,4.43570619463604,27.4223517511758));
#28253=CARTESIAN_POINT('Ctrl Pts',(-1.99176054517494,4.49759430032889,27.4139916974572));
#28254=CARTESIAN_POINT('Ctrl Pts',(-1.9190265629286,4.52910602667835,27.4094875489816));
#28255=CARTESIAN_POINT('Ctrl Pts',(-1.69731274489711,4.61886271730072,27.395859724521));
#28256=CARTESIAN_POINT('Ctrl Pts',(-1.54622382371118,4.67161153653316,27.3867063946848));
#28257=CARTESIAN_POINT('Ctrl Pts',(-1.28069652815407,4.75001801494066,27.3708589550009));
#28258=CARTESIAN_POINT('Ctrl Pts',(-1.16741108866242,4.77912194835796,27.3641714159793));
#28259=CARTESIAN_POINT('Ctrl Pts',(-1.01822230305812,4.81182795844294,27.3554831431432));
#28260=CARTESIAN_POINT('Ctrl Pts',(-0.983166313800091,4.81911288473193,
27.353450136301));
#28261=CARTESIAN_POINT('Ctrl Pts',(-0.906667609463635,4.83414047086758,
27.3490338982472));
#28262=CARTESIAN_POINT('Ctrl Pts',(-0.865198451120929,4.84173439395674,
27.3466526685673));
#28263=CARTESIAN_POINT('Ctrl Pts',(-0.773235502627993,4.857355605201,27.3413943076014));
#28264=CARTESIAN_POINT('Ctrl Pts',(-0.722703773281822,4.86513061892693,
27.338519729489));
#28265=CARTESIAN_POINT('Ctrl Pts',(-0.552666011687396,4.88858562741374,
27.3288815440531));
#28266=CARTESIAN_POINT('Ctrl Pts',(-0.432706841024413,4.90066058416014,
27.3221383498482));
#28267=CARTESIAN_POINT('Ctrl Pts',(-0.180503025085497,4.9167139099475,27.3079759729082));
#28268=CARTESIAN_POINT('Ctrl Pts',(-0.0482973586361654,4.91978899569347,
27.3005599703677));
#28269=CARTESIAN_POINT('Ctrl Pts',(0.146919523155377,4.91645950808169,27.2895530335701));
#28270=CARTESIAN_POINT('Ctrl Pts',(0.209941926458302,4.91417172282328,27.2859912497351));
#28271=CARTESIAN_POINT('Ctrl Pts',(0.344877120279991,4.90667292419014,27.2783401675765));
#28272=CARTESIAN_POINT('Ctrl Pts',(0.416754548684503,4.90109119449554,27.2742492427617));
#28273=CARTESIAN_POINT('Ctrl Pts',(0.631465975187671,4.87965999625878,27.2619735399502));
#28274=CARTESIAN_POINT('Ctrl Pts',(0.77375355326237,4.85912909117222,27.253763005014));
#28275=CARTESIAN_POINT('Ctrl Pts',(1.04582118161549,4.80761751102473,27.2379140907233));
#28276=CARTESIAN_POINT('Ctrl Pts',(1.17564618194848,4.77752912240826,27.2302844844276));
#28277=CARTESIAN_POINT('Ctrl Pts',(1.35203791184395,4.72902203616986,27.2198552035504));
#28278=CARTESIAN_POINT('Ctrl Pts',(1.39978359947179,4.71510995505442,27.2170259562016));
#28279=CARTESIAN_POINT('Ctrl Pts',(1.48336692702505,4.68937404645186,27.2120653086015));
#28280=CARTESIAN_POINT('Ctrl Pts',(1.51929435034912,4.67785753215388,27.2099308855668));
#28281=CARTESIAN_POINT('Ctrl Pts',(1.63107751393597,4.64060182953047,27.2032786634592));
#28282=CARTESIAN_POINT('Ctrl Pts',(1.70643958853681,4.61342209022953,27.1987767585127));
#28283=CARTESIAN_POINT('Ctrl Pts',(1.94585397673784,4.52040645982469,27.1843651287646));
#28284=CARTESIAN_POINT('Ctrl Pts',(2.1070327679654,4.44756508149975,27.1744905806663));
#28285=CARTESIAN_POINT('Ctrl Pts',(2.33679635745353,4.32842938821258,27.1599508385517));
#28286=CARTESIAN_POINT('Ctrl Pts',(2.40869499412891,4.28883508742562,27.1553317773876));
#28287=CARTESIAN_POINT('Ctrl Pts',(2.53785697157189,4.21343333173724,27.1468890915158));
#28288=CARTESIAN_POINT('Ctrl Pts',(2.5954382013193,4.17821000643685,27.1430708264778));
#28289=CARTESIAN_POINT('Ctrl Pts',(2.72321235052482,4.09638779933686,27.1344660712232));
#28290=CARTESIAN_POINT('Ctrl Pts',(2.79296949765636,4.04914801503473,27.1296756625979));
#28291=CARTESIAN_POINT('Ctrl Pts',(3.01703128682595,3.88886665497159,27.1139684256475));
#28292=CARTESIAN_POINT('Ctrl Pts',(3.16596041457574,3.7686145058122,27.1030077072156));
#28293=CARTESIAN_POINT('Ctrl Pts',(3.36369269603077,3.5889438410337,27.0877322332719));
#28294=CARTESIAN_POINT('Ctrl Pts',(3.41868973334464,3.53659541807505,27.0833987732702));
#28295=CARTESIAN_POINT('Ctrl Pts',(3.4972102838737,3.45831250770342,27.0770935067622));
#28296=CARTESIAN_POINT('Ctrl Pts',(3.52170357172565,3.43336703032634,27.0751091512852));
#28297=CARTESIAN_POINT('Ctrl Pts',(3.57626947536161,3.37659543238593,27.0706500002222));
#28298=CARTESIAN_POINT('Ctrl Pts',(3.60618729483753,3.34462454237405,27.0681778028635));
#28299=CARTESIAN_POINT('Ctrl Pts',(3.67214701018624,3.27222437387932,27.0626588042039));
#28300=CARTESIAN_POINT('Ctrl Pts',(3.70795607643927,3.23159060307155,27.0596149917805));
#28301=CARTESIAN_POINT('Ctrl Pts',(3.83326393563282,3.08457389389448,27.0487722407558));
#28302=CARTESIAN_POINT('Ctrl Pts',(3.91891484837524,2.97499833659421,27.0409988678308));
#28303=CARTESIAN_POINT('Ctrl Pts',(4.06165631414309,2.77550490662336,27.0272430812276));
#28304=CARTESIAN_POINT('Ctrl Pts',(4.12068495731941,2.68708664159231,27.0212740155317));
#28305=CARTESIAN_POINT('Ctrl Pts',(4.21013213851027,2.54321749510737,27.0117238845032));
#28306=CARTESIAN_POINT('Ctrl Pts',(4.24242669102736,2.48897238134715,27.0081584266551));
#28307=CARTESIAN_POINT('Ctrl Pts',(4.30929395651268,2.37157128262066,27.0005095079028));
#28308=CARTESIAN_POINT('Ctrl Pts',(4.34354216065408,2.30824740636024,26.9964244660516));
#28309=CARTESIAN_POINT('Ctrl Pts',(4.39474752026173,2.20839222607463,26.9900404791641));
#28310=CARTESIAN_POINT('Ctrl Pts',(4.41266703051343,2.17236544895714,26.9877486659967));
#28311=CARTESIAN_POINT('Ctrl Pts',(4.51411473668546,1.96197129839419,26.9744291338578));
#28312=CARTESIAN_POINT('Ctrl Pts',(4.58774466734351,1.78302022990197,26.9633474004599));
#28313=CARTESIAN_POINT('Ctrl Pts',(4.67438371846522,1.53122224161548,26.9481255631684));
#28314=CARTESIAN_POINT('Ctrl Pts',(4.69658115126848,1.46172171490275,26.9439626184082));
#28315=CARTESIAN_POINT('Ctrl Pts',(4.72793355463609,1.35545547087873,26.9376632577862));
#28316=CARTESIAN_POINT('Ctrl Pts',(4.73822334484207,1.31903556602557,26.9355160209801));
#28317=CARTESIAN_POINT('Ctrl Pts',(4.76051713811959,1.23649913735366,26.9306775392048));
#28318=CARTESIAN_POINT('Ctrl Pts',(4.77227333332955,1.19031963983346,26.927989157465));
#28319=CARTESIAN_POINT('Ctrl Pts',(4.81949318119061,0.992877276003605,26.9165584291248));
#28320=CARTESIAN_POINT('Ctrl Pts',(4.84845019829669,0.840149594657339,26.907871860414));
#28321=CARTESIAN_POINT('Ctrl Pts',(4.88943092519163,0.549344588365354,26.891414914993));
#28322=CARTESIAN_POINT('Ctrl Pts',(4.90294542595198,0.411630541058711,26.88365631214));
#28323=CARTESIAN_POINT('Ctrl Pts',(4.91412316198807,0.210959712626267,26.8723242173166));
#28324=CARTESIAN_POINT('Ctrl Pts',(4.91641224255763,0.148327365530215,26.8687838896767));
#28325=CARTESIAN_POINT('Ctrl Pts',(4.91877088284774,0.0129383021127199,
26.8611166523174));
#28326=CARTESIAN_POINT('Ctrl Pts',(4.91842422953663,-0.0598107800746115,
26.8569878329261));
#28327=CARTESIAN_POINT('Ctrl Pts',(4.9143286050754,-0.211752099166897,26.8483392282834));
#28328=CARTESIAN_POINT('Ctrl Pts',(4.91027825149939,-0.290915639716645,
26.8438187725225));
#28329=CARTESIAN_POINT('Ctrl Pts',(4.89098413574901,-0.546694666853374,
26.8291620544453));
#28330=CARTESIAN_POINT('Ctrl Pts',(4.86810643566972,-0.722592926676408,
26.8189991404571));
#28331=CARTESIAN_POINT('Ctrl Pts',(4.8249483881279,-0.955294051612906,26.805489534729));
#28332=CARTESIAN_POINT('Ctrl Pts',(4.81305505929978,-1.01351605319028,26.8021044849998));
#28333=CARTESIAN_POINT('Ctrl Pts',(4.79210261696473,-1.10737811894963,26.7966441315826));
#28334=CARTESIAN_POINT('Ctrl Pts',(4.7836938257061,-1.14315668679057,26.7945623471964));
#28335=CARTESIAN_POINT('Ctrl Pts',(4.76019350058588,-1.23834477064705,26.7890212947696));
#28336=CARTESIAN_POINT('Ctrl Pts',(4.74439106995902,-1.29757213460608,26.7855700165795));
#28337=CARTESIAN_POINT('Ctrl Pts',(4.70163834685193,-1.44656918815566,26.7768588656913));
#28338=CARTESIAN_POINT('Ctrl Pts',(4.67322156482481,-1.53589255807802,26.771609522555));
#28339=CARTESIAN_POINT('Ctrl Pts',(4.58886742171799,-1.77697037894829,26.7573009755254));
#28340=CARTESIAN_POINT('Ctrl Pts',(4.52797145819568,-1.9268631519593,26.748246425354));
#28341=CARTESIAN_POINT('Ctrl Pts',(4.4293459748742,-2.13899433707183,26.7350670915183));
#28342=CARTESIAN_POINT('Ctrl Pts',(4.39744829908983,-2.20382640813193,26.7309882800607));
#28343=CARTESIAN_POINT('Ctrl Pts',(4.33110799349748,-2.33148368999399,26.7228442466557));
#28344=CARTESIAN_POINT('Ctrl Pts',(4.2966976653546,-2.39430609174228,26.7187801881253));
#28345=CARTESIAN_POINT('Ctrl Pts',(4.18117738833755,-2.59469396752875,26.705623068095));
#28346=CARTESIAN_POINT('Ctrl Pts',(4.09473774498144,-2.7290662853541,26.6964953200188));
#28347=CARTESIAN_POINT('Ctrl Pts',(3.92196476841252,-2.9709076771374,26.6794815137971));
#28348=CARTESIAN_POINT('Ctrl Pts',(3.83735288569841,-3.079419346278,26.6716069654977));
#28349=CARTESIAN_POINT('Ctrl Pts',(3.72136750334687,-3.2159505495092,26.6614102768428));
#28350=CARTESIAN_POINT('Ctrl Pts',(3.69402958449487,-3.2473157401144,26.65904696373));
#28351=CARTESIAN_POINT('Ctrl Pts',(3.63819695717747,-3.30975574758314,26.654302114897));
#28352=CARTESIAN_POINT('Ctrl Pts',(3.60969403369218,-3.34081864912121,26.6519209105823));
#28353=CARTESIAN_POINT('Ctrl Pts',(3.54575033274494,-3.4087315984533,26.6466626217176));
#28354=CARTESIAN_POINT('Ctrl Pts',(3.51012718253375,-3.44540327975182,26.6437880902243));
#28355=CARTESIAN_POINT('Ctrl Pts',(3.38862565914825,-3.56664045899597,26.6341502151322));
#28356=CARTESIAN_POINT('Ctrl Pts',(3.30021224138485,-3.64860348596269,26.6274072833686));
#28357=CARTESIAN_POINT('Ctrl Pts',(3.10868852854766,-3.8134913716271,26.6132443678981));
#28358=CARTESIAN_POINT('Ctrl Pts',(3.00506369191737,-3.8956709818707,26.6058275618341));
#28359=CARTESIAN_POINT('Ctrl Pts',(2.84730966573292,-4.0107339661912,26.5948198824504));
#28360=CARTESIAN_POINT('Ctrl Pts',(2.79565460639087,-4.04690925212025,26.5912581688691));
#28361=CARTESIAN_POINT('Ctrl Pts',(2.68348682992467,-4.12229039869624,26.5836070437771));
#28362=CARTESIAN_POINT('Ctrl Pts',(2.62277871392765,-4.16117908204585,26.5795160048968));
#28363=CARTESIAN_POINT('Ctrl Pts',(2.43854776265057,-4.27356082551775,26.5672389237854));
#28364=CARTESIAN_POINT('Ctrl Pts',(2.31263710137224,-4.34298815174005,26.5590271146051));
#28365=CARTESIAN_POINT('Ctrl Pts',(2.0648012072018,-4.46580764068894,26.5431954614029));
#28366=CARTESIAN_POINT('Ctrl Pts',(1.94339033898596,-4.51996419008817,26.5355844203629));
#28367=CARTESIAN_POINT('Ctrl Pts',(1.77360090035928,-4.58759309109774,26.5251650076955));
#28368=CARTESIAN_POINT('Ctrl Pts',(1.72698825890711,-4.60534278391403,26.5223273599875));
#28369=CARTESIAN_POINT('Ctrl Pts',(1.64468872980568,-4.63525649118953,26.5173602912255));
#28370=CARTESIAN_POINT('Ctrl Pts',(1.6091173639672,-4.64772472211019,26.5152277931673));
#28371=CARTESIAN_POINT('Ctrl Pts',(1.49800159162702,-4.68524367862435,26.5086064342846));
#28372=CARTESIAN_POINT('Ctrl Pts',(1.42198976562632,-4.7088706134757,26.5041332318151));
#28373=CARTESIAN_POINT('Ctrl Pts',(1.19088013671228,-4.77460027483214,26.4906511007212));
#28374=CARTESIAN_POINT('Ctrl Pts',(1.03426150879265,-4.81095691991202,26.481670528841));
#28375=CARTESIAN_POINT('Ctrl Pts',(0.778333401567124,-4.85728944992974,
26.4670702921644));
#28376=CARTESIAN_POINT('Ctrl Pts',(0.680008613754562,-4.87202746556686,
26.4614793409982));
#28377=CARTESIAN_POINT('Ctrl Pts',(0.516820198808213,-4.89145144586059,
26.4522019503655));
#28378=CARTESIAN_POINT('Ctrl Pts',(0.452189419176299,-4.89784901508398,
26.4485282482567));
#28379=CARTESIAN_POINT('Ctrl Pts',(0.315824625756783,-4.90862509277537,
26.4407716597912));
#28380=CARTESIAN_POINT('Ctrl Pts',(0.244082985159172,-4.91271501681042,
26.4366877325577));
#28381=CARTESIAN_POINT('Ctrl Pts',(0.080506099021611,-4.91844836047242,
26.4273631404639));
#28382=CARTESIAN_POINT('Ctrl Pts',(-0.0113373198127981,-4.91909409761994,
26.4221182616299));
#28383=CARTESIAN_POINT('Ctrl Pts',(-0.290191398105914,-4.91324475883017,
26.4061633589779));
#28384=CARTESIAN_POINT('Ctrl Pts',(-0.476863367831023,-4.89865158055568,
26.3954359061231));
#28385=CARTESIAN_POINT('Ctrl Pts',(-0.701075958242673,-4.86818352561199,
26.3825649330758));
#28386=CARTESIAN_POINT('Ctrl Pts',(-0.739837655438666,-4.86244369047897,
26.3803406367033));
#28387=CARTESIAN_POINT('Ctrl Pts',(-0.815656108875953,-4.85028887539322,
26.3759931987426));
#28388=CARTESIAN_POINT('Ctrl Pts',(-0.852715979703553,-4.84391087442513,
26.3738694840199));
#28389=CARTESIAN_POINT('Ctrl Pts',(-0.893477122236693,-4.83641359369834,
26.3715330345062));
#28390=CARTESIAN_POINT('Ctrl Pts',(-0.897254130788829,-4.83571430525909,
26.3713165285209));
#28391=CARTESIAN_POINT('Ctrl Pts',(-0.905498595786359,-4.83417790471142,
26.370843921455));
#28392=CARTESIAN_POINT('Ctrl Pts',(-0.909965719689209,-4.83333902291333,
26.3705878362863));
#28393=CARTESIAN_POINT('Ctrl Pts',(-0.970764398347969,-4.82183435507857,
26.3671022590888));
#28394=CARTESIAN_POINT('Ctrl Pts',(-1.02690678412038,-4.81019049555959,
26.3638813134181));
#28395=CARTESIAN_POINT('Ctrl Pts',(-1.24077041667061,-4.76192049122991,
26.3515794844854));
#28396=CARTESIAN_POINT('Ctrl Pts',(-1.39685108212735,-4.71849606398248,
26.3425307538868));
#28397=CARTESIAN_POINT('Ctrl Pts',(-1.64402203672741,-4.63638707311834,
26.3279091109782));
#28398=CARTESIAN_POINT('Ctrl Pts',(-1.73658321896128,-4.60251799943816,
26.3223660724372));
#28399=CARTESIAN_POINT('Ctrl Pts',(-1.87641862523985,-4.54653156012294,
26.3138624481865));
#28400=CARTESIAN_POINT('Ctrl Pts',(-1.92446276681263,-4.52640465290204,
26.3109169509253));
#28401=CARTESIAN_POINT('Ctrl Pts',(-2.03939878595792,-4.47609429003001,
26.3038085132982));
#28402=CARTESIAN_POINT('Ctrl Pts',(-2.10595222314233,-4.44516957677413,
26.2996409284886));
#28403=CARTESIAN_POINT('Ctrl Pts',(-2.24767910674318,-4.37541725628407,
26.290647681846));
#28404=CARTESIAN_POINT('Ctrl Pts',(-2.32259321675628,-4.33611555257538,
26.2858201376729));
#28405=CARTESIAN_POINT('Ctrl Pts',(-2.5512966163641,-4.2085043421337,26.2708470617046));
#28406=CARTESIAN_POINT('Ctrl Pts',(-2.70135190529194,-4.11379646437946,
26.2606801329224));
#28407=CARTESIAN_POINT('Ctrl Pts',(-2.88773957098651,-3.98155332275614,
26.2476484521273));
#28408=CARTESIAN_POINT('Ctrl Pts',(-2.9290491304873,-3.95126283213868,26.2447335599257));
#28409=CARTESIAN_POINT('Ctrl Pts',(-2.99762864449907,-3.89930988744348,
26.2398525423825));
#28410=CARTESIAN_POINT('Ctrl Pts',(-3.02515491053225,-3.87799340885901,
26.2378820988019));
#28411=CARTESIAN_POINT('Ctrl Pts',(-3.05968157330942,-3.85066445242693,
26.2353948780981));
#28412=CARTESIAN_POINT('Ctrl Pts',(-3.06689419292561,-3.84492237440164,
26.2348744114903));
#28413=CARTESIAN_POINT('Ctrl Pts',(-3.08050459899719,-3.83402425569698,
26.2338905452295));
#28414=CARTESIAN_POINT('Ctrl Pts',(-3.0869056901489,-3.8288723977435,26.2334270954222));
#28415=CARTESIAN_POINT('Ctrl Pts',(-3.10291754508265,-3.81591915510387,
26.2322659308781));
#28416=CARTESIAN_POINT('Ctrl Pts',(-3.11251183270786,-3.80809747541361,
26.2315684571914));
#28417=CARTESIAN_POINT('Ctrl Pts',(-3.16847594732679,-3.76212030980905,
26.2274896610047));
#28418=CARTESIAN_POINT('Ctrl Pts',(-3.21417365981904,-3.72315415049807,
26.2241171454808));
#28419=CARTESIAN_POINT('Ctrl Pts',(-3.39773050482049,-3.56073762100317,
26.2103682015441));
#28420=CARTESIAN_POINT('Ctrl Pts',(-3.52928312686911,-3.43039143590329,
26.2000305896804));
#28421=CARTESIAN_POINT('Ctrl Pts',(-3.70921370855081,-3.23077721904066,
26.1849228291555));
#28422=CARTESIAN_POINT('Ctrl Pts',(-3.76365347986991,-3.16719118956933,
26.1802079751842));
#28423=CARTESIAN_POINT('Ctrl Pts',(-3.83250274439961,-3.08249151982606,
26.1740399489608));
#28424=CARTESIAN_POINT('Ctrl Pts',(-3.84840803776563,-3.06261111198495,
26.1726000434062));
#28425=CARTESIAN_POINT('Ctrl Pts',(-3.8714032244837,-3.0334068783846,26.1704959022487));
#28426=CARTESIAN_POINT('Ctrl Pts',(-3.87861534485782,-3.02417976024834,
26.1698326914501));
#28427=CARTESIAN_POINT('Ctrl Pts',(-3.89023284715783,-3.00920652010283,
26.1687590178432));
#28428=CARTESIAN_POINT('Ctrl Pts',(-3.89465862316918,-3.00347626834985,
26.1683487234224));
#28429=CARTESIAN_POINT('Ctrl Pts',(-3.90426824045027,-2.99097730790976,
26.1674550754577));
#28430=CARTESIAN_POINT('Ctrl Pts',(-3.90944716653823,-2.98420485248403,
26.1669716836808));
#28431=CARTESIAN_POINT('Ctrl Pts',(-3.96461188899948,-2.91167616544092,
26.1618035901253));
#28432=CARTESIAN_POINT('Ctrl Pts',(-4.01295079305615,-2.84468473177401,
26.1571062475886));
#28433=CARTESIAN_POINT('Ctrl Pts',(-4.11787063596362,-2.69127967795946,
26.1465101734134));
#28434=CARTESIAN_POINT('Ctrl Pts',(-4.17346312471482,-2.60423696052733,
26.1406071861521));
#28435=CARTESIAN_POINT('Ctrl Pts',(-4.30661010575211,-2.38053849813489,
26.1257079032542));
#28436=CARTESIAN_POINT('Ctrl Pts',(-4.38043473350752,-2.24179535634945,
26.116709422727));
#28437=CARTESIAN_POINT('Ctrl Pts',(-4.465047696652,-2.06257670001851,26.1054302956516));
#28438=CARTESIAN_POINT('Ctrl Pts',(-4.48213459307556,-2.02517730684825,
26.1030950568623));
#28439=CARTESIAN_POINT('Ctrl Pts',(-4.51521357793691,-1.95030483789718,
26.0984587733466));
#28440=CARTESIAN_POINT('Ctrl Pts',(-4.53121301799591,-1.91283853226417,
26.0961576911522));
#28441=CARTESIAN_POINT('Ctrl Pts',(-4.63989458995137,-1.64931818970439,
26.0800878910288));
#28442=CARTESIAN_POINT('Ctrl Pts',(-4.7160860033962,-1.41683011621999,26.0664808773928));
#28443=CARTESIAN_POINT('Ctrl Pts',(-4.79422268247865,-1.10056653420995,
26.0481782450019));
#28444=CARTESIAN_POINT('Ctrl Pts',(-4.81179183044261,-1.02101763275938,
26.0435933944782));
#28445=CARTESIAN_POINT('Ctrl Pts',(-4.8397925158082,-0.877383363066244,
26.0353321621244));
#28446=CARTESIAN_POINT('Ctrl Pts',(-4.85094621396667,-0.813457971635867,
26.0316615536937));
#28447=CARTESIAN_POINT('Ctrl Pts',(-4.87052539044151,-0.686449919960619,
26.0243744957381));
#28448=CARTESIAN_POINT('Ctrl Pts',(-4.87899780821496,-0.623386998595736,
26.0207590700356));
#28449=CARTESIAN_POINT('Ctrl Pts',(-4.90756838396048,-0.374175436473399,
26.0064755421049));
#28450=CARTESIAN_POINT('Ctrl Pts',(-4.91825410378982,-0.187108860318732,
25.9957559094304));
#28451=CARTESIAN_POINT('Ctrl Pts',(-4.91824999881774,0.000107839092156406,
25.985042837665));
#28452=CARTESIAN_POINT('Ctrl Pts',(-4.91824999881714,0.00010786642811769,
25.9850428361008));
#28453=CARTESIAN_POINT('Ctrl Pts',(-4.91824859447662,0.0641398167640534,
25.9813787458714));
#28454=CARTESIAN_POINT('Ctrl Pts',(-4.91699671764731,0.12816596342371,25.9777175108798));
#28455=CARTESIAN_POINT('Ctrl Pts',(-4.91299657002833,0.23047530219885,25.9718756339816));
#28456=CARTESIAN_POINT('Ctrl Pts',(-4.91104981305733,0.268782304395479,
25.9696902343865));
#28457=CARTESIAN_POINT('Ctrl Pts',(-4.90660886371666,0.339774585574197,
25.965645209907));
#28458=CARTESIAN_POINT('Ctrl Pts',(-4.90423561074501,0.372465318778533,
25.9637845410905));
#28459=CARTESIAN_POINT('Ctrl Pts',(-4.89805355438409,0.447259984964282,
25.9595333058903));
#28460=CARTESIAN_POINT('Ctrl Pts',(-4.89402830481027,0.48934356351924,25.9571455411912));
#28461=CARTESIAN_POINT('Ctrl Pts',(-4.8751761641213,0.662813556767806,25.9473094579166));
#28462=CARTESIAN_POINT('Ctrl Pts',(-4.85559662887549,0.793628730723643,
25.9399057938522));
#28463=CARTESIAN_POINT('Ctrl Pts',(-4.81162092519639,1.02366360476718,25.9267854602727));
#28464=CARTESIAN_POINT('Ctrl Pts',(-4.78936417432496,1.12319526975691,25.9210745997888));
#28465=CARTESIAN_POINT('Ctrl Pts',(-4.76403457790608,1.22194828164502,25.9153493127618));
#28466=CARTESIAN_POINT('',(-4.91787650032817,4.95708214059191E-5,25.6398490687309));
#28467=CARTESIAN_POINT('Ctrl Pts',(-4.76438990516341,1.22203958205891,25.5699245627443));
#28468=CARTESIAN_POINT('Ctrl Pts',(-4.77868589190668,1.16644466560101,25.5731760999306));
#28469=CARTESIAN_POINT('Ctrl Pts',(-4.87410541215778,0.766055703403716,
25.5964877222952));
#28470=CARTESIAN_POINT('Ctrl Pts',(-4.91798476554411,0.354353816740224,
25.6197993446597));
#28471=CARTESIAN_POINT('Ctrl Pts',(-4.91785849824545,5.01597051061138E-5,
25.6398594298379));
#28472=CARTESIAN_POINT('Ctrl Pts',(-4.91824999985816,3.73529137002939E-5,
25.6396341009043));
#28473=CARTESIAN_POINT('Ctrl Pts',(-4.91825040859229,-0.0537805815385731,
25.6426695501133));
#28474=CARTESIAN_POINT('Ctrl Pts',(-4.91736746376412,-0.107594589358031,
25.6457101258233));
#28475=CARTESIAN_POINT('Ctrl Pts',(-4.91368567495012,-0.219739063851807,
25.6520618332672));
#28476=CARTESIAN_POINT('Ctrl Pts',(-4.91073079301712,-0.278056036895246,
25.6553735176413));
#28477=CARTESIAN_POINT('Ctrl Pts',(-4.89794772651726,-0.464562163061656,
25.6659983254188));
#28478=CARTESIAN_POINT('Ctrl Pts',(-4.88413191376792,-0.592422708574879,
25.6733344125371));
#28479=CARTESIAN_POINT('Ctrl Pts',(-4.83785904150373,-0.905283383512189,
25.6914253924981));
#28480=CARTESIAN_POINT('Ctrl Pts',(-4.79978685301425,-1.08924979830331,
25.7021890384979));
#28481=CARTESIAN_POINT('Ctrl Pts',(-4.74267753754525,-1.30280657669003,
25.7147647340652));
#28482=CARTESIAN_POINT('Ctrl Pts',(-4.73373465495577,-1.33493499672673,
25.7166586611372));
#28483=CARTESIAN_POINT('Ctrl Pts',(-4.71307798310571,-1.40632773011291,
25.7208702750094));
#28484=CARTESIAN_POINT('Ctrl Pts',(-4.70119888806464,-1.44554170314726,
25.7231855202486));
#28485=CARTESIAN_POINT('Ctrl Pts',(-4.66185901973552,-1.56978906912364,
25.7305350828253));
#28486=CARTESIAN_POINT('Ctrl Pts',(-4.63257017947281,-1.65422521931918,
25.7355507560079));
#28487=CARTESIAN_POINT('Ctrl Pts',(-4.55060396554596,-1.87123671444251,
25.74855645122));
#28488=CARTESIAN_POINT('Ctrl Pts',(-4.4944314471968,-2.00240084949664,25.7565324253232));
#28489=CARTESIAN_POINT('Ctrl Pts',(-4.40034139238856,-2.19812086833262,
25.7687240375858));
#28490=CARTESIAN_POINT('Ctrl Pts',(-4.36652104575094,-2.26456034090919,
25.7729152997698));
#28491=CARTESIAN_POINT('Ctrl Pts',(-4.30104537182488,-2.38626143498539,
25.7807053323999));
#28492=CARTESIAN_POINT('Ctrl Pts',(-4.26980158285057,-2.44172669635751,
25.7843004517781));
#28493=CARTESIAN_POINT('Ctrl Pts',(-4.2043133732387,-2.55288148334038,25.791603956434));
#28494=CARTESIAN_POINT('Ctrl Pts',(-4.17001752754772,-2.6085261176518,25.7953120739215));
#28495=CARTESIAN_POINT('Ctrl Pts',(-4.01705790516058,-2.84597212864427,
25.8113729266473));
#28496=CARTESIAN_POINT('Ctrl Pts',(-3.88753937882274,-3.02048782914107,
25.8238035693995));
#28497=CARTESIAN_POINT('Ctrl Pts',(-3.69736190117411,-3.24415643752122,
25.8406007897869));
#28498=CARTESIAN_POINT('Ctrl Pts',(-3.64645131567586,-3.30127687115357,
25.8449728920762));
#28499=CARTESIAN_POINT('Ctrl Pts',(-3.58238140833934,-3.36987058295376,
25.8503200040556));
#28500=CARTESIAN_POINT('Ctrl Pts',(-3.57046700460818,-3.38249163677978,
25.851307998478));
#28501=CARTESIAN_POINT('Ctrl Pts',(-3.53572481569087,-3.41890630385694,
25.8541704363925));
#28502=CARTESIAN_POINT('Ctrl Pts',(-3.51272413658165,-3.44253387118795,
25.8560425433234));
#28503=CARTESIAN_POINT('Ctrl Pts',(-3.4639499993639,-3.49163954099752,25.8599635783725));
#28504=CARTESIAN_POINT('Ctrl Pts',(-3.43812898162748,-3.51706773077636,
25.8620115186904));
#28505=CARTESIAN_POINT('Ctrl Pts',(-3.31963520249257,-3.63120675998014,
25.8712922229284));
#28506=CARTESIAN_POINT('Ctrl Pts',(-3.22379343426538,-3.71655715237029,
25.8784793836466));
#28507=CARTESIAN_POINT('Ctrl Pts',(-3.05546061576027,-3.85504707898954,
25.8906915275745));
#28508=CARTESIAN_POINT('Ctrl Pts',(-2.98465202713447,-3.91012528812961,
25.8957138257999));
#28509=CARTESIAN_POINT('Ctrl Pts',(-2.84802385193446,-4.01052626171237,
25.9052261529284));
#28510=CARTESIAN_POINT('Ctrl Pts',(-2.78252866025655,-4.05624146875458,
25.9097127091704));
#28511=CARTESIAN_POINT('Ctrl Pts',(-2.66304590075251,-4.1353834612991,25.9177856209571));
#28512=CARTESIAN_POINT('Ctrl Pts',(-2.60946906248705,-4.16939815161943,
25.9213667842976));
#28513=CARTESIAN_POINT('Ctrl Pts',(-2.49988940170245,-4.23602807884815,
25.9286211505654));
#28514=CARTESIAN_POINT('Ctrl Pts',(-2.44387001459963,-4.26859228993453,
25.9322939985358));
#28515=CARTESIAN_POINT('Ctrl Pts',(-2.37879808908558,-4.3047178296398,25.9365227741421));
#28516=CARTESIAN_POINT('Ctrl Pts',(-2.37035838399485,-4.30937084416066,
25.9370705199698));
#28517=CARTESIAN_POINT('Ctrl Pts',(-2.18705071069695,-4.40973139603089,
25.9489519640084));
#28518=CARTESIAN_POINT('Ctrl Pts',(-2.00653981441087,-4.49474334129122,
25.9603577960101));
#28519=CARTESIAN_POINT('Ctrl Pts',(-1.74893341503838,-4.59744454929035,
25.9762310078727));
#28520=CARTESIAN_POINT('Ctrl Pts',(-1.67581759305062,-4.62459727881428,
25.9806917174213));
#28521=CARTESIAN_POINT('Ctrl Pts',(-1.58673872780013,-4.65528804670007,
25.9860670813078));
#28522=CARTESIAN_POINT('Ctrl Pts',(-1.57136454106792,-4.66049998061225,
25.9869927041249));
#28523=CARTESIAN_POINT('Ctrl Pts',(-1.54674636598691,-4.66871001162847,
25.9884714059344));
#28524=CARTESIAN_POINT('Ctrl Pts',(-1.5375188261714,-4.67175698780145,25.9890248862812));
#28525=CARTESIAN_POINT('Ctrl Pts',(-1.52192544953536,-4.67685478896045,
25.9899588673247));
#28526=CARTESIAN_POINT('Ctrl Pts',(-1.51556435619285,-4.67892001143318,
25.9903394984017));
#28527=CARTESIAN_POINT('Ctrl Pts',(-1.50464115804381,-4.68244177561402,
25.9909924665278));
#28528=CARTESIAN_POINT('Ctrl Pts',(-1.50008110489058,-4.68390463986185,
25.9912648646033));
#28529=CARTESIAN_POINT('Ctrl Pts',(-1.46381173816561,-4.69548144812348,
25.9934298924547));
#28530=CARTESIAN_POINT('Ctrl Pts',(-1.43200240630764,-4.70528001028981,
25.9953192834575));
#28531=CARTESIAN_POINT('Ctrl Pts',(-1.3586682919955,-4.72705734302042,25.9996522344145));
#28532=CARTESIAN_POINT('Ctrl Pts',(-1.31708006187238,-4.73881322923037,
26.0020928535323));
#28533=CARTESIAN_POINT('Ctrl Pts',(-1.15859548088905,-4.78136506264894,
26.0113415311648));
#28534=CARTESIAN_POINT('Ctrl Pts',(-1.0407318244373,-4.80839611628701,26.018113728618));
#28535=CARTESIAN_POINT('Ctrl Pts',(-0.803965475358392,-4.85358218279611,
26.0316176166877));
#28536=CARTESIAN_POINT('Ctrl Pts',(-0.68515453877262,-4.87177416621673,
26.0383447839683));
#28537=CARTESIAN_POINT('Ctrl Pts',(-0.495750199940035,-4.89370894214521,
26.0490564875577));
#28538=CARTESIAN_POINT('Ctrl Pts',(-0.425537172511849,-4.90031360823001,
26.0530244097853));
#28539=CARTESIAN_POINT('Ctrl Pts',(-0.290476346275886,-4.9100935398953,
26.0606629847065));
#28540=CARTESIAN_POINT('Ctrl Pts',(-0.225659827915283,-4.91349901821122,
26.0643313804438));
#28541=CARTESIAN_POINT('Ctrl Pts',(-0.101281824537473,-4.91756756016072,
26.071382255988));
#28542=CARTESIAN_POINT('Ctrl Pts',(-0.0417382149532846,-4.91843334272117,
26.0747627611501));
#28543=CARTESIAN_POINT('Ctrl Pts',(0.234591691365004,-4.91743291183178,
26.0904821790489));
#28544=CARTESIAN_POINT('Ctrl Pts',(0.451086288873915,-4.90231563740987,
26.1028989425571));
#28545=CARTESIAN_POINT('Ctrl Pts',(0.729249590932683,-4.86430568448546,
26.1189585800842));
#28546=CARTESIAN_POINT('Ctrl Pts',(0.792452379629289,-4.85440975576246,
26.1226137092565));
#28547=CARTESIAN_POINT('Ctrl Pts',(0.860793676013052,-4.84233898201005,
26.1265694001584));
#28548=CARTESIAN_POINT('Ctrl Pts',(0.866141335162508,-4.84138531382986,
26.1268789522083));
#28549=CARTESIAN_POINT('Ctrl Pts',(0.874551674958665,-4.83987108551856,
26.1273658202207));
#28550=CARTESIAN_POINT('Ctrl Pts',(0.877615419377672,-4.83931647366641,
26.1275431844897));
#28551=CARTESIAN_POINT('Ctrl Pts',(0.882438829332563,-4.83843858862532,
26.1278224277101));
#28552=CARTESIAN_POINT('Ctrl Pts',(0.884198847748647,-4.83811726408688,
26.1279243230252));
#28553=CARTESIAN_POINT('Ctrl Pts',(0.886972856960731,-4.8376092521557,26.12808492582));
#28554=CARTESIAN_POINT('Ctrl Pts',(0.887986964688287,-4.83742320621956,
26.1281436387854));
#28555=CARTESIAN_POINT('Ctrl Pts',(0.893133086309332,-4.83647743749058,
26.1284415827391));
#28556=CARTESIAN_POINT('Ctrl Pts',(0.897264186507807,-4.83571273887016,
26.1286807705489));
#28557=CARTESIAN_POINT('Ctrl Pts',(0.904777232580385,-4.83431205694023,
26.1291157875209));
#28558=CARTESIAN_POINT('Ctrl Pts',(0.908159499733299,-4.83367781586063,
26.1293116322337));
#28559=CARTESIAN_POINT('Ctrl Pts',(0.914339297063946,-4.83251226804212,
26.1296694736812));
#28560=CARTESIAN_POINT('Ctrl Pts',(0.917137036981733,-4.83198208050818,
26.1298314807881));
#28561=CARTESIAN_POINT('Ctrl Pts',(0.952632174762279,-4.82522361277532,
26.1318869216686));
#28562=CARTESIAN_POINT('Ctrl Pts',(0.985266196142221,-4.81866594857339,
26.1337771670697));
#28563=CARTESIAN_POINT('Ctrl Pts',(1.05808748839538,-4.80326212061486,26.1379949237472));
#28564=CARTESIAN_POINT('Ctrl Pts',(1.09823546317319,-4.79424186320412,26.1403199402036));
#28565=CARTESIAN_POINT('Ctrl Pts',(1.28373735212449,-4.75011169454736,26.1510724301594));
#28566=CARTESIAN_POINT('Ctrl Pts',(1.42755670843052,-4.7088879343418,26.1594393002119));
#28567=CARTESIAN_POINT('Ctrl Pts',(1.71143664854336,-4.61331422892605,26.1762199744508));
#28568=CARTESIAN_POINT('Ctrl Pts',(1.85133244635808,-4.55897477595555,26.1846252365243));
#28569=CARTESIAN_POINT('Ctrl Pts',(2.05452876874757,-4.46915008430794,26.1971434030274));
#28570=CARTESIAN_POINT('Ctrl Pts',(2.1198821306596,-4.43852346288277,26.2012184279503));
#28571=CARTESIAN_POINT('Ctrl Pts',(2.25009330177091,-4.37397039416366,26.20944709754));
#28572=CARTESIAN_POINT('Ctrl Pts',(2.31491523994003,-4.34001199742697,26.2136000244399));
#28573=CARTESIAN_POINT('Ctrl Pts',(2.51357490332917,-4.23022243736658,26.2265147976526));
#28574=CARTESIAN_POINT('Ctrl Pts',(2.6446293533403,-4.1495512085368,26.2353072501324));
#28575=CARTESIAN_POINT('Ctrl Pts',(2.88713303167341,-3.98411553545176,26.2521118233183));
#28576=CARTESIAN_POINT('Ctrl Pts',(2.99917130923328,-3.90047251353154,26.2601137333992));
#28577=CARTESIAN_POINT('Ctrl Pts',(3.13986554985452,-3.78578544069449,26.2704450151212));
#28578=CARTESIAN_POINT('Ctrl Pts',(3.17189798434813,-3.758987936902,26.272817110337));
#28579=CARTESIAN_POINT('Ctrl Pts',(3.23618731368198,-3.70379817253545,26.2776164356285));
#28580=CARTESIAN_POINT('Ctrl Pts',(3.26842124194076,-3.67538458879895,26.2800431605997));
#28581=CARTESIAN_POINT('Ctrl Pts',(3.38062651664995,-3.57383422029942,26.2885730710926));
#28582=CARTESIAN_POINT('Ctrl Pts',(3.45854956636096,-3.49847996069592,26.2946482350454));
#28583=CARTESIAN_POINT('Ctrl Pts',(3.64587904095812,-3.30494520139774,26.3097404047203));
#28584=CARTESIAN_POINT('Ctrl Pts',(3.75209073661534,-3.18385164988183,26.3187467637863));
#28585=CARTESIAN_POINT('Ctrl Pts',(3.90158449887951,-2.99551965493498,26.3322748885748));
#28586=CARTESIAN_POINT('Ctrl Pts',(3.94948008914669,-2.93208226831146,26.3367559177101));
#28587=CARTESIAN_POINT('Ctrl Pts',(4.03607887990098,-2.81140872363503,26.3451550564722));
#28588=CARTESIAN_POINT('Ctrl Pts',(4.07515431866081,-2.75446344510613,26.3490689653624));
#28589=CARTESIAN_POINT('Ctrl Pts',(4.17586748288883,-2.60085617079348,26.3595050471999));
#28590=CARTESIAN_POINT('Ctrl Pts',(4.23534647895956,-2.50283074145014,26.3660414440821));
#28591=CARTESIAN_POINT('Ctrl Pts',(4.36011015746943,-2.2800073449136,26.380640774059));
#28592=CARTESIAN_POINT('Ctrl Pts',(4.42357082275289,-2.15430155508098,26.3887061156512));
#28593=CARTESIAN_POINT('Ctrl Pts',(4.51259338007746,-1.95738650523794,26.4010583221707));
#28594=CARTESIAN_POINT('Ctrl Pts',(4.542052407799,-1.88802041228342,26.4053575015165));
#28595=CARTESIAN_POINT('Ctrl Pts',(4.58372911427865,-1.78325793209245,26.4117648966076));
#28596=CARTESIAN_POINT('Ctrl Pts',(4.59715532277651,-1.74835478078894,26.4138854410428));
#28597=CARTESIAN_POINT('Ctrl Pts',(4.62834401390971,-1.66443169034465,26.4189498397435));
#28598=CARTESIAN_POINT('Ctrl Pts',(4.64572764167704,-1.61527580757656,26.4218892312632));
#28599=CARTESIAN_POINT('Ctrl Pts',(4.71423170970352,-1.41130490566337,26.4339958058489));
#28600=CARTESIAN_POINT('Ctrl Pts',(4.75842065735715,-1.25427101848321,26.4431067195492));
#28601=CARTESIAN_POINT('Ctrl Pts',(4.81481354507434,-1.00741564395819,26.4573007741237));
#28602=CARTESIAN_POINT('Ctrl Pts',(4.83247565071357,-0.918963898365818,
26.4623610283136));
#28603=CARTESIAN_POINT('Ctrl Pts',(4.8609006102615,-0.752960594551082,26.4718384525242));
#28604=CARTESIAN_POINT('Ctrl Pts',(4.87226325181618,-0.675540531863483,
26.4762506224585));
#28605=CARTESIAN_POINT('Ctrl Pts',(4.89011642676261,-0.529767593658105,
26.4845567575378));
#28606=CARTESIAN_POINT('Ctrl Pts',(4.89703209295423,-0.461485545991866,
26.4884468296596));
#28607=CARTESIAN_POINT('Ctrl Pts',(4.91200254672783,-0.274773983746103,
26.4990905819884));
#28608=CARTESIAN_POINT('Ctrl Pts',(4.91720269088325,-0.156162962670973,
26.5058602653956));
#28609=CARTESIAN_POINT('Ctrl Pts',(4.91914573379363,0.0987920828655218,
26.5204390560551));
#28610=CARTESIAN_POINT('Ctrl Pts',(4.9145199352676,0.235049807511419,26.528247709637));
#28611=CARTESIAN_POINT('Ctrl Pts',(4.90017711414828,0.424678402147387,26.5391168377062));
#28612=CARTESIAN_POINT('Ctrl Pts',(4.89522942812055,0.478347583147858,26.5421929967283));
#28613=CARTESIAN_POINT('Ctrl Pts',(4.88467037024237,0.575405393523894,26.5477523830584));
#28614=CARTESIAN_POINT('Ctrl Pts',(4.87936024028821,0.61882121655799,26.5502378518366));
#28615=CARTESIAN_POINT('Ctrl Pts',(4.86793498053317,0.702910586215343,26.5550466184873));
#28616=CARTESIAN_POINT('Ctrl Pts',(4.86188736587435,0.743589639034716,26.5573703689379));
#28617=CARTESIAN_POINT('Ctrl Pts',(4.83143540358408,0.932134065475232,26.5681403476853));
#28618=CARTESIAN_POINT('Ctrl Pts',(4.80079073392387,1.07891211142336,26.5765256467456));
#28619=CARTESIAN_POINT('Ctrl Pts',(4.72693526481078,1.36632375563199,26.5931501917273));
#28620=CARTESIAN_POINT('Ctrl Pts',(4.68402463959099,1.50687427726627,26.6013807250745));
#28621=CARTESIAN_POINT('Ctrl Pts',(4.61052791486324,1.71391904922801,26.6137579780051));
#28622=CARTESIAN_POINT('Ctrl Pts',(4.58464580641479,1.78199574295386,26.6178693593295));
#28623=CARTESIAN_POINT('Ctrl Pts',(4.53331723578677,1.90847385561338,26.6255964773817));
#28624=CARTESIAN_POINT('Ctrl Pts',(4.50822918027319,1.9670046169679,26.629208851209));
#28625=CARTESIAN_POINT('Ctrl Pts',(4.41576030385953,2.17166644270623,26.6419776718008));
#28626=CARTESIAN_POINT('Ctrl Pts',(4.34235331671887,2.31496017985609,26.6511724253238));
#28627=CARTESIAN_POINT('Ctrl Pts',(4.21167834579522,2.54187716135869,26.6661615330596));
#28628=CARTESIAN_POINT('Ctrl Pts',(4.15861871017481,2.62778700683347,26.6719418772543));
#28629=CARTESIAN_POINT('Ctrl Pts',(4.06767856992004,2.76536910764251,26.6813601378892));
#28630=CARTESIAN_POINT('Ctrl Pts',(4.03136622085359,2.81804219039155,26.6850061787983));
#28631=CARTESIAN_POINT('Ctrl Pts',(3.97235678848928,2.90016290534226,26.6907493160788));
#28632=CARTESIAN_POINT('Ctrl Pts',(3.95033592998315,2.93008693012193,26.6928544350659));
#28633=CARTESIAN_POINT('Ctrl Pts',(3.89257787131946,3.00673924381634,26.6982798803932));
#28634=CARTESIAN_POINT('Ctrl Pts',(3.85633758185636,3.05308105731361,26.70159325527));
#28635=CARTESIAN_POINT('Ctrl Pts',(3.70678678051953,3.23740484613984,26.7149364741965));
#28636=CARTESIAN_POINT('Ctrl Pts',(3.58683284525733,3.3698203452651,26.7249072239713));
#28637=CARTESIAN_POINT('Ctrl Pts',(3.40327167194179,3.5515185244322,26.7393977259043));
#28638=CARTESIAN_POINT('Ctrl Pts',(3.34524290805063,3.60622955867942,26.7438777186817));
#28639=CARTESIAN_POINT('Ctrl Pts',(3.23139855942059,3.70845165417342,26.752496386426));
#28640=CARTESIAN_POINT('Ctrl Pts',(3.17580067471761,3.75617361557201,26.7566321014895));
#28641=CARTESIAN_POINT('Ctrl Pts',(3.07013305238742,3.84284876891761,26.7643682024507));
#28642=CARTESIAN_POINT('Ctrl Pts',(3.02033536837647,3.88210996381428,26.7679650237071));
#28643=CARTESIAN_POINT('Ctrl Pts',(2.86426643508893,4.00033584702172,26.7790958408212));
#28644=CARTESIAN_POINT('Ctrl Pts',(2.75555660580643,4.07598038924907,26.7866531499899));
#28645=CARTESIAN_POINT('Ctrl Pts',(2.51700580286307,4.22806362256582,26.802839336601));
#28646=CARTESIAN_POINT('Ctrl Pts',(2.38643430220917,4.30311188126951,26.8114653101268));
#28647=CARTESIAN_POINT('Ctrl Pts',(2.20574939255053,4.39620671937522,26.8230577787829));
#28648=CARTESIAN_POINT('Ctrl Pts',(2.15848624081726,4.41960418392969,26.8260592723019));
#28649=CARTESIAN_POINT('Ctrl Pts',(2.07684420374067,4.45839872436785,26.8311878713766));
#28650=CARTESIAN_POINT('Ctrl Pts',(2.04264841659635,4.47416902981631,26.8333189737312));
#28651=CARTESIAN_POINT('Ctrl Pts',(1.9557553649703,4.51303824362907,26.8386945536448));
#28652=CARTESIAN_POINT('Ctrl Pts',(1.90282765404571,4.53560803664727,26.8419329612138));
#28653=CARTESIAN_POINT('Ctrl Pts',(1.69357365133645,4.62053185482621,26.8546215721765));
#28654=CARTESIAN_POINT('Ctrl Pts',(1.53448539735802,4.67577387874527,26.8640236731188));
#28655=CARTESIAN_POINT('Ctrl Pts',(1.29536194768947,4.74528577345838,26.8779932710233));
#28656=CARTESIAN_POINT('Ctrl Pts',(1.21730286033883,4.76590738805358,26.8825278833075));
#28657=CARTESIAN_POINT('Ctrl Pts',(1.06704415092572,4.80167014653708,26.8912274125101));
#28658=CARTESIAN_POINT('Ctrl Pts',(0.994941911260006,4.81712672050747,26.8953891865255));
#28659=CARTESIAN_POINT('Ctrl Pts',(0.860488589443576,4.84280194404223,26.9031366822528));
#28660=CARTESIAN_POINT('Ctrl Pts',(0.798235177612503,4.85345153192027,26.9067186302735));
#28661=CARTESIAN_POINT('Ctrl Pts',(0.614608929264103,4.88123560884879,26.9172754554385));
#28662=CARTESIAN_POINT('Ctrl Pts',(0.492781691930183,4.89503532013962,26.9242692969759));
#28663=CARTESIAN_POINT('Ctrl Pts',(0.189299844147326,4.91796647922178,26.9416768905423));
#28664=CARTESIAN_POINT('Ctrl Pts',(0.00741124822885696,4.92160283021055,
26.9521002709487));
#28665=CARTESIAN_POINT('Ctrl Pts',(-0.217658076684673,4.913623276149,26.9649235858452));
#28666=CARTESIAN_POINT('Ctrl Pts',(-0.261033246241738,4.91150999605861,
26.9673911142584));
#28667=CARTESIAN_POINT('Ctrl Pts',(-0.340050833136463,4.90661045407957,
26.9718770381134));
#28668=CARTESIAN_POINT('Ctrl Pts',(-0.375701643491329,4.90400948423775,
26.9738974383605));
#28669=CARTESIAN_POINT('Ctrl Pts',(-0.491658626285695,4.89427772315574,
26.9804626746688));
#28670=CARTESIAN_POINT('Ctrl Pts',(-0.571818979186006,4.8855609641989,26.9849915547972));
#28671=CARTESIAN_POINT('Ctrl Pts',(-0.801651984965655,4.85483425670535,
26.9979981257927));
#28672=CARTESIAN_POINT('Ctrl Pts',(-0.950569965781884,4.8278854908312,27.0064540580447));
#28673=CARTESIAN_POINT('Ctrl Pts',(-1.14467393831461,4.78342936621185,27.0176311561061));
#28674=CARTESIAN_POINT('Ctrl Pts',(-1.19118034920191,4.77206079887855,27.0203208314883));
#28675=CARTESIAN_POINT('Ctrl Pts',(-1.31421137649138,4.74007507728931,27.0274730647507));
#28676=CARTESIAN_POINT('Ctrl Pts',(-1.39041576096083,4.71828433768648,27.0319413595728));
#28677=CARTESIAN_POINT('Ctrl Pts',(-1.53203342596999,4.67405965262473,27.040331209171));
#28678=CARTESIAN_POINT('Ctrl Pts',(-1.59756500433706,4.65206899845181,27.0442486564887));
#28679=CARTESIAN_POINT('Ctrl Pts',(-1.7751779802153,4.58827118192,27.0549716373847));
#28680=CARTESIAN_POINT('Ctrl Pts',(-1.88623141693507,4.5437451225111,27.0617934797819));
#28681=CARTESIAN_POINT('Ctrl Pts',(-2.12047679604748,4.43975715565054,27.0764478925027));
#28682=CARTESIAN_POINT('Ctrl Pts',(-2.24303742141698,4.37911504145828,27.0842798403112));
#28683=CARTESIAN_POINT('Ctrl Pts',(-2.41023352067622,4.28752477156363,27.0951758467351));
#28684=CARTESIAN_POINT('Ctrl Pts',(-2.45712482674021,4.26082526582539,27.0982556273639));
#28685=CARTESIAN_POINT('Ctrl Pts',(-2.54124283435571,4.21107869534848,27.1038205485562));
#28686=CARTESIAN_POINT('Ctrl Pts',(-2.57861928832987,4.18829578077866,27.1063079375272));
#28687=CARTESIAN_POINT('Ctrl Pts',(-2.65049120055705,4.14315924749024,27.1111171747242));
#28688=CARTESIAN_POINT('Ctrl Pts',(-2.68502037060214,4.12086614758497,27.1134394906808));
#28689=CARTESIAN_POINT('Ctrl Pts',(-2.80913679515193,4.03851040077335,27.1218392195867));
#28690=CARTESIAN_POINT('Ctrl Pts',(-2.8970223957585,3.97593731245132,27.1278873569205));
#28691=CARTESIAN_POINT('Ctrl Pts',(-2.99065558434452,3.90451793965808,27.134486478428));
#28692=CARTESIAN_POINT('Ctrl Pts',(-2.99851268673053,3.89848724929369,27.1350414598712));
#28693=CARTESIAN_POINT('Ctrl Pts',(-3.14411574666091,3.78602956644793,27.1453493582073));
#28694=CARTESIAN_POINT('Ctrl Pts',(-3.27613278389825,3.67238844288121,27.1550890698183));
#28695=CARTESIAN_POINT('Ctrl Pts',(-3.45534262376687,3.50075382597196,27.1690642405637));
#28696=CARTESIAN_POINT('Ctrl Pts',(-3.50767444370431,3.44831695537903,27.1732449953358));
#28697=CARTESIAN_POINT('Ctrl Pts',(-3.60811517231498,3.3430214468718,27.181480680634));
#28698=CARTESIAN_POINT('Ctrl Pts',(-3.65629604267182,3.29025630919129,27.1855338221875));
#28699=CARTESIAN_POINT('Ctrl Pts',(-3.82946513058828,3.0921081296754,27.2004996309676));
#28700=CARTESIAN_POINT('Ctrl Pts',(-3.94707078820502,2.94050442093864,27.2114682040348));
#28701=CARTESIAN_POINT('Ctrl Pts',(-4.10059238470354,2.71673904660358,27.227001027709));
#28702=CARTESIAN_POINT('Ctrl Pts',(-4.14405712253853,2.64996597019552,27.2315581508474));
#28703=CARTESIAN_POINT('Ctrl Pts',(-4.20005209579265,2.55919401502383,27.2376435628737));
#28704=CARTESIAN_POINT('Ctrl Pts',(-4.21403390123245,2.53610526270841,27.2391821707683));
#28705=CARTESIAN_POINT('Ctrl Pts',(-4.24973472362664,2.47604052547092,27.243160224577));
#28706=CARTESIAN_POINT('Ctrl Pts',(-4.27116161117316,2.43889328452574,27.2455966174518));
#28707=CARTESIAN_POINT('Ctrl Pts',(-4.31252859415273,2.36495889888351,27.2503965622793));
#28708=CARTESIAN_POINT('Ctrl Pts',(-4.33249050729194,2.32818803435896,27.2527601703785));
#28709=CARTESIAN_POINT('Ctrl Pts',(-4.41608745863257,2.16939891621032,27.2628775788631));
#28710=CARTESIAN_POINT('Ctrl Pts',(-4.47505587469502,2.04499287394127,27.2705816853467));
#28711=CARTESIAN_POINT('Ctrl Pts',(-4.59136235872545,1.77041276027475,27.2872868489375));
#28712=CARTESIAN_POINT('Ctrl Pts',(-4.64671467407092,1.61957140937564,27.2962808524593));
#28713=CARTESIAN_POINT('Ctrl Pts',(-4.71606775494272,1.39752583687116,27.309388817397));
#28714=CARTESIAN_POINT('Ctrl Pts',(-4.73603295104073,1.32829411728723,27.313457166485));
#28715=CARTESIAN_POINT('Ctrl Pts',(-4.75770540297722,1.24642777435912,27.3182521627716));
#28716=CARTESIAN_POINT('Ctrl Pts',(-4.76089362727495,1.23419397003609,27.3189682926657));
#28717=CARTESIAN_POINT('Ctrl Pts',(-4.76403458719828,1.22194824541733,27.3196847251172));
#28718=CARTESIAN_POINT('Origin',(0.,0.,-3.23514056400928));
#28719=CARTESIAN_POINT('',(-4.76403458343061,1.22194826010642,29.4150832822139));
#28720=CARTESIAN_POINT('',(-4.76403458843593,1.2219482405921,29.0701077704777));
#28721=CARTESIAN_POINT('',(-4.76403458704967,1.22194824599672,-3.23514056400928));
#28722=CARTESIAN_POINT('Ctrl Pts',(-4.76403458343061,1.22194826010642,29.4150832822139));
#28723=CARTESIAN_POINT('Ctrl Pts',(-4.75082584336757,1.27344544416756,29.4121019759593));
#28724=CARTESIAN_POINT('Ctrl Pts',(-4.73678161207201,1.32473039678181,29.4091233894005));
#28725=CARTESIAN_POINT('Ctrl Pts',(-4.68989367983414,1.48565729250495,29.3997331065548));
#28726=CARTESIAN_POINT('Ctrl Pts',(-4.65405535264088,1.59438040222996,29.3933236026385));
#28727=CARTESIAN_POINT('Ctrl Pts',(-4.5842473291198,1.78367109953656,29.3819867965666));
#28728=CARTESIAN_POINT('Ctrl Pts',(-4.55186153069621,1.86476875787112,29.3770706029348));
#28729=CARTESIAN_POINT('Ctrl Pts',(-4.49658445658056,1.99315440738091,29.3691746899046));
#28730=CARTESIAN_POINT('Ctrl Pts',(-4.47506460434152,2.04101273644553,29.3662056059117));
#28731=CARTESIAN_POINT('Ctrl Pts',(-4.41840090257451,2.16182149582261,29.3586406872943));
#28732=CARTESIAN_POINT('Ctrl Pts',(-4.38221394979193,2.23426484378479,29.3540381212687));
#28733=CARTESIAN_POINT('Ctrl Pts',(-4.25402715683615,2.47577786470135,29.3384558359654));
#28734=CARTESIAN_POINT('Ctrl Pts',(-4.15389876209381,2.64033084521303,29.3274286720098));
#28735=CARTESIAN_POINT('Ctrl Pts',(-4.00976788111575,2.84862181633944,29.3129425178816));
#28736=CARTESIAN_POINT('Ctrl Pts',(-3.97422233823533,2.89800648793335,29.3094669669052));
#28737=CARTESIAN_POINT('Ctrl Pts',(-3.91546259315499,2.97652850453381,29.303878226607));
#28738=CARTESIAN_POINT('Ctrl Pts',(-3.89281773616238,3.00608372522347,29.3017599355913));
#28739=CARTESIAN_POINT('Ctrl Pts',(-3.85979261480422,3.04818782764127,29.2987220076966));
#28740=CARTESIAN_POINT('Ctrl Pts',(-3.84968231971051,3.06094660238635,29.2977987136193));
#28741=CARTESIAN_POINT('Ctrl Pts',(-3.81364002311545,3.10596945523011,29.2945312207628));
#28742=CARTESIAN_POINT('Ctrl Pts',(-3.7873641024971,3.1379562913966,29.2921926494902));
#28743=CARTESIAN_POINT('Ctrl Pts',(-3.65545957550888,3.29445883444423,29.2806525508195));
#28744=CARTESIAN_POINT('Ctrl Pts',(-3.54407850142492,3.41399363134801,29.2715230835065));
#28745=CARTESIAN_POINT('Ctrl Pts',(-3.35529150774579,3.5973858078391,29.2567757000638));
#28746=CARTESIAN_POINT('Ctrl Pts',(-3.2815211618636,3.66480346020288,29.2511743138697));
#28747=CARTESIAN_POINT('Ctrl Pts',(-3.14452200048387,3.78254971726782,29.2410160553056));
#28748=CARTESIAN_POINT('Ctrl Pts',(-3.08200894919188,3.83365642771109,29.2364667532505));
#28749=CARTESIAN_POINT('Ctrl Pts',(-2.96738571182935,3.92274878474073,29.2282618180793));
#28750=CARTESIAN_POINT('Ctrl Pts',(-2.9157326205245,3.96129261211287,29.2246119273679));
#28751=CARTESIAN_POINT('Ctrl Pts',(-2.78609656380595,4.05411817099791,29.2155605683656));
#28752=CARTESIAN_POINT('Ctrl Pts',(-2.70727015443826,4.10717618130111,29.2101508682175));
#28753=CARTESIAN_POINT('Ctrl Pts',(-2.48719807153855,4.24621693888233,29.1952893204701));
#28754=CARTESIAN_POINT('Ctrl Pts',(-2.3430759033633,4.32741347774685,29.1858158160558));
#28755=CARTESIAN_POINT('Ctrl Pts',(-2.14345300429715,4.42697734971275,29.1730611964079));
#28756=CARTESIAN_POINT('Ctrl Pts',(-2.09131518082595,4.45184457596452,29.1697627445903));
#28757=CARTESIAN_POINT('Ctrl Pts',(-1.997716071379,4.49447959439262,29.1639034027648));
#28758=CARTESIAN_POINT('Ctrl Pts',(-1.95642550501508,4.51260630152774,29.161339700742));
#28759=CARTESIAN_POINT('Ctrl Pts',(-1.89493118927968,4.53859983222549,29.1575547135367));
#28760=CARTESIAN_POINT('Ctrl Pts',(-1.87491566104948,4.54690487237889,29.1563279768096));
#28761=CARTESIAN_POINT('Ctrl Pts',(-1.80349534186036,4.57598751204332,29.1519682444504));
#28762=CARTESIAN_POINT('Ctrl Pts',(-1.75179456962918,4.59602796441462,29.1488442631436));
#28763=CARTESIAN_POINT('Ctrl Pts',(-1.54469427979363,4.6723026010606,29.136433634258));
#28764=CARTESIAN_POINT('Ctrl Pts',(-1.38684215392434,4.72156346145487,29.1271998802425));
#28765=CARTESIAN_POINT('Ctrl Pts',(-1.14372278208686,4.78418673568879,29.1131227926476));
#28766=CARTESIAN_POINT('Ctrl Pts',(-1.06009065201677,4.80341047135995,29.1083063374818));
#28767=CARTESIAN_POINT('Ctrl Pts',(-0.948245608302949,4.82605585951622,
29.1018826139212));
#28768=CARTESIAN_POINT('Ctrl Pts',(-0.920444222794154,4.83143532676495,
29.1002873237115));
#28769=CARTESIAN_POINT('Ctrl Pts',(-0.834829466712585,4.84723567528032,
29.0953779563197));
#28770=CARTESIAN_POINT('Ctrl Pts',(-0.776874931367547,4.85686104231159,
29.0920593253163));
#28771=CARTESIAN_POINT('Ctrl Pts',(-0.647467285981693,4.87597816647436,
29.0846534864372));
#28772=CARTESIAN_POINT('Ctrl Pts',(-0.575950000280785,4.88494200591665,
29.0805635427757));
#28773=CARTESIAN_POINT('Ctrl Pts',(-0.320595731570073,4.91126187245817,
29.0659594553486));
#28774=CARTESIAN_POINT('Ctrl Pts',(-0.136010932940788,4.91983477811692,
29.0553953648375));
#28775=CARTESIAN_POINT('Ctrl Pts',(0.128969922322148,4.9172154037837,29.0402273090635));
#28776=CARTESIAN_POINT('Ctrl Pts',(0.209293466004387,4.91445184518138,29.035630124057));
#28777=CARTESIAN_POINT('Ctrl Pts',(0.331999682883111,4.90721617874198,29.0286163117156));
#28778=CARTESIAN_POINT('Ctrl Pts',(0.374451813036639,4.90415948940137,29.0261914875896));
#28779=CARTESIAN_POINT('Ctrl Pts',(0.444122588101571,4.89823303472761,29.0222165631893));
#28780=CARTESIAN_POINT('Ctrl Pts',(0.471366341021327,4.89568642010676,29.0206633895326));
#28781=CARTESIAN_POINT('Ctrl Pts',(0.533789692564847,4.8893254835398,29.0171080507327));
#28782=CARTESIAN_POINT('Ctrl Pts',(0.568952290553136,4.8853585783892,29.015107954135));
#28783=CARTESIAN_POINT('Ctrl Pts',(0.682748953676971,4.87127521771701,29.0086383936479));
#28784=CARTESIAN_POINT('Ctrl Pts',(0.761182511036733,4.85963679702101,29.0041843237681));
#28785=CARTESIAN_POINT('Ctrl Pts',(0.879189315227419,4.83919910814305,28.9974659577898));
#28786=CARTESIAN_POINT('Ctrl Pts',(0.918990840490816,4.83179859963066,28.9951970610114));
#28787=CARTESIAN_POINT('Ctrl Pts',(1.11574588411971,4.79269578224991,28.9839568545066));
#28788=CARTESIAN_POINT('Ctrl Pts',(1.2711762602996,4.75383341187199,28.9749977294899));
#28789=CARTESIAN_POINT('Ctrl Pts',(1.49978563207011,4.68465837064174,28.9615593314483));
#28790=CARTESIAN_POINT('Ctrl Pts',(1.57457944470942,4.6600515412891,28.9571204311089));
#28791=CARTESIAN_POINT('Ctrl Pts',(1.71315975420425,4.61074187319669,28.9488026946925));
#28792=CARTESIAN_POINT('Ctrl Pts',(1.77708439254845,4.58648317189403,28.9449279747287));
#28793=CARTESIAN_POINT('Ctrl Pts',(1.94791002130315,4.5175490791475,28.9344623280718));
#28794=CARTESIAN_POINT('Ctrl Pts',(2.05377163748794,4.47041660688822,28.9278564696221));
#28795=CARTESIAN_POINT('Ctrl Pts',(2.28381650759807,4.35809700366819,28.9132212837328));
#28796=CARTESIAN_POINT('Ctrl Pts',(2.40707758460842,4.29124746150916,28.9051901541277));
#28797=CARTESIAN_POINT('Ctrl Pts',(2.57392232021584,4.19130750527635,28.8940737030792));
#28798=CARTESIAN_POINT('Ctrl Pts',(2.62006419385679,4.16261917593578,28.8909724060079));
#28799=CARTESIAN_POINT('Ctrl Pts',(2.70259286869878,4.10939166475372,28.8853798551658));
#28800=CARTESIAN_POINT('Ctrl Pts',(2.73914463873038,4.08511869793034,28.8828863050773));
#28801=CARTESIAN_POINT('Ctrl Pts',(2.80419498356768,4.04065500701107,28.8784208550286));
#28802=CARTESIAN_POINT('Ctrl Pts',(2.83281234032829,4.0206438116517,28.8764466805228));
#28803=CARTESIAN_POINT('Ctrl Pts',(2.92273426468888,3.95632763152877,28.8702077623125));
#28804=CARTESIAN_POINT('Ctrl Pts',(2.98323148779616,3.91091217116087,28.865956981962));
#28805=CARTESIAN_POINT('Ctrl Pts',(3.19073765697843,3.74751911508068,28.8511373988682));
#28806=CARTESIAN_POINT('Ctrl Pts',(3.33199236294721,3.62250370720793,28.8406103638568));
#28807=CARTESIAN_POINT('Ctrl Pts',(3.49433961987341,3.4612714790846,28.8277491265928));
#28808=CARTESIAN_POINT('Ctrl Pts',(3.52260509811511,3.43250097306734,28.8254798459358));
#28809=CARTESIAN_POINT('Ctrl Pts',(3.60038496075583,3.35135871342138,28.8191472682971));
#28810=CARTESIAN_POINT('Ctrl Pts',(3.64910650179652,3.29824175468706,28.8150782253401));
#28811=CARTESIAN_POINT('Ctrl Pts',(3.73824307419844,3.19667006027388,28.8074279991796));
#28812=CARTESIAN_POINT('Ctrl Pts',(3.77892734082992,3.14847086682724,28.8038500848095));
#28813=CARTESIAN_POINT('Ctrl Pts',(3.90291797670219,2.99571098362214,28.7926642794351));
#28814=CARTESIAN_POINT('Ctrl Pts',(3.98289523673599,2.88852865508529,28.7850324642389));
#28815=CARTESIAN_POINT('Ctrl Pts',(4.12587220363088,2.6796690481053,28.7705504119382));
#28816=CARTESIAN_POINT('Ctrl Pts',(4.18972615988816,2.57869006361858,28.7637086143219));
#28817=CARTESIAN_POINT('Ctrl Pts',(4.27547465437232,2.43147964609988,28.7539747655522));
#28818=CARTESIAN_POINT('Ctrl Pts',(4.30042347123166,2.38707662618484,28.7510688997632));
#28819=CARTESIAN_POINT('Ctrl Pts',(4.34470492693294,2.30531786396045,28.7457760470853));
#28820=CARTESIAN_POINT('Ctrl Pts',(4.36425667661212,2.26808621327702,28.7433871316244));
#28821=CARTESIAN_POINT('Ctrl Pts',(4.40224367665935,2.19343862986354,28.7386420950249));
#28822=CARTESIAN_POINT('Ctrl Pts',(4.42068526302609,2.15602974686191,28.7362860852714));
#28823=CARTESIAN_POINT('Ctrl Pts',(4.49702822495673,1.9960688725973,28.7262933768309));
#28824=CARTESIAN_POINT('Ctrl Pts',(4.55032673259614,1.87138484245546,28.7187045513967));
#28825=CARTESIAN_POINT('Ctrl Pts',(4.65613028612378,1.59251760921237,28.7019953268884));
#28826=CARTESIAN_POINT('Ctrl Pts',(4.70626642038934,1.43760811619959,28.6928819578242));
#28827=CARTESIAN_POINT('Ctrl Pts',(4.76720336013819,1.21162842505632,28.6796929239233));
#28828=CARTESIAN_POINT('Ctrl Pts',(4.78427446455127,1.14236115624937,28.6756647116931));
#28829=CARTESIAN_POINT('Ctrl Pts',(4.81566182351191,1.00192358554424,28.667516885903));
#28830=CARTESIAN_POINT('Ctrl Pts',(4.82992114587517,0.930758415957353,28.6633978956885));
#28831=CARTESIAN_POINT('Ctrl Pts',(4.87211086684007,0.692998708541581,28.649658617036));
#28832=CARTESIAN_POINT('Ctrl Pts',(4.89303442400027,0.525285032389969,28.6399989006004));
#28833=CARTESIAN_POINT('Ctrl Pts',(4.91438654770056,0.23176079275549,28.6231518094096));
#28834=CARTESIAN_POINT('Ctrl Pts',(4.91869803143934,0.106388047788207,28.615975747272));
#28835=CARTESIAN_POINT('Ctrl Pts',(4.91805402182035,-0.0602012732167473,
28.6064947129578));
#28836=CARTESIAN_POINT('Ctrl Pts',(4.91737739574035,-0.101386193032589,
28.6041553037917));
#28837=CARTESIAN_POINT('Ctrl Pts',(4.91494826580533,-0.185155898626823,
28.5994084498092));
#28838=CARTESIAN_POINT('Ctrl Pts',(4.91315941543167,-0.227736201860754,
28.5970015557087));
#28839=CARTESIAN_POINT('Ctrl Pts',(4.90404400537677,-0.39335244500484,28.5876524074803));
#28840=CARTESIAN_POINT('Ctrl Pts',(4.89264699589848,-0.516119898883973,
28.5807479683299));
#28841=CARTESIAN_POINT('Ctrl Pts',(4.86121339365576,-0.756263048734239,
28.5671794639173));
#28842=CARTESIAN_POINT('Ctrl Pts',(4.84150376345247,-0.873596328068323,
28.5605199581225));
#28843=CARTESIAN_POINT('Ctrl Pts',(4.79940138535841,-1.07845537266142,28.5487701412546));
#28844=CARTESIAN_POINT('Ctrl Pts',(4.77881536090128,-1.16629461163767,28.5436919260915));
#28845=CARTESIAN_POINT('Ctrl Pts',(4.73868641570457,-1.31854323022843,28.5347984421455));
#28846=CARTESIAN_POINT('Ctrl Pts',(4.72021547604169,-1.3832103681458,28.5309916830454));
#28847=CARTESIAN_POINT('Ctrl Pts',(4.67344532373865,-1.53508803583103,28.5219736806671));
#28848=CARTESIAN_POINT('Ctrl Pts',(4.6440222416752,-1.62192588725829,28.5167560722468));
#28849=CARTESIAN_POINT('Ctrl Pts',(4.58912224889926,-1.77018438931629,28.5077341915746));
#28850=CARTESIAN_POINT('Ctrl Pts',(4.56479503071419,-1.8320049237038,28.5039373566651));
#28851=CARTESIAN_POINT('Ctrl Pts',(4.48504799691656,-2.02319861718643,28.4920855497587));
#28852=CARTESIAN_POINT('Ctrl Pts',(4.42532283772658,-2.15069899606934,28.484021710605));
#28853=CARTESIAN_POINT('Ctrl Pts',(4.3331186173798,-2.32737954618943,28.4726467235227));
#28854=CARTESIAN_POINT('Ctrl Pts',(4.30509942384662,-2.37880885568943,28.4693108595645));
#28855=CARTESIAN_POINT('Ctrl Pts',(4.25800538593239,-2.46169146782939,28.4638988307489));
#28856=CARTESIAN_POINT('Ctrl Pts',(4.23948465038511,-2.49345236290626,28.4618164869513));
#28857=CARTESIAN_POINT('Ctrl Pts',(4.18864551776687,-2.57843131621966,28.4562204857773));
#28858=CARTESIAN_POINT('Ctrl Pts',(4.15566981960058,-2.63124833810635,28.4527151949306));
#28859=CARTESIAN_POINT('Ctrl Pts',(4.02684667137273,-2.82911869896542,28.4394477574002));
#28860=CARTESIAN_POINT('Ctrl Pts',(3.92433486848256,-2.96968063394021,28.4297369522528));
#28861=CARTESIAN_POINT('Ctrl Pts',(3.76484475588937,-3.16564987382452,28.4155602963498));
#28862=CARTESIAN_POINT('Ctrl Pts',(3.71363169563772,-3.22557508585818,28.4111319328015));
#28863=CARTESIAN_POINT('Ctrl Pts',(3.61256757647745,-3.33823295370424,28.402606133697));
#28864=CARTESIAN_POINT('Ctrl Pts',(3.56294609548388,-3.39114415914643,28.3985115485807));
#28865=CARTESIAN_POINT('Ctrl Pts',(3.46821995864917,-3.48777516600229,28.3908519508957));
#28866=CARTESIAN_POINT('Ctrl Pts',(3.42341261555455,-3.53176602362439,28.3872904166371));
#28867=CARTESIAN_POINT('Ctrl Pts',(3.28739847880043,-3.66028065542001,28.3766528290028));
#28868=CARTESIAN_POINT('Ctrl Pts',(3.19381649631292,-3.74221575795378,28.3695570047693));
#28869=CARTESIAN_POINT('Ctrl Pts',(2.97791420174895,-3.91724432883539,28.3536589291943));
#28870=CARTESIAN_POINT('Ctrl Pts',(2.85413078134223,-4.00833055703138,28.3448557107084));
#28871=CARTESIAN_POINT('Ctrl Pts',(2.70404869273423,-4.10828646808451,28.3345674504822));
#28872=CARTESIAN_POINT('Ctrl Pts',(2.68168889447427,-4.1229166520633,28.3330443747271));
#28873=CARTESIAN_POINT('Ctrl Pts',(2.62345898189416,-4.16034280572474,28.3291036352203));
#28874=CARTESIAN_POINT('Ctrl Pts',(2.58741042650245,-4.18285747201517,28.3266889765835));
#28875=CARTESIAN_POINT('Ctrl Pts',(2.51577288142438,-4.22631929151112,28.321941617306));
#28876=CARTESIAN_POINT('Ctrl Pts',(2.48020287929744,-4.24729109786057,28.3196088159887));
#28877=CARTESIAN_POINT('Ctrl Pts',(2.32000592830706,-4.33904326669952,28.3091996452963));
#28878=CARTESIAN_POINT('Ctrl Pts',(2.19258353294268,-4.40480446241282,28.3011779419278));
#28879=CARTESIAN_POINT('Ctrl Pts',(1.92174134904492,-4.52991432187993,28.2844642346539));
#28880=CARTESIAN_POINT('Ctrl Pts',(1.77801908751773,-4.58823069536822,28.2757796773237));
#28881=CARTESIAN_POINT('Ctrl Pts',(1.56428110258131,-4.66340305399406,28.2630129381502));
#28882=CARTESIAN_POINT('Ctrl Pts',(1.49626818032756,-4.68566801954334,28.2589722982437));
#28883=CARTESIAN_POINT('Ctrl Pts',(1.35859224421439,-4.72743480499193,28.2508266400555));
#28884=CARTESIAN_POINT('Ctrl Pts',(1.28893619601291,-4.746899623988,28.2467223836671));
#28885=CARTESIAN_POINT('Ctrl Pts',(1.05730812633487,-4.80615181408327,28.2331198366327));
#28886=CARTESIAN_POINT('Ctrl Pts',(0.893743505257881,-4.83923723718358,
28.223583210395));
#28887=CARTESIAN_POINT('Ctrl Pts',(0.639430687359732,-4.87734361969033,
28.2088625556191));
#28888=CARTESIAN_POINT('Ctrl Pts',(0.549691649591653,-4.88827082062962,
28.2036892891148));
#28889=CARTESIAN_POINT('Ctrl Pts',(0.399903521268695,-4.90233287734534,
28.1951008670836));
#28890=CARTESIAN_POINT('Ctrl Pts',(0.340006440079352,-4.9068509464964,28.1916789501077));
#28891=CARTESIAN_POINT('Ctrl Pts',(0.243352693047611,-4.91236327573058,
28.1861820595237));
#28892=CARTESIAN_POINT('Ctrl Pts',(0.206641871403309,-4.91404443027282,
28.1841003788821));
#28893=CARTESIAN_POINT('Ctrl Pts',(0.109335115299174,-4.91740818138489,
28.1785975410169));
#28894=CARTESIAN_POINT('Ctrl Pts',(0.0487209742579251,-4.91838223281956,
28.175184110936));
#28895=CARTESIAN_POINT('Ctrl Pts',(-0.187692170263738,-4.91781039979649,
28.1618972305394));
#28896=CARTESIAN_POINT('Ctrl Pts',(-0.363339583257405,-4.90796010438973,
28.1520783582331));
#28897=CARTESIAN_POINT('Ctrl Pts',(-0.616677363874846,-4.88007623812464,
28.1377786726159));
#28898=CARTESIAN_POINT('Ctrl Pts',(-0.695051742352843,-4.86953159773891,
28.1333362667401));
#28899=CARTESIAN_POINT('Ctrl Pts',(-0.844885963560833,-4.84568148718336,
28.1247896521021));
#28900=CARTESIAN_POINT('Ctrl Pts',(-0.916372183786456,-4.83267247249283,
28.1206883399193));
#28901=CARTESIAN_POINT('Ctrl Pts',(-1.04898444224154,-4.80549147280676,
28.1130259636676));
#28902=CARTESIAN_POINT('Ctrl Pts',(-1.11017852766317,-4.79172413481118,
28.109468431861));
#28903=CARTESIAN_POINT('Ctrl Pts',(-1.29047034106932,-4.74752325757581,
28.0989160919381));
#28904=CARTESIAN_POINT('Ctrl Pts',(-1.40870815750662,-4.71379162498846,
28.0919021062682));
#28905=CARTESIAN_POINT('Ctrl Pts',(-1.66886780773246,-4.62890783711941,
28.0762496413292));
#28906=CARTESIAN_POINT('Ctrl Pts',(-1.80995355126799,-4.57558475579388,
28.0676102402097));
#28907=CARTESIAN_POINT('Ctrl Pts',(-2.00168774356557,-4.49286117612384,
28.0556922182234));
#28908=CARTESIAN_POINT('Ctrl Pts',(-2.05459707093001,-4.46891333115277,
28.0523844514683));
#28909=CARTESIAN_POINT('Ctrl Pts',(-2.14030123789195,-4.42827801956524,
28.0469997925566));
#28910=CARTESIAN_POINT('Ctrl Pts',(-2.17335440202981,-4.41214984870694,
28.0449168938041));
#28911=CARTESIAN_POINT('Ctrl Pts',(-2.26239313806218,-4.36746037239851,
28.0392872755184));
#28912=CARTESIAN_POINT('Ctrl Pts',(-2.31801726630154,-4.3381941994672,28.0357491525871));
#28913=CARTESIAN_POINT('Ctrl Pts',(-2.46725521424797,-4.2559838569226,28.0261756144991));
#28914=CARTESIAN_POINT('Ctrl Pts',(-2.55971819137861,-4.2010224823229,28.0201554799623));
#28915=CARTESIAN_POINT('Ctrl Pts',(-2.77277881973725,-4.06472858171268,
28.0059856983017));
#28916=CARTESIAN_POINT('Ctrl Pts',(-2.8917168285538,-3.98099157645261,27.9978382151075));
#28917=CARTESIAN_POINT('Ctrl Pts',(-3.06393422329267,-3.84794856499916,
27.9855780091501));
#28918=CARTESIAN_POINT('Ctrl Pts',(-3.12011853845704,-3.80253352789468,
27.9814997558853));
#28919=CARTESIAN_POINT('Ctrl Pts',(-3.22998344081184,-3.70965240351697,
27.9733557472801));
#28920=CARTESIAN_POINT('Ctrl Pts',(-3.28366786876934,-3.66221779127964,
27.9692911497143));
#28921=CARTESIAN_POINT('Ctrl Pts',(-3.46519603675754,-3.49462117479818,
27.9552372996803));
#28922=CARTESIAN_POINT('Ctrl Pts',(-3.58763409094668,-3.36880407902093,
27.9452038028274));
#28923=CARTESIAN_POINT('Ctrl Pts',(-3.76027709422345,-3.17128543387896,
27.9301867077049));
#28924=CARTESIAN_POINT('Ctrl Pts',(-3.81572401225558,-3.1043494527562,27.9252134911518));
#28925=CARTESIAN_POINT('Ctrl Pts',(-3.90562272710818,-2.98977316165656,
27.9169009698753));
#28926=CARTESIAN_POINT('Ctrl Pts',(-3.94104672394121,-2.94292087592703,
27.9135553547005));
#28927=CARTESIAN_POINT('Ctrl Pts',(-3.99726567535598,-2.86572881244737,
27.9081337858815));
#28928=CARTESIAN_POINT('Ctrl Pts',(-4.0185741382421,-2.83577087210833,27.9060515934832));
#28929=CARTESIAN_POINT('Ctrl Pts',(-4.07494777897715,-2.75460257606128,
27.9004668685001));
#28930=CARTESIAN_POINT('Ctrl Pts',(-4.10938286800527,-2.70296269616736,
27.8969726252212));
#28931=CARTESIAN_POINT('Ctrl Pts',(-4.23665238355761,-2.50404948110928,
27.8837030140401));
#28932=CARTESIAN_POINT('Ctrl Pts',(-4.32262202227835,-2.35253620214854,
27.8739793669459));
#28933=CARTESIAN_POINT('Ctrl Pts',(-4.43559540137678,-2.1262392522269,27.8597880819054));
#28934=CARTESIAN_POINT('Ctrl Pts',(-4.46911147023485,-2.05485825172903,
27.8553580398559));
#28935=CARTESIAN_POINT('Ctrl Pts',(-4.53014206231349,-1.91631384345852,
27.8468297530431));
#28936=CARTESIAN_POINT('Ctrl Pts',(-4.55791459892568,-1.84928640286371,
27.8427343642298));
#28937=CARTESIAN_POINT('Ctrl Pts',(-4.60693621162391,-1.72315495123165,
27.835074441021));
#28938=CARTESIAN_POINT('Ctrl Pts',(-4.62855565957063,-1.66421051614048,
27.8315133914064));
#28939=CARTESIAN_POINT('Ctrl Pts',(-4.68954478183092,-1.48753507241695,
27.8208882987025));
#28940=CARTESIAN_POINT('Ctrl Pts',(-4.72559198590939,-1.3687112895878,27.8138045739214));
#28941=CARTESIAN_POINT('Ctrl Pts',(-4.79612881753825,-1.09998073693306,
27.7979125073896));
#28942=CARTESIAN_POINT('Ctrl Pts',(-4.82816152421967,-0.949560843799994,
27.7891030807693));
#28943=CARTESIAN_POINT('Ctrl Pts',(-4.8574396520405,-0.771478708199486,
27.7788060671457));
#28944=CARTESIAN_POINT('Ctrl Pts',(-4.86156593947712,-0.745034225156998,
27.7772804870861));
#28945=CARTESIAN_POINT('Ctrl Pts',(-4.87169198966455,-0.67646898112936,
27.7733346555453));
#28946=CARTESIAN_POINT('Ctrl Pts',(-4.87736146312451,-0.634301456955381,
27.7709174104673));
#28947=CARTESIAN_POINT('Ctrl Pts',(-4.88744892573398,-0.551114924222624,
27.766169708302));
#28948=CARTESIAN_POINT('Ctrl Pts',(-4.89189935573698,-0.510103324827477,
27.7638391295451));
#28949=CARTESIAN_POINT('Ctrl Pts',(-4.91076504978367,-0.313183595528192,
27.7526850318103));
#28950=CARTESIAN_POINT('Ctrl Pts',(-4.91824595464928,-0.156700958163355,
27.7439276774648));
#28951=CARTESIAN_POINT('Ctrl Pts',(-4.91825379372826,0.14683102211351,27.7269217677402));
#28952=CARTESIAN_POINT('Ctrl Pts',(-4.91167091055946,0.293713875980202,
27.718683709383));
#28953=CARTESIAN_POINT('Ctrl Pts',(-4.89283750911437,0.503348143663679,
27.7068200120076));
#28954=CARTESIAN_POINT('Ctrl Pts',(-4.88592836520935,0.566499907694041,
27.7032326011517));
#28955=CARTESIAN_POINT('Ctrl Pts',(-4.86865561443171,0.700341104485991,
27.6955935757652));
#28956=CARTESIAN_POINT('Ctrl Pts',(-4.85797112896173,0.770974387565499,
27.6915406377498));
#28957=CARTESIAN_POINT('Ctrl Pts',(-4.83897493905174,0.880382960974645,
27.685224379158));
#28958=CARTESIAN_POINT('Ctrl Pts',(-4.83172631538794,0.919333132115322,
27.6829681573647));
#28959=CARTESIAN_POINT('Ctrl Pts',(-4.80643809105385,1.04664653224309,27.6755675693476));
#28960=CARTESIAN_POINT('Ctrl Pts',(-4.7864392512841,1.13459872400571,27.6704137044303));
#28961=CARTESIAN_POINT('Ctrl Pts',(-4.76403458666814,1.22194824748421,27.665253726697));
#28962=CARTESIAN_POINT('Ctrl Pts',(-4.76403458719828,1.22194824541733,27.3196847251172));
#28963=CARTESIAN_POINT('Ctrl Pts',(-4.77910664015462,1.16318652465431,27.3231225619925));
#28964=CARTESIAN_POINT('Ctrl Pts',(-4.79309037920283,1.10415033058226,27.3265674431487));
#28965=CARTESIAN_POINT('Ctrl Pts',(-4.83800512637114,0.897560678186405,
27.3385971236683));
#28966=CARTESIAN_POINT('Ctrl Pts',(-4.86324160138916,0.7488584231117,27.347214074077));
#28967=CARTESIAN_POINT('Ctrl Pts',(-4.89374282737757,0.500382881879463,
27.3615443944353));
#28968=CARTESIAN_POINT('Ctrl Pts',(-4.9028718385305,0.401185446940015,27.3672467937488));
#28969=CARTESIAN_POINT('Ctrl Pts',(-4.91287943812325,0.238393742513765,
27.3765605922703));
#28970=CARTESIAN_POINT('Ctrl Pts',(-4.91554805580891,0.174938281813134,
27.3801799444996));
#28971=CARTESIAN_POINT('Ctrl Pts',(-4.91782876595764,0.0743157801970953,
27.3858959242168));
#28972=CARTESIAN_POINT('Ctrl Pts',(-4.91824975924163,0.0371746791460664,
27.3880004070586));
#28973=CARTESIAN_POINT('Ctrl Pts',(-4.91825038350036,-0.0591733338559681,
27.3934466552362));
#28974=CARTESIAN_POINT('Ctrl Pts',(-4.9171817109405,-0.118374257695531,
27.3967813210792));
#28975=CARTESIAN_POINT('Ctrl Pts',(-4.91187445633915,-0.265299510453831,
27.4050456816419));
#28976=CARTESIAN_POINT('Ctrl Pts',(-4.9063546617951,-0.352956948820379,
27.4099661560081));
#28977=CARTESIAN_POINT('Ctrl Pts',(-4.88301364469107,-0.612563181497254,
27.4245690237881));
#28978=CARTESIAN_POINT('Ctrl Pts',(-4.8584730876663,-0.783769267478875,
27.4342428868047));
#28979=CARTESIAN_POINT('Ctrl Pts',(-4.81091144111903,-1.02448809335753,
27.4480673149166));
#28980=CARTESIAN_POINT('Ctrl Pts',(-4.79527870697443,-1.09532949785959,
27.4521629199823));
#28981=CARTESIAN_POINT('Ctrl Pts',(-4.76083643912707,-1.23649288348221,
27.4603891778399));
#28982=CARTESIAN_POINT('Ctrl Pts',(-4.74202117946711,-1.3067950173025,27.4645188864308));
#28983=CARTESIAN_POINT('Ctrl Pts',(-4.64245842199569,-1.6482759436614,27.4847555348174));
#28984=CARTESIAN_POINT('Ctrl Pts',(-4.53997421977378,-1.91255445917514,
27.5010039107848));
#28985=CARTESIAN_POINT('Ctrl Pts',(-4.39463029901634,-2.20875940860351,
27.5198042747874));
#28986=CARTESIAN_POINT('Ctrl Pts',(-4.37331470323292,-2.25066927095974,
27.5224778509426));
#28987=CARTESIAN_POINT('Ctrl Pts',(-4.33312522327585,-2.32696078842439,
27.527366802253));
#28988=CARTESIAN_POINT('Ctrl Pts',(-4.31443491596287,-2.36143433030609,
27.5295840067727));
#28989=CARTESIAN_POINT('Ctrl Pts',(-4.24644045659418,-2.48334493347704,
27.537460588288));
#28990=CARTESIAN_POINT('Ctrl Pts',(-4.19487397899062,-2.56949242933904,
27.5430936468505));
#28991=CARTESIAN_POINT('Ctrl Pts',(-4.0231019911428,-2.83748672226185,27.5609372813293));
#28992=CARTESIAN_POINT('Ctrl Pts',(-3.89343225242221,-3.01294948038046,
27.5731146645195));
#28993=CARTESIAN_POINT('Ctrl Pts',(-3.70788460697584,-3.23195765169718,
27.5893012497431));
#28994=CARTESIAN_POINT('Ctrl Pts',(-3.66210834404674,-3.28373580776761,
27.5932064897484));
#28995=CARTESIAN_POINT('Ctrl Pts',(-3.56315170049135,-3.39102333201989,
27.6014757949685));
#28996=CARTESIAN_POINT('Ctrl Pts',(-3.50973027259484,-3.44628531884541,
27.6058411116085));
#28997=CARTESIAN_POINT('Ctrl Pts',(-3.4228426786759,-3.53205001566902,27.6127933091156));
#28998=CARTESIAN_POINT('Ctrl Pts',(-3.39021222726756,-3.56338186800688,
27.6153726607297));
#28999=CARTESIAN_POINT('Ctrl Pts',(-3.25940096587514,-3.68556382399977,
27.6255909525159));
#29000=CARTESIAN_POINT('Ctrl Pts',(-3.15796386571308,-3.77284232720343,
27.6332502647967));
#29001=CARTESIAN_POINT('Ctrl Pts',(-2.97191923716549,-3.92015309130047,
27.6468317229035));
#29002=CARTESIAN_POINT('Ctrl Pts',(-2.88873190932659,-3.98185039197198,
27.652751621383));
#29003=CARTESIAN_POINT('Ctrl Pts',(-2.77000195668949,-4.06422813092343,
27.6609748508818));
#29004=CARTESIAN_POINT('Ctrl Pts',(-2.73605455053267,-4.08715875627356,
27.6633011676505));
#29005=CARTESIAN_POINT('Ctrl Pts',(-2.66510113670529,-4.13380580959951,
27.6681100472185));
#29006=CARTESIAN_POINT('Ctrl Pts',(-2.62805568685837,-4.15745570133223,
27.6705916441454));
#29007=CARTESIAN_POINT('Ctrl Pts',(-2.54454908869513,-4.20920426839388,
27.6761276461851));
#29008=CARTESIAN_POINT('Ctrl Pts',(-2.49792954644835,-4.23703654608929,
27.6791790489374));
#29009=CARTESIAN_POINT('Ctrl Pts',(-2.33045925713928,-4.33329292100694,
27.6900211157437));
#29010=CARTESIAN_POINT('Ctrl Pts',(-2.20718288335394,-4.39736418719206,
27.6977861998675));
#29011=CARTESIAN_POINT('Ctrl Pts',(-1.98447673868918,-4.50138527487068,
27.7115696326598));
#29012=CARTESIAN_POINT('Ctrl Pts',(-1.88614371151672,-4.54346551083741,
27.717574829586));
#29013=CARTESIAN_POINT('Ctrl Pts',(-1.72724240243759,-4.60541685865395,
27.7271894087988));
#29014=CARTESIAN_POINT('Ctrl Pts',(-1.66752417403003,-4.62737439351549,
27.7307829767372));
#29015=CARTESIAN_POINT('Ctrl Pts',(-1.53849391678187,-4.67199475104879,
27.73851258233));
#29016=CARTESIAN_POINT('Ctrl Pts',(-1.46906988242569,-4.69428716614386,
27.742650320869));
#29017=CARTESIAN_POINT('Ctrl Pts',(-1.22864869051116,-4.76563174826191,
27.7569185713084));
#29018=CARTESIAN_POINT('Ctrl Pts',(-1.05550294794784,-4.80694660336261,
27.7670942024636));
#29019=CARTESIAN_POINT('Ctrl Pts',(-0.874285127402896,-4.83992236715171,
27.7776380610375));
#29020=CARTESIAN_POINT('Ctrl Pts',(-0.868065124335707,-4.84104182423246,
27.7779998260933));
#29021=CARTESIAN_POINT('Ctrl Pts',(-0.754704902465243,-4.86121854857971,
27.7845905317701));
#29022=CARTESIAN_POINT('Ctrl Pts',(-0.646962526460831,-4.87672688904921,
27.7908147037166));
#29023=CARTESIAN_POINT('Ctrl Pts',(-0.496658874532557,-4.89329234176036,
27.799422628598));
#29024=CARTESIAN_POINT('Ctrl Pts',(-0.45446533803561,-4.89739127410771,
27.8018308083105));
#29025=CARTESIAN_POINT('Ctrl Pts',(-0.370069509806744,-4.90448989954287,
27.8066287791068));
#29026=CARTESIAN_POINT('Ctrl Pts',(-0.327870910336513,-4.9074915525872,
27.8090183894714));
#29027=CARTESIAN_POINT('Ctrl Pts',(-0.146909841241898,-4.91801904687589,
27.819237007519));
#29028=CARTESIAN_POINT('Ctrl Pts',(-0.00789989540734039,-4.92020652804115,
27.8270158579821));
#29029=CARTESIAN_POINT('Ctrl Pts',(0.284002930291091,-4.91242778017491,
27.8433742517987));
#29030=CARTESIAN_POINT('Ctrl Pts',(0.436713707293883,-4.90121258153072,
27.8519468360676));
#29031=CARTESIAN_POINT('Ctrl Pts',(0.661331175253825,-4.87413410312265,
27.864691344429));
#29032=CARTESIAN_POINT('Ctrl Pts',(0.733805651596501,-4.86375074189372,
27.8688239785514));
#29033=CARTESIAN_POINT('Ctrl Pts',(0.877179276310579,-4.83993211356035,
27.8770509599861));
#29034=CARTESIAN_POINT('Ctrl Pts',(0.948068523726121,-4.82654661819982,
27.8811439799378));
#29035=CARTESIAN_POINT('Ctrl Pts',(1.15863519648576,-4.78196878133797,27.8933870235219));
#29036=CARTESIAN_POINT('Ctrl Pts',(1.29727150988756,-4.74623500225425,27.9015626863158));
#29037=CARTESIAN_POINT('Ctrl Pts',(1.58643060053522,-4.65808600591162,27.9188647782499));
#29038=CARTESIAN_POINT('Ctrl Pts',(1.73636811638668,-4.60429732463017,27.927985182208));
#29039=CARTESIAN_POINT('Ctrl Pts',(1.91707041808016,-4.52938737170299,27.9391141958223));
#29040=CARTESIAN_POINT('Ctrl Pts',(1.95055176319624,-4.5150699669035,27.9411820112999));
#29041=CARTESIAN_POINT('Ctrl Pts',(2.02255444516446,-4.48332953897129,27.9456397871455));
#29042=CARTESIAN_POINT('Ctrl Pts',(2.06101648713512,-4.46577891681136,27.9480278258118));
#29043=CARTESIAN_POINT('Ctrl Pts',(2.22480973452424,-4.3884715576397,27.9582382582339));
#29044=CARTESIAN_POINT('Ctrl Pts',(2.34780725451158,-4.32391754107525,27.9660105519726));
#29045=CARTESIAN_POINT('Ctrl Pts',(2.60049118808474,-4.17733430289584,27.9823754677308));
#29046=CARTESIAN_POINT('Ctrl Pts',(2.72940375384149,-4.09426803169487,27.9909611339227));
#29047=CARTESIAN_POINT('Ctrl Pts',(2.91383420081883,-3.96284125572686,28.003718286534));
#29048=CARTESIAN_POINT('Ctrl Pts',(2.97248648528547,-3.91903872114196,28.0078503109845));
#29049=CARTESIAN_POINT('Ctrl Pts',(3.08696388672708,-3.82949627216603,28.0160772341931));
#29050=CARTESIAN_POINT('Ctrl Pts',(3.14280357230726,-3.78380407513375,28.02017081168));
#29051=CARTESIAN_POINT('Ctrl Pts',(3.32147034195998,-3.63092122824225,28.0335467222205));
#29052=CARTESIAN_POINT('Ctrl Pts',(3.4399764785869,-3.51885134876122,28.0428655863589));
#29053=CARTESIAN_POINT('Ctrl Pts',(3.64559122903578,-3.30407211351771,28.0598866260259));
#29054=CARTESIAN_POINT('Ctrl Pts',(3.73447134754491,-3.2032721210055,28.0675768165405));
#29055=CARTESIAN_POINT('Ctrl Pts',(3.84557456830109,-3.06635008590321,28.0776134155582));
#29056=CARTESIAN_POINT('Ctrl Pts',(3.87161659684506,-3.03340264294529,28.0799989003056));
#29057=CARTESIAN_POINT('Ctrl Pts',(3.92328721785823,-2.96628128885746,28.084797167374));
#29058=CARTESIAN_POINT('Ctrl Pts',(3.94889901175741,-2.93209889512633,28.0872095684976));
#29059=CARTESIAN_POINT('Ctrl Pts',(3.98986705139168,-2.87591091834472,28.0911292349841));
#29060=CARTESIAN_POINT('Ctrl Pts',(4.00549405280397,-2.85410583221753,28.0926393691978));
#29061=CARTESIAN_POINT('Ctrl Pts',(4.10967540892214,-2.70619571221932,28.1028137701286));
#29062=CARTESIAN_POINT('Ctrl Pts',(4.19243997129744,-2.57611624429883,28.1114274060668));
#29063=CARTESIAN_POINT('Ctrl Pts',(4.3307752579448,-2.33432280005618,28.1270417462924));
#29064=CARTESIAN_POINT('Ctrl Pts',(4.38846439105853,-2.22397324877504,28.1340280022549));
#29065=CARTESIAN_POINT('Ctrl Pts',(4.46906365041017,-2.0544232361273,28.1446126969438));
#29066=CARTESIAN_POINT('Ctrl Pts',(4.49511763558463,-1.99677291606188,28.1481863014903));
#29067=CARTESIAN_POINT('Ctrl Pts',(4.54903526955737,-1.87106058262689,28.1559316198618));
#29068=CARTESIAN_POINT('Ctrl Pts',(4.57649907058771,-1.8028437737091,28.1601053044635));
#29069=CARTESIAN_POINT('Ctrl Pts',(4.63073524212418,-1.6588919832399,28.1688588076293));
#29070=CARTESIAN_POINT('Ctrl Pts',(4.65720268325658,-1.58306490147948,28.1734393486251));
#29071=CARTESIAN_POINT('Ctrl Pts',(4.70976921594585,-1.41971558076114,28.1832454113134));
#29072=CARTESIAN_POINT('Ctrl Pts',(4.73531140851136,-1.33204510402438,28.1884715648637));
#29073=CARTESIAN_POINT('Ctrl Pts',(4.78958757012964,-1.12438690326965,28.2007582338738));
#29074=CARTESIAN_POINT('Ctrl Pts',(4.81627724596558,-1.00392680529061,28.2078151586513));
#29075=CARTESIAN_POINT('Ctrl Pts',(4.84572218818662,-0.842507910818403,
28.2171516126431));
#29076=CARTESIAN_POINT('Ctrl Pts',(4.85253542969403,-0.802336009036839,
28.2194652432138));
#29077=CARTESIAN_POINT('Ctrl Pts',(4.8657060745939,-0.718363381883734,28.2242786989092));
#29078=CARTESIAN_POINT('Ctrl Pts',(4.87197301337525,-0.674552127083557,
28.2267774183482));
#29079=CARTESIAN_POINT('Ctrl Pts',(4.88468395043512,-0.576243554208115,
28.2323629679027));
#29080=CARTESIAN_POINT('Ctrl Pts',(4.89080890646822,-0.521710883021132,
28.235446709414));
#29081=CARTESIAN_POINT('Ctrl Pts',(4.90957613459096,-0.32499216151347,28.2465377996089));
#29082=CARTESIAN_POINT('Ctrl Pts',(4.91693984605702,-0.182374478022377,
28.2545184644196));
#29083=CARTESIAN_POINT('Ctrl Pts',(4.91901000778737,0.0744768507860042,
28.2689243698687));
#29084=CARTESIAN_POINT('Ctrl Pts',(4.91595770000967,0.188588645362122,28.2753357668821));
#29085=CARTESIAN_POINT('Ctrl Pts',(4.90470715233717,0.371167568836646,28.2856561716284));
#29086=CARTESIAN_POINT('Ctrl Pts',(4.89903447178249,0.439748470178235,28.2895466610095));
#29087=CARTESIAN_POINT('Ctrl Pts',(4.88360393041411,0.58828634100926,28.2980117794138));
#29088=CARTESIAN_POINT('Ctrl Pts',(4.87331705197115,0.668168286972844,28.3025888262391));
#29089=CARTESIAN_POINT('Ctrl Pts',(4.8366481225033,0.906547112142942,28.3163318323835));
#29090=CARTESIAN_POINT('Ctrl Pts',(4.80445739636777,1.06403993018608,28.3255272030696));
#29091=CARTESIAN_POINT('Ctrl Pts',(4.73761872025567,1.32514335527237,28.340954341513));
#29092=CARTESIAN_POINT('Ctrl Pts',(4.70712491068458,1.42968931271677,28.3471808706842));
#29093=CARTESIAN_POINT('Ctrl Pts',(4.66017496057225,1.57279835443528,28.3557532613764));
#29094=CARTESIAN_POINT('Ctrl Pts',(4.64665897807504,1.61229207254418,28.358124155228));
#29095=CARTESIAN_POINT('Ctrl Pts',(4.61820498123549,1.69210342842257,28.3629236100915));
#29096=CARTESIAN_POINT('Ctrl Pts',(4.60323773958668,1.73240688994969,28.3653516546656));
#29097=CARTESIAN_POINT('Ctrl Pts',(4.57797811034502,1.79778579336996,28.3693021325725));
#29098=CARTESIAN_POINT('Ctrl Pts',(4.56800355722883,1.82298130805904,28.3708274386453));
#29099=CARTESIAN_POINT('Ctrl Pts',(4.52769759397163,1.92238504865047,28.3768593199991));
#29100=CARTESIAN_POINT('Ctrl Pts',(4.49576183275263,1.99592972571498,28.381353508632));
#29101=CARTESIAN_POINT('Ctrl Pts',(4.38092286391547,2.24363406392164,28.3966522881875));
#29102=CARTESIAN_POINT('Ctrl Pts',(4.28958227150522,2.41368220504275,28.4074395892206));
#29103=CARTESIAN_POINT('Ctrl Pts',(4.15493754422802,2.63244670094294,28.4219187033801));
#29104=CARTESIAN_POINT('Ctrl Pts',(4.12032001285049,2.6863068532354,28.4255342467014));
#29105=CARTESIAN_POINT('Ctrl Pts',(4.04437768201028,2.79953973034755,28.4332522700233));
#29106=CARTESIAN_POINT('Ctrl Pts',(4.00277455314677,2.85870761861537,28.4373561820006));
#29107=CARTESIAN_POINT('Ctrl Pts',(3.93600042075573,2.94935674138122,28.4437608182109));
#29108=CARTESIAN_POINT('Ctrl Pts',(3.91172149589689,2.98148275417654,28.4460542928108));
#29109=CARTESIAN_POINT('Ctrl Pts',(3.76930565852005,3.16519375123499,28.4593089850434));
#29110=CARTESIAN_POINT('Ctrl Pts',(3.64275957807015,3.31004808286288,28.4703238265961));
#29111=CARTESIAN_POINT('Ctrl Pts',(3.45581488703851,3.50029769952538,28.4855725612512));
#29112=CARTESIAN_POINT('Ctrl Pts',(3.40236244327276,3.55227680707081,28.489827317804));
#29113=CARTESIAN_POINT('Ctrl Pts',(3.32213028544329,3.62682455259156,28.4960546674957));
#29114=CARTESIAN_POINT('Ctrl Pts',(3.29625847313596,3.65035424186864,28.4980393804124));
#29115=CARTESIAN_POINT('Ctrl Pts',(3.23639542235603,3.70364259294379,28.5025772213728));
#29116=CARTESIAN_POINT('Ctrl Pts',(3.20224066367408,3.73321290359667,28.5051273548071));
#29117=CARTESIAN_POINT('Ctrl Pts',(3.124363064727,3.79878209935102,28.5108626629883));
#29118=CARTESIAN_POINT('Ctrl Pts',(3.08041601933012,3.83450482160636,28.5140444825973));
#29119=CARTESIAN_POINT('Ctrl Pts',(2.91370875684388,3.96529828432435,28.5259347697592));
#29120=CARTESIAN_POINT('Ctrl Pts',(2.78708621106047,4.05529774066534,28.5346129459366));
#29121=CARTESIAN_POINT('Ctrl Pts',(2.56895289199282,4.19529086741223,28.5491583369249));
#29122=CARTESIAN_POINT('Ctrl Pts',(2.47973018609867,4.2486376927477,28.5550018884223));
#29123=CARTESIAN_POINT('Ctrl Pts',(2.32922551944268,4.33226843972326,28.5647200173306));
#29124=CARTESIAN_POINT('Ctrl Pts',(2.26888255180403,4.36417382575838,28.5685806733646));
#29125=CARTESIAN_POINT('Ctrl Pts',(2.13276396672084,4.43255799619636,28.5772188586075));
#29126=CARTESIAN_POINT('Ctrl Pts',(2.0566774316101,4.46836997392018,28.5820000482211));
#29127=CARTESIAN_POINT('Ctrl Pts',(1.85033588765594,4.55910237034454,28.5948509739652));
#29128=CARTESIAN_POINT('Ctrl Pts',(1.71856967190759,4.61038772860394,28.6029387109716));
#29129=CARTESIAN_POINT('Ctrl Pts',(1.47068824604421,4.69476134028943,28.6179279555619));
#29130=CARTESIAN_POINT('Ctrl Pts',(1.35520716814436,4.72938917808434,28.6248232913193));
#29131=CARTESIAN_POINT('Ctrl Pts',(1.19872264178285,4.77010926744782,28.6340250560022));
#29132=CARTESIAN_POINT('Ctrl Pts',(1.15874622440408,4.77997757778943,28.6363634428941));
#29133=CARTESIAN_POINT('Ctrl Pts',(1.07612275012614,4.79927600229902,28.6411688102927));
#29134=CARTESIAN_POINT('Ctrl Pts',(1.03346447869706,4.80864238131384,28.643634952647));
#29135=CARTESIAN_POINT('Ctrl Pts',(0.987976504581639,4.81799679797234,28.6462520646928));
#29136=CARTESIAN_POINT('Ctrl Pts',(0.985265733875814,4.81855187297385,28.646407979021));
#29137=CARTESIAN_POINT('Ctrl Pts',(0.979138229391013,4.81980119364637,28.6467603064267));
#29138=CARTESIAN_POINT('Ctrl Pts',(0.97572122229174,4.82049409448077,28.6469567077));
#29139=CARTESIAN_POINT('Ctrl Pts',(0.967957982456228,4.82205973190601,28.6474027543141));
#29140=CARTESIAN_POINT('Ctrl Pts',(0.963611299782327,4.82293022724261,28.6476523805736));
#29141=CARTESIAN_POINT('Ctrl Pts',(0.89733369705242,4.83611024079225,28.6514568960207));
#29142=CARTESIAN_POINT('Ctrl Pts',(0.835172132741159,4.84723195573967,28.6550019207052));
#29143=CARTESIAN_POINT('Ctrl Pts',(0.565439360243222,4.89014867084298,28.6703193184863));
#29144=CARTESIAN_POINT('Ctrl Pts',(0.356166504937161,4.90982896225183,28.6820466056942));
#29145=CARTESIAN_POINT('Ctrl Pts',(0.0718565180112681,4.91828865017303,
28.6980644157156));
#29146=CARTESIAN_POINT('Ctrl Pts',(-0.00260559164015547,4.91881282876319,
28.7022663170975));
#29147=CARTESIAN_POINT('Ctrl Pts',(-0.102471169947986,4.91724812293407,
28.7079185593585));
#29148=CARTESIAN_POINT('Ctrl Pts',(-0.127888523762721,4.91665271921554,
28.7093585874028));
#29149=CARTESIAN_POINT('Ctrl Pts',(-0.217155594013457,4.91386894483474,
28.7144217171674));
#29150=CARTESIAN_POINT('Ctrl Pts',(-0.280965825585294,4.91063363047964,
28.7180512531133));
#29151=CARTESIAN_POINT('Ctrl Pts',(-0.429180193272093,4.90022045396422,
28.7265100472542));
#29152=CARTESIAN_POINT('Ctrl Pts',(-0.513497897093821,4.89210341733593,
28.7313437472703));
#29153=CARTESIAN_POINT('Ctrl Pts',(-0.762648780010405,4.86160585268035,
28.7456943287239));
#29154=CARTESIAN_POINT('Ctrl Pts',(-0.926603012511395,4.8330375120958,28.7552290214487));
#29155=CARTESIAN_POINT('Ctrl Pts',(-1.14469831378069,4.78352747945629,28.7679927519579));
#29156=CARTESIAN_POINT('Ctrl Pts',(-1.20037664019074,4.76986010368093,28.7712579791606));
#29157=CARTESIAN_POINT('Ctrl Pts',(-1.29014985538233,4.74615195106764,28.7765292355202));
#29158=CARTESIAN_POINT('Ctrl Pts',(-1.32439671379123,4.73670965661069,28.77854135565));
#29159=CARTESIAN_POINT('Ctrl Pts',(-1.36179459480854,4.72596128003796,28.7807405335028));
#29160=CARTESIAN_POINT('Ctrl Pts',(-1.36504950452029,4.72502215752535,28.7809319566299));
#29161=CARTESIAN_POINT('Ctrl Pts',(-1.3715141144292,4.72314971916441,28.7813121837065));
#29162=CARTESIAN_POINT('Ctrl Pts',(-1.3747238385518,4.72221649265107,28.7815009885362));
#29163=CARTESIAN_POINT('Ctrl Pts',(-1.38126323497621,4.72030793234563,28.781885696161));
#29164=CARTESIAN_POINT('Ctrl Pts',(-1.38459283172663,4.71933234587507,28.7820815961177));
#29165=CARTESIAN_POINT('Ctrl Pts',(-1.39151162511814,4.71729715671113,28.7824887193799));
#29166=CARTESIAN_POINT('Ctrl Pts',(-1.3951006506325,4.71623697901138,28.782699936512));
#29167=CARTESIAN_POINT('Ctrl Pts',(-1.40267892084696,4.71398899366806,28.7831459864932));
#29168=CARTESIAN_POINT('Ctrl Pts',(-1.40666787529463,4.7128002160153,28.7833808092733));
#29169=CARTESIAN_POINT('Ctrl Pts',(-1.41275565697022,4.71097753370377,28.7837392460887));
#29170=CARTESIAN_POINT('Ctrl Pts',(-1.41485557539758,4.71034728763562,28.7838628960867));
#29171=CARTESIAN_POINT('Ctrl Pts',(-1.41992992337434,4.70882063004978,28.7841617172675));
#29172=CARTESIAN_POINT('Ctrl Pts',(-1.42290392711492,4.70792280390154,28.7843368746921));
#29173=CARTESIAN_POINT('Ctrl Pts',(-1.43022165360188,4.70570607788711,28.7847679187994));
#29174=CARTESIAN_POINT('Ctrl Pts',(-1.434564406371,4.70438398028115,28.785023775135));
#29175=CARTESIAN_POINT('Ctrl Pts',(-1.44545804675964,4.70105105853871,28.7856657161714));
#29176=CARTESIAN_POINT('Ctrl Pts',(-1.45200657750312,4.69903255138802,28.786051730575));
#29177=CARTESIAN_POINT('Ctrl Pts',(-1.46872298743884,4.69384163538837,28.7870374484657));
#29178=CARTESIAN_POINT('Ctrl Pts',(-1.47888482673903,4.6906498677499,28.7876369846345));
#29179=CARTESIAN_POINT('Ctrl Pts',(-1.55713229242439,4.66579329752412,28.7922562884239));
#29180=CARTESIAN_POINT('Ctrl Pts',(-1.62474931117814,4.64268003105917,28.7962645004704));
#29181=CARTESIAN_POINT('Ctrl Pts',(-1.88541671192035,4.54718466822189,28.811825196722));
#29182=CARTESIAN_POINT('Ctrl Pts',(-2.07434217828095,4.46416711954959,28.8233469248984));
#29183=CARTESIAN_POINT('Ctrl Pts',(-2.31408634113183,4.34030464060959,28.8385548453371));
#29184=CARTESIAN_POINT('Ctrl Pts',(-2.37010044196303,4.3099725930651,28.8421513388132));
#29185=CARTESIAN_POINT('Ctrl Pts',(-2.48153187233769,4.2468023037472,28.8494009983861));
#29186=CARTESIAN_POINT('Ctrl Pts',(-2.53692491444979,4.21394614370595,28.8530536517444));
#29187=CARTESIAN_POINT('Ctrl Pts',(-2.65383921936443,4.14145790538518,28.8608736196204));
#29188=CARTESIAN_POINT('Ctrl Pts',(-2.71515354863834,4.10152133284737,28.8650423667111));
#29189=CARTESIAN_POINT('Ctrl Pts',(-2.88662013502916,3.98430766146196,28.8768995480995));
#29190=CARTESIAN_POINT('Ctrl Pts',(-2.99452400915693,3.90385821332883,28.884603488743));
#29191=CARTESIAN_POINT('Ctrl Pts',(-3.17846201463924,3.75460196662519,28.8981602068985));
#29192=CARTESIAN_POINT('Ctrl Pts',(-3.25589964909399,3.68765163061946,28.9040110664808));
#29193=CARTESIAN_POINT('Ctrl Pts',(-3.36131336781451,3.59060325587615,28.9121645545975));
#29194=CARTESIAN_POINT('Ctrl Pts',(-3.39108694317198,3.56249753738953,28.91448957866));
#29195=CARTESIAN_POINT('Ctrl Pts',(-3.42326688529033,3.53135125039662,28.9170258180568));
#29196=CARTESIAN_POINT('Ctrl Pts',(-3.42602426245999,3.52867617877976,28.9172433301593));
#29197=CARTESIAN_POINT('Ctrl Pts',(-3.46123304208364,3.49443818120701,28.9200232042756));
#29198=CARTESIAN_POINT('Ctrl Pts',(-3.49325056492841,3.46243164976422,28.9225780511367));
#29199=CARTESIAN_POINT('Ctrl Pts',(-3.55376359562376,3.40024551650027,28.9274652764312));
#29200=CARTESIAN_POINT('Ctrl Pts',(-3.58232785172381,3.37013834466104,28.9297982582826));
#29201=CARTESIAN_POINT('Ctrl Pts',(-3.69141267097097,3.25220716644448,28.9388189721813));
#29202=CARTESIAN_POINT('Ctrl Pts',(-3.76911279712212,3.16182983409066,28.9454853046441));
#29203=CARTESIAN_POINT('Ctrl Pts',(-3.92593905871077,2.96541094130583,28.9595701864866));
#29204=CARTESIAN_POINT('Ctrl Pts',(-4.00422415830557,2.85881930647059,28.966985760214));
#29205=CARTESIAN_POINT('Ctrl Pts',(-4.11130943689565,2.69997098343283,28.9777840104923));
#29206=CARTESIAN_POINT('Ctrl Pts',(-4.14360505763804,2.65014068205228,28.9811368928025));
#29207=CARTESIAN_POINT('Ctrl Pts',(-4.19105812528317,2.57393450913857,28.9862172341388));
#29208=CARTESIAN_POINT('Ctrl Pts',(-4.20688628874769,2.54798249757374,28.987939229281));
#29209=CARTESIAN_POINT('Ctrl Pts',(-4.25547606531191,2.46662709552304,28.9933131560861));
#29210=CARTESIAN_POINT('Ctrl Pts',(-4.28739118937481,2.41072653934366,28.9969710587362));
#29211=CARTESIAN_POINT('Ctrl Pts',(-4.36036909069504,2.27686747961953,29.0056535591906));
#29212=CARTESIAN_POINT('Ctrl Pts',(-4.40045223983104,2.19840032675795,29.0106833445267));
#29213=CARTESIAN_POINT('Ctrl Pts',(-4.50925167170404,1.97050088067716,29.0251254555451));
#29214=CARTESIAN_POINT('Ctrl Pts',(-4.57261031405347,1.8186422181361,29.0345521930793));
#29215=CARTESIAN_POINT('Ctrl Pts',(-4.6463560602586,1.6135132112343,29.0469868174237));
#29216=CARTESIAN_POINT('Ctrl Pts',(-4.66364523893352,1.56283802791021,29.05003482225));
#29217=CARTESIAN_POINT('Ctrl Pts',(-4.69060112825528,1.47939522869703,29.0550111931308));
#29218=CARTESIAN_POINT('Ctrl Pts',(-4.7007598099838,1.44679176879886,29.0569447754866));
#29219=CARTESIAN_POINT('Ctrl Pts',(-4.72483473814913,1.36659372332528,29.0616762149042));
#29220=CARTESIAN_POINT('Ctrl Pts',(-4.73837233632022,1.31888945107595,29.0644698259977));
#29221=CARTESIAN_POINT('Ctrl Pts',(-4.75555358007278,1.2546628245821,29.0682088437209));
#29222=CARTESIAN_POINT('Ctrl Pts',(-4.75983637069872,1.23831591791709,29.0691585809229));
#29223=CARTESIAN_POINT('Ctrl Pts',(-4.76403458843593,1.2219482405921,29.0701077704777));
#29224=CARTESIAN_POINT('Origin',(0.,0.,-3.23514056400928));
#29225=CARTESIAN_POINT('',(-4.76403458668766,1.2219482474081,31.1654428831549));
#29226=CARTESIAN_POINT('',(-4.76403458704967,1.22194824599672,30.8199238152312));
#29227=CARTESIAN_POINT('',(-4.76403458704967,1.22194824599672,-3.23514056400928));
#29228=CARTESIAN_POINT('',(-4.91824995130769,0.000107359571118153,29.4853029780633));
#29229=CARTESIAN_POINT('Ctrl Pts',(-4.76403458668766,1.2219482474081,31.1654428831549));
#29230=CARTESIAN_POINT('Ctrl Pts',(-4.75747531537793,1.24752101241618,31.1639437083435));
#29231=CARTESIAN_POINT('Ctrl Pts',(-4.7507100794633,1.27304118690602,31.1624431868895));
#29232=CARTESIAN_POINT('Ctrl Pts',(-4.70273686558152,1.44829827449206,31.1521070958768));
#29233=CARTESIAN_POINT('Ctrl Pts',(-4.65466277484179,1.59606243649511,31.1432307642279));
#29234=CARTESIAN_POINT('Ctrl Pts',(-4.54929617340791,1.87439009344354,31.1261951866103));
#29235=CARTESIAN_POINT('Ctrl Pts',(-4.49316021950789,2.00522960892285,31.1180465608187));
#29236=CARTESIAN_POINT('Ctrl Pts',(-4.41349333381479,2.17070710999003,31.1075938485764));
#29237=CARTESIAN_POINT('Ctrl Pts',(-4.39508779041059,2.20773552225107,31.1052452508279));
#29238=CARTESIAN_POINT('Ctrl Pts',(-4.35685174862786,2.28228538330546,31.1004994382882));
#29239=CARTESIAN_POINT('Ctrl Pts',(-4.33699813998058,2.31979113722606,31.0981026882424));
#29240=CARTESIAN_POINT('Ctrl Pts',(-4.26391079915593,2.45364287839366,31.0895062631372));
#29241=CARTESIAN_POINT('Ctrl Pts',(-4.20793129825726,2.54845312823083,31.0833358918565));
#29242=CARTESIAN_POINT('Ctrl Pts',(-4.0474840780041,2.80047475603626,31.0665956161659));
#29243=CARTESIAN_POINT('Ctrl Pts',(-3.93707598730645,2.95367869615756,31.0560402687495));
#29244=CARTESIAN_POINT('Ctrl Pts',(-3.77348996620301,3.15515043602749,31.0414138581479));
#29245=CARTESIAN_POINT('Ctrl Pts',(-3.72765689908364,3.20917040534007,31.0374130690057));
#29246=CARTESIAN_POINT('Ctrl Pts',(-3.63212474204785,3.31695800390257,31.0292569899486));
#29247=CARTESIAN_POINT('Ctrl Pts',(-3.58235967906493,3.37064378152434,31.0251020008058));
#29248=CARTESIAN_POINT('Ctrl Pts',(-3.47559637167496,3.48078217889091,31.0163730626085));
#29249=CARTESIAN_POINT('Ctrl Pts',(-3.41837758207695,3.53699155275009,31.0117983289139));
#29250=CARTESIAN_POINT('Ctrl Pts',(-3.22484868904486,3.71802186933397,30.9966545487602));
#29251=CARTESIAN_POINT('Ctrl Pts',(-3.08287878122176,3.83656019996987,30.9860566616643));
#29252=CARTESIAN_POINT('Ctrl Pts',(-2.8920143667442,3.978473184575,30.9724897751801));
#29253=CARTESIAN_POINT('Ctrl Pts',(-2.84894350929977,4.00942850673985,30.9694704631617));
#29254=CARTESIAN_POINT('Ctrl Pts',(-2.77807365240271,4.05864448870143,30.9645738548085));
#29255=CARTESIAN_POINT('Ctrl Pts',(-2.75057567527664,4.0773302274215,30.9626912872225));
#29256=CARTESIAN_POINT('Ctrl Pts',(-2.67134815790107,4.1300015467316,30.9573148163061));
#29257=CARTESIAN_POINT('Ctrl Pts',(-2.61916359822708,4.1632914792067,30.9538300409974));
#29258=CARTESIAN_POINT('Ctrl Pts',(-2.48500337199467,4.24535483080896,30.9449925147789));
#29259=CARTESIAN_POINT('Ctrl Pts',(-2.40221169471751,4.29274487466121,30.939650674331));
#29260=CARTESIAN_POINT('Ctrl Pts',(-2.17852872115839,4.41228252387011,30.9254424417252));
#29261=CARTESIAN_POINT('Ctrl Pts',(-2.03544626049433,4.48008729879932,30.9165799502979));
#29262=CARTESIAN_POINT('Ctrl Pts',(-1.82246262903994,4.56870449987658,30.9035845490042));
#29263=CARTESIAN_POINT('Ctrl Pts',(-1.75497333668192,4.59505160679282,30.8994948981396));
#29264=CARTESIAN_POINT('Ctrl Pts',(-1.61981661652591,4.64440324797767,30.8913501275608));
#29265=CARTESIAN_POINT('Ctrl Pts',(-1.55218051364651,4.66744286472769,30.8872962796406));
#29266=CARTESIAN_POINT('Ctrl Pts',(-1.34069098583087,4.73437922629607,30.8746785770657));
#29267=CARTESIAN_POINT('Ctrl Pts',(-1.19531061153262,4.77315729089733,30.8660850747287));
#29268=CARTESIAN_POINT('Ctrl Pts',(-0.90228417064475,4.8370887566735,30.8489178906732));
#29269=CARTESIAN_POINT('Ctrl Pts',(-0.754805171813162,4.86228487674438,
30.8403533381151));
#29270=CARTESIAN_POINT('Ctrl Pts',(-0.565824311542138,4.8857648611962,30.8295161727133));
#29271=CARTESIAN_POINT('Ctrl Pts',(-0.525180080183103,4.89030074459523,
30.8271936406343));
#29272=CARTESIAN_POINT('Ctrl Pts',(-0.441726505655083,4.89856171191949,
30.822443908699));
#29273=CARTESIAN_POINT('Ctrl Pts',(-0.398915374270311,4.90223374935372,
30.8200174234302));
#29274=CARTESIAN_POINT('Ctrl Pts',(-0.328959622948482,4.90731158583249,
30.8160642960322));
#29275=CARTESIAN_POINT('Ctrl Pts',(-0.301841996113542,4.90905417103023,
30.814534818718));
#29276=CARTESIAN_POINT('Ctrl Pts',(-0.194050481796607,4.91508433199235,
30.8084640918898));
#29277=CARTESIAN_POINT('Ctrl Pts',(-0.113290324852295,4.91760867010689,
30.803935327558));
#29278=CARTESIAN_POINT('Ctrl Pts',(0.159168546390112,4.91940936694677,30.7886683059716));
#29279=CARTESIAN_POINT('Ctrl Pts',(0.350749640771354,4.90947010715552,30.777946326266));
#29280=CARTESIAN_POINT('Ctrl Pts',(0.604314000039364,4.88139449940297,30.7635663169093));
#29281=CARTESIAN_POINT('Ctrl Pts',(0.667227018044355,4.87319357990585,30.7599835039854));
#29282=CARTESIAN_POINT('Ctrl Pts',(0.800709250460242,4.85316035979293,30.7523428035817));
#29283=CARTESIAN_POINT('Ctrl Pts',(0.871214505773545,4.84100050686251,30.7482835406051));
#29284=CARTESIAN_POINT('Ctrl Pts',(1.09794506296865,4.79678316629855,30.7351437485202));
#29285=CARTESIAN_POINT('Ctrl Pts',(1.25288238607207,4.75866543109589,30.7260285979407));
#29286=CARTESIAN_POINT('Ctrl Pts',(1.53814217159968,4.67358591925001,30.7089884859344));
#29287=CARTESIAN_POINT('Ctrl Pts',(1.6688694393235,4.62851618701025,30.7010750264283));
#29288=CARTESIAN_POINT('Ctrl Pts',(1.836219632701,4.56280709568751,30.6908418920887));
#29289=CARTESIAN_POINT('Ctrl Pts',(1.87471996684793,4.54712395183278,30.6884805799674));
#29290=CARTESIAN_POINT('Ctrl Pts',(1.95188771987945,4.51454290638366,30.6837356486427));
#29291=CARTESIAN_POINT('Ctrl Pts',(1.99054581427608,4.49763168137312,30.6813523786775));
#29292=CARTESIAN_POINT('Ctrl Pts',(2.07561292067222,4.45910691741121,30.6760882171418));
#29293=CARTESIAN_POINT('Ctrl Pts',(2.12191180179166,4.43726197876472,30.6732098881597));
#29294=CARTESIAN_POINT('Ctrl Pts',(2.27638670229846,4.36140624034259,30.6635466975161));
#29295=CARTESIAN_POINT('Ctrl Pts',(2.38291030268977,4.30413051792195,30.6567823524661));
#29296=CARTESIAN_POINT('Ctrl Pts',(2.60027529792051,4.17671239505201,30.6426621986406));
#29297=CARTESIAN_POINT('Ctrl Pts',(2.71064012418522,4.10594539304553,30.6353097755382));
#29298=CARTESIAN_POINT('Ctrl Pts',(2.86980891315586,3.99466755691141,30.6243616261251));
#29299=CARTESIAN_POINT('Ctrl Pts',(2.92086974028756,3.95748555791618,30.6207943183749));
#29300=CARTESIAN_POINT('Ctrl Pts',(3.02852364592336,3.87587435989815,30.6131464294742));
#29301=CARTESIAN_POINT('Ctrl Pts',(3.08488657032127,3.8311659079648,30.6090642900197));
#29302=CARTESIAN_POINT('Ctrl Pts',(3.17117214094017,3.75958305794207,30.6026864109259));
#29303=CARTESIAN_POINT('Ctrl Pts',(3.20178045922284,3.73355050629159,30.6003978001166));
#29304=CARTESIAN_POINT('Ctrl Pts',(3.37871767862999,3.57928821865468,30.5870119455222));
#29305=CARTESIAN_POINT('Ctrl Pts',(3.51765245924632,3.44284148755095,30.5758598417647));
#29306=CARTESIAN_POINT('Ctrl Pts',(3.69848522217757,3.24284222763085,30.5604475568804));
#29307=CARTESIAN_POINT('Ctrl Pts',(3.74755180551059,3.18601229112869,30.5561640899859));
#29308=CARTESIAN_POINT('Ctrl Pts',(3.81896963361591,3.09936108751663,30.5497818390881));
#29309=CARTESIAN_POINT('Ctrl Pts',(3.84231402129371,3.07037314203322,30.5476709332088));
#29310=CARTESIAN_POINT('Ctrl Pts',(3.89623069721223,3.00184397405024,30.5427376361647));
#29311=CARTESIAN_POINT('Ctrl Pts',(3.9265337328691,2.9620961864868,30.5399190173322));
#29312=CARTESIAN_POINT('Ctrl Pts',(3.99574295663878,2.86838730947251,30.5333622522042));
#29313=CARTESIAN_POINT('Ctrl Pts',(4.03417071841867,2.81408497662551,30.52962909689));
#29314=CARTESIAN_POINT('Ctrl Pts',(4.19833314793241,2.57183047101487,30.5132213320537));
#29315=CARTESIAN_POINT('Ctrl Pts',(4.31211955121054,2.37611803777547,30.5005917090974));
#29316=CARTESIAN_POINT('Ctrl Pts',(4.44221423223513,2.1120085215405,30.4839877415829));
#29317=CARTESIAN_POINT('Ctrl Pts',(4.47111281545186,2.05012129744831,30.4801279288461));
#29318=CARTESIAN_POINT('Ctrl Pts',(4.52959758855043,1.91775099326645,30.471928519319));
#29319=CARTESIAN_POINT('Ctrl Pts',(4.55884843365432,1.84713939787589,30.467587558904));
#29320=CARTESIAN_POINT('Ctrl Pts',(4.62542245390094,1.67520287119621,30.4570881917116));
#29321=CARTESIAN_POINT('Ctrl Pts',(4.66107748433156,1.57327488035465,30.4509214655097));
#29322=CARTESIAN_POINT('Ctrl Pts',(4.7446797778377,1.306399974715,30.4349201464463));
#29323=CARTESIAN_POINT('Ctrl Pts',(4.78739440141907,1.13996608300871,30.4250781393178));
#29324=CARTESIAN_POINT('Ctrl Pts',(4.82952520913053,0.930911086693913,30.4129400434828));
#29325=CARTESIAN_POINT('Ctrl Pts',(4.83721676751018,0.890080443924282,30.4105800675428));
#29326=CARTESIAN_POINT('Ctrl Pts',(4.85167922569719,0.807572975481787,30.4058350728294));
#29327=CARTESIAN_POINT('Ctrl Pts',(4.858432663947,0.765896549925473,30.4034504152531));
#29328=CARTESIAN_POINT('Ctrl Pts',(4.86854280318443,0.697978178813625,30.3995796172955));
#29329=CARTESIAN_POINT('Ctrl Pts',(4.87222582391646,0.671787239702785,30.3980906525679));
#29330=CARTESIAN_POINT('Ctrl Pts',(4.89623220584169,0.490477300675998,30.3878044091572));
#29331=CARTESIAN_POINT('Ctrl Pts',(4.90935555213833,0.334494400992546,30.3790597983883));
#29332=CARTESIAN_POINT('Ctrl Pts',(4.91947459127942,0.0553193741177052,
30.3634003525522));
#29333=CARTESIAN_POINT('Ctrl Pts',(4.91932063394959,-0.0676347365759319,
30.3565012782735));
#29334=CARTESIAN_POINT('Ctrl Pts',(4.91213242227513,-0.25312390782555,30.3460350832642));
#29335=CARTESIAN_POINT('Ctrl Pts',(4.90850518984122,-0.315742525446427,
30.3424920372609));
#29336=CARTESIAN_POINT('Ctrl Pts',(4.89809360166084,-0.450711053718308,
30.3348272133237));
#29337=CARTESIAN_POINT('Ctrl Pts',(4.89090144516376,-0.523014600482981,
30.3307035633953));
#29338=CARTESIAN_POINT('Ctrl Pts',(4.87254250870178,-0.673620520373063,
30.3220708429589));
#29339=CARTESIAN_POINT('Ctrl Pts',(4.8610833637056,-0.751866652358065,30.3175611244853));
#29340=CARTESIAN_POINT('Ctrl Pts',(4.81808231297128,-1.00308087681873,30.3029983105498));
#29341=CARTESIAN_POINT('Ctrl Pts',(4.77915247976308,-1.174644586987,30.2929189763384));
#29342=CARTESIAN_POINT('Ctrl Pts',(4.71455997206945,-1.40206329645317,30.2794222431633));
#29343=CARTESIAN_POINT('Ctrl Pts',(4.6969222462346,-1.46006121678644,30.275968597111));
#29344=CARTESIAN_POINT('Ctrl Pts',(4.66687678524039,-1.55267335795665,30.2704400636562));
#29345=CARTESIAN_POINT('Ctrl Pts',(4.65514530592551,-1.58749982878772,30.2683582742569));
#29346=CARTESIAN_POINT('Ctrl Pts',(4.62321379020557,-1.67889394644738,30.2628864638555));
#29347=CARTESIAN_POINT('Ctrl Pts',(4.60236591329271,-1.73522873487296,30.259503956053));
#29348=CARTESIAN_POINT('Ctrl Pts',(4.54757305528337,-1.87534859517788,30.2510477491439));
#29349=CARTESIAN_POINT('Ctrl Pts',(4.51234029602041,-1.9586062071877,30.2459838294301));
#29350=CARTESIAN_POINT('Ctrl Pts',(4.40563612213864,-2.19256966591863,30.2315776129323));
#29351=CARTESIAN_POINT('Ctrl Pts',(4.32876809807629,-2.34067453818446,30.2222417888935));
#29352=CARTESIAN_POINT('Ctrl Pts',(4.20799355066273,-2.54699886581245,30.2087733311054));
#29353=CARTESIAN_POINT('Ctrl Pts',(4.17008838194017,-2.60859649475921,30.204690531341));
#29354=CARTESIAN_POINT('Ctrl Pts',(4.0920031424588,-2.72943464719803,30.1965462826716));
#29355=CARTESIAN_POINT('Ctrl Pts',(4.05186057758402,-2.78867870358175,30.1924860373212));
#29356=CARTESIAN_POINT('Ctrl Pts',(3.90299964121195,-2.99837050147047,30.177858376316));
#29357=CARTESIAN_POINT('Ctrl Pts',(3.78707936746813,-3.14351079058454,30.1672398971431));
#29358=CARTESIAN_POINT('Ctrl Pts',(3.63267188146699,-3.31586734446963,30.153994238295));
#29359=CARTESIAN_POINT('Ctrl Pts',(3.60163224687229,-3.34955615245243,30.1513730208839));
#29360=CARTESIAN_POINT('Ctrl Pts',(3.51826088620866,-3.43754413051739,30.1444428580303));
#29361=CARTESIAN_POINT('Ctrl Pts',(3.46514280449843,-3.49108218910521,30.1401386862681));
#29362=CARTESIAN_POINT('Ctrl Pts',(3.38568068009294,-3.56757150125414,30.1338667449964));
#29363=CARTESIAN_POINT('Ctrl Pts',(3.36029009124276,-3.59149698991795,30.13188658925));
#29364=CARTESIAN_POINT('Ctrl Pts',(3.30234063612166,-3.64495008103297,30.1274222110345));
#29365=CARTESIAN_POINT('Ctrl Pts',(3.26963613202736,-3.67431550025022,30.1249406476618));
#29366=CARTESIAN_POINT('Ctrl Pts',(3.19552588414164,-3.73908608464441,30.1193945683724));
#29367=CARTESIAN_POINT('Ctrl Pts',(3.15391660508507,-3.77424966673595,30.1163330881093));
#29368=CARTESIAN_POINT('Ctrl Pts',(3.0024456320413,-3.898001905774,30.1053547203128));
#29369=CARTESIAN_POINT('Ctrl Pts',(2.88936721758554,-3.98254389682634,30.0974639975508));
#29370=CARTESIAN_POINT('Ctrl Pts',(2.67784462600841,-4.12693006687821,30.08310115895));
#29371=CARTESIAN_POINT('Ctrl Pts',(2.58063615465586,-4.18840305810381,30.0766419043654));
#29372=CARTESIAN_POINT('Ctrl Pts',(2.42238011074505,-4.2808789617415,30.066301301867));
#29373=CARTESIAN_POINT('Ctrl Pts',(2.36268521310744,-4.31411271659658,30.0624389758384));
#29374=CARTESIAN_POINT('Ctrl Pts',(2.23257113084391,-4.38303992352201,30.0540934005721));
#29375=CARTESIAN_POINT('Ctrl Pts',(2.16194566632971,-4.41830324378555,30.0496080682049));
#29376=CARTESIAN_POINT('Ctrl Pts',(1.94563120670292,-4.51988030742191,30.0359933051998));
#29377=CARTESIAN_POINT('Ctrl Pts',(1.79752642820525,-4.58079650503639,30.0268339467352));
#29378=CARTESIAN_POINT('Ctrl Pts',(1.60371963417071,-4.64966113206032,30.0150609270679));
#29379=CARTESIAN_POINT('Ctrl Pts',(1.56051110414909,-4.66434029818212,30.0124496790555));
#29380=CARTESIAN_POINT('Ctrl Pts',(1.44526002767175,-4.70171361508314,30.005522549396));
#29381=CARTESIAN_POINT('Ctrl Pts',(1.37288779678485,-4.7233533382413,30.0012114669173));
#29382=CARTESIAN_POINT('Ctrl Pts',(1.26638371390079,-4.7525439061861,29.9949316557589));
#29383=CARTESIAN_POINT('Ctrl Pts',(1.2326244756697,-4.76141137004005,29.9929505025669));
#29384=CARTESIAN_POINT('Ctrl Pts',(1.15618681874447,-4.78062164076533,29.9884873932739));
#29385=CARTESIAN_POINT('Ctrl Pts',(1.11345844758248,-4.79075375889872,29.9860080816439));
#29386=CARTESIAN_POINT('Ctrl Pts',(1.06940890741174,-4.80057800062057,29.9834649708523));
#29387=CARTESIAN_POINT('Ctrl Pts',(1.0682179059898,-4.80084316101012,29.9833962204472));
#29388=CARTESIAN_POINT('Ctrl Pts',(1.06551327634014,-4.80144425400972,29.9832401178028));
#29389=CARTESIAN_POINT('Ctrl Pts',(1.06399958756485,-4.80177991416559,29.983152767958));
#29390=CARTESIAN_POINT('Ctrl Pts',(1.06055042317784,-4.802543054591,29.9829537633351));
#29391=CARTESIAN_POINT('Ctrl Pts',(1.05861484715097,-4.80297008076242,29.9828421124938));
#29392=CARTESIAN_POINT('Ctrl Pts',(1.05418707035387,-4.80394412888943,29.9825867594659));
#29393=CARTESIAN_POINT('Ctrl Pts',(1.05169470064238,-4.80449038186596,29.9824430638311));
#29394=CARTESIAN_POINT('Ctrl Pts',(0.989865462182989,-4.81799108663865,
29.9788793523748));
#29395=CARTESIAN_POINT('Ctrl Pts',(0.930293736296707,-4.82984734747352,
29.9754686546393));
#29396=CARTESIAN_POINT('Ctrl Pts',(0.682099650101073,-4.87448177055396,
29.9613234338234));
#29397=CARTESIAN_POINT('Ctrl Pts',(0.491864966075864,-4.89733611519763,
29.9506295299418));
#29398=CARTESIAN_POINT('Ctrl Pts',(0.21949888699607,-4.91402435211442,29.9352827515274));
#29399=CARTESIAN_POINT('Ctrl Pts',(0.13810357490624,-4.91698508066162,29.9306929577632));
#29400=CARTESIAN_POINT('Ctrl Pts',(0.0511315716101662,-4.91798732577079,
29.925776122007));
#29401=CARTESIAN_POINT('Ctrl Pts',(0.0455900380226175,-4.91804181787991,
29.9254627861361));
#29402=CARTESIAN_POINT('Ctrl Pts',(0.0334229200019035,-4.91814089582433,
29.9247746970467));
#29403=CARTESIAN_POINT('Ctrl Pts',(0.0267973150226865,-4.9181814592938,
29.9243999188639));
#29404=CARTESIAN_POINT('Ctrl Pts',(0.00912120295854194,-4.91825395650327,
29.9233998468002));
#29405=CARTESIAN_POINT('Ctrl Pts',(-0.00192935498148004,-4.9182620359225,
29.9227744026962));
#29406=CARTESIAN_POINT('Ctrl Pts',(-0.0584732946038119,-4.91811280938267,
29.9195728506077));
#29407=CARTESIAN_POINT('Ctrl Pts',(-0.103962664961447,-4.91736153388182,
29.9169930353557));
#29408=CARTESIAN_POINT('Ctrl Pts',(-0.217646920461575,-4.91390578558918,
29.9105331018305));
#29409=CARTESIAN_POINT('Ctrl Pts',(-0.285807983913625,-4.91041280562472,
29.9066485207759));
#29410=CARTESIAN_POINT('Ctrl Pts',(-0.463973274432121,-4.89756029486546,
29.8964604732729));
#29411=CARTESIAN_POINT('Ctrl Pts',(-0.573773468573468,-4.88591360358744,
29.8901469859518));
#29412=CARTESIAN_POINT('Ctrl Pts',(-0.824046138394972,-4.850813445637,29.8756805854009));
#29413=CARTESIAN_POINT('Ctrl Pts',(-0.964080927585995,-4.82493437621554,
29.8675300954511));
#29414=CARTESIAN_POINT('Ctrl Pts',(-1.14309058440367,-4.78374712213418,
29.8570756480477));
#29415=CARTESIAN_POINT('Ctrl Pts',(-1.18326632280902,-4.7739683156292,29.85472715603));
#29416=CARTESIAN_POINT('Ctrl Pts',(-1.25860896504974,-4.75462032132464,
29.8503209951568));
#29417=CARTESIAN_POINT('Ctrl Pts',(-1.29380206662514,-4.74516460995912,
29.8482619749614));
#29418=CARTESIAN_POINT('Ctrl Pts',(-1.33275660035233,-4.7342326790389,29.845980008386));
#29419=CARTESIAN_POINT('Ctrl Pts',(-1.33662481011624,-4.73314201478103,
29.8457533761171));
#29420=CARTESIAN_POINT('Ctrl Pts',(-1.34498948779896,-4.73077247327524,
29.8452632298105));
#29421=CARTESIAN_POINT('Ctrl Pts',(-1.34948547883623,-4.72949192394501,
29.8449997317813));
#29422=CARTESIAN_POINT('Ctrl Pts',(-1.35672287348843,-4.72741940697912,
29.8445754880534));
#29423=CARTESIAN_POINT('Ctrl Pts',(-1.35946542348374,-4.72663146091334,
29.8444147060849));
#29424=CARTESIAN_POINT('Ctrl Pts',(-1.36649066691624,-4.72460645889999,
29.8440028021501));
#29425=CARTESIAN_POINT('Ctrl Pts',(-1.37077236860935,-4.72336596589306,
29.8437517107176));
#29426=CARTESIAN_POINT('Ctrl Pts',(-1.38190360390953,-4.72012461820929,
29.843098813186));
#29427=CARTESIAN_POINT('Ctrl Pts',(-1.38875048394198,-4.71811467383661,
29.8426970848728));
#29428=CARTESIAN_POINT('Ctrl Pts',(-1.45985156396179,-4.69707432662595,
29.838523902809));
#29429=CARTESIAN_POINT('Ctrl Pts',(-1.52371520757566,-4.67674736271437,
29.8347630660861));
#29430=CARTESIAN_POINT('Ctrl Pts',(-1.79332549445003,-4.58482488576176,
29.818792431599));
#29431=CARTESIAN_POINT('Ctrl Pts',(-1.99460731550415,-4.50090836886034,
29.806623722021));
#29432=CARTESIAN_POINT('Ctrl Pts',(-2.24256082913721,-4.37762426311005,
29.7910140444091));
#29433=CARTESIAN_POINT('Ctrl Pts',(-2.2949821369226,-4.35037126747936,29.7876777714377));
#29434=CARTESIAN_POINT('Ctrl Pts',(-2.40213268175558,-4.29218963006874,
29.7807773661977));
#29435=CARTESIAN_POINT('Ctrl Pts',(-2.45678558507369,-4.26114277177896,
29.7772129157356));
#29436=CARTESIAN_POINT('Ctrl Pts',(-2.57248588014391,-4.19245050055632,
29.7695651184003));
#29437=CARTESIAN_POINT('Ctrl Pts',(-2.63333530200902,-4.15449995182853,
29.7654803060246));
#29438=CARTESIAN_POINT('Ctrl Pts',(-2.80064675331285,-4.04499814984928,
29.7540673346843));
#29439=CARTESIAN_POINT('Ctrl Pts',(-2.90517184214477,-3.97059296435249,
29.7467251352135));
#29440=CARTESIAN_POINT('Ctrl Pts',(-3.09281361627793,-3.82564195891981,
29.7331533973296));
#29441=CARTESIAN_POINT('Ctrl Pts',(-3.17672659235729,-3.75625358796593,
29.7269275545366));
#29442=CARTESIAN_POINT('Ctrl Pts',(-3.28965870601234,-3.65637589943658,
29.718345808016));
#29443=CARTESIAN_POINT('Ctrl Pts',(-3.32069309855417,-3.62821395717062,
29.7159652553322));
#29444=CARTESIAN_POINT('Ctrl Pts',(-3.35347088896619,-3.59769708924375,
29.7134281816362));
#29445=CARTESIAN_POINT('Ctrl Pts',(-3.35557604286721,-3.59573369003486,
29.7132651363252));
#29446=CARTESIAN_POINT('Ctrl Pts',(-3.38822643278234,-3.56522823433971,
29.7107347520871));
#29447=CARTESIAN_POINT('Ctrl Pts',(-3.41840850072128,-3.53629949211714,
29.7083739758083));
#29448=CARTESIAN_POINT('Ctrl Pts',(-3.45025032786775,-3.50499127797175,
29.7058571756585));
#29449=CARTESIAN_POINT('Ctrl Pts',(-3.45228062840131,-3.50299152816395,
29.7056965839487));
#29450=CARTESIAN_POINT('Ctrl Pts',(-3.46240967550334,-3.49299753779086,
29.7048948211928));
#29451=CARTESIAN_POINT('Ctrl Pts',(-3.47048240991077,-3.48497695879883,
29.7042539703571));
#29452=CARTESIAN_POINT('Ctrl Pts',(-3.51240214971891,-3.44303794267927,
29.7009162286683));
#29453=CARTESIAN_POINT('Ctrl Pts',(-3.5457801345098,-3.40865404806003,29.6982245705546));
#29454=CARTESIAN_POINT('Ctrl Pts',(-3.68739863510194,-3.25843620557217,
29.6866401274311));
#29455=CARTESIAN_POINT('Ctrl Pts',(-3.79050595290947,-3.13789418341467,
29.6777796324722));
#29456=CARTESIAN_POINT('Ctrl Pts',(-3.9486059775107,-2.93387280179996,29.6632921670813));
#29457=CARTESIAN_POINT('Ctrl Pts',(-4.00719539490756,-2.85332849633604,
29.6576922071448));
#29458=CARTESIAN_POINT('Ctrl Pts',(-4.08910679468821,-2.73321913042239,
29.6494865026446));
#29459=CARTESIAN_POINT('Ctrl Pts',(-4.1143845920288,-2.69501773285806,29.6468973165264));
#29460=CARTESIAN_POINT('Ctrl Pts',(-4.14810390777172,-2.64247864418189,
29.6433626446547));
#29461=CARTESIAN_POINT('Ctrl Pts',(-4.15701185161429,-2.62844286187267,
29.6424208796467));
#29462=CARTESIAN_POINT('Ctrl Pts',(-4.20755422117715,-2.54790625883081,
29.6370311783321));
#29463=CARTESIAN_POINT('Ctrl Pts',(-4.24766344702677,-2.48046242978804,
29.6325721896692));
#29464=CARTESIAN_POINT('Ctrl Pts',(-4.3317425213843,-2.33105878309729,29.6228046503494));
#29465=CARTESIAN_POINT('Ctrl Pts',(-4.37503593334096,-2.24875269162539,
29.6174934452591));
#29466=CARTESIAN_POINT('Ctrl Pts',(-4.49794751591431,-1.99808004554011,
29.601522019668));
#29467=CARTESIAN_POINT('Ctrl Pts',(-4.57036468051255,-1.82636889336943,
29.5908457800909));
#29468=CARTESIAN_POINT('Ctrl Pts',(-4.64467458684734,-1.61784344218231,
29.5782559940762));
#29469=CARTESIAN_POINT('Ctrl Pts',(-4.65612234394557,-1.584595904262,29.5762599249588));
#29470=CARTESIAN_POINT('Ctrl Pts',(-4.67449806939939,-1.5293084754238,29.5729603718675));
#29471=CARTESIAN_POINT('Ctrl Pts',(-4.68162898859386,-1.50733759874811,
29.5716542142019));
#29472=CARTESIAN_POINT('Ctrl Pts',(-4.70948606665194,-1.41940295962438,
29.5664449569709));
#29473=CARTESIAN_POINT('Ctrl Pts',(-4.72897514321561,-1.35305507856757,
29.5625556342458));
#29474=CARTESIAN_POINT('Ctrl Pts',(-4.81388319122366,-1.03970832326431,
29.5443271335567));
#29475=CARTESIAN_POINT('Ctrl Pts',(-4.86138849432607,-0.788267845529706,
29.5300833764657));
#29476=CARTESIAN_POINT('Ctrl Pts',(-4.89654818846978,-0.466523700483106,
29.5118331429605));
#29477=CARTESIAN_POINT('Ctrl Pts',(-4.90254299392909,-0.398623358220403,
29.507981847529));
#29478=CARTESIAN_POINT('Ctrl Pts',(-4.91059576867979,-0.279102874042,29.5011959178355));
#29479=CARTESIAN_POINT('Ctrl Pts',(-4.91325529364975,-0.227533683441403,
29.4982658407896));
#29480=CARTESIAN_POINT('Ctrl Pts',(-4.91720189917998,-0.117275649014002,
29.4919940337311));
#29481=CARTESIAN_POINT('Ctrl Pts',(-4.91825128049374,-0.0585862957523841,
29.4886512846965));
#29482=CARTESIAN_POINT('Ctrl Pts',(-4.91824999882741,0.000107397491747315,
29.4853030582774));
#29483=CARTESIAN_POINT('Ctrl Pts',(-4.91824999882813,0.000107364256212508,
29.4853030601734));
#29484=CARTESIAN_POINT('Ctrl Pts',(-4.91824536563938,0.212349141886051,
29.4731955663798));
#29485=CARTESIAN_POINT('Ctrl Pts',(-4.90450219779015,0.424366907549726,
29.4610215256331));
#29486=CARTESIAN_POINT('Ctrl Pts',(-4.8713386361668,0.679146533038959,29.446355223248));
#29487=CARTESIAN_POINT('Ctrl Pts',(-4.86496664387682,0.723380759594618,
29.4438080300108));
#29488=CARTESIAN_POINT('Ctrl Pts',(-4.85290081965428,0.799750775122579,
29.4394109504458));
#29489=CARTESIAN_POINT('Ctrl Pts',(-4.84748836227862,0.831928044753747,
29.4375585114712));
#29490=CARTESIAN_POINT('Ctrl Pts',(-4.83441170691769,0.905203931302206,
29.433341770966));
#29491=CARTESIAN_POINT('Ctrl Pts',(-4.82654285598595,0.946263611344807,
29.4309802071808));
#29492=CARTESIAN_POINT('Ctrl Pts',(-4.80203008909085,1.06589898087157,29.4240954527912));
#29493=CARTESIAN_POINT('Ctrl Pts',(-4.78398537213812,1.14416571360072,29.4195863166346));
#29494=CARTESIAN_POINT('Ctrl Pts',(-4.76403458343061,1.22194826010642,29.4150832822139));
#29495=CARTESIAN_POINT('',(-4.91824999938284,-7.79148190512436E-5,29.1398594360263));
#29496=CARTESIAN_POINT('Ctrl Pts',(-4.76403458843593,1.2219482405921,29.0701077704777));
#29497=CARTESIAN_POINT('Ctrl Pts',(-4.802042410005,1.07376636956748,29.0787010901888));
#29498=CARTESIAN_POINT('Ctrl Pts',(-4.83311838314403,0.923882229251823,
29.0872522276148));
#29499=CARTESIAN_POINT('Ctrl Pts',(-4.87533993350278,0.658508237472935,
29.1023205217532));
#29500=CARTESIAN_POINT('Ctrl Pts',(-4.88948270101306,0.543627632427015,
29.1088198289951));
#29501=CARTESIAN_POINT('Ctrl Pts',(-4.90547693217398,0.360684861074001,
29.119178406903));
#29502=CARTESIAN_POINT('Ctrl Pts',(-4.90999061135142,0.292898552021269,
29.1230182534322));
#29503=CARTESIAN_POINT('Ctrl Pts',(-4.91653386527548,0.150046150226172,
29.131121967292));
#29504=CARTESIAN_POINT('Ctrl Pts',(-4.91825135989444,0.0749831078358474,
29.1353869217918));
#29505=CARTESIAN_POINT('Ctrl Pts',(-4.91824999919212,-8.91444442064763E-5,
29.1396622504236));
#29506=CARTESIAN_POINT('Ctrl Pts',(-4.91824999938284,-7.79148190512436E-5,
29.1398594360263));
#29507=CARTESIAN_POINT('Ctrl Pts',(-4.91824765848413,-0.147843451538412,
29.1482253307768));
#29508=CARTESIAN_POINT('Ctrl Pts',(-4.91158170501074,-0.295582196842949,
29.1565912255273));
#29509=CARTESIAN_POINT('Ctrl Pts',(-4.89828533696788,-0.442700598763389,
29.1649571202777));
#29510=CARTESIAN_POINT('Ctrl Pts',(-4.88498458454875,-0.589867511858225,
29.1733257736184));
#29511=CARTESIAN_POINT('Ctrl Pts',(-4.86504907810585,-0.736413378442218,
29.1816944269591));
#29512=CARTESIAN_POINT('Ctrl Pts',(-4.83856387762818,-0.881749774375791,
29.1900630802997));
#29513=CARTESIAN_POINT('Ctrl Pts',(-4.83420068304682,-0.905692616558404,
29.1914417394094));
#29514=CARTESIAN_POINT('Ctrl Pts',(-4.829659845967,-0.929602652504876,29.192820398519));
#29515=CARTESIAN_POINT('Ctrl Pts',(-4.82494188036517,-0.953477274820037,
29.1941990576287));
#29516=CARTESIAN_POINT('Ctrl Pts',(-4.79702989473963,-1.09472207631175,
29.2023553513574));
#29517=CARTESIAN_POINT('Ctrl Pts',(-4.76290624681523,-1.23476683647118,
29.2105116450862));
#29518=CARTESIAN_POINT('Ctrl Pts',(-4.7226989765346,-1.3730613385931,29.218667938815));
#29519=CARTESIAN_POINT('Ctrl Pts',(-4.6824999011205,-1.51132765414629,29.2268225701644));
#29520=CARTESIAN_POINT('Ctrl Pts',(-4.63621977031956,-1.64784410216371,
29.2349772015138));
#29521=CARTESIAN_POINT('Ctrl Pts',(-4.58403679062399,-1.78207456766143,
29.2431318328631));
#29522=CARTESIAN_POINT('Ctrl Pts',(-4.53185195965433,-1.91630979519814,
29.251286753511));
#29523=CARTESIAN_POINT('Ctrl Pts',(-4.47376397850035,-2.04825856467408,
29.2594416741589));
#29524=CARTESIAN_POINT('Ctrl Pts',(-4.40999979152046,-2.17740324728552,
29.2675965948068));
#29525=CARTESIAN_POINT('Ctrl Pts',(-4.34623935342989,-2.30654033709063,
29.2757510360022));
#29526=CARTESIAN_POINT('Ctrl Pts',(-4.27680352617805,-2.43287337019581,
29.2839054771976));
#29527=CARTESIAN_POINT('Ctrl Pts',(-4.20196592304876,-2.55590794905391,
29.2920599183931));
#29528=CARTESIAN_POINT('Ctrl Pts',(-4.12710987323732,-2.67897285464183,
29.3002163695725));
#29529=CARTESIAN_POINT('Ctrl Pts',(-4.04684956074285,-2.79873739519221,
29.3083728207519));
#29530=CARTESIAN_POINT('Ctrl Pts',(-3.96150309315888,-2.91473434559526,
29.3165292719314));
#29531=CARTESIAN_POINT('Ctrl Pts',(-3.90329093529433,-2.99385223974859,
29.3220925323347));
#29532=CARTESIAN_POINT('Ctrl Pts',(-3.84271352873989,-3.07121795879998,
29.327655792738));
#29533=CARTESIAN_POINT('Ctrl Pts',(-3.77988294458199,-3.14669159400126,
29.3332190531413));
#29534=CARTESIAN_POINT('Ctrl Pts',(-3.68776705167079,-3.25734345871013,
29.3413753468701));
#29535=CARTESIAN_POINT('Ctrl Pts',(-3.59077176250648,-3.36396837172811,
29.349531640599));
#29536=CARTESIAN_POINT('Ctrl Pts',(-3.48927286645023,-3.46614453333299,
29.3576879343279));
#29537=CARTESIAN_POINT('Ctrl Pts',(-3.38779465744623,-3.56829986984838,
29.3658425656773));
#29538=CARTESIAN_POINT('Ctrl Pts',(-3.28181490841962,-3.66600802653415,
29.3739971970268));
#29539=CARTESIAN_POINT('Ctrl Pts',(-3.17174670474582,-3.75888359801604,
29.3821518283762));
#29540=CARTESIAN_POINT('Ctrl Pts',(-3.06167459622795,-3.85176246440612,
29.3903067490242));
#29541=CARTESIAN_POINT('Ctrl Pts',(-2.94751399615763,-3.93980818385149,
29.3984616696721));
#29542=CARTESIAN_POINT('Ctrl Pts',(-2.82971193284848,-4.02267491100075,
29.40661659032));
#29543=CARTESIAN_POINT('Ctrl Pts',(-2.71191679547886,-4.10553676616454,
29.4147710315155));
#29544=CARTESIAN_POINT('Ctrl Pts',(-2.59048089746017,-4.18322004642729,
29.422925472711));
#29545=CARTESIAN_POINT('Ctrl Pts',(-2.4658811222088,-4.25542164228579,29.4310799139065));
#29546=CARTESIAN_POINT('Ctrl Pts',(-2.34125063442296,-4.32764103507849,
29.439236365086));
#29547=CARTESIAN_POINT('Ctrl Pts',(-2.21345500063114,-4.3943758754473,29.4473928162655));
#29548=CARTESIAN_POINT('Ctrl Pts',(-2.08299716353332,-4.45536820916208,
29.455549267445));
#29549=CARTESIAN_POINT('Ctrl Pts',(-1.99401595057698,-4.49696917354807,
29.4611125278479));
#29550=CARTESIAN_POINT('Ctrl Pts',(-1.90379676687354,-4.53589956732471,
29.4666757882507));
#29551=CARTESIAN_POINT('Ctrl Pts',(-1.81250498017415,-4.57209019588895,
29.4722390486536));
#29552=CARTESIAN_POINT('Ctrl Pts',(-1.67866213022207,-4.62514926115345,
29.4803953423824));
#29553=CARTESIAN_POINT('Ctrl Pts',(-1.54246275836423,-4.67233706997473,
29.4885516361112));
#29554=CARTESIAN_POINT('Ctrl Pts',(-1.40443870803326,-4.71346316182463,
29.49670792984));
#29555=CARTESIAN_POINT('Ctrl Pts',(-1.26644278914871,-4.7545808715379,29.5048625611894));
#29556=CARTESIAN_POINT('Ctrl Pts',(-1.1266232542291,-4.78963923346716,29.5130171925388));
#29557=CARTESIAN_POINT('Ctrl Pts',(-0.985527271686252,-4.81849759357236,
29.5211718238881));
#29558=CARTESIAN_POINT('Ctrl Pts',(-0.844426283539492,-4.84735697747369,
29.529326744536));
#29559=CARTESIAN_POINT('Ctrl Pts',(-0.70204908425379,-4.87001584867918,
29.5374816651839));
#29560=CARTESIAN_POINT('Ctrl Pts',(-0.558953707926475,-4.8863845340799,
29.5456365858317));
#29561=CARTESIAN_POINT('Ctrl Pts',(-0.415866744608908,-4.90275225711612,
29.5537910270272));
#29562=CARTESIAN_POINT('Ctrl Pts',(-0.272062021327598,-4.91283049712567,
29.5619454682226));
#29563=CARTESIAN_POINT('Ctrl Pts',(-0.128103328596984,-4.91658139358054,
29.570099909418));
#29564=CARTESIAN_POINT('Ctrl Pts',(0.0158908484375917,-4.92033321459194,
29.5782563605975));
#29565=CARTESIAN_POINT('Ctrl Pts',(0.160038736072495,-4.9177545666176,29.5864128117769));
#29566=CARTESIAN_POINT('Ctrl Pts',(0.303775278191233,-4.90885970902203,
29.5945692629564));
#29567=CARTESIAN_POINT('Ctrl Pts',(0.401813480797395,-4.90279280468265,
29.6001325233597));
#29568=CARTESIAN_POINT('Ctrl Pts',(0.499660302309726,-4.89378857294753,
29.605695783763));
#29569=CARTESIAN_POINT('Ctrl Pts',(0.597137429250602,-4.88186541734694,
29.6112590441663));
#29570=CARTESIAN_POINT('Ctrl Pts',(0.740048603910757,-4.864384883954,29.6194153378952));
#29571=CARTESIAN_POINT('Ctrl Pts',(0.882218417583596,-4.84062141879297,
29.627571631624));
#29572=CARTESIAN_POINT('Ctrl Pts',(1.02308874644461,-4.81066237428884,29.6357279253529));
#29573=CARTESIAN_POINT('Ctrl Pts',(1.16393036374331,-4.78070943590359,29.6438825567024));
#29574=CARTESIAN_POINT('Ctrl Pts',(1.30347269746603,-4.74456350686749,29.6520371880518));
#29575=CARTESIAN_POINT('Ctrl Pts',(1.44116800925092,-4.7023630050871,29.6601918194013));
#29576=CARTESIAN_POINT('Ctrl Pts',(1.57886820599569,-4.66016100617688,29.6683467400492));
#29577=CARTESIAN_POINT('Ctrl Pts',(1.71472092863266,-4.61190409917613,29.6765016606972));
#29578=CARTESIAN_POINT('Ctrl Pts',(1.84819330167373,-4.55778066411147,29.6846565813451));
#29579=CARTESIAN_POINT('Ctrl Pts',(1.98165782747046,-4.50366041112719,29.6928110225406));
#29580=CARTESIAN_POINT('Ctrl Pts',(2.11274197387535,-4.44367444675716,29.7009654637361));
#29581=CARTESIAN_POINT('Ctrl Pts',(2.24093261227665,-4.3780593976938,29.7091199049317));
#29582=CARTESIAN_POINT('Ctrl Pts',(2.36915484832234,-4.3124281752108,29.7172763561112));
#29583=CARTESIAN_POINT('Ctrl Pts',(2.49448185305424,-4.24116524781992,29.7254328072907));
#29584=CARTESIAN_POINT('Ctrl Pts',(2.61642433475618,-4.16455360909134,29.7335892584702));
#29585=CARTESIAN_POINT('Ctrl Pts',(2.69959748996079,-4.11229920496967,29.739152518873));
#29586=CARTESIAN_POINT('Ctrl Pts',(2.78119661061453,-4.05755744599145,29.7447157792758));
#29587=CARTESIAN_POINT('Ctrl Pts',(2.86107394730348,-4.00042984322451,29.7502790396786));
#29588=CARTESIAN_POINT('Ctrl Pts',(2.97818207691382,-3.91667508891653,29.7584353334074));
#29589=CARTESIAN_POINT('Ctrl Pts',(3.0916318601361,-3.82775880872764,29.7665916271362));
#29590=CARTESIAN_POINT('Ctrl Pts',(3.20097507904098,-3.73402485340666,29.774747920865));
#29591=CARTESIAN_POINT('Ctrl Pts',(3.31029601209859,-3.64031000252245,29.7829025522144));
#29592=CARTESIAN_POINT('Ctrl Pts',(3.41551179664554,-3.54177965304348,29.7910571835638));
#29593=CARTESIAN_POINT('Ctrl Pts',(3.51620777652833,-3.43881751984337,29.7992118149132));
#29594=CARTESIAN_POINT('Ctrl Pts',(3.61690732876088,-3.33585173389811,29.807366735561));
#29595=CARTESIAN_POINT('Ctrl Pts',(3.71308651880639,-3.22845408623791,29.8155216562089));
#29596=CARTESIAN_POINT('Ctrl Pts',(3.80436765529465,-3.11704504392347,29.8236765768568));
#29597=CARTESIAN_POINT('Ctrl Pts',(3.8956434250889,-3.00564255168349,29.8318310180522));
#29598=CARTESIAN_POINT('Ctrl Pts',(3.98202150608234,-2.89022939609205,29.8399854592477));
#29599=CARTESIAN_POINT('Ctrl Pts',(4.06316463869261,-2.7712589524218,29.8481399004431));
#29600=CARTESIAN_POINT('Ctrl Pts',(4.14432777223184,-2.65225918378817,29.8562963516225));
#29601=CARTESIAN_POINT('Ctrl Pts',(4.22025319011674,-2.52970065142921,29.864452802802));
#29602=CARTESIAN_POINT('Ctrl Pts',(4.29064675578168,-2.40406603062398,29.8726092539814));
#29603=CARTESIAN_POINT('Ctrl Pts',(4.33866000663017,-2.31837458273388,29.8781725143847));
#29604=CARTESIAN_POINT('Ctrl Pts',(4.38410064538988,-2.23125268526632,29.883735774788));
#29605=CARTESIAN_POINT('Ctrl Pts',(4.42688753864598,-2.1428601873853,29.8892990351913));
#29606=CARTESIAN_POINT('Ctrl Pts',(4.48961738478709,-2.01326798355508,29.8974553289202));
#29607=CARTESIAN_POINT('Ctrl Pts',(4.54666456236093,-1.88089510972097,29.9056116226491));
#29608=CARTESIAN_POINT('Ctrl Pts',(4.59780012777975,-1.74625801286308,29.913767916378));
#29609=CARTESIAN_POINT('Ctrl Pts',(4.64892527097563,-1.61164835713792,29.9219225477274));
#29610=CARTESIAN_POINT('Ctrl Pts',(4.69414108692694,-1.47477571168039,29.9300771790769));
#29611=CARTESIAN_POINT('Ctrl Pts',(4.73326718081661,-1.33617545910121,29.9382318104263));
#29612=CARTESIAN_POINT('Ctrl Pts',(4.77239466276659,-1.19757028945801,29.9463867310743));
#29613=CARTESIAN_POINT('Ctrl Pts',(4.8054318958188,-1.05723771108288,29.9545416517222));
#29614=CARTESIAN_POINT('Ctrl Pts',(4.83224853217211,-0.915727681038694,
29.9626965723702));
#29615=CARTESIAN_POINT('Ctrl Pts',(4.85906359189428,-0.774225970797069,
29.9708510135657));
#29616=CARTESIAN_POINT('Ctrl Pts',(4.87965872522313,-0.631547276370576,
29.9790054547612));
#29617=CARTESIAN_POINT('Ctrl Pts',(4.89395483540549,-0.488251094736334,
29.9871598959567));
#29618=CARTESIAN_POINT('Ctrl Pts',(4.90825446942869,-0.344919592100032,
29.9953163471362));
#29619=CARTESIAN_POINT('Ctrl Pts',(4.91625194430766,-0.200970631246002,
30.0034727983157));
#29620=CARTESIAN_POINT('Ctrl Pts',(4.91792005009626,-0.0569687928709609,
30.0116292494952));
#29621=CARTESIAN_POINT('Ctrl Pts',(4.91905781291457,0.0412503600095018,
30.017192509898));
#29622=CARTESIAN_POINT('Ctrl Pts',(4.91725212223471,0.139494017049788,30.0227557703008));
#29623=CARTESIAN_POINT('Ctrl Pts',(4.91250825778637,0.237582995352652,30.0283190307037));
#29624=CARTESIAN_POINT('Ctrl Pts',(4.90555328012063,0.381391205047743,30.0364753244324));
#29625=CARTESIAN_POINT('Ctrl Pts',(4.89227792431803,0.524920725092011,30.0446316181612));
#29626=CARTESIAN_POINT('Ctrl Pts',(4.87272838503889,0.667608529106876,30.05278791189));
#29627=CARTESIAN_POINT('Ctrl Pts',(4.85318283025969,0.81026725112974,30.0609425432394));
#29628=CARTESIAN_POINT('Ctrl Pts',(4.8273656884833,0.952084268009815,30.0690971745888));
#29629=CARTESIAN_POINT('Ctrl Pts',(4.79537484388121,1.09250316666418,30.0772518059382));
#29630=CARTESIAN_POINT('Ctrl Pts',(4.76338286435311,1.23292704690194,30.085406726586));
#29631=CARTESIAN_POINT('Ctrl Pts',(4.72521681440178,1.3719523825493,30.0935616472339));
#29632=CARTESIAN_POINT('Ctrl Pts',(4.68102549561008,1.50903392007881,30.1017165678818));
#29633=CARTESIAN_POINT('Ctrl Pts',(4.63683677495964,1.6461073981702,30.1098710090772));
#29634=CARTESIAN_POINT('Ctrl Pts',(4.58662359776409,1.78123698854771,30.1180254502726));
#29635=CARTESIAN_POINT('Ctrl Pts',(4.53058433028458,1.91389359387606,30.1261798914681));
#29636=CARTESIAN_POINT('Ctrl Pts',(4.47453124971487,2.04658289766279,30.1343363426475));
#29637=CARTESIAN_POINT('Ctrl Pts',(4.41264933934322,2.17679768984758,30.1424927938269));
#29638=CARTESIAN_POINT('Ctrl Pts',(4.34518495526843,2.30402924612707,30.1506492450064));
#29639=CARTESIAN_POINT('Ctrl Pts',(4.2991696076251,2.39080991378888,30.1562125054097));
#29640=CARTESIAN_POINT('Ctrl Pts',(4.25055818921169,2.47620316099904,30.161775765813));
#29641=CARTESIAN_POINT('Ctrl Pts',(4.19944110460985,2.56005419306179,30.1673390262164));
#29642=CARTESIAN_POINT('Ctrl Pts',(4.12449836845348,2.68298815577239,30.1754953199452));
#29643=CARTESIAN_POINT('Ctrl Pts',(4.04413976298961,2.80265207148643,30.1836516136741));
#29644=CARTESIAN_POINT('Ctrl Pts',(3.95867534929238,2.91857371697288,30.1918079074029));
#29645=CARTESIAN_POINT('Ctrl Pts',(3.87322835457088,3.03447173582639,30.1999625387523));
#29646=CARTESIAN_POINT('Ctrl Pts',(3.78267782610433,3.14662873686053,30.2081171701018));
#29647=CARTESIAN_POINT('Ctrl Pts',(3.68737604260045,3.25460304537378,30.2162718014512));
#29648=CARTESIAN_POINT('Ctrl Pts',(3.59207087811443,3.3625811844471,30.2244267220991));
#29649=CARTESIAN_POINT('Ctrl Pts',(3.49201433992864,3.46637608069595,30.2325816427471));
#29650=CARTESIAN_POINT('Ctrl Pts',(3.38759807033757,3.56558022996892,30.240736563395));
#29651=CARTESIAN_POINT('Ctrl Pts',(3.28318793969473,3.66477854672996,30.2488910045905));
#29652=CARTESIAN_POINT('Ctrl Pts',(3.17441883372558,3.75938642666932,30.257045445786));
#29653=CARTESIAN_POINT('Ctrl Pts',(3.06171817888996,3.84903427570537,30.2651998869814));
#29654=CARTESIAN_POINT('Ctrl Pts',(2.94898974452789,3.93870422199363,30.2733563381609));
#29655=CARTESIAN_POINT('Ctrl Pts',(2.83232808672348,4.02341148575304,30.2815127893404));
#29656=CARTESIAN_POINT('Ctrl Pts',(2.71219301493423,4.10282733151688,30.2896692405199));
#29657=CARTESIAN_POINT('Ctrl Pts',(2.63025263753481,4.15699439760729,30.2952325009229));
#29658=CARTESIAN_POINT('Ctrl Pts',(2.54669703231131,4.20870065935219,30.3007957613258));
#29659=CARTESIAN_POINT('Ctrl Pts',(2.46167966931954,4.25785348129299,30.3063590217287));
#29660=CARTESIAN_POINT('Ctrl Pts',(2.33703574931766,4.32991641279615,30.3145153154575));
#29661=CARTESIAN_POINT('Ctrl Pts',(2.20920198048032,4.39651585529299,30.3226716091864));
#29662=CARTESIAN_POINT('Ctrl Pts',(2.07867663313013,4.45738561461523,30.3308279029152));
#29663=CARTESIAN_POINT('Ctrl Pts',(1.9481778888743,4.51824296773451,30.3389825342646));
#29664=CARTESIAN_POINT('Ctrl Pts',(1.81498896361117,4.57337282601228,30.3471371656141));
#29665=CARTESIAN_POINT('Ctrl Pts',(1.67963057200864,4.62255602497946,30.3552917969635));
#29666=CARTESIAN_POINT('Ctrl Pts',(1.5442673783522,4.67174096879874,30.3634467176114));
#29667=CARTESIAN_POINT('Ctrl Pts',(1.40673487758352,4.71497871334307,30.3716016382593));
#29668=CARTESIAN_POINT('Ctrl Pts',(1.26757198913018,4.75209893782448,30.3797565589072));
#29669=CARTESIAN_POINT('Ctrl Pts',(1.1284172824838,4.78921697989566,30.3879110001027));
#29670=CARTESIAN_POINT('Ctrl Pts',(0.987632703526648,4.82021813612847,30.3960654412981));
#29671=CARTESIAN_POINT('Ctrl Pts',(0.845770443741198,4.84498249934856,30.4042198824936));
#29672=CARTESIAN_POINT('Ctrl Pts',(0.703873216400462,4.86975296672378,30.4123763336731));
#29673=CARTESIAN_POINT('Ctrl Pts',(0.56089810720643,4.88828351140401,30.4205327848526));
#29674=CARTESIAN_POINT('Ctrl Pts',(0.417406182111368,4.90050560061257,30.4286892360321));
#29675=CARTESIAN_POINT('Ctrl Pts',(0.319534825135521,4.90884190563552,30.4342524964351));
#29676=CARTESIAN_POINT('Ctrl Pts',(0.221423210660194,4.91424447664097,30.4398157568382));
#29677=CARTESIAN_POINT('Ctrl Pts',(0.123250426401515,4.91670544113554,30.4453790172413));
#29678=CARTESIAN_POINT('Ctrl Pts',(-0.0206806511637789,4.92031346014232,
30.4535353109701));
#29679=CARTESIAN_POINT('Ctrl Pts',(-0.164797210693284,4.91759767932967,
30.461691604699));
#29680=CARTESIAN_POINT('Ctrl Pts',(-0.308534354211583,4.90856288691214,
30.4698478984278));
#29681=CARTESIAN_POINT('Ctrl Pts',(-0.452242201866507,4.8995299359257,30.4780025297772));
#29682=CARTESIAN_POINT('Ctrl Pts',(-0.595570453989007,4.88418056362306,
30.4861571611267));
#29683=CARTESIAN_POINT('Ctrl Pts',(-0.737957018130757,4.86257159349778,
30.4943117924761));
#29684=CARTESIAN_POINT('Ctrl Pts',(-0.88034863366171,4.84096185676001,30.502466713124));
#29685=CARTESIAN_POINT('Ctrl Pts',(-1.02179816294776,4.81309212432972,30.5106216337719));
#29686=CARTESIAN_POINT('Ctrl Pts',(-1.16175090970224,4.77907081829784,30.5187765544199));
#29687=CARTESIAN_POINT('Ctrl Pts',(-1.30169542821143,4.74505151248145,30.5269309956153));
#29688=CARTESIAN_POINT('Ctrl Pts',(-1.44014301527523,4.70488143660295,30.5350854368108));
#29689=CARTESIAN_POINT('Ctrl Pts',(-1.57655145314084,4.6587196286211,30.5432398780063));
#29690=CARTESIAN_POINT('Ctrl Pts',(-1.71299351425211,4.61254644223895,30.5513963291857));
#29691=CARTESIAN_POINT('Ctrl Pts',(-1.84739510458777,4.56037867967971,30.5595527803652));
#29692=CARTESIAN_POINT('Ctrl Pts',(-1.97923080588844,4.50242473335449,30.5677092315447));
#29693=CARTESIAN_POINT('Ctrl Pts',(-2.06915181695286,4.46289615803442,30.5732724919478));
#29694=CARTESIAN_POINT('Ctrl Pts',(-2.15787949060853,4.42067677153921,30.5788357523508));
#29695=CARTESIAN_POINT('Ctrl Pts',(-2.24525282018892,4.37584538528656,30.5843990127539));
#29696=CARTESIAN_POINT('Ctrl Pts',(-2.37335082180918,4.31011810882348,30.5925553064828));
#29697=CARTESIAN_POINT('Ctrl Pts',(-2.49858467956924,4.23874977504249,30.6007116002116));
#29698=CARTESIAN_POINT('Ctrl Pts',(-2.62046070707022,4.1620149861817,30.6088678939405));
#29699=CARTESIAN_POINT('Ctrl Pts',(-2.7423118943428,4.08529583706336,30.6170225252899));
#29700=CARTESIAN_POINT('Ctrl Pts',(-2.86080633362388,4.00321259306017,30.6251771566394));
#29701=CARTESIAN_POINT('Ctrl Pts',(-2.97547770934493,3.91608420028113,30.6333317879888));
#29702=CARTESIAN_POINT('Ctrl Pts',(-3.09015315321498,3.8289527164841,30.6414867086368));
#29703=CARTESIAN_POINT('Ctrl Pts',(-3.20100499340322,3.73677592521895,30.6496416292847));
#29704=CARTESIAN_POINT('Ctrl Pts',(-3.30759810670668,3.63991453567393,30.6577965499326));
#29705=CARTESIAN_POINT('Ctrl Pts',(-3.41418495307859,3.54305884090299,30.6659509911281));
#29706=CARTESIAN_POINT('Ctrl Pts',(-3.51651332644803,3.4415193246371,30.6741054323236));
#29707=CARTESIAN_POINT('Ctrl Pts',(-3.61418328788132,3.33569516354528,30.6822598735191));
#29708=CARTESIAN_POINT('Ctrl Pts',(-3.71187732393316,3.22984491791044,30.6904163246986));
#29709=CARTESIAN_POINT('Ctrl Pts',(-3.80491042634352,3.11970816295925,30.6985727758781));
#29710=CARTESIAN_POINT('Ctrl Pts',(-3.89292103043636,3.00571936702119,30.7067292270576));
#29711=CARTESIAN_POINT('Ctrl Pts',(-3.95295031253593,2.92797117226574,30.7122924874605));
#29712=CARTESIAN_POINT('Ctrl Pts',(-4.01064384535679,2.84843166674513,30.7178557478634));
#29713=CARTESIAN_POINT('Ctrl Pts',(-4.06589799008391,2.76724711522691,30.7234190082663));
#29714=CARTESIAN_POINT('Ctrl Pts',(-4.14691033137735,2.64821621486946,30.7315757312179));
#29715=CARTESIAN_POINT('Ctrl Pts',(-4.22270722572797,2.52560308161383,30.7397324541694));
#29716=CARTESIAN_POINT('Ctrl Pts',(-4.29298661487559,2.39988520287929,30.747889177121));
#29717=CARTESIAN_POINT('Ctrl Pts',(-4.36324999464958,2.27419596219239,30.7560440420025));
#29718=CARTESIAN_POINT('Ctrl Pts',(-4.42799821415893,2.14540367937789,30.7641989068841));
#29719=CARTESIAN_POINT('Ctrl Pts',(-4.48697450016212,2.01401164281514,30.7723537717656));
#29720=CARTESIAN_POINT('Ctrl Pts',(-4.54595262536498,1.88261550873781,30.78050889096));
#29721=CARTESIAN_POINT('Ctrl Pts',(-4.59915831640787,1.74861976248036,30.7886640101543));
#29722=CARTESIAN_POINT('Ctrl Pts',(-4.64638218564289,1.61254942480544,30.7968191293487));
#29723=CARTESIAN_POINT('Ctrl Pts',(-4.69097963986471,1.48404681047704,30.8045206913095));
#29724=CARTESIAN_POINT('Ctrl Pts',(-4.73024244860134,1.35369434642745,30.8122222532703));
#29725=CARTESIAN_POINT('Ctrl Pts',(-4.76403458704967,1.22194824599672,30.8199238152312));
#29726=CARTESIAN_POINT('Origin',(0.,0.,-3.23514056400928));
#29727=CARTESIAN_POINT('',(-4.76403458699526,1.22194824620887,32.9149784811847));
#29728=CARTESIAN_POINT('',(-4.7639087307945,1.22191632179108,32.5699348864137));
#29729=CARTESIAN_POINT('',(-4.76403458704967,1.22194824599672,-3.23514056400928));
#29730=CARTESIAN_POINT('Ctrl Pts',(-4.76403458699526,1.22194824620887,32.9149784811847));
#29731=CARTESIAN_POINT('Ctrl Pts',(-4.76018292856304,1.23696478561248,32.914096809347));
#29732=CARTESIAN_POINT('Ctrl Pts',(-4.75626023845671,1.25196323894184,32.913215832861));
#29733=CARTESIAN_POINT('Ctrl Pts',(-4.74299936564893,1.30170438629748,32.9102931210259));
#29734=CARTESIAN_POINT('Ctrl Pts',(-4.73335096376061,1.33636296809984,32.9082552859967));
#29735=CARTESIAN_POINT('Ctrl Pts',(-4.70648053371979,1.42894194166121,32.9028069210402));
#29736=CARTESIAN_POINT('Ctrl Pts',(-4.68856992295052,1.48665607831358,32.8994042528157));
#29737=CARTESIAN_POINT('Ctrl Pts',(-4.61433833648949,1.71115478318329,32.886114885965));
#29738=CARTESIAN_POINT('Ctrl Pts',(-4.55014354245029,1.87519686592309,32.8762831571679));
#29739=CARTESIAN_POINT('Ctrl Pts',(-4.4445569498971,2.10745185009664,32.8619688464675));
#29740=CARTESIAN_POINT('Ctrl Pts',(-4.41008908127384,2.17865874367186,32.8575247823227));
#29741=CARTESIAN_POINT('Ctrl Pts',(-4.34517185633154,2.30491144609587,32.8495277519827));
#29742=CARTESIAN_POINT('Ctrl Pts',(-4.31535542122827,2.36026327349465,32.8459798651798));
#29743=CARTESIAN_POINT('Ctrl Pts',(-4.25255231288962,2.47168188483448,32.8387452102819));
#29744=CARTESIAN_POINT('Ctrl Pts',(-4.21949797038691,2.52769643564737,32.835058580705));
#29745=CARTESIAN_POINT('Ctrl Pts',(-4.12707306785472,2.67745412836762,32.8250596862963));
#29746=CARTESIAN_POINT('Ctrl Pts',(-4.06562578694426,2.76986988618575,32.8187336113795));
#29747=CARTESIAN_POINT('Ctrl Pts',(-3.89306218684569,3.01127358511089,32.8017718474213));
#29748=CARTESIAN_POINT('Ctrl Pts',(-3.77654000587387,3.15617610581573,32.7911169611383));
#29749=CARTESIAN_POINT('Ctrl Pts',(-3.63442343299359,3.31373594136351,32.7790205807154));
#29750=CARTESIAN_POINT('Ctrl Pts',(-3.61658937575484,3.33319079522321,32.7775176231088));
#29751=CARTESIAN_POINT('Ctrl Pts',(-3.57633705161436,3.37639793655675,32.7741592419134));
#29752=CARTESIAN_POINT('Ctrl Pts',(-3.55383695770197,3.40007244587523,32.7723049630081));
#29753=CARTESIAN_POINT('Ctrl Pts',(-3.50208408780507,3.45345160756979,32.7680929386374));
#29754=CARTESIAN_POINT('Ctrl Pts',(-3.47268599138694,3.48301206161135,32.7657378992747));
#29755=CARTESIAN_POINT('Ctrl Pts',(-3.36516536396561,3.58841178598861,32.7572493145126));
#29756=CARTESIAN_POINT('Ctrl Pts',(-3.28490511314195,3.66202620814661,32.7511449553386));
#29757=CARTESIAN_POINT('Ctrl Pts',(-3.09565416227081,3.82437435529634,32.7371728841549));
#29758=CARTESIAN_POINT('Ctrl Pts',(-2.98517245241386,3.91122219310184,32.7293129700433));
#29759=CARTESIAN_POINT('Ctrl Pts',(-2.81526543242159,4.03338531598615,32.7175533308351));
#29760=CARTESIAN_POINT('Ctrl Pts',(-2.7585688035132,4.07237210951318,32.7136807670107));
#29761=CARTESIAN_POINT('Ctrl Pts',(-2.6468363617085,4.14579936914446,32.7061370505693));
#29762=CARTESIAN_POINT('Ctrl Pts',(-2.59189956983937,4.18036501229515,32.7024676775597));
#29763=CARTESIAN_POINT('Ctrl Pts',(-2.493951415639,4.23931975303067,32.6959886889768));
#29764=CARTESIAN_POINT('Ctrl Pts',(-2.45122605717117,4.26416655353984,32.6931831198771));
#29765=CARTESIAN_POINT('Ctrl Pts',(-2.28216540303006,4.35910265538149,32.6821579417854));
#29766=CARTESIAN_POINT('Ctrl Pts',(-2.15314288106775,4.42425470442737,32.6739061271532));
#29767=CARTESIAN_POINT('Ctrl Pts',(-1.92078185345519,4.52901447172894,32.6593188151783));
#29768=CARTESIAN_POINT('Ctrl Pts',(-1.81862210390815,4.57099428774983,32.6529947957574));
#29769=CARTESIAN_POINT('Ctrl Pts',(-1.68382211936691,4.62115163674049,32.6447788025502));
#29770=CARTESIAN_POINT('Ctrl Pts',(-1.65239019751979,4.63248378638489,32.6428720335531));
#29771=CARTESIAN_POINT('Ctrl Pts',(-1.60873744627857,4.64772109200645,32.6402369563724));
#29772=CARTESIAN_POINT('Ctrl Pts',(-1.59661324796914,4.65190000513202,32.6395064701106));
#29773=CARTESIAN_POINT('Ctrl Pts',(-1.57646755726513,4.65875569322073,32.6382950315472));
#29774=CARTESIAN_POINT('Ctrl Pts',(-1.56845526880095,4.66145928206874,32.6378138351496));
#29775=CARTESIAN_POINT('Ctrl Pts',(-1.52924068565654,4.67457891824853,32.6354617549767));
#29776=CARTESIAN_POINT('Ctrl Pts',(-1.49794121652518,4.68470247466156,32.6335938203768));
#29777=CARTESIAN_POINT('Ctrl Pts',(-1.42749105346604,4.7067107607663,32.6294116986244));
#29778=CARTESIAN_POINT('Ctrl Pts',(-1.38828878761749,4.71842253080182,32.6270999992584));
#29779=CARTESIAN_POINT('Ctrl Pts',(-1.26988528690195,4.75219246801465,32.6201569861744));
#29780=CARTESIAN_POINT('Ctrl Pts',(-1.19027218020022,4.77275541734493,32.6155406316724));
#29781=CARTESIAN_POINT('Ctrl Pts',(-0.967442638585062,4.82438656597629,
32.6027136715575));
#29782=CARTESIAN_POINT('Ctrl Pts',(-0.823298387203489,4.85106490491087,
32.5945208375277));
#29783=CARTESIAN_POINT('Ctrl Pts',(-0.604038665995732,4.88159027870891,
32.5820938449706));
#29784=CARTESIAN_POINT('Ctrl Pts',(-0.529673063597622,4.89021805896607,
32.5778855295306));
#29785=CARTESIAN_POINT('Ctrl Pts',(-0.392486488953327,4.90296816158783,
32.5701200485514));
#29786=CARTESIAN_POINT('Ctrl Pts',(-0.329727398983781,4.90758822378181,
32.5665667637238));
#29787=CARTESIAN_POINT('Ctrl Pts',(-0.203981771667592,4.91442209888197,
32.5594390330053));
#29788=CARTESIAN_POINT('Ctrl Pts',(-0.141006709061911,4.91663199026831,
32.5558652248059));
#29789=CARTESIAN_POINT('Ctrl Pts',(0.142638215829047,4.92113137197392,32.5397397685698));
#29790=CARTESIAN_POINT('Ctrl Pts',(0.363266470963693,4.9097774368799,32.5271056694717));
#29791=CARTESIAN_POINT('Ctrl Pts',(0.649454668650239,4.87564914118715,32.5106155754782));
#29792=CARTESIAN_POINT('Ctrl Pts',(0.716356795105859,4.8662695113464,32.5067545327153));
#29793=CARTESIAN_POINT('Ctrl Pts',(0.793427863182637,4.85384032499064,32.5023034779221));
#29794=CARTESIAN_POINT('Ctrl Pts',(0.803805554382793,4.85213255238824,32.5017040757773));
#29795=CARTESIAN_POINT('Ctrl Pts',(0.820567929498528,4.84931885125798,32.5007358256911));
#29796=CARTESIAN_POINT('Ctrl Pts',(0.826956036905678,4.84823357123718,32.500366809505));
#29797=CARTESIAN_POINT('Ctrl Pts',(0.837254210250674,4.84646306163683,32.4997719011601));
#29798=CARTESIAN_POINT('Ctrl Pts',(0.841165620263379,4.84578571747843,32.4995459401999));
#29799=CARTESIAN_POINT('Ctrl Pts',(0.847477672439167,4.84468477815542,32.4991812877789));
#29800=CARTESIAN_POINT('Ctrl Pts',(0.849878825761404,4.8442641326114,32.4990425695278));
#29801=CARTESIAN_POINT('Ctrl Pts',(0.853760958144185,4.84358106683526,32.4988182905467));
#29802=CARTESIAN_POINT('Ctrl Pts',(0.855242130736293,4.8433197522435,32.4987327195303));
#29803=CARTESIAN_POINT('Ctrl Pts',(0.860443616203352,4.84239962421464,32.4984322150544));
#29804=CARTESIAN_POINT('Ctrl Pts',(0.864163291764906,4.84173720295352,32.498217315764));
#29805=CARTESIAN_POINT('Ctrl Pts',(0.900114224704042,4.83529210472728,32.4961402760202));
#29806=CARTESIAN_POINT('Ctrl Pts',(0.932287951571422,4.82919191577159,32.4942812808667));
#29807=CARTESIAN_POINT('Ctrl Pts',(1.0057818365604,4.8144955100474,32.490035696042));
#29808=CARTESIAN_POINT('Ctrl Pts',(1.04705721484502,4.80568781375992,32.4876518998469));
#29809=CARTESIAN_POINT('Ctrl Pts',(1.237784048469,4.76241497201226,32.4766271864561));
#29810=CARTESIAN_POINT('Ctrl Pts',(1.38568612253881,4.72150195589864,32.4680480810393));
#29811=CARTESIAN_POINT('Ctrl Pts',(1.62996084104978,4.64146099469856,32.4536462924904));
#29812=CARTESIAN_POINT('Ctrl Pts',(1.72744002102068,4.60607026231088,32.4478354389095));
#29813=CARTESIAN_POINT('Ctrl Pts',(1.86049615142849,4.55294460933225,32.4397806885209));
#29814=CARTESIAN_POINT('Ctrl Pts',(1.89708635675511,4.53782038841545,32.4375525732523));
#29815=CARTESIAN_POINT('Ctrl Pts',(1.99914616857937,4.49418473312649,32.4312979293522));
#29816=CARTESIAN_POINT('Ctrl Pts',(2.06418286655256,4.46468708399541,32.4272656470407));
#29817=CARTESIAN_POINT('Ctrl Pts',(2.18583592533629,4.40628435941377,32.4196250876773));
#29818=CARTESIAN_POINT('Ctrl Pts',(2.24257937561657,4.37767725864049,32.4160197626599));
#29819=CARTESIAN_POINT('Ctrl Pts',(2.39664270532158,4.29622483668842,32.4061101028396));
#29820=CARTESIAN_POINT('Ctrl Pts',(2.49275652416012,4.24118008997661,32.3997920427883));
#29821=CARTESIAN_POINT('Ctrl Pts',(2.70086432245889,4.11247627398828,32.3857994867055));
#29822=CARTESIAN_POINT('Ctrl Pts',(2.81187257550138,4.03738799354103,32.3781237791633));
#29823=CARTESIAN_POINT('Ctrl Pts',(2.96262852986172,3.92617677435083,32.3674170679473));
#29824=CARTESIAN_POINT('Ctrl Pts',(3.00506197851664,3.89379435023872,32.3643706497929));
#29825=CARTESIAN_POINT('Ctrl Pts',(3.08100310135131,3.83386016017592,32.3588619565415));
#29826=CARTESIAN_POINT('Ctrl Pts',(3.11468945864057,3.80654350727084,32.3563974897815));
#29827=CARTESIAN_POINT('Ctrl Pts',(3.17501683146691,3.75628629235269,32.3519480826966));
#29828=CARTESIAN_POINT('Ctrl Pts',(3.20178139767933,3.73349896181448,32.3499610428675));
#29829=CARTESIAN_POINT('Ctrl Pts',(3.2866283975543,3.65967684559354,32.3436149107833));
#29830=CARTESIAN_POINT('Ctrl Pts',(3.34375294630614,3.6075583560906,32.3392704268443));
#29831=CARTESIAN_POINT('Ctrl Pts',(3.53372647687359,3.4258425243478,32.3245213267037));
#29832=CARTESIAN_POINT('Ctrl Pts',(3.6604598571039,3.29008408981024,32.3141552575836));
#29833=CARTESIAN_POINT('Ctrl Pts',(3.80506657998011,3.11645355866329,32.3014541254059));
#29834=CARTESIAN_POINT('Ctrl Pts',(3.83053158783609,3.08510002955052,32.2991815122524));
#29835=CARTESIAN_POINT('Ctrl Pts',(3.90038456975401,2.99689591143864,32.2928426034525));
#29836=CARTESIAN_POINT('Ctrl Pts',(3.94391223809736,2.9393776545411,32.2887705624053));
#29837=CARTESIAN_POINT('Ctrl Pts',(4.02308190031293,2.82983539840941,32.281119339032));
#29838=CARTESIAN_POINT('Ctrl Pts',(4.05901904386205,2.77804259343399,32.2775434505342));
#29839=CARTESIAN_POINT('Ctrl Pts',(4.16562944127532,2.61790834981748,32.266606251059));
#29840=CARTESIAN_POINT('Ctrl Pts',(4.23303249981231,2.50745845763278,32.2592230363756));
#29841=CARTESIAN_POINT('Ctrl Pts',(4.36330262097211,2.273737399233,32.2439150719001));
#29842=CARTESIAN_POINT('Ctrl Pts',(4.42548213529523,2.15020919278186,32.2359945087281));
#29843=CARTESIAN_POINT('Ctrl Pts',(4.50728083199563,1.96907700271781,32.22464834033));
#29844=CARTESIAN_POINT('Ctrl Pts',(4.53116625406901,1.91347256187222,32.2212006027623));
#29845=CARTESIAN_POINT('Ctrl Pts',(4.56789802601181,1.82341467905926,32.2156779749613));
#29846=CARTESIAN_POINT('Ctrl Pts',(4.58139456278496,1.78923373776153,32.2135962190511));
#29847=CARTESIAN_POINT('Ctrl Pts',(4.61597437639223,1.69870048477678,32.2081187551943));
#29848=CARTESIAN_POINT('Ctrl Pts',(4.63640890647218,1.64210698853568,32.2047305994798));
#29849=CARTESIAN_POINT('Ctrl Pts',(4.71263510317002,1.41822066592116,32.1914378081139));
#29850=CARTESIAN_POINT('Ctrl Pts',(4.76045126248027,1.24835244530733,32.1815886750155));
#29851=CARTESIAN_POINT('Ctrl Pts',(4.8224956688736,0.971702539606581,32.1656814287329));
#29852=CARTESIAN_POINT('Ctrl Pts',(4.8425250117809,0.866384096647093,32.1596569747165));
#29853=CARTESIAN_POINT('Ctrl Pts',(4.86959068225973,0.693451372460276,32.1497793112096));
#29854=CARTESIAN_POINT('Ctrl Pts',(4.87869507938473,0.626196778192807,32.145941542014));
#29855=CARTESIAN_POINT('Ctrl Pts',(4.89563000022488,0.478103625737029,32.1374908114927));
#29856=CARTESIAN_POINT('Ctrl Pts',(4.90285583936344,0.397216025658544,32.1328749618724));
#29857=CARTESIAN_POINT('Ctrl Pts',(4.92041646629665,0.124628013814521,32.1173075435281));
#29858=CARTESIAN_POINT('Ctrl Pts',(4.92153172102713,-0.0674884544777613,
32.1063090537897));
#29859=CARTESIAN_POINT('Ctrl Pts',(4.90918679588407,-0.301427036670187,
32.0929113966732));
#29860=CARTESIAN_POINT('Ctrl Pts',(4.90641202517168,-0.343648541149271,
32.0904935439874));
#29861=CARTESIAN_POINT('Ctrl Pts',(4.89863565198554,-0.442470216021985,
32.084836833841));
#29862=CARTESIAN_POINT('Ctrl Pts',(4.8931973174559,-0.499030324074055,32.081601070888));
#29863=CARTESIAN_POINT('Ctrl Pts',(4.88262133299154,-0.592070839501786,
32.0762856762812));
#29864=CARTESIAN_POINT('Ctrl Pts',(4.87805172631186,-0.628609855692929,
32.07420047991));
#29865=CARTESIAN_POINT('Ctrl Pts',(4.86435175545564,-0.728987976991618,
32.0684763348319));
#29866=CARTESIAN_POINT('Ctrl Pts',(4.85437550692771,-0.792704271327938,
32.0648466293617));
#29867=CARTESIAN_POINT('Ctrl Pts',(4.81332895339126,-1.02488492589481,32.05160072899));
#29868=CARTESIAN_POINT('Ctrl Pts',(4.7747169036367,-1.19189078407979,32.0420317813659));
#29869=CARTESIAN_POINT('Ctrl Pts',(4.71358837224592,-1.40492025934216,32.0295963251768));
#29870=CARTESIAN_POINT('Ctrl Pts',(4.69896440756757,-1.45308283903252,32.0267696845918));
#29871=CARTESIAN_POINT('Ctrl Pts',(4.67194198512438,-1.53740081787702,32.0217898143954));
#29872=CARTESIAN_POINT('Ctrl Pts',(4.65985647048045,-1.57365207107422,32.0196385019994));
#29873=CARTESIAN_POINT('Ctrl Pts',(4.62437344509401,-1.67609104737681,32.0135273384163));
#29874=CARTESIAN_POINT('Ctrl Pts',(4.59997975761903,-1.74192337387047,32.0095617136981));
#29875=CARTESIAN_POINT('Ctrl Pts',(4.54694043371693,-1.87616988835343,32.0013863474544));
#29876=CARTESIAN_POINT('Ctrl Pts',(4.51813961937075,-1.94450378304214,31.9971764500812));
#29877=CARTESIAN_POINT('Ctrl Pts',(4.42285734052015,-2.15701587907758,31.9839203144985));
#29878=CARTESIAN_POINT('Ctrl Pts',(4.35093476627361,-2.29864094116732,31.9748416627817));
#29879=CARTESIAN_POINT('Ctrl Pts',(4.20813272919024,-2.54903385339887,31.9583406935008));
#29880=CARTESIAN_POINT('Ctrl Pts',(4.13955608773341,-2.65895291696665,31.9509285618532));
#29881=CARTESIAN_POINT('Ctrl Pts',(4.04354906234367,-2.80010563883098,31.9412131265006));
#29882=CARTESIAN_POINT('Ctrl Pts',(4.01994996802421,-2.83388124665608,31.9388729832889));
#29883=CARTESIAN_POINT('Ctrl Pts',(3.9710925466402,-2.90196862377059,31.9341262255734));
#29884=CARTESIAN_POINT('Ctrl Pts',(3.94580716555951,-2.93625676265668,31.9317201548369));
#29885=CARTESIAN_POINT('Ctrl Pts',(3.84557476440126,-3.06854325311272,31.9223651272712));
#29886=CARTESIAN_POINT('Ctrl Pts',(3.76739601596059,-3.16403711250589,31.9154540826268));
#29887=CARTESIAN_POINT('Ctrl Pts',(3.57432088167013,-3.38256027600637,31.8991175607479));
#29888=CARTESIAN_POINT('Ctrl Pts',(3.45653911578827,-3.50283032408301,31.8897001418591));
#29889=CARTESIAN_POINT('Ctrl Pts',(3.27962601469965,-3.66585188926085,31.8761474393099));
#29890=CARTESIAN_POINT('Ctrl Pts',(3.22534946573542,-3.71369594000595,31.8720631359297));
#29891=CARTESIAN_POINT('Ctrl Pts',(3.11534787214414,-3.80642973586241,31.8639187889937));
#29892=CARTESIAN_POINT('Ctrl Pts',(3.05965912469724,-3.85133555797317,31.8598599640447));
#29893=CARTESIAN_POINT('Ctrl Pts',(2.86341742712058,-4.00263580087408,31.8457649633492));
#29894=CARTESIAN_POINT('Ctrl Pts',(2.71814028785715,-4.1026777396443,31.8356839266383));
#29895=CARTESIAN_POINT('Ctrl Pts',(2.46771310301434,-4.25597801744582,31.8188757304435));
#29896=CARTESIAN_POINT('Ctrl Pts',(2.36545500087633,-4.31365041671854,31.812160277848));
#29897=CARTESIAN_POINT('Ctrl Pts',(2.22286554409817,-4.38747288319392,31.8030177059554));
#29898=CARTESIAN_POINT('Ctrl Pts',(2.18423947857324,-4.4068296411166,31.8005627224517));
#29899=CARTESIAN_POINT('Ctrl Pts',(2.10873297993352,-4.44343170822524,31.7958079337076));
#29900=CARTESIAN_POINT('Ctrl Pts',(2.0718835719005,-4.46073297032506,31.7935077063911));
#29901=CARTESIAN_POINT('Ctrl Pts',(1.89035643111482,-4.54322755398639,31.7822633208131));
#29902=CARTESIAN_POINT('Ctrl Pts',(1.74279501859907,-4.60185079598211,31.7733882080577));
#29903=CARTESIAN_POINT('Ctrl Pts',(1.49518597957512,-4.68659956494461,31.7587253056825));
#29904=CARTESIAN_POINT('Ctrl Pts',(1.39669155875464,-4.7168897660678,31.7529510233837));
#29905=CARTESIAN_POINT('Ctrl Pts',(1.21651225788719,-4.76616187936163,31.7424488838611));
#29906=CARTESIAN_POINT('Ctrl Pts',(1.13515459040011,-4.78619107022724,31.7377289381991));
#29907=CARTESIAN_POINT('Ctrl Pts',(0.987357167351199,-4.81859626347323,
31.7291775912551));
#29908=CARTESIAN_POINT('Ctrl Pts',(0.921098137390741,-4.83169972288105,
31.7253522608998));
#29909=CARTESIAN_POINT('Ctrl Pts',(0.755088710929473,-4.86099094832161,
31.7157807794224));
#29910=CARTESIAN_POINT('Ctrl Pts',(0.65507024041673,-4.87547685333203,31.7100251178952));
#29911=CARTESIAN_POINT('Ctrl Pts',(0.397283520256164,-4.90473658301958,
31.6952074155762));
#29912=CARTESIAN_POINT('Ctrl Pts',(0.239118382497657,-4.91498700220826,
31.6861299678684));
#29913=CARTESIAN_POINT('Ctrl Pts',(0.00162993316986859,-4.91888603726153,
31.6725504439781));
#29914=CARTESIAN_POINT('Ctrl Pts',(-0.0774966152352732,-4.91827581665873,
31.668035089894));
#29915=CARTESIAN_POINT('Ctrl Pts',(-0.194215459421216,-4.91455813778132,
31.6613974300692));
#29916=CARTESIAN_POINT('Ctrl Pts',(-0.23184160426101,-4.91292691408511,
31.6592613797802));
#29917=CARTESIAN_POINT('Ctrl Pts',(-0.319382480133557,-4.90812378369549,
31.6543011786491));
#29918=CARTESIAN_POINT('Ctrl Pts',(-0.369274920689384,-4.90462234638863,
31.6514806837639));
#29919=CARTESIAN_POINT('Ctrl Pts',(-0.579434353461689,-4.88664836133908,
31.6396091066608));
#29920=CARTESIAN_POINT('Ctrl Pts',(-0.738994742042416,-4.86507594824511,
31.6306150444924));
#29921=CARTESIAN_POINT('Ctrl Pts',(-1.02549528895035,-4.81191914111337,
31.6142829566083));
#29922=CARTESIAN_POINT('Ctrl Pts',(-1.1527801836611,-4.78302243700408,31.6069607211795));
#29923=CARTESIAN_POINT('Ctrl Pts',(-1.34553160870584,-4.73112131137844,
31.5957037557488));
#29924=CARTESIAN_POINT('Ctrl Pts',(-1.41191201724013,-4.71173731081854,
31.5917960856352));
#29925=CARTESIAN_POINT('Ctrl Pts',(-1.55062423205501,-4.66803679412807,
31.5835561354923));
#29926=CARTESIAN_POINT('Ctrl Pts',(-1.62284347518102,-4.6434235092388,31.579222780513));
#29927=CARTESIAN_POINT('Ctrl Pts',(-1.79147463122629,-4.58153697966321,
31.5689939831573));
#29928=CARTESIAN_POINT('Ctrl Pts',(-1.88734188464374,-4.54288484641345,
31.5630917669334));
#29929=CARTESIAN_POINT('Ctrl Pts',(-2.09449406887103,-4.45167469675351,
31.5501427815741));
#29930=CARTESIAN_POINT('Ctrl Pts',(-2.20516966381219,-4.3979017539788,31.5430960680165));
#29931=CARTESIAN_POINT('Ctrl Pts',(-2.35920951919484,-4.31578170723857,
31.5331215532521));
#29932=CARTESIAN_POINT('Ctrl Pts',(-2.40432226589841,-4.29081295383114,
31.5301795111084));
#29933=CARTESIAN_POINT('Ctrl Pts',(-2.4857973875931,-4.24403010529337,31.5248309590377));
#29934=CARTESIAN_POINT('Ctrl Pts',(-2.52228627875029,-4.22244623056907,
31.5224224535096));
#29935=CARTESIAN_POINT('Ctrl Pts',(-2.58895037522541,-4.18184061595814,
31.5180000327539));
#29936=CARTESIAN_POINT('Ctrl Pts',(-2.61920642241261,-4.16295720984173,
31.515984355191));
#29937=CARTESIAN_POINT('Ctrl Pts',(-2.72761138505175,-4.09364979464148,
31.508725560008));
#29938=CARTESIAN_POINT('Ctrl Pts',(-2.8045322821114,-4.04134031442693,31.5035048204836));
#29939=CARTESIAN_POINT('Ctrl Pts',(-2.98211058633536,-3.91306658362485,
31.4912228687434));
#29940=CARTESIAN_POINT('Ctrl Pts',(-3.08142110118553,-3.83535104102186,
31.4841709378827));
#29941=CARTESIAN_POINT('Ctrl Pts',(-3.23825104032613,-3.7025964070266,31.472643003271));
#29942=CARTESIAN_POINT('Ctrl Pts',(-3.29761403155249,-3.64982622821028,
31.4681813515752));
#29943=CARTESIAN_POINT('Ctrl Pts',(-3.40890906717953,-3.54595890547476,
31.4596061964944));
#29944=CARTESIAN_POINT('Ctrl Pts',(-3.46103489451756,-3.49509983900012,
31.4554956530768));
#29945=CARTESIAN_POINT('Ctrl Pts',(-3.55585517044263,-3.39838185768247,
31.4478292706966));
#29946=CARTESIAN_POINT('Ctrl Pts',(-3.59883996381569,-3.35282806764481,
31.4442770372839));
#29947=CARTESIAN_POINT('Ctrl Pts',(-3.78848543252156,-3.14399837843591,
31.4282419773723));
#29948=CARTESIAN_POINT('Ctrl Pts',(-3.92498640670963,-2.97183895602579,
31.4156776589896));
#29949=CARTESIAN_POINT('Ctrl Pts',(-4.07718537579441,-2.75102109919743,
31.4003329315466));
#29950=CARTESIAN_POINT('Ctrl Pts',(-4.10424228942476,-2.71048942786026,
31.3975466365238));
#29951=CARTESIAN_POINT('Ctrl Pts',(-4.16419258859877,-2.61772656015373,
31.3912404470853));
#29952=CARTESIAN_POINT('Ctrl Pts',(-4.19671429913832,-2.56526440778693,
31.3877234786657));
#29953=CARTESIAN_POINT('Ctrl Pts',(-4.24701543741232,-2.48060355787563,
31.3821312994515));
#29954=CARTESIAN_POINT('Ctrl Pts',(-4.26543580505892,-2.44879390149749,
31.3800487968995));
#29955=CARTESIAN_POINT('Ctrl Pts',(-4.31250644559897,-2.36536596286729,
31.3746342415875));
#29956=CARTESIAN_POINT('Ctrl Pts',(-4.3405870209525,-2.31343303744498,31.3713093051831));
#29957=CARTESIAN_POINT('Ctrl Pts',(-4.4494291926429,-2.10317590795498,31.3580006141759));
#29958=CARTESIAN_POINT('Ctrl Pts',(-4.52251756330337,-1.94103182669218,
31.3480747426424));
#29959=CARTESIAN_POINT('Ctrl Pts',(-4.61529951089046,-1.70131848953204,
31.3336534107982));
#29960=CARTESIAN_POINT('Ctrl Pts',(-4.64213582261033,-1.62666807509976,
31.3291972816092));
#29961=CARTESIAN_POINT('Ctrl Pts',(-4.69010956012718,-1.48234643152991,
31.3206303173598));
#29962=CARTESIAN_POINT('Ctrl Pts',(-4.71152853707399,-1.41279061141428,
31.3165224240597));
#29963=CARTESIAN_POINT('Ctrl Pts',(-4.74850175640768,-1.2825129780289,31.3088572140402));
#29964=CARTESIAN_POINT('Ctrl Pts',(-4.76445396557959,-1.22191929837059,
31.3053034819171));
#29965=CARTESIAN_POINT('Ctrl Pts',(-4.81185372010229,-1.02680507536187,
31.2938897757146));
#29966=CARTESIAN_POINT('Ctrl Pts',(-4.83879327110196,-0.891259620807821,
31.2860034399518));
#29967=CARTESIAN_POINT('Ctrl Pts',(-4.8781202976721,-0.638028776126936,
31.2713401896921));
#29968=CARTESIAN_POINT('Ctrl Pts',(-4.8920374740413,-0.520680138724421,
31.2645731393547));
#29969=CARTESIAN_POINT('Ctrl Pts',(-4.90586920547575,-0.352420624249749,
31.2549273557728));
#29970=CARTESIAN_POINT('Ctrl Pts',(-4.90924112300201,-0.301835410350173,
31.2520349682412));
#29971=CARTESIAN_POINT('Ctrl Pts',(-4.9139717327666,-0.209338117679563,
31.2467628927219));
#29972=CARTESIAN_POINT('Ctrl Pts',(-4.91557762641747,-0.167443394703228,
31.2443813010125));
#29973=CARTESIAN_POINT('Ctrl Pts',(-4.91771536839545,-0.0837161899047983,
31.2396365451753));
#29974=CARTESIAN_POINT('Ctrl Pts',(-4.91824952237092,-0.0418871676881771,
31.2372735538595));
#29975=CARTESIAN_POINT('Ctrl Pts',(-4.91825149861551,0.131305456968749,
31.2275096094303));
#29976=CARTESIAN_POINT('Ctrl Pts',(-4.9129901901366,0.262615805166311,31.2201531886595));
#29977=CARTESIAN_POINT('Ctrl Pts',(-4.88944461670753,0.555917895767881,
31.2036689342295));
#29978=CARTESIAN_POINT('Ctrl Pts',(-4.86835359385957,0.717527581964215,
31.1945482689874));
#29979=CARTESIAN_POINT('Ctrl Pts',(-4.82640190675748,0.948808230003812,
31.1813057443297));
#29980=CARTESIAN_POINT('Ctrl Pts',(-4.81195860808438,1.01953254902896,31.1772308136538));
#29981=CARTESIAN_POINT('Ctrl Pts',(-4.78592903657929,1.13407097096521,31.170581542657));
#29982=CARTESIAN_POINT('Ctrl Pts',(-4.77528476076275,1.1780869639915,31.1680142019493));
#29983=CARTESIAN_POINT('Ctrl Pts',(-4.76403458668766,1.2219482474081,31.1654428831549));
#29984=CARTESIAN_POINT('',(-4.91824999844923,0.000123507507276638,30.8898594359908));
#29985=CARTESIAN_POINT('Ctrl Pts',(-4.76403458704967,1.22194824599672,30.8199238152312));
#29986=CARTESIAN_POINT('Ctrl Pts',(-4.79982283587317,1.08241986927238,30.8280803104528));
#29987=CARTESIAN_POINT('Ctrl Pts',(-4.82947448833597,0.94132853557534,30.8362368056745));
#29988=CARTESIAN_POINT('Ctrl Pts',(-4.85287721761797,0.799228236002976,
30.8443933008961));
#29989=CARTESIAN_POINT('Ctrl Pts',(-4.87013621133165,0.694432417212852,
30.8504085351904));
#29990=CARTESIAN_POINT('Ctrl Pts',(-4.88399762918098,0.589088131054119,
30.8564237694847));
#29991=CARTESIAN_POINT('Ctrl Pts',(-4.89443437256851,0.483420350336929,
30.8624390037789));
#29992=CARTESIAN_POINT('Ctrl Pts',(-4.90948242451799,0.331064946493519,
30.8711119733813));
#29993=CARTESIAN_POINT('Ctrl Pts',(-4.91741278380546,0.178001677768284,
30.8797849429838));
#29994=CARTESIAN_POINT('Ctrl Pts',(-4.91818712165292,0.0248696382643597,
30.8884579125863));
#29995=CARTESIAN_POINT('Ctrl Pts',(-4.91822883180395,0.0166210933719668,
30.8889250870544));
#29996=CARTESIAN_POINT('Ctrl Pts',(-4.91824979130361,0.00837234974432156,
30.8893922615226));
#29997=CARTESIAN_POINT('Ctrl Pts',(-4.91824999844923,0.000123507507276638,
30.8898594359908));
#29998=CARTESIAN_POINT('Ctrl Pts',(-4.91833690826082,0.000123432691201461,
30.8898594403516));
#29999=CARTESIAN_POINT('Ctrl Pts',(-4.91765989171386,-0.656721429210889,
30.9270592933315));
#30000=CARTESIAN_POINT('Ctrl Pts',(-4.62027241517956,-2.13239495771996,
31.0105991448156));
#30001=CARTESIAN_POINT('Ctrl Pts',(-3.18782294371806,-4.0156960603218,31.1404789948039));
#30002=CARTESIAN_POINT('Ctrl Pts',(-0.876714416284051,-5.05167316853129,
31.2794989903164));
#30003=CARTESIAN_POINT('Ctrl Pts',(1.64831882804362,-4.85500515040882,31.4185189858289));
#30004=CARTESIAN_POINT('Ctrl Pts',(3.77115024690762,-3.47368043789694,31.5575389813414));
#30005=CARTESIAN_POINT('Ctrl Pts',(4.97379347911828,-1.24475234342413,31.696558976854));
#30006=CARTESIAN_POINT('Ctrl Pts',(4.96279479767373,1.28790440854975,31.8355789723664));
#30007=CARTESIAN_POINT('Ctrl Pts',(3.7408379611281,3.50630308415606,31.974598967879));
#30008=CARTESIAN_POINT('Ctrl Pts',(1.60608935691497,4.86913821399472,32.1136189633915));
#30009=CARTESIAN_POINT('Ctrl Pts',(-0.920556773564781,5.04386807876885,
32.2526389589041));
#30010=CARTESIAN_POINT('Ctrl Pts',(-3.22258033195988,3.98785731608399,32.3916589544165));
#30011=CARTESIAN_POINT('Ctrl Pts',(-4.37570558480373,2.44415159686769,32.4974242635864));
#30012=CARTESIAN_POINT('Ctrl Pts',(-4.70671521754109,1.44580583700442,32.5568495742522));
#30013=CARTESIAN_POINT('Ctrl Pts',(-4.7639087307945,1.22191632179108,32.5699348864137));
#30014=CARTESIAN_POINT('Origin',(0.,0.,-3.23514056400928));
#30015=CARTESIAN_POINT('',(-4.76374291154778,1.22187309174177,34.6652037882801));
#30016=CARTESIAN_POINT('',(-4.76403458704967,1.22194824599671,34.3199237602016));
#30017=CARTESIAN_POINT('',(-4.76403458704967,1.22194824599672,-3.23514056400928));
#30018=CARTESIAN_POINT('',(-4.91786285480381,-3.23909219955966E-5,32.9851526239175));
#30019=CARTESIAN_POINT('Ctrl Pts',(-4.91784190852614,-3.30751234541968E-5,
32.9851405682246));
#30020=CARTESIAN_POINT('Ctrl Pts',(-4.91792932869888,-0.373298708305577,
33.006274043888));
#30021=CARTESIAN_POINT('Ctrl Pts',(-4.78405248732222,-1.56453986243927,
33.073722981313));
#30022=CARTESIAN_POINT('Ctrl Pts',(-3.83240713769111,-3.40563728872529,
33.1874873804997));
#30023=CARTESIAN_POINT('Ctrl Pts',(-1.73594721364791,-4.82412656164927,
33.3264337657849));
#30024=CARTESIAN_POINT('Ctrl Pts',(0.783657389885535,-5.06671401469037,
33.46538015107));
#30025=CARTESIAN_POINT('Ctrl Pts',(3.11224209807527,-4.07426790164198,33.6043265363551));
#30026=CARTESIAN_POINT('Ctrl Pts',(4.68220426594096,-2.08870127672345,33.7432729216403));
#30027=CARTESIAN_POINT('Ctrl Pts',(5.11085879043896,0.405995363982041,33.8822193069254));
#30028=CARTESIAN_POINT('Ctrl Pts',(4.29371926786136,2.80172886985484,34.0211656922105));
#30029=CARTESIAN_POINT('Ctrl Pts',(2.42996700894246,4.51452878458352,34.1601120774956));
#30030=CARTESIAN_POINT('Ctrl Pts',(-0.0261002714740853,5.12689268341077,
34.2990584627807));
#30031=CARTESIAN_POINT('Ctrl Pts',(-2.47580549726093,4.48955420405128,34.4380048480659));
#30032=CARTESIAN_POINT('Ctrl Pts',(-4.09749498730757,2.96846620137155,34.560053289899));
#30033=CARTESIAN_POINT('Ctrl Pts',(-4.6343106032874,1.72504109344374,34.6357862699704));
#30034=CARTESIAN_POINT('Ctrl Pts',(-4.76374291154778,1.22187309174177,34.6652037882801));
#30035=CARTESIAN_POINT('Ctrl Pts',(-4.91824999996037,-1.97449862875235E-5,
32.9853754464731));
#30036=CARTESIAN_POINT('Ctrl Pts',(-4.91825017361617,0.0432359271112932,
32.9829326257254));
#30037=CARTESIAN_POINT('Ctrl Pts',(-4.91767970138599,0.0864895187082102,
32.9804863497487));
#30038=CARTESIAN_POINT('Ctrl Pts',(-4.9153025743111,0.176578622886849,32.9753817507004));
#30039=CARTESIAN_POINT('Ctrl Pts',(-4.91339684882255,0.223407179894823,
32.972723027043));
#30040=CARTESIAN_POINT('Ctrl Pts',(-4.90485341734412,0.378681430613462,
32.9638865071782));
#30041=CARTESIAN_POINT('Ctrl Pts',(-4.89529185867349,0.486933085201178,
32.9576917406495));
#30042=CARTESIAN_POINT('Ctrl Pts',(-4.86028271416837,0.774300823744014,
32.9411447028977));
#30043=CARTESIAN_POINT('Ctrl Pts',(-4.82852675005391,0.952480656005482,
32.9307742699252));
#30044=CARTESIAN_POINT('Ctrl Pts',(-4.77966978282832,1.15972790237745,32.9186300745121));
#30045=CARTESIAN_POINT('Ctrl Pts',(-4.77200424158646,1.19087679106607,32.916802791448));
#30046=CARTESIAN_POINT('Ctrl Pts',(-4.76403458699526,1.22194824620887,32.9149784811847));
#30047=CARTESIAN_POINT('',(-4.91824999837229,-0.000126534489980439,32.6398594359908));
#30048=CARTESIAN_POINT('Ctrl Pts',(-4.7639087307945,1.22191632179108,32.5699348864137));
#30049=CARTESIAN_POINT('Ctrl Pts',(-4.86578454630458,0.823113631607463,
32.593243068965));
#30050=CARTESIAN_POINT('Ctrl Pts',(-4.91786568948866,0.411441406548216,
32.6165512515163));
#30051=CARTESIAN_POINT('Ctrl Pts',(-4.91829166267875,-0.000126501603607826,
32.6398594340676));
#30052=CARTESIAN_POINT('Ctrl Pts',(-4.91824999837229,-0.000126534489980439,
32.6398594359908));
#30053=CARTESIAN_POINT('Ctrl Pts',(-4.9182460739844,-0.152662975038819,
32.6484980527229));
#30054=CARTESIAN_POINT('Ctrl Pts',(-4.91114158002739,-0.305164623492694,
32.6571366694551));
#30055=CARTESIAN_POINT('Ctrl Pts',(-4.89697215839355,-0.456997529991619,
32.6657752861872));
#30056=CARTESIAN_POINT('Ctrl Pts',(-4.8948269082127,-0.479985029308245,
32.6670831726053));
#30057=CARTESIAN_POINT('Ctrl Pts',(-4.89251981310438,-0.502957206987885,
32.6683910590234));
#30058=CARTESIAN_POINT('Ctrl Pts',(-4.89005110050666,-0.525911871831763,
32.6696989454414));
#30059=CARTESIAN_POINT('Ctrl Pts',(-4.87465561600517,-0.669062673252445,
32.6778552391703));
#30060=CARTESIAN_POINT('Ctrl Pts',(-4.85296706059036,-0.811563777669985,
32.6860115328992));
#30061=CARTESIAN_POINT('Ctrl Pts',(-4.82506464173119,-0.952855847237913,
32.6941678266281));
#30062=CARTESIAN_POINT('Ctrl Pts',(-4.79716790981858,-1.09411911928639,
32.7023224579775));
#30063=CARTESIAN_POINT('Ctrl Pts',(-4.76305990581221,-1.23417351996479,
32.710477089327));
#30064=CARTESIAN_POINT('Ctrl Pts',(-4.72287104862409,-1.37246935141314,
32.7186317206764));
#30065=CARTESIAN_POINT('Ctrl Pts',(-4.68268076567248,-1.51077008912558,
32.7267866413244));
#30066=CARTESIAN_POINT('Ctrl Pts',(-4.63640928763732,-1.64731181037433,
32.7349415619723));
#30067=CARTESIAN_POINT('Ctrl Pts',(-4.58423720689594,-1.78155895030474,
32.7430964826203));
#30068=CARTESIAN_POINT('Ctrl Pts',(-4.53206819350884,-1.9157981974401,32.7512509238158));
#30069=CARTESIAN_POINT('Ctrl Pts',(-4.47399939357257,-2.04774282155977,
32.7594053650113));
#30070=CARTESIAN_POINT('Ctrl Pts',(-4.41025992885093,-2.17687629930407,
32.7675598062068));
#30071=CARTESIAN_POINT('Ctrl Pts',(-4.34650475302151,-2.30604160709268,
32.7757162573863));
#30072=CARTESIAN_POINT('Ctrl Pts',(-4.27707626735019,-2.43239408357324,
32.7838727085658));
#30073=CARTESIAN_POINT('Ctrl Pts',(-4.20225030301852,-2.55544036386701,
32.7920291597454));
#30074=CARTESIAN_POINT('Ctrl Pts',(-4.15121385158712,-2.63936638559112,
32.7975924201483));
#30075=CARTESIAN_POINT('Ctrl Pts',(-4.0976673651435,-2.72175479774588,32.8031556805512));
#30076=CARTESIAN_POINT('Ctrl Pts',(-4.04171019025238,-2.80245638690597,
32.8087189409541));
#30077=CARTESIAN_POINT('Ctrl Pts',(-3.95967139976016,-2.92077295271503,
32.8168752346829));
#30078=CARTESIAN_POINT('Ctrl Pts',(-3.8724183047003,-3.035506799502,32.8250315284118));
#30079=CARTESIAN_POINT('Ctrl Pts',(-3.78028818569261,-3.14620474470637,
32.8331878221406));
#30080=CARTESIAN_POINT('Ctrl Pts',(-3.6881768442351,-3.25688012794899,32.84134245349));
#30081=CARTESIAN_POINT('Ctrl Pts',(-3.59119067577382,-3.36352099353832,
32.8494970848394));
#30082=CARTESIAN_POINT('Ctrl Pts',(-3.48970731004212,-3.46570713603134,
32.8576517161888));
#30083=CARTESIAN_POINT('Ctrl Pts',(-3.38822034402671,-3.5678969037402,32.8658066368368));
#30084=CARTESIAN_POINT('Ctrl Pts',(-3.28223609462846,-3.66563139202599,
32.8739615574847));
#30085=CARTESIAN_POINT('Ctrl Pts',(-3.17216947869226,-3.75852682057123,
32.8821164781326));
#30086=CARTESIAN_POINT('Ctrl Pts',(-3.06210933390539,-3.8514167875132,32.8902709193281));
#30087=CARTESIAN_POINT('Ctrl Pts',(-2.94796755912266,-3.93946804877225,
32.8984253605235));
#30088=CARTESIAN_POINT('Ctrl Pts',(-2.83019256527175,-4.02233677182561,
32.906579801719));
#30089=CARTESIAN_POINT('Ctrl Pts',(-2.71238854112305,-4.10522592114799,
32.9147362528985));
#30090=CARTESIAN_POINT('Ctrl Pts',(-2.59094978207838,-4.18292978679778,
32.922892704078));
#30091=CARTESIAN_POINT('Ctrl Pts',(-2.46635462455556,-4.25514722758607,
32.9310491552575));
#30092=CARTESIAN_POINT('Ctrl Pts',(-2.38137216208393,-4.30440448664498,
32.9366124156605));
#30093=CARTESIAN_POINT('Ctrl Pts',(-2.29492190149264,-4.35111025836679,
32.9421756760636));
#30094=CARTESIAN_POINT('Ctrl Pts',(-2.2071624922942,-4.39518108786312,32.9477389364667));
#30095=CARTESIAN_POINT('Ctrl Pts',(-2.07849845950931,-4.45979331238655,
32.9558952301956));
#30096=CARTESIAN_POINT('Ctrl Pts',(-1.9469712168772,-4.5187640054613,32.9640515239244));
#30097=CARTESIAN_POINT('Ctrl Pts',(-1.81309381923539,-4.57185671966548,
32.9722078176532));
#30098=CARTESIAN_POINT('Ctrl Pts',(-1.67924370788772,-4.62493861274943,
32.9803624490027));
#30099=CARTESIAN_POINT('Ctrl Pts',(-1.54304470799748,-4.67214479365301,
32.9885170803521));
#30100=CARTESIAN_POINT('Ctrl Pts',(-1.40502951570803,-4.71328708254539,
32.9966717117016));
#30101=CARTESIAN_POINT('Ctrl Pts',(-1.2670094271106,-4.75443083102576,33.0048266323495));
#30102=CARTESIAN_POINT('Ctrl Pts',(-1.127173336803,-4.7895101578229,33.0129815529974));
#30103=CARTESIAN_POINT('Ctrl Pts',(-0.986069243359014,-4.81838671235522,
33.0211364736454));
#30104=CARTESIAN_POINT('Ctrl Pts',(-0.844973445851323,-4.8472615691476,
33.0292909148408));
#30105=CARTESIAN_POINT('Ctrl Pts',(-0.702610122412683,-4.86993431709509,
33.0374453560363));
#30106=CARTESIAN_POINT('Ctrl Pts',(-0.559537557595221,-4.88631771215712,
33.0455997972318));
#30107=CARTESIAN_POINT('Ctrl Pts',(-0.416429726894918,-4.90270514555376,
33.0537562484113));
#30108=CARTESIAN_POINT('Ctrl Pts',(-0.272612638089836,-4.9128000899778,
33.0619126995908));
#30109=CARTESIAN_POINT('Ctrl Pts',(-0.128650415256635,-4.91656710857833,
33.0700691507703));
#30110=CARTESIAN_POINT('Ctrl Pts',(-0.0304582828971516,-4.91913647421985,
33.0756324111732));
#30111=CARTESIAN_POINT('Ctrl Pts',(0.0678012572343151,-4.9187630562909,
33.0811956715761));
#30112=CARTESIAN_POINT('Ctrl Pts',(0.165948964316552,-4.91544952204193,
33.086758931979));
#30113=CARTESIAN_POINT('Ctrl Pts',(0.309843276247919,-4.91059155087796,
33.0949152257078));
#30114=CARTESIAN_POINT('Ctrl Pts',(0.453551059204196,-4.89940981069101,
33.1030715194366));
#30115=CARTESIAN_POINT('Ctrl Pts',(0.596508673255385,-4.88194228409463,
33.1112278131654));
#30116=CARTESIAN_POINT('Ctrl Pts',(0.739437150323049,-4.86447831765164,
33.1193824445148));
#30117=CARTESIAN_POINT('Ctrl Pts',(0.881615431522648,-4.84073116116138,
33.1275370758641));
#30118=CARTESIAN_POINT('Ctrl Pts',(1.02248573604808,-4.8107905776575,33.1356917072135));
#30119=CARTESIAN_POINT('Ctrl Pts',(1.16336103817132,-4.78084893196387,33.1438466278614));
#30120=CARTESIAN_POINT('Ctrl Pts',(1.30292794265939,-4.74471348548312,33.1520015485092));
#30121=CARTESIAN_POINT('Ctrl Pts',(1.44063908486165,-4.70252507592134,33.1601564691571));
#30122=CARTESIAN_POINT('Ctrl Pts',(1.57834213060943,-4.66033914674373,33.1683109103525));
#30123=CARTESIAN_POINT('Ctrl Pts',(1.71418931264419,-4.61210106538802,33.176465351548));
#30124=CARTESIAN_POINT('Ctrl Pts',(1.84764869829509,-4.55800146447853,33.1846197927434));
#30125=CARTESIAN_POINT('Ctrl Pts',(1.9811409802813,-4.50388852858625,33.1927762439228));
#30126=CARTESIAN_POINT('Ctrl Pts',(2.11224397942654,-4.44391131166096,33.2009326951023));
#30127=CARTESIAN_POINT('Ctrl Pts',(2.24044543438769,-4.37830872804001,33.2090891462817));
#30128=CARTESIAN_POINT('Ctrl Pts',(2.32788763962418,-4.33356325629193,33.214652406685));
#30129=CARTESIAN_POINT('Ctrl Pts',(2.41398041429648,-4.28620176541063,33.2202156670884));
#30130=CARTESIAN_POINT('Ctrl Pts',(2.49856766234332,-4.23631239395683,33.2257789274917));
#30131=CARTESIAN_POINT('Ctrl Pts',(2.62258099099763,-4.16316960752842,33.2339352212206));
#30132=CARTESIAN_POINT('Ctrl Pts',(2.74340356628593,-4.08456386030267,33.2420915149494));
#30133=CARTESIAN_POINT('Ctrl Pts',(2.86055869544279,-4.00079829689359,33.2502478086783));
#30134=CARTESIAN_POINT('Ctrl Pts',(2.97768994656362,-3.91704980620813,33.2584024400278));
#30135=CARTESIAN_POINT('Ctrl Pts',(3.09115497067334,-3.82814379184214,33.2665570713772));
#30136=CARTESIAN_POINT('Ctrl Pts',(3.20050700489114,-3.73442605685837,33.2747117027267));
#30137=CARTESIAN_POINT('Ctrl Pts',(3.309862918546,-3.64070499708913,33.2828666233746));
#30138=CARTESIAN_POINT('Ctrl Pts',(3.41510529379355,-3.54217209003059,33.2910215440226));
#30139=CARTESIAN_POINT('Ctrl Pts',(3.5158209608763,-3.43921299624824,33.2991764646705));
#30140=CARTESIAN_POINT('Ctrl Pts',(3.61653070658046,-3.33625995574233,33.3073309058661));
#30141=CARTESIAN_POINT('Ctrl Pts',(3.71271404321985,-3.2288814890323,33.3154853470616));
#30142=CARTESIAN_POINT('Ctrl Pts',(3.80399518545927,-3.11749958965558,33.3236397882571));
#30143=CARTESIAN_POINT('Ctrl Pts',(3.89529882754045,-3.00609023581182,33.3317962394366));
#30144=CARTESIAN_POINT('Ctrl Pts',(3.98169764828788,-2.89067573625114,33.3399526906161));
#30145=CARTESIAN_POINT('Ctrl Pts',(4.06285624459877,-2.77171105965698,33.3481091417956));
#30146=CARTESIAN_POINT('Ctrl Pts',(4.11821198636284,-2.69056897223881,33.3536724021985));
#30147=CARTESIAN_POINT('Ctrl Pts',(4.17113073013441,-2.6077759578888,33.3592356626013));
#30148=CARTESIAN_POINT('Ctrl Pts',(4.22151761319054,-2.52348412002573,33.3647989230041));
#30149=CARTESIAN_POINT('Ctrl Pts',(4.29538980117511,-2.39990389210712,33.3729552167329));
#30150=CARTESIAN_POINT('Ctrl Pts',(4.36384557851417,-2.27305451392679,33.3811115104617));
#30151=CARTESIAN_POINT('Ctrl Pts',(4.42661151612109,-2.1434303226007,33.3892678041905));
#30152=CARTESIAN_POINT('Ctrl Pts',(4.48936466105444,-2.01383255069937,33.3974224355399));
#30153=CARTESIAN_POINT('Ctrl Pts',(4.54643013398506,-1.8814613949083,33.4055770668892));
#30154=CARTESIAN_POINT('Ctrl Pts',(4.59758120336134,-1.7468343198479,33.4137316982386));
#30155=CARTESIAN_POINT('Ctrl Pts',(4.64873408740304,-1.61220246867823,33.4218866188865));
#30156=CARTESIAN_POINT('Ctrl Pts',(4.6939720256624,-1.47531484957851,33.4300415395344));
#30157=CARTESIAN_POINT('Ctrl Pts',(4.73311685971175,-1.33670784198058,33.4381964601822));
#30158=CARTESIAN_POINT('Ctrl Pts',(4.77225939231794,-1.19810898350777,33.4463509013777));
#30159=CARTESIAN_POINT('Ctrl Pts',(4.80530944735878,-1.05779126110086,33.4545053425731));
#30160=CARTESIAN_POINT('Ctrl Pts',(4.83213908119947,-0.916305059707026,
33.4626597837685));
#30161=CARTESIAN_POINT('Ctrl Pts',(4.85897532826281,-0.774783983452207,
33.4708162349479));
#30162=CARTESIAN_POINT('Ctrl Pts',(4.87958802770654,-0.63209418158598,33.4789726861274));
#30163=CARTESIAN_POINT('Ctrl Pts',(4.89390047547349,-0.488795661458185,
33.4871291373068));
#30164=CARTESIAN_POINT('Ctrl Pts',(4.90366254873117,-0.391056219960537,
33.4926923977102));
#30165=CARTESIAN_POINT('Ctrl Pts',(4.9104947018656,-0.2930337819537,33.4982556581135));
#30166=CARTESIAN_POINT('Ctrl Pts',(4.91438645268894,-0.194907301370204,
33.5038189185168));
#30167=CARTESIAN_POINT('Ctrl Pts',(4.92009214692821,-0.0510441096090894,
33.5119752122457));
#30168=CARTESIAN_POINT('Ctrl Pts',(4.91947741697528,0.0930967253521199,
33.5201315059745));
#30169=CARTESIAN_POINT('Ctrl Pts',(4.91253881611527,0.236950295760079,33.5282877997034));
#30170=CARTESIAN_POINT('Ctrl Pts',(4.90560162944995,0.380774546574776,33.5364424310529));
#30171=CARTESIAN_POINT('Ctrl Pts',(4.89234315927421,0.524311315575884,33.5445970624023));
#30172=CARTESIAN_POINT('Ctrl Pts',(4.87281202951924,0.666997741729757,33.5527516937518));
#30173=CARTESIAN_POINT('Ctrl Pts',(4.85328020686642,0.809689229911189,33.5609066143997));
#30174=CARTESIAN_POINT('Ctrl Pts',(4.82747532100132,0.951529982823226,33.5690615350477));
#30175=CARTESIAN_POINT('Ctrl Pts',(4.79549769678287,1.09196378266416,33.5772164556956));
#30176=CARTESIAN_POINT('Ctrl Pts',(4.76352195262564,1.23238932597733,33.5853708968911));
#30177=CARTESIAN_POINT('Ctrl Pts',(4.72537427139847,1.37140775560834,33.5935253380866));
#30178=CARTESIAN_POINT('Ctrl Pts',(4.68120577034772,1.50847459314474,33.6016797792821));
#30179=CARTESIAN_POINT('Ctrl Pts',(4.63702638222589,1.64557521621536,33.6098362304617));
#30180=CARTESIAN_POINT('Ctrl Pts',(4.58682331124454,1.78072296721192,33.6179926816412));
#30181=CARTESIAN_POINT('Ctrl Pts',(4.53079726874191,1.91338944599914,33.6261491328207));
#30182=CARTESIAN_POINT('Ctrl Pts',(4.49258365636061,2.00387710441492,33.6317123932235));
#30183=CARTESIAN_POINT('Ctrl Pts',(4.4516621236224,2.09321077570324,33.6372756536263));
#30184=CARTESIAN_POINT('Ctrl Pts',(4.40810912660491,2.18122832148368,33.6428389140291));
#30185=CARTESIAN_POINT('Ctrl Pts',(4.34425609605752,2.3102708082078,33.6509952077579));
#30186=CARTESIAN_POINT('Ctrl Pts',(4.27472085740843,2.43653168410303,33.6591515014867));
#30187=CARTESIAN_POINT('Ctrl Pts',(4.19977078733812,2.55951331239384,33.6673077952155));
#30188=CARTESIAN_POINT('Ctrl Pts',(4.12483599325682,2.68246987511768,33.6754624265649));
#30189=CARTESIAN_POINT('Ctrl Pts',(4.04448874347453,2.80214823798555,33.6836170579143));
#30190=CARTESIAN_POINT('Ctrl Pts',(3.95904115281108,2.91807748575124,33.6917716892636));
#30191=CARTESIAN_POINT('Ctrl Pts',(3.87359053075878,3.03401084629094,33.6999266099115));
#30192=CARTESIAN_POINT('Ctrl Pts',(3.78303940127665,3.1461945539773,33.7080815305594));
#30193=CARTESIAN_POINT('Ctrl Pts',(3.68774209251233,3.2541882738423,33.7162364512073));
#30194=CARTESIAN_POINT('Ctrl Pts',(3.59245038656494,3.36217564442998,33.7243908924027));
#30195=CARTESIAN_POINT('Ctrl Pts',(3.49241328173855,3.46597326972859,33.7325453335981));
#30196=CARTESIAN_POINT('Ctrl Pts',(3.38802408244951,3.5651754345673,33.7406997747935));
#30197=CARTESIAN_POINT('Ctrl Pts',(3.28360915232045,3.66440205169659,33.748856225973));
#30198=CARTESIAN_POINT('Ctrl Pts',(3.17484022667796,3.75903071410694,33.7570126771524));
#30199=CARTESIAN_POINT('Ctrl Pts',(3.06214645722417,3.84869356236755,33.7651691283319));
#30200=CARTESIAN_POINT('Ctrl Pts',(2.98528155954885,3.90984978857451,33.7707323887352));
#30201=CARTESIAN_POINT('Ctrl Pts',(2.90659149361485,3.96869662529929,33.7762956491385));
#30202=CARTESIAN_POINT('Ctrl Pts',(2.8262209979243,4.02512831266182,33.7818589095418));
#30203=CARTESIAN_POINT('Ctrl Pts',(2.70838984811907,4.1078627856826,33.7900152032706));
#30204=CARTESIAN_POINT('Ctrl Pts',(2.58690120655491,4.18543512719117,33.7981714969995));
#30205=CARTESIAN_POINT('Ctrl Pts',(2.46222803144597,4.2575363983954,33.8063277907284));
#30206=CARTESIAN_POINT('Ctrl Pts',(2.33758026666753,4.32962297424012,33.8144824220779));
#30207=CARTESIAN_POINT('Ctrl Pts',(2.20974955269506,4.39624053687945,33.8226370534273));
#30208=CARTESIAN_POINT('Ctrl Pts',(2.07923533694281,4.457125023612,33.8307916847768));
#30209=CARTESIAN_POINT('Ctrl Pts',(1.94871649099163,4.51801167031835,33.8389466054247));
#30210=CARTESIAN_POINT('Ctrl Pts',(1.81551425443547,4.57316468925295,33.8471015260727));
#30211=CARTESIAN_POINT('Ctrl Pts',(1.68015050005635,4.62236707322779,33.8552564467206));
#30212=CARTESIAN_POINT('Ctrl Pts',(1.54479470412168,4.67156656444568,33.8634108879161));
#30213=CARTESIAN_POINT('Ctrl Pts',(1.40727795946292,4.71481600719977,33.8715653291117));
#30214=CARTESIAN_POINT('Ctrl Pts',(1.26813978851806,4.75194744702394,33.8797197703072));
#30215=CARTESIAN_POINT('Ctrl Pts',(1.12896732147702,4.78908803935762,33.8878762214867));
#30216=CARTESIAN_POINT('Ctrl Pts',(0.988172952954542,4.82010752884014,33.8960326726662));
#30217=CARTESIAN_POINT('Ctrl Pts',(0.846309558868826,4.84488835713138,33.9041891238457));
#30218=CARTESIAN_POINT('Ctrl Pts',(0.749548971996745,4.8617905855328,33.9097523842485));
#30219=CARTESIAN_POINT('Ctrl Pts',(0.652291323342216,4.87579152998842,33.9153156446513));
#30220=CARTESIAN_POINT('Ctrl Pts',(0.55471431658077,4.88686761530127,33.9208789050541));
#30221=CARTESIAN_POINT('Ctrl Pts',(0.411656708146348,4.90310625930421,33.9290351987829));
#30222=CARTESIAN_POINT('Ctrl Pts',(0.267858778981811,4.91306184888029,33.9371914925117));
#30223=CARTESIAN_POINT('Ctrl Pts',(0.123883663578513,4.91668952654104,33.9453477862405));
#30224=CARTESIAN_POINT('Ctrl Pts',(-0.0200621074589962,4.92031646482472,
33.9535024175899));
#30225=CARTESIAN_POINT('Ctrl Pts',(-0.164184658347153,4.91761805569537,
33.9616570489393));
#30226=CARTESIAN_POINT('Ctrl Pts',(-0.307919077891934,4.90860152222302,
33.9698116802887));
#30227=CARTESIAN_POINT('Ctrl Pts',(-0.451658596643225,4.89958466887484,
33.9779666009366));
#30228=CARTESIAN_POINT('Ctrl Pts',(-0.595009622280352,4.88424925986398,
33.9861215215845));
#30229=CARTESIAN_POINT('Ctrl Pts',(-0.737410078155,4.86265456712025,33.9942764422323));
#30230=CARTESIAN_POINT('Ctrl Pts',(-0.87980216187628,4.84106114399381,34.0024308834278));
#30231=CARTESIAN_POINT('Ctrl Pts',(-1.0212434569048,4.81320922448485,34.0105853246232));
#30232=CARTESIAN_POINT('Ctrl Pts',(-1.16117987019393,4.77920959694764,34.0187397658186));
#30233=CARTESIAN_POINT('Ctrl Pts',(-1.30115077633757,4.74520158885973,34.0268962169981));
#30234=CARTESIAN_POINT('Ctrl Pts',(-1.4396157341306,4.70504292356356,34.0350526681775));
#30235=CARTESIAN_POINT('Ctrl Pts',(-1.57603304919831,4.65889502890274,34.043209119357));
#30236=CARTESIAN_POINT('Ctrl Pts',(-1.66907903580995,4.62741899239935,34.0487723797603));
#30237=CARTESIAN_POINT('Ctrl Pts',(-1.76117269102492,4.59315771194547,34.0543356401636));
#30238=CARTESIAN_POINT('Ctrl Pts',(-1.8521467069881,4.55617554954735,34.0598989005668));
#30239=CARTESIAN_POINT('Ctrl Pts',(-1.98552367338919,4.50195601686662,34.0680551942957));
#30240=CARTESIAN_POINT('Ctrl Pts',(-2.11654314582965,4.4418656179856,34.0762114880246));
#30241=CARTESIAN_POINT('Ctrl Pts',(-2.24468922246724,4.37613452227413,34.0843677817535));
#30242=CARTESIAN_POINT('Ctrl Pts',(-2.37280918094275,4.31041682358157,34.0925224131029));
#30243=CARTESIAN_POINT('Ctrl Pts',(-2.49805661435159,4.23906087420696,34.1006770444524));
#30244=CARTESIAN_POINT('Ctrl Pts',(-2.61993899017471,4.16234342050993,34.1088316758018));
#30245=CARTESIAN_POINT('Ctrl Pts',(-2.74182568996874,4.08562324513935,34.1169865964498));
#30246=CARTESIAN_POINT('Ctrl Pts',(-2.86034680808497,4.00354135991706,34.1251415170977));
#30247=CARTESIAN_POINT('Ctrl Pts',(-2.97503721481366,3.91641885310724,34.1332964377457));
#30248=CARTESIAN_POINT('Ctrl Pts',(-3.08972087854659,3.82930146849298,34.1414508789412));
#30249=CARTESIAN_POINT('Ctrl Pts',(-3.20057401555088,3.73714425837669,34.1496053201367));
#30250=CARTESIAN_POINT('Ctrl Pts',(-3.30716316491905,3.64030972076589,34.1577597613322));
#30251=CARTESIAN_POINT('Ctrl Pts',(-3.41377858739181,3.54345131445973,34.1659162125117));
#30252=CARTESIAN_POINT('Ctrl Pts',(-3.51612767407156,3.44191350184174,34.1740726636912));
#30253=CARTESIAN_POINT('Ctrl Pts',(-3.61381208950851,3.33609730736712,34.1822291148708));
#30254=CARTESIAN_POINT('Ctrl Pts',(-3.68043957594954,3.26392338862007,34.1877923752735));
#30255=CARTESIAN_POINT('Ctrl Pts',(-3.74489771362711,3.18975988577272,34.1933556356764));
#30256=CARTESIAN_POINT('Ctrl Pts',(-3.80707041484449,3.11374339323519,34.1989188960792));
#30257=CARTESIAN_POINT('Ctrl Pts',(-3.89822110671353,3.00229647597761,34.2070751290372));
#30258=CARTESIAN_POINT('Ctrl Pts',(-3.98449180843724,2.88682347498688,34.2152313619953));
#30259=CARTESIAN_POINT('Ctrl Pts',(-4.06553974214529,2.76777341333015,34.2233875949534));
#30260=CARTESIAN_POINT('Ctrl Pts',(-4.14658036526241,2.64873409008785,34.2315430922125));
#30261=CARTESIAN_POINT('Ctrl Pts',(-4.22239896825741,2.52611862391255,34.2396985894717));
#30262=CARTESIAN_POINT('Ctrl Pts',(-4.29269548527147,2.40040591009728,34.2478540867308));
#30263=CARTESIAN_POINT('Ctrl Pts',(-4.36298184084889,2.27471136818909,34.256008405104));
#30264=CARTESIAN_POINT('Ctrl Pts',(-4.42774754135432,2.14592076487399,34.2641627234773));
#30265=CARTESIAN_POINT('Ctrl Pts',(-4.4867379583526,2.01453854656048,34.2723170418506));
#30266=CARTESIAN_POINT('Ctrl Pts',(-4.54573832761712,1.88313416276849,34.2804727359379));
#30267=CARTESIAN_POINT('Ctrl Pts',(-4.59896132667297,1.74913759456132,34.2886284300253));
#30268=CARTESIAN_POINT('Ctrl Pts',(-4.64619980387587,1.61307484171189,34.2967841241126));
#30269=CARTESIAN_POINT('Ctrl Pts',(-4.69087538718258,1.48439408801705,34.3044973361423));
#30270=CARTESIAN_POINT('Ctrl Pts',(-4.73019850764378,1.35386565993627,34.312210548172));
#30271=CARTESIAN_POINT('Ctrl Pts',(-4.76403458704967,1.22194824599671,34.3199237602016));
#30272=CARTESIAN_POINT('Origin',(0.,0.,-3.23514056400928));
#30273=CARTESIAN_POINT('',(-4.76403458704968,1.22194824599668,36.4152130395234));
#30274=CARTESIAN_POINT('',(-4.76403458739297,1.22194824465831,36.0696927553338));
#30275=CARTESIAN_POINT('',(-4.76403458704967,1.22194824599672,-3.23514056400928));
#30276=CARTESIAN_POINT('',(-4.91824999894343,0.000101945896325419,34.7351405653851));
#30277=CARTESIAN_POINT('Ctrl Pts',(-4.91824999894343,0.000101945896325419,
34.7351405653851));
#30278=CARTESIAN_POINT('Ctrl Pts',(-4.91825297185789,-0.14332252814081,
34.7432643671499));
#30279=CARTESIAN_POINT('Ctrl Pts',(-4.91197785217775,-0.286773541245251,
34.7513881689147));
#30280=CARTESIAN_POINT('Ctrl Pts',(-4.89944373927689,-0.429690712211137,
34.7595119706796));
#30281=CARTESIAN_POINT('Ctrl Pts',(-4.88690997830694,-0.57260387037042,
34.7676355443455));
#30282=CARTESIAN_POINT('Ctrl Pts',(-4.86811759880276,-0.714982877260633,
34.7757591180115));
#30283=CARTESIAN_POINT('Ctrl Pts',(-4.84313767764064,-0.856271275891921,
34.7838826916774));
#30284=CARTESIAN_POINT('Ctrl Pts',(-4.81816023339163,-0.99754566490791,
34.792005459841));
#30285=CARTESIAN_POINT('Ctrl Pts',(-4.78699653311575,-1.13772932710976,
34.8001282280046));
#30286=CARTESIAN_POINT('Ctrl Pts',(-4.74976898696445,-1.27627490493652,
34.8082509961681));
#30287=CARTESIAN_POINT('Ctrl Pts',(-4.71253137452548,-1.41485794533563,
34.8163759607193));
#30288=CARTESIAN_POINT('Ctrl Pts',(-4.66922672622055,-1.55180168728186,
34.8245009252705));
#30289=CARTESIAN_POINT('Ctrl Pts',(-4.62002782714359,-1.6865722453897,34.8326258898216));
#30290=CARTESIAN_POINT('Ctrl Pts',(-4.57518222622321,-1.80941781263029,
34.8400319278548));
#30291=CARTESIAN_POINT('Ctrl Pts',(-4.52543997650175,-1.93045775236507,
34.847437965888));
#30292=CARTESIAN_POINT('Ctrl Pts',(-4.47096718960992,-2.04930121064024,
34.8548440039212));
#30293=CARTESIAN_POINT('Ctrl Pts',(-4.41097510319836,-2.18018614282575,
34.8630004376013));
#30294=CARTESIAN_POINT('Ctrl Pts',(-4.34522048768164,-2.30845937613391,
34.8711568712814));
#30295=CARTESIAN_POINT('Ctrl Pts',(-4.27395583508463,-2.43361553706539,
34.8793133049615));
#30296=CARTESIAN_POINT('Ctrl Pts',(-4.20270568685358,-2.55874622518958,
34.8874680785773));
#30297=CARTESIAN_POINT('Ctrl Pts',(-4.12594790424494,-2.68076081593636,
34.8956228521932));
#30298=CARTESIAN_POINT('Ctrl Pts',(-4.04398049103538,-2.79917931734022,
34.9037776258091));
#30299=CARTESIAN_POINT('Ctrl Pts',(-3.96201017100346,-2.9176020182367,34.911932688619));
#30300=CARTESIAN_POINT('Ctrl Pts',(-3.87483003804373,-3.03242809733651,
34.9200877514288));
#30301=CARTESIAN_POINT('Ctrl Pts',(-3.7827811984389,-3.14320687630279,34.9282428142386));
#30302=CARTESIAN_POINT('Ctrl Pts',(-3.69073775749174,-3.25397915810184,
34.9363973987546));
#30303=CARTESIAN_POINT('Ctrl Pts',(-3.59382639577598,-3.36070435789163,
34.9445519832706));
#30304=CARTESIAN_POINT('Ctrl Pts',(-3.49242820674477,-3.46296524430054,
34.9527065677866));
#30305=CARTESIAN_POINT('Ctrl Pts',(-3.39100508746049,-3.56525127306951,
34.9608631572285));
#30306=CARTESIAN_POINT('Ctrl Pts',(-3.28509317207918,-3.66307055729281,
34.9690197466704));
#30307=CARTESIAN_POINT('Ctrl Pts',(-3.17511050902387,-3.75604264059744,
34.9771763361123));
#30308=CARTESIAN_POINT('Ctrl Pts',(-3.10043641407023,-3.81916719117534,
34.9827143538103));
#30309=CARTESIAN_POINT('Ctrl Pts',(-3.02388650556722,-3.88005800371298,
34.9882523715084));
#30310=CARTESIAN_POINT('Ctrl Pts',(-2.94560038055085,-3.93860653792667,
34.9937903892065));
#30311=CARTESIAN_POINT('Ctrl Pts',(-2.83029999301516,-4.02483725483945,
35.0019468228866));
#30312=CARTESIAN_POINT('Ctrl Pts',(-2.71118892597505,-4.10601758221992,
35.0101032565667));
#30313=CARTESIAN_POINT('Ctrl Pts',(-2.58873068694449,-4.1818245411509,35.0182596902468));
#30314=CARTESIAN_POINT('Ctrl Pts',(-2.46629737161713,-4.25761607122907,
35.0264144638627));
#30315=CARTESIAN_POINT('Ctrl Pts',(-2.34051852769332,-4.3280362385645,35.0345692374786));
#30316=CARTESIAN_POINT('Ctrl Pts',(-2.21188548417436,-4.39280612677122,
35.0427240110946));
#30317=CARTESIAN_POINT('Ctrl Pts',(-2.0832478789233,-4.45757831192178,35.0508790739044));
#30318=CARTESIAN_POINT('Ctrl Pts',(-1.95175616871635,-4.51669966315225,
35.0590341367143));
#30319=CARTESIAN_POINT('Ctrl Pts',(-1.81792550717558,-4.56993762680197,
35.0671891995241));
#30320=CARTESIAN_POINT('Ctrl Pts',(-1.68410269479296,-4.62317246804915,
35.0753437840402));
#30321=CARTESIAN_POINT('Ctrl Pts',(-1.54794151681425,-4.67052448924647,
35.0834983685562));
#30322=CARTESIAN_POINT('Ctrl Pts',(-1.40997623830103,-4.71180963854934,
35.0916529530722));
#30323=CARTESIAN_POINT('Ctrl Pts',(-1.2719770389722,-4.75310493842018,35.0998095425142));
#30324=CARTESIAN_POINT('Ctrl Pts',(-1.13217317343178,-4.78833028960078,
35.1079661319561));
#30325=CARTESIAN_POINT('Ctrl Pts',(-0.99111376328778,-4.81735161377302,
35.116122721398));
#30326=CARTESIAN_POINT('Ctrl Pts',(-0.895339724961226,-4.83705600223404,
35.1216607390959));
#30327=CARTESIAN_POINT('Ctrl Pts',(-0.798987190987151,-4.85390143898352,
35.1271987567937));
#30328=CARTESIAN_POINT('Ctrl Pts',(-0.702230674208628,-4.86785940046552,
35.1327367744915));
#30329=CARTESIAN_POINT('Ctrl Pts',(-0.55972695622198,-4.88841679001326,
35.1408932081716));
#30330=CARTESIAN_POINT('Ctrl Pts',(-0.41629327802585,-4.90271615377631,
35.1490496418517));
#30331=CARTESIAN_POINT('Ctrl Pts',(-0.272491180651915,-4.91069563493472,
35.1572060755317));
#30332=CARTESIAN_POINT('Ctrl Pts',(-0.128718351058837,-4.91867349204376,
35.1653608491476));
#30333=CARTESIAN_POINT('Ctrl Pts',(0.0154224142110825,-4.92033401406274,
35.1735156227635));
#30334=CARTESIAN_POINT('Ctrl Pts',(0.159366224511822,-4.91566734726678,
35.1816703963793));
#30335=CARTESIAN_POINT('Ctrl Pts',(0.303315139513225,-4.91100051497613,
35.1898254591892));
#30336=CARTESIAN_POINT('Ctrl Pts',(0.447066751008784,-4.90000605197425,
35.197980521999));
#30337=CARTESIAN_POINT('Ctrl Pts',(0.590057428971841,-4.88272621524238,
35.2061355848088));
#30338=CARTESIAN_POINT('Ctrl Pts',(0.733039720541969,-4.86544739197168,
35.2142901693248));
#30339=CARTESIAN_POINT('Ctrl Pts',(0.87526083575672,-4.84188397357044,35.2224447538407));
#30340=CARTESIAN_POINT('Ctrl Pts',(1.01616356737732,-4.81212995115832,35.2305993383567));
#30341=CARTESIAN_POINT('Ctrl Pts',(1.15710094203062,-4.78236861327716,35.2387559277986));
#30342=CARTESIAN_POINT('Ctrl Pts',(1.29671895777609,-4.74641369894058,35.2469125172405));
#30343=CARTESIAN_POINT('Ctrl Pts',(1.43447127059977,-4.70441019005825,35.2550691066824));
#30344=CARTESIAN_POINT('Ctrl Pts',(1.52799991413489,-4.67589138606177,35.2606071243805));
#30345=CARTESIAN_POINT('Ctrl Pts',(1.62066872458696,-4.64458529858958,35.2661451420786));
#30346=CARTESIAN_POINT('Ctrl Pts',(1.7123108115699,-4.6105503735542,35.2716831597767));
#30347=CARTESIAN_POINT('Ctrl Pts',(1.84728195928515,-4.56042348267184,35.2798395934567));
#30348=CARTESIAN_POINT('Ctrl Pts',(1.98007566607134,-4.50435635074101,35.2879960271368));
#30349=CARTESIAN_POINT('Ctrl Pts',(2.11016923544657,-4.44256332090774,35.2961524608169));
#30350=CARTESIAN_POINT('Ctrl Pts',(2.24023632711345,-4.38078286769782,35.3043072344328));
#30351=CARTESIAN_POINT('Ctrl Pts',(2.36760407561693,-4.31327898494002,35.3124620080487));
#30352=CARTESIAN_POINT('Ctrl Pts',(2.49177172321678,-4.24031328345881,35.3206167816646));
#30353=CARTESIAN_POINT('Ctrl Pts',(2.61594377419179,-4.16734499438443,35.3287718444745));
#30354=CARTESIAN_POINT('Ctrl Pts',(2.73691520678645,-4.0889146652997,35.3369269072843));
#30355=CARTESIAN_POINT('Ctrl Pts',(2.85421130183859,-4.00532906350488,35.3450819700941));
#30356=CARTESIAN_POINT('Ctrl Pts',(2.9715005174835,-3.92174836399937,35.3532365546101));
#30357=CARTESIAN_POINT('Ctrl Pts',(3.08511455486701,-3.83301319166472,35.3613911391261));
#30358=CARTESIAN_POINT('Ctrl Pts',(3.19460908625978,-3.73947266984082,35.3695457236421));
#30359=CARTESIAN_POINT('Ctrl Pts',(3.3041305385117,-3.64590914968833,35.377702313084));
#30360=CARTESIAN_POINT('Ctrl Pts',(3.40953020620542,-3.54753813649967,35.3858589025259));
#30361=CARTESIAN_POINT('Ctrl Pts',(3.51039769664934,-3.44474833244158,35.3940154919678));
#30362=CARTESIAN_POINT('Ctrl Pts',(3.57888293195628,-3.37495791843314,35.3995535096658));
#30363=CARTESIAN_POINT('Ctrl Pts',(3.6452795935013,-3.30313130164868,35.4050915273638));
#30364=CARTESIAN_POINT('Ctrl Pts',(3.70946909361247,-3.229399651024,35.4106295450617));
#30365=CARTESIAN_POINT('Ctrl Pts',(3.80400786708083,-3.12080712726568,35.4187859787418));
#30366=CARTESIAN_POINT('Ctrl Pts',(3.8937925591734,-3.00804010677295,35.4269424124219));
#30367=CARTESIAN_POINT('Ctrl Pts',(3.97846672749768,-2.89153688558419,35.435098846102));
#30368=CARTESIAN_POINT('Ctrl Pts',(4.06312366224199,-2.77505737608482,35.4432536197179));
#30369=CARTESIAN_POINT('Ctrl Pts',(4.14267195161278,-2.65484345341187,35.4514083933338));
#30370=CARTESIAN_POINT('Ctrl Pts',(4.21679703265162,-2.53136442416348,35.4595631669497));
#30371=CARTESIAN_POINT('Ctrl Pts',(4.2909247423989,-2.40788101596046,35.4677182297596));
#30372=CARTESIAN_POINT('Ctrl Pts',(4.35962868353461,-2.281132554444,35.4758732925694));
#30373=CARTESIAN_POINT('Ctrl Pts',(4.42263876262049,-2.15161554137042,35.4840283553792));
#30374=CARTESIAN_POINT('Ctrl Pts',(4.48564514616972,-2.02210612446042,35.4921829398952));
#30375=CARTESIAN_POINT('Ctrl Pts',(4.5429581902288,-1.88982878218134,35.5003375244112));
#30376=CARTESIAN_POINT('Ctrl Pts',(4.59435475339333,-1.75530266976156,35.5084921089272));
#30377=CARTESIAN_POINT('Ctrl Pts',(4.64576395316754,-1.62074348209575,35.5166486983691));
#30378=CARTESIAN_POINT('Ctrl Pts',(4.69125364563663,-1.48393473213877,35.524805287811));
#30379=CARTESIAN_POINT('Ctrl Pts',(4.73064942443394,-1.34541409447159,35.5329618772529));
#30380=CARTESIAN_POINT('Ctrl Pts',(4.7573976777033,-1.25136378724406,35.5384998949509));
#30381=CARTESIAN_POINT('Ctrl Pts',(4.78133771546532,-1.15652469121814,35.5440379126489));
#30382=CARTESIAN_POINT('Ctrl Pts',(4.80242815902273,-1.06106872535455,35.5495759303469));
#30383=CARTESIAN_POINT('Ctrl Pts',(4.83349032125123,-0.920480468437998,
35.557732364027));
#30384=CARTESIAN_POINT('Ctrl Pts',(4.85838058965853,-0.778501010826628,
35.5658887977071));
#30385=CARTESIAN_POINT('Ctrl Pts',(4.87699566032415,-0.635685764886574,
35.5740452313871));
#30386=CARTESIAN_POINT('Ctrl Pts',(4.89560694229816,-0.492899585874827,
35.5822000050031));
#30387=CARTESIAN_POINT('Ctrl Pts',(4.90794553120562,-0.349278289508366,
35.590354778619));
#30388=CARTESIAN_POINT('Ctrl Pts',(4.91395973495841,-0.20538448263561,35.5985095522349));
#30389=CARTESIAN_POINT('Ctrl Pts',(4.91997415199377,-0.0614855728359807,
35.6066646150447));
#30390=CARTESIAN_POINT('Ctrl Pts',(4.91966371736256,0.0826855326418441,
35.6148196778545));
#30391=CARTESIAN_POINT('Ctrl Pts',(4.91302879980008,0.226563622046861,35.6229747406644));
#30392=CARTESIAN_POINT('Ctrl Pts',(4.906394271375,0.370433273012985,35.6311293251804));
#30393=CARTESIAN_POINT('Ctrl Pts',(4.8934360184806,0.514009608047258,35.6392839096964));
#30394=CARTESIAN_POINT('Ctrl Pts',(4.87420647772475,0.656729986376489,35.6474384942125));
#30395=CARTESIAN_POINT('Ctrl Pts',(4.85497220910031,0.799485454633476,35.6555950836544));
#30396=CARTESIAN_POINT('Ctrl Pts',(4.82946361606154,0.941384213849286,35.6637516730963));
#30397=CARTESIAN_POINT('Ctrl Pts',(4.79778479087673,1.08187067754511,35.6719082625382));
#30398=CARTESIAN_POINT('Ctrl Pts',(4.77627605909945,1.17725570676714,35.6774462802361));
#30399=CARTESIAN_POINT('Ctrl Pts',(4.75192398480672,1.27198984011147,35.6829842979341));
#30400=CARTESIAN_POINT('Ctrl Pts',(4.72477448451324,1.36590231458644,35.688522315632));
#30401=CARTESIAN_POINT('Ctrl Pts',(4.68478849843133,1.50421730590053,35.6966787493121));
#30402=CARTESIAN_POINT('Ctrl Pts',(4.63871723203097,1.64080109065291,35.7048351829922));
#30403=CARTESIAN_POINT('Ctrl Pts',(4.58673570064337,1.77511652432834,35.7129916166723));
#30404=CARTESIAN_POINT('Ctrl Pts',(4.53476474896289,1.90940462102638,35.7211463902882));
#30405=CARTESIAN_POINT('Ctrl Pts',(4.47688605272524,2.04142497577482,35.7293011639041));
#30406=CARTESIAN_POINT('Ctrl Pts',(4.41332339088377,2.17065881933991,35.73745593752));
#30407=CARTESIAN_POINT('Ctrl Pts',(4.34975847491045,2.29989724594348,35.7456110003298));
#30408=CARTESIAN_POINT('Ctrl Pts',(4.28050933430343,2.42634866171021,35.7537660631396));
#30409=CARTESIAN_POINT('Ctrl Pts',(4.20584671009077,2.54951691771572,35.7619211259494));
#30410=CARTESIAN_POINT('Ctrl Pts',(4.13118846483564,2.67267794991188,35.7700757104653));
#30411=CARTESIAN_POINT('Ctrl Pts',(4.05111754546079,2.79255592190872,35.7782302949813));
#30412=CARTESIAN_POINT('Ctrl Pts',(3.96594918493528,2.90868185352252,35.7863848794973));
#30413=CARTESIAN_POINT('Ctrl Pts',(3.88075988450122,3.02483633642429,35.7945414689391));
#30414=CARTESIAN_POINT('Ctrl Pts',(3.79047083639418,3.13723666550547,35.802698058381));
#30415=CARTESIAN_POINT('Ctrl Pts',(3.6954392585745,3.24544476900876,35.8108546478229));
#30416=CARTESIAN_POINT('Ctrl Pts',(3.63091638861855,3.31891400471662,35.816392665521));
#30417=CARTESIAN_POINT('Ctrl Pts',(3.56420812623701,3.39045131857025,35.8219306832191));
#30418=CARTESIAN_POINT('Ctrl Pts',(3.49543649080652,3.45992872776856,35.8274687009172));
#30419=CARTESIAN_POINT('Ctrl Pts',(3.39414911434074,3.56225557309202,35.8356251345972));
#30420=CARTESIAN_POINT('Ctrl Pts',(3.28834638458959,3.66015079372222,35.8437815682773));
#30421=CARTESIAN_POINT('Ctrl Pts',(3.17843897538824,3.75322644430534,35.8519380019574));
#30422=CARTESIAN_POINT('Ctrl Pts',(3.0685539354429,3.84628315136982,35.8600927755733));
#30423=CARTESIAN_POINT('Ctrl Pts',(2.95456613786648,3.93452202913846,35.8682475491892));
#30424=CARTESIAN_POINT('Ctrl Pts',(2.8369202855612,4.01759459824798,35.8764023228051));
#30425=CARTESIAN_POINT('Ctrl Pts',(2.71927026116367,4.10067011337229,35.884557385615));
#30426=CARTESIAN_POINT('Ctrl Pts',(2.59796219362905,4.1785787571513,35.8927124484248));
#30427=CARTESIAN_POINT('Ctrl Pts',(2.47347120197562,4.2510143819443,35.9008675112347));
#30428=CARTESIAN_POINT('Ctrl Pts',(2.3489875117094,4.3234457583934,35.9090220957507));
#30429=CARTESIAN_POINT('Ctrl Pts',(2.22132156051851,4.39040459057065,35.9171766802667));
#30430=CARTESIAN_POINT('Ctrl Pts',(2.0909745383266,4.45162987484021,35.9253312647828));
#30431=CARTESIAN_POINT('Ctrl Pts',(1.96059546838083,4.51287021225642,35.9334878542247));
#30432=CARTESIAN_POINT('Ctrl Pts',(1.82753431316723,4.56837404238567,35.9416444436666));
#30433=CARTESIAN_POINT('Ctrl Pts',(1.69231434290758,4.61792759008727,35.9498010331085));
#30434=CARTESIAN_POINT('Ctrl Pts',(1.60050506480937,4.65157258670245,35.9553390508064));
#30435=CARTESIAN_POINT('Ctrl Pts',(1.5077010432793,4.68247554983713,35.9608770685043));
#30436=CARTESIAN_POINT('Ctrl Pts',(1.41407065780245,4.71058247324491,35.9664150862022));
#30437=CARTESIAN_POINT('Ctrl Pts',(1.27617112926228,4.75197855921538,35.9745715198823));
#30438=CARTESIAN_POINT('Ctrl Pts',(1.13642681146136,4.78732283014429,35.9827279535624));
#30439=CARTESIAN_POINT('Ctrl Pts',(0.995383933206272,4.81647110320563,35.9908843872425));
#30440=CARTESIAN_POINT('Ctrl Pts',(0.854369761154215,4.84561344377144,35.9990391608584));
#30441=CARTESIAN_POINT('Ctrl Pts',(0.712057883404491,4.86856223452924,36.0071939344742));
#30442=CARTESIAN_POINT('Ctrl Pts',(0.569005528542592,4.88522422934587,36.0153487080901));
#30443=CARTESIAN_POINT('Ctrl Pts',(0.425948100593104,4.90188681504938,36.0235037708999));
#30444=CARTESIAN_POINT('Ctrl Pts',(0.282150474919354,4.91226211624998,36.0316588337098));
#30445=CARTESIAN_POINT('Ctrl Pts',(0.13817633620382,4.9163086114089,36.0398138965196));
#30446=CARTESIAN_POINT('Ctrl Pts',(-0.00578935843962983,4.92035486924119,
36.0479684810357));
#30447=CARTESIAN_POINT('Ctrl Pts',(-0.149931210878958,4.91807305518458,
36.0561230655517));
#30448=CARTESIAN_POINT('Ctrl Pts',(-0.29368424145842,4.90947376292195,36.0642776500678));
#30449=CARTESIAN_POINT('Ctrl Pts',(-0.437472615858507,4.90087235639542,
36.0724342395097));
#30450=CARTESIAN_POINT('Ctrl Pts',(-0.580871643178157,4.88595038770334,
36.0805908289516));
#30451=CARTESIAN_POINT('Ctrl Pts',(-0.723319550325413,4.8647704869415,36.0887474183935));
#30452=CARTESIAN_POINT('Ctrl Pts',(-0.820036325938714,4.85039013028679,
36.0942854360915));
#30453=CARTESIAN_POINT('Ctrl Pts',(-0.916314722954619,4.83312601110554,
36.0998234537895));
#30454=CARTESIAN_POINT('Ctrl Pts',(-1.01198104501103,4.81301126396338,36.1053614714875));
#30455=CARTESIAN_POINT('Ctrl Pts',(-1.15287911609435,4.78338611467638,36.1135179051677));
#30456=CARTESIAN_POINT('Ctrl Pts',(-1.29250173701214,4.74756411622313,36.1216743388478));
#30457=CARTESIAN_POINT('Ctrl Pts',(-1.43030026963249,4.70567999349607,36.1298307725279));
#30458=CARTESIAN_POINT('Ctrl Pts',(-1.5680707563656,4.6638043953691,36.1379855461437));
#30459=CARTESIAN_POINT('Ctrl Pts',(-1.70401757545809,4.61586923161095,36.1461403197596));
#30460=CARTESIAN_POINT('Ctrl Pts',(-1.83760679953115,4.56205921846888,36.1542950933754));
#30461=CARTESIAN_POINT('Ctrl Pts',(-1.97120076109933,4.50824729705406,36.1624501561853));
#30462=CARTESIAN_POINT('Ctrl Pts',(-2.10243664856603,4.44856023090712,36.1706052189951));
#30463=CARTESIAN_POINT('Ctrl Pts',(-2.23079961217624,4.38323124564679,36.1787602818049));
#30464=CARTESIAN_POINT('Ctrl Pts',(-2.35915504730866,4.31790609192635,36.186914866321));
#30465=CARTESIAN_POINT('Ctrl Pts',(-2.48463759787963,4.246939833731,36.195069450837));
#30466=CARTESIAN_POINT('Ctrl Pts',(-2.60675621074842,4.1706120798061,36.2032240353531));
#30467=CARTESIAN_POINT('Ctrl Pts',(-2.72890484829438,4.09426555956771,36.211380624795));
#30468=CARTESIAN_POINT('Ctrl Pts',(-2.847687611455,4.01255508678855,36.2195372142369));
#30469=CARTESIAN_POINT('Ctrl Pts',(-2.96264115890128,3.92580443044277,36.2276938036788));
#30470=CARTESIAN_POINT('Ctrl Pts',(-3.0406902975429,3.86690399496428,36.2332318213767));
#30471=CARTESIAN_POINT('Ctrl Pts',(-3.11697479224663,3.80568099756497,36.2387698390746));
#30472=CARTESIAN_POINT('Ctrl Pts',(-3.1913579690167,3.74224763692806,36.2443078567726));
#30473=CARTESIAN_POINT('Ctrl Pts',(-3.30091006533164,3.64882251130377,36.2524642904526));
#30474=CARTESIAN_POINT('Ctrl Pts',(-3.40637736857711,3.55056601131062,36.2606207241326));
#30475=CARTESIAN_POINT('Ctrl Pts',(-3.50734256422543,3.44785892978129,36.2687771578127));
#30476=CARTESIAN_POINT('Ctrl Pts',(-3.60828721061027,3.34517275203831,36.2769319314285));
#30477=CARTESIAN_POINT('Ctrl Pts',(-3.7047313429311,3.23803803830448,36.2850867050444));
#30478=CARTESIAN_POINT('Ctrl Pts',(-3.79629448213534,3.12687244181926,36.2932414786603));
#30479=CARTESIAN_POINT('Ctrl Pts',(-3.88786086845674,3.01570290305203,36.3013965414701));
#30480=CARTESIAN_POINT('Ctrl Pts',(-3.97454569966372,2.90050245139121,36.3095516042799));
#30481=CARTESIAN_POINT('Ctrl Pts',(-4.05600845779462,2.78172220985462,36.3177066670897));
#30482=CARTESIAN_POINT('Ctrl Pts',(-4.13746643814055,2.66294893477077,36.3258612516057));
#30483=CARTESIAN_POINT('Ctrl Pts',(-4.21370276966811,2.54059656636371,36.3340158361216));
#30484=CARTESIAN_POINT('Ctrl Pts',(-4.28442002208921,2.41514557259414,36.3421704206376));
#30485=CARTESIAN_POINT('Ctrl Pts',(-4.35515466139905,2.28966373483112,36.3503270100795));
#30486=CARTESIAN_POINT('Ctrl Pts',(-4.42036734553155,2.16108204090106,36.3584835995213));
#30487=CARTESIAN_POINT('Ctrl Pts',(-4.47980610638382,2.02990647856156,36.3666401889632));
#30488=CARTESIAN_POINT('Ctrl Pts',(-4.52016279123364,1.94084320144363,36.3721782066614));
#30489=CARTESIAN_POINT('Ctrl Pts',(-4.55785870643562,1.85058469757476,36.3777162243595));
#30490=CARTESIAN_POINT('Ctrl Pts',(-4.59282751524086,1.75929488083905,36.3832542420577));
#30491=CARTESIAN_POINT('Ctrl Pts',(-4.6441959739934,1.62519202330009,36.3913894758108));
#30492=CARTESIAN_POINT('Ctrl Pts',(-4.68969766571455,1.48880998238945,36.3995247095639));
#30493=CARTESIAN_POINT('Ctrl Pts',(-4.72914863910647,1.35067990720875,36.407659943317));
#30494=CARTESIAN_POINT('Ctrl Pts',(-4.74135795832662,1.30793129958807,36.4101776420524));
#30495=CARTESIAN_POINT('Ctrl Pts',(-4.75298810446264,1.26501539330207,36.4126953407879));
#30496=CARTESIAN_POINT('Ctrl Pts',(-4.76403458704968,1.22194824599668,36.4152130395234));
#30497=CARTESIAN_POINT('Ctrl Pts',(-4.76374291154778,1.22187309174177,34.6652037882801));
#30498=CARTESIAN_POINT('Ctrl Pts',(-4.83809112144176,0.932844481302283,
34.6821017317321));
#30499=CARTESIAN_POINT('Ctrl Pts',(-4.90466058528984,0.52491922363429,34.7054139903085));
#30500=CARTESIAN_POINT('Ctrl Pts',(-4.91858708601659,0.113351080789942,
34.7287262488849));
#30501=CARTESIAN_POINT('Ctrl Pts',(-4.918482524436,0.000101975006558605,
34.7351405640093));
#30502=CARTESIAN_POINT('',(-4.91824999921026,8.81380467261397E-5,34.3898594359908));
#30503=CARTESIAN_POINT('Ctrl Pts',(-4.76403458704967,1.22194824599671,34.3199237602016));
#30504=CARTESIAN_POINT('Ctrl Pts',(-4.79037732700833,1.11924526762439,34.3259288039984));
#30505=CARTESIAN_POINT('Ctrl Pts',(-4.81339501831344,1.0157006926628,34.3319338477951));
#30506=CARTESIAN_POINT('Ctrl Pts',(-4.83304115288514,0.9115351211109,34.3379388915919));
#30507=CARTESIAN_POINT('Ctrl Pts',(-4.86135174302733,0.761429827249134,
34.3465923156584));
#30508=CARTESIAN_POINT('Ctrl Pts',(-4.88266723294743,0.609990304203609,
34.3552457397249));
#30509=CARTESIAN_POINT('Ctrl Pts',(-4.89689112312491,0.457865035529576,
34.3638991637913));
#30510=CARTESIAN_POINT('Ctrl Pts',(-4.91111501330238,0.305739766855543,
34.3725525878578));
#30511=CARTESIAN_POINT('Ctrl Pts',(-4.91824726020695,0.152929090369015,
34.3812060119243));
#30512=CARTESIAN_POINT('Ctrl Pts',(-4.91824999921026,8.81380467261397E-5,
34.3898594359908));
#30513=CARTESIAN_POINT('Ctrl Pts',(-4.91824999938303,7.79028443291767E-5,
34.3896774359301));
#30514=CARTESIAN_POINT('Ctrl Pts',(-4.91825074414469,-0.0469412282994122,
34.3923216676047));
#30515=CARTESIAN_POINT('Ctrl Pts',(-4.91757722521463,-0.0939577480454042,
34.3949691675867));
#30516=CARTESIAN_POINT('Ctrl Pts',(-4.91500835274931,-0.183553522053632,
34.4000241138427));
#30517=CARTESIAN_POINT('Ctrl Pts',(-4.91323348613992,-0.226131998448165,
34.4024305931114));
#30518=CARTESIAN_POINT('Ctrl Pts',(-4.90719185527896,-0.336559556576164,
34.4086854898363));
#30519=CARTESIAN_POINT('Ctrl Pts',(-4.90207131642267,-0.404352457993183,
34.4125389499999));
#30520=CARTESIAN_POINT('Ctrl Pts',(-4.88447473963195,-0.58685625090398,
34.4229573023208));
#30521=CARTESIAN_POINT('Ctrl Pts',(-4.86936491820749,-0.701269199383594,
34.4295369919425));
#30522=CARTESIAN_POINT('Ctrl Pts',(-4.82106155443031,-0.988717887391323,
34.446201637765));
#30523=CARTESIAN_POINT('Ctrl Pts',(-4.78256986429135,-1.16069948524653,
34.4562994768585));
#30524=CARTESIAN_POINT('Ctrl Pts',(-4.72291365775679,-1.37304253060127,
34.4688779055031));
#30525=CARTESIAN_POINT('Ctrl Pts',(-4.71031039376294,-1.41567484180246,
34.4714086792694));
#30526=CARTESIAN_POINT('Ctrl Pts',(-4.68674507289465,-1.49158668918534,
34.4759223949944));
#30527=CARTESIAN_POINT('Ctrl Pts',(-4.67600215783279,-1.52493084691938,
34.4779073461427));
#30528=CARTESIAN_POINT('Ctrl Pts',(-4.64717933540673,-1.61122229437934,
34.4830508795125));
#30529=CARTESIAN_POINT('Ctrl Pts',(-4.62855058951403,-1.66398095118079,
34.4862030395873));
#30530=CARTESIAN_POINT('Ctrl Pts',(-4.55118306562789,-1.87173361758746,
34.4986689023063));
#30531=CARTESIAN_POINT('Ctrl Pts',(-4.4855256519364,-2.02403417003301,34.507929636316));
#30532=CARTESIAN_POINT('Ctrl Pts',(-4.37437913226233,-2.24974670939476,
34.5220370575558));
#30533=CARTESIAN_POINT('Ctrl Pts',(-4.33444412179511,-2.32575730145814,
34.5268564192795));
#30534=CARTESIAN_POINT('Ctrl Pts',(-4.26128310972199,-2.45657281426278,
34.5352939920868));
#30535=CARTESIAN_POINT('Ctrl Pts',(-4.22893745168335,-2.51184626432518,
34.538905397353));
#30536=CARTESIAN_POINT('Ctrl Pts',(-4.17932890940758,-2.59294347892429,
34.5442792923364));
#30537=CARTESIAN_POINT('Ctrl Pts',(-4.16288573415952,-2.61926103492093,
34.5460352463685));
#30538=CARTESIAN_POINT('Ctrl Pts',(-4.11530054319865,-2.6938417747727,34.5510468622103));
#30539=CARTESIAN_POINT('Ctrl Pts',(-4.08356079159473,-2.74171720776653,
34.554306867514));
#30540=CARTESIAN_POINT('Ctrl Pts',(-3.94365473255752,-2.94492727599082,
34.5683372832408));
#30541=CARTESIAN_POINT('Ctrl Pts',(-3.82741036747741,-3.0945011581524,34.5791655424194));
#30542=CARTESIAN_POINT('Ctrl Pts',(-3.64930129493728,-3.29824191828655,
34.59465592058));
#30543=CARTESIAN_POINT('Ctrl Pts',(-3.59425339245277,-3.35814567455288,
34.5993096786689));
#30544=CARTESIAN_POINT('Ctrl Pts',(-3.52101267723659,-3.43398207957179,
34.6053257622797));
#30545=CARTESIAN_POINT('Ctrl Pts',(-3.50415331489639,-3.45118425311468,
34.6066990137477));
#30546=CARTESIAN_POINT('Ctrl Pts',(-3.45647102549121,-3.49912646949745,
34.6105500535178));
#30547=CARTESIAN_POINT('Ctrl Pts',(-3.42536517517964,-3.52958233706649,
34.6130243872956));
#30548=CARTESIAN_POINT('Ctrl Pts',(-3.39134947615652,-3.56201401099534,
34.6156883959412));
#30549=CARTESIAN_POINT('Ctrl Pts',(-3.38883753453079,-3.56440391209304,
34.6158848812093));
#30550=CARTESIAN_POINT('Ctrl Pts',(-3.35599358006014,-3.59558606874761,
34.6184507766804));
#30551=CARTESIAN_POINT('Ctrl Pts',(-3.32529782845277,-3.62399316905981,
34.62081346202));
#30552=CARTESIAN_POINT('Ctrl Pts',(-3.22467620665868,-3.71475757311403,
34.6284535313758));
#30553=CARTESIAN_POINT('Ctrl Pts',(-3.15332959417629,-3.77550966987126,
34.6337105129599));
#30554=CARTESIAN_POINT('Ctrl Pts',(-2.9723991507809,-3.92086469062726,34.6467198304326));
#30555=CARTESIAN_POINT('Ctrl Pts',(-2.86089735463021,-4.00294926583454,
34.6544611036323));
#30556=CARTESIAN_POINT('Ctrl Pts',(-2.68483018214487,-4.12144650700363,
34.6663770741605));
#30557=CARTESIAN_POINT('Ctrl Pts',(-2.62265734073695,-4.16128618960683,
34.6705289536987));
#30558=CARTESIAN_POINT('Ctrl Pts',(-2.50428681509076,-4.23342986445814,
34.6783438937375));
#30559=CARTESIAN_POINT('Ctrl Pts',(-2.44830150448164,-4.26605209723561,
34.6820037504808));
#30560=CARTESIAN_POINT('Ctrl Pts',(-2.33804144834147,-4.32741431101967,
34.6891486301119));
#30561=CARTESIAN_POINT('Ctrl Pts',(-2.28384046379989,-4.35626274096333,
34.692632129344));
#30562=CARTESIAN_POINT('Ctrl Pts',(-2.03488902598885,-4.48284346803885,
34.7085119069185));
#30563=CARTESIAN_POINT('Ctrl Pts',(-1.83431814494171,-4.56858111255541,
34.7209879871812));
#30564=CARTESIAN_POINT('Ctrl Pts',(-1.56534041689761,-4.66298245892528,
34.7372974480912));
#30565=CARTESIAN_POINT('Ctrl Pts',(-1.50150283873288,-4.68392841090857,
34.741137197226));
#30566=CARTESIAN_POINT('Ctrl Pts',(-1.4293050322267,-4.70598972660754,34.7454413219094));
#30567=CARTESIAN_POINT('Ctrl Pts',(-1.42134796902732,-4.70839910514521,
34.745915165219));
#30568=CARTESIAN_POINT('Ctrl Pts',(-1.40829187019663,-4.71231634591387,
34.7466917867901));
#30569=CARTESIAN_POINT('Ctrl Pts',(-1.40319643566884,-4.71383613404634,
34.7469946639745));
#30570=CARTESIAN_POINT('Ctrl Pts',(-1.39474115994718,-4.71634311964407,
34.7474968902665));
#30571=CARTESIAN_POINT('Ctrl Pts',(-1.39138271322317,-4.7173349966728,34.7476962803704));
#30572=CARTESIAN_POINT('Ctrl Pts',(-1.38574834577608,-4.71899249920192,
34.748030631234));
#30573=CARTESIAN_POINT('Ctrl Pts',(-1.38347299877258,-4.71966006689258,
34.748165609608));
#30574=CARTESIAN_POINT('Ctrl Pts',(-1.37961899918934,-4.72078777148888,
34.7483941625807));
#30575=CARTESIAN_POINT('Ctrl Pts',(-1.37804059744594,-4.72124876257932,
34.7484877451053));
#30576=CARTESIAN_POINT('Ctrl Pts',(-1.34066744397065,-4.73214370012445,
34.7507030762123));
#30577=CARTESIAN_POINT('Ctrl Pts',(-1.30475517350021,-4.74217114508611,
34.7528209325033));
#30578=CARTESIAN_POINT('Ctrl Pts',(-1.23427474626808,-4.7609894840203,34.7569545438997));
#30579=CARTESIAN_POINT('Ctrl Pts',(-1.19971812253121,-4.76981461600973,
34.7589704975439));
#30580=CARTESIAN_POINT('Ctrl Pts',(-0.988413008190155,-4.82133645570441,
34.7712418842116));
#30581=CARTESIAN_POINT('Ctrl Pts',(-0.809502653869499,-4.85458058385838,
34.7814005214382));
#30582=CARTESIAN_POINT('Ctrl Pts',(-0.53503184515812,-4.8899827937999,34.7969097036767));
#30583=CARTESIAN_POINT('Ctrl Pts',(-0.440571400842349,-4.89939663984047,
34.802232847028));
#30584=CARTESIAN_POINT('Ctrl Pts',(-0.2805173499409,-4.91068111455807,34.8112586686447));
#30585=CARTESIAN_POINT('Ctrl Pts',(-0.215051137126121,-4.91398330175008,
34.8149521171336));
#30586=CARTESIAN_POINT('Ctrl Pts',(-0.0971283758486763,-4.91757039098498,
34.8216159470215));
#30587=CARTESIAN_POINT('Ctrl Pts',(-0.0446959804318531,-4.91832641024141,
34.8245827596083));
#30588=CARTESIAN_POINT('Ctrl Pts',(0.0888433687528893,-4.91811630500611,
34.8321529104713));
#30589=CARTESIAN_POINT('Ctrl Pts',(0.169932281921091,-4.91598249892155,
34.8367630425071));
#30590=CARTESIAN_POINT('Ctrl Pts',(0.444079372031434,-4.90197719218596,
34.8524062061807));
#30591=CARTESIAN_POINT('Ctrl Pts',(0.636476855251575,-4.88072565023785,
34.863487525507));
#30592=CARTESIAN_POINT('Ctrl Pts',(0.887380490528332,-4.8379206236326,34.8780445052179));
#30593=CARTESIAN_POINT('Ctrl Pts',(0.947444544338079,-4.8265172761627,34.8815366919209));
#30594=CARTESIAN_POINT('Ctrl Pts',(1.01056458987187,-4.81331003865799,34.8852115037291));
#30595=CARTESIAN_POINT('Ctrl Pts',(1.01384777450257,-4.81261955786096,34.8854026627514));
#30596=CARTESIAN_POINT('Ctrl Pts',(1.01970547135941,-4.81138137568049,34.8857437432547));
#30597=CARTESIAN_POINT('Ctrl Pts',(1.02228025473819,-4.81083496613095,34.8858936753608));
#30598=CARTESIAN_POINT('Ctrl Pts',(1.0268914922173,-4.80985251987779,34.8861622064881));
#30599=CARTESIAN_POINT('Ctrl Pts',(1.02892811000402,-4.80941725619766,34.8862808120459));
#30600=CARTESIAN_POINT('Ctrl Pts',(1.07387820941106,-4.79978071209952,34.8888986578261));
#30601=CARTESIAN_POINT('Ctrl Pts',(1.11666724303579,-4.79000664106514,34.8913928347294));
#30602=CARTESIAN_POINT('Ctrl Pts',(1.19917343997252,-4.76999453458668,34.8962038056025));
#30603=CARTESIAN_POINT('Ctrl Pts',(1.23890463824402,-4.75982984340485,34.8985211206678));
#30604=CARTESIAN_POINT('Ctrl Pts',(1.38187652545527,-4.72134097149887,34.9068707506923));
#30605=CARTESIAN_POINT('Ctrl Pts',(1.484313719197,-4.69014462031996,34.9128742179225));
#30606=CARTESIAN_POINT('Ctrl Pts',(1.68434726808814,-4.62201557986683,34.924716213517));
#30607=CARTESIAN_POINT('Ctrl Pts',(1.78194848922946,-4.5852713408477,34.9305519340014));
#30608=CARTESIAN_POINT('Ctrl Pts',(1.95334612389233,-4.51444506211634,34.9409550618655));
#30609=CARTESIAN_POINT('Ctrl Pts',(2.02760457068747,-4.48158396551061,34.9455156362989));
#30610=CARTESIAN_POINT('Ctrl Pts',(2.16788278557622,-4.41530709007382,34.95425362842));
#30611=CARTESIAN_POINT('Ctrl Pts',(2.23402892831928,-4.3822102927466,34.9584278156849));
#30612=CARTESIAN_POINT('Ctrl Pts',(2.35512967413449,-4.31816180740378,34.9661813093189));
#30613=CARTESIAN_POINT('Ctrl Pts',(2.41028406758654,-4.28762029343483,34.9697567446153));
#30614=CARTESIAN_POINT('Ctrl Pts',(2.56959412290019,-4.19535746381459,34.9802210705023));
#30615=CARTESIAN_POINT('Ctrl Pts',(2.67207566435028,-4.13084122715434,34.9871283272968));
#30616=CARTESIAN_POINT('Ctrl Pts',(2.88045431370102,-3.98865667594585,35.0015560980037));
#30617=CARTESIAN_POINT('Ctrl Pts',(2.98583455478219,-3.91039526977784,35.0090739592291));
#30618=CARTESIAN_POINT('Ctrl Pts',(3.14475690520836,-3.78219675358706,35.0207430164225));
#30619=CARTESIAN_POINT('Ctrl Pts',(3.20052847828905,-3.73512060430727,35.0249057257574));
#30620=CARTESIAN_POINT('Ctrl Pts',(3.28338290054233,-3.66196532314146,35.0311862835869));
#30621=CARTESIAN_POINT('Ctrl Pts',(3.31124806450737,-3.63678836472118,35.0333154705501));
#30622=CARTESIAN_POINT('Ctrl Pts',(3.37721092763697,-3.57580239473911,35.0383963404359));
#30623=CARTESIAN_POINT('Ctrl Pts',(3.41503130954039,-3.53970022218039,35.0413435921193));
#30624=CARTESIAN_POINT('Ctrl Pts',(3.56877194759443,-3.38818614303303,35.0534874992304));
#30625=CARTESIAN_POINT('Ctrl Pts',(3.67947516945032,-3.26762938574615,35.0626282366291));
#30626=CARTESIAN_POINT('Ctrl Pts',(3.84108437563824,-3.07298697472029,35.0768102810035));
#30627=CARTESIAN_POINT('Ctrl Pts',(3.89631578321361,-3.00264903960497,35.0818279271654));
#30628=CARTESIAN_POINT('Ctrl Pts',(3.99600755078186,-2.86830469104892,35.0912425446493));
#30629=CARTESIAN_POINT('Ctrl Pts',(4.04092399201479,-2.80467132565798,35.0956346738854));
#30630=CARTESIAN_POINT('Ctrl Pts',(4.1226044377536,-2.68291642884286,35.1039272487882));
#30631=CARTESIAN_POINT('Ctrl Pts',(4.15969752499579,-2.62503795634039,35.1078239510336));
#30632=CARTESIAN_POINT('Ctrl Pts',(4.25849930897197,-2.46351634486478,35.1185838220245));
#30633=CARTESIAN_POINT('Ctrl Pts',(4.31762708375117,-2.35835215793882,35.1254637639571));
#30634=CARTESIAN_POINT('Ctrl Pts',(4.37948025635084,-2.23820171788697,35.1331916014403));
#30635=CARTESIAN_POINT('Ctrl Pts',(4.3860744321992,-2.2252517431404,35.1340228158859));
#30636=CARTESIAN_POINT('Ctrl Pts',(4.46182235116031,-2.07484933382165,35.1436568720369));
#30637=CARTESIAN_POINT('Ctrl Pts',(4.52454670835785,-1.93425330871263,35.1524752345383));
#30638=CARTESIAN_POINT('Ctrl Pts',(4.59977867133716,-1.74183804071068,35.1642583112145));
#30639=CARTESIAN_POINT('Ctrl Pts',(4.61818931818931,-1.69242166698918,35.1672596324175));
#30640=CARTESIAN_POINT('Ctrl Pts',(4.64837931057808,-1.60722458043099,35.1723880856175));
#30641=CARTESIAN_POINT('Ctrl Pts',(4.66054863892969,-1.57158756684254,35.1745192133171));
#30642=CARTESIAN_POINT('Ctrl Pts',(4.69027507393914,-1.48115274608639,35.1798950581512));
#30643=CARTESIAN_POINT('Ctrl Pts',(4.70728203525076,-1.42618009876383,35.183133703897));
#30644=CARTESIAN_POINT('Ctrl Pts',(4.77022980523184,-1.20930222265085,35.1958222020602));
#30645=CARTESIAN_POINT('Ctrl Pts',(4.80881298324741,-1.04538147024358,35.2052239607812));
#30646=CARTESIAN_POINT('Ctrl Pts',(4.85335831839818,-0.800382789422243,
35.2191931890541));
#30647=CARTESIAN_POINT('Ctrl Pts',(4.86584119484062,-0.720617014055338,
35.223727776923));
#30648=CARTESIAN_POINT('Ctrl Pts',(4.88595833330758,-0.567477356665587,
35.2324272699616));
#30649=CARTESIAN_POINT('Ctrl Pts',(4.89391635714192,-0.494167893012595,
35.2365890323102));
#30650=CARTESIAN_POINT('Ctrl Pts',(4.90635657566737,-0.349269603322752,
35.2448203684671));
#30651=CARTESIAN_POINT('Ctrl Pts',(4.91092691024947,-0.277706364567444,
35.2488883312892));
#30652=CARTESIAN_POINT('Ctrl Pts',(4.92191132562743,-0.0157719820459993,
35.2637990267744));
#30653=CARTESIAN_POINT('Ctrl Pts',(4.91883053997718,0.174826206695605,35.2746965227519));
#30654=CARTESIAN_POINT('Ctrl Pts',(4.89879635409299,0.444212418833327,35.290158576961));
#30655=CARTESIAN_POINT('Ctrl Pts',(4.89095794756022,0.52350823523645,35.29471621915));
#30656=CARTESIAN_POINT('Ctrl Pts',(4.87788952290732,0.629369143233817,35.3008022574634));
#30657=CARTESIAN_POINT('Ctrl Pts',(4.87436178539507,0.656131779136851,35.3023409740495));
#30658=CARTESIAN_POINT('Ctrl Pts',(4.86465979669225,0.725332430524917,35.3063192485691));
#30659=CARTESIAN_POINT('Ctrl Pts',(4.85815046860718,0.767721403762226,35.3087557534089));
#30660=CARTESIAN_POINT('Ctrl Pts',(4.84419728172664,0.851284921245567,35.3135557108691));
#30661=CARTESIAN_POINT('Ctrl Pts',(4.83678072377878,0.892460420300843,35.3159192205619));
#30662=CARTESIAN_POINT('Ctrl Pts',(4.80816732466374,1.04046696157637,35.3244183385387));
#30663=CARTESIAN_POINT('Ctrl Pts',(4.78394864532835,1.14668232795667,35.3305246482754));
#30664=CARTESIAN_POINT('Ctrl Pts',(4.71531869157069,1.40739926996597,35.3456314857569));
#30665=CARTESIAN_POINT('Ctrl Pts',(4.66682342105925,1.56069270403046,35.3546208389073));
#30666=CARTESIAN_POINT('Ctrl Pts',(4.58293239882621,1.78672319446491,35.3681831994747));
#30667=CARTESIAN_POINT('Ctrl Pts',(4.55310816560508,1.86141209030977,35.3727162804049));
#30668=CARTESIAN_POINT('Ctrl Pts',(4.49438042703801,1.99861594648758,35.3811547706978));
#30669=CARTESIAN_POINT('Ctrl Pts',(4.46596909107252,2.06132022223891,35.3850556024099));
#30670=CARTESIAN_POINT('Ctrl Pts',(4.38678715884847,2.22674820904172,35.3954745487949));
#30671=CARTESIAN_POINT('Ctrl Pts',(4.3337277062924,2.32832832495043,35.4020069803053));
#30672=CARTESIAN_POINT('Ctrl Pts',(4.20695761677324,2.55165032044152,35.4166864261798));
#30673=CARTESIAN_POINT('Ctrl Pts',(4.13141289242162,2.67223486606339,35.4248364362686));
#30674=CARTESIAN_POINT('Ctrl Pts',(4.01967174683556,2.83450607149908,35.4360982966265));
#30675=CARTESIAN_POINT('Ctrl Pts',(3.98784228832422,2.87911437359183,35.4392263456227));
#30676=CARTESIAN_POINT('Ctrl Pts',(3.92899460527035,2.95873949708962,35.4448649364504));
#30677=CARTESIAN_POINT('Ctrl Pts',(3.90223678956224,2.99394156912474,35.4473778195897));
#30678=CARTESIAN_POINT('Ctrl Pts',(3.8532304820134,3.05664005760154,35.4518875807057));
#30679=CARTESIAN_POINT('Ctrl Pts',(3.83115332220221,3.08426617472947,35.4538867358657));
#30680=CARTESIAN_POINT('Ctrl Pts',(3.75985666853106,3.17153597972852,35.4602456957619));
#30681=CARTESIAN_POINT('Ctrl Pts',(3.70952741897562,3.23025837795004,35.4645908826303));
#30682=CARTESIAN_POINT('Ctrl Pts',(3.53329343628597,3.42632886065381,35.4793816893668));
#30683=CARTESIAN_POINT('Ctrl Pts',(3.40098078254064,3.55769891295114,35.4897881856924));
#30684=CARTESIAN_POINT('Ctrl Pts',(3.2311778263141,3.70814211254616,35.5025399427339));
#30685=CARTESIAN_POINT('Ctrl Pts',(3.20048872811925,3.73466195917086,35.5048220391819));
#30686=CARTESIAN_POINT('Ctrl Pts',(3.11397377532801,3.80757385763631,35.5111964149503));
#30687=CARTESIAN_POINT('Ctrl Pts',(3.05744411629576,3.85311389255301,35.5152945406126));
#30688=CARTESIAN_POINT('Ctrl Pts',(2.94934317972048,3.9363222325257,35.523017533691));
#30689=CARTESIAN_POINT('Ctrl Pts',(2.89800568544457,3.9742698503756,35.5266391511902));
#30690=CARTESIAN_POINT('Ctrl Pts',(2.68800168978644,4.12326731880424,35.5412799856154));
#30691=CARTESIAN_POINT('Ctrl Pts',(2.52357997662633,4.22589974555402,35.5523590464138));
#30692=CARTESIAN_POINT('Ctrl Pts',(2.28301200225218,4.35700477835287,35.5680412992763));
#30693=CARTESIAN_POINT('Ctrl Pts',(2.21155366352692,4.39370742774931,35.5726363150185));
#30694=CARTESIAN_POINT('Ctrl Pts',(2.08861779721544,4.45309081895141,35.5804265026641));
#30695=CARTESIAN_POINT('Ctrl Pts',(2.03759150475456,4.47666875156929,35.5836271366221));
#30696=CARTESIAN_POINT('Ctrl Pts',(1.95206899331457,4.5144212635825,35.5889331523417));
#30697=CARTESIAN_POINT('Ctrl Pts',(1.91779607910989,4.52908720742882,35.5910437831288));
#30698=CARTESIAN_POINT('Ctrl Pts',(1.82269681133135,4.56850869247828,35.5968595098942));
#30699=CARTESIAN_POINT('Ctrl Pts',(1.76153622343746,4.59243787452308,35.6005550265257));
#30700=CARTESIAN_POINT('Ctrl Pts',(1.54066140989137,4.67379372397906,35.6137762428182));
#30701=CARTESIAN_POINT('Ctrl Pts',(1.37847871486517,4.72416999752524,35.6232572068654));
#30702=CARTESIAN_POINT('Ctrl Pts',(1.13785854630853,4.78546104250795,35.6371897550111));
#30703=CARTESIAN_POINT('Ctrl Pts',(1.06124681526641,4.80303180326041,35.6416057346478));
#30704=CARTESIAN_POINT('Ctrl Pts',(0.913005491220411,4.83331058426471,35.6501297807318));
#30705=CARTESIAN_POINT('Ctrl Pts',(0.841450119119143,4.84628019884829,35.6542351000095));
#30706=CARTESIAN_POINT('Ctrl Pts',(0.706672533809823,4.86763399012172,35.6619602598687));
#30707=CARTESIAN_POINT('Ctrl Pts',(0.643523430792517,4.87638433808347,35.6655767889284));
#30708=CARTESIAN_POINT('Ctrl Pts',(0.42281232046767,4.90260548144071,35.6782141367267));
#30709=CARTESIAN_POINT('Ctrl Pts',(0.264591900243389,4.91368504302276,35.6872718082509));
#30710=CARTESIAN_POINT('Ctrl Pts',(0.00391130861140477,4.91931075411147,
35.7021969841897));
#30711=CARTESIAN_POINT('Ctrl Pts',(-0.0983369850662696,4.91832934726269,
35.7080507257407));
#30712=CARTESIAN_POINT('Ctrl Pts',(-0.264829880287277,4.91153702295192,
35.7175670470198));
#30713=CARTESIAN_POINT('Ctrl Pts',(-0.329122045356827,4.90764807403482,
35.7212379117332));
#30714=CARTESIAN_POINT('Ctrl Pts',(-0.430363191619516,4.89952565381932,
35.7270063843158));
#30715=CARTESIAN_POINT('Ctrl Pts',(-0.467371827186547,4.89613395752886,
35.7291121706339));
#30716=CARTESIAN_POINT('Ctrl Pts',(-0.56251269438262,4.8863260919902,35.7345190140703));
#30717=CARTESIAN_POINT('Ctrl Pts',(-0.620575357441604,4.8792919113134,35.737813252619));
#30718=CARTESIAN_POINT('Ctrl Pts',(-0.8520809972973,4.8470461346637,35.7509534417743));
#30719=CARTESIAN_POINT('Ctrl Pts',(-1.02424714000991,4.81360745164655,35.7607422030468));
#30720=CARTESIAN_POINT('Ctrl Pts',(-1.27291597077947,4.75136214304163,35.7751218579547));
#30721=CARTESIAN_POINT('Ctrl Pts',(-1.3510714039057,4.72973182974689,35.7796762632042));
#30722=CARTESIAN_POINT('Ctrl Pts',(-1.4993714977581,4.68471234091248,35.7884051144431));
#30723=CARTESIAN_POINT('Ctrl Pts',(-1.56959373461958,4.66165420689913,35.7925763508389));
#30724=CARTESIAN_POINT('Ctrl Pts',(-1.70674774442866,4.61316785025342,35.8008097182712));
#30725=CARTESIAN_POINT('Ctrl Pts',(-1.77369703218023,4.58784308318062,35.8048701489063));
#30726=CARTESIAN_POINT('Ctrl Pts',(-2.00817701243273,4.49324691822329,35.8192500710691));
#30727=CARTESIAN_POINT('Ctrl Pts',(-2.17240482237042,4.41618596522244,35.8296180705753));
#30728=CARTESIAN_POINT('Ctrl Pts',(-2.43382792269626,4.275399467294,35.8466151909248));
#30729=CARTESIAN_POINT('Ctrl Pts',(-2.53368969942039,4.21698658978817,35.8532324416303));
#30730=CARTESIAN_POINT('Ctrl Pts',(-2.66791069323429,4.1319853891978,35.8622780887086));
#30731=CARTESIAN_POINT('Ctrl Pts',(-2.70411538560231,4.10838298641798,35.864733687263));
#30732=CARTESIAN_POINT('Ctrl Pts',(-2.77450515324051,4.06116118919716,35.8695363196967));
#30733=CARTESIAN_POINT('Ctrl Pts',(-2.80871133408824,4.03757968823795,35.8718835670622));
#30734=CARTESIAN_POINT('Ctrl Pts',(-2.95943388126726,3.93083023077026,35.882297553027));
#30735=CARTESIAN_POINT('Ctrl Pts',(-3.07258632622914,3.84303127655233,35.890309712356));
#30736=CARTESIAN_POINT('Ctrl Pts',(-3.30008203783178,3.65003050180804,35.9070226926995));
#30737=CARTESIAN_POINT('Ctrl Pts',(-3.41359665507696,3.54409667055748,35.9157160760218));
#30738=CARTESIAN_POINT('Ctrl Pts',(-3.57230006490842,3.38128177480475,35.9285272479206));
#30739=CARTESIAN_POINT('Ctrl Pts',(-3.62154332756609,3.32848583616918,35.9326035210023));
#30740=CARTESIAN_POINT('Ctrl Pts',(-3.71229839944081,3.2267840166484,35.9403210647821));
#30741=CARTESIAN_POINT('Ctrl Pts',(-3.75405053938842,3.17811247902906,35.9439592773417));
#30742=CARTESIAN_POINT('Ctrl Pts',(-3.86796237286903,3.03994471280065,35.9541421979463));
#30743=CARTESIAN_POINT('Ctrl Pts',(-3.93795322476101,2.94871508723163,35.9607021659529));
#30744=CARTESIAN_POINT('Ctrl Pts',(-4.0806436240454,2.74857283843998,35.9747603210542));
#30745=CARTESIAN_POINT('Ctrl Pts',(-4.15232231793356,2.63903854233169,35.9822575754484));
#30746=CARTESIAN_POINT('Ctrl Pts',(-4.25699061142251,2.46424950146359,35.9939007057588));
#30747=CARTESIAN_POINT('Ctrl Pts',(-4.29303938975728,2.4008972618599,35.9980580617457));
#30748=CARTESIAN_POINT('Ctrl Pts',(-4.3455069459514,2.30372790713162,36.0043329788738));
#30749=CARTESIAN_POINT('Ctrl Pts',(-4.36296781754265,2.27048557921604,36.0064618431766));
#30750=CARTESIAN_POINT('Ctrl Pts',(-4.40384441819539,2.1904508355273,36.0115446006063));
#30751=CARTESIAN_POINT('Ctrl Pts',(-4.42689745977726,2.14347836363896,36.0144940474605));
#30752=CARTESIAN_POINT('Ctrl Pts',(-4.51892298387864,1.9481486768789,36.0266417500765));
#30753=CARTESIAN_POINT('Ctrl Pts',(-4.58122170532503,1.79676282753445,36.0357841157447));
#30754=CARTESIAN_POINT('Ctrl Pts',(-4.66570810398347,1.55831266185887,36.0499654484953));
#30755=CARTESIAN_POINT('Ctrl Pts',(-4.69325394094342,1.47327448889247,36.0549807112711));
#30756=CARTESIAN_POINT('Ctrl Pts',(-4.73461952527767,1.33260607176634,36.0632322216301));
#30757=CARTESIAN_POINT('Ctrl Pts',(-4.74981087387954,1.27740252714152,36.0664592637781));
#30758=CARTESIAN_POINT('Ctrl Pts',(-4.76403458739297,1.22194824465831,36.0696927553338));
#30759=CARTESIAN_POINT('Origin',(0.,0.,-3.23514056400928));
#30760=CARTESIAN_POINT('',(-4.76417305830272,1.22198379731345,38.1652023751175));
#30761=CARTESIAN_POINT('',(-4.76403458711433,1.22194824574464,37.8201594747841));
#30762=CARTESIAN_POINT('',(-4.76403458704967,1.22194824599672,-3.23514056400928));
#30763=CARTESIAN_POINT('',(-4.91815853856044,-0.000126264742759089,36.485140567961));
#30764=CARTESIAN_POINT('Ctrl Pts',(-4.91815853856044,-0.000126264742759089,
36.485140567961));
#30765=CARTESIAN_POINT('Ctrl Pts',(-4.9183727443974,-0.218274538310673,
36.4974939210882));
#30766=CARTESIAN_POINT('Ctrl Pts',(-4.85071591826797,-1.25417721681692,
36.5561627359772));
#30767=CARTESIAN_POINT('Ctrl Pts',(-4.13688039937621,-3.02851950177622,
36.6611470126279));
#30768=CARTESIAN_POINT('Ctrl Pts',(-2.18373858264853,-4.63864156990321,
36.800093397913));
#30769=CARTESIAN_POINT('Ctrl Pts',(0.301699006312604,-5.11807459118877,
36.9390397831982));
#30770=CARTESIAN_POINT('Ctrl Pts',(2.71359615099928,-4.34995468259888,37.0779861684833));
#30771=CARTESIAN_POINT('Ctrl Pts',(4.46404243787587,-2.52151441087003,37.2169325537684));
#30772=CARTESIAN_POINT('Ctrl Pts',(5.12635897532519,-0.0784440404670848,
37.3558789390535));
#30773=CARTESIAN_POINT('Ctrl Pts',(4.53910322825366,2.383747405796,37.4948253243387));
#30774=CARTESIAN_POINT('Ctrl Pts',(2.84542133781098,4.26489005974503,37.6337717096238));
#30775=CARTESIAN_POINT('Ctrl Pts',(0.458155627228689,5.1064472221517,37.7727180949089));
#30776=CARTESIAN_POINT('Ctrl Pts',(-2.04078750909336,4.70328567642987,37.911664480194));
#30777=CARTESIAN_POINT('Ctrl Pts',(-3.92533759866974,3.24421753779699,38.0424925735969));
#30778=CARTESIAN_POINT('Ctrl Pts',(-4.59593587221692,1.87509631612692,38.127005205238));
#30779=CARTESIAN_POINT('Ctrl Pts',(-4.76417305830272,1.22198379731345,38.1652023751175));
#30780=CARTESIAN_POINT('Ctrl Pts',(-4.76403458704968,1.22194824599668,36.4152130395234));
#30781=CARTESIAN_POINT('Ctrl Pts',(-4.79972046865974,1.0828189704184,36.4233465153422));
#30782=CARTESIAN_POINT('Ctrl Pts',(-4.82931125243571,0.942110445198123,
36.4314799911609));
#30783=CARTESIAN_POINT('Ctrl Pts',(-4.85268865924507,0.800372312698471,
36.4396134669797));
#30784=CARTESIAN_POINT('Ctrl Pts',(-4.87606781843622,0.658623555439367,
36.4477475524878));
#30785=CARTESIAN_POINT('Ctrl Pts',(-4.89323261137389,0.515845369784952,
36.4558816379958));
#30786=CARTESIAN_POINT('Ctrl Pts',(-4.90411614098923,0.372596213331416,
36.4640157235039));
#30787=CARTESIAN_POINT('Ctrl Pts',(-4.91353792651271,0.248586551371808,
36.4710573370057));
#30788=CARTESIAN_POINT('Ctrl Pts',(-4.91825318908601,0.124224198834564,
36.4780989505075));
#30789=CARTESIAN_POINT('Ctrl Pts',(-4.91824999838095,-0.000126197307044433,
36.4851405640093));
#30790=CARTESIAN_POINT('Ctrl Pts',(-4.76403458739297,1.22194824465831,36.0696927553338));
#30791=CARTESIAN_POINT('Ctrl Pts',(-4.76915365858994,1.20199041719359,36.070856479102));
#30792=CARTESIAN_POINT('Ctrl Pts',(-4.77414739613201,1.18200011230845,36.0720210311605));
#30793=CARTESIAN_POINT('Ctrl Pts',(-4.79525687143362,1.09518051212781,36.0770746475064));
#30794=CARTESIAN_POINT('Ctrl Pts',(-4.81009585453188,1.02804987461523,36.0809717342797));
#30795=CARTESIAN_POINT('Ctrl Pts',(-4.86834654471026,0.73556130694027,36.0979195148213));
#30796=CARTESIAN_POINT('Ctrl Pts',(-4.89736196884957,0.507633011785284,
36.1110600136259));
#30797=CARTESIAN_POINT('Ctrl Pts',(-4.91561843347707,0.185766226537681,
36.1295031537217));
#30798=CARTESIAN_POINT('Ctrl Pts',(-4.91825037702714,0.092882873750499,
36.1348100284067));
#30799=CARTESIAN_POINT('Ctrl Pts',(-4.91824985764764,-0.0350876821920873,
36.1420868305489));
#30800=CARTESIAN_POINT('Ctrl Pts',(-4.91787465981299,-0.0701546963813987,
36.1440771817146));
#30801=CARTESIAN_POINT('Ctrl Pts',(-4.91616350889335,-0.150123722229815,
36.1486062881711));
#30802=CARTESIAN_POINT('Ctrl Pts',(-4.91458736888693,-0.195017528460413,
36.1511421422222));
#30803=CARTESIAN_POINT('Ctrl Pts',(-4.90965832228768,-0.295955705186828,
36.1568357064839));
#30804=CARTESIAN_POINT('Ctrl Pts',(-4.90596034311486,-0.351977004863166,
36.1599901367399));
#30805=CARTESIAN_POINT('Ctrl Pts',(-4.8887269443645,-0.559040894279331,
36.1716502725919));
#30806=CARTESIAN_POINT('Ctrl Pts',(-4.86916758142504,-0.709496338106361,
36.1801267343971));
#30807=CARTESIAN_POINT('Ctrl Pts',(-4.82405283840344,-0.963891740085001,
36.1946230874154));
#30808=CARTESIAN_POINT('Ctrl Pts',(-4.80200176752851,-1.06834062535704,
36.2006223805234));
#30809=CARTESIAN_POINT('Ctrl Pts',(-4.76027223083158,-1.23841404828793,
36.2105051232522));
#30810=CARTESIAN_POINT('Ctrl Pts',(-4.74259017863045,-1.30449197949791,
36.2143734370645));
#30811=CARTESIAN_POINT('Ctrl Pts',(-4.70043830961648,-1.44980573098613,
36.2229523507716));
#30812=CARTESIAN_POINT('Ctrl Pts',(-4.67533109172692,-1.52883481968609,
36.2276662087741));
#30813=CARTESIAN_POINT('Ctrl Pts',(-4.57287602866743,-1.8251503429335,36.2455380171558));
#30814=CARTESIAN_POINT('Ctrl Pts',(-4.48227722362476,-2.03753736275619,
36.2587696446889));
#30815=CARTESIAN_POINT('Ctrl Pts',(-4.35116810217376,-2.29341583938602,
36.2751775824367));
#30816=CARTESIAN_POINT('Ctrl Pts',(-4.32434655824455,-2.34359702566997,
36.2784180459329));
#30817=CARTESIAN_POINT('Ctrl Pts',(-4.27857355765126,-2.42577262890232,
36.283757947967));
#30818=CARTESIAN_POINT('Ctrl Pts',(-4.26011942324112,-2.45803723976721,
36.2858628635063));
#30819=CARTESIAN_POINT('Ctrl Pts',(-4.20858540441802,-2.5458137013304,36.291614191006));
#30820=CARTESIAN_POINT('Ctrl Pts',(-4.17477442051568,-2.60088777153404,
36.2952513703655));
#30821=CARTESIAN_POINT('Ctrl Pts',(-4.08435117684644,-2.7418680341201,36.3046605879271));
#30822=CARTESIAN_POINT('Ctrl Pts',(-4.02611142905145,-2.82669273457415,
36.3104199277061));
#30823=CARTESIAN_POINT('Ctrl Pts',(-3.87217013280134,-3.03648457217969,
36.3249975394785));
#30824=CARTESIAN_POINT('Ctrl Pts',(-3.77305297749951,-3.15879889369088,
36.3338141331148));
#30825=CARTESIAN_POINT('Ctrl Pts',(-3.6257598569724,-3.32372026083363,36.3462787700566));
#30826=CARTESIAN_POINT('Ctrl Pts',(-3.58235384825361,-3.37045867916036,
36.3498810564949));
#30827=CARTESIAN_POINT('Ctrl Pts',(-3.48757739788449,-3.46861167924278,
36.3576054318407));
#30828=CARTESIAN_POINT('Ctrl Pts',(-3.43595150810933,-3.5197585364517,36.3617291118343));
#30829=CARTESIAN_POINT('Ctrl Pts',(-3.27792643239327,-3.66952629230834,
36.3741154567728));
#30830=CARTESIAN_POINT('Ctrl Pts',(-3.16827919646488,-3.76460236233875,
36.3824044328307));
#30831=CARTESIAN_POINT('Ctrl Pts',(-2.96279456250041,-3.92743552580013,
36.397411293512));
#30832=CARTESIAN_POINT('Ctrl Pts',(-2.86842759957285,-3.99687687535657,
36.4041190283989));
#30833=CARTESIAN_POINT('Ctrl Pts',(-2.72426787117915,-4.09522166724581,
36.4140786490599));
#30834=CARTESIAN_POINT('Ctrl Pts',(-2.67630152045202,-4.12672827072678,
36.4173471574357));
#30835=CARTESIAN_POINT('Ctrl Pts',(-2.59639012578395,-4.17723851743229,
36.422714119074));
#30836=CARTESIAN_POINT('Ctrl Pts',(-2.56476189492292,-4.19673203539651,
36.4248182203869));
#30837=CARTESIAN_POINT('Ctrl Pts',(-2.47809149356706,-4.24880409266185,
36.430531595401));
#30838=CARTESIAN_POINT('Ctrl Pts',(-2.42262977658445,-4.28067036623187,
36.434131900227));
#30839=CARTESIAN_POINT('Ctrl Pts',(-2.27809865825806,-4.36000380224147,
36.4433948881115));
#30840=CARTESIAN_POINT('Ctrl Pts',(-2.18816146882649,-4.40582753155394,
36.4490453437659));
#30841=CARTESIAN_POINT('Ctrl Pts',(-1.95126547375955,-4.51748374854374,
36.4637167856342));
#30842=CARTESIAN_POINT('Ctrl Pts',(-1.80237279492715,-4.57892430172765,
36.4727356618099));
#30843=CARTESIAN_POINT('Ctrl Pts',(-1.59075766756926,-4.65432351409807,
36.4853995559263));
#30844=CARTESIAN_POINT('Ctrl Pts',(-1.53036915096628,-4.6745275143435,36.4889959686534));
#30845=CARTESIAN_POINT('Ctrl Pts',(-1.4001071016717,-4.71531406958335,36.4967237688206));
#30846=CARTESIAN_POINT('Ctrl Pts',(-1.33013419623863,-4.73552843126685,
36.5008568208325));
#30847=CARTESIAN_POINT('Ctrl Pts',(-1.18354059721869,-4.77437205824853,
36.5094848613463));
#30848=CARTESIAN_POINT('Ctrl Pts',(-1.10686851233857,-4.79272770136382,
36.5139803912809));
#30849=CARTESIAN_POINT('Ctrl Pts',(-0.862099947135587,-4.84513938545707,
36.5282822763344));
#30850=CARTESIAN_POINT('Ctrl Pts',(-0.692648075571482,-4.87225106859554,
36.5381136708041));
#30851=CARTESIAN_POINT('Ctrl Pts',(-0.45771661135187,-4.89733341688776,
36.5516073274126));
#30852=CARTESIAN_POINT('Ctrl Pts',(-0.393175739072369,-4.9029370869517,
36.5552996437567));
#30853=CARTESIAN_POINT('Ctrl Pts',(-0.291453084146704,-4.9097474430385,
36.5610900653705));
#30854=CARTESIAN_POINT('Ctrl Pts',(-0.254336584095457,-4.91181003327085,
36.5631964839663));
#30855=CARTESIAN_POINT('Ctrl Pts',(-0.159061500614999,-4.91602168059029,
36.5685878054371));
#30856=CARTESIAN_POINT('Ctrl Pts',(-0.100881673223977,-4.91755963187683,
36.5718660010508));
#30857=CARTESIAN_POINT('Ctrl Pts',(0.108699118375107,-4.91937875025216,
36.5836488592819));
#30858=CARTESIAN_POINT('Ctrl Pts',(0.260066795118579,-4.91370212603069,
36.592112023372));
#30859=CARTESIAN_POINT('Ctrl Pts',(0.533586397255727,-4.89076870533044,
36.607497826894));
#30860=CARTESIAN_POINT('Ctrl Pts',(0.655810477627973,-4.8758840281008,36.6144066117279));
#30861=CARTESIAN_POINT('Ctrl Pts',(0.8397378360262,-4.84644363229078,36.6249090992425));
#30862=CARTESIAN_POINT('Ctrl Pts',(0.901930784488347,-4.83525555333189,
36.6284786899739));
#30863=CARTESIAN_POINT('Ctrl Pts',(1.03612870172869,-4.80843500302867,36.6362278924348));
#30864=CARTESIAN_POINT('Ctrl Pts',(1.10803284803315,-4.79237653984517,36.6404095328151));
#30865=CARTESIAN_POINT('Ctrl Pts',(1.25778653838397,-4.75538125074671,36.6491875557834));
#30866=CARTESIAN_POINT('Ctrl Pts',(1.3355370758514,-4.73413332663268,36.6537846962049));
#30867=CARTESIAN_POINT('Ctrl Pts',(1.61137584802014,-4.65141481377237,36.6702416063608));
#30868=CARTESIAN_POINT('Ctrl Pts',(1.80605539531741,-4.5793401484156,36.6821406405479));
#30869=CARTESIAN_POINT('Ctrl Pts',(2.03507818297181,-4.47766738938773,36.6964075302048));
#30870=CARTESIAN_POINT('Ctrl Pts',(2.07432106109065,-4.45962337584138,36.6988616261605));
#30871=CARTESIAN_POINT('Ctrl Pts',(2.15085572429808,-4.42320365267304,36.7036640114162));
#30872=CARTESIAN_POINT('Ctrl Pts',(2.18816231028214,-4.40486738176892,36.7060125019989));
#30873=CARTESIAN_POINT('Ctrl Pts',(2.24816515866717,-4.37442542191196,36.7098062108382));
#30874=CARTESIAN_POINT('Ctrl Pts',(2.27100659201765,-4.36261084914746,36.7112542875156));
#30875=CARTESIAN_POINT('Ctrl Pts',(2.42761967201566,-4.2800405177099,36.7212141084749));
#30876=CARTESIAN_POINT('Ctrl Pts',(2.55815713848632,-4.20332211675965,36.7296748834678));
#30877=CARTESIAN_POINT('Ctrl Pts',(2.79535887450648,-4.04876737336505,36.7455413947904));
#30878=CARTESIAN_POINT('Ctrl Pts',(2.90283066170729,-3.97242016958557,36.7529353450391));
#30879=CARTESIAN_POINT('Ctrl Pts',(3.05710596234772,-3.85321667938635,36.7639280127181));
#30880=CARTESIAN_POINT('Ctrl Pts',(3.1063567228369,-3.81362340112572,36.7674976596078));
#30881=CARTESIAN_POINT('Ctrl Pts',(3.21134346892449,-3.72583986514702,36.7752468058592));
#30882=CARTESIAN_POINT('Ctrl Pts',(3.26678710764764,-3.67732394500727,36.7794283330527));
#30883=CARTESIAN_POINT('Ctrl Pts',(3.38055788639135,-3.57316463836555,36.7882060072511));
#30884=CARTESIAN_POINT('Ctrl Pts',(3.43864926588164,-3.51729558064057,36.7928029115859));
#30885=CARTESIAN_POINT('Ctrl Pts',(3.63786059521919,-3.31605090794667,36.808985175974));
#30886=CARTESIAN_POINT('Ctrl Pts',(3.77134836138037,-3.16340879050152,36.8206074351496));
#30887=CARTESIAN_POINT('Ctrl Pts',(3.92265364090943,-2.96715630393549,36.834722765214));
#30888=CARTESIAN_POINT('Ctrl Pts',(3.94977029072956,-2.93096278269341,36.8372934393489));
#30889=CARTESIAN_POINT('Ctrl Pts',(3.99999551027771,-2.86196238409177,36.8421307986737));
#30890=CARTESIAN_POINT('Ctrl Pts',(4.02320910019249,-2.82923688308017,36.8443985764278));
#30891=CARTESIAN_POINT('Ctrl Pts',(4.12006346219044,-2.68909298197594,36.8540080299212));
#30892=CARTESIAN_POINT('Ctrl Pts',(4.18982321592747,-2.57905529323885,36.8613035060759));
#30893=CARTESIAN_POINT('Ctrl Pts',(4.34510123776315,-2.31116089382878,36.8786506666839));
#30894=CARTESIAN_POINT('Ctrl Pts',(4.42650742263402,-2.15113932963113,36.8886929152544));
#30895=CARTESIAN_POINT('Ctrl Pts',(4.52473862876919,-1.92872647022129,36.902398987217));
#30896=CARTESIAN_POINT('Ctrl Pts',(4.54935310344817,-1.86992825671265,36.9059989145167));
#30897=CARTESIAN_POINT('Ctrl Pts',(4.59959277319203,-1.74304869485935,36.9137246176184));
#30898=CARTESIAN_POINT('Ctrl Pts',(4.62486442537564,-1.67484366784924,36.9178520137867));
#30899=CARTESIAN_POINT('Ctrl Pts',(4.6962248560521,-1.46830217097573,36.930284139322));
#30900=CARTESIAN_POINT('Ctrl Pts',(4.73768411650814,-1.32845303780736,36.9386155180457));
#30901=CARTESIAN_POINT('Ctrl Pts',(4.79837909957649,-1.08439547331938,36.9530107281173));
#30902=CARTESIAN_POINT('Ctrl Pts',(4.82057543841378,-0.981024011397351,
36.9590637111313));
#30903=CARTESIAN_POINT('Ctrl Pts',(4.85088758435772,-0.813760173383621,
36.9687716407984));
#30904=CARTESIAN_POINT('Ctrl Pts',(4.86111003255971,-0.750283528148921,
36.972435899526));
#30905=CARTESIAN_POINT('Ctrl Pts',(4.87527298311822,-0.649828618438256,
36.9781976231457));
#30906=CARTESIAN_POINT('Ctrl Pts',(4.88004356932441,-0.612975285299537,
36.9803032249921));
#30907=CARTESIAN_POINT('Ctrl Pts',(4.89125660588522,-0.517902075131387,
36.9857149504015));
#30908=CARTESIAN_POINT('Ctrl Pts',(4.8970775079715,-0.45961478095763,36.9890142204667));
#30909=CARTESIAN_POINT('Ctrl Pts',(4.90888722511114,-0.315337114742292,
36.9971521125751));
#30910=CARTESIAN_POINT('Ctrl Pts',(4.91365934784131,-0.229266796234206,
37.0019818681607));
#30911=CARTESIAN_POINT('Ctrl Pts',(4.92137141890658,0.0356514832284077,
37.0168303411873));
#30912=CARTESIAN_POINT('Ctrl Pts',(4.91682088426007,0.214567202374961,37.0268388529457));
#30913=CARTESIAN_POINT('Ctrl Pts',(4.89680124701929,0.464409699242177,37.0409631330739));
#30914=CARTESIAN_POINT('Ctrl Pts',(4.88949939728122,0.535849146955819,37.0450181385255));
#30915=CARTESIAN_POINT('Ctrl Pts',(4.87155096025943,0.680140738863191,37.0532514739268));
#30916=CARTESIAN_POINT('Ctrl Pts',(4.86082744378178,0.752965186673622,37.0574293176773));
#30917=CARTESIAN_POINT('Ctrl Pts',(4.83496994747732,0.904832194723154,37.0661956407366));
#30918=CARTESIAN_POINT('Ctrl Pts',(4.81952216143642,0.98379959792492,37.0707848609837));
#30919=CARTESIAN_POINT('Ctrl Pts',(4.76503426862988,1.23010096849234,37.0852003531169));
#30920=CARTESIAN_POINT('Ctrl Pts',(4.7191599004821,1.39579000797142,37.0950502339182));
#30921=CARTESIAN_POINT('Ctrl Pts',(4.64518331278746,1.61717379493152,37.1083770337312));
#30922=CARTESIAN_POINT('Ctrl Pts',(4.6245601732874,1.67523802130459,37.1118877803724));
#30923=CARTESIAN_POINT('Ctrl Pts',(4.58977248063143,1.76763953902369,37.1174942274581));
#30924=CARTESIAN_POINT('Ctrl Pts',(4.57630067287657,1.80223005114025,37.1195971051009));
#30925=CARTESIAN_POINT('Ctrl Pts',(4.5396929749308,1.89316680174464,37.1251375950794));
#30926=CARTESIAN_POINT('Ctrl Pts',(4.51589974070905,1.94924152212843,37.12856744341));
#30927=CARTESIAN_POINT('Ctrl Pts',(4.45343689537089,2.08916402458212,37.1371792107406));
#30928=CARTESIAN_POINT('Ctrl Pts',(4.41343635217545,2.17239182678577,37.1423509056104));
#30929=CARTESIAN_POINT('Ctrl Pts',(4.30838920675485,2.37606652267735,37.1551892608679));
#30930=CARTESIAN_POINT('Ctrl Pts',(4.24061337211479,2.49501653053431,37.1628518148848));
#30931=CARTESIAN_POINT('Ctrl Pts',(4.12484860677061,2.67981411048286,37.1751170017326));
#30932=CARTESIAN_POINT('Ctrl Pts',(4.08003299963365,2.74756441308388,37.1796950442693));
#30933=CARTESIAN_POINT('Ctrl Pts',(3.99426859348585,2.87049072220417,37.1881691233165));
#30934=CARTESIAN_POINT('Ctrl Pts',(3.9538016592187,2.92597861923693,37.1920602613161));
#30935=CARTESIAN_POINT('Ctrl Pts',(3.84450798527856,3.06943200279022,37.2023044399441));
#30936=CARTESIAN_POINT('Ctrl Pts',(3.77382427321572,3.15593160804204,37.2086706925013));
#30937=CARTESIAN_POINT('Ctrl Pts',(3.5724346226182,3.38593328248438,37.2261434429111));
#30938=CARTESIAN_POINT('Ctrl Pts',(3.4360836985779,3.52422507944231,37.2372732668762));
#30939=CARTESIAN_POINT('Ctrl Pts',(3.25659611627805,3.68592258255789,37.251040096925));
#30940=CARTESIAN_POINT('Ctrl Pts',(3.22081216307909,3.71723185069398,37.2537439762873));
#30941=CARTESIAN_POINT('Ctrl Pts',(3.15486294948704,3.77326694559638,37.2586509126666));
#30942=CARTESIAN_POINT('Ctrl Pts',(3.12484712788844,3.79816194076146,37.2608560090299));
#30943=CARTESIAN_POINT('Ctrl Pts',(3.01979070371403,3.88320688457817,37.2684835395084));
#30944=CARTESIAN_POINT('Ctrl Pts',(2.94328382915175,3.94151142288682,37.2738820112885));
#30945=CARTESIAN_POINT('Ctrl Pts',(2.68280056517236,4.12820513036423,37.2918494349101));
#30946=CARTESIAN_POINT('Ctrl Pts',(2.49176121249271,4.24624790575298,37.3043788073436));
#30947=CARTESIAN_POINT('Ctrl Pts',(2.23237591464222,4.38297037470432,37.3209148486011));
#30948=CARTESIAN_POINT('Ctrl Pts',(2.17074865777022,4.41381712957403,37.3248093750886));
#30949=CARTESIAN_POINT('Ctrl Pts',(2.03859081144828,4.47652961057704,37.333097849338));
#30950=CARTESIAN_POINT('Ctrl Pts',(1.96791507519602,4.50804613002256,37.3374932572073));
#30951=CARTESIAN_POINT('Ctrl Pts',(1.79802663513586,4.57904793868868,37.3479795050177));
#30952=CARTESIAN_POINT('Ctrl Pts',(1.69821397042713,4.61699564189424,37.354077925755));
#30953=CARTESIAN_POINT('Ctrl Pts',(1.43473985138644,4.70746499598242,37.3700171980796));
#30954=CARTESIAN_POINT('Ctrl Pts',(1.26941980741697,4.75471126598224,37.3798657421152));
#30955=CARTESIAN_POINT('Ctrl Pts',(1.06121854151851,4.802577057846,37.3920251590479));
#30956=CARTESIAN_POINT('Ctrl Pts',(1.02035277231022,4.81142509740532,37.3944000812988));
#30957=CARTESIAN_POINT('Ctrl Pts',(0.94697174834649,4.82633620394941,37.3986416046695));
#30958=CARTESIAN_POINT('Ctrl Pts',(0.914498867274258,4.83259438552585,37.4005106020057));
#30959=CARTESIAN_POINT('Ctrl Pts',(0.878210596228608,4.83920900315252,37.4025917516664));
#30960=CARTESIAN_POINT('Ctrl Pts',(0.874455248824459,4.83988901167726,37.4028070338407));
#30961=CARTESIAN_POINT('Ctrl Pts',(0.869586956238884,4.84076469836626,37.4030860050825));
#30962=CARTESIAN_POINT('Ctrl Pts',(0.868474731580764,4.8409643646712,37.4031497320734));
#30963=CARTESIAN_POINT('Ctrl Pts',(0.865544675632951,4.84148932533259,37.4033175951875));
#30964=CARTESIAN_POINT('Ctrl Pts',(0.863726729452476,4.84181397924985,37.4034217252602));
#30965=CARTESIAN_POINT('Ctrl Pts',(0.858922939870501,4.84266906183712,37.403696828573));
#30966=CARTESIAN_POINT('Ctrl Pts',(0.85593678711114,4.84319775309633,37.4038677856434));
#30967=CARTESIAN_POINT('Ctrl Pts',(0.848022984751394,4.84459132533947,37.4043207102209));
#30968=CARTESIAN_POINT('Ctrl Pts',(0.843094498914097,4.8454514504014,37.4046026345484));
#30969=CARTESIAN_POINT('Ctrl Pts',(0.830025694823135,4.84771169041316,37.4053498396787));
#30970=CARTESIAN_POINT('Ctrl Pts',(0.821883141434145,4.84909882241837,37.4058150074393));
#30971=CARTESIAN_POINT('Ctrl Pts',(0.750782145772908,4.86102706320264,37.4098737126302));
#30972=CARTESIAN_POINT('Ctrl Pts',(0.687627111697836,4.87036210111441,37.4134573467778));
#30973=CARTESIAN_POINT('Ctrl Pts',(0.410350552395102,4.90584579308773,37.4291335294651));
#30974=CARTESIAN_POINT('Ctrl Pts',(0.194825184235147,4.91912114573091,37.4411798229461));
#30975=CARTESIAN_POINT('Ctrl Pts',(-0.0863308533219903,4.91792789965569,
37.4570199485428));
#30976=CARTESIAN_POINT('Ctrl Pts',(-0.151775949126505,4.91634333481699,
37.4607149545633));
#30977=CARTESIAN_POINT('Ctrl Pts',(-0.28141185302162,4.91061356473325,37.4680574544334));
#30978=CARTESIAN_POINT('Ctrl Pts',(-0.345591927526374,4.90651447731638,
37.4717039275781));
#30979=CARTESIAN_POINT('Ctrl Pts',(-0.481291363410916,4.89517178017584,
37.4794431028436));
#30980=CARTESIAN_POINT('Ctrl Pts',(-0.552769702195023,4.88761635646434,
37.4835369425077));
#30981=CARTESIAN_POINT('Ctrl Pts',(-0.750362476975425,4.86234033424924,
37.4949063055543));
#30982=CARTESIAN_POINT('Ctrl Pts',(-0.875992938351217,4.84128427121603,
37.5021956352467));
#30983=CARTESIAN_POINT('Ctrl Pts',(-1.02269996240819,4.81079769069408,37.5107726807931));
#30984=CARTESIAN_POINT('Ctrl Pts',(-1.0447046516616,4.80606718908558,37.5120608451116));
#30985=CARTESIAN_POINT('Ctrl Pts',(-1.16125003399877,4.78017438267656,37.5188919378874));
#30986=CARTESIAN_POINT('Ctrl Pts',(-1.25518340029912,4.75637296168653,37.5244277682988));
#30987=CARTESIAN_POINT('Ctrl Pts',(-1.38256588247471,4.72005935126867,37.5319613306906));
#30988=CARTESIAN_POINT('Ctrl Pts',(-1.4166720689071,4.70993513645557,37.5339809810342));
#30989=CARTESIAN_POINT('Ctrl Pts',(-1.4824835311819,4.68961986585549,37.5378817238552));
#30990=CARTESIAN_POINT('Ctrl Pts',(-1.51420101865333,4.67947509977371,37.5397634152908));
#30991=CARTESIAN_POINT('Ctrl Pts',(-1.55376046307042,4.66637777806139,37.5421141832611));
#30992=CARTESIAN_POINT('Ctrl Pts',(-1.56170098350097,4.66372631944484,37.5425862325198));
#30993=CARTESIAN_POINT('Ctrl Pts',(-1.58063143798559,4.65735138910722,37.5437121253483));
#30994=CARTESIAN_POINT('Ctrl Pts',(-1.59161504915292,4.65360927029664,37.5443657908606));
#30995=CARTESIAN_POINT('Ctrl Pts',(-1.62331845714446,4.64268254069482,37.5462538979492));
#30996=CARTESIAN_POINT('Ctrl Pts',(-1.64400361325797,4.63539816108357,37.5474874786266));
#30997=CARTESIAN_POINT('Ctrl Pts',(-1.7485712537359,4.59778616217263,37.5537337284135));
#30998=CARTESIAN_POINT('Ctrl Pts',(-1.83166676742684,4.56531883323016,37.5587311911084));
#30999=CARTESIAN_POINT('Ctrl Pts',(-2.07849843915366,4.4610514586551,37.5737426081891));
#31000=CARTESIAN_POINT('Ctrl Pts',(-2.23924689646878,4.38256867160318,37.5837484506122));
#31001=CARTESIAN_POINT('Ctrl Pts',(-2.4314788493592,4.27537173817518,37.5961554127492));
#31002=CARTESIAN_POINT('Ctrl Pts',(-2.46733771663527,4.25477819125951,37.5984892666716));
#31003=CARTESIAN_POINT('Ctrl Pts',(-2.56055473744722,4.19966942606904,37.6046101837079));
#31004=CARTESIAN_POINT('Ctrl Pts',(-2.61747508770703,4.16443127988252,37.6084022023059));
#31005=CARTESIAN_POINT('Ctrl Pts',(-2.73070012924449,4.0910974825056,37.6160624784095));
#31006=CARTESIAN_POINT('Ctrl Pts',(-2.78696992643701,4.05297425481835,37.6199301963578));
#31007=CARTESIAN_POINT('Ctrl Pts',(-2.99993253720415,3.90215781347006,37.6348112009915));
#31008=CARTESIAN_POINT('Ctrl Pts',(-3.15073130341971,3.78144444881562,37.6458733125078));
#31009=CARTESIAN_POINT('Ctrl Pts',(-3.34868432918662,3.60290306530415,37.6611123192323));
#31010=CARTESIAN_POINT('Ctrl Pts',(-3.40221167507765,3.55240103849283,37.6653114850938));
#31011=CARTESIAN_POINT('Ctrl Pts',(-3.48185718223459,3.47380505642974,37.6716735291493));
#31012=CARTESIAN_POINT('Ctrl Pts',(-3.50881304296983,3.4465754161021,37.6738473756669));
#31013=CARTESIAN_POINT('Ctrl Pts',(-3.55954048976114,3.3941207449958,37.6779768906759));
#31014=CARTESIAN_POINT('Ctrl Pts',(-3.58336884734312,3.36895412013561,37.6799337687668));
#31015=CARTESIAN_POINT('Ctrl Pts',(-3.64081556853383,3.30698195472023,37.6846972754829));
#31016=CARTESIAN_POINT('Ctrl Pts',(-3.67414430623344,3.26991304636743,37.6875001847029));
#31017=CARTESIAN_POINT('Ctrl Pts',(-3.7844066043997,3.14346246168126,37.6969213208271));
#31018=CARTESIAN_POINT('Ctrl Pts',(-3.85868775066657,3.05182218593411,37.7035196519911));
#31019=CARTESIAN_POINT('Ctrl Pts',(-4.00908140001213,2.85200230180349,37.7175338517272));
#31020=CARTESIAN_POINT('Ctrl Pts',(-4.0842698593523,2.74324441503253,37.7249469077476));
#31021=CARTESIAN_POINT('Ctrl Pts',(-4.19132552979462,2.5742155938858,37.736223374973));
#31022=CARTESIAN_POINT('Ctrl Pts',(-4.22647239041994,2.51609352374469,37.7400589774292));
#31023=CARTESIAN_POINT('Ctrl Pts',(-4.29218162557632,2.40216679832502,37.7475052072134));
#31024=CARTESIAN_POINT('Ctrl Pts',(-4.32288718079736,2.34646004520824,37.7511139419817));
#31025=CARTESIAN_POINT('Ctrl Pts',(-4.38738524844168,2.22388067773893,37.7589901106813));
#31026=CARTESIAN_POINT('Ctrl Pts',(-4.4207476225241,2.15679968694377,37.7632596135832));
#31027=CARTESIAN_POINT('Ctrl Pts',(-4.51409155944719,1.95784171071394,37.775809157908));
#31028=CARTESIAN_POINT('Ctrl Pts',(-4.56979450790952,1.82404621302096,37.7841072297769));
#31029=CARTESIAN_POINT('Ctrl Pts',(-4.63625768489655,1.6421567416116,37.7951858567299));
#31030=CARTESIAN_POINT('Ctrl Pts',(-4.65232188913736,1.59607805567092,37.7979753020625));
#31031=CARTESIAN_POINT('Ctrl Pts',(-4.68623118588717,1.49394769216465,37.8041175372925));
#31032=CARTESIAN_POINT('Ctrl Pts',(-4.70376192678936,1.4377991129602,37.8074679208683));
#31033=CARTESIAN_POINT('Ctrl Pts',(-4.73026274992449,1.34724174591711,37.8128246000106));
#31034=CARTESIAN_POINT('Ctrl Pts',(-4.73987403156545,1.31302711503208,37.814837534469));
#31035=CARTESIAN_POINT('Ctrl Pts',(-4.75420028048348,1.25981963272418,37.817951762854));
#31036=CARTESIAN_POINT('Ctrl Pts',(-4.75917397327971,1.24089842019217,37.8190561662389));
#31037=CARTESIAN_POINT('Ctrl Pts',(-4.76403458711433,1.22194824574464,37.8201594747841));
#31038=CARTESIAN_POINT('Origin',(0.,0.,-3.23514056400928));
#31039=CARTESIAN_POINT('',(-4.76403458699542,1.22194824620825,39.9154303604093));
#31040=CARTESIAN_POINT('',(-4.76374161084644,1.22187275725133,39.5699226582762));
#31041=CARTESIAN_POINT('',(-4.76403458704967,1.22194824599672,-3.23514056400928));
#31042=CARTESIAN_POINT('',(-4.91801823864715,0.000109808377098883,38.2351405640093));
#31043=CARTESIAN_POINT('Ctrl Pts',(-4.76403458699542,1.22194824620825,39.9154303604093));
#31044=CARTESIAN_POINT('Ctrl Pts',(-4.76226888768041,1.22883221419384,39.9150262275596));
#31045=CARTESIAN_POINT('Ctrl Pts',(-4.76048825187975,1.23571241595701,39.9146219985247));
#31046=CARTESIAN_POINT('Ctrl Pts',(-4.72218457861485,1.38240246304848,39.9059967734601));
#31047=CARTESIAN_POINT('Ctrl Pts',(-4.67953286590494,1.52053774692604,39.897739744708));
#31048=CARTESIAN_POINT('Ctrl Pts',(-4.59002992174783,1.77073549763694,39.8825303168297));
#31049=CARTESIAN_POINT('Ctrl Pts',(-4.54499144113064,1.88333001439706,39.8755876860244));
#31050=CARTESIAN_POINT('Ctrl Pts',(-4.4735792175259,2.04433021541214,39.8655386112798));
#31051=CARTESIAN_POINT('Ctrl Pts',(-4.4504807492959,2.09413902234831,39.8624124595704));
#31052=CARTESIAN_POINT('Ctrl Pts',(-4.41049122053387,2.17671964077631,39.8572044089465));
#31053=CARTESIAN_POINT('Ctrl Pts',(-4.39405710892769,2.20970662269982,39.8551176305458));
#31054=CARTESIAN_POINT('Ctrl Pts',(-4.34746112244599,2.30065952462245,39.8493437879833));
#31055=CARTESIAN_POINT('Ctrl Pts',(-4.31651246047074,2.35821389944226,39.8456663074602));
#31056=CARTESIAN_POINT('Ctrl Pts',(-4.23263617040839,2.50700962124998,39.8360713127913));
#31057=CARTESIAN_POINT('Ctrl Pts',(-4.17790430488023,2.59719502856669,39.8301671141549));
#31058=CARTESIAN_POINT('Ctrl Pts',(-4.03730539533373,2.81290933102471,39.8157414122895));
#31059=CARTESIAN_POINT('Ctrl Pts',(-3.94843619728096,2.93634884622942,39.8072212314393));
#31060=CARTESIAN_POINT('Ctrl Pts',(-3.81458497318871,3.10518091172412,39.7950767132423));
#31061=CARTESIAN_POINT('Ctrl Pts',(-3.77421837457664,3.15412152027172,39.7914941862384));
#31062=CARTESIAN_POINT('Ctrl Pts',(-3.68633375761085,3.25656954447343,39.7838533751558));
#31063=CARTESIAN_POINT('Ctrl Pts',(-3.6385718268744,3.30984843640951,39.7797937123147));
#31064=CARTESIAN_POINT('Ctrl Pts',(-3.47989020820409,3.47927219468329,39.7665897396737));
#31065=CARTESIAN_POINT('Ctrl Pts',(-3.36444212654279,3.59103033630064,39.7574101680859));
#31066=CARTESIAN_POINT('Ctrl Pts',(-3.14084163402903,3.78721992620003,39.7403818984161));
#31067=CARTESIAN_POINT('Ctrl Pts',(-3.03422213400287,3.87316635127496,39.7325448809477));
#31068=CARTESIAN_POINT('Ctrl Pts',(-2.89067646817213,3.97930978356815,39.7223833712935));
#31069=CARTESIAN_POINT('Ctrl Pts',(-2.8568837251367,4.00363987308693,39.7200181516101));
#31070=CARTESIAN_POINT('Ctrl Pts',(-2.78829291408903,4.05171320388529,39.7152733676541));
#31071=CARTESIAN_POINT('Ctrl Pts',(-2.75349056108777,4.07544439865203,39.7128941178801));
#31072=CARTESIAN_POINT('Ctrl Pts',(-2.67583738742511,4.12694611427883,39.7076413839367));
#31073=CARTESIAN_POINT('Ctrl Pts',(-2.63285023185272,4.15450233792234,39.7047704438202));
#31074=CARTESIAN_POINT('Ctrl Pts',(-2.48728661874389,4.24464675796873,39.6951564440135));
#31075=CARTESIAN_POINT('Ctrl Pts',(-2.38284728595317,4.30414449687835,39.6884336974947));
#31076=CARTESIAN_POINT('Ctrl Pts',(-2.22069780329699,4.3888066168109,39.6781827033342));
#31077=CARTESIAN_POINT('Ctrl Pts',(-2.16451112073421,4.41678772543179,39.6746636013246));
#31078=CARTESIAN_POINT('Ctrl Pts',(-2.02207063641701,4.48435251633549,39.6658103974578));
#31079=CARTESIAN_POINT('Ctrl Pts',(-1.93517859377164,4.52252923160447,39.6604709322254));
#31080=CARTESIAN_POINT('Ctrl Pts',(-1.78486454346354,4.58344531307038,39.651312632398));
#31081=CARTESIAN_POINT('Ctrl Pts',(-1.72197986770229,4.60743937323632,39.6475041255071));
#31082=CARTESIAN_POINT('Ctrl Pts',(-1.57623715913091,4.65964783215472,39.6387218457337));
#31083=CARTESIAN_POINT('Ctrl Pts',(-1.49307895660277,4.68695599071738,39.6337430714126));
#31084=CARTESIAN_POINT('Ctrl Pts',(-1.30191896994236,4.74412662427354,39.6223622313465));
#31085=CARTESIAN_POINT('Ctrl Pts',(-1.19353615377101,4.77254665449531,39.6159549300532));
#31086=CARTESIAN_POINT('Ctrl Pts',(-0.948977861495143,4.82782202743262,
39.6016024346359));
#31087=CARTESIAN_POINT('Ctrl Pts',(-0.812442962099693,4.85266540797225,
39.5936603580244));
#31088=CARTESIAN_POINT('Ctrl Pts',(-0.63388901456503,4.87740645159984,39.5834004383169));
#31089=CARTESIAN_POINT('Ctrl Pts',(-0.592667121670689,4.88258688764306,
39.5810406143829));
#31090=CARTESIAN_POINT('Ctrl Pts',(-0.50942959525157,4.89197783583892,39.5762956120336));
#31091=CARTESIAN_POINT('Ctrl Pts',(-0.46741541310621,4.89617080441049,39.5739107961787));
#31092=CARTESIAN_POINT('Ctrl Pts',(-0.399000421103954,4.90210988992745,
39.5700396873988));
#31093=CARTESIAN_POINT('Ctrl Pts',(-0.372630573636632,4.90418486342901,
39.5685505700832));
#31094=CARTESIAN_POINT('Ctrl Pts',(-0.193692573615001,4.91681344604834,
39.5584617011572));
#31095=CARTESIAN_POINT('Ctrl Pts',(-0.0407198531436483,4.92045869720686,
39.5499122295538));
#31096=CARTESIAN_POINT('Ctrl Pts',(0.237675233164923,4.91410746627151,39.5343040191604));
#31097=CARTESIAN_POINT('Ctrl Pts',(0.363019134542659,4.90644048785214,39.5272589346098));
#31098=CARTESIAN_POINT('Ctrl Pts',(0.550478308213643,4.88775078511209,39.516637712046));
#31099=CARTESIAN_POINT('Ctrl Pts',(0.612899795705358,4.88031636673526,39.5130870131365));
#31100=CARTESIAN_POINT('Ctrl Pts',(0.746886235170257,4.86174735103065,39.5054283840337));
#31101=CARTESIAN_POINT('Ctrl Pts',(0.81838241311975,4.85022436748832,39.5013186849675));
#31102=CARTESIAN_POINT('Ctrl Pts',(1.03455307575027,4.81046835603453,39.4888133427834));
#31103=CARTESIAN_POINT('Ctrl Pts',(1.17823548646428,4.77730741010397,39.4803902503027));
#31104=CARTESIAN_POINT('Ctrl Pts',(1.46288214905752,4.69798838529512,39.463476323209));
#31105=CARTESIAN_POINT('Ctrl Pts',(1.60368691055606,4.65180696472423,39.4549939643085));
#31106=CARTESIAN_POINT('Ctrl Pts',(1.78052716017062,4.58482130568957,39.4442323166427));
#31107=CARTESIAN_POINT('Ctrl Pts',(1.81867809098722,4.56982203514822,39.4419042139383));
#31108=CARTESIAN_POINT('Ctrl Pts',(1.89631494019438,4.53817239126163,39.4371555767541));
#31109=CARTESIAN_POINT('Ctrl Pts',(1.93577976217076,4.52147937903724,39.4347357018761));
#31110=CARTESIAN_POINT('Ctrl Pts',(1.99980215401641,4.49340700816309,39.4307956115768));
#31111=CARTESIAN_POINT('Ctrl Pts',(2.02449261170527,4.48233698777984,39.4292725625656));
#31112=CARTESIAN_POINT('Ctrl Pts',(2.18948049865964,4.40672296422198,39.4190668725454));
#31113=CARTESIAN_POINT('Ctrl Pts',(2.3267629568682,4.33580521688991,39.410434324733));
#31114=CARTESIAN_POINT('Ctrl Pts',(2.5668034932147,4.19711578312782,39.3948943487093));
#31115=CARTESIAN_POINT('Ctrl Pts',(2.67078647829326,4.13172604706275,39.3880019430391));
#31116=CARTESIAN_POINT('Ctrl Pts',(2.82401233012307,4.02716651299461,39.3775428649606));
#31117=CARTESIAN_POINT('Ctrl Pts',(2.87513116626288,3.99083154684322,39.37400020615));
#31118=CARTESIAN_POINT('Ctrl Pts',(2.98395227579363,3.9103058748551,39.3663350455311));
#31119=CARTESIAN_POINT('Ctrl Pts',(3.04139813112048,3.86579363923212,39.3622106663965));
#31120=CARTESIAN_POINT('Ctrl Pts',(3.15927050713853,3.7702054484251,39.3535757049503));
#31121=CARTESIAN_POINT('Ctrl Pts',(3.21949360144223,3.71891113607392,39.3490644714927));
#31122=CARTESIAN_POINT('Ctrl Pts',(3.409650195705,3.54886541152646,39.334488457462));
#31123=CARTESIAN_POINT('Ctrl Pts',(3.53445486657579,3.42458594224403,39.3243973802742));
#31124=CARTESIAN_POINT('Ctrl Pts',(3.692810595625,3.24899778386449,39.3108989219688));
#31125=CARTESIAN_POINT('Ctrl Pts',(3.73246186029148,3.20336780308052,39.3074550002844));
#31126=CARTESIAN_POINT('Ctrl Pts',(3.79485061794772,3.12884039994491,39.3019361833758));
#31127=CARTESIAN_POINT('Ctrl Pts',(3.81812244439937,3.10039908733556,39.2998544459276));
#31128=CARTESIAN_POINT('Ctrl Pts',(3.87869025885567,3.0246607362004,39.2943733011372));
#31129=CARTESIAN_POINT('Ctrl Pts',(3.91543997479883,2.97693477030682,39.2909814714282));
#31130=CARTESIAN_POINT('Ctrl Pts',(4.03333006413394,2.81787301114302,39.2798537812124));
#31131=CARTESIAN_POINT('Ctrl Pts',(4.11067045099002,2.70380261278462,39.2721493847202));
#31132=CARTESIAN_POINT('Ctrl Pts',(4.21707090008802,2.53173127072188,39.2608112220651));
#31133=CARTESIAN_POINT('Ctrl Pts',(4.2499368429498,2.47616376228464,39.2571913528747));
#31134=CARTESIAN_POINT('Ctrl Pts',(4.32729968765962,2.33928395105995,39.2483601270319));
#31135=CARTESIAN_POINT('Ctrl Pts',(4.37061002448932,2.25733021780282,39.2431440427045));
#31136=CARTESIAN_POINT('Ctrl Pts',(4.44131058089824,2.11387483281484,39.2341118950906));
#31137=CARTESIAN_POINT('Ctrl Pts',(4.46980168289862,2.05294404864993,39.23030529415));
#31138=CARTESIAN_POINT('Ctrl Pts',(4.53318897893135,1.90980461493238,39.2214233167043));
#31139=CARTESIAN_POINT('Ctrl Pts',(4.5671134619615,1.82719192339286,39.216342355559));
#31140=CARTESIAN_POINT('Ctrl Pts',(4.64008957660375,1.63472767797632,39.2045992667209));
#31141=CARTESIAN_POINT('Ctrl Pts',(4.67752242416655,1.52431935826938,39.1979311506441));
#31142=CARTESIAN_POINT('Ctrl Pts',(4.7480649890382,1.28907548577166,39.1838721818453));
#31143=CARTESIAN_POINT('Ctrl Pts',(4.78025306883592,1.16405235565174,39.1764856726978));
#31144=CARTESIAN_POINT('Ctrl Pts',(4.81635666307974,0.996823995008947,39.1667470189971));
#31145=CARTESIAN_POINT('Ctrl Pts',(4.82469940481146,0.955628217649391,39.1643593134903));
#31146=CARTESIAN_POINT('Ctrl Pts',(4.84027022024472,0.873331729859529,39.159614335306));
#31147=CARTESIAN_POINT('Ctrl Pts',(4.84750530856395,0.832235814823772,39.1572571841265));
#31148=CARTESIAN_POINT('Ctrl Pts',(4.8583943874849,0.765416044221063,39.1534403453621));
#31149=CARTESIAN_POINT('Ctrl Pts',(4.86236901657948,0.739746781968841,39.151977840823));
#31150=CARTESIAN_POINT('Ctrl Pts',(4.87177178080422,0.675668144782082,39.1483348516107));
#31151=CARTESIAN_POINT('Ctrl Pts',(4.87694922006158,0.637223707954985,39.1461562542479));
#31152=CARTESIAN_POINT('Ctrl Pts',(4.90074261961795,0.443224534146613,39.1351885635246));
#31153=CARTESIAN_POINT('Ctrl Pts',(4.91237335646857,0.286904716768253,39.1264321642819));
#31154=CARTESIAN_POINT('Ctrl Pts',(4.91923444692432,0.0280134831669276,
39.1118971280989));
#31155=CARTESIAN_POINT('Ctrl Pts',(4.91875260533546,-0.0743285839474307,
39.1061435218152));
#31156=CARTESIAN_POINT('Ctrl Pts',(4.91265210273125,-0.244135101471975,
39.0965527967804));
#31157=CARTESIAN_POINT('Ctrl Pts',(4.9088326281508,-0.31163235419062,39.0927290265234));
#31158=CARTESIAN_POINT('Ctrl Pts',(4.89721435249451,-0.461941857409463,
39.0841801486178));
#31159=CARTESIAN_POINT('Ctrl Pts',(4.88870372793514,-0.544678176938047,
39.0794514827065));
#31160=CARTESIAN_POINT('Ctrl Pts',(4.86514312858313,-0.727934904613118,
39.0689184545321));
#31161=CARTESIAN_POINT('Ctrl Pts',(4.8490669333082,-0.82828527111731,39.0631104686996));
#31162=CARTESIAN_POINT('Ctrl Pts',(4.79892384203584,-1.08924314946118,39.0479025562572));
#31163=CARTESIAN_POINT('Ctrl Pts',(4.75990457932159,-1.2487713559981,39.0384984560371));
#31164=CARTESIAN_POINT('Ctrl Pts',(4.70267666919145,-1.44059527716543,39.027110160454));
#31165=CARTESIAN_POINT('Ctrl Pts',(4.69199120515729,-1.47502582123768,39.0250630311218));
#31166=CARTESIAN_POINT('Ctrl Pts',(4.66811043924559,-1.54908762644346,39.0206545955774));
#31167=CARTESIAN_POINT('Ctrl Pts',(4.65478682240799,-1.58867467987585,39.0182951466843));
#31168=CARTESIAN_POINT('Ctrl Pts',(4.59841808967512,-1.7493571131665,39.0086950858514));
#31169=CARTESIAN_POINT('Ctrl Pts',(4.55113836542247,-1.86891399582052,39.0014969630169));
#31170=CARTESIAN_POINT('Ctrl Pts',(4.43706318923243,-2.12728546348757,38.985674225092));
#31171=CARTESIAN_POINT('Ctrl Pts',(4.36832167212134,-2.26509123902372,38.9770565349013));
#31172=CARTESIAN_POINT('Ctrl Pts',(4.25645034538123,-2.46525814720661,38.9641471208801));
#31173=CARTESIAN_POINT('Ctrl Pts',(4.2181602050814,-2.53021571861341,38.959893604808));
#31174=CARTESIAN_POINT('Ctrl Pts',(4.14171529562556,-2.65333983704687,38.9516944358007));
#31175=CARTESIAN_POINT('Ctrl Pts',(4.10378995201621,-2.7116278807087,38.9477514987004));
#31176=CARTESIAN_POINT('Ctrl Pts',(3.98594082008995,-2.88461402753731,38.9358531950217));
#31177=CARTESIAN_POINT('Ctrl Pts',(3.9023515181653,-2.99672722423762,38.9278724879442));
#31178=CARTESIAN_POINT('Ctrl Pts',(3.70845354506083,-3.23489680078571,38.9102989927824));
#31179=CARTESIAN_POINT('Ctrl Pts',(3.59625046210315,-3.35919161974612,38.9007086726743));
#31180=CARTESIAN_POINT('Ctrl Pts',(3.44831532434259,-3.50714396096354,38.8887991921053));
#31181=CARTESIAN_POINT('Ctrl Pts',(3.41832315609936,-3.5363829251366,38.8864198591102));
#31182=CARTESIAN_POINT('Ctrl Pts',(3.35760974500172,-3.59407747865262,38.8816751540646));
#31183=CARTESIAN_POINT('Ctrl Pts',(3.32689123134357,-3.62253100904149,38.8793099738672));
#31184=CARTESIAN_POINT('Ctrl Pts',(3.19706760101372,-3.73973795681526,38.8694496077892));
#31185=CARTESIAN_POINT('Ctrl Pts',(3.09474474986734,-3.82484469333287,38.8620001711711));
#31186=CARTESIAN_POINT('Ctrl Pts',(2.86161190001133,-4.0032651575686,38.8455537110574));
#31187=CARTESIAN_POINT('Ctrl Pts',(2.72942788170617,-4.09453015973498,38.8365636761315));
#31188=CARTESIAN_POINT('Ctrl Pts',(2.53157276894922,-4.21729196914811,38.8234460624785));
#31189=CARTESIAN_POINT('Ctrl Pts',(2.46929361425007,-4.25405701947805,38.8193635337122));
#31190=CARTESIAN_POINT('Ctrl Pts',(2.34381648906955,-4.32444541097243,38.8112193017649));
#31191=CARTESIAN_POINT('Ctrl Pts',(2.28064983350614,-4.35808903357751,38.8071587994209));
#31192=CARTESIAN_POINT('Ctrl Pts',(2.18127633109587,-4.40826471524024,38.8008265465051));
#31193=CARTESIAN_POINT('Ctrl Pts',(2.14556461847156,-4.42575605697535,38.7985619023984));
#31194=CARTESIAN_POINT('Ctrl Pts',(1.9957484613591,-4.49689543053981,38.789105664532));
#31195=CARTESIAN_POINT('Ctrl Pts',(1.8798152508781,-4.54657834076028,38.7818928878107));
#31196=CARTESIAN_POINT('Ctrl Pts',(1.63997090369856,-4.63861953808499,38.7671867562889));
#31197=CARTESIAN_POINT('Ctrl Pts',(1.51601722892208,-4.68059698128877,38.7596987394821));
#31198=CARTESIAN_POINT('Ctrl Pts',(1.3503280354426,-4.72943490070241,38.749866099238));
#31199=CARTESIAN_POINT('Ctrl Pts',(1.30996894616915,-4.74077226801363,38.7474847502543));
#31200=CARTESIAN_POINT('Ctrl Pts',(1.22905255661804,-4.76239047212999,38.7427400005994));
#31201=CARTESIAN_POINT('Ctrl Pts',(1.18849910264559,-4.77267253568953,38.7403767747798));
#31202=CARTESIAN_POINT('Ctrl Pts',(1.14580002865878,-4.7829206211638,38.7379012040744));
#31203=CARTESIAN_POINT('Ctrl Pts',(1.14378063822835,-4.78340393711924,38.7377841552889));
#31204=CARTESIAN_POINT('Ctrl Pts',(1.13955837206968,-4.78441165733066,38.737539483943));
#31205=CARTESIAN_POINT('Ctrl Pts',(1.13735543891617,-4.78493581939512,38.7374118636207));
#31206=CARTESIAN_POINT('Ctrl Pts',(1.13273759460993,-4.78603121201167,38.7371444151133));
#31207=CARTESIAN_POINT('Ctrl Pts',(1.13032261139427,-4.78660213666986,38.7370045896998));
#31208=CARTESIAN_POINT('Ctrl Pts',(1.12715956771992,-4.78734738256734,38.7368215059007));
#31209=CARTESIAN_POINT('Ctrl Pts',(1.12641189787147,-4.78752335647679,38.7367782330802));
#31210=CARTESIAN_POINT('Ctrl Pts',(1.12470692845255,-4.78792422189296,38.7366795636331));
#31211=CARTESIAN_POINT('Ctrl Pts',(1.12374960255776,-4.78814900146709,38.7366241679812));
#31212=CARTESIAN_POINT('Ctrl Pts',(1.12156137598197,-4.78866210341169,38.7364975608455));
#31213=CARTESIAN_POINT('Ctrl Pts',(1.12033043132739,-4.78895023834961,38.7364263509783));
#31214=CARTESIAN_POINT('Ctrl Pts',(1.06223654430143,-4.80252501455946,38.7330661267533));
#31215=CARTESIAN_POINT('Ctrl Pts',(1.00514122116211,-4.81479845911944,38.7297859349637));
#31216=CARTESIAN_POINT('Ctrl Pts',(0.78050394419513,-4.85891740162198,38.7169419842515));
#31217=CARTESIAN_POINT('Ctrl Pts',(0.611571474909233,-4.88305693549449,
38.7074128759114));
#31218=CARTESIAN_POINT('Ctrl Pts',(0.349264561199292,-4.90671134325719,
38.6926201216086));
#31219=CARTESIAN_POINT('Ctrl Pts',(0.256585154504632,-4.91242971500897,
38.6873950383847));
#31220=CARTESIAN_POINT('Ctrl Pts',(0.098595075308817,-4.91769443130679,
38.6784676655964));
#31221=CARTESIAN_POINT('Ctrl Pts',(0.0333535360516099,-4.91856960186443,
38.6747753858831));
#31222=CARTESIAN_POINT('Ctrl Pts',(-0.109510367245702,-4.91764337860662,
38.666670761035));
#31223=CARTESIAN_POINT('Ctrl Pts',(-0.18711168213534,-4.91530242668106,
38.6622558641897));
#31224=CARTESIAN_POINT('Ctrl Pts',(-0.366305919494645,-4.90564696914728,
38.652025460237));
#31225=CARTESIAN_POINT('Ctrl Pts',(-0.467792071977703,-4.89701159036208,
38.6462046449401));
#31226=CARTESIAN_POINT('Ctrl Pts',(-0.731590117253801,-4.8662895621965,
38.6310052437245));
#31227=CARTESIAN_POINT('Ctrl Pts',(-0.89319775116091,-4.83923514659879,
38.6216226876822));
#31228=CARTESIAN_POINT('Ctrl Pts',(-1.08834251606943,-4.79645611658005,
38.6102572419994));
#31229=CARTESIAN_POINT('Ctrl Pts',(-1.12344427202847,-4.78835605539061,
38.6082116258924));
#31230=CARTESIAN_POINT('Ctrl Pts',(-1.19347508286451,-4.77138332144673,
38.6041294523743));
#31231=CARTESIAN_POINT('Ctrl Pts',(-1.22840197390703,-4.76251091327946,
38.6020930300535));
#31232=CARTESIAN_POINT('Ctrl Pts',(-1.26658014263471,-4.75236465690808,
38.5998646704706));
#31233=CARTESIAN_POINT('Ctrl Pts',(-1.26993091771608,-4.75147035707909,
38.5996690744923));
#31234=CARTESIAN_POINT('Ctrl Pts',(-1.27712730916522,-4.74954153131194,
38.5992489508562));
#31235=CARTESIAN_POINT('Ctrl Pts',(-1.28097262117994,-4.74850587714698,
38.5990244341232));
#31236=CARTESIAN_POINT('Ctrl Pts',(-1.28932319287547,-4.74624594421492,
38.5985368019319));
#31237=CARTESIAN_POINT('Ctrl Pts',(-1.29382797660832,-4.74501991836387,
38.5982737028405));
#31238=CARTESIAN_POINT('Ctrl Pts',(-1.3004400014129,-4.74321026797663,38.5978874649188));
#31239=CARTESIAN_POINT('Ctrl Pts',(-1.30254860740403,-4.74263165013583,
38.5977642818467));
#31240=CARTESIAN_POINT('Ctrl Pts',(-1.30800436124589,-4.74113063600515,
38.5974455343492));
#31241=CARTESIAN_POINT('Ctrl Pts',(-1.31135092042317,-4.74020610102918,
38.5972499885996));
#31242=CARTESIAN_POINT('Ctrl Pts',(-1.32012002824678,-4.73777351207704,
38.5967375211165));
#31243=CARTESIAN_POINT('Ctrl Pts',(-1.32554097458688,-4.73625969151886,
38.5964206482785));
#31244=CARTESIAN_POINT('Ctrl Pts',(-1.39434857854842,-4.71691751268915,
38.5923976148445));
#31245=CARTESIAN_POINT('Ctrl Pts',(-1.45737400449448,-4.6978271463955,38.5887018504978));
#31246=CARTESIAN_POINT('Ctrl Pts',(-1.73102000633406,-4.60890287719874,
38.5725684115556));
#31247=CARTESIAN_POINT('Ctrl Pts',(-1.93715838440445,-4.52612773716528,
38.5601753831499));
#31248=CARTESIAN_POINT('Ctrl Pts',(-2.18812955254942,-4.40505330480025,
38.544465955373));
#31249=CARTESIAN_POINT('Ctrl Pts',(-2.23882669251638,-4.37950459753855,
38.5412600158807));
#31250=CARTESIAN_POINT('Ctrl Pts',(-2.34420031919172,-4.32409386226783,
38.534522467246));
#31251=CARTESIAN_POINT('Ctrl Pts',(-2.39877464489883,-4.29405903118504,
38.5309901082451));
#31252=CARTESIAN_POINT('Ctrl Pts',(-2.51457123515964,-4.2274341413938,38.5233974296439));
#31253=CARTESIAN_POINT('Ctrl Pts',(-2.57559792278348,-4.19053255777091,
38.5193355979906));
#31254=CARTESIAN_POINT('Ctrl Pts',(-2.74226922564166,-4.0847332619287,38.5080686675776));
#31255=CARTESIAN_POINT('Ctrl Pts',(-2.84609889261695,-4.01307950018809,
38.5008500254866));
#31256=CARTESIAN_POINT('Ctrl Pts',(-2.97302490791104,-3.91808089209701,
38.4917750617003));
#31257=CARTESIAN_POINT('Ctrl Pts',(-2.99879790881972,-3.89839019167147,
38.4899188755996));
#31258=CARTESIAN_POINT('Ctrl Pts',(-3.0502715924491,-3.85825151621077,38.4861849763177));
#31259=CARTESIAN_POINT('Ctrl Pts',(-3.07596605150839,-3.83779811999458,
38.4843073764962));
#31260=CARTESIAN_POINT('Ctrl Pts',(-3.14869659537006,-3.77870323698239,
38.4789542433377));
#31261=CARTESIAN_POINT('Ctrl Pts',(-3.1952230868871,-3.73944353396493,38.4754831124882));
#31262=CARTESIAN_POINT('Ctrl Pts',(-3.26922617887872,-3.67460890286862,
38.4698904078534));
#31263=CARTESIAN_POINT('Ctrl Pts',(-3.29715967091668,-3.64956553033259,
38.4677623973218));
#31264=CARTESIAN_POINT('Ctrl Pts',(-3.35992050289029,-3.59198945593125,
38.4629432954941));
#31265=CARTESIAN_POINT('Ctrl Pts',(-3.39456698019871,-3.55926525103117,
38.4602550965803));
#31266=CARTESIAN_POINT('Ctrl Pts',(-3.45282208457417,-3.50261783925194,
38.4556805321384));
#31267=CARTESIAN_POINT('Ctrl Pts',(-3.47667092006059,-3.4789468818189,38.4537916343882));
#31268=CARTESIAN_POINT('Ctrl Pts',(-3.57977881714836,-3.37448883369365,
38.4455485711046));
#31269=CARTESIAN_POINT('Ctrl Pts',(-3.65647876685172,-3.29122386186867,
38.4392149358211));
#31270=CARTESIAN_POINT('Ctrl Pts',(-3.82294254343825,-3.09750324837499,
38.4249035794577));
#31271=CARTESIAN_POINT('Ctrl Pts',(-3.91092205507343,-2.98564968185524,
38.416927298866));
#31272=CARTESIAN_POINT('Ctrl Pts',(-4.03410624633866,-2.81423342762668,
38.405027667454));
#31273=CARTESIAN_POINT('Ctrl Pts',(-4.07310468205173,-2.75748818700039,
38.4011383913222));
#31274=CARTESIAN_POINT('Ctrl Pts',(-4.11685570183872,-2.69087345347245,
38.3966247162756));
#31275=CARTESIAN_POINT('Ctrl Pts',(-4.12278261567562,-2.68178379361217,
38.3960099246217));
#31276=CARTESIAN_POINT('Ctrl Pts',(-4.17064502236606,-2.60784717153851,
38.3910179608201));
#31277=CARTESIAN_POINT('Ctrl Pts',(-4.21107761584773,-2.54204089098516,
38.3866297731041));
#31278=CARTESIAN_POINT('Ctrl Pts',(-4.29562213547851,-2.39688356770791,
38.3770606821016));
#31279=CARTESIAN_POINT('Ctrl Pts',(-4.33912064763474,-2.31720783433195,
38.3718773626993));
#31280=CARTESIAN_POINT('Ctrl Pts',(-4.45407414201297,-2.09204832402128,
38.357416983894));
#31281=CARTESIAN_POINT('Ctrl Pts',(-4.52058115066674,-1.94416795913786,
38.3481284516612));
#31282=CARTESIAN_POINT('Ctrl Pts',(-4.59832478621222,-1.74562616652423,
38.3359701872842));
#31283=CARTESIAN_POINT('Ctrl Pts',(-4.61623803360097,-1.69768903375906,
38.3330581733992));
#31284=CARTESIAN_POINT('Ctrl Pts',(-4.6456379223541,-1.61510459136912,38.3280849867555));
#31285=CARTESIAN_POINT('Ctrl Pts',(-4.65749278056879,-1.58059342382598,
38.3260199867548));
#31286=CARTESIAN_POINT('Ctrl Pts',(-4.69033268897614,-1.48141298564855,
38.3201198589345));
#31287=CARTESIAN_POINT('Ctrl Pts',(-4.71036241766494,-1.41643610183184,
38.3162953629141));
#31288=CARTESIAN_POINT('Ctrl Pts',(-4.78146111828876,-1.16757414712526,
38.3017621176116));
#31289=CARTESIAN_POINT('Ctrl Pts',(-4.82315968132596,-0.981188428389662,
38.2911070746136));
#31290=CARTESIAN_POINT('Ctrl Pts',(-4.8686028279121,-0.702980734757526,
38.2752712097921));
#31291=CARTESIAN_POINT('Ctrl Pts',(-4.88078369307783,-0.612719895725724,
38.2701450987969));
#31292=CARTESIAN_POINT('Ctrl Pts',(-4.89708474214341,-0.46005138977395,
38.2614731311142));
#31293=CARTESIAN_POINT('Ctrl Pts',(-4.90253346691393,-0.397808687289228,
38.2579372395336));
#31294=CARTESIAN_POINT('Ctrl Pts',(-4.91024137641091,-0.285071165663136,
38.2515272870964));
#31295=CARTESIAN_POINT('Ctrl Pts',(-4.91291081207015,-0.234612962061103,
38.248656387333));
#31296=CARTESIAN_POINT('Ctrl Pts',(-4.91710205017738,-0.12273600534833,
38.2422845533916));
#31297=CARTESIAN_POINT('Ctrl Pts',(-4.91825146531259,-0.0613118016263361,
38.2387818971424));
#31298=CARTESIAN_POINT('Ctrl Pts',(-4.91824999859808,0.000117430551467993,
38.2352739421131));
#31299=CARTESIAN_POINT('Ctrl Pts',(-4.76417305830272,1.22198379731345,38.1652023751175));
#31300=CARTESIAN_POINT('Ctrl Pts',(-4.79992959697842,1.08317356408338,38.1733206669997));
#31301=CARTESIAN_POINT('Ctrl Pts',(-4.88511646459839,0.68011126137427,38.1966333966303));
#31302=CARTESIAN_POINT('Ctrl Pts',(-4.91823750901205,0.268450859973121,
38.2199461262609));
#31303=CARTESIAN_POINT('Ctrl Pts',(-4.91801823864715,0.000109808377098883,
38.2351405640093));
#31304=CARTESIAN_POINT('',(-4.91786390629002,-3.8137431901149E-5,37.8898484442262));
#31305=CARTESIAN_POINT('Ctrl Pts',(-4.76403458711433,1.22194824574464,37.8201594747841));
#31306=CARTESIAN_POINT('Ctrl Pts',(-4.77168918472963,1.19210510965708,37.8218969884493));
#31307=CARTESIAN_POINT('Ctrl Pts',(-4.77906333949699,1.16219014635735,37.8236317891998));
#31308=CARTESIAN_POINT('Ctrl Pts',(-4.82722030109097,0.958617240570028,
37.835397210521));
#31309=CARTESIAN_POINT('Ctrl Pts',(-4.85881042990668,0.782920717595789,
37.8453594523882));
#31310=CARTESIAN_POINT('Ctrl Pts',(-4.89436812730833,0.496486354594997,
37.861548849846));
#31311=CARTESIAN_POINT('Ctrl Pts',(-4.90426733166406,0.386651749871982,
37.8677434591192));
#31312=CARTESIAN_POINT('Ctrl Pts',(-4.91315075192891,0.228932496530562,
37.8766552215315));
#31313=CARTESIAN_POINT('Ctrl Pts',(-4.91514075959246,0.181250284693678,
37.8793514780635));
#31314=CARTESIAN_POINT('Ctrl Pts',(-4.91764592424943,0.0890244001506232,
37.8845731483227));
#31315=CARTESIAN_POINT('Ctrl Pts',(-4.91825045937924,0.0444877371853263,
37.8870977200385));
#31316=CARTESIAN_POINT('Ctrl Pts',(-4.91824999973809,-5.07567696672655E-5,
37.8896262308883));
#31317=CARTESIAN_POINT('Ctrl Pts',(-4.91784480820938,-3.75132173967632E-5,
37.8898594359907));
#31318=CARTESIAN_POINT('Ctrl Pts',(-4.91794292181926,-0.368586153414599,
37.9107258822996));
#31319=CARTESIAN_POINT('Ctrl Pts',(-4.78626629645783,-1.55553496917534,
37.9779323271126));
#31320=CARTESIAN_POINT('Ctrl Pts',(-3.84145891917051,-3.39576550157761,
38.0914787704297));
#31321=CARTESIAN_POINT('Ctrl Pts',(-1.74734491989153,-4.82025058480454,
38.2304987659423));
#31322=CARTESIAN_POINT('Ctrl Pts',(0.773133994074016,-5.06855934133029,
38.3695187614548));
#31323=CARTESIAN_POINT('Ctrl Pts',(3.10496257022011,-4.08010262210541,38.5085387569673));
#31324=CARTESIAN_POINT('Ctrl Pts',(4.67915761546661,-2.09607108157144,38.6475587524798));
#31325=CARTESIAN_POINT('Ctrl Pts',(5.11160404839724,0.399417102523584,38.7865787479924));
#31326=CARTESIAN_POINT('Ctrl Pts',(4.29678178286066,2.79744459817457,38.9255987435048));
#31327=CARTESIAN_POINT('Ctrl Pts',(2.43351339920456,4.51287519274255,39.0646187390174));
#31328=CARTESIAN_POINT('Ctrl Pts',(-0.0235500165765371,5.12713129986921,
39.2036387345299));
#31329=CARTESIAN_POINT('Ctrl Pts',(-2.47486705641651,4.49032994583289,39.3426587300424));
#31330=CARTESIAN_POINT('Ctrl Pts',(-4.09737808320941,2.96877998133387,39.4647533712912));
#31331=CARTESIAN_POINT('Ctrl Pts',(-4.63432213820682,1.72499203924927,39.5405080140358));
#31332=CARTESIAN_POINT('Ctrl Pts',(-4.76374161084644,1.22187275725133,39.5699226582762));
#31333=CARTESIAN_POINT('Origin',(0.,0.,-3.23514056400928));
#31334=CARTESIAN_POINT('',(-4.76403458703735,1.22194824604475,41.6649672278726));
#31335=CARTESIAN_POINT('',(-4.76403458753695,1.22194824409695,41.3199466556564));
#31336=CARTESIAN_POINT('',(-4.76403458704967,1.22194824599672,-3.23514056400928));
#31337=CARTESIAN_POINT('Ctrl Pts',(-4.76403458703735,1.22194824604475,41.6649672278726));
#31338=CARTESIAN_POINT('Ctrl Pts',(-4.76127012557744,1.23272610840693,41.6643359433539));
#31339=CARTESIAN_POINT('Ctrl Pts',(-4.75846907609556,1.2434946412027,41.6637050875201));
#31340=CARTESIAN_POINT('Ctrl Pts',(-4.74504793833352,1.29438226263213,41.6607234763439));
#31341=CARTESIAN_POINT('Ctrl Pts',(-4.73395682140785,1.33437560005354,41.658378907746));
#31342=CARTESIAN_POINT('Ctrl Pts',(-4.67508088305431,1.53669590136459,41.6464987161115));
#31343=CARTESIAN_POINT('Ctrl Pts',(-4.61944724187694,1.69662136101325,41.6370405664665));
#31344=CARTESIAN_POINT('Ctrl Pts',(-4.51357840235773,1.95685364602639,41.6212973888434));
#31345=CARTESIAN_POINT('Ctrl Pts',(-4.4679615957932,2.05887955640786,41.6150315473424));
#31346=CARTESIAN_POINT('Ctrl Pts',(-4.39098051602284,2.21642060072307,41.6051614540538));
#31347=CARTESIAN_POINT('Ctrl Pts',(-4.36194457291228,2.27303093021728,41.6015740438707));
#31348=CARTESIAN_POINT('Ctrl Pts',(-4.30107521832979,2.38624176509895,41.5943090217789));
#31349=CARTESIAN_POINT('Ctrl Pts',(-4.26920264831027,2.44280707843993,41.5906317800841));
#31350=CARTESIAN_POINT('Ctrl Pts',(-4.18718885180447,2.58184941225385,41.5814668750217));
#31351=CARTESIAN_POINT('Ctrl Pts',(-4.13572222172027,2.66351238507201,41.5759705967678));
#31352=CARTESIAN_POINT('Ctrl Pts',(-3.99093908488945,2.87891797954815,41.5611512126468));
#31353=CARTESIAN_POINT('Ctrl Pts',(-3.8933195210266,3.00962227236982,41.5518084117889));
#31354=CARTESIAN_POINT('Ctrl Pts',(-3.74360396144366,3.19057538634981,41.5383803318057));
#31355=CARTESIAN_POINT('Ctrl Pts',(-3.69661045832224,3.24490573029522,41.5342800811727));
#31356=CARTESIAN_POINT('Ctrl Pts',(-3.6261955408353,3.32279846319194,41.5283064202999));
#31357=CARTESIAN_POINT('Ctrl Pts',(-3.60369888278384,3.34718360963317,41.5264221623577));
#31358=CARTESIAN_POINT('Ctrl Pts',(-3.5534321376645,3.40057575898001,41.5222662582524));
#31359=CARTESIAN_POINT('Ctrl Pts',(-3.52555012892606,3.42947397930547,41.5199968785908));
#31360=CARTESIAN_POINT('Ctrl Pts',(-3.43486186490294,3.52119262246206,41.5127219175477));
#31361=CARTESIAN_POINT('Ctrl Pts',(-3.3707062478194,3.58265449201192,41.5077350954234));
#31362=CARTESIAN_POINT('Ctrl Pts',(-3.19853901279424,3.73887225268478,41.4947001992828));
#31363=CARTESIAN_POINT('Ctrl Pts',(-3.08797963509335,3.83069174281939,41.4866669955951));
#31364=CARTESIAN_POINT('Ctrl Pts',(-2.914308013696,3.96251504192322,41.4744266560372));
#31365=CARTESIAN_POINT('Ctrl Pts',(-2.85404320278021,4.00613952749576,41.4702442694101));
#31366=CARTESIAN_POINT('Ctrl Pts',(-2.74097827088411,4.08413842010144,41.462501859737));
#31367=CARTESIAN_POINT('Ctrl Pts',(-2.68846237352837,4.11889772584592,41.4589455778651));
#31368=CARTESIAN_POINT('Ctrl Pts',(-2.57813592491649,4.18891166886341,41.4515492150936));
#31369=CARTESIAN_POINT('Ctrl Pts',(-2.52023558181634,4.22400027151912,41.4477086358015));
#31370=CARTESIAN_POINT('Ctrl Pts',(-2.27203187227084,4.36749547096227,41.4314054757767));
#31371=CARTESIAN_POINT('Ctrl Pts',(-2.07532605824382,4.4643213175208,41.4188642024773));
#31372=CARTESIAN_POINT('Ctrl Pts',(-1.80154390889707,4.57706955416008,41.4019256048073));
#31373=CARTESIAN_POINT('Ctrl Pts',(-1.72957954469765,4.60474547902596,41.3975207409046));
#31374=CARTESIAN_POINT('Ctrl Pts',(-1.64205675192484,4.63606345670309,41.3922268003096));
#31375=CARTESIAN_POINT('Ctrl Pts',(-1.62709372730172,4.64133609601798,41.3913239502535));
#31376=CARTESIAN_POINT('Ctrl Pts',(-1.58083908428008,4.65738404150837,41.3885399932151));
#31377=CARTESIAN_POINT('Ctrl Pts',(-1.5494638195863,4.66791604738023,41.3866614306249));
#31378=CARTESIAN_POINT('Ctrl Pts',(-1.47705507728195,4.69141161654292,41.382349908059));
#31379=CARTESIAN_POINT('Ctrl Pts',(-1.4359528809273,4.70415497607896,41.379919843149));
#31380=CARTESIAN_POINT('Ctrl Pts',(-1.19522586104527,4.77534109809547,41.3657717301727));
#31381=CARTESIAN_POINT('Ctrl Pts',(-0.992220497007273,4.82161256708251,
41.3541679785016));
#31382=CARTESIAN_POINT('Ctrl Pts',(-0.708083399112774,4.86766631645762,
41.3380193845171));
#31383=CARTESIAN_POINT('Ctrl Pts',(-0.628973195036945,4.87851924570152,
41.333534174749));
#31384=CARTESIAN_POINT('Ctrl Pts',(-0.48712049490661,4.89447178982773,41.3254937797367));
#31385=CARTESIAN_POINT('Ctrl Pts',(-0.424477867849351,4.90030192070997,
41.3219438746532));
#31386=CARTESIAN_POINT('Ctrl Pts',(-0.294555258300993,4.90988378166817,
41.3145755311625));
#31387=CARTESIAN_POINT('Ctrl Pts',(-0.22727524051386,4.91345778250953,41.3107566670574));
#31388=CARTESIAN_POINT('Ctrl Pts',(-0.0477222785081193,4.91930001104523,
41.3005488390981));
#31389=CARTESIAN_POINT('Ctrl Pts',(0.0645899568266395,4.91910740345627,
41.294146191484));
#31390=CARTESIAN_POINT('Ctrl Pts',(0.318021825071502,4.90999142257998,41.2796492933961));
#31391=CARTESIAN_POINT('Ctrl Pts',(0.458963024904282,4.89882705562738,41.2715516604399));
#31392=CARTESIAN_POINT('Ctrl Pts',(0.646351159819651,4.87582478765226,41.260760374117));
#31393=CARTESIAN_POINT('Ctrl Pts',(0.693389027364387,4.86935815922265,41.2580496634431));
#31394=CARTESIAN_POINT('Ctrl Pts',(0.75509310129909,4.85996302360793,41.254492996489));
#31395=CARTESIAN_POINT('Ctrl Pts',(0.769849820403595,4.8576473151558,41.2536423531267));
#31396=CARTESIAN_POINT('Ctrl Pts',(0.790498206432284,4.85431059949587,41.2524520767375));
#31397=CARTESIAN_POINT('Ctrl Pts',(0.796398882350495,4.85334602424806,41.2521119310035));
#31398=CARTESIAN_POINT('Ctrl Pts',(0.834542189679698,4.84703935620124,41.2499131646396));
#31399=CARTESIAN_POINT('Ctrl Pts',(0.866732850906196,4.8413867206099,41.2480575914216));
#31400=CARTESIAN_POINT('Ctrl Pts',(0.939772114062169,4.82780930199566,41.2438487777712));
#31401=CARTESIAN_POINT('Ctrl Pts',(0.980581426389653,4.81968613089237,41.241498221529));
#31402=CARTESIAN_POINT('Ctrl Pts',(1.15576708138316,4.78249793214748,41.2314012733404));
#31403=CARTESIAN_POINT('Ctrl Pts',(1.28899648590461,4.74832316799393,41.2237043983724));
#31404=CARTESIAN_POINT('Ctrl Pts',(1.57361139306861,4.66245291709921,41.207049933443));
#31405=CARTESIAN_POINT('Ctrl Pts',(1.72426065722136,4.60886584550659,41.1980993591963));
#31406=CARTESIAN_POINT('Ctrl Pts',(1.93824741008034,4.5207861376355,41.1850604484116));
#31407=CARTESIAN_POINT('Ctrl Pts',(2.00385879921705,4.49208861025668,41.181017136032));
#31408=CARTESIAN_POINT('Ctrl Pts',(2.13437915203234,4.43157203681371,41.1728718296125));
#31409=CARTESIAN_POINT('Ctrl Pts',(2.19926015001516,4.39973405004222,41.1687706267095));
#31410=CARTESIAN_POINT('Ctrl Pts',(2.40670357795528,4.29220330295604,41.1554771674057));
#31411=CARTESIAN_POINT('Ctrl Pts',(2.54624714685475,4.21092099440199,41.1462496963559));
#31412=CARTESIAN_POINT('Ctrl Pts',(2.76021925332452,4.07175414611854,41.1316381030135));
#31413=CARTESIAN_POINT('Ctrl Pts',(2.83741793384337,4.01833942818293,41.1262653315481));
#31414=CARTESIAN_POINT('Ctrl Pts',(2.9624680785184,3.9264142851043,41.1174042451881));
#31415=CARTESIAN_POINT('Ctrl Pts',(3.01121138725378,3.88915831070677,41.1139087209731));
#31416=CARTESIAN_POINT('Ctrl Pts',(3.08802281659371,3.82813909206122,41.108338165352));
#31417=CARTESIAN_POINT('Ctrl Pts',(3.11654315697061,3.80495632252344,41.1062559742967));
#31418=CARTESIAN_POINT('Ctrl Pts',(3.19044983606742,3.74349273800337,41.1008226890684));
#31419=CARTESIAN_POINT('Ctrl Pts',(3.23540757819331,3.70470592141908,41.0974788414106));
#31420=CARTESIAN_POINT('Ctrl Pts',(3.4037301011422,3.55408596325554,41.0847825342693));
#31421=CARTESIAN_POINT('Ctrl Pts',(3.52209022323534,3.43682799440656,41.0754798461348));
#31422=CARTESIAN_POINT('Ctrl Pts',(3.71128779954039,3.22933280322472,41.059731337927));
#31423=CARTESIAN_POINT('Ctrl Pts',(3.7853316133196,3.1422144405286,41.0533100279584));
#31424=CARTESIAN_POINT('Ctrl Pts',(3.89864898287532,2.99906331369223,41.0430098556726));
#31425=CARTESIAN_POINT('Ctrl Pts',(3.9399058912837,2.94465381343115,41.0391496909832));
#31426=CARTESIAN_POINT('Ctrl Pts',(4.02648296510146,2.82539799668982,41.0307968407793));
#31427=CARTESIAN_POINT('Ctrl Pts',(4.07139838603363,2.76028148596165,41.0263020120701));
#31428=CARTESIAN_POINT('Ctrl Pts',(4.19225613370118,2.57569507955791,41.0137319866517));
#31429=CARTESIAN_POINT('Ctrl Pts',(4.26464014440258,2.45398866927749,41.0056361057063));
#31430=CARTESIAN_POINT('Ctrl Pts',(4.39300520140962,2.21527832575622,40.9901206837461));
#31431=CARTESIAN_POINT('Ctrl Pts',(4.44980870248769,2.09884630724671,40.9827085399044));
#31432=CARTESIAN_POINT('Ctrl Pts',(4.51877714079427,1.94205625501779,40.9729586557662));
#31433=CARTESIAN_POINT('Ctrl Pts',(4.535115022309,1.90359164067747,40.9705848043272));
#31434=CARTESIAN_POINT('Ctrl Pts',(4.56462476294707,1.83157919888971,40.9661761248724));
#31435=CARTESIAN_POINT('Ctrl Pts',(4.57792191807458,1.79808579765527,40.9641397503168));
#31436=CARTESIAN_POINT('Ctrl Pts',(4.64967272521397,1.61140022607851,40.9528582216726));
#31437=CARTESIAN_POINT('Ctrl Pts',(4.70080603863717,1.45550370805503,40.9436896444015));
#31438=CARTESIAN_POINT('Ctrl Pts',(4.77088618060545,1.19923829566586,40.9288041962419));
#31439=CARTESIAN_POINT('Ctrl Pts',(4.79466491796991,1.10032519941727,40.9231030361316));
#31440=CARTESIAN_POINT('Ctrl Pts',(4.83228980989685,0.919282989847636,40.9127060638676));
#31441=CARTESIAN_POINT('Ctrl Pts',(4.84714979631333,0.837403516293261,40.9080178496487));
#31442=CARTESIAN_POINT('Ctrl Pts',(4.87030432989658,0.688395029301021,40.8994949259284));
#31443=CARTESIAN_POINT('Ctrl Pts',(4.87930509953652,0.621396485327472,40.8956660709592));
#31444=CARTESIAN_POINT('Ctrl Pts',(4.89844165093083,0.452661270867243,40.8860234273353));
#31445=CARTESIAN_POINT('Ctrl Pts',(4.90679156300431,0.35075487925224,40.8801997175755));
#31446=CARTESIAN_POINT('Ctrl Pts',(4.91988711428797,0.0920726518648833,
40.8654051299495));
#31447=CARTESIAN_POINT('Ctrl Pts',(4.92032176764996,-0.0648074796190918,
40.8564201614287));
#31448=CARTESIAN_POINT('Ctrl Pts',(4.91151532301408,-0.260203900777127,
40.8452378296772));
#31449=CARTESIAN_POINT('Ctrl Pts',(4.9093094790622,-0.298946982803085,40.8430212267564));
#31450=CARTESIAN_POINT('Ctrl Pts',(4.90486167097758,-0.363579498427921,
40.8393255995916));
#31451=CARTESIAN_POINT('Ctrl Pts',(4.90287261503604,-0.389484522573766,
40.837844964514));
#31452=CARTESIAN_POINT('Ctrl Pts',(4.89715386951535,-0.456955821325617,
40.8339907258432));
#31453=CARTESIAN_POINT('Ctrl Pts',(4.89310020846959,-0.498492777046296,
40.8316201046153));
#31454=CARTESIAN_POINT('Ctrl Pts',(4.88455800569197,-0.575827538727203,
40.8272125631839));
#31455=CARTESIAN_POINT('Ctrl Pts',(4.88020329122169,-0.611637259458739,
40.8251741172176));
#31456=CARTESIAN_POINT('Ctrl Pts',(4.85382436935202,-0.810293466766594,
40.8138701301806));
#31457=CARTESIAN_POINT('Ctrl Pts',(4.82404304726574,-0.972006434915165,
40.8046814331215));
#31458=CARTESIAN_POINT('Ctrl Pts',(4.76286889319268,-1.23067442687123,40.7897887058167));
#31459=CARTESIAN_POINT('Ctrl Pts',(4.73646500303619,-1.32867554207821,40.7841006304361));
#31460=CARTESIAN_POINT('Ctrl Pts',(4.68295779333109,-1.50532231612577,40.7737225104314));
#31461=CARTESIAN_POINT('Ctrl Pts',(4.65685509938529,-1.58423146298085,40.7690400081237));
#31462=CARTESIAN_POINT('Ctrl Pts',(4.60591444700487,-1.7260665128362,40.7605221570072));
#31463=CARTESIAN_POINT('Ctrl Pts',(4.58175369392048,-1.78921392019121,40.7566926237168));
#31464=CARTESIAN_POINT('Ctrl Pts',(4.51772548402142,-1.94674980259616,40.7470366110536));
#31465=CARTESIAN_POINT('Ctrl Pts',(4.47619631815472,-2.04042751803428,40.7412001331203));
#31466=CARTESIAN_POINT('Ctrl Pts',(4.3639116619959,-2.27375192740842,40.726409692148));
#31467=CARTESIAN_POINT('Ctrl Pts',(4.28935928111048,-2.41144552078567,40.7174418803514));
#31468=CARTESIAN_POINT('Ctrl Pts',(4.18830501496816,-2.5785242576005,40.7062786111037));
#31469=CARTESIAN_POINT('Ctrl Pts',(4.16784819878627,-2.61146082850883,40.7040639264697));
#31470=CARTESIAN_POINT('Ctrl Pts',(4.13304389542213,-2.66604678875744,40.7003710345483));
#31471=CARTESIAN_POINT('Ctrl Pts',(4.11891055103188,-2.687830575652,40.6988912189603));
#31472=CARTESIAN_POINT('Ctrl Pts',(4.08162285119034,-2.74431745765307,40.6950386506098));
#31473=CARTESIAN_POINT('Ctrl Pts',(4.05819816463289,-2.77883988724328,40.6926688797651));
#31474=CARTESIAN_POINT('Ctrl Pts',(4.01029230312024,-2.84754384696619,40.6879241974873));
#31475=CARTESIAN_POINT('Ctrl Pts',(3.98580635563148,-2.88171790208906,40.6855495605213));
#31476=CARTESIAN_POINT('Ctrl Pts',(3.88445472840469,-3.01940678943945,40.6759114796982));
#31477=CARTESIAN_POINT('Ctrl Pts',(3.80397018577044,-3.12019509478082,40.6686905226161));
#31478=CARTESIAN_POINT('Ctrl Pts',(3.64333477628409,-3.30588716271997,40.6549352870396));
#31479=CARTESIAN_POINT('Ctrl Pts',(3.56394043146482,-3.39132814704771,40.6484059320886));
#31480=CARTESIAN_POINT('Ctrl Pts',(3.41850245671627,-3.53708928199259,40.6368366085084));
#31481=CARTESIAN_POINT('Ctrl Pts',(3.35370985647061,-3.59858160481833,40.6318080748863));
#31482=CARTESIAN_POINT('Ctrl Pts',(3.23725330713151,-3.70322797967979,40.6229638174593));
#31483=CARTESIAN_POINT('Ctrl Pts',(3.18631069491693,-3.74714964550685,40.6191562630126));
#31484=CARTESIAN_POINT('Ctrl Pts',(3.063085191658,-3.84906180221732,40.6100813325401));
#31485=CARTESIAN_POINT('Ctrl Pts',(2.99003293003017,-3.90608120891154,40.6048072677707));
#31486=CARTESIAN_POINT('Ctrl Pts',(2.86339029042916,-3.99929391888486,40.5958329208454));
#31487=CARTESIAN_POINT('Ctrl Pts',(2.81061698608563,-4.03655644016261,40.5921406362612));
#31488=CARTESIAN_POINT('Ctrl Pts',(2.64304214184509,-4.14999889126037,40.5805631747692));
#31489=CARTESIAN_POINT('Ctrl Pts',(2.52576417070549,-4.22240193500484,40.5726694856033));
#31490=CARTESIAN_POINT('Ctrl Pts',(2.35307115826591,-4.31924372768505,40.5613666374717));
#31491=CARTESIAN_POINT('Ctrl Pts',(2.30000368458892,-4.34773428701329,40.5579352840458));
#31492=CARTESIAN_POINT('Ctrl Pts',(2.21373536687171,-4.39202791280347,40.552429001109));
#31493=CARTESIAN_POINT('Ctrl Pts',(2.18085766640212,-4.40844568303518,40.5503473066003));
#31494=CARTESIAN_POINT('Ctrl Pts',(2.09341828856982,-4.45089170928469,40.5448538701359));
#31495=CARTESIAN_POINT('Ctrl Pts',(2.03855540942028,-4.47628519111695,40.5414497905662));
#31496=CARTESIAN_POINT('Ctrl Pts',(1.82218346700338,-4.57163052739899,40.5281607523585));
#31497=CARTESIAN_POINT('Ctrl Pts',(1.6574350816683,-4.63390416202332,40.5183307120094));
#31498=CARTESIAN_POINT('Ctrl Pts',(1.41432341579592,-4.71117060158908,40.5040183218915));
#31499=CARTESIAN_POINT('Ctrl Pts',(1.33837699845439,-4.73330603453515,40.4995744753822));
#31500=CARTESIAN_POINT('Ctrl Pts',(1.19169855837149,-4.77224451623979,40.4910257248124));
#31501=CARTESIAN_POINT('Ctrl Pts',(1.12106277791577,-4.78932993890191,40.48692372207));
#31502=CARTESIAN_POINT('Ctrl Pts',(0.988809572068376,-4.81823322542175,
40.4792610537538));
#31503=CARTESIAN_POINT('Ctrl Pts',(0.927294127842371,-4.830449386652,40.4757039259542));
#31504=CARTESIAN_POINT('Ctrl Pts',(0.744683672134529,-4.86309654144218,
40.4651587298516));
#31505=CARTESIAN_POINT('Ctrl Pts',(0.623039361243161,-4.88017244297477,
40.4581515322236));
#31506=CARTESIAN_POINT('Ctrl Pts',(0.347257412911509,-4.90840546064777,
40.4422951712435));
#31507=CARTESIAN_POINT('Ctrl Pts',(0.192973982276927,-4.91688856340486,
40.4334441485654));
#31508=CARTESIAN_POINT('Ctrl Pts',(0.0114908346716353,-4.91831100326869,
40.423088420495));
#31509=CARTESIAN_POINT('Ctrl Pts',(-0.0155670981207993,-4.91829979159156,
40.4215459996912));
#31510=CARTESIAN_POINT('Ctrl Pts',(-0.0854693359728234,-4.91769396625693,
40.4175659650834));
#31511=CARTESIAN_POINT('Ctrl Pts',(-0.128308678464229,-4.9167627452191,
40.4151313662233));
#31512=CARTESIAN_POINT('Ctrl Pts',(-0.21209805116757,-4.91384552448128,
40.410380877063));
#31513=CARTESIAN_POINT('Ctrl Pts',(-0.253046257479163,-4.91190706934958,
40.4080647256208));
#31514=CARTESIAN_POINT('Ctrl Pts',(-0.441802045227604,-4.90060485653567,
40.3974019782434));
#31515=CARTESIAN_POINT('Ctrl Pts',(-0.589164823893292,-4.8850796126689,
40.3891145210953));
#31516=CARTESIAN_POINT('Ctrl Pts',(-0.881335476444615,-4.84088366236685,
40.3725600806903));
#31517=CARTESIAN_POINT('Ctrl Pts',(-1.02600154734095,-4.81229955324352,
40.3643014367101));
#31518=CARTESIAN_POINT('Ctrl Pts',(-1.23949923693228,-4.76004916349649,
40.3519191590435));
#31519=CARTESIAN_POINT('Ctrl Pts',(-1.30944507470617,-4.74128461852585,
40.3478312085033));
#31520=CARTESIAN_POINT('Ctrl Pts',(-1.43928653541154,-4.70335926244195,
40.3401742294546));
#31521=CARTESIAN_POINT('Ctrl Pts',(-1.49927869188953,-4.6845808113581,40.3366086255711));
#31522=CARTESIAN_POINT('Ctrl Pts',(-1.68223966891118,-4.62343661130429,
40.3256420127992));
#31523=CARTESIAN_POINT('Ctrl Pts',(-1.80390042499715,-4.57733972253791,
40.3182186702065));
#31524=CARTESIAN_POINT('Ctrl Pts',(-2.03670624979136,-4.47840561511,40.3037471662076));
#31525=CARTESIAN_POINT('Ctrl Pts',(-2.14798127852132,-4.4261118041256,40.2967060105874));
#31526=CARTESIAN_POINT('Ctrl Pts',(-2.3198982158494,-4.33730773823601,40.2856495087172));
#31527=CARTESIAN_POINT('Ctrl Pts',(-2.38191182290566,-4.30356391780155,
40.28162349304));
#31528=CARTESIAN_POINT('Ctrl Pts',(-2.47538609803914,-4.25006163907513,
40.2755040224618));
#31529=CARTESIAN_POINT('Ctrl Pts',(-2.50738462099791,-4.23126254031497,
40.2734000766671));
#31530=CARTESIAN_POINT('Ctrl Pts',(-2.58375524397054,-4.18522429557003,
40.2683567975792));
#31531=CARTESIAN_POINT('Ctrl Pts',(-2.62791354361724,-4.15763924155213,
40.2654219260389));
#31532=CARTESIAN_POINT('Ctrl Pts',(-2.80866745312201,-4.04069447324324,
40.2533099295796));
#31533=CARTESIAN_POINT('Ctrl Pts',(-2.94121125220358,-3.94526321342507,
40.244188384022));
#31534=CARTESIAN_POINT('Ctrl Pts',(-3.13841208648988,-3.78780883130564,
40.2300419995351));
#31535=CARTESIAN_POINT('Ctrl Pts',(-3.20653417846862,-3.73031694925138,
40.2250406554286));
#31536=CARTESIAN_POINT('Ctrl Pts',(-3.33088507147023,-3.61944613791084,
40.2156651433138));
#31537=CARTESIAN_POINT('Ctrl Pts',(-3.38748718848314,-3.56652717127812,
40.2112958065381));
#31538=CARTESIAN_POINT('Ctrl Pts',(-3.49133606069609,-3.46473258874863,
40.2030712723929));
#31539=CARTESIAN_POINT('Ctrl Pts',(-3.5388658321118,-3.41617152450963,40.1992198807745));
#31540=CARTESIAN_POINT('Ctrl Pts',(-3.66769395098982,-3.27897338735749,
40.1885260062558));
#31541=CARTESIAN_POINT('Ctrl Pts',(-3.74676990167051,-3.18831618374307,
40.1816666469326));
#31542=CARTESIAN_POINT('Ctrl Pts',(-3.90763839537789,-2.9896280456453,40.1670484457888));
#31543=CARTESIAN_POINT('Ctrl Pts',(-3.98845277301097,-2.88093008319467,
40.1592908320748));
#31544=CARTESIAN_POINT('Ctrl Pts',(-4.09485606079001,-2.72474030229458,
40.1484894546837));
#31545=CARTESIAN_POINT('Ctrl Pts',(-4.12430681336699,-2.67995321797789,
40.1454301402173));
#31546=CARTESIAN_POINT('Ctrl Pts',(-4.17631587965217,-2.59797226531116,
40.1399017194316));
#31547=CARTESIAN_POINT('Ctrl Pts',(-4.19912409790724,-2.56094339783189,
40.1374303969522));
#31548=CARTESIAN_POINT('Ctrl Pts',(-4.24221522708388,-2.48886171012647,
40.1326714156966));
#31549=CARTESIAN_POINT('Ctrl Pts',(-4.26256219317296,-2.45385130643173,
40.1303832079428));
#31550=CARTESIAN_POINT('Ctrl Pts',(-4.34292643774065,-2.31155461747833,
40.1211667494932));
#31551=CARTESIAN_POINT('Ctrl Pts',(-4.39934459991836,-2.20228575645318,
40.114278357886));
#31552=CARTESIAN_POINT('Ctrl Pts',(-4.49040945495615,-2.00841587798372,
40.1022778635949));
#31553=CARTESIAN_POINT('Ctrl Pts',(-4.52690234577645,-1.92475102358778,
40.0971679709301));
#31554=CARTESIAN_POINT('Ctrl Pts',(-4.59096954896794,-1.76594967120052,
40.0875613691223));
#31555=CARTESIAN_POINT('Ctrl Pts',(-4.61907900418149,-1.69106139324119,
40.0830684497223));
#31556=CARTESIAN_POINT('Ctrl Pts',(-4.66935764089449,-1.54648773988445,
40.074446902422));
#31557=CARTESIAN_POINT('Ctrl Pts',(-4.69182361231053,-1.47692793855491,
40.0703213378629));
#31558=CARTESIAN_POINT('Ctrl Pts',(-4.73060568485256,-1.34701801958561,
40.06264798708));
#31559=CARTESIAN_POINT('Ctrl Pts',(-4.74733761229574,-1.28680735883147,
40.0591039239372));
#31560=CARTESIAN_POINT('Ctrl Pts',(-4.79278337010759,-1.11029643957127,
40.0487438184267));
#31561=CARTESIAN_POINT('Ctrl Pts',(-4.81840120607102,-0.993247122121397,
40.0419098369365));
#31562=CARTESIAN_POINT('Ctrl Pts',(-4.86322047056684,-0.745454737457813,
40.0275087980453));
#31563=CARTESIAN_POINT('Ctrl Pts',(-4.88147926804105,-0.614635079622523,
40.019943777298));
#31564=CARTESIAN_POINT('Ctrl Pts',(-4.90162769916389,-0.410563376290089,
40.0082243532188));
#31565=CARTESIAN_POINT('Ctrl Pts',(-4.90718363383326,-0.337735641736515,
40.0040583875519));
#31566=CARTESIAN_POINT('Ctrl Pts',(-4.91312187312776,-0.227606454765455,
39.9977912084183));
#31567=CARTESIAN_POINT('Ctrl Pts',(-4.9147051369929,-0.190380433108299,
39.9956785946174));
#31568=CARTESIAN_POINT('Ctrl Pts',(-4.91745419764362,-0.102134038920577,
39.9906847619314));
#31569=CARTESIAN_POINT('Ctrl Pts',(-4.91824921726208,-0.0511064683498441,
39.9878076141425));
#31570=CARTESIAN_POINT('Ctrl Pts',(-4.91825229998802,0.150019757647768,
39.9764904476838));
#31571=CARTESIAN_POINT('Ctrl Pts',(-4.91138369861575,0.300037440534878,
39.9680977432507));
#31572=CARTESIAN_POINT('Ctrl Pts',(-4.88625459014518,0.573835310482956,
39.9526896390735));
#31573=CARTESIAN_POINT('Ctrl Pts',(-4.87011380743797,0.697683223990364,
39.9456861149759));
#31574=CARTESIAN_POINT('Ctrl Pts',(-4.83731210447299,0.891479717866304,
39.9346113163893));
#31575=CARTESIAN_POINT('Ctrl Pts',(-4.82380129474772,0.961907166196714,
39.9305625354046));
#31576=CARTESIAN_POINT('Ctrl Pts',(-4.79510592311643,1.0956157219789,39.9228201984772));
#31577=CARTESIAN_POINT('Ctrl Pts',(-4.78019591494569,1.15893974681738,39.9191293614024));
#31578=CARTESIAN_POINT('Ctrl Pts',(-4.76403458699542,1.22194824620825,39.9154303604093));
#31579=CARTESIAN_POINT('',(-4.91848456985419,0.000101914598987455,39.6398594359908));
#31580=CARTESIAN_POINT('Ctrl Pts',(-4.76374161084644,1.22187275725133,39.5699226582762));
#31581=CARTESIAN_POINT('Ctrl Pts',(-4.83821031443323,0.932375049404611,
39.58684801254));
#31582=CARTESIAN_POINT('Ctrl Pts',(-4.90472206789031,0.524434703871696,
39.6101602717781));
#31583=CARTESIAN_POINT('Ctrl Pts',(-4.91858862069526,0.112866935379977,
39.6334725310163));
#31584=CARTESIAN_POINT('Ctrl Pts',(-4.91848456985419,0.000101914598987455,
39.6398594359908));
#31585=CARTESIAN_POINT('Ctrl Pts',(-4.91824999878197,0.000109458262579736,
39.6399944356597));
#31586=CARTESIAN_POINT('Ctrl Pts',(-4.91825380405249,-0.170871437005476,
39.6495859678532));
#31587=CARTESIAN_POINT('Ctrl Pts',(-4.90934150834709,-0.341736064180338,
39.6591402713725));
#31588=CARTESIAN_POINT('Ctrl Pts',(-4.88416414869687,-0.582374933733232,
39.6727317641722));
#31589=CARTESIAN_POINT('Ctrl Pts',(-4.87525199054741,-0.652792382767571,
39.6767249503495));
#31590=CARTESIAN_POINT('Ctrl Pts',(-4.85531216028108,-0.78696218483098,
39.6843757529689));
#31591=CARTESIAN_POINT('Ctrl Pts',(-4.84454433577162,-0.850738335762799,
39.688030934994));
#31592=CARTESIAN_POINT('Ctrl Pts',(-4.81831674870789,-0.989366502816203,
39.6960238846444));
#31593=CARTESIAN_POINT('Ctrl Pts',(-4.80236362562827,-1.06410797581266,
39.7003640493471));
#31594=CARTESIAN_POINT('Ctrl Pts',(-4.72062103491384,-1.40765657936257,
39.720471850089));
#31595=CARTESIAN_POINT('Ctrl Pts',(-4.63396087787739,-1.67097701880662,
39.7363671056722));
#31596=CARTESIAN_POINT('Ctrl Pts',(-4.50888362915507,-1.96493725022399,
39.7545587172262));
#31597=CARTESIAN_POINT('Ctrl Pts',(-4.49163686654724,-2.00404797674673,
39.7569878356097));
#31598=CARTESIAN_POINT('Ctrl Pts',(-4.45720878502796,-2.07944324109466,
39.7616852607083));
#31599=CARTESIAN_POINT('Ctrl Pts',(-4.44008879425048,-2.11575184783079,
39.7639539235128));
#31600=CARTESIAN_POINT('Ctrl Pts',(-4.34996130050543,-2.30098395932659,
39.7755727541387));
#31601=CARTESIAN_POINT('Ctrl Pts',(-4.26989828670354,-2.4463565675653,39.7848457459926));
#31602=CARTESIAN_POINT('Ctrl Pts',(-4.129598375601,-2.67315675435193,39.799788144739));
#31603=CARTESIAN_POINT('Ctrl Pts',(-4.07392928326103,-2.75725402415036,
39.8054405691831));
#31604=CARTESIAN_POINT('Ctrl Pts',(-3.96871867005731,-2.90604215939763,
39.8156874692169));
#31605=CARTESIAN_POINT('Ctrl Pts',(-3.92007997359551,-2.97132658977595,
39.8202741984091));
#31606=CARTESIAN_POINT('Ctrl Pts',(-3.86502005635664,-3.04152332213673,
39.8253164067597));
#31607=CARTESIAN_POINT('Ctrl Pts',(-3.86018153268147,-3.04766183978437,
39.8257582784446));
#31608=CARTESIAN_POINT('Ctrl Pts',(-3.84697764023086,-3.064331408321,39.8269608007248));
#31609=CARTESIAN_POINT('Ctrl Pts',(-3.83858368339721,-3.07483971109781,
39.8277216799806));
#31610=CARTESIAN_POINT('Ctrl Pts',(-3.79048970413415,-3.13454417932209,
39.8320610348507));
#31611=CARTESIAN_POINT('Ctrl Pts',(-3.74988746088526,-3.18300539260527,
39.835646728471));
#31612=CARTESIAN_POINT('Ctrl Pts',(-3.62716353657138,-3.32387549084481,
39.8462671682976));
#31613=CARTESIAN_POINT('Ctrl Pts',(-3.54248025997216,-3.41398543796978,
39.8533213071857));
#31614=CARTESIAN_POINT('Ctrl Pts',(-3.37474670909175,-3.57949991103548,
39.8668000842906));
#31615=CARTESIAN_POINT('Ctrl Pts',(-3.29233455531089,-3.65544362948992,
39.8732176907365));
#31616=CARTESIAN_POINT('Ctrl Pts',(-3.16181580181251,-3.76772075223153,
39.8830634686469));
#31617=CARTESIAN_POINT('Ctrl Pts',(-3.11551492340916,-3.80609585759247,
39.8864981807686));
#31618=CARTESIAN_POINT('Ctrl Pts',(-3.03219316867195,-3.87261521154067,
39.8925732721704));
#31619=CARTESIAN_POINT('Ctrl Pts',(-2.99545488666384,-3.90110164939895,
39.8952167120479));
#31620=CARTESIAN_POINT('Ctrl Pts',(-2.92735731573845,-3.95237450034852,
39.9000499073559));
#31621=CARTESIAN_POINT('Ctrl Pts',(-2.89612222976877,-3.97531899386409,
39.9022414377925));
#31622=CARTESIAN_POINT('Ctrl Pts',(-2.80255975533688,-4.04235952871821,
39.9087368107064));
#31623=CARTESIAN_POINT('Ctrl Pts',(-2.73947306651016,-4.08537627094839,
39.9130272283708));
#31624=CARTESIAN_POINT('Ctrl Pts',(-2.54493574657071,-4.21149180140599,
39.9260352763269));
#31625=CARTESIAN_POINT('Ctrl Pts',(-2.41052357468821,-4.28984117615114,
39.9347265769696));
#31626=CARTESIAN_POINT('Ctrl Pts',(-2.20472033538892,-4.39707338898737,
39.9477511439824));
#31627=CARTESIAN_POINT('Ctrl Pts',(-2.13599790362256,-4.43086435736537,
39.9520549745192));
#31628=CARTESIAN_POINT('Ctrl Pts',(-2.00570345418328,-4.4911944533872,39.9601463359329));
#31629=CARTESIAN_POINT('Ctrl Pts',(-1.94432313575945,-4.51810595055532,
39.9639303844588));
#31630=CARTESIAN_POINT('Ctrl Pts',(-1.83193200935231,-4.5646679868378,39.9708167495842));
#31631=CARTESIAN_POINT('Ctrl Pts',(-1.78110676819378,-4.58473852314179,
39.9739154421669));
#31632=CARTESIAN_POINT('Ctrl Pts',(-1.61818168800316,-4.64595835812933,
39.983804487152));
#31633=CARTESIAN_POINT('Ctrl Pts',(-1.50491416145742,-4.68387380341578,
39.9906147339127));
#31634=CARTESIAN_POINT('Ctrl Pts',(-1.25906589890843,-4.75633024829885,
40.005269774266));
#31635=CARTESIAN_POINT('Ctrl Pts',(-1.12619279710575,-4.78953172313279,
40.0131140799779));
#31636=CARTESIAN_POINT('Ctrl Pts',(-0.939228885663524,-4.82803759207858,
40.0240243409718));
#31637=CARTESIAN_POINT('Ctrl Pts',(-0.88617351712668,-4.83805688855832,
40.0271060380122));
#31638=CARTESIAN_POINT('Ctrl Pts',(-0.794217816583256,-4.85385894891157,
40.0324190957173));
#31639=CARTESIAN_POINT('Ctrl Pts',(-0.755393247203296,-4.86005244012726,
40.0346536961606));
#31640=CARTESIAN_POINT('Ctrl Pts',(-0.687365714579173,-4.87006966581824,
40.0385524034825));
#31641=CARTESIAN_POINT('Ctrl Pts',(-0.658195217830814,-4.87409778761951,
40.0402186475269));
#31642=CARTESIAN_POINT('Ctrl Pts',(-0.560804454528446,-4.88665611686589,
40.0457657363222));
#31643=CARTESIAN_POINT('Ctrl Pts',(-0.492441355987468,-4.89401791274671,
40.049633815286));
#31644=CARTESIAN_POINT('Ctrl Pts',(-0.25742644258563,-4.91435153091155,
40.0628808816306));
#31645=CARTESIAN_POINT('Ctrl Pts',(-0.0902805606894244,-4.92026107802224,
40.072219110002));
#31646=CARTESIAN_POINT('Ctrl Pts',(0.181084879859672,-4.9160208166942,40.0874481640124));
#31647=CARTESIAN_POINT('Ctrl Pts',(0.285249127677867,-4.9110777795041,40.0933093068804));
#31648=CARTESIAN_POINT('Ctrl Pts',(0.433520850873622,-4.89930827197351,
40.1017032653211));
#31649=CARTESIAN_POINT('Ctrl Pts',(0.477815160072979,-4.89518687147136,
40.104217272108));
#31650=CARTESIAN_POINT('Ctrl Pts',(0.53113761744237,-4.88949480727931,40.1072527800906));
#31651=CARTESIAN_POINT('Ctrl Pts',(0.540225261002683,-4.88849908521108,
40.1077704339065));
#31652=CARTESIAN_POINT('Ctrl Pts',(0.624104688839324,-4.87907176630438,
40.1125514192457));
#31653=CARTESIAN_POINT('Ctrl Pts',(0.698695851383743,-4.86894977252967,
40.1168253081762));
#31654=CARTESIAN_POINT('Ctrl Pts',(0.882107812899771,-4.83975922914403,
40.1273977247081));
#31655=CARTESIAN_POINT('Ctrl Pts',(0.990574165129971,-4.81872867058308,
40.1337060305085));
#31656=CARTESIAN_POINT('Ctrl Pts',(1.21703565956611,-4.766850159978,40.1469982071036));
#31657=CARTESIAN_POINT('Ctrl Pts',(1.33477950833735,-4.73522966597282,40.1539801603826));
#31658=CARTESIAN_POINT('Ctrl Pts',(1.50044562213065,-4.68406868950492,40.1638872846454));
#31659=CARTESIAN_POINT('Ctrl Pts',(1.54942259776311,-4.6680966388798,40.1668266074534));
#31660=CARTESIAN_POINT('Ctrl Pts',(1.63829550845636,-4.63756118208562,40.1721761248854));
#31661=CARTESIAN_POINT('Ctrl Pts',(1.6782710987365,-4.62324475510122,40.1745883022877));
#31662=CARTESIAN_POINT('Ctrl Pts',(1.75763041877068,-4.59365890410072,40.1793864014169));
#31663=CARTESIAN_POINT('Ctrl Pts',(1.79701288812756,-4.57839617672405,40.1817721764296));
#31664=CARTESIAN_POINT('Ctrl Pts',(1.97952007660285,-4.50494757728266,40.1928628089835));
#31665=CARTESIAN_POINT('Ctrl Pts',(2.12005011548457,-4.44054512171268,40.2015044643823));
#31666=CARTESIAN_POINT('Ctrl Pts',(2.38290784497685,-4.30475501852256,40.2180801838806));
#31667=CARTESIAN_POINT('Ctrl Pts',(2.50564239405402,-4.23449183527942,40.226003933801));
#31668=CARTESIAN_POINT('Ctrl Pts',(2.68634879532864,-4.12043028504605,40.2380441945136));
#31669=CARTESIAN_POINT('Ctrl Pts',(2.74665899280869,-4.08047543812533,40.2421286570757));
#31670=CARTESIAN_POINT('Ctrl Pts',(2.85863465239956,-4.00268512649904,40.2498480334147));
#31671=CARTESIAN_POINT('Ctrl Pts',(2.91048543662297,-3.96514245728844,40.2534798163193));
#31672=CARTESIAN_POINT('Ctrl Pts',(3.11636713309874,-3.80985874636241,40.2681434893905));
#31673=CARTESIAN_POINT('Ctrl Pts',(3.26410627944244,-3.68407058501565,40.2792351899149));
#31674=CARTESIAN_POINT('Ctrl Pts',(3.46150416980243,-3.49478354881989,40.2948894113038));
#31675=CARTESIAN_POINT('Ctrl Pts',(3.51762923628789,-3.43828559777132,40.2994444483396));
#31676=CARTESIAN_POINT('Ctrl Pts',(3.59090501574226,-3.36084994769392,40.3055273431877));
#31677=CARTESIAN_POINT('Ctrl Pts',(3.60929037297623,-3.34109775626211,40.3070655141585));
#31678=CARTESIAN_POINT('Ctrl Pts',(3.65646417692722,-3.28957306578256,40.311042680713));
#31679=CARTESIAN_POINT('Ctrl Pts',(3.6850015495682,-3.2575734633346,40.3134786234767));
#31680=CARTESIAN_POINT('Ctrl Pts',(3.7405574267787,-3.19361303210002,40.3182785178885));
#31681=CARTESIAN_POINT('Ctrl Pts',(3.76759368551343,-3.16167233171011,40.3206425219592));
#31682=CARTESIAN_POINT('Ctrl Pts',(3.88168774424247,-3.02333935585963,40.3307522163886));
#31683=CARTESIAN_POINT('Ctrl Pts',(3.96467250334307,-2.91366665555636,40.3384483356752));
#31684=CARTESIAN_POINT('Ctrl Pts',(4.13446596625642,-2.66855763522293,40.3551522609846));
#31685=CARTESIAN_POINT('Ctrl Pts',(4.21944680064033,-2.53204986832389,40.3641530158703));
#31686=CARTESIAN_POINT('Ctrl Pts',(4.33262594742223,-2.32867473918436,40.3772678647632));
#31687=CARTESIAN_POINT('Ctrl Pts',(4.36627225693209,-2.26495917423766,40.3813362550234));
#31688=CARTESIAN_POINT('Ctrl Pts',(4.43130602307156,-2.13496699029808,40.3895661997115));
#31689=CARTESIAN_POINT('Ctrl Pts',(4.46263535629884,-2.06868137368618,40.3937271117874));
#31690=CARTESIAN_POINT('Ctrl Pts',(4.55383461287824,-1.86400246975567,40.4064772546395));
#31691=CARTESIAN_POINT('Ctrl Pts',(4.6088322883087,-1.723536731297,40.4150953682651));
#31692=CARTESIAN_POINT('Ctrl Pts',(4.68929700832626,-1.48647008250853,40.4294262331924));
#31693=CARTESIAN_POINT('Ctrl Pts',(4.71843245351833,-1.3912207082221,40.4351280122482));
#31694=CARTESIAN_POINT('Ctrl Pts',(4.76137847641793,-1.23389241068017,40.4444409781371));
#31695=CARTESIAN_POINT('Ctrl Pts',(4.77691281317847,-1.17231377775277,40.4480601166233));
#31696=CARTESIAN_POINT('Ctrl Pts',(4.79963651653507,-1.07426808123617,40.4537758792679));
#31697=CARTESIAN_POINT('Ctrl Pts',(4.80761241121767,-1.03799111234175,40.4558803574403));
#31698=CARTESIAN_POINT('Ctrl Pts',(4.82723479497463,-0.943659324131473,
40.4613267756976));
#31699=CARTESIAN_POINT('Ctrl Pts',(4.83824523540743,-0.885478318761359,
40.464661615081));
#31700=CARTESIAN_POINT('Ctrl Pts',(4.87814730463323,-0.651588277276984,
40.4779990118264));
#31701=CARTESIAN_POINT('Ctrl Pts',(4.89853807301753,-0.474566944708308,
40.4879433117897));
#31702=CARTESIAN_POINT('Ctrl Pts',(4.91409360002124,-0.217293229452264,
40.5024037716249));
#31703=CARTESIAN_POINT('Ctrl Pts',(4.91696898605229,-0.137652057999693,
40.5068804031427));
#31704=CARTESIAN_POINT('Ctrl Pts',(4.91877154398843,0.0152508559710218,
40.5154940979235));
#31705=CARTESIAN_POINT('Ctrl Pts',(4.91799916601728,0.0884880131010949,
40.5196282124979));
#31706=CARTESIAN_POINT('Ctrl Pts',(4.91350680327257,0.225070280268358,40.5273636706882));
#31707=CARTESIAN_POINT('Ctrl Pts',(4.91019582971013,0.288413833167033,40.5309614627255));
#31708=CARTESIAN_POINT('Ctrl Pts',(4.89615185819561,0.484318938605563,40.5421273142273));
#31709=CARTESIAN_POINT('Ctrl Pts',(4.88126714874111,0.616520971278551,40.5497189623331));
#31710=CARTESIAN_POINT('Ctrl Pts',(4.84266064773769,0.86742879772177,40.5642435882752));
#31711=CARTESIAN_POINT('Ctrl Pts',(4.8198792788169,0.986183903647256,40.5711684564434));
#31712=CARTESIAN_POINT('Ctrl Pts',(4.78122261590757,1.15400554892581,40.5810085312252));
#31713=CARTESIAN_POINT('Ctrl Pts',(4.76891667289989,1.20384896883195,40.5839377705937));
#31714=CARTESIAN_POINT('Ctrl Pts',(4.74503533034857,1.294456464318,40.5892717663854));
#31715=CARTESIAN_POINT('Ctrl Pts',(4.73370912296363,1.33528117599438,40.5916784867908));
#31716=CARTESIAN_POINT('Ctrl Pts',(4.71001478470901,1.41659291396916,40.5964764237059));
#31717=CARTESIAN_POINT('Ctrl Pts',(4.69764855134786,1.45707683399495,40.598867447045));
#31718=CARTESIAN_POINT('Ctrl Pts',(4.64565269589739,1.61975130641064,40.6084949389549));
#31719=CARTESIAN_POINT('Ctrl Pts',(4.6017653778865,1.7405284755397,40.6156892851189));
#31720=CARTESIAN_POINT('Ctrl Pts',(4.49289156162443,2.00712573965965,40.6318219193209));
#31721=CARTESIAN_POINT('Ctrl Pts',(4.42543504490809,2.15177885685023,40.6407530513677));
#31722=CARTESIAN_POINT('Ctrl Pts',(4.31646630008613,2.35856119924585,40.6539164922645));
#31723=CARTESIAN_POINT('Ctrl Pts',(4.28038124290289,2.42343320415657,40.6581055718187));
#31724=CARTESIAN_POINT('Ctrl Pts',(4.20676162634252,2.54900548150244,40.6663435008808));
#31725=CARTESIAN_POINT('Ctrl Pts',(4.16934661066024,2.60975497074282,40.6703904849311));
#31726=CARTESIAN_POINT('Ctrl Pts',(4.06911924840025,2.76483096808158,40.6808910946124));
#31727=CARTESIAN_POINT('Ctrl Pts',(4.00434517016673,2.85783852081929,40.6873573124425));
#31728=CARTESIAN_POINT('Ctrl Pts',(3.85766946311584,3.05365739186701,40.7013500266205));
#31729=CARTESIAN_POINT('Ctrl Pts',(3.77474120876909,3.15559280988947,40.7088761983449));
#31730=CARTESIAN_POINT('Ctrl Pts',(3.63952518434315,3.3088321486454,40.7205557069877));
#31731=CARTESIAN_POINT('Ctrl Pts',(3.59000463550267,3.36249619568968,40.7247205706407));
#31732=CARTESIAN_POINT('Ctrl Pts',(3.51323041248651,3.44206413862823,40.7310033986718));
#31733=CARTESIAN_POINT('Ctrl Pts',(3.48684462088458,3.46879058325829,40.7331327157336));
#31734=CARTESIAN_POINT('Ctrl Pts',(3.42301168752941,3.53198326123077,40.7382128296772));
#31735=CARTESIAN_POINT('Ctrl Pts',(3.38528431836948,3.56815988240232,40.7411592013476));
#31736=CARTESIAN_POINT('Ctrl Pts',(3.22714317723627,3.71503453358388,40.7533015844116));
#31737=CARTESIAN_POINT('Ctrl Pts',(3.10182062141677,3.82029374217735,40.7624416666057));
#31738=CARTESIAN_POINT('Ctrl Pts',(2.90022211939522,3.97314646910845,40.7766239956036));
#31739=CARTESIAN_POINT('Ctrl Pts',(2.82749778510871,4.02522512314026,40.7816425990572));
#31740=CARTESIAN_POINT('Ctrl Pts',(2.68885704562708,4.11889514288085,40.7910586284024));
#31741=CARTESIAN_POINT('Ctrl Pts',(2.62329348441445,4.16095908560212,40.7954512086737));
#31742=CARTESIAN_POINT('Ctrl Pts',(2.4980419819297,4.23717993590698,40.8037440839669));
#31743=CARTESIAN_POINT('Ctrl Pts',(2.43858257343126,4.27167677179018,40.8076406321834));
#31744=CARTESIAN_POINT('Ctrl Pts',(2.26891637771215,4.36541553953362,40.8186559488885));
#31745=CARTESIAN_POINT('Ctrl Pts',(2.15714528485309,4.42171436295713,40.8257934924014));
#31746=CARTESIAN_POINT('Ctrl Pts',(1.87424050601356,4.55093067861764,40.8435816087837));
#31747=CARTESIAN_POINT('Ctrl Pts',(1.70088588605657,4.61852090806383,40.8542427797494));
#31748=CARTESIAN_POINT('Ctrl Pts',(1.48368011510898,4.68931611296052,40.8672479811749));
#31749=CARTESIAN_POINT('Ctrl Pts',(1.44306938097336,4.70197225735915,40.8696644799418));
#31750=CARTESIAN_POINT('Ctrl Pts',(1.36755566561905,4.72443525714269,40.8741277826841));
#31751=CARTESIAN_POINT('Ctrl Pts',(1.33269860848281,4.73438606911129,40.8761762732633));
#31752=CARTESIAN_POINT('Ctrl Pts',(1.13905398316217,4.78735865039544,40.8875008827966));
#31753=CARTESIAN_POINT('Ctrl Pts',(0.978293493822922,4.82277824465111,40.8966997066159));
#31754=CARTESIAN_POINT('Ctrl Pts',(0.715559786213942,4.86698503455403,40.9116270542556));
#31755=CARTESIAN_POINT('Ctrl Pts',(0.614559663888879,4.88076687964144,40.9173396501757));
#31756=CARTESIAN_POINT('Ctrl Pts',(0.474073919237509,4.89550662134189,40.925282170632));
#31757=CARTESIAN_POINT('Ctrl Pts',(0.434895122296926,4.89914251381362,40.9274967489058));
#31758=CARTESIAN_POINT('Ctrl Pts',(0.324400570819698,4.90806079493912,40.9337441490601));
#31759=CARTESIAN_POINT('Ctrl Pts',(0.253007662664536,4.91225848914196,40.9377828339007));
#31760=CARTESIAN_POINT('Ctrl Pts',(0.107612537255581,4.91762917406558,40.9460219374882));
#31761=CARTESIAN_POINT('Ctrl Pts',(0.0336242836440473,4.91869153173761,
40.9502220685086));
#31762=CARTESIAN_POINT('Ctrl Pts',(-0.20218934826509,4.91675638125509,40.963642690932));
#31763=CARTESIAN_POINT('Ctrl Pts',(-0.363853708336036,4.90744161532399,
40.9728977025432));
#31764=CARTESIAN_POINT('Ctrl Pts',(-0.615182301461178,4.8804716733818,40.9873678651629));
#31765=CARTESIAN_POINT('Ctrl Pts',(-0.705316357912556,4.8682627283663,40.9925730679019));
#31766=CARTESIAN_POINT('Ctrl Pts',(-0.854659235233268,4.84379892228501,
41.0012122650179));
#31767=CARTESIAN_POINT('Ctrl Pts',(-0.914073810919858,4.83293902321936,
41.0046531009655));
#31768=CARTESIAN_POINT('Ctrl Pts',(-1.00966294806102,4.81364123458574,41.0101900135744));
#31769=CARTESIAN_POINT('Ctrl Pts',(-1.04596781231514,4.8058831217296,41.0122928324722));
#31770=CARTESIAN_POINT('Ctrl Pts',(-1.14281285486558,4.78403856520235,41.0179034113745));
#31771=CARTESIAN_POINT('Ctrl Pts',(-1.20317972634694,4.76921428551848,41.0214029176017));
#31772=CARTESIAN_POINT('Ctrl Pts',(-1.43190349461411,4.70842739372774,41.0347018143988));
#31773=CARTESIAN_POINT('Ctrl Pts',(-1.59805257712061,4.65466052639345,41.0444489906849));
#31774=CARTESIAN_POINT('Ctrl Pts',(-1.83496484749956,4.56381021311958,41.0586852454443));
#31775=CARTESIAN_POINT('Ctrl Pts',(-1.90824057283842,4.53366048709048,41.0631364932948));
#31776=CARTESIAN_POINT('Ctrl Pts',(-2.0475872034986,4.47234847398694,41.0717126478637));
#31777=CARTESIAN_POINT('Ctrl Pts',(-2.11375521471139,4.44145842680702,41.0758346904216));
#31778=CARTESIAN_POINT('Ctrl Pts',(-2.236185689482,4.38094690606733,41.0835655307352));
#31779=CARTESIAN_POINT('Ctrl Pts',(-2.29260931302714,4.35168526633352,41.087170876352));
#31780=CARTESIAN_POINT('Ctrl Pts',(-2.5206479958865,4.22775668742044,41.1019264655134));
#31781=CARTESIAN_POINT('Ctrl Pts',(-2.68709676478735,4.12396676932475,41.1131385912332));
#31782=CARTESIAN_POINT('Ctrl Pts',(-2.91209416945621,3.96425043423538,41.1289322758749));
#31783=CARTESIAN_POINT('Ctrl Pts',(-2.97614513104901,3.91639301420836,41.133505603347));
#31784=CARTESIAN_POINT('Ctrl Pts',(-3.06027010316607,3.85028073015547,41.1396105635951));
#31785=CARTESIAN_POINT('Ctrl Pts',(-3.08140068626419,3.83339074794697,41.1411525607872));
#31786=CARTESIAN_POINT('Ctrl Pts',(-3.13571229212046,3.78923944164817,41.1451374956286));
#31787=CARTESIAN_POINT('Ctrl Pts',(-3.16867773142135,3.76171617972036,41.1475773785419));
#31788=CARTESIAN_POINT('Ctrl Pts',(-3.23299913147575,3.70656788949798,41.1523777342265));
#31789=CARTESIAN_POINT('Ctrl Pts',(-3.26437189973619,3.67896793319757,41.1547382919601));
#31790=CARTESIAN_POINT('Ctrl Pts',(-3.37622277209184,3.5780106432003,41.1632334742143));
#31791=CARTESIAN_POINT('Ctrl Pts',(-3.45461167480752,3.50238476311132,41.1693387667494));
#31792=CARTESIAN_POINT('Ctrl Pts',(-3.64228781453872,3.30888754907747,41.1844435796004));
#31793=CARTESIAN_POINT('Ctrl Pts',(-3.74843005721304,3.18814506200019,41.1934318874686));
#31794=CARTESIAN_POINT('Ctrl Pts',(-3.89858136444738,2.99945375229901,41.2069967199575));
#31795=CARTESIAN_POINT('Ctrl Pts',(-3.94713751378956,2.93526228913609,41.2115333717542));
#31796=CARTESIAN_POINT('Ctrl Pts',(-4.03425418939779,2.81402067247793,41.2199746374233));
#31797=CARTESIAN_POINT('Ctrl Pts',(-4.07323422168457,2.75729614690125,41.2238746480174));
#31798=CARTESIAN_POINT('Ctrl Pts',(-4.17376648376287,2.60421318625216,41.234278772206));
#31799=CARTESIAN_POINT('Ctrl Pts',(-4.23317050561093,2.50649554384115,41.2407971078437));
#31800=CARTESIAN_POINT('Ctrl Pts',(-4.35885218952251,2.28252029276776,41.2554782933823));
#31801=CARTESIAN_POINT('Ctrl Pts',(-4.42315497298407,2.15527058597694,41.2636443295072));
#31802=CARTESIAN_POINT('Ctrl Pts',(-4.50442402279167,1.97543776803799,41.2749245689562));
#31803=CARTESIAN_POINT('Ctrl Pts',(-4.52616950938839,1.92509215259191,41.2780549932424));
#31804=CARTESIAN_POINT('Ctrl Pts',(-4.56392768442045,1.83349503360702,41.2836972046173));
#31805=CARTESIAN_POINT('Ctrl Pts',(-4.58023430526373,1.79237097641657,41.2862113376064));
#31806=CARTESIAN_POINT('Ctrl Pts',(-4.61049448332292,1.71294622759946,41.2910280207994));
#31807=CARTESIAN_POINT('Ctrl Pts',(-4.62453099647541,1.67468124173679,41.2933312389981));
#31808=CARTESIAN_POINT('Ctrl Pts',(-4.6790932645764,1.52001944019533,41.3025805678251));
#31809=CARTESIAN_POINT('Ctrl Pts',(-4.71571331130518,1.40229152375044,41.3094865621716));
#31810=CARTESIAN_POINT('Ctrl Pts',(-4.75339206495188,1.26289128003114,41.3175768139253));
#31811=CARTESIAN_POINT('Ctrl Pts',(-4.7587794745832,1.24243646034837,41.3187617358029));
#31812=CARTESIAN_POINT('Ctrl Pts',(-4.76403458753695,1.22194824409695,41.3199466556564));
#31813=CARTESIAN_POINT('Origin',(0.,0.,-3.23514056400928));
#31814=CARTESIAN_POINT('',(-4.76403458704966,1.22194824599677,43.4152064557962));
#31815=CARTESIAN_POINT('',(-4.76403458776301,1.22194824321562,43.0699834446552));
#31816=CARTESIAN_POINT('',(-4.76403458704967,1.22194824599672,-3.23514056400928));
#31817=CARTESIAN_POINT('',(-4.91824999998163,-1.34407408516682E-5,41.7351405640093));
#31818=CARTESIAN_POINT('Ctrl Pts',(-4.91824999998163,-1.34407408516682E-5,
41.7351405640093));
#31819=CARTESIAN_POINT('Ctrl Pts',(-4.9182496007205,-0.146111492021241,
41.7434115561549));
#31820=CARTESIAN_POINT('Ctrl Pts',(-4.91173503323865,-0.292193156995082,
41.7516825483005));
#31821=CARTESIAN_POINT('Ctrl Pts',(-4.89873667140923,-0.437678062838914,
41.7599535404461));
#31822=CARTESIAN_POINT('Ctrl Pts',(-4.88573395304958,-0.583211729395645,
41.768227304697));
#31823=CARTESIAN_POINT('Ctrl Pts',(-4.86624312668477,-0.728147924347313,
41.7765010689479));
#31824=CARTESIAN_POINT('Ctrl Pts',(-4.84034647390028,-0.871911162390469,
41.7847748331988));
#31825=CARTESIAN_POINT('Ctrl Pts',(-4.82220470072196,-0.972623794160462,
41.7905709781917));
#31826=CARTESIAN_POINT('Ctrl Pts',(-4.80092026754504,-1.07276089085213,
41.7963671231846));
#31827=CARTESIAN_POINT('Ctrl Pts',(-4.77653643689978,-1.17212743738414,
41.8021632681775));
#31828=CARTESIAN_POINT('Ctrl Pts',(-4.74222309626264,-1.31195772937941,
41.8103197018576));
#31829=CARTESIAN_POINT('Ctrl Pts',(-4.70175895042439,-1.45030636416344,
41.8184761355377));
#31830=CARTESIAN_POINT('Ctrl Pts',(-4.65529696866333,-1.58662950812534,
41.8266325692178));
#31831=CARTESIAN_POINT('Ctrl Pts',(-4.6088444432254,-1.72292490648424,41.8347873428337));
#31832=CARTESIAN_POINT('Ctrl Pts',(-4.55639662503431,-1.85719531987858,
41.8429421164495));
#31833=CARTESIAN_POINT('Ctrl Pts',(-4.49815595564138,-1.98891328650295,
41.8510968900654));
#31834=CARTESIAN_POINT('Ctrl Pts',(-4.43991322085102,-2.12063592426096,
41.8592519528753));
#31835=CARTESIAN_POINT('Ctrl Pts',(-4.37587735567236,-2.24980562657217,
41.8674070156851));
#31836=CARTESIAN_POINT('Ctrl Pts',(-4.30629864695912,-2.37591561838759,
41.8755620784949));
#31837=CARTESIAN_POINT('Ctrl Pts',(-4.23672401903191,-2.50201821386147,
41.8837166630109));
#31838=CARTESIAN_POINT('Ctrl Pts',(-4.16160736044227,-2.6250611653142,41.8918712475269));
#31839=CARTESIAN_POINT('Ctrl Pts',(-4.08124452071586,-2.74456302981491,
41.9000258320429));
#31840=CARTESIAN_POINT('Ctrl Pts',(-4.00086192258999,-2.86409427562645,
41.9081824214848));
#31841=CARTESIAN_POINT('Ctrl Pts',(-3.91523075255369,-2.98008241684767,
41.9163390109267));
#31842=CARTESIAN_POINT('Ctrl Pts',(-3.82469007041437,-3.09207518145561,
41.9244956003686));
#31843=CARTESIAN_POINT('Ctrl Pts',(-3.7632163498541,-3.16811405982065,41.9300336180666));
#31844=CARTESIAN_POINT('Ctrl Pts',(-3.69948028552799,-3.24231172587062,
41.9355716357646));
#31845=CARTESIAN_POINT('Ctrl Pts',(-3.63359857721944,-3.31453532823666,
41.9411096534626));
#31846=CARTESIAN_POINT('Ctrl Pts',(-3.53656750692421,-3.42090678729676,
41.9492660871427));
#31847=CARTESIAN_POINT('Ctrl Pts',(-3.43484415123915,-3.52303440723009,
41.9574225208228));
#31848=CARTESIAN_POINT('Ctrl Pts',(-3.32882302515633,-3.62051382122608,
41.9655789545029));
#31849=CARTESIAN_POINT('Ctrl Pts',(-3.22282347736149,-3.71797339541329,
41.9737337281188));
#31850=CARTESIAN_POINT('Ctrl Pts',(-3.1125281503641,-3.81078642461029,41.9818885017348));
#31851=CARTESIAN_POINT('Ctrl Pts',(-2.99836716903939,-3.89858658774263,
41.9900432753507));
#31852=CARTESIAN_POINT('Ctrl Pts',(-2.88420213920718,-3.98638986454493,
41.9981983381605));
#31853=CARTESIAN_POINT('Ctrl Pts',(-2.76617144368788,-4.06917971259167,
42.0063534009703));
#31854=CARTESIAN_POINT('Ctrl Pts',(-2.64473732413514,-4.14663086720129,
42.0145084637802));
#31855=CARTESIAN_POINT('Ctrl Pts',(-2.52331032668454,-4.22407747930641,
42.0226630482962));
#31856=CARTESIAN_POINT('Ctrl Pts',(-2.39848058719828,-4.29618584525402,
42.0308176328122));
#31857=CARTESIAN_POINT('Ctrl Pts',(-2.27073823717365,-4.3626747438627,42.0389722173282));
#31858=CARTESIAN_POINT('Ctrl Pts',(-2.14296447979213,-4.42917998975611,
42.0471288067701));
#31859=CARTESIAN_POINT('Ctrl Pts',(-2.01227697778862,-4.4900628527459,42.055285396212));
#31860=CARTESIAN_POINT('Ctrl Pts',(-1.87918985020415,-4.54508840061331,
42.0634419856539));
#31861=CARTESIAN_POINT('Ctrl Pts',(-1.78882869212653,-4.58244867969815,
42.0689800033519));
#31862=CARTESIAN_POINT('Ctrl Pts',(-1.69736181924629,-4.61710976318445,
42.0745180210498));
#31863=CARTESIAN_POINT('Ctrl Pts',(-1.60495526908678,-4.64901082454436,
42.0800560387478));
#31864=CARTESIAN_POINT('Ctrl Pts',(-1.4688582143122,-4.69599494512641,42.0882124724279));
#31865=CARTESIAN_POINT('Ctrl Pts',(-1.3306711589202,-4.73700749890126,42.096368906108));
#31866=CARTESIAN_POINT('Ctrl Pts',(-1.19093399887237,-4.77188215202658,
42.1045253397881));
#31867=CARTESIAN_POINT('Ctrl Pts',(-1.05122527927597,-4.80674970717683,
42.112680113404));
#31868=CARTESIAN_POINT('Ctrl Pts',(-0.909967408882027,-4.83548177285114,
42.1208348870199));
#31869=CARTESIAN_POINT('Ctrl Pts',(-0.767713351081594,-4.8579624610603,
42.1289896606358));
#31870=CARTESIAN_POINT('Ctrl Pts',(-0.625454248504764,-4.88044394650539,
42.1371447234456));
#31871=CARTESIAN_POINT('Ctrl Pts',(-0.482199217757345,-4.89667355493871,
42.1452997862555));
#31872=CARTESIAN_POINT('Ctrl Pts',(-0.338509781880459,-4.90658681672619,
42.1534548490653));
#31873=CARTESIAN_POINT('Ctrl Pts',(-0.194828773378184,-4.91649949710161,
42.1616094335813));
#31874=CARTESIAN_POINT('Ctrl Pts',(-0.0507137446299321,-4.92009654988941,
42.1697640180973));
#31875=CARTESIAN_POINT('Ctrl Pts',(0.0932703625784521,-4.91736552454304,
42.1779186026133));
#31876=CARTESIAN_POINT('Ctrl Pts',(0.23728987042118,-4.91463382773348,42.1860751920552));
#31877=CARTESIAN_POINT('Ctrl Pts',(0.381178057679785,-4.90557094998026,
42.1942317814971));
#31878=CARTESIAN_POINT('Ctrl Pts',(0.524371064830764,-4.89021656461841,
42.202388370939));
#31879=CARTESIAN_POINT('Ctrl Pts',(0.621593735344925,-4.87979151399139,
42.207926388637));
#31880=CARTESIAN_POINT('Ctrl Pts',(0.718495968908813,-4.86646722514291,
42.213464406335));
#31881=CARTESIAN_POINT('Ctrl Pts',(0.814902862627231,-4.85026972311664,
42.219002424033));
#31882=CARTESIAN_POINT('Ctrl Pts',(0.956891653165912,-4.82641392158884,
42.2271588577131));
#31883=CARTESIAN_POINT('Ctrl Pts',(1.09785871281386,-4.7963144209411,42.2353152913931));
#31884=CARTESIAN_POINT('Ctrl Pts',(1.23725036662756,-4.76008346489639,42.2434717250732));
#31885=CARTESIAN_POINT('Ctrl Pts',(1.37661365031004,-4.72385988287263,42.2516264986891));
#31886=CARTESIAN_POINT('Ctrl Pts',(1.51440184414399,-4.68150741911794,42.259781272305));
#31887=CARTESIAN_POINT('Ctrl Pts',(1.65007393345286,-4.63318886692949,42.2679360459209));
#31888=CARTESIAN_POINT('Ctrl Pts',(1.78575083412094,-4.58486860121314,42.2760911087307));
#31889=CARTESIAN_POINT('Ctrl Pts',(1.91931116362224,-4.53058193242733,42.2842461715406));
#31890=CARTESIAN_POINT('Ctrl Pts',(2.05023099121036,-4.47054090073903,42.2924012343504));
#31891=CARTESIAN_POINT('Ctrl Pts',(2.18114314036044,-4.41050339045273,42.3005558188664));
#31892=CARTESIAN_POINT('Ctrl Pts',(2.30941479364516,-4.34471233282722,42.3087104033824));
#31893=CARTESIAN_POINT('Ctrl Pts',(2.43454390600623,-4.27342708282567,42.3168649878984));
#31894=CARTESIAN_POINT('Ctrl Pts',(2.55970378322067,-4.20212430628515,42.3250215773403));
#31895=CARTESIAN_POINT('Ctrl Pts',(2.68171928460811,-4.12532480363762,42.3331781667822));
#31896=CARTESIAN_POINT('Ctrl Pts',(2.80011425337252,-4.04333318322397,42.3413347562241));
#31897=CARTESIAN_POINT('Ctrl Pts',(2.88049998775817,-3.987663954293,42.3468727739221));
#31898=CARTESIAN_POINT('Ctrl Pts',(2.95921724134023,-3.9296021464371,42.3524107916201));
#31899=CARTESIAN_POINT('Ctrl Pts',(3.03612487919264,-3.86925429255399,42.357948809318));
#31900=CARTESIAN_POINT('Ctrl Pts',(3.14939502057598,-3.7803735242402,42.3661052429981));
#31901=CARTESIAN_POINT('Ctrl Pts',(3.25878075090655,-3.68649885329559,42.3742616766782));
#31902=CARTESIAN_POINT('Ctrl Pts',(3.36384957693318,-3.58799374111305,42.3824181103582));
#31903=CARTESIAN_POINT('Ctrl Pts',(3.46889701849171,-3.48950867749782,42.3905728839741));
#31904=CARTESIAN_POINT('Ctrl Pts',(3.56962906455316,-3.38639528146084,42.39872765759));
#31905=CARTESIAN_POINT('Ctrl Pts',(3.66564852383467,-3.27905534601182,42.4068824312059));
#31906=CARTESIAN_POINT('Ctrl Pts',(3.76167138826832,-3.17171160395096,42.4150374940157));
#31907=CARTESIAN_POINT('Ctrl Pts',(3.85298110562048,-3.0601412694471,42.4231925568255));
#31908=CARTESIAN_POINT('Ctrl Pts',(3.93921904783645,-2.94478120675586,42.4313476196353));
#31909=CARTESIAN_POINT('Ctrl Pts',(4.02545193220359,-2.82942790992361,42.4395022041513));
#31910=CARTESIAN_POINT('Ctrl Pts',(4.1066134369395,-2.71028559817519,42.4476567886673));
#31911=CARTESIAN_POINT('Ctrl Pts',(4.18238678937876,-2.58782221308382,42.4558113731833));
#31912=CARTESIAN_POINT('Ctrl Pts',(4.25817877182373,-2.46532871854776,42.4639679626251));
#31913=CARTESIAN_POINT('Ctrl Pts',(4.32857977847528,-2.33951280362419,42.472124552067));
#31914=CARTESIAN_POINT('Ctrl Pts',(4.39331742055376,-2.21086976205268,42.4802811415089));
#31915=CARTESIAN_POINT('Ctrl Pts',(4.43727184661854,-2.1235259713621,42.485819159207));
#31916=CARTESIAN_POINT('Ctrl Pts',(4.47861644747507,-2.03487946255657,42.4913571769051));
#31917=CARTESIAN_POINT('Ctrl Pts',(4.51727825841816,-1.94509130853095,42.4968951946032));
#31918=CARTESIAN_POINT('Ctrl Pts',(4.57421966129932,-1.81285064707162,42.5050516282833));
#31919=CARTESIAN_POINT('Ctrl Pts',(4.62536081504526,-1.67808316494529,42.5132080619634));
#31920=CARTESIAN_POINT('Ctrl Pts',(4.67049583020718,-1.54131494592031,42.5213644956435));
#31921=CARTESIAN_POINT('Ctrl Pts',(4.7156216591211,-1.4045745630836,42.5295192692594));
#31922=CARTESIAN_POINT('Ctrl Pts',(4.75474368330076,-1.26583457328144,42.5376740428753));
#31923=CARTESIAN_POINT('Ctrl Pts',(4.78770535195877,-1.12563783044339,42.5458288164913));
#31924=CARTESIAN_POINT('Ctrl Pts',(4.82066818954128,-0.985436115787674,
42.5539838793011));
#31925=CARTESIAN_POINT('Ctrl Pts',(4.84747015421667,-0.843777869596382,
42.5621389421109));
#31926=CARTESIAN_POINT('Ctrl Pts',(4.86800533776923,-0.701218292652367,
42.5702940049208));
#31927=CARTESIAN_POINT('Ctrl Pts',(4.88853931693481,-0.558667076816868,
42.5784485894368));
#31928=CARTESIAN_POINT('Ctrl Pts',(4.9028072035336,-0.415214967344868,42.5866031739529));
#31929=CARTESIAN_POINT('Ctrl Pts',(4.91075471200728,-0.271424429627003,
42.5947577584689));
#31930=CARTESIAN_POINT('Ctrl Pts',(4.91870417449412,-0.127598538866687,
42.6029143479108));
#31931=CARTESIAN_POINT('Ctrl Pts',(4.92033013500527,0.0165656121496476,
42.6110709373527));
#31932=CARTESIAN_POINT('Ctrl Pts',(4.91563036872653,0.160502774285812,42.6192275267946));
#31933=CARTESIAN_POINT('Ctrl Pts',(4.91243940404543,0.258230698066434,42.6247655444925));
#31934=CARTESIAN_POINT('Ctrl Pts',(4.90633342599113,0.355853935948479,42.6303035621903));
#31935=CARTESIAN_POINT('Ctrl Pts',(4.89732542554343,0.453196137258323,42.6358415798882));
#31936=CARTESIAN_POINT('Ctrl Pts',(4.88405837544527,0.596562455781503,42.6439980135683));
#31937=CARTESIAN_POINT('Ctrl Pts',(4.8644890740699,0.739372589486145,42.6521544472484));
#31938=CARTESIAN_POINT('Ctrl Pts',(4.83868842221904,0.881066067433885,42.6603108809285));
#31939=CARTESIAN_POINT('Ctrl Pts',(4.81289302152819,1.02273070676431,42.6684656545444));
#31940=CARTESIAN_POINT('Ctrl Pts',(4.78086886036851,1.16327881471372,42.6766204281603));
#31941=CARTESIAN_POINT('Ctrl Pts',(4.74273818838301,1.30215879943787,42.6847752017762));
#31942=CARTESIAN_POINT('Ctrl Pts',(4.70460616416389,1.4410437092833,42.692930264586));
#31943=CARTESIAN_POINT('Ctrl Pts',(4.66036728076453,1.57826005386353,42.7010853273959));
#31944=CARTESIAN_POINT('Ctrl Pts',(4.61019416539617,1.71326962847273,42.7092403902057));
#31945=CARTESIAN_POINT('Ctrl Pts',(4.56002399267726,1.84827128478053,42.7173949747217));
#31946=CARTESIAN_POINT('Ctrl Pts',(4.50392040175792,1.98106611670505,42.7255495592377));
#31947=CARTESIAN_POINT('Ctrl Pts',(4.44210482652777,2.11113423842225,42.7337041437537));
#31948=CARTESIAN_POINT('Ctrl Pts',(4.38027405301901,2.24123433932179,42.7418607331956));
#31949=CARTESIAN_POINT('Ctrl Pts',(4.31272863244719,2.368606087938,42.7500173226375));
#31950=CARTESIAN_POINT('Ctrl Pts',(4.23973704627174,2.4927520616722,42.7581739120795));
#31951=CARTESIAN_POINT('Ctrl Pts',(4.19017850235765,2.57704251230405,42.7637119297775));
#31952=CARTESIAN_POINT('Ctrl Pts',(4.13811030408637,2.65984639066669,42.7692499474755));
#31953=CARTESIAN_POINT('Ctrl Pts',(4.08362823151483,2.74101505455097,42.7747879651735));
#31954=CARTESIAN_POINT('Ctrl Pts',(4.00338662957051,2.86056086678492,42.7829443988536));
#31955=CARTESIAN_POINT('Ctrl Pts',(3.91787697535166,2.97660306118204,42.7911008325337));
#31956=CARTESIAN_POINT('Ctrl Pts',(3.8274296775319,3.08868339686153,42.7992572662139));
#31957=CARTESIAN_POINT('Ctrl Pts',(3.73700078828703,3.20074092103308,42.8074120398298));
#31958=CARTESIAN_POINT('Ctrl Pts',(3.64163647027939,3.30883793485481,42.8155668134457));
#31959=CARTESIAN_POINT('Ctrl Pts',(3.54170797470053,3.41254856147758,42.8237215870616));
#31960=CARTESIAN_POINT('Ctrl Pts',(3.44177593534285,3.51626286600543,42.8318766498715));
#31961=CARTESIAN_POINT('Ctrl Pts',(3.3372796240035,3.61559022850392,42.8400317126813));
#31962=CARTESIAN_POINT('Ctrl Pts',(3.22862812468748,3.71014063008089,42.8481867754912));
#31963=CARTESIAN_POINT('Ctrl Pts',(3.11998299777377,3.80468548628387,42.8563413600072));
#31964=CARTESIAN_POINT('Ctrl Pts',(3.00718342350491,3.89445372312028,42.8644959445232));
#31965=CARTESIAN_POINT('Ctrl Pts',(2.89067257974526,3.97909475876221,42.8726505290392));
#31966=CARTESIAN_POINT('Ctrl Pts',(2.77413309006171,4.06375660466169,42.8808071184811));
#31967=CARTESIAN_POINT('Ctrl Pts',(2.65388077829091,4.1432885334677,42.8889637079231));
#31968=CARTESIAN_POINT('Ctrl Pts',(2.53038938864306,4.21738219803975,42.897120297365));
#31969=CARTESIAN_POINT('Ctrl Pts',(2.44654337600825,4.26768901176646,42.9026583150629));
#31970=CARTESIAN_POINT('Ctrl Pts',(2.36120480719153,4.31548972530622,42.9081963327607));
#31971=CARTESIAN_POINT('Ctrl Pts',(2.27452890452171,4.36069963709899,42.9137343504586));
#31972=CARTESIAN_POINT('Ctrl Pts',(2.14687199001629,4.42728513164541,42.9218907841386));
#31973=CARTESIAN_POINT('Ctrl Pts',(2.01626533288119,4.48827359741473,42.9300472178187));
#31974=CARTESIAN_POINT('Ctrl Pts',(1.88321831111146,4.54342072179041,42.9382036514988));
#31975=CARTESIAN_POINT('Ctrl Pts',(1.75019836816146,4.5985566221716,42.9463584251146));
#31976=CARTESIAN_POINT('Ctrl Pts',(1.61473936037004,4.64785342484836,42.9545131987305));
#31977=CARTESIAN_POINT('Ctrl Pts',(1.4773710463855,4.69111477729993,42.9626679723464));
#31978=CARTESIAN_POINT('Ctrl Pts',(1.33999786088837,4.73437766393517,42.9708230351562));
#31979=CARTESIAN_POINT('Ctrl Pts',(1.20071555174455,4.77160456796668,42.9789780979659));
#31980=CARTESIAN_POINT('Ctrl Pts',(1.06006994374836,4.80264872511631,42.9871331607757));
#31981=CARTESIAN_POINT('Ctrl Pts',(0.91943258460651,4.83369106152846,42.9952877452917));
#31982=CARTESIAN_POINT('Ctrl Pts',(0.777432413556998,4.85855130532537,43.0034423298077));
#31983=CARTESIAN_POINT('Ctrl Pts',(0.634626325908003,4.87713363451982,43.0115969143237));
#31984=CARTESIAN_POINT('Ctrl Pts',(0.491785127258248,4.8957205324563,43.0197535037656));
#31985=CARTESIAN_POINT('Ctrl Pts',(0.348137948020462,4.90802638808052,43.0279100932075));
#31986=CARTESIAN_POINT('Ctrl Pts',(0.204248317945032,4.91400709066609,43.0360666826493));
#31987=CARTESIAN_POINT('Ctrl Pts',(0.106552666642415,4.91806776296081,43.0416047003474));
#31988=CARTESIAN_POINT('Ctrl Pts',(0.00874537439048287,4.91921367996508,
43.0471427180455));
#31989=CARTESIAN_POINT('Ctrl Pts',(-0.0889967303273905,4.91744472714143,
43.0526807357436));
#31990=CARTESIAN_POINT('Ctrl Pts',(-0.232952029559441,4.91483940025809,
43.0608371694237));
#31991=CARTESIAN_POINT('Ctrl Pts',(-0.376819749187822,4.905907933752,43.0689936031038));
#31992=CARTESIAN_POINT('Ctrl Pts',(-0.52003570499664,4.89067949553318,43.0771500367839));
#31993=CARTESIAN_POINT('Ctrl Pts',(-0.663222512320933,4.87545415673085,
43.0853048103998));
#31994=CARTESIAN_POINT('Ctrl Pts',(-0.805757487907615,4.85393443831742,
43.0934595840157));
#31995=CARTESIAN_POINT('Ctrl Pts',(-0.94708149662502,4.82620137388096,43.1016143576316));
#31996=CARTESIAN_POINT('Ctrl Pts',(-1.08841051713654,4.79846732594277,43.1097694204414));
#31997=CARTESIAN_POINT('Ctrl Pts',(-1.22852815577192,4.76451955182446,43.1179244832513));
#31998=CARTESIAN_POINT('Ctrl Pts',(-1.36688489411388,4.72449031629268,43.1260795460611));
#31999=CARTESIAN_POINT('Ctrl Pts',(-1.5052335178435,4.68446342847256,43.1342341305771));
#32000=CARTESIAN_POINT('Ctrl Pts',(-1.64182112670667,4.63835588673699,43.1423887150931));
#32001=CARTESIAN_POINT('Ctrl Pts',(-1.77611285360357,4.58634998596533,43.1505432996091));
#32002=CARTESIAN_POINT('Ctrl Pts',(-1.91043759811896,4.53433129876944,43.158699889051));
#32003=CARTESIAN_POINT('Ctrl Pts',(-2.04246502045123,4.47641147540973,43.1668564784929));
#32004=CARTESIAN_POINT('Ctrl Pts',(-2.17167916813614,4.41282139375519,43.1750130679348));
#32005=CARTESIAN_POINT('Ctrl Pts',(-2.2594107184132,4.36964611809264,43.1805510856328));
#32006=CARTESIAN_POINT('Ctrl Pts',(-2.34584578144019,4.32385791630896,43.1860891033308));
#32007=CARTESIAN_POINT('Ctrl Pts',(-2.43082902529071,4.27554128880826,43.1916271210288));
#32008=CARTESIAN_POINT('Ctrl Pts',(-2.55599297928736,4.20438020024817,43.1997835547089));
#32009=CARTESIAN_POINT('Ctrl Pts',(-2.67805337935609,4.12770588525251,43.207939988389));
#32010=CARTESIAN_POINT('Ctrl Pts',(-2.79652875741529,4.04581388245298,43.2160964220691));
#32011=CARTESIAN_POINT('Ctrl Pts',(-2.91498002239503,3.9639385469847,43.224251195685));
#32012=CARTESIAN_POINT('Ctrl Pts',(-3.02984744587769,3.87684783239057,43.2324059693009));
#32013=CARTESIAN_POINT('Ctrl Pts',(-3.14067880786713,3.78488040607815,43.2405607429167));
#32014=CARTESIAN_POINT('Ctrl Pts',(-3.25151410028544,3.69290971831139,43.2487158057266));
#32015=CARTESIAN_POINT('Ctrl Pts',(-3.35831278490299,3.59606218355564,43.2568708685364));
#32016=CARTESIAN_POINT('Ctrl Pts',(-3.46065559718248,3.49471685551055,43.2650259313462));
#32017=CARTESIAN_POINT('Ctrl Pts',(-3.56299240706367,3.39337747136139,43.2731805158622));
#32018=CARTESIAN_POINT('Ctrl Pts',(-3.66087363033313,3.2875410578211,43.2813351003782));
#32019=CARTESIAN_POINT('Ctrl Pts',(-3.75391680428009,3.17762359146636,43.2894896848942));
#32020=CARTESIAN_POINT('Ctrl Pts',(-3.84698285427533,3.06767910026755,43.2976462743361));
#32021=CARTESIAN_POINT('Ctrl Pts',(-3.93520826158491,2.95365180664556,43.3058028637779));
#32022=CARTESIAN_POINT('Ctrl Pts',(-4.01825041668673,2.8359912995806,43.3139594532198));
#32023=CARTESIAN_POINT('Ctrl Pts',(-4.07463291919139,2.7561042370862,43.3194974709179));
#32024=CARTESIAN_POINT('Ctrl Pts',(-4.12862683064958,2.67454298974028,43.3250354886159));
#32025=CARTESIAN_POINT('Ctrl Pts',(-4.18013617852421,2.59145607554769,43.3305735063139));
#32026=CARTESIAN_POINT('Ctrl Pts',(-4.25600134786581,2.46908211673472,43.3387301355048));
#32027=CARTESIAN_POINT('Ctrl Pts',(-4.32650323642781,2.34335155656871,43.3468867646957));
#32028=CARTESIAN_POINT('Ctrl Pts',(-4.39136043250718,2.21475430111566,43.3550433938866));
#32029=CARTESIAN_POINT('Ctrl Pts',(-4.45620317192563,2.08618570997482,43.3631982049659));
#32030=CARTESIAN_POINT('Ctrl Pts',(-4.51540357895127,1.95475199723756,43.3713530160451));
#32031=CARTESIAN_POINT('Ctrl Pts',(-4.56872657731634,1.82096692013427,43.3795078271244));
#32032=CARTESIAN_POINT('Ctrl Pts',(-4.62204717503142,1.68718786615712,43.3876622710666));
#32033=CARTESIAN_POINT('Ctrl Pts',(-4.66949076638975,1.55105796907826,43.3958167150089));
#32034=CARTESIAN_POINT('Ctrl Pts',(-4.71087058034712,1.41311055396241,43.4039711589511));
#32035=CARTESIAN_POINT('Ctrl Pts',(-4.72987512545567,1.34975531810086,43.4077162578995));
#32036=CARTESIAN_POINT('Ctrl Pts',(-4.74760132066462,1.2860169573297,43.4114613568478));
#32037=CARTESIAN_POINT('Ctrl Pts',(-4.76403458704966,1.22194824599677,43.4152064557962));
#32038=CARTESIAN_POINT('Ctrl Pts',(-4.91825,1.96574826549505E-7,41.7353816909288));
#32039=CARTESIAN_POINT('Ctrl Pts',(-4.91824999834295,0.0414589360189329,
41.7330369454177));
#32040=CARTESIAN_POINT('Ctrl Pts',(-4.91772577769449,0.0829158324192955,
41.7306889405423));
#32041=CARTESIAN_POINT('Ctrl Pts',(-4.91548943751206,0.171330746432081,
41.7256725857789));
#32042=CARTESIAN_POINT('Ctrl Pts',(-4.91362840060294,0.218280854469932,
41.7230035077778));
#32043=CARTESIAN_POINT('Ctrl Pts',(-4.89973690176757,0.47553305094118,41.7083457066833));
#32044=CARTESIAN_POINT('Ctrl Pts',(-4.8748779851534,0.684920402260462,41.6962822342288));
#32045=CARTESIAN_POINT('Ctrl Pts',(-4.82016070712283,0.981591332392883,
41.6790240941856));
#32046=CARTESIAN_POINT('Ctrl Pts',(-4.80116587870783,1.07064340167463,41.6738235979937));
#32047=CARTESIAN_POINT('Ctrl Pts',(-4.77462291799058,1.18009533524281,41.6674182063602));
#32048=CARTESIAN_POINT('Ctrl Pts',(-4.76939760283999,1.20103934678713,41.6661919108348));
#32049=CARTESIAN_POINT('Ctrl Pts',(-4.76403458703735,1.22194824604475,41.6649672278726));
#32050=CARTESIAN_POINT('Ctrl Pts',(-4.76403458753695,1.22194824409695,41.3199466556564));
#32051=CARTESIAN_POINT('Ctrl Pts',(-4.78146826213841,1.15397922070302,41.3238775906026));
#32052=CARTESIAN_POINT('Ctrl Pts',(-4.79744593121697,1.08564265453963,41.3278086211273));
#32053=CARTESIAN_POINT('Ctrl Pts',(-4.82856266766962,0.938411061313462,
41.3362508087374));
#32054=CARTESIAN_POINT('Ctrl Pts',(-4.84324183803197,0.85944231530701,41.3407623404201));
#32055=CARTESIAN_POINT('Ctrl Pts',(-4.86764476894113,0.707548263030418,
41.3494276890275));
#32056=CARTESIAN_POINT('Ctrl Pts',(-4.87767903794038,0.634694554188753,
41.3535784405592));
#32057=CARTESIAN_POINT('Ctrl Pts',(-4.89329972388572,0.498800862294033,
41.3613209097401));
#32058=CARTESIAN_POINT('Ctrl Pts',(-4.8993102704684,0.435824793795507,41.3649089413183));
#32059=CARTESIAN_POINT('Ctrl Pts',(-4.91353476725405,0.248679868191117,
41.3755781364691));
#32060=CARTESIAN_POINT('Ctrl Pts',(-4.91825326332636,0.124297130125559,
41.3826790327516));
#32061=CARTESIAN_POINT('Ctrl Pts',(-4.91824574010828,-0.1624042430336,41.3990785586708));
#32062=CARTESIAN_POINT('Ctrl Pts',(-4.91021021276699,-0.324580208915229,
41.4083802955372));
#32063=CARTESIAN_POINT('Ctrl Pts',(-4.88910641188229,-0.537074989393775,
41.4205565815289));
#32064=CARTESIAN_POINT('Ctrl Pts',(-4.88324277856568,-0.588006039819476,
41.4234737795619));
#32065=CARTESIAN_POINT('Ctrl Pts',(-4.87216394035304,-0.672576795189148,
41.4283123647917));
#32066=CARTESIAN_POINT('Ctrl Pts',(-4.86739390232583,-0.706270223200602,
41.4302383250399));
#32067=CARTESIAN_POINT('Ctrl Pts',(-4.85179189954285,-0.808797601554587,
41.4360963932494));
#32068=CARTESIAN_POINT('Ctrl Pts',(-4.83984645842322,-0.877453497385237,
41.4400163536086));
#32069=CARTESIAN_POINT('Ctrl Pts',(-4.8035306635876,-1.06276764506488,41.4506201536484));
#32070=CARTESIAN_POINT('Ctrl Pts',(-4.77637297764575,-1.1788313272625,41.4572871740324));
#32071=CARTESIAN_POINT('Ctrl Pts',(-4.72158223677762,-1.3797779098776,41.4689588645705));
#32072=CARTESIAN_POINT('Ctrl Pts',(-4.69580498276877,-1.4651079493051,41.4739565132086));
#32073=CARTESIAN_POINT('Ctrl Pts',(-4.64125945435373,-1.62940110503214,
41.4836895547584));
#32074=CARTESIAN_POINT('Ctrl Pts',(-4.61275798093255,-1.70842057510187,
41.4884218349828));
#32075=CARTESIAN_POINT('Ctrl Pts',(-4.55768556048281,-1.84966397523924,
41.4969901704153));
#32076=CARTESIAN_POINT('Ctrl Pts',(-4.53182761265929,-1.91214352038963,
41.5008200851241));
#32077=CARTESIAN_POINT('Ctrl Pts',(-4.46325790356814,-2.06861484280862,
41.5105206741375));
#32078=CARTESIAN_POINT('Ctrl Pts',(-4.41885999090842,-2.1618312711739,41.5164016534291));
#32079=CARTESIAN_POINT('Ctrl Pts',(-4.29866052499536,-2.39499775533076,
41.5313862491259));
#32080=CARTESIAN_POINT('Ctrl Pts',(-4.218939539997,-2.53279399962172,41.5405044053925));
#32081=CARTESIAN_POINT('Ctrl Pts',(-4.093039384906,-2.72792189764397,41.5537789531341));
#32082=CARTESIAN_POINT('Ctrl Pts',(-4.05203221930347,-2.78846989642242,
41.5579514992963));
#32083=CARTESIAN_POINT('Ctrl Pts',(-3.9876225795225,-2.87914942521153,41.5642752737863));
#32084=CARTESIAN_POINT('Ctrl Pts',(-3.96519455160005,-2.90996004754042,
41.5664373587103));
#32085=CARTESIAN_POINT('Ctrl Pts',(-3.9133204888078,-2.97950888002416,41.5713473573929));
#32086=CARTESIAN_POINT('Ctrl Pts',(-3.88365313393125,-3.01807700826094,
41.5740921488104));
#32087=CARTESIAN_POINT('Ctrl Pts',(-3.81392824469116,-3.10598985877714,
41.5804091673296));
#32088=CARTESIAN_POINT('Ctrl Pts',(-3.77347674232078,-3.15501109885914,
41.5839769189638));
#32089=CARTESIAN_POINT('Ctrl Pts',(-3.61433353977853,-3.3404287153667,41.597680022568));
#32090=CARTESIAN_POINT('Ctrl Pts',(-3.48910572376429,-3.47102461797935,
41.6077826755011));
#32091=CARTESIAN_POINT('Ctrl Pts',(-3.29552091304719,-3.65182080666722,
41.6226752660742));
#32092=CARTESIAN_POINT('Ctrl Pts',(-3.23260775601761,-3.70762729462033,
41.6274128515409));
#32093=CARTESIAN_POINT('Ctrl Pts',(-3.11658926656789,-3.80534156308915,
41.6359858943804));
#32094=CARTESIAN_POINT('Ctrl Pts',(-3.06399109516278,-3.84781905772406,
41.6398151745791));
#32095=CARTESIAN_POINT('Ctrl Pts',(-2.92906990638334,-3.95225828566908,
41.6495033929913));
#32096=CARTESIAN_POINT('Ctrl Pts',(-2.84564497834878,-4.01274224378397,
41.6553725639357));
#32097=CARTESIAN_POINT('Ctrl Pts',(-2.62934323322113,-4.15942366759067,
41.6703010095844));
#32098=CARTESIAN_POINT('Ctrl Pts',(-2.49408883822089,-4.24190660855192,
41.6793746433789));
#32099=CARTESIAN_POINT('Ctrl Pts',(-2.29031221491431,-4.35305618020056,
41.6926441160747));
#32100=CARTESIAN_POINT('Ctrl Pts',(-2.22474380789676,-4.38692868939593,
41.6968553380419));
#32101=CARTESIAN_POINT('Ctrl Pts',(-2.12410379889378,-4.43608229456852,
41.7032235085133));
#32102=CARTESIAN_POINT('Ctrl Pts',(-2.08957541505977,-4.45245075421542,
41.7053915271734));
#32103=CARTESIAN_POINT('Ctrl Pts',(-2.01095020546772,-4.48860758762265,
41.7102891033817));
#32104=CARTESIAN_POINT('Ctrl Pts',(-1.96674540493424,-4.50815166045702,
41.7130156688082));
#32105=CARTESIAN_POINT('Ctrl Pts',(-1.75946466278393,-4.59616662170835,
41.725694401423));
#32106=CARTESIAN_POINT('Ctrl Pts',(-1.59305844408722,-4.65646103651712,
41.735573553184));
#32107=CARTESIAN_POINT('Ctrl Pts',(-1.31732343863914,-4.73985319136102,
41.7517240623595));
#32108=CARTESIAN_POINT('Ctrl Pts',(-1.20982105121891,-4.76842551994967,
41.757967355431));
#32109=CARTESIAN_POINT('Ctrl Pts',(-1.03905534991093,-4.80766521969745,
41.76784349767));
#32110=CARTESIAN_POINT('Ctrl Pts',(-0.976393545826604,-4.82078172258966,
41.7714587199712));
#32111=CARTESIAN_POINT('Ctrl Pts',(-0.842422662975426,-4.84610552273386,
41.7791768761075));
#32112=CARTESIAN_POINT('Ctrl Pts',(-0.771064179777369,-4.85797020850202,
41.7832812456696));
#32113=CARTESIAN_POINT('Ctrl Pts',(-0.659604062264066,-4.87398478606708,
41.7896868500276));
#32114=CARTESIAN_POINT('Ctrl Pts',(-0.61966882467819,-4.87922286191881,
41.7919808347281));
#32115=CARTESIAN_POINT('Ctrl Pts',(-0.388317381686593,-4.90668175349458,
41.8052656342146));
#32116=CARTESIAN_POINT('Ctrl Pts',(-0.195792174507083,-4.91812776017984,
41.816310381747));
#32117=CARTESIAN_POINT('Ctrl Pts',(0.0703404427072187,-4.91829523973346,
41.831524776406));
#32118=CARTESIAN_POINT('Ctrl Pts',(0.143768449695054,-4.91669672222125,
41.8357159642206));
#32119=CARTESIAN_POINT('Ctrl Pts',(0.252195212667689,-4.91190516517075,
41.8418875414384));
#32120=CARTESIAN_POINT('Ctrl Pts',(0.28723949564373,-4.90998047784177,41.8438795131818));
#32121=CARTESIAN_POINT('Ctrl Pts',(0.367011835674681,-4.90474226574988,
41.8484062294555));
#32122=CARTESIAN_POINT('Ctrl Pts',(0.411721264180349,-4.90119169651795,
41.8509380988311));
#32123=CARTESIAN_POINT('Ctrl Pts',(0.512136669721743,-4.89183353431111,
41.8566200353967));
#32124=CARTESIAN_POINT('Ctrl Pts',(0.567804666801672,-4.88568492997573,
41.8597668434518));
#32125=CARTESIAN_POINT('Ctrl Pts',(0.772791134399405,-4.85949302046122,
41.8713639172521));
#32126=CARTESIAN_POINT('Ctrl Pts',(0.921270353701851,-4.83354317513823,
41.8797852251462));
#32127=CARTESIAN_POINT('Ctrl Pts',(1.17326617207594,-4.77746666718741,41.8942693710833));
#32128=CARTESIAN_POINT('Ctrl Pts',(1.27741335768919,-4.75067952679031,41.9003124181546));
#32129=CARTESIAN_POINT('Ctrl Pts',(1.44628443532835,-4.70129005464826,41.9102415177723));
#32130=CARTESIAN_POINT('Ctrl Pts',(1.5115622398915,-4.68071002102609,41.9141120872799));
#32131=CARTESIAN_POINT('Ctrl Pts',(1.65464142399416,-4.63229634138064,41.9226762255247));
#32132=CARTESIAN_POINT('Ctrl Pts',(1.7322137797442,-4.60385086888244,41.9273729490046));
#32133=CARTESIAN_POINT('Ctrl Pts',(1.85425940333453,-4.5555757781442,41.934853965427));
#32134=CARTESIAN_POINT('Ctrl Pts',(1.89921861626164,-4.5370163340833,41.9376299426208));
#32135=CARTESIAN_POINT('Ctrl Pts',(2.10339276094308,-4.44916523608741,41.9503299228384));
#32136=CARTESIAN_POINT('Ctrl Pts',(2.25914398675065,-4.37213914781538,41.960284849285));
#32137=CARTESIAN_POINT('Ctrl Pts',(2.46532365935948,-4.25620945680664,41.9737915474427));
#32138=CARTESIAN_POINT('Ctrl Pts',(2.51955652948589,-4.22433127473398,41.9773762863516));
#32139=CARTESIAN_POINT('Ctrl Pts',(2.60480794058896,-4.1719944195412,41.983057178481));
#32140=CARTESIAN_POINT('Ctrl Pts',(2.63623149898349,-4.152209697445,41.9851609705178));
#32141=CARTESIAN_POINT('Ctrl Pts',(2.7176023189276,-4.09968135243938,41.9906355123418));
#32142=CARTESIAN_POINT('Ctrl Pts',(2.76718258044623,-4.066380485095,41.9939989621819));
#32143=CARTESIAN_POINT('Ctrl Pts',(2.85374281739485,-4.00592538377377,41.9999335679571));
#32144=CARTESIAN_POINT('Ctrl Pts',(2.89097217574454,-3.97914138467089,42.002507123327));
#32145=CARTESIAN_POINT('Ctrl Pts',(3.11348802312907,-3.81428485716825,42.0180358591635));
#32146=CARTESIAN_POINT('Ctrl Pts',(3.28922797512425,-3.66381696173719,42.0309388891167));
#32147=CARTESIAN_POINT('Ctrl Pts',(3.50264312886879,-3.45331621944992,42.0478459158636));
#32148=CARTESIAN_POINT('Ctrl Pts',(3.55053288105708,-3.40405903592437,42.0517286284355));
#32149=CARTESIAN_POINT('Ctrl Pts',(3.65057592248512,-3.29675070719402,42.0600420731277));
#32150=CARTESIAN_POINT('Ctrl Pts',(3.70241120154293,-3.23842876781273,42.0644745158542));
#32151=CARTESIAN_POINT('Ctrl Pts',(3.81303424578794,-3.10783316743587,42.0742228383146));
#32152=CARTESIAN_POINT('Ctrl Pts',(3.87120050215024,-3.03507225320405,42.0795416393546));
#32153=CARTESIAN_POINT('Ctrl Pts',(4.02498294934978,-2.83108549920251,42.0941540510023));
#32154=CARTESIAN_POINT('Ctrl Pts',(4.11622385892783,-2.69670805516866,42.1034587297558));
#32155=CARTESIAN_POINT('Ctrl Pts',(4.22734513521814,-2.51423345371774,42.1156411936139));
#32156=CARTESIAN_POINT('Ctrl Pts',(4.25334981672572,-2.46998627023712,42.1185615790627));
#32157=CARTESIAN_POINT('Ctrl Pts',(4.29543329902736,-2.39574479742117,42.1234028100309));
#32158=CARTESIAN_POINT('Ctrl Pts',(4.31190159806422,-2.36597654064881,42.1253282482596));
#32159=CARTESIAN_POINT('Ctrl Pts',(4.36109527402262,-2.27483374092049,42.1311786574019));
#32160=CARTESIAN_POINT('Ctrl Pts',(4.39282891291845,-2.21293354247245,42.1350915324189));
#32161=CARTESIAN_POINT('Ctrl Pts',(4.47514653178693,-2.04360978529466,42.1456636650785));
#32162=CARTESIAN_POINT('Ctrl Pts',(4.52317095601327,-1.934994096763,42.1523062186312));
#32163=CARTESIAN_POINT('Ctrl Pts',(4.61849258626033,-1.69641050550479,42.1667033427042));
#32164=CARTESIAN_POINT('Ctrl Pts',(4.66433442413089,-1.56597128063498,42.174455701559));
#32165=CARTESIAN_POINT('Ctrl Pts',(4.72301572900435,-1.37342146409309,42.1858057609224));
#32166=CARTESIAN_POINT('Ctrl Pts',(4.74024615203225,-1.31271870740899,42.1893703817511));
#32167=CARTESIAN_POINT('Ctrl Pts',(4.7750972473327,-1.18028907343636,42.197124778236));
#32168=CARTESIAN_POINT('Ctrl Pts',(4.79227982713729,-1.10846285581646,42.2013166561303));
#32169=CARTESIAN_POINT('Ctrl Pts',(4.82489694221028,-0.957134852701533,
42.2101262170268));
#32170=CARTESIAN_POINT('Ctrl Pts',(4.83999841036697,-0.877583519891493,
42.2147447034327));
#32171=CARTESIAN_POINT('Ctrl Pts',(4.88128329827952,-0.626409115539993,
42.2292918013363));
#32172=CARTESIAN_POINT('Ctrl Pts',(4.90034941114294,-0.453751745148835,
42.2392442297513));
#32173=CARTESIAN_POINT('Ctrl Pts',(4.91364998682027,-0.220878031865666,
42.2525589626708));
#32174=CARTESIAN_POINT('Ctrl Pts',(4.91596805240399,-0.161249893960139,
42.255958178116));
#32175=CARTESIAN_POINT('Ctrl Pts',(4.91796763627068,-0.0644689256229611,
42.2614541200559));
#32176=CARTESIAN_POINT('Ctrl Pts',(4.91831421026547,-0.0273364577794288,
42.2635573301803));
#32177=CARTESIAN_POINT('Ctrl Pts',(4.91811482613601,0.0727585668633859,
42.2692137532208));
#32178=CARTESIAN_POINT('Ctrl Pts',(4.91678039762902,0.135712632036464,42.2727583931672));
#32179=CARTESIAN_POINT('Ctrl Pts',(4.91027865480378,0.296574726575932,42.2818043622942));
#32180=CARTESIAN_POINT('Ctrl Pts',(4.90339202350842,0.394385463358169,42.2872941489556));
#32181=CARTESIAN_POINT('Ctrl Pts',(4.87821013162124,0.644890503382736,42.3013983236737));
#32182=CARTESIAN_POINT('Ctrl Pts',(4.8556698595457,0.797049138790904,42.31000967247));
#32183=CARTESIAN_POINT('Ctrl Pts',(4.81193781434942,1.01970183974714,42.3227916363123));
#32184=CARTESIAN_POINT('Ctrl Pts',(4.79623455846469,1.09117884259339,42.3269224504351));
#32185=CARTESIAN_POINT('Ctrl Pts',(4.761889151693,1.23239693843704,42.3351492623066));
#32186=CARTESIAN_POINT('Ctrl Pts',(4.74329471029247,1.30213118950776,42.3392439508935));
#32187=CARTESIAN_POINT('Ctrl Pts',(4.67551976107667,1.53554644809615,42.3530697073029));
#32188=CARTESIAN_POINT('Ctrl Pts',(4.61934581909466,1.69706534359335,42.3628420665752));
#32189=CARTESIAN_POINT('Ctrl Pts',(4.50793384068396,1.97058445732451,42.379749043948));
#32190=CARTESIAN_POINT('Ctrl Pts',(4.45662949106227,2.08401648138289,42.3868714550785));
#32191=CARTESIAN_POINT('Ctrl Pts',(4.38199739879884,2.23363135011527,42.396389986966));
#32192=CARTESIAN_POINT('Ctrl Pts',(4.36241905275076,2.2716316330271,42.3988185436065));
#32193=CARTESIAN_POINT('Ctrl Pts',(4.32264400770027,2.34642125744497,42.4036176959562));
#32194=CARTESIAN_POINT('Ctrl Pts',(4.30246683418375,2.38321697022707,42.4059882827341));
#32195=CARTESIAN_POINT('Ctrl Pts',(4.26897887899566,2.44247491864791,42.4098257045104));
#32196=CARTESIAN_POINT('Ctrl Pts',(4.25595590086876,2.46509711315591,42.4112953992567));
#32197=CARTESIAN_POINT('Ctrl Pts',(4.22304820135549,2.52122286989272,42.4149550547808));
#32198=CARTESIAN_POINT('Ctrl Pts',(4.20294428298014,2.55459590699801,42.4171431101807));
#32199=CARTESIAN_POINT('Ctrl Pts',(4.09959651579776,2.7216330402359,42.4281650431971));
#32200=CARTESIAN_POINT('Ctrl Pts',(4.01036416074755,2.85148336686231,42.4369659108808));
#32201=CARTESIAN_POINT('Ctrl Pts',(3.85314607296535,3.05825296477085,42.4515444357786));
#32202=CARTESIAN_POINT('Ctrl Pts',(3.78871071201494,3.13772475324658,42.4572964803272));
#32203=CARTESIAN_POINT('Ctrl Pts',(3.67727937162022,3.26671808171373,42.466918262427));
#32204=CARTESIAN_POINT('Ctrl Pts',(3.6316463498605,3.31737475322205,42.470774777077));
#32205=CARTESIAN_POINT('Ctrl Pts',(3.52687976890691,3.42892160478497,42.4794533848701));
#32206=CARTESIAN_POINT('Ctrl Pts',(3.46719346185386,3.48926260437263,42.4842794034255));
#32207=CARTESIAN_POINT('Ctrl Pts',(3.3302643955707,3.62070945306302,42.495101915236));
#32208=CARTESIAN_POINT('Ctrl Pts',(3.25224577050737,3.69094771674969,42.5011024751879));
#32209=CARTESIAN_POINT('Ctrl Pts',(3.06031456817439,3.85292498969766,42.5154772245449));
#32210=CARTESIAN_POINT('Ctrl Pts',(2.94443930401921,3.94218644690316,42.5238516332486));
#32211=CARTESIAN_POINT('Ctrl Pts',(2.78817973782896,4.05181855244548,42.5347233063918));
#32212=CARTESIAN_POINT('Ctrl Pts',(2.75125136656222,4.07698366603932,42.5372631715959));
#32213=CARTESIAN_POINT('Ctrl Pts',(2.68024814915421,4.12396525308612,42.5420884841774));
#32214=CARTESIAN_POINT('Ctrl Pts',(2.64623720515661,4.14587122816908,42.5443747948112));
#32215=CARTESIAN_POINT('Ctrl Pts',(2.50070328490251,4.23708704330978,42.5540622592568));
#32216=CARTESIAN_POINT('Ctrl Pts',(2.3866978821204,4.30233628899259,42.5614168332966));
#32217=CARTESIAN_POINT('Ctrl Pts',(2.12034410681707,4.44093093359853,42.5782377961459));
#32218=CARTESIAN_POINT('Ctrl Pts',(1.96655363436262,4.51114094362899,42.5876958784504));
#32219=CARTESIAN_POINT('Ctrl Pts',(1.74207641943565,4.59995692338875,42.6012972717376));
#32220=CARTESIAN_POINT('Ctrl Pts',(1.67411537574065,4.6251239438558,42.6053887537905));
#32221=CARTESIAN_POINT('Ctrl Pts',(1.53676941519557,4.67256131950116,42.6136153181782));
#32222=CARTESIAN_POINT('Ctrl Pts',(1.46739589457291,4.69480975555188,42.6177495008221));
#32223=CARTESIAN_POINT('Ctrl Pts',(1.25647007972896,4.75732269014025,42.6302658115973));
#32224=CARTESIAN_POINT('Ctrl Pts',(1.1135817956926,4.79278321057714,42.6386752162634));
#32225=CARTESIAN_POINT('Ctrl Pts',(0.82283836947627,4.85123121956217,42.655650466277));
#32226=CARTESIAN_POINT('Ctrl Pts',(0.675088926216493,4.87398840557148,42.664207994878));
#32227=CARTESIAN_POINT('Ctrl Pts',(0.485613891280755,4.89439025113594,42.6750528853812));
#32228=CARTESIAN_POINT('Ctrl Pts',(0.44464152595815,4.89828242925173,42.677390146362));
#32229=CARTESIAN_POINT('Ctrl Pts',(0.373172931873519,4.9041674755618,42.6814514838657));
#32230=CARTESIAN_POINT('Ctrl Pts',(0.342698195547312,4.906391202701,42.6831784322127));
#32231=CARTESIAN_POINT('Ctrl Pts',(0.267370112003826,4.91118260147091,42.6874377134781));
#32232=CARTESIAN_POINT('Ctrl Pts',(0.222498420766049,4.91341997237629,42.6899666637));
#32233=CARTESIAN_POINT('Ctrl Pts',(0.0881691570063345,4.91827388017301,
42.6975219476056));
#32234=CARTESIAN_POINT('Ctrl Pts',(-0.00133584464349756,4.91906395062976,
42.7025358593237));
#32235=CARTESIAN_POINT('Ctrl Pts',(-0.267548819225381,4.91414763037331,
42.7174524170193));
#32236=CARTESIAN_POINT('Ctrl Pts',(-0.443978456498547,4.90135811955894,
42.7273472855319));
#32237=CARTESIAN_POINT('Ctrl Pts',(-0.688651192920981,4.87030027957279,
42.7412487119144));
#32238=CARTESIAN_POINT('Ctrl Pts',(-0.757771915560402,4.86002539675946,
42.7451953835747));
#32239=CARTESIAN_POINT('Ctrl Pts',(-0.892579329077979,4.83704024000851,
42.7529396669971));
#32240=CARTESIAN_POINT('Ctrl Pts',(-0.958272284839683,4.82445543459781,
42.7567356097733));
#32241=CARTESIAN_POINT('Ctrl Pts',(-1.03624041182122,4.8078637229758,42.7612702051106));
#32242=CARTESIAN_POINT('Ctrl Pts',(-1.04878265084448,4.8051433610489,42.7620005632548));
#32243=CARTESIAN_POINT('Ctrl Pts',(-1.14409409369169,4.78407974174795,42.7675577146463));
#32244=CARTESIAN_POINT('Ctrl Pts',(-1.2263866504212,4.76364837644357,42.7723962213351));
#32245=CARTESIAN_POINT('Ctrl Pts',(-1.46839870945811,4.69687522113875,42.7867494447251));
#32246=CARTESIAN_POINT('Ctrl Pts',(-1.62634219057828,4.64454979553626,42.7962818887211));
#32247=CARTESIAN_POINT('Ctrl Pts',(-1.83466955684611,4.56360002301108,42.8090373401861));
#32248=CARTESIAN_POINT('Ctrl Pts',(-1.8876422479082,4.54194500264105,42.8122966466697));
#32249=CARTESIAN_POINT('Ctrl Pts',(-1.95666861961231,4.5123110696327,42.8165611780751));
#32250=CARTESIAN_POINT('Ctrl Pts',(-1.97307327511633,4.50516205399251,42.8175759824567));
#32251=CARTESIAN_POINT('Ctrl Pts',(-2.02355886129832,4.48283220070061,42.8207028098465));
#32252=CARTESIAN_POINT('Ctrl Pts',(-2.05750652017929,4.46735290334963,42.8228107355714));
#32253=CARTESIAN_POINT('Ctrl Pts',(-2.13523119218239,4.43083845345193,42.8276536085707));
#32254=CARTESIAN_POINT('Ctrl Pts',(-2.17887940099541,4.40953810049727,42.8303856012945));
#32255=CARTESIAN_POINT('Ctrl Pts',(-2.31696911647927,4.33959916798679,42.8390806380816));
#32256=CARTESIAN_POINT('Ctrl Pts',(-2.41015364556278,4.28854595845796,42.8450270439978));
#32257=CARTESIAN_POINT('Ctrl Pts',(-2.63199588235986,4.15748887254156,42.8594622899541));
#32258=CARTESIAN_POINT('Ctrl Pts',(-2.75875114599003,4.07448246509674,42.867949850611));
#32259=CARTESIAN_POINT('Ctrl Pts',(-2.93795315082703,3.94492985015892,42.8804142172744));
#32260=CARTESIAN_POINT('Ctrl Pts',(-2.99355816187002,3.90290271797784,42.8843509852368));
#32261=CARTESIAN_POINT('Ctrl Pts',(-3.08440312362127,3.83115682498211,42.890906758271));
#32262=CARTESIAN_POINT('Ctrl Pts',(-3.12015226109768,3.80209877189608,42.8935197178163));
#32263=CARTESIAN_POINT('Ctrl Pts',(-3.24396531794798,3.69853717286071,42.90268991511));
#32264=CARTESIAN_POINT('Ctrl Pts',(-3.32981107334528,3.62144251197732,42.9092671208973));
#32265=CARTESIAN_POINT('Ctrl Pts',(-3.53288014011062,3.42574388892629,42.9253893071764));
#32266=CARTESIAN_POINT('Ctrl Pts',(-3.6469373827041,3.30405978711162,42.9349444609925));
#32267=CARTESIAN_POINT('Ctrl Pts',(-3.79268107286734,3.13180934805247,42.9478233518442));
#32268=CARTESIAN_POINT('Ctrl Pts',(-3.82995358195832,3.0861165228147,42.9511820532796));
#32269=CARTESIAN_POINT('Ctrl Pts',(-3.87143139036323,3.03335926540453,42.9549920174652));
#32270=CARTESIAN_POINT('Ctrl Pts',(-3.87645106761062,3.02694178407111,42.9554543419386));
#32271=CARTESIAN_POINT('Ctrl Pts',(-3.8857439279696,3.01500015990591,42.9563125299532));
#32272=CARTESIAN_POINT('Ctrl Pts',(-3.89002133424432,3.00947933327095,42.9567084549936));
#32273=CARTESIAN_POINT('Ctrl Pts',(-3.8988101777436,2.99808557321972,42.9575238358861));
#32274=CARTESIAN_POINT('Ctrl Pts',(-3.90332012976419,2.99221153517322,42.9579432639995));
#32275=CARTESIAN_POINT('Ctrl Pts',(-3.91893154896809,2.97178290833572,42.9593987236394));
#32276=CARTESIAN_POINT('Ctrl Pts',(-3.92996504307406,2.95717650889248,42.9604337221512));
#32277=CARTESIAN_POINT('Ctrl Pts',(-3.98092501990951,2.88892555672449,42.9652447742594));
#32278=CARTESIAN_POINT('Ctrl Pts',(-4.0198366551823,2.83453141035297,42.9690072756262));
#32279=CARTESIAN_POINT('Ctrl Pts',(-4.12204467152367,2.68531648394671,42.9791645813815));
#32280=CARTESIAN_POINT('Ctrl Pts',(-4.18317332321165,2.58906123063226,42.985543652617));
#32281=CARTESIAN_POINT('Ctrl Pts',(-4.31291479187739,2.3681571857558,42.9998980479385));
#32282=CARTESIAN_POINT('Ctrl Pts',(-4.37957514475913,2.2424815012222,43.0078718919144));
#32283=CARTESIAN_POINT('Ctrl Pts',(-4.47047247709351,2.05155002280497,43.0197932973901));
#32284=CARTESIAN_POINT('Ctrl Pts',(-4.49892386330193,1.9883826579067,43.0237068213598));
#32285=CARTESIAN_POINT('Ctrl Pts',(-4.5501795236974,1.86784831648449,43.031125494135));
#32286=CARTESIAN_POINT('Ctrl Pts',(-4.57325664898741,1.81061165126279,43.0346279032179));
#32287=CARTESIAN_POINT('Ctrl Pts',(-4.65598482595438,1.59374561061086,43.0478294624908));
#32288=CARTESIAN_POINT('Ctrl Pts',(-4.70840320228429,1.43148792899286,43.0575726033839));
#32289=CARTESIAN_POINT('Ctrl Pts',(-4.75627833364298,1.2518940575934,43.0682126656554));
#32290=CARTESIAN_POINT('Ctrl Pts',(-4.76019186091467,1.23692996090985,43.0690981020617));
#32291=CARTESIAN_POINT('Ctrl Pts',(-4.76403458776301,1.22194824321562,43.0699834446552));
#32292=CARTESIAN_POINT('Origin',(0.,0.,-3.23514056400928));
#32293=CARTESIAN_POINT('',(-4.76410171059494,1.22196554825755,45.1652160615516));
#32294=CARTESIAN_POINT('',(-4.76403458711239,1.22194824575222,44.8197276177568));
#32295=CARTESIAN_POINT('',(-4.76403458704967,1.22194824599672,-3.23514056400928));
#32296=CARTESIAN_POINT('',(-4.91826402150649,8.74528832110429E-5,43.4851405645849));
#32297=CARTESIAN_POINT('Ctrl Pts',(-4.91853989040247,8.72578364425628E-5,
43.4851405759104));
#32298=CARTESIAN_POINT('Ctrl Pts',(-4.91793986603997,-0.725688019748913,
43.5262491429017));
#32299=CARTESIAN_POINT('Ctrl Pts',(-4.57197699803157,-2.26971971343868,
43.6136731716547));
#32300=CARTESIAN_POINT('Ctrl Pts',(-3.0169439135882,-4.14532980999643,43.7474126621693));
#32301=CARTESIAN_POINT('Ctrl Pts',(-0.665975355898803,-5.08352108648301,
43.8863590474545));
#32302=CARTESIAN_POINT('Ctrl Pts',(1.84732758978621,-4.78258200007033,44.0253054327396));
#32303=CARTESIAN_POINT('Ctrl Pts',(3.91033640512676,-3.31586776125381,44.1642518180246));
#32304=CARTESIAN_POINT('Ctrl Pts',(5.02018372348306,-1.04089634155263,44.3031982033099));
#32305=CARTESIAN_POINT('Ctrl Pts',(4.90633943649889,1.48779808617899,44.4421445885949));
#32306=CARTESIAN_POINT('Ctrl Pts',(3.59655358400776,3.65383526294536,44.5810909738801));
#32307=CARTESIAN_POINT('Ctrl Pts',(1.41009216119427,4.9292342111448,44.7200373591652));
#32308=CARTESIAN_POINT('Ctrl Pts',(-1.12008535558171,5.00311089299382,44.8589837444503));
#32309=CARTESIAN_POINT('Ctrl Pts',(-3.37723719792296,3.85745754614969,44.9979301297354));
#32310=CARTESIAN_POINT('Ctrl Pts',(-4.43068290595709,2.32502529465259,45.1000075687692));
#32311=CARTESIAN_POINT('Ctrl Pts',(-4.72283062116011,1.38357984648488,45.1557695460413));
#32312=CARTESIAN_POINT('Ctrl Pts',(-4.76410171059494,1.22196554825755,45.1652160615516));
#32313=CARTESIAN_POINT('Ctrl Pts',(-4.76403458704966,1.22194824599677,43.4152064557962));
#32314=CARTESIAN_POINT('Ctrl Pts',(-4.79981655617157,1.08244435207326,43.4233610741045));
#32315=CARTESIAN_POINT('Ctrl Pts',(-4.8294652316512,0.941373571802003,43.4315156924128));
#32316=CARTESIAN_POINT('Ctrl Pts',(-4.85286714489056,0.79928939473872,43.4396703107211));
#32317=CARTESIAN_POINT('Ctrl Pts',(-4.87627408384022,0.657174704191096,
43.4478266802858));
#32318=CARTESIAN_POINT('Ctrl Pts',(-4.89343152795028,0.514046512543163,
43.4559830498505));
#32319=CARTESIAN_POINT('Ctrl Pts',(-4.90427748832079,0.370466435794071,
43.4641394194152));
#32320=CARTESIAN_POINT('Ctrl Pts',(-4.90666238876036,0.338894848174818,
43.4659329101431));
#32321=CARTESIAN_POINT('Ctrl Pts',(-4.90874232238476,0.307301430314587,
43.4677264008711));
#32322=CARTESIAN_POINT('Ctrl Pts',(-4.91051696718809,0.275692178811611,
43.469519891599));
#32323=CARTESIAN_POINT('Ctrl Pts',(-4.91566914420344,0.183923697163315,
43.4747267824024));
#32324=CARTESIAN_POINT('Ctrl Pts',(-4.9182483645321,0.0920101472215629,
43.4799336732058));
#32325=CARTESIAN_POINT('Ctrl Pts',(-4.91824999922231,8.74627973450961E-5,
43.4851405640092));
#32326=CARTESIAN_POINT('',(-4.91824996470145,0.000108738790900998,43.139742923523));
#32327=CARTESIAN_POINT('Ctrl Pts',(-4.76403458776301,1.22194824321562,43.0699834446552));
#32328=CARTESIAN_POINT('Ctrl Pts',(-4.79189833239463,1.11331529259219,43.0764030942714));
#32329=CARTESIAN_POINT('Ctrl Pts',(-4.81603955611608,1.00375592104383,43.0828186703034));
#32330=CARTESIAN_POINT('Ctrl Pts',(-4.84411789010124,0.851764604974871,
43.0916172854435));
#32331=CARTESIAN_POINT('Ctrl Pts',(-4.8512814194585,0.809968962579472,43.0940262068267));
#32332=CARTESIAN_POINT('Ctrl Pts',(-4.86304828365612,0.735547190689884,
43.0982946416439));
#32333=CARTESIAN_POINT('Ctrl Pts',(-4.86786593734639,0.702957695771933,
43.1001567008045));
#32334=CARTESIAN_POINT('Ctrl Pts',(-4.87850356111361,0.625636224684664,
43.1045608288938));
#32335=CARTESIAN_POINT('Ctrl Pts',(-4.88403629378671,0.58086763831187,43.1070999139326));
#32336=CARTESIAN_POINT('Ctrl Pts',(-4.9084655631868,0.358055942048074,43.1196982949649));
#32337=CARTESIAN_POINT('Ctrl Pts',(-4.91824603941655,0.179149652822579,
43.1296969762547));
#32338=CARTESIAN_POINT('Ctrl Pts',(-4.91824999879737,0.0001087641201062,
43.1397428629973));
#32339=CARTESIAN_POINT('Ctrl Pts',(-4.91824999879801,0.000108735485710791,
43.1397428646039));
#32340=CARTESIAN_POINT('Ctrl Pts',(-4.91825152194942,-0.0687854197295842,
43.1436084781282));
#32341=CARTESIAN_POINT('Ctrl Pts',(-4.9168054561655,-0.137671642017828,
43.1474788561221));
#32342=CARTESIAN_POINT('Ctrl Pts',(-4.91160569186403,-0.261403590180769,
43.1544514189466));
#32343=CARTESIAN_POINT('Ctrl Pts',(-4.90837874198007,-0.316259967515485,
43.1575499875871));
#32344=CARTESIAN_POINT('Ctrl Pts',(-4.89945320902016,-0.434230174882583,
43.164234601591));
#32345=CARTESIAN_POINT('Ctrl Pts',(-4.89345267333092,-0.497311184277488,
43.1678220396809));
#32346=CARTESIAN_POINT('Ctrl Pts',(-4.87562860837595,-0.652761965568253,
43.176701583363));
#32347=CARTESIAN_POINT('Ctrl Pts',(-4.86239746973484,-0.74494498870768,
43.1820016202339));
#32348=CARTESIAN_POINT('Ctrl Pts',(-4.81391824608007,-1.02576070165565,
43.1982653853273));
#32349=CARTESIAN_POINT('Ctrl Pts',(-4.77024343597705,-1.21275342141534,
43.2092662593913));
#32350=CARTESIAN_POINT('Ctrl Pts',(-4.69748845637275,-1.45839771490939,
43.2239010116868));
#32351=CARTESIAN_POINT('Ctrl Pts',(-4.67801035633782,-1.51971738745896,
43.2275691629555));
#32352=CARTESIAN_POINT('Ctrl Pts',(-4.64530932989608,-1.61607066537207,
43.2333509970956));
#32353=CARTESIAN_POINT('Ctrl Pts',(-4.63287982700165,-1.65136541355251,
43.2354725534302));
#32354=CARTESIAN_POINT('Ctrl Pts',(-4.60218738190195,-1.73544445172709,
43.2405349039856));
#32355=CARTESIAN_POINT('Ctrl Pts',(-4.58354985423037,-1.78408715263861,
43.2434712945121));
#32356=CARTESIAN_POINT('Ctrl Pts',(-4.50325552019519,-1.98408160034568,
43.2555962912099));
#32357=CARTESIAN_POINT('Ctrl Pts',(-4.43484659970565,-2.13261025295212,
43.264728842634));
#32358=CARTESIAN_POINT('Ctrl Pts',(-4.31766666575353,-2.35689859237798,
43.2789143731951));
#32359=CARTESIAN_POINT('Ctrl Pts',(-4.27399931413035,-2.43518912683911,
43.2839439081805));
#32360=CARTESIAN_POINT('Ctrl Pts',(-4.1889920758613,-2.57826015933935,43.2933092356987));
#32361=CARTESIAN_POINT('Ctrl Pts',(-4.14822629805028,-2.64334985518144,
43.2976398604482));
#32362=CARTESIAN_POINT('Ctrl Pts',(-4.10154774336163,-2.71413950040063,
43.3024353799353));
#32363=CARTESIAN_POINT('Ctrl Pts',(-4.09712557371794,-2.72081038510047,
43.3028881406173));
#32364=CARTESIAN_POINT('Ctrl Pts',(-4.05424209950545,-2.78515888950665,
43.3072638649707));
#32365=CARTESIAN_POINT('Ctrl Pts',(-4.01458193948964,-2.8420275766671,43.3111957826454));
#32366=CARTESIAN_POINT('Ctrl Pts',(-3.85883546036585,-3.05558408193904,
43.3262232539209));
#32367=CARTESIAN_POINT('Ctrl Pts',(-3.73467142405501,-3.2061554208934,43.3373783649993));
#32368=CARTESIAN_POINT('Ctrl Pts',(-3.54715267866821,-3.40783732797696,
43.3531416420693));
#32369=CARTESIAN_POINT('Ctrl Pts',(-3.49096980813066,-3.4653682783922,43.3577412841364));
#32370=CARTESIAN_POINT('Ctrl Pts',(-3.42012805940218,-3.53443783255248,
43.3633868034433));
#32371=CARTESIAN_POINT('Ctrl Pts',(-3.40678135616785,-3.54730426230337,
43.3644439141571));
#32372=CARTESIAN_POINT('Ctrl Pts',(-3.38327652929071,-3.56970826894852,
43.3662940902315));
#32373=CARTESIAN_POINT('Ctrl Pts',(-3.37315003515859,-3.57927870400781,
43.3670875064247));
#32374=CARTESIAN_POINT('Ctrl Pts',(-3.33409833211508,-3.61587310702537,
43.3701329697306));
#32375=CARTESIAN_POINT('Ctrl Pts',(-3.30488771661572,-3.64259073257102,
43.3723811388362));
#32376=CARTESIAN_POINT('Ctrl Pts',(-3.2433600458981,-3.69751787899867,43.3770530295919));
#32377=CARTESIAN_POINT('Ctrl Pts',(-3.21099000400205,-3.72566317654222,
43.3794756011215));
#32378=CARTESIAN_POINT('Ctrl Pts',(-3.08418950153598,-3.8330341975231,43.3888408558411));
#32379=CARTESIAN_POINT('Ctrl Pts',(-2.9871612144794,-3.90912324501609,43.3957457254493));
#32380=CARTESIAN_POINT('Ctrl Pts',(-2.79082122974245,-4.05150908185092,
43.4093332183293));
#32381=CARTESIAN_POINT('Ctrl Pts',(-2.6917514812885,-4.11799498736891,43.4160112617119));
#32382=CARTESIAN_POINT('Ctrl Pts',(-2.53056583311945,-4.21786297190447,
43.4266641301714));
#32383=CARTESIAN_POINT('Ctrl Pts',(-2.46998067228436,-4.25362514070655,
43.4306226212917));
#32384=CARTESIAN_POINT('Ctrl Pts',(-2.35533552972503,-4.31802232909803,
43.438040267627));
#32385=CARTESIAN_POINT('Ctrl Pts',(-2.30146783739031,-4.3469722781125,43.4414963826605));
#32386=CARTESIAN_POINT('Ctrl Pts',(-2.17971443465775,-4.40950819080015,
43.4492497933608));
#32387=CARTESIAN_POINT('Ctrl Pts',(-2.11156464249852,-4.44254567513833,
43.4535502341621));
#32388=CARTESIAN_POINT('Ctrl Pts',(-1.85495803309457,-4.55970383136814,
43.4696100326151));
#32389=CARTESIAN_POINT('Ctrl Pts',(-1.66202950947703,-4.63351103337953,
43.481431899591));
#32390=CARTESIAN_POINT('Ctrl Pts',(-1.40518128028971,-4.71365893260436,
43.496821811754));
#32391=CARTESIAN_POINT('Ctrl Pts',(-1.34497087940044,-4.73119101145091,
43.5004044386737));
#32392=CARTESIAN_POINT('Ctrl Pts',(-1.28044691334274,-4.74864779581115,
43.5042140730092));
#32393=CARTESIAN_POINT('Ctrl Pts',(-1.27645103650703,-4.74972345910679,
43.5044498773198));
#32394=CARTESIAN_POINT('Ctrl Pts',(-1.26994867456583,-4.75146505326014,
43.504833395909));
#32395=CARTESIAN_POINT('Ctrl Pts',(-1.26744301332547,-4.75213404654851,
43.5049811355492));
#32396=CARTESIAN_POINT('Ctrl Pts',(-1.26026571492561,-4.75404425253578,
43.5054041881589));
#32397=CARTESIAN_POINT('Ctrl Pts',(-1.2555927731346,-4.75528056116606,43.5056794591307));
#32398=CARTESIAN_POINT('Ctrl Pts',(-1.24693613082025,-4.75755717781354,
43.5061890875975));
#32399=CARTESIAN_POINT('Ctrl Pts',(-1.24295293264208,-4.75859937605481,
43.5064234617508));
#32400=CARTESIAN_POINT('Ctrl Pts',(-1.23550191162642,-4.76053893166058,
43.506861654641));
#32401=CARTESIAN_POINT('Ctrl Pts',(-1.23203440854394,-4.76143750454435,
43.5070654845116));
#32402=CARTESIAN_POINT('Ctrl Pts',(-1.2254779833316,-4.76312890281656,43.5074507127246));
#32403=CARTESIAN_POINT('Ctrl Pts',(-1.22238926604898,-4.76392251351199,
43.5076321184935));
#32404=CARTESIAN_POINT('Ctrl Pts',(-1.21647893336233,-4.76543497966646,
43.5079790994748));
#32405=CARTESIAN_POINT('Ctrl Pts',(-1.21365744738248,-4.76615433459436,
43.5081446795374));
#32406=CARTESIAN_POINT('Ctrl Pts',(-1.20818530755234,-4.76754431555724,
43.5084656926403));
#32407=CARTESIAN_POINT('Ctrl Pts',(-1.20553473012765,-4.76821523766048,
43.5086211286155));
#32408=CARTESIAN_POINT('Ctrl Pts',(-1.20031339704241,-4.76953224515539,
43.508927210094));
#32409=CARTESIAN_POINT('Ctrl Pts',(-1.1977426758357,-4.77017846324344,43.5090778569212));
#32410=CARTESIAN_POINT('Ctrl Pts',(-1.19258302455681,-4.77147104280929,
43.5093801121957));
#32411=CARTESIAN_POINT('Ctrl Pts',(-1.1899940883102,-4.77211737624181,43.5095317203012));
#32412=CARTESIAN_POINT('Ctrl Pts',(-1.18467288872386,-4.77344122552053,
43.509843219756));
#32413=CARTESIAN_POINT('Ctrl Pts',(-1.18194056694358,-4.77411850324285,
43.5100031084844));
#32414=CARTESIAN_POINT('Ctrl Pts',(-1.17613687005925,-4.77555181422003,
43.5103425993022));
#32415=CARTESIAN_POINT('Ctrl Pts',(-1.17306534360852,-4.77630723122596,
43.5105221945211));
#32416=CARTESIAN_POINT('Ctrl Pts',(-1.16499849169799,-4.77828295721755,
43.5109936715882));
#32417=CARTESIAN_POINT('Ctrl Pts',(-1.16000197425946,-4.77949839676865,
43.5112854981055));
#32418=CARTESIAN_POINT('Ctrl Pts',(-1.14101242568745,-4.78408621206411,
43.5123938292887));
#32419=CARTESIAN_POINT('Ctrl Pts',(-1.1270064778424,-4.78740500087081,43.513209693763));
#32420=CARTESIAN_POINT('Ctrl Pts',(-1.09857621702696,-4.79401003440417,
43.5148624930978));
#32421=CARTESIAN_POINT('Ctrl Pts',(-1.08415126491305,-4.79729277321717,
43.5156993958202));
#32422=CARTESIAN_POINT('Ctrl Pts',(-1.0109486525758,-4.81360472404153,43.5199384505068));
#32423=CARTESIAN_POINT('Ctrl Pts',(-0.951949604644167,-4.82561909995732,
43.5233289638008));
#32424=CARTESIAN_POINT('Ctrl Pts',(-0.718843264655956,-4.8686465656558,
43.5366521493606));
#32425=CARTESIAN_POINT('Ctrl Pts',(-0.543336824073945,-4.8913434457931,
43.5465286802935));
#32426=CARTESIAN_POINT('Ctrl Pts',(-0.28768509905184,-4.91047296356192,
43.5609121230679));
#32427=CARTESIAN_POINT('Ctrl Pts',(-0.20824910604204,-4.91448263746963,
43.5653800949922));
#32428=CARTESIAN_POINT('Ctrl Pts',(-0.0625257815231578,-4.91829873303621,
43.5735917279016));
#32429=CARTESIAN_POINT('Ctrl Pts',(0.00372761654206807,-4.91869473374925,
43.5773308871879));
#32430=CARTESIAN_POINT('Ctrl Pts',(0.133591835348735,-4.9168470646973,43.5846792309233));
#32431=CARTESIAN_POINT('Ctrl Pts',(0.197191344654252,-4.91470724423495,
43.5882870112361));
#32432=CARTESIAN_POINT('Ctrl Pts',(0.264306035919613,-4.91114428612059,
43.5921062525523));
#32433=CARTESIAN_POINT('Ctrl Pts',(0.267880906296425,-4.91095059023615,
43.5923097206624));
#32434=CARTESIAN_POINT('Ctrl Pts',(0.277024215157225,-4.91044516835131,
43.5928302157821));
#32435=CARTESIAN_POINT('Ctrl Pts',(0.282592338782104,-4.91012787380908,
43.5931472764935));
#32436=CARTESIAN_POINT('Ctrl Pts',(0.419981805093912,-4.90206438304695,
43.6009727177338));
#32437=CARTESIAN_POINT('Ctrl Pts',(0.551437185719577,-4.88902201066443,
43.608511856771));
#32438=CARTESIAN_POINT('Ctrl Pts',(0.800702634722884,-4.85410909537207,
43.6229133671223));
#32439=CARTESIAN_POINT('Ctrl Pts',(0.918553642928687,-4.83319346971291,
43.6297678095367));
#32440=CARTESIAN_POINT('Ctrl Pts',(1.10378012428121,-4.79330026578439,43.6405936498856));
#32441=CARTESIAN_POINT('Ctrl Pts',(1.17171561318913,-4.77714775757889,43.6445753914178));
#32442=CARTESIAN_POINT('Ctrl Pts',(1.27222541599587,-4.75097718474871,43.6504761216196));
#32443=CARTESIAN_POINT('Ctrl Pts',(1.30507640472475,-4.74205834412482,43.6524061444718));
#32444=CARTESIAN_POINT('Ctrl Pts',(1.38710409641628,-4.7188713645488,43.6572284453613));
#32445=CARTESIAN_POINT('Ctrl Pts',(1.43615557325238,-4.70417495287262,43.6601156540084));
#32446=CARTESIAN_POINT('Ctrl Pts',(1.63961572576907,-4.63973682689297,43.6721257048677));
#32447=CARTESIAN_POINT('Ctrl Pts',(1.79174573737449,-4.58313708931061,43.6811916988123));
#32448=CARTESIAN_POINT('Ctrl Pts',(2.02467078138749,-4.48310414457963,43.6954006543413));
#32449=CARTESIAN_POINT('Ctrl Pts',(2.10752090735759,-4.44475758323726,43.7005218232959));
#32450=CARTESIAN_POINT('Ctrl Pts',(2.25977492548273,-4.36907337798522,43.7100889134839));
#32451=CARTESIAN_POINT('Ctrl Pts',(2.32944172869235,-4.33233031184398,43.714529606242));
#32452=CARTESIAN_POINT('Ctrl Pts',(2.45797913870795,-4.26054110918708,43.7228557515115));
#32453=CARTESIAN_POINT('Ctrl Pts',(2.5170583063794,-4.22590692402754,43.7267371005422));
#32454=CARTESIAN_POINT('Ctrl Pts',(2.6778979148647,-4.1270476308415,43.7374642158904));
#32455=CARTESIAN_POINT('Ctrl Pts',(2.77805364377879,-4.06030500447411,43.7443267719396));
#32456=CARTESIAN_POINT('Ctrl Pts',(2.98593512170801,-3.91047975207628,43.7589792175998));
#32457=CARTESIAN_POINT('Ctrl Pts',(3.09286788981614,-3.82646424809568,43.7667680185261));
#32458=CARTESIAN_POINT('Ctrl Pts',(3.23710332245792,-3.70313971808879,43.7776142300466));
#32459=CARTESIAN_POINT('Ctrl Pts',(3.27744670811001,-3.66748208397733,43.7806872929668));
#32460=CARTESIAN_POINT('Ctrl Pts',(3.34946688956328,-3.60168919332307,43.7862419467441));
#32461=CARTESIAN_POINT('Ctrl Pts',(3.38134289213546,-3.57178019971043,43.7887257731442));
#32462=CARTESIAN_POINT('Ctrl Pts',(3.43845085668424,-3.51674653172386,43.7932198893034));
#32463=CARTESIAN_POINT('Ctrl Pts',(3.46381666399771,-3.49176525674311,43.7952322845823));
#32464=CARTESIAN_POINT('Ctrl Pts',(3.53761271156044,-3.41749238387668,43.8011398078678));
#32465=CARTESIAN_POINT('Ctrl Pts',(3.58527826249944,-3.36745272188013,43.8050241595341));
#32466=CARTESIAN_POINT('Ctrl Pts',(3.76314911357139,-3.1726632967138,43.8198284837509));
#32467=CARTESIAN_POINT('Ctrl Pts',(3.88577237932801,-3.02123428987749,43.83069907988));
#32468=CARTESIAN_POINT('Ctrl Pts',(4.02257731209639,-2.83013814319236,43.8439100293275));
#32469=CARTESIAN_POINT('Ctrl Pts',(4.04565323581996,-2.7970520218841,43.8461797843625));
#32470=CARTESIAN_POINT('Ctrl Pts',(4.10899410627445,-2.70381027725212,43.8525308285746));
#32471=CARTESIAN_POINT('Ctrl Pts',(4.14834163122497,-2.64304448146158,43.8566179668104));
#32472=CARTESIAN_POINT('Ctrl Pts',(4.22461127774127,-2.51935729789091,43.8648449470911));
#32473=CARTESIAN_POINT('Ctrl Pts',(4.26150342148319,-2.45643849157217,43.8689839367867));
#32474=CARTESIAN_POINT('Ctrl Pts',(4.37410946980738,-2.25421441809336,43.882152972803));
#32475=CARTESIAN_POINT('Ctrl Pts',(4.44449343058884,-2.11205902867539,43.8912164077224));
#32476=CARTESIAN_POINT('Ctrl Pts',(4.5618893399295,-1.84298249834645,43.9080219693431));
#32477=CARTESIAN_POINT('Ctrl Pts',(4.61077025079294,-1.71703730889549,43.9157530254212));
#32478=CARTESIAN_POINT('Ctrl Pts',(4.66802201502881,-1.54936405509511,43.925838364569));
#32479=CARTESIAN_POINT('Ctrl Pts',(4.68112459044695,-1.50931478938031,43.9282319666503));
#32480=CARTESIAN_POINT('Ctrl Pts',(4.70642425042748,-1.42848356832004,43.9330299208329));
#32481=CARTESIAN_POINT('Ctrl Pts',(4.7186098155937,-1.38770169528908,43.9354339648089));
#32482=CARTESIAN_POINT('Ctrl Pts',(4.76478296272886,-1.22552718041598,43.9449389932172));
#32483=CARTESIAN_POINT('Ctrl Pts',(4.79462780010521,-1.1030042958544,43.9519998448588));
#32484=CARTESIAN_POINT('Ctrl Pts',(4.85361559189301,-0.812739563426895,
43.9685934888011));
#32485=CARTESIAN_POINT('Ctrl Pts',(4.87882382755338,-0.644365628404013,
43.9781183433983));
#32486=CARTESIAN_POINT('Ctrl Pts',(4.90221759773451,-0.403287236064732,
43.9917663677502));
#32487=CARTESIAN_POINT('Ctrl Pts',(4.90760111699421,-0.331404719414036,
43.995836419478));
#32488=CARTESIAN_POINT('Ctrl Pts',(4.91526798566742,-0.186259532728857,
44.0040660205995));
#32489=CARTESIAN_POINT('Ctrl Pts',(4.91749734151612,-0.113011991461616,
44.008224908637));
#32490=CARTESIAN_POINT('Ctrl Pts',(4.91931423056557,0.111825301323258,44.0210185839678));
#32491=CARTESIAN_POINT('Ctrl Pts',(4.91353173762474,0.263367203574707,44.0296827038052));
#32492=CARTESIAN_POINT('Ctrl Pts',(4.89240617472781,0.513202781487619,44.044035220973));
#32493=CARTESIAN_POINT('Ctrl Pts',(4.88106529612849,0.611732774583815,44.0497125846265));
#32494=CARTESIAN_POINT('Ctrl Pts',(4.85760980282273,0.772543745433108,44.0589927581509));
#32495=CARTESIAN_POINT('Ctrl Pts',(4.84725528944837,0.835052773569074,44.062603465774));
#32496=CARTESIAN_POINT('Ctrl Pts',(4.82891980000988,0.933860782855306,44.0683106679693));
#32497=CARTESIAN_POINT('Ctrl Pts',(4.82173023134731,0.970298931859938,44.0704149637746));
#32498=CARTESIAN_POINT('Ctrl Pts',(4.80198473120465,1.06472810337526,44.0758681358995));
#32499=CARTESIAN_POINT('Ctrl Pts',(4.78879092047,1.12257959120609,44.0792098635822));
#32500=CARTESIAN_POINT('Ctrl Pts',(4.73186296571308,1.35288842193023,44.0925454329489));
#32501=CARTESIAN_POINT('Ctrl Pts',(4.67983255726093,1.52315530015966,44.1024812832804));
#32502=CARTESIAN_POINT('Ctrl Pts',(4.59131419391572,1.76503913388939,44.1169321438822));
#32503=CARTESIAN_POINT('Ctrl Pts',(4.56212365262991,1.83917285515254,44.1214076994404));
#32504=CARTESIAN_POINT('Ctrl Pts',(4.50267115091603,1.98002455630716,44.1300198024367));
#32505=CARTESIAN_POINT('Ctrl Pts',(4.47269393182329,2.04683989701316,44.1341534047749));
#32506=CARTESIAN_POINT('Ctrl Pts',(4.4139858934759,2.17023845461827,44.1418886587215));
#32507=CARTESIAN_POINT('Ctrl Pts',(4.38563005420559,2.22698346058748,44.1454867629376));
#32508=CARTESIAN_POINT('Ctrl Pts',(4.29435899740368,2.40112497673351,44.1566641574443));
#32509=CARTESIAN_POINT('Ctrl Pts',(4.22776795189248,2.51652493076823,44.1642671275171));
#32510=CARTESIAN_POINT('Ctrl Pts',(4.09204669346087,2.73110041870683,44.1787938270226));
#32511=CARTESIAN_POINT('Ctrl Pts',(4.02378243538841,2.83071203725729,44.185709372804));
#32512=CARTESIAN_POINT('Ctrl Pts',(3.9213802026044,2.96893800221093,44.1955384898348));
#32513=CARTESIAN_POINT('Ctrl Pts',(3.89019450002176,3.00968476244383,44.1984660742475));
#32514=CARTESIAN_POINT('Ctrl Pts',(3.83211505739118,3.08315920574389,44.2037975218062));
#32515=CARTESIAN_POINT('Ctrl Pts',(3.80542510614915,3.11604177090318,44.2062033458529));
#32516=CARTESIAN_POINT('Ctrl Pts',(3.75503337655157,3.17651220958853,44.2106625547058));
#32517=CARTESIAN_POINT('Ctrl Pts',(3.73144385901205,3.20418979464799,44.2127175589637));
#32518=CARTESIAN_POINT('Ctrl Pts',(3.64675734031835,3.30134882480061,44.2199875894225));
#32519=CARTESIAN_POINT('Ctrl Pts',(3.58400871081726,3.3693656765768,44.2251808833597));
#32520=CARTESIAN_POINT('Ctrl Pts',(3.40078275337822,3.5570611626929,44.2398863386702));
#32521=CARTESIAN_POINT('Ctrl Pts',(3.27597656962778,3.67232687045935,44.2493771226828));
#32522=CARTESIAN_POINT('Ctrl Pts',(3.11465286673802,3.80653735209783,44.261174233773));
#32523=CARTESIAN_POINT('Ctrl Pts',(3.08353295378834,3.8317898680272,44.2634294158171));
#32524=CARTESIAN_POINT('Ctrl Pts',(2.99553047140354,3.90143384544104,44.2697529721591));
#32525=CARTESIAN_POINT('Ctrl Pts',(2.93797496275479,3.9449577709444,44.2738271988745));
#32526=CARTESIAN_POINT('Ctrl Pts',(2.82015164935803,4.0300476360955,44.2820560083392));
#32527=CARTESIAN_POINT('Ctrl Pts',(2.75987150822825,4.07156583672237,44.2862098823285));
#32528=CARTESIAN_POINT('Ctrl Pts',(2.57038848720667,4.19593110155218,44.2991060364627));
#32529=CARTESIAN_POINT('Ctrl Pts',(2.4382194291894,4.27408701243943,44.3078787247829));
#32530=CARTESIAN_POINT('Ctrl Pts',(2.1802038551831,4.41079189045899,44.324593648911));
#32531=CARTESIAN_POINT('Ctrl Pts',(2.05510640848856,4.47044876979039,44.3325256961509));
#32532=CARTESIAN_POINT('Ctrl Pts',(1.88870662544854,4.54133932124927,44.3428217522653));
#32533=CARTESIAN_POINT('Ctrl Pts',(1.84954332404184,4.55742965889241,44.3452269303542));
#32534=CARTESIAN_POINT('Ctrl Pts',(1.77079475246199,4.58860141814315,44.3500248391241));
#32535=CARTESIAN_POINT('Ctrl Pts',(1.73121258765669,4.60368114258355,44.3524173633981));
#32536=CARTESIAN_POINT('Ctrl Pts',(1.60719969005676,4.64910105499918,44.3598624188259));
#32537=CARTESIAN_POINT('Ctrl Pts',(1.52212989081448,4.67764388889822,44.3648969773721));
#32538=CARTESIAN_POINT('Ctrl Pts',(1.41643970189314,4.70991655851346,44.3710918161928));
#32539=CARTESIAN_POINT('Ctrl Pts',(1.39651469062305,4.71586282003662,44.3722570723154));
#32540=CARTESIAN_POINT('Ctrl Pts',(1.2219272239183,4.76676179962567,44.3824467752625));
#32541=CARTESIAN_POINT('Ctrl Pts',(1.06518191466581,4.80421805641786,44.391458088435));
#32542=CARTESIAN_POINT('Ctrl Pts',(0.829006286209752,4.8485265656227,44.4049779487915));
#32543=CARTESIAN_POINT('Ctrl Pts',(0.750788706982978,4.86125265716742,44.4094455413212));
#32544=CARTESIAN_POINT('Ctrl Pts',(0.60382814628672,4.88153173638036,44.4178348827674));
#32545=CARTESIAN_POINT('Ctrl Pts',(0.535166757228402,4.88953545036023,44.4217525293836));
#32546=CARTESIAN_POINT('Ctrl Pts',(0.347228864718613,4.90743682421646,44.432479229111));
#32547=CARTESIAN_POINT('Ctrl Pts',(0.227724530074298,4.91443231737883,44.4393046159908));
#32548=CARTESIAN_POINT('Ctrl Pts',(-0.0284992312444243,4.92006455991003,
44.4539588428542));
#32549=CARTESIAN_POINT('Ctrl Pts',(-0.165149669952706,4.91737460881972,
44.4617870193344));
#32550=CARTESIAN_POINT('Ctrl Pts',(-0.355354550713006,4.90569223810771,
44.4726786749573));
#32551=CARTESIAN_POINT('Ctrl Pts',(-0.409140973214535,4.90149945678584,
44.4757578700689));
#32552=CARTESIAN_POINT('Ctrl Pts',(-0.506418699326991,4.89230401232429,
44.4813218964911));
#32553=CARTESIAN_POINT('Ctrl Pts',(-0.549933019911619,4.88760393050412,
44.4838089750873));
#32554=CARTESIAN_POINT('Ctrl Pts',(-0.634181586608494,4.87736467880084,
44.4886181356272));
#32555=CARTESIAN_POINT('Ctrl Pts',(-0.674920539169764,4.87189437521179,
44.490940682854));
#32556=CARTESIAN_POINT('Ctrl Pts',(-0.835270375089106,4.84831316159673,
44.500080271994));
#32557=CARTESIAN_POINT('Ctrl Pts',(-0.954265594341402,4.82630240713895,
44.5068592329808));
#32558=CARTESIAN_POINT('Ctrl Pts',(-1.23079571487627,4.76452410618217,44.5227341499816));
#32559=CARTESIAN_POINT('Ctrl Pts',(-1.38741068144754,4.72129632564498,44.5318211275747));
#32560=CARTESIAN_POINT('Ctrl Pts',(-1.61423249430184,4.64642732618781,44.5452666552413));
#32561=CARTESIAN_POINT('Ctrl Pts',(-1.68629601843619,4.62076173346113,44.5495814572408));
#32562=CARTESIAN_POINT('Ctrl Pts',(-1.82241014731488,4.56867598705532,44.5578262192476));
#32563=CARTESIAN_POINT('Ctrl Pts',(-1.8865587344623,4.54256260446731,44.5617530296328));
#32564=CARTESIAN_POINT('Ctrl Pts',(-2.14553186450071,4.43070862474541,44.5777874913885));
#32565=CARTESIAN_POINT('Ctrl Pts',(-2.33524290391109,4.33371942045568,44.5899694233154));
#32566=CARTESIAN_POINT('Ctrl Pts',(-2.60732342661571,4.17155171382374,44.608095779479));
#32567=CARTESIAN_POINT('Ctrl Pts',(-2.69486924348881,4.11553876427635,44.6140348314711));
#32568=CARTESIAN_POINT('Ctrl Pts',(-2.81305613806979,4.03453204446409,44.6221842074669));
#32569=CARTESIAN_POINT('Ctrl Pts',(-2.84526829709359,4.01188011238394,44.624419209061));
#32570=CARTESIAN_POINT('Ctrl Pts',(-2.91503657216522,3.96155533802634,44.6292887831803));
#32571=CARTESIAN_POINT('Ctrl Pts',(-2.95247803262843,3.9337300938032,44.6319212070173));
#32572=CARTESIAN_POINT('Ctrl Pts',(-3.14467766014315,3.78660360301213,44.6455531729767));
#32573=CARTESIAN_POINT('Ctrl Pts',(-3.29262223916538,3.65868891842791,44.6564593687879));
#32574=CARTESIAN_POINT('Ctrl Pts',(-3.49128952495236,3.4650835679661,44.6720190452396));
#32575=CARTESIAN_POINT('Ctrl Pts',(-3.54857319080975,3.4063961635706,44.6766243590785));
#32576=CARTESIAN_POINT('Ctrl Pts',(-3.65494335109643,3.29182302379609,44.6854286590018));
#32577=CARTESIAN_POINT('Ctrl Pts',(-3.70428201514352,3.23620214148702,44.6896242629739));
#32578=CARTESIAN_POINT('Ctrl Pts',(-3.79840661379017,3.12511887595006,44.6978640857508));
#32579=CARTESIAN_POINT('Ctrl Pts',(-3.84328532062073,3.06975871671379,44.7019063797617));
#32580=CARTESIAN_POINT('Ctrl Pts',(-4.00255738073668,2.86431874773125,44.7166889804901));
#32581=CARTESIAN_POINT('Ctrl Pts',(-4.10949075247443,2.70866599345547,44.7274832124058));
#32582=CARTESIAN_POINT('Ctrl Pts',(-4.24965152698669,2.47716742973605,44.7429741166421));
#32583=CARTESIAN_POINT('Ctrl Pts',(-4.29032986445171,2.40602709019556,44.7476619728084));
#32584=CARTESIAN_POINT('Ctrl Pts',(-4.34224490486388,2.30972866904664,44.7539048644201));
#32585=CARTESIAN_POINT('Ctrl Pts',(-4.35507502159775,2.28544501256247,44.7554705843189));
#32586=CARTESIAN_POINT('Ctrl Pts',(-4.38763808194379,2.22254264641352,44.7595036035274));
#32587=CARTESIAN_POINT('Ctrl Pts',(-4.40706496472573,2.1837678925486,44.7619678364715));
#32588=CARTESIAN_POINT('Ctrl Pts',(-4.44403863021987,2.10746750041819,44.7667720063706));
#32589=CARTESIAN_POINT('Ctrl Pts',(-4.46162918476925,2.06996707114031,44.7691122265992));
#32590=CARTESIAN_POINT('Ctrl Pts',(-4.51849525913774,1.94464353446965,44.7768722064486));
#32591=CARTESIAN_POINT('Ctrl Pts',(-4.55566793852529,1.85589004967326,44.7822699029138));
#32592=CARTESIAN_POINT('Ctrl Pts',(-4.63959016408138,1.6377708246366,44.7953695725174));
#32593=CARTESIAN_POINT('Ctrl Pts',(-4.68356273362564,1.50742500397142,44.8030611906426));
#32594=CARTESIAN_POINT('Ctrl Pts',(-4.73483317319724,1.33140471479133,44.8133551025073));
#32595=CARTESIAN_POINT('Ctrl Pts',(-4.74703467783705,1.28722392333865,44.8159310232576));
#32596=CARTESIAN_POINT('Ctrl Pts',(-4.76043811642558,1.23590612239217,44.8189161372267));
#32597=CARTESIAN_POINT('Ctrl Pts',(-4.76224403384605,1.22892911234828,44.8193218361234));
#32598=CARTESIAN_POINT('Ctrl Pts',(-4.76403458711239,1.22194824575222,44.8197276177568));
#32599=CARTESIAN_POINT('Origin',(0.,0.,-3.23514056400928));
#32600=CARTESIAN_POINT('',(-4.76403458328184,1.22194826068645,46.9151580697526));
#32601=CARTESIAN_POINT('',(-4.7640345870679,1.22194824592564,46.5701705954582));
#32602=CARTESIAN_POINT('',(-4.76403458704967,1.22194824599672,-3.23514056400928));
#32603=CARTESIAN_POINT('',(-4.91809585794598,-0.000121275114829886,45.2351405640092));
#32604=CARTESIAN_POINT('Ctrl Pts',(-4.76403458328184,1.22194826068643,46.9151580697526));
#32605=CARTESIAN_POINT('Ctrl Pts',(-4.71829633738443,1.40026889196382,46.9048442910559));
#32606=CARTESIAN_POINT('Ctrl Pts',(-4.66257828953066,1.57589625349177,46.8945393837931));
#32607=CARTESIAN_POINT('Ctrl Pts',(-4.57485811836119,1.80659514119114,46.8806232551198));
#32608=CARTESIAN_POINT('Ctrl Pts',(-4.55146015251469,1.86475821003725,46.877081893628));
#32609=CARTESIAN_POINT('Ctrl Pts',(-4.4985369661167,1.98938045016523,46.8694155881345));
#32610=CARTESIAN_POINT('Ctrl Pts',(-4.46863670209117,2.05566419179987,46.8652887488593));
#32611=CARTESIAN_POINT('Ctrl Pts',(-4.40312557083084,2.19270118742757,46.8566462277294));
#32612=CARTESIAN_POINT('Ctrl Pts',(-4.36725278360166,2.26330648404268,46.8521298839995));
#32613=CARTESIAN_POINT('Ctrl Pts',(-4.24587540400877,2.48856295555406,46.8375092242518));
#32614=CARTESIAN_POINT('Ctrl Pts',(-4.15373819642433,2.63948147354595,46.8273784154705));
#32615=CARTESIAN_POINT('Ctrl Pts',(-4.01977395516314,2.83446387712191,46.8138739176265));
#32616=CARTESIAN_POINT('Ctrl Pts',(-3.98496898468178,2.8831910161078,46.8104626875148));
#32617=CARTESIAN_POINT('Ctrl Pts',(-3.92738047219344,2.96077965509931,46.8049764144071));
#32618=CARTESIAN_POINT('Ctrl Pts',(-3.90514815369414,2.9900420526465,46.8028947300049));
#32619=CARTESIAN_POINT('Ctrl Pts',(-3.84526250171788,3.06705673866384,46.7973810619885));
#32620=CARTESIAN_POINT('Ctrl Pts',(-3.8070479376242,3.1143646027068,46.7939568800489));
#32621=CARTESIAN_POINT('Ctrl Pts',(-3.73744712227841,3.19733121443554,46.787870657866));
#32622=CARTESIAN_POINT('Ctrl Pts',(-3.70640321966736,3.23326662893186,46.7852063645276));
#32623=CARTESIAN_POINT('Ctrl Pts',(-3.52498281349164,3.43722601838593,46.7699015439434));
#32624=CARTESIAN_POINT('Ctrl Pts',(-3.36371447869876,3.59519821461685,46.7573069935311));
#32625=CARTESIAN_POINT('Ctrl Pts',(-3.14020836540225,3.78588715187681,46.7407378109123));
#32626=CARTESIAN_POINT('Ctrl Pts',(-3.08731951954971,3.82913934868015,46.7368768655856));
#32627=CARTESIAN_POINT('Ctrl Pts',(-2.97343879118533,3.91837675327876,46.7286795283935));
#32628=CARTESIAN_POINT('Ctrl Pts',(-2.91224195402836,3.96407129564699,46.7243417949505));
#32629=CARTESIAN_POINT('Ctrl Pts',(-2.76228098598692,4.0706968954961,46.7138637119489));
#32630=CARTESIAN_POINT('Ctrl Pts',(-2.67253209244462,4.13017448846413,46.7077151318762));
#32631=CARTESIAN_POINT('Ctrl Pts',(-2.43379607890237,4.27734553015157,46.6916687777684));
#32632=CARTESIAN_POINT('Ctrl Pts',(-2.28200887370927,4.36021609426409,46.6817631515585));
#32633=CARTESIAN_POINT('Ctrl Pts',(-2.08891893302936,4.45278651543154,46.6695759620893));
#32634=CARTESIAN_POINT('Ctrl Pts',(-2.05143937259055,4.47017747054437,46.6672292422945));
#32635=CARTESIAN_POINT('Ctrl Pts',(-1.97499716930681,4.50448365712826,46.6624832453279));
#32636=CARTESIAN_POINT('Ctrl Pts',(-1.93602556904247,4.5213705763197,46.6600844502966));
#32637=CARTESIAN_POINT('Ctrl Pts',(-1.87221255391581,4.5480452610561,46.6561858685435));
#32638=CARTESIAN_POINT('Ctrl Pts',(-1.84750176980017,4.55813917784168,46.6546832536173));
#32639=CARTESIAN_POINT('Ctrl Pts',(-1.68011192540942,4.62493012222541,46.6445477994749));
#32640=CARTESIAN_POINT('Ctrl Pts',(-1.53492696585616,4.67512080476925,46.6359651676596));
#32641=CARTESIAN_POINT('Ctrl Pts',(-1.26821306145229,4.75355792218286,46.6203821569913));
#32642=CARTESIAN_POINT('Ctrl Pts',(-1.14750526013454,4.78413089519121,46.6133959611574));
#32643=CARTESIAN_POINT('Ctrl Pts',(-0.964357641728391,4.82318776978269,
46.6028377616425));
#32644=CARTESIAN_POINT('Ctrl Pts',(-0.902701577565472,4.83510658410881,
46.5992906476204));
#32645=CARTESIAN_POINT('Ctrl Pts',(-0.769380522184149,4.85824001980595,
46.5916292234332));
#32646=CARTESIAN_POINT('Ctrl Pts',(-0.697661492040328,4.86905645431831,
46.5875130966142));
#32647=CARTESIAN_POINT('Ctrl Pts',(-0.547571828709803,4.88830823290698,
46.5789035041631));
#32648=CARTESIAN_POINT('Ctrl Pts',(-0.469184453617907,4.89645362118847,
46.5744094233842));
#32649=CARTESIAN_POINT('Ctrl Pts',(-0.217473951707847,4.91650928446453,
46.5599819139811));
#32650=CARTESIAN_POINT('Ctrl Pts',(-0.0437030836795273,4.92112267538409,
46.5500228363498));
#32651=CARTESIAN_POINT('Ctrl Pts',(0.192304227126251,4.91488487502529,46.5365421886008));
#32652=CARTESIAN_POINT('Ctrl Pts',(0.254625398569367,4.91205051805763,46.5329873186813));
#32653=CARTESIAN_POINT('Ctrl Pts',(0.353567273468456,4.90566255337063,46.5273567588795));
#32654=CARTESIAN_POINT('Ctrl Pts',(0.390230646557007,4.90288231451022,46.525273543407));
#32655=CARTESIAN_POINT('Ctrl Pts',(0.485099032185484,4.89461740406166,46.5198905551969));
#32656=CARTESIAN_POINT('Ctrl Pts',(0.543243609524901,4.88850561057316,46.5165976785536));
#32657=CARTESIAN_POINT('Ctrl Pts',(0.686824790330378,4.87081986581729,46.5084651316182));
#32658=CARTESIAN_POINT('Ctrl Pts',(0.772092326465536,4.85803335332093,46.5036343240458));
#32659=CARTESIAN_POINT('Ctrl Pts',(1.03210607265405,4.81202343571052,46.4888403984732));
#32660=CARTESIAN_POINT('Ctrl Pts',(1.20542061327895,4.77155872572109,46.4788872265183));
#32661=CARTESIAN_POINT('Ctrl Pts',(1.44466309460734,4.70183185228411,46.4648448524049));
#32662=CARTESIAN_POINT('Ctrl Pts',(1.51272226326294,4.6803787693242,46.46081551324));
#32663=CARTESIAN_POINT('Ctrl Pts',(1.64899073096502,4.63414240051098,46.4526679213942));
#32664=CARTESIAN_POINT('Ctrl Pts',(1.71716665962803,4.60931499431087,46.4485503048024));
#32665=CARTESIAN_POINT('Ctrl Pts',(1.85824513156154,4.55437435756275,46.4399361312323));
#32666=CARTESIAN_POINT('Ctrl Pts',(1.93102308037085,4.52399717607071,46.4354389526067));
#32667=CARTESIAN_POINT('Ctrl Pts',(2.16206595986506,4.42096961395716,46.420984776249));
#32668=CARTESIAN_POINT('Ctrl Pts',(2.31721480760218,4.34166062297294,46.4110020137675));
#32669=CARTESIAN_POINT('Ctrl Pts',(2.52148431848557,4.22316792620064,46.3975184266756));
#32670=CARTESIAN_POINT('Ctrl Pts',(2.57454526237661,4.19103177350427,46.3939837301457));
#32671=CARTESIAN_POINT('Ctrl Pts',(2.65806273235386,4.13826497142618,46.3883736237236));
#32672=CARTESIAN_POINT('Ctrl Pts',(2.68891984521939,4.11828174988093,46.3862908127575));
#32673=CARTESIAN_POINT('Ctrl Pts',(2.76851107397061,4.06546213526557,46.3808912603567));
#32674=CARTESIAN_POINT('Ctrl Pts',(2.81688592508844,4.03209495761634,46.3775815307427));
#32675=CARTESIAN_POINT('Ctrl Pts',(2.97986067101228,3.91531626694129,46.3663109617165));
#32676=CARTESIAN_POINT('Ctrl Pts',(3.09144805251376,3.82782189873297,46.3583850282051));
#32677=CARTESIAN_POINT('Ctrl Pts',(3.28333377693483,3.66349572118424,46.3442262202962));
#32678=CARTESIAN_POINT('Ctrl Pts',(3.36510175102538,3.58853332738484,46.3380046869931));
#32679=CARTESIAN_POINT('Ctrl Pts',(3.49712502614329,3.45901473316727,46.3275897818657));
#32680=CARTESIAN_POINT('Ctrl Pts',(3.54880654167161,3.40597098250362,46.3234109394979));
#32681=CARTESIAN_POINT('Ctrl Pts',(3.64715120612894,3.30036473128972,46.3152449062796));
#32682=CARTESIAN_POINT('Ctrl Pts',(3.69392446893139,3.24792874710778,46.3112598096743));
#32683=CARTESIAN_POINT('Ctrl Pts',(3.8442606265884,3.07194215766255,46.2980993818115));
#32684=CARTESIAN_POINT('Ctrl Pts',(3.94287285336128,2.94430311175795,46.2888874862038));
#32685=CARTESIAN_POINT('Ctrl Pts',(4.11704541404574,2.69438161071431,46.2714501179665));
#32686=CARTESIAN_POINT('Ctrl Pts',(4.19386668191552,2.57317665846754,46.2632368223855));
#32687=CARTESIAN_POINT('Ctrl Pts',(4.28583639555978,2.41298441772688,46.2527239727575));
#32688=CARTESIAN_POINT('Ctrl Pts',(4.30594005857007,2.37692399513839,46.2503790955165));
#32689=CARTESIAN_POINT('Ctrl Pts',(4.34581672495327,2.30322966723391,46.2456329036836));
#32690=CARTESIAN_POINT('Ctrl Pts',(4.36556062182158,2.26558390277515,46.2432320883855));
#32691=CARTESIAN_POINT('Ctrl Pts',(4.3969201104466,2.20385819730931,46.2393295327536));
#32692=CARTESIAN_POINT('Ctrl Pts',(4.40883166269966,2.17993137319487,46.2378249636799));
#32693=CARTESIAN_POINT('Ctrl Pts',(4.48788547468902,2.01783677074203,46.2276827769044));
#32694=CARTESIAN_POINT('Ctrl Pts',(4.54871794328296,1.87668509633149,46.2190953559161));
#32695=CARTESIAN_POINT('Ctrl Pts',(4.64664277458122,1.61658455481906,46.2035170184832));
#32696=CARTESIAN_POINT('Ctrl Pts',(4.68601429891415,1.49863409309824,46.1965403654574));
#32697=CARTESIAN_POINT('Ctrl Pts',(4.73848308488248,1.31905389560385,46.1859921495881));
#32698=CARTESIAN_POINT('Ctrl Pts',(4.75493557021535,1.25845649207369,46.1824453855905));
#32699=CARTESIAN_POINT('Ctrl Pts',(4.78788457113782,1.12721134326059,46.1747836785361));
#32700=CARTESIAN_POINT('Ctrl Pts',(4.80398728777969,1.05648002941471,46.1706669141112));
#32701=CARTESIAN_POINT('Ctrl Pts',(4.83431240041154,0.908195753898404,46.1620553609223));
#32702=CARTESIAN_POINT('Ctrl Pts',(4.8482462702304,0.830604505002049,46.1575599542294));
#32703=CARTESIAN_POINT('Ctrl Pts',(4.88692178095068,0.580874442767008,46.1431210393416));
#32704=CARTESIAN_POINT('Ctrl Pts',(4.90440235258711,0.407746317549911,46.133151832666));
#32705=CARTESIAN_POINT('Ctrl Pts',(4.91563894851584,0.17189882885378,46.119669941679));
#32706=CARTESIAN_POINT('Ctrl Pts',(4.91742044614293,0.109689423657436,46.1161237133948));
#32707=CARTESIAN_POINT('Ctrl Pts',(4.91837577122531,0.0106994988674436,
46.1105019219746));
#32708=CARTESIAN_POINT('Ctrl Pts',(4.91831833985244,-0.0260663951433238,
46.1084188866038));
#32709=CARTESIAN_POINT('Ctrl Pts',(4.91710024160612,-0.121411742409218,
46.1030288676961));
#32710=CARTESIAN_POINT('Ctrl Pts',(4.91530506649278,-0.179977281530277,
46.0997288294157));
#32711=CARTESIAN_POINT('Ctrl Pts',(4.90564257606118,-0.379001129087812,
46.0885275193828));
#32712=CARTESIAN_POINT('Ctrl Pts',(4.89279636445741,-0.519148470412448,
46.0806606819802));
#32713=CARTESIAN_POINT('Ctrl Pts',(4.86509016957856,-0.7242025145272,46.0690643097286));
#32714=CARTESIAN_POINT('Ctrl Pts',(4.85489433259876,-0.789666130355734,
46.0653494360601));
#32715=CARTESIAN_POINT('Ctrl Pts',(4.82742813259212,-0.945273422047215,
46.0564734425241));
#32716=CARTESIAN_POINT('Ctrl Pts',(4.80895100234762,-1.0351783370182,46.0513080612167));
#32717=CARTESIAN_POINT('Ctrl Pts',(4.77259420047312,-1.18997893895328,46.0423272270238));
#32718=CARTESIAN_POINT('Ctrl Pts',(4.75587775141555,-1.25512228792961,46.0385208845561));
#32719=CARTESIAN_POINT('Ctrl Pts',(4.7136476917026,-1.40670846880949,46.0295922723431));
#32720=CARTESIAN_POINT('Ctrl Pts',(4.68708352755543,-1.49283320902282,46.024464148853));
#32721=CARTESIAN_POINT('Ctrl Pts',(4.62008054158398,-1.69059991955772,46.0125503270132));
#32722=CARTESIAN_POINT('Ctrl Pts',(4.57793534893185,-1.80160481476745,46.0057582715919));
#32723=CARTESIAN_POINT('Ctrl Pts',(4.48368623628308,-2.02511352720993,45.9918725160006));
#32724=CARTESIAN_POINT('Ctrl Pts',(4.43126123044029,-2.13739361469917,45.984783386783));
#32725=CARTESIAN_POINT('Ctrl Pts',(4.35521275984951,-2.28541342564937,45.9753093380816));
#32726=CARTESIAN_POINT('Ctrl Pts',(4.33528231373689,-2.32299806834949,45.9728923727802));
#32727=CARTESIAN_POINT('Ctrl Pts',(4.29506805752893,-2.39651317463609,45.9681447086321));
#32728=CARTESIAN_POINT('Ctrl Pts',(4.27481473373422,-2.43245638287808,45.9658138903839));
#32729=CARTESIAN_POINT('Ctrl Pts',(4.18269845006276,-2.59122890727786,45.9554639504351));
#32730=CARTESIAN_POINT('Ctrl Pts',(4.10597613768451,-2.71116108722591,45.947498707409));
#32731=CARTESIAN_POINT('Ctrl Pts',(3.93742793656346,-2.95103427388295,45.9310748895479));
#32732=CARTESIAN_POINT('Ctrl Pts',(3.84506251068321,-3.07041294065444,45.9226236895386));
#32733=CARTESIAN_POINT('Ctrl Pts',(3.70020168996147,-3.24083194870978,45.9100246764066));
#32734=CARTESIAN_POINT('Ctrl Pts',(3.65182025248989,-3.29525309312637,45.90591463613));
#32735=CARTESIAN_POINT('Ctrl Pts',(3.55381731617338,-3.40068017127785,45.8977672463934));
#32736=CARTESIAN_POINT('Ctrl Pts',(3.50426149556493,-3.45172338956551,45.8937313668823));
#32737=CARTESIAN_POINT('Ctrl Pts',(3.33925555592471,-3.61446478811092,45.8805501341912));
#32738=CARTESIAN_POINT('Ctrl Pts',(3.21943917343033,-3.72158482322258,45.871369199878));
#32739=CARTESIAN_POINT('Ctrl Pts',(2.98655140186315,-3.91011748273077,45.854217062773));
#32740=CARTESIAN_POINT('Ctrl Pts',(2.87484361366755,-3.99296666932025,45.8462576994823));
#32741=CARTESIAN_POINT('Ctrl Pts',(2.72540167993102,-4.09427568056966,45.8359816074918));
#32742=CARTESIAN_POINT('Ctrl Pts',(2.6907334647845,-4.11714235151632,45.8336226896286));
#32743=CARTESIAN_POINT('Ctrl Pts',(2.62022911982501,-4.1623750968099,45.8288776399587));
#32744=CARTESIAN_POINT('Ctrl Pts',(2.58438608307903,-4.18472409079444,45.8264918788485));
#32745=CARTESIAN_POINT('Ctrl Pts',(2.43378455237123,-4.27595476609958,45.8165662075385));
#32746=CARTESIAN_POINT('Ctrl Pts',(2.31652553851776,-4.34059979757258,45.8090722171698));
#32747=CARTESIAN_POINT('Ctrl Pts',(2.05517012920957,-4.471074611123,45.7927075363262));
#32748=CARTESIAN_POINT('Ctrl Pts',(1.91023678398102,-4.53488997572871,45.7838436410365));
#32749=CARTESIAN_POINT('Ctrl Pts',(1.69485149291074,-4.61756527383395,45.7708468930203));
#32750=CARTESIAN_POINT('Ctrl Pts',(1.62665768730089,-4.64202706256713,45.7667573187759));
#32751=CARTESIAN_POINT('Ctrl Pts',(1.49018242909036,-4.68760534848185,45.7586125550724));
#32752=CARTESIAN_POINT('Ctrl Pts',(1.42193127862445,-4.70875767643545,45.7545586366489));
#32753=CARTESIAN_POINT('Ctrl Pts',(1.31513742115687,-4.73932143739167,45.7482403036438));
#32754=CARTESIAN_POINT('Ctrl Pts',(1.27690040848821,-4.74976625173223,45.7459829888365));
#32755=CARTESIAN_POINT('Ctrl Pts',(1.05951530639952,-4.80633237304636,45.7331759636513));
#32756=CARTESIAN_POINT('Ctrl Pts',(0.87800434484672,-4.84277926103134,45.7225764625679));
#32757=CARTESIAN_POINT('Ctrl Pts',(0.615322965076392,-4.88026823936189,
45.7074016408119));
#32758=CARTESIAN_POINT('Ctrl Pts',(0.535504223934996,-4.88967032495199,
45.7028131341762));
#32759=CARTESIAN_POINT('Ctrl Pts',(0.416644779359256,-4.90072568377732,
45.6960233371103));
#32760=CARTESIAN_POINT('Ctrl Pts',(0.377757163252485,-4.9038764958753,45.6938087915722));
#32761=CARTESIAN_POINT('Ctrl Pts',(0.294426287644029,-4.90963112990521,
45.689079850044));
#32762=CARTESIAN_POINT('Ctrl Pts',(0.249976850757127,-4.91209490004657,
45.6865670378003));
#32763=CARTESIAN_POINT('Ctrl Pts',(0.149126167680454,-4.91631243814184,
45.6808805802136));
#32764=CARTESIAN_POINT('Ctrl Pts',(0.0927158106556685,-4.91769971238357,
45.6777103648157));
#32765=CARTESIAN_POINT('Ctrl Pts',(-0.118632671288443,-4.91925938131254,
45.6658500944445));
#32766=CARTESIAN_POINT('Ctrl Pts',(-0.273526647587613,-4.91308150290417,
45.6571901711359));
#32767=CARTESIAN_POINT('Ctrl Pts',(-0.531096265295244,-4.89058858306286,
45.6426806924273));
#32768=CARTESIAN_POINT('Ctrl Pts',(-0.634010610454954,-4.87831426813296,
45.6368546467032));
#32769=CARTESIAN_POINT('Ctrl Pts',(-0.798060326823833,-4.8534693248098,
45.6274900316041));
#32770=CARTESIAN_POINT('Ctrl Pts',(-0.859477973920052,-4.84297039832362,
45.6239666039346));
#32771=CARTESIAN_POINT('Ctrl Pts',(-0.997534905257617,-4.8166615502822,
45.6160004844995));
#32772=CARTESIAN_POINT('Ctrl Pts',(-1.07402957555589,-4.8001838137992,45.6115542391892));
#32773=CARTESIAN_POINT('Ctrl Pts',(-1.23980319591408,-4.7603133949289,45.6018405855674));
#32774=CARTESIAN_POINT('Ctrl Pts',(-1.32888295479029,-4.73621847495473,
45.5965706526828));
#32775=CARTESIAN_POINT('Ctrl Pts',(-1.5952954816186,-4.65604911203259,45.5806554692814));
#32776=CARTESIAN_POINT('Ctrl Pts',(-1.77017828285838,-4.59241012163614,
45.569993560613));
#32777=CARTESIAN_POINT('Ctrl Pts',(-1.97381314194537,-4.50494363580632,
45.5573868473431));
#32778=CARTESIAN_POINT('Ctrl Pts',(-2.00643472182376,-4.49050946167834,
45.5553614692509));
#32779=CARTESIAN_POINT('Ctrl Pts',(-2.0722276873717,-4.46053774599917,45.5512661881276));
#32780=CARTESIAN_POINT('Ctrl Pts',(-2.1053883419589,-4.44498195027296,45.5491966218872));
#32781=CARTESIAN_POINT('Ctrl Pts',(-2.18119156068468,-4.40838375251777,
45.5444490418963));
#32782=CARTESIAN_POINT('Ctrl Pts',(-2.2237089892051,-4.38709041637629,45.5417738555316));
#32783=CARTESIAN_POINT('Ctrl Pts',(-2.35642603836265,-4.31819868952703,
45.5333730602532));
#32784=CARTESIAN_POINT('Ctrl Pts',(-2.44545801023026,-4.26840941292869,
45.5276629591504));
#32785=CARTESIAN_POINT('Ctrl Pts',(-2.66849277034031,-4.13441159042388,
45.5130863070386));
#32786=CARTESIAN_POINT('Ctrl Pts',(-2.80009584349005,-4.04643982449125,
45.5042215704652));
#32787=CARTESIAN_POINT('Ctrl Pts',(-2.98266977194936,-3.91121769796303,
45.4914144368207));
#32788=CARTESIAN_POINT('Ctrl Pts',(-3.03724017144362,-3.86899403593224,
45.4875172119113));
#32789=CARTESIAN_POINT('Ctrl Pts',(-3.11812769450088,-3.80364137067469,
45.481628016656));
#32790=CARTESIAN_POINT('Ctrl Pts',(-3.14511586641018,-3.78135612761962,
45.4796435766889));
#32791=CARTESIAN_POINT('Ctrl Pts',(-3.24354500284124,-3.69829635506482,
45.4723322009953));
#32792=CARTESIAN_POINT('Ctrl Pts',(-3.31348057206347,-3.63577038494733,
45.4669914571636));
#32793=CARTESIAN_POINT('Ctrl Pts',(-3.47919239790801,-3.47886081016615,
45.4539633308183));
#32794=CARTESIAN_POINT('Ctrl Pts',(-3.5729694486368,-3.38247560916495,45.4462660998323));
#32795=CARTESIAN_POINT('Ctrl Pts',(-3.73071931371786,-3.20644820971547,
45.4327386917358));
#32796=CARTESIAN_POINT('Ctrl Pts',(-3.79638231995738,-3.12842745854271,
45.4269103566911));
#32797=CARTESIAN_POINT('Ctrl Pts',(-3.88478515410035,-3.01650159951331,
45.4187942619907));
#32798=CARTESIAN_POINT('Ctrl Pts',(-3.90960010995299,-2.9842695309423,45.4164842906093));
#32799=CARTESIAN_POINT('Ctrl Pts',(-3.94016573632975,-2.94353225687743,
45.4135999223398));
#32800=CARTESIAN_POINT('Ctrl Pts',(-3.94629324613586,-2.93531221395766,
45.4130196662068));
#32801=CARTESIAN_POINT('Ctrl Pts',(-3.97819155417054,-2.89224027434051,
45.4099881611807));
#32802=CARTESIAN_POINT('Ctrl Pts',(-4.00352667541658,-2.85706773806111,
45.4075431858685));
#32803=CARTESIAN_POINT('Ctrl Pts',(-4.06403028740322,-2.77068574808417,
45.4016051695881));
#32804=CARTESIAN_POINT('Ctrl Pts',(-4.09869998123625,-2.71913593828919,
45.3981173214067));
#32805=CARTESIAN_POINT('Ctrl Pts',(-4.24245398656462,-2.49639148142515,
45.3832485894215));
#32806=CARTESIAN_POINT('Ctrl Pts',(-4.34185928119416,-2.31919031614372,
45.3719111584013));
#32807=CARTESIAN_POINT('Ctrl Pts',(-4.46322210869182,-2.06752761826943,
45.3561848729021));
#32808=CARTESIAN_POINT('Ctrl Pts',(-4.49480514123492,-1.99793608595011,
45.3518746839423));
#32809=CARTESIAN_POINT('Ctrl Pts',(-4.54736991113381,-1.87455052746062,
45.3442882728012));
#32810=CARTESIAN_POINT('Ctrl Pts',(-4.56904990644319,-1.82106992082375,
45.3410179082324));
#32811=CARTESIAN_POINT('Ctrl Pts',(-4.6248079596991,-1.67625641721646,45.3322052631621));
#32812=CARTESIAN_POINT('Ctrl Pts',(-4.65711992502933,-1.58427203858187,
45.3266522593378));
#32813=CARTESIAN_POINT('Ctrl Pts',(-4.73251613712062,-1.34734014180293,
45.3124518738064));
#32814=CARTESIAN_POINT('Ctrl Pts',(-4.77168960456113,-1.20125453203193,
45.3037906890913));
#32815=CARTESIAN_POINT('Ctrl Pts',(-4.82128742319234,-0.975104243802025,
45.2905499286726));
#32816=CARTESIAN_POINT('Ctrl Pts',(-4.83657599270369,-0.89619952656837,
45.2859613501807));
#32817=CARTESIAN_POINT('Ctrl Pts',(-4.85640129066845,-0.778504932870294,
45.2791727311883));
#32818=CARTESIAN_POINT('Ctrl Pts',(-4.86242068863167,-0.739978739340114,
45.2769594213734));
#32819=CARTESIAN_POINT('Ctrl Pts',(-4.87276911943305,-0.668155141811244,
45.2728512291904));
#32820=CARTESIAN_POINT('Ctrl Pts',(-4.8772165272004,-0.63487727907879,45.2709547399077));
#32821=CARTESIAN_POINT('Ctrl Pts',(-4.9059127981702,-0.402021658618577,
45.2577235429393));
#32822=CARTESIAN_POINT('Ctrl Pts',(-4.91824524434851,-0.201164899637867,
45.246503398605));
#32823=CARTESIAN_POINT('Ctrl Pts',(-4.91824999862486,-0.000116303819701243,
45.2352292809051));
#32824=CARTESIAN_POINT('Ctrl Pts',(-4.76410171059494,1.22196554825755,45.1652160615516));
#32825=CARTESIAN_POINT('Ctrl Pts',(-4.86593327629969,0.823201249710175,
45.1885242290375));
#32826=CARTESIAN_POINT('Ctrl Pts',(-4.91771545987082,0.411493494414974,
45.2118323965233));
#32827=CARTESIAN_POINT('Ctrl Pts',(-4.91809585794598,-0.000121275114829886,
45.2351405640092));
#32828=CARTESIAN_POINT('Ctrl Pts',(-4.76403458711239,1.22194824575222,44.8197276177568));
#32829=CARTESIAN_POINT('Ctrl Pts',(-4.78147306724803,1.15396048702209,44.8236795889637));
#32830=CARTESIAN_POINT('Ctrl Pts',(-4.79745423809204,1.08560693764343,44.8276395483669));
#32831=CARTESIAN_POINT('Ctrl Pts',(-4.82621356990646,0.949522500739756,
44.835507064092));
#32832=CARTESIAN_POINT('Ctrl Pts',(-4.83904177594388,0.881819113438545,
44.8394133260436));
#32833=CARTESIAN_POINT('Ctrl Pts',(-4.88760472540874,0.592396864119301,
44.8560915905761));
#32834=CARTESIAN_POINT('Ctrl Pts',(-4.90955337029353,0.368641935581625,
44.8689486163543));
#32835=CARTESIAN_POINT('Ctrl Pts',(-4.91754602003831,0.0961080499181013,
44.8845482598853));
#32836=CARTESIAN_POINT('Ctrl Pts',(-4.91825066357339,0.0480214367964797,
44.8872977785004));
#32837=CARTESIAN_POINT('Ctrl Pts',(-4.91824915193266,-0.0614515277800697,
44.8935479337799));
#32838=CARTESIAN_POINT('Ctrl Pts',(-4.91709913051757,-0.122830297982319,
44.8970455825798));
#32839=CARTESIAN_POINT('Ctrl Pts',(-4.91341047784258,-0.221265452992939,
44.9026389389286));
#32840=CARTESIAN_POINT('Ctrl Pts',(-4.91160058697769,-0.258342098878533,
44.9047417421161));
#32841=CARTESIAN_POINT('Ctrl Pts',(-4.90569947848665,-0.356416578897101,
44.910294751197));
#32842=CARTESIAN_POINT('Ctrl Pts',(-4.90089042376304,-0.417364756830315,
44.9137371053922));
#32843=CARTESIAN_POINT('Ctrl Pts',(-4.89030397002876,-0.525727918636804,
44.919856063389));
#32844=CARTESIAN_POINT('Ctrl Pts',(-4.88496978675967,-0.573177965872096,
44.9225349406054));
#32845=CARTESIAN_POINT('Ctrl Pts',(-4.85048853898785,-0.844282686854085,
44.9378572043362));
#32846=CARTESIAN_POINT('Ctrl Pts',(-4.80667514669203,-1.06579787208497,
44.9504548561697));
#32847=CARTESIAN_POINT('Ctrl Pts',(-4.72984274491612,-1.35000509945235,
44.9670586788879));
#32848=CARTESIAN_POINT('Ctrl Pts',(-4.71047529309354,-1.41610329152046,
44.9709510725384));
#32849=CARTESIAN_POINT('Ctrl Pts',(-4.66638171085826,-1.5556569962177,44.9792437336011));
#32850=CARTESIAN_POINT('Ctrl Pts',(-4.64129448645505,-1.62897889896192,
44.9836455046313));
#32851=CARTESIAN_POINT('Ctrl Pts',(-4.58383752609168,-1.78478658035925,
44.993103171769));
#32852=CARTESIAN_POINT('Ctrl Pts',(-4.55094981229441,-1.86705254122267,
44.9981608313546));
#32853=CARTESIAN_POINT('Ctrl Pts',(-4.43965684316422,-2.12500123890288,
45.0142274204489));
#32854=CARTESIAN_POINT('Ctrl Pts',(-4.35315904673104,-2.29699591107445,
45.0252592667991));
#32855=CARTESIAN_POINT('Ctrl Pts',(-4.23635465308391,-2.49882976287675,
45.0385286882637));
#32856=CARTESIAN_POINT('Ctrl Pts',(-4.21545903316833,-2.53392109838937,
45.0408478323642));
#32857=CARTESIAN_POINT('Ctrl Pts',(-4.17108537046679,-2.60637227553136,
45.045659182157));
#32858=CARTESIAN_POINT('Ctrl Pts',(-4.14753674819023,-2.64368466175158,
45.0481503436669));
#32859=CARTESIAN_POINT('Ctrl Pts',(-4.09372132608914,-2.72646503287223,
45.053714003143));
#32860=CARTESIAN_POINT('Ctrl Pts',(-4.0631927155725,-2.7717559239983,45.0567834507257));
#32861=CARTESIAN_POINT('Ctrl Pts',(-3.95116145863184,-2.93213083132849,
45.0677636302119));
#32862=CARTESIAN_POINT('Ctrl Pts',(-3.86547246288805,-3.04420612027864,
45.0756481712745));
#32863=CARTESIAN_POINT('Ctrl Pts',(-3.70176399972585,-3.24024877220388,
45.0899715782027));
#32864=CARTESIAN_POINT('Ctrl Pts',(-3.62540139433064,-3.32546734697227,
45.0963975378458));
#32865=CARTESIAN_POINT('Ctrl Pts',(-3.49829802155035,-3.45772478439933,
45.106745162313));
#32866=CARTESIAN_POINT('Ctrl Pts',(-3.44941569582427,-3.50649125863305,
45.1106482971718));
#32867=CARTESIAN_POINT('Ctrl Pts',(-3.3420480249422,-3.60918600269272,45.1190690694249));
#32868=CARTESIAN_POINT('Ctrl Pts',(-3.28324817274271,-3.66275713458285,
45.1235887592863));
#32869=CARTESIAN_POINT('Ctrl Pts',(-3.1015997039072,-3.8203625438863,45.137290088674));
#32870=CARTESIAN_POINT('Ctrl Pts',(-2.97491976406715,-3.91981404814937,
45.1465019642358));
#32871=CARTESIAN_POINT('Ctrl Pts',(-2.75509996294093,-4.07558225388335,
45.1619234007074));
#32872=CARTESIAN_POINT('Ctrl Pts',(-2.66455543958162,-4.1353465643569,45.1681270977999));
#32873=CARTESIAN_POINT('Ctrl Pts',(-2.53556579594329,-4.21449015284746,
45.1767428586038));
#32874=CARTESIAN_POINT('Ctrl Pts',(-2.49873113073566,-4.23643292728247,
45.1791787489918));
#32875=CARTESIAN_POINT('Ctrl Pts',(-2.42538674489026,-4.27883550380349,
45.1839786375755));
#32876=CARTESIAN_POINT('Ctrl Pts',(-2.38889339339521,-4.29931651966843,
45.1863426877605));
#32877=CARTESIAN_POINT('Ctrl Pts',(-2.32931919006218,-4.33175836946534,
45.1901672043361));
#32878=CARTESIAN_POINT('Ctrl Pts',(-2.30639727224754,-4.34400622616873,
45.1916305298068));
#32879=CARTESIAN_POINT('Ctrl Pts',(-2.14570565593726,-4.42823805645539,
45.2018361203679));
#32880=CARTESIAN_POINT('Ctrl Pts',(-2.00468730842697,-4.49383739311481,
45.2105251286182));
#32881=CARTESIAN_POINT('Ctrl Pts',(-1.74399514514285,-4.60038980030157,
45.2263102457428));
#32882=CARTESIAN_POINT('Ctrl Pts',(-1.62539858494433,-4.64361758291524,
45.2333918448791));
#32883=CARTESIAN_POINT('Ctrl Pts',(-1.44504962988017,-4.70159720010369,
45.2440728013173));
#32884=CARTESIAN_POINT('Ctrl Pts',(-1.38445951213296,-4.71979410733264,
45.2476463712113));
#32885=CARTESIAN_POINT('Ctrl Pts',(-1.25271796180907,-4.75660461544544,
45.2553917219798));
#32886=CARTESIAN_POINT('Ctrl Pts',(-1.18146597885301,-4.77480132867078,
45.2595654741251));
#32887=CARTESIAN_POINT('Ctrl Pts',(-1.03160015752544,-4.80951484064551,
45.2683191855076));
#32888=CARTESIAN_POINT('Ctrl Pts',(-0.952935360993312,-4.82571713900363,
45.2728998674771));
#32889=CARTESIAN_POINT('Ctrl Pts',(-0.784055679698201,-4.85621012026275,
45.2827065869128));
#32890=CARTESIAN_POINT('Ctrl Pts',(-0.693767484465915,-4.86992881010696,
45.2879332572902));
#32891=CARTESIAN_POINT('Ctrl Pts',(-0.480772577535112,-4.89624812934193,
45.3002188192861));
#32892=CARTESIAN_POINT('Ctrl Pts',(-0.357868443759488,-4.906762551033,45.3072741196621));
#32893=CARTESIAN_POINT('Ctrl Pts',(-0.193997010645465,-4.91459139746558,
45.3166092103907));
#32894=CARTESIAN_POINT('Ctrl Pts',(-0.153272672446668,-4.916030003469,45.3189230803034));
#32895=CARTESIAN_POINT('Ctrl Pts',(-0.0682974750299268,-4.91797483546348,
45.3237364407185));
#32896=CARTESIAN_POINT('Ctrl Pts',(-0.0240481534612602,-4.91839026268566,
45.3262348282295));
#32897=CARTESIAN_POINT('Ctrl Pts',(0.0750607126872912,-4.91798318241482,
45.331819415762));
#32898=CARTESIAN_POINT('Ctrl Pts',(0.129913093959658,-4.91683997672672,
45.3349025288631));
#32899=CARTESIAN_POINT('Ctrl Pts',(0.327297973552554,-4.90942073636624,
45.3459887146251));
#32900=CARTESIAN_POINT('Ctrl Pts',(0.469560334053181,-4.89786169636462,
45.3539651252594));
#32901=CARTESIAN_POINT('Ctrl Pts',(0.724419954522954,-4.8659466958023,45.3683704476158));
#32902=CARTESIAN_POINT('Ctrl Pts',(0.837191476444289,-4.84781718668231,
45.3747855686281));
#32903=CARTESIAN_POINT('Ctrl Pts',(1.01674672871117,-4.81249875069379,45.3851099342859));
#32904=CARTESIAN_POINT('Ctrl Pts',(1.08397814171372,-4.79780255767535,45.3890006288279));
#32905=CARTESIAN_POINT('Ctrl Pts',(1.22915563487059,-4.76286066769494,45.3974649394445));
#32906=CARTESIAN_POINT('Ctrl Pts',(1.30695761432919,-4.74210152671356,45.4020409669084));
#32907=CARTESIAN_POINT('Ctrl Pts',(1.53837871150379,-4.67422562807143,45.4157832002721));
#32908=CARTESIAN_POINT('Ctrl Pts',(1.69023383771123,-4.62148276795247,45.4249788318269));
#32909=CARTESIAN_POINT('Ctrl Pts',(1.94021197405011,-4.5206874544515,45.440406653718));
#32910=CARTESIAN_POINT('Ctrl Pts',(2.03981162916243,-4.47662892002235,45.4466335932149));
#32911=CARTESIAN_POINT('Ctrl Pts',(2.17547080189338,-4.41115101470767,45.4552071992276));
#32912=CARTESIAN_POINT('Ctrl Pts',(2.21284176093993,-4.39252295204843,45.4575788890642));
#32913=CARTESIAN_POINT('Ctrl Pts',(2.28818566128753,-4.35376116652488,45.462378257421));
#32914=CARTESIAN_POINT('Ctrl Pts',(2.32614103420452,-4.33360102719604,45.4648054270167));
#32915=CARTESIAN_POINT('Ctrl Pts',(2.38757678877729,-4.29992948677457,45.4687541801362));
#32916=CARTESIAN_POINT('Ctrl Pts',(2.41121815923586,-4.28671710203116,45.470278636189));
#32917=CARTESIAN_POINT('Ctrl Pts',(2.50434035968479,-4.2336600558457,45.4763055907572));
#32918=CARTESIAN_POINT('Ctrl Pts',(2.57295291932214,-4.19231577167686,45.4807957195664));
#32919=CARTESIAN_POINT('Ctrl Pts',(2.76532995400544,-4.06989157198333,45.4935728907672));
#32920=CARTESIAN_POINT('Ctrl Pts',(2.88648683390808,-3.9848789883527,45.5018500353024));
#32921=CARTESIAN_POINT('Ctrl Pts',(3.0701713919727,-3.84321385976401,45.5148906865811));
#32922=CARTESIAN_POINT('Ctrl Pts',(3.13538891367781,-3.79019541417164,45.5196249140204));
#32923=CARTESIAN_POINT('Ctrl Pts',(3.25094911806792,-3.69122639542088,45.528222906272));
#32924=CARTESIAN_POINT('Ctrl Pts',(3.30175638848861,-3.64585066650713,45.5320806511759));
#32925=CARTESIAN_POINT('Ctrl Pts',(3.42548881726068,-3.53063753149932,45.5416796818153));
#32926=CARTESIAN_POINT('Ctrl Pts',(3.49723662300532,-3.45958243495677,45.5474303063531));
#32927=CARTESIAN_POINT('Ctrl Pts',(3.67060040491588,-3.27698440018866,45.5618104408424));
#32928=CARTESIAN_POINT('Ctrl Pts',(3.76936744070082,-3.16287888960564,45.570452604867));
#32929=CARTESIAN_POINT('Ctrl Pts',(3.91256339638757,-2.98119286481434,45.5836829904189));
#32930=CARTESIAN_POINT('Ctrl Pts',(3.96083360627183,-2.91675514774713,45.5882798741798));
#32931=CARTESIAN_POINT('Ctrl Pts',(4.02834085870301,-2.82186911917654,45.5949039482558));
#32932=CARTESIAN_POINT('Ctrl Pts',(4.04885930054713,-2.79234915496851,45.5969450939073));
#32933=CARTESIAN_POINT('Ctrl Pts',(4.09323065663019,-2.726994439585,45.6014194959053));
#32934=CARTESIAN_POINT('Ctrl Pts',(4.11694055136381,-2.69106604098175,45.6038505428661));
#32935=CARTESIAN_POINT('Ctrl Pts',(4.15483112291298,-2.63197616066168,45.6078069404788));
#32936=CARTESIAN_POINT('Ctrl Pts',(4.16929688215022,-2.60900051542786,45.6093351645887));
#32937=CARTESIAN_POINT('Ctrl Pts',(4.26500760017117,-2.4541562857412,45.6195716104849));
#32938=CARTESIAN_POINT('Ctrl Pts',(4.34017487930515,-2.31863225346499,45.6282293075763));
#32939=CARTESIAN_POINT('Ctrl Pts',(4.46334856339671,-2.06950201170173,45.6438078149792));
#32940=CARTESIAN_POINT('Ctrl Pts',(4.51371724031227,-1.95721105543012,45.6507134327288));
#32941=CARTESIAN_POINT('Ctrl Pts',(4.58350017711509,-1.78457311327604,45.6612125309867));
#32942=CARTESIAN_POINT('Ctrl Pts',(4.60604708267867,-1.72554490935836,45.6647819285775));
#32943=CARTESIAN_POINT('Ctrl Pts',(4.65240790264874,-1.59678162770063,45.6725313247727));
#32944=CARTESIAN_POINT('Ctrl Pts',(4.67580457067836,-1.52691267040807,45.6767133548468));
#32945=CARTESIAN_POINT('Ctrl Pts',(4.72149373703652,-1.37955680553916,45.6854925785876));
#32946=CARTESIAN_POINT('Ctrl Pts',(4.74346834116466,-1.30199385716819,45.690090531822));
#32947=CARTESIAN_POINT('Ctrl Pts',(4.80615380373544,-1.05802179905042,45.7044857041688));
#32948=CARTESIAN_POINT('Ctrl Pts',(4.84008449222577,-0.890003687634916,
45.7143061898907));
#32949=CARTESIAN_POINT('Ctrl Pts',(4.87421350493816,-0.65956612092834,45.7276064794889));
#32950=CARTESIAN_POINT('Ctrl Pts',(4.88209915447133,-0.59840850403533,45.7311198635342));
#32951=CARTESIAN_POINT('Ctrl Pts',(4.89288675943224,-0.500220087212699,
45.7367289499389));
#32952=CARTESIAN_POINT('Ctrl Pts',(4.89652278201866,-0.463277091424875,
45.7388318459252));
#32953=CARTESIAN_POINT('Ctrl Pts',(4.90501570200407,-0.365661572513761,
45.7443698473908));
#32954=CARTESIAN_POINT('Ctrl Pts',(4.90916519024006,-0.304933912648089,
45.7477972063098));
#32955=CARTESIAN_POINT('Ctrl Pts',(4.91453866462116,-0.196819580531643,
45.7538808705548));
#32956=CARTESIAN_POINT('Ctrl Pts',(4.91620677564324,-0.14946306025981,45.756539474544));
#32957=CARTESIAN_POINT('Ctrl Pts',(4.92189361766895,0.124445970225819,45.7719002336401));
#32958=CARTESIAN_POINT('Ctrl Pts',(4.91093653285998,0.35103376294935,45.7845554754239));
#32959=CARTESIAN_POINT('Ctrl Pts',(4.87633525461716,0.644419187943354,45.801216469747));
#32960=CARTESIAN_POINT('Ctrl Pts',(4.86683833838516,0.712605116679588,45.8051070538033));
#32961=CARTESIAN_POINT('Ctrl Pts',(4.84360078178829,0.857165824375748,45.8134033725237));
#32962=CARTESIAN_POINT('Ctrl Pts',(4.82947756941413,0.933460224990087,45.8178106482833));
#32963=CARTESIAN_POINT('Ctrl Pts',(4.7925450630197,1.10958346863074,45.8280595391863));
#32964=CARTESIAN_POINT('Ctrl Pts',(4.7684112608404,1.20909775560047,45.8339071619055));
#32965=CARTESIAN_POINT('Ctrl Pts',(4.69363257252425,1.48019723089021,45.8499966389717));
#32966=CARTESIAN_POINT('Ctrl Pts',(4.63670598893177,1.64988755801779,45.8602497912168));
#32967=CARTESIAN_POINT('Ctrl Pts',(4.55565763015683,1.85386569439065,45.8727386064233));
#32968=CARTESIAN_POINT('Ctrl Pts',(4.54018436532252,1.89144401138239,45.8750461274306));
#32969=CARTESIAN_POINT('Ctrl Pts',(4.50683097991679,1.96967756261372,45.8798621378424));
#32970=CARTESIAN_POINT('Ctrl Pts',(4.48886231822726,2.01029110656977,45.8823694520126));
#32971=CARTESIAN_POINT('Ctrl Pts',(4.44734563362257,2.1007957745788,45.8879799326976));
#32972=CARTESIAN_POINT('Ctrl Pts',(4.42350323855633,2.15054533695899,45.8910799668493));
#32973=CARTESIAN_POINT('Ctrl Pts',(4.33408973731834,2.32933420408152,45.9022991385344));
#32974=CARTESIAN_POINT('Ctrl Pts',(4.26366779019489,2.45586417089325,45.9103910202634));
#32975=CARTESIAN_POINT('Ctrl Pts',(4.13423258206288,2.66603198931017,45.9242355283345));
#32976=CARTESIAN_POINT('Ctrl Pts',(4.07800350870618,2.75127109863211,45.9299709606919));
#32977=CARTESIAN_POINT('Ctrl Pts',(3.98276619241932,2.88630288358257,45.9392878330335));
#32978=CARTESIAN_POINT('Ctrl Pts',(3.94537908589322,2.9372018384532,45.9428554071447));
#32979=CARTESIAN_POINT('Ctrl Pts',(3.86223383904292,3.04594322102908,45.9506066642937));
#32980=CARTESIAN_POINT('Ctrl Pts',(3.81613385355502,3.10350488505543,45.9547924055763));
#32981=CARTESIAN_POINT('Ctrl Pts',(3.71688262317771,3.22187605485955,45.9635830636077));
#32982=CARTESIAN_POINT('Ctrl Pts',(3.6634924841453,3.28245706514346,45.9681887564415));
#32983=CARTESIAN_POINT('Ctrl Pts',(3.49410966722076,3.46537044293843,45.9824354613477));
#32984=CARTESIAN_POINT('Ctrl Pts',(3.37330172476866,3.58307550573625,45.992098569051));
#32985=CARTESIAN_POINT('Ctrl Pts',(3.19928904300579,3.7360025212468,46.0053271329495));
#32986=CARTESIAN_POINT('Ctrl Pts',(3.15109042672226,3.77674389937413,46.0089234974014));
#32987=CARTESIAN_POINT('Ctrl Pts',(3.07330409305374,3.83996927440544,46.0146161569135));
#32988=CARTESIAN_POINT('Ctrl Pts',(3.04422297677568,3.86306466273359,46.0167201634709));
#32989=CARTESIAN_POINT('Ctrl Pts',(2.96783759724997,3.92232948639487,46.0221850312358));
#32990=CARTESIAN_POINT('Ctrl Pts',(2.92013309032495,3.95797315113337,46.0255386609284));
#32991=CARTESIAN_POINT('Ctrl Pts',(2.74281942140944,4.08550658480868,46.0378157037036));
#32992=CARTESIAN_POINT('Ctrl Pts',(2.60942651138046,4.17196791134512,46.046694222768));
#32993=CARTESIAN_POINT('Ctrl Pts',(2.37761780984614,4.30674550923241,46.0617287780626));
#32994=CARTESIAN_POINT('Ctrl Pts',(2.28134937478438,4.35850524529504,46.0678644043568));
#32995=CARTESIAN_POINT('Ctrl Pts',(2.12623389667045,4.43535658165048,46.0776224300681));
#32996=CARTESIAN_POINT('Ctrl Pts',(2.06848398677221,4.46258136903618,46.0812280333307));
#32997=CARTESIAN_POINT('Ctrl Pts',(1.94398460985409,4.518337533471,46.088950646614));
#32998=CARTESIAN_POINT('Ctrl Pts',(1.87710039746283,4.54653100302939,46.0930692070675));
#32999=CARTESIAN_POINT('Ctrl Pts',(1.67116933721871,4.62801741629052,46.1056683798968));
#33000=CARTESIAN_POINT('Ctrl Pts',(1.53030648425855,4.67648514033887,46.1141773521644));
#33001=CARTESIAN_POINT('Ctrl Pts',(1.24482303005975,4.76043111830867,46.1312104941889));
#33002=CARTESIAN_POINT('Ctrl Pts',(1.10035218850052,4.79588517080334,46.1397258550696));
#33003=CARTESIAN_POINT('Ctrl Pts',(0.914075982469187,4.83273689943749,46.150531978856));
#33004=CARTESIAN_POINT('Ctrl Pts',(0.873556017561933,4.84022528260812,46.152872071233));
#33005=CARTESIAN_POINT('Ctrl Pts',(0.800161749142142,4.85283739778018,46.1570897455529));
#33006=CARTESIAN_POINT('Ctrl Pts',(0.767320586425377,4.85813840678994,46.158969551156));
#33007=CARTESIAN_POINT('Ctrl Pts',(0.688458665127323,4.87004816219177,46.1634688761364));
#33008=CARTESIAN_POINT('Ctrl Pts',(0.64239293493654,4.87633836058237,46.1660851459559));
#33009=CARTESIAN_POINT('Ctrl Pts',(0.500571608007378,4.89365926467313,46.1741135716464));
#33010=CARTESIAN_POINT('Ctrl Pts',(0.404575224987392,4.9025291443336,46.1795116060477));
#33011=CARTESIAN_POINT('Ctrl Pts',(0.151696715111516,4.91841617697642,46.1937059351767));
#33012=CARTESIAN_POINT('Ctrl Pts',(-0.00536645851149809,4.92075197685467,
46.2024986355026));
#33013=CARTESIAN_POINT('Ctrl Pts',(-0.234024423337686,4.9132036235554,46.2153867872758));
#33014=CARTESIAN_POINT('Ctrl Pts',(-0.305717154346934,4.90926411420714,
46.2194397057122));
#33015=CARTESIAN_POINT('Ctrl Pts',(-0.440949467733291,4.89885927575076,
46.227116910916));
#33016=CARTESIAN_POINT('Ctrl Pts',(-0.504499709232383,4.89272302161677,
46.2307381972687));
#33017=CARTESIAN_POINT('Ctrl Pts',(-0.640936127073086,4.87686256991019,
46.2385468276733));
#33018=CARTESIAN_POINT('Ctrl Pts',(-0.713760196841688,4.86673749824665,
46.2427358358964));
#33019=CARTESIAN_POINT('Ctrl Pts',(-0.921122730406577,4.83315237106078,
46.2547286568073));
#33020=CARTESIAN_POINT('Ctrl Pts',(-1.05494785602666,4.80571676176551,46.262548459722));
#33021=CARTESIAN_POINT('Ctrl Pts',(-1.28355799641268,4.74883870666813,46.2760300861809));
#33022=CARTESIAN_POINT('Ctrl Pts',(-1.37891600958028,4.7220314666776,46.281690961334));
#33023=CARTESIAN_POINT('Ctrl Pts',(-1.51247704811039,4.68009335263922,46.289657048049));
#33024=CARTESIAN_POINT('Ctrl Pts',(-1.55139937187478,4.66733549915466,46.2919829932017));
#33025=CARTESIAN_POINT('Ctrl Pts',(-1.62172062730431,4.64330892283432,46.2961914964924));
#33026=CARTESIAN_POINT('Ctrl Pts',(-1.65317279934575,4.63220414806112,46.2980762050619));
#33027=CARTESIAN_POINT('Ctrl Pts',(-1.72850363467977,4.60474222141809,46.3025992078367));
#33028=CARTESIAN_POINT('Ctrl Pts',(-1.77226649997432,4.58807663937436,46.3052341896939));
#33029=CARTESIAN_POINT('Ctrl Pts',(-1.90678503063754,4.53463799956344,46.313367181336));
#33030=CARTESIAN_POINT('Ctrl Pts',(-1.99668569373937,4.49577772737781,46.3188506841471));
#33031=CARTESIAN_POINT('Ctrl Pts',(-2.22479790096022,4.38898161815378,46.332960827835));
#33032=CARTESIAN_POINT('Ctrl Pts',(-2.36108582819033,4.31719333819467,46.3415843953433));
#33033=CARTESIAN_POINT('Ctrl Pts',(-2.55579287632227,4.20265179746592,46.3543096493054));
#33034=CARTESIAN_POINT('Ctrl Pts',(-2.61699645376738,4.16481557356469,46.3583710833446));
#33035=CARTESIAN_POINT('Ctrl Pts',(-2.73093110491114,4.0908775022895,46.366058860214));
#33036=CARTESIAN_POINT('Ctrl Pts',(-2.78383178685674,4.05506398308684,46.369682164309));
#33037=CARTESIAN_POINT('Ctrl Pts',(-2.89594346897092,3.97593688581185,46.377483053367));
#33038=CARTESIAN_POINT('Ctrl Pts',(-2.95491341700867,3.93230838627995,46.3816622509292));
#33039=CARTESIAN_POINT('Ctrl Pts',(-3.12004082878083,3.80432753147657,46.3935891831376));
#33040=CARTESIAN_POINT('Ctrl Pts',(-3.22371628748125,3.71688252225012,46.4013526723324));
#33041=CARTESIAN_POINT('Ctrl Pts',(-3.39813335670504,3.55697690137453,46.4148945207923));
#33042=CARTESIAN_POINT('Ctrl Pts',(-3.47049909523308,3.4864066567695,46.4206713908966));
#33043=CARTESIAN_POINT('Ctrl Pts',(-3.56896221032236,3.38428085408461,46.4287435889162));
#33044=CARTESIAN_POINT('Ctrl Pts',(-3.59691811318429,3.35455336935347,46.4310607812354));
#33045=CARTESIAN_POINT('Ctrl Pts',(-3.64708576399759,3.29985830680953,46.4352637811368));
#33046=CARTESIAN_POINT('Ctrl Pts',(-3.66941909082484,3.27500579829361,46.4371516928107));
#33047=CARTESIAN_POINT('Ctrl Pts',(-3.7225833251807,3.21461809975419,46.4416900609624));
#33048=CARTESIAN_POINT('Ctrl Pts',(-3.75316107328171,3.17886428675401,46.4443371644146));
#33049=CARTESIAN_POINT('Ctrl Pts',(-3.84643118164115,3.06658375184157,46.4525385286616));
#33050=CARTESIAN_POINT('Ctrl Pts',(-3.90733120635388,2.98860030472879,46.4580780285142));
#33051=CARTESIAN_POINT('Ctrl Pts',(-4.05574806752662,2.78625206504129,46.4721360378995));
#33052=CARTESIAN_POINT('Ctrl Pts',(-4.13992539438346,2.65956950794021,46.4806517584734));
#33053=CARTESIAN_POINT('Ctrl Pts',(-4.25514462496286,2.46741092487962,46.4932727921975));
#33054=CARTESIAN_POINT('Ctrl Pts',(-4.2908274658301,2.40482264480861,46.4973392684591));
#33055=CARTESIAN_POINT('Ctrl Pts',(-4.35554409044418,2.2852794172165,46.5050333304892));
#33056=CARTESIAN_POINT('Ctrl Pts',(-4.38486748948721,2.22849799730318,46.5086578548998));
#33057=CARTESIAN_POINT('Ctrl Pts',(-4.44541123581498,2.10543754354329,46.5164543251374));
#33058=CARTESIAN_POINT('Ctrl Pts',(-4.476273967928,2.03899963735559,46.5206278535098));
#33059=CARTESIAN_POINT('Ctrl Pts',(-4.5597712063157,1.84821459636023,46.5325168921725));
#33060=CARTESIAN_POINT('Ctrl Pts',(-4.60878526973432,1.72235554743886,46.5402480220065));
#33061=CARTESIAN_POINT('Ctrl Pts',(-4.68552732309619,1.49845122849291,46.5537938975573));
#33062=CARTESIAN_POINT('Ctrl Pts',(-4.7155051100487,1.40126168137821,46.5596069261676));
#33063=CARTESIAN_POINT('Ctrl Pts',(-4.74987553743386,1.27618611588959,46.5669880081433));
#33064=CARTESIAN_POINT('Ctrl Pts',(-4.75707104127008,1.24909716417162,46.5685806726222));
#33065=CARTESIAN_POINT('Ctrl Pts',(-4.7640345870679,1.22194824592564,46.5701705954582));
#33066=CARTESIAN_POINT('Origin',(0.,0.,-3.23514056400928));
#33067=CARTESIAN_POINT('',(-4.76403458580012,1.22194825086837,48.6654127926075));
#33068=CARTESIAN_POINT('',(-4.76366299354682,1.22185269443844,48.3199247396258));
#33069=CARTESIAN_POINT('',(-4.76403458704967,1.22194824599672,-3.23514056400928));
#33070=CARTESIAN_POINT('Ctrl Pts',(-4.76403458580012,1.22194825086837,48.6654127926075));
#33071=CARTESIAN_POINT('Ctrl Pts',(-4.75303754389474,1.26482264259609,48.6628924344214));
#33072=CARTESIAN_POINT('Ctrl Pts',(-4.74146170699504,1.30754864644256,48.6603686712803));
#33073=CARTESIAN_POINT('Ctrl Pts',(-4.6642949204399,1.5778558275802,48.6443229989067));
#33074=CARTESIAN_POINT('Ctrl Pts',(-4.58291454291531,1.80060275079479,48.6307254558902));
#33075=CARTESIAN_POINT('Ctrl Pts',(-4.46932232969459,2.05327950110843,48.6149576556254));
#33076=CARTESIAN_POINT('Ctrl Pts',(-4.45239183251398,2.08973821655184,48.6126743042949));
#33077=CARTESIAN_POINT('Ctrl Pts',(-4.41707807004089,2.16340621913512,48.608045903262));
#33078=CARTESIAN_POINT('Ctrl Pts',(-4.39866693276733,2.20059864818217,48.6057014917757));
#33079=CARTESIAN_POINT('Ctrl Pts',(-4.31628671382158,2.36184966075428,48.5954922648057));
#33080=CARTESIAN_POINT('Ctrl Pts',(-4.24752314980106,2.4833873582621,48.587678779137));
#33081=CARTESIAN_POINT('Ctrl Pts',(-4.1146351352696,2.69655694146925,48.5736062541915));
#33082=CARTESIAN_POINT('Ctrl Pts',(-4.05238031777689,2.7892391736651,48.5673538816942));
#33083=CARTESIAN_POINT('Ctrl Pts',(-3.93628663267689,2.94997292719581,48.5562110966866));
#33084=CARTESIAN_POINT('Ctrl Pts',(-3.88369927891628,3.01886938925748,48.5513309266917));
#33085=CARTESIAN_POINT('Ctrl Pts',(-3.81163004673214,3.10828796741809,48.5448426748559));
#33086=CARTESIAN_POINT('Ctrl Pts',(-3.79375213020502,3.13008345995897,48.5432486240844));
#33087=CARTESIAN_POINT('Ctrl Pts',(-3.73546804546558,3.1999063612482,48.538100321165));
#33088=CARTESIAN_POINT('Ctrl Pts',(-3.69432988336773,3.24731409694626,48.5345401929561));
#33089=CARTESIAN_POINT('Ctrl Pts',(-3.56936625662945,3.385873621345,48.5239332958891));
#33090=CARTESIAN_POINT('Ctrl Pts',(-3.48299441442204,3.47466040436883,48.5168669703973));
#33091=CARTESIAN_POINT('Ctrl Pts',(-3.30086857688185,3.64825689531583,48.502475260776));
#33092=CARTESIAN_POINT('Ctrl Pts',(-3.20497104389534,3.73278346399049,48.4951541685068));
#33093=CARTESIAN_POINT('Ctrl Pts',(-3.0652842607331,3.84655145807064,48.4848591277372));
#33094=CARTESIAN_POINT('Ctrl Pts',(-3.02415178075368,3.87897303298115,48.4818703976402));
#33095=CARTESIAN_POINT('Ctrl Pts',(-2.97239359215439,3.91844627820362,48.4781643582133));
#33096=CARTESIAN_POINT('Ctrl Pts',(-2.96224812801155,3.92612161442486,48.4774404833506));
#33097=CARTESIAN_POINT('Ctrl Pts',(-2.92272183294512,3.95578396832812,48.474630372241));
#33098=CARTESIAN_POINT('Ctrl Pts',(-2.89312481939677,3.97748143284406,48.4725477342435));
#33099=CARTESIAN_POINT('Ctrl Pts',(-2.82621348676924,4.02539185159751,48.4678888505519));
#33100=CARTESIAN_POINT('Ctrl Pts',(-2.78877184680265,4.05142121789256,48.4653152037406));
#33101=CARTESIAN_POINT('Ctrl Pts',(-2.58817034026317,4.18678039714364,48.4516838354521));
#33102=CARTESIAN_POINT('Ctrl Pts',(-2.41893191871587,4.28678499770639,48.4407220192644));
#33103=CARTESIAN_POINT('Ctrl Pts',(-2.17135187563102,4.41374107318464,48.4251157639514));
#33104=CARTESIAN_POINT('Ctrl Pts',(-2.09761701939299,4.44925633162107,48.4205199426548));
#33105=CARTESIAN_POINT('Ctrl Pts',(-1.96386414320659,4.50961576188982,48.4122563520596));
#33106=CARTESIAN_POINT('Ctrl Pts',(-1.90417495083866,4.53514215172833,48.408594016453));
#33107=CARTESIAN_POINT('Ctrl Pts',(-1.78176302313206,4.58464942672549,48.4011264682826));
#33108=CARTESIAN_POINT('Ctrl Pts',(-1.71901927760205,4.6085423321158,48.3973214322091));
#33109=CARTESIAN_POINT('Ctrl Pts',(-1.54639272399786,4.67026277032317,48.3869057516458));
#33110=CARTESIAN_POINT('Ctrl Pts',(-1.43562806269652,4.70549214286965,48.3802796869801));
#33111=CARTESIAN_POINT('Ctrl Pts',(-1.1891168777845,4.77438136079565,48.3656467942903));
#33112=CARTESIAN_POINT('Ctrl Pts',(-1.05297062617578,4.80624272507219,48.3576384230074));
#33113=CARTESIAN_POINT('Ctrl Pts',(-0.862331998949356,4.8423663412981,48.3465481135928));
#33114=CARTESIAN_POINT('Ctrl Pts',(-0.808847239355958,4.85158679943994,
48.343450234862));
#33115=CARTESIAN_POINT('Ctrl Pts',(-0.750515640683471,4.86065139734147,
48.3400885263398));
#33116=CARTESIAN_POINT('Ctrl Pts',(-0.745809651932119,4.86137569999868,
48.3398174351423));
#33117=CARTESIAN_POINT('Ctrl Pts',(-0.737053794662226,4.86271030805719,
48.3393132743604));
#33118=CARTESIAN_POINT('Ctrl Pts',(-0.733004201968457,4.86332239073774,
48.3390801891424));
#33119=CARTESIAN_POINT('Ctrl Pts',(-0.725392381982326,4.86446316910591,
48.3386422406758));
#33120=CARTESIAN_POINT('Ctrl Pts',(-0.721830329842567,4.86499301195546,
48.3384373669482));
#33121=CARTESIAN_POINT('Ctrl Pts',(-0.686263474119796,4.87024353586656,
48.336392422659));
#33122=CARTESIAN_POINT('Ctrl Pts',(-0.654213216469832,4.87465226937502,
48.3345553714382));
#33123=CARTESIAN_POINT('Ctrl Pts',(-0.58211396174379,4.88384613156159,48.330436817779));
#33124=CARTESIAN_POINT('Ctrl Pts',(-0.542044820161591,4.8884554979055,48.3281577666747));
#33125=CARTESIAN_POINT('Ctrl Pts',(-0.399496136925092,4.9030794032398,48.3200765610388));
#33126=CARTESIAN_POINT('Ctrl Pts',(-0.296763194101059,4.91036829958464,
48.3143009176158));
#33127=CARTESIAN_POINT('Ctrl Pts',(-0.0600540263897964,4.91970658415861,
48.3010241931034));
#33128=CARTESIAN_POINT('Ctrl Pts',(0.0739277198397528,4.91951764794321,
48.2935313154881));
#33129=CARTESIAN_POINT('Ctrl Pts',(0.280398341796046,4.91078907786969,48.2819269053482));
#33130=CARTESIAN_POINT('Ctrl Pts',(0.352985059510516,4.90610578889122,48.2778365879361));
#33131=CARTESIAN_POINT('Ctrl Pts',(0.481394691086985,4.89495624746205,48.2705695095219));
#33132=CARTESIAN_POINT('Ctrl Pts',(0.537260985603083,4.88913980890141,48.2673974260488));
#33133=CARTESIAN_POINT('Ctrl Pts',(0.6067623182586,4.88069813929903,48.2634351632392));
#33134=CARTESIAN_POINT('Ctrl Pts',(0.620502446742907,4.87897033709223,48.262651062411));
#33135=CARTESIAN_POINT('Ctrl Pts',(0.64136944592651,4.87625676686008,48.2614590300712));
#33136=CARTESIAN_POINT('Ctrl Pts',(0.648501768587642,4.87531335182571,48.2610513765754));
#33137=CARTESIAN_POINT('Ctrl Pts',(0.661435319590417,4.87357370606498,48.2603117472468));
#33138=CARTESIAN_POINT('Ctrl Pts',(0.667237246958959,4.87278275799693,48.2599798062885));
#33139=CARTESIAN_POINT('Ctrl Pts',(0.754304513682832,4.8607548885599,48.2549962632995));
#33140=CARTESIAN_POINT('Ctrl Pts',(0.835276931303859,4.84749683903627,48.2503320819304));
#33141=CARTESIAN_POINT('Ctrl Pts',(1.04662543163158,4.80743871304497,48.2380710341535));
#33142=CARTESIAN_POINT('Ctrl Pts',(1.1763111593641,4.77736154029793,48.230458737242));
#33143=CARTESIAN_POINT('Ctrl Pts',(1.42998068659116,4.70757305959692,48.2153979006798));
#33144=CARTESIAN_POINT('Ctrl Pts',(1.5539292727806,4.66812523867936,48.2079555835195));
#33145=CARTESIAN_POINT('Ctrl Pts',(1.71546723190841,4.60956640886055,48.1981751634847));
#33146=CARTESIAN_POINT('Ctrl Pts',(1.75458190978384,4.59482020077466,48.1958006552776));
#33147=CARTESIAN_POINT('Ctrl Pts',(1.82704982883147,4.56643952044413,48.1913918016926));
#33148=CARTESIAN_POINT('Ctrl Pts',(1.8604503941377,4.55293370666031,48.1893559053022));
#33149=CARTESIAN_POINT('Ctrl Pts',(2.04489923213447,4.47598152621719,48.1780823379656));
#33150=CARTESIAN_POINT('Ctrl Pts',(2.19285423533883,4.40538478572691,48.1689211344716));
#33151=CARTESIAN_POINT('Ctrl Pts',(2.45843468403153,4.2619626263181,48.1520098539088));
#33152=CARTESIAN_POINT('Ctrl Pts',(2.57704349331808,4.19130919054859,48.1442732035657));
#33153=CARTESIAN_POINT('Ctrl Pts',(2.75253858464446,4.07650067528572,48.132456942591));
#33154=CARTESIAN_POINT('Ctrl Pts',(2.8116875800779,4.03593102166855,48.1284074160317));
#33155=CARTESIAN_POINT('Ctrl Pts',(2.9213405831657,3.95714041618647,48.1207629412454));
#33156=CARTESIAN_POINT('Ctrl Pts',(2.9720348988324,3.91920904338425,48.1171710961738));
#33157=CARTESIAN_POINT('Ctrl Pts',(3.17553927009412,3.76071999014652,48.102504903297));
#33158=CARTESIAN_POINT('Ctrl Pts',(3.32186002951284,3.632121765171,48.0913699268091));
#33159=CARTESIAN_POINT('Ctrl Pts',(3.51668074889294,3.43925313872698,48.0756785460131));
#33160=CARTESIAN_POINT('Ctrl Pts',(3.57182382760129,3.38194918804823,48.0711298591407));
#33161=CARTESIAN_POINT('Ctrl Pts',(3.64373552795213,3.30349791769414,48.065057587666));
#33162=CARTESIAN_POINT('Ctrl Pts',(3.66175447186355,3.28351355835378,48.0635237535942));
#33163=CARTESIAN_POINT('Ctrl Pts',(3.70793661102508,3.23144114360145,48.0595611483295));
#33164=CARTESIAN_POINT('Ctrl Pts',(3.73584777409445,3.19913226373311,48.0571353877461));
#33165=CARTESIAN_POINT('Ctrl Pts',(3.78981022463852,3.13499801644038,48.0523864005284));
#33166=CARTESIAN_POINT('Ctrl Pts',(3.8158900242568,3.10320116501748,48.0500629835909));
#33167=CARTESIAN_POINT('Ctrl Pts',(3.9753005955451,2.90379691050782,48.0356679482412));
#33168=CARTESIAN_POINT('Ctrl Pts',(4.09796491273494,2.7279547252578,48.0237231670548));
#33169=CARTESIAN_POINT('Ctrl Pts',(4.24985461810598,2.47673615945525,48.0072528160032));
#33170=CARTESIAN_POINT('Ctrl Pts',(4.28928064730019,2.4078117972733,48.0027924499705));
#33171=CARTESIAN_POINT('Ctrl Pts',(4.36163080785308,2.27390867707941,47.9942191983198));
#33172=CARTESIAN_POINT('Ctrl Pts',(4.39481397379133,2.20909346782165,47.9901092684121));
#33173=CARTESIAN_POINT('Ctrl Pts',(4.45754972226028,2.07954175005782,47.9819618793521));
#33174=CARTESIAN_POINT('Ctrl Pts',(4.4871607051686,2.01485286459132,47.9779258890107));
#33175=CARTESIAN_POINT('Ctrl Pts',(4.58985476581203,1.77700227111699,47.9631910844896));
#33176=CARTESIAN_POINT('Ctrl Pts',(4.65439960562896,1.60033322789052,47.9524392017229));
#33177=CARTESIAN_POINT('Ctrl Pts',(4.73202577667529,1.34300116146957,47.9370539730218));
#33178=CARTESIAN_POINT('Ctrl Pts',(4.7534638685057,1.26503021618401,47.9324284489329));
#33179=CARTESIAN_POINT('Ctrl Pts',(4.77952911296729,1.16018258193309,47.9262635610203));
#33180=CARTESIAN_POINT('Ctrl Pts',(4.78586920606005,1.13374517334062,47.9247137333008));
#33181=CARTESIAN_POINT('Ctrl Pts',(4.80166596832494,1.06537987070928,47.9207186763261));
#33182=CARTESIAN_POINT('Ctrl Pts',(4.81079287292074,1.02337790240683,47.9182764657055));
#33183=CARTESIAN_POINT('Ctrl Pts',(4.82641953903688,0.94662908029733,47.9138384416466));
#33184=CARTESIAN_POINT('Ctrl Pts',(4.83309748216093,0.911921563760926,47.9118406586812));
#33185=CARTESIAN_POINT('Ctrl Pts',(4.85347192577036,0.799511289832573,47.9053948598819));
#33186=CARTESIAN_POINT('Ctrl Pts',(4.86567307431019,0.721549583718809,47.9009620806211));
#33187=CARTESIAN_POINT('Ctrl Pts',(4.89593234926585,0.492204455999454,47.8879847305294));
#33188=CARTESIAN_POINT('Ctrl Pts',(4.90883470072782,0.34023624816981,47.879463315341));
#33189=CARTESIAN_POINT('Ctrl Pts',(4.91852211739972,0.0868748200415349,
47.8652321187964));
#33190=CARTESIAN_POINT('Ctrl Pts',(4.91926858074732,-0.0142592399419988,
47.8595457113945));
#33191=CARTESIAN_POINT('Ctrl Pts',(4.91531335454737,-0.182863935874622,
47.8500258182428));
#33192=CARTESIAN_POINT('Ctrl Pts',(4.91233877781006,-0.250344142856869,
47.846205177139));
#33193=CARTESIAN_POINT('Ctrl Pts',(4.90256575788774,-0.401302687876723,
47.837626502624));
#33194=CARTESIAN_POINT('Ctrl Pts',(4.89502290207981,-0.484711670499982,
47.8328647172573));
#33195=CARTESIAN_POINT('Ctrl Pts',(4.86452766185561,-0.747052866051986,
47.8178073628029));
#33196=CARTESIAN_POINT('Ctrl Pts',(4.83386061011668,-0.924936762342858,
47.8074740292203));
#33197=CARTESIAN_POINT('Ctrl Pts',(4.78353618054063,-1.1440908347425,47.794612060784));
#33198=CARTESIAN_POINT('Ctrl Pts',(4.77299167587137,-1.18731323513527,47.7920692481349));
#33199=CARTESIAN_POINT('Ctrl Pts',(4.74721779457032,-1.28706371613804,47.7861888479533));
#33200=CARTESIAN_POINT('Ctrl Pts',(4.73156256312988,-1.34347520497131,47.7828543092827));
#33201=CARTESIAN_POINT('Ctrl Pts',(4.70444145324473,-1.43483984963031,47.7774435781429));
#33202=CARTESIAN_POINT('Ctrl Pts',(4.69358409291108,-1.46996706811822,47.7753612148406));
#33203=CARTESIAN_POINT('Ctrl Pts',(4.66327426867004,-1.56426844229901,47.7697636854469));
#33204=CARTESIAN_POINT('Ctrl Pts',(4.64308987378551,-1.62320030460303,47.7662568963771));
#33205=CARTESIAN_POINT('Ctrl Pts',(4.56235645420327,-1.84507437534824,47.7529897459448));
#33206=CARTESIAN_POINT('Ctrl Pts',(4.49430402249567,-2.00515029816352,47.7432806749226));
#33207=CARTESIAN_POINT('Ctrl Pts',(4.38328656983293,-2.2320827424771,47.7291059923235));
#33208=CARTESIAN_POINT('Ctrl Pts',(4.34695641970232,-2.30203480719245,47.7246778532811));
#33209=CARTESIAN_POINT('Ctrl Pts',(4.27399531316522,-2.43462677535857,47.7161523846378));
#33210=CARTESIAN_POINT('Ctrl Pts',(4.23762827201911,-2.49738862415717,47.7120579047293));
#33211=CARTESIAN_POINT('Ctrl Pts',(4.16721354162531,-2.61294024875061,47.7043983415211));
#33212=CARTESIAN_POINT('Ctrl Pts',(4.133516656118,-2.66592674138782,47.7008367356476));
#33213=CARTESIAN_POINT('Ctrl Pts',(4.03007693956113,-2.82190199976728,47.690197289983));
#33214=CARTESIAN_POINT('Ctrl Pts',(3.95743303831563,-2.9229050853989,47.683099666067));
#33215=CARTESIAN_POINT('Ctrl Pts',(3.78670043297433,-3.14223981312442,47.6672006945333));
#33216=CARTESIAN_POINT('Ctrl Pts',(3.68673563025272,-3.25894950128983,47.65839839722));
#33217=CARTESIAN_POINT('Ctrl Pts',(3.56316523770292,-3.39024338074211,47.6481114343637));
#33218=CARTESIAN_POINT('Ctrl Pts',(3.54469828562453,-3.40954700302093,47.6465887288417));
#33219=CARTESIAN_POINT('Ctrl Pts',(3.49645136405402,-3.45916414534776,47.6426487413427));
#33220=CARTESIAN_POINT('Ctrl Pts',(3.46643400080861,-3.48924405841904,47.64023446429));
#33221=CARTESIAN_POINT('Ctrl Pts',(3.40648358352317,-3.54778212904583,47.6354871483765));
#33222=CARTESIAN_POINT('Ctrl Pts',(3.37657437468378,-3.57625977524213,47.6331540119713));
#33223=CARTESIAN_POINT('Ctrl Pts',(3.24135203266903,-3.70180110992867,47.622750328646));
#33224=CARTESIAN_POINT('Ctrl Pts',(3.13218679708534,-3.79461476924618,47.6147343540386));
#33225=CARTESIAN_POINT('Ctrl Pts',(2.89679303577249,-3.97766111285555,47.5980292700516));
#33226=CARTESIAN_POINT('Ctrl Pts',(2.77003357136678,-4.0669535342024,47.5893475961262));
#33227=CARTESIAN_POINT('Ctrl Pts',(2.57886482687568,-4.18852766879431,47.576582091614));
#33228=CARTESIAN_POINT('Ctrl Pts',(2.51762692349932,-4.22561975885131,47.5725397445375));
#33229=CARTESIAN_POINT('Ctrl Pts',(2.39297341365977,-4.29745111162775,47.5643943211198));
#33230=CARTESIAN_POINT('Ctrl Pts',(2.32955763837787,-4.33215522126321,47.5602920254007));
#33231=CARTESIAN_POINT('Ctrl Pts',(2.11722984382941,-4.4423403438575,47.5466822876123));
#33232=CARTESIAN_POINT('Ctrl Pts',(1.96524204965621,-4.51163743901042,47.5371363871577));
#33233=CARTESIAN_POINT('Ctrl Pts',(1.72599907859158,-4.60633012185658,47.5224071868318));
#33234=CARTESIAN_POINT('Ctrl Pts',(1.64106937830969,-4.63726659179377,47.5172346760096));
#33235=CARTESIAN_POINT('Ctrl Pts',(1.49836072064465,-4.68483777982797,47.508647291654));
#33236=CARTESIAN_POINT('Ctrl Pts',(1.4410425100728,-4.7027849706762,47.5052256583635));
#33237=CARTESIAN_POINT('Ctrl Pts',(1.34814514675965,-4.73001460341539,47.4997290512453));
#33238=CARTESIAN_POINT('Ctrl Pts',(1.31276596276615,-4.73995559599478,47.4976473721149));
#33239=CARTESIAN_POINT('Ctrl Pts',(1.21873704019795,-4.76524270245113,47.4921442587624));
#33240=CARTESIAN_POINT('Ctrl Pts',(1.15990925898567,-4.77990257526431,47.4887305535973));
#33241=CARTESIAN_POINT('Ctrl Pts',(0.929494315149827,-4.83281757634785,
47.4754437350207));
#33242=CARTESIAN_POINT('Ctrl Pts',(0.756176683350233,-4.86295000914482,
47.465625189658));
#33243=CARTESIAN_POINT('Ctrl Pts',(0.503103990241899,-4.89308913848179,
47.4513258755639));
#33244=CARTESIAN_POINT('Ctrl Pts',(0.42437644322709,-4.90054480863743,47.4468835114652));
#33245=CARTESIAN_POINT('Ctrl Pts',(0.273031839978224,-4.91120300227536,
47.4383369583662));
#33246=CARTESIAN_POINT('Ctrl Pts',(0.200456141789944,-4.91470024410186,
47.434235665806));
#33247=CARTESIAN_POINT('Ctrl Pts',(0.0651328152686634,-4.91821862052928,
47.426573296535));
#33248=CARTESIAN_POINT('Ctrl Pts',(0.00241042781142184,-4.9186492825689,
47.4230157519239));
#33249=CARTESIAN_POINT('Ctrl Pts',(-0.186097200726497,-4.91633782000799,
47.4122990793651));
#33250=CARTESIAN_POINT('Ctrl Pts',(-0.311784935807075,-4.90996937023799,
47.4051194869341));
#33251=CARTESIAN_POINT('Ctrl Pts',(-0.589663021321053,-4.88517603174792,
47.3891611670502));
#33252=CARTESIAN_POINT('Ctrl Pts',(-0.741518491739819,-4.86444220063292,
47.3803821241481));
#33253=CARTESIAN_POINT('Ctrl Pts',(-0.94629052197749,-4.82667041349628,
47.3685022456834));
#33254=CARTESIAN_POINT('Ctrl Pts',(-1.00025149998599,-4.81577720316449,
47.3653680582164));
#33255=CARTESIAN_POINT('Ctrl Pts',(-1.09009215122276,-4.79606569015607,
47.3601478672556));
#33256=CARTESIAN_POINT('Ctrl Pts',(-1.12607529254975,-4.78774492534716,
47.3580569241787));
#33257=CARTESIAN_POINT('Ctrl Pts',(-1.22530216223133,-4.7636190918068,47.3522880574088));
#33258=CARTESIAN_POINT('Ctrl Pts',(-1.28833070625862,-4.7469607526224,47.3486195796319));
#33259=CARTESIAN_POINT('Ctrl Pts',(-1.44937972124869,-4.70095180164654,
47.3392113475052));
#33260=CARTESIAN_POINT('Ctrl Pts',(-1.54684908956789,-4.66978666546042,
47.333483619902));
#33261=CARTESIAN_POINT('Ctrl Pts',(-1.78061095577791,-4.58692039981277,
47.3195889336479));
#33262=CARTESIAN_POINT('Ctrl Pts',(-1.91571347933162,-4.53215790936684,
47.3114236486186));
#33263=CARTESIAN_POINT('Ctrl Pts',(-2.11388373748844,-4.44138499816671,
47.2991438858045));
#33264=CARTESIAN_POINT('Ctrl Pts',(-2.17891160660056,-4.40984684646401,
47.2950640704293));
#33265=CARTESIAN_POINT('Ctrl Pts',(-2.30694319855285,-4.34422873869995,
47.2869199893593));
#33266=CARTESIAN_POINT('Ctrl Pts',(-2.36994462660249,-4.3101824280194,47.2828568972153));
#33267=CARTESIAN_POINT('Ctrl Pts',(-2.58484756171685,-4.18791100942648,
47.2687925096789));
#33268=CARTESIAN_POINT('Ctrl Pts',(-2.73275081375529,-4.0929337997907,47.2587468117316));
#33269=CARTESIAN_POINT('Ctrl Pts',(-2.94571173711156,-3.93948058655288,
47.2437208855272));
#33270=CARTESIAN_POINT('Ctrl Pts',(-3.01481278215812,-3.88685334847058,
47.2387510416746));
#33271=CARTESIAN_POINT('Ctrl Pts',(-3.12823159189639,-3.79562865324191,
47.2304431938363));
#33272=CARTESIAN_POINT('Ctrl Pts',(-3.1733167350476,-3.75801686829642,47.2270988870086));
#33273=CARTESIAN_POINT('Ctrl Pts',(-3.24552095616936,-3.69555520318063,
47.2216785996092));
#33274=CARTESIAN_POINT('Ctrl Pts',(-3.27305333608773,-3.67119278076716,
47.2195963883072));
#33275=CARTESIAN_POINT('Ctrl Pts',(-3.34634430804191,-3.60486030139422,
47.2140101632542));
#33276=CARTESIAN_POINT('Ctrl Pts',(-3.39158562006607,-3.56232861226026,
47.2105144490869));
#33277=CARTESIAN_POINT('Ctrl Pts',(-3.5588455171225,-3.39901102313036,47.1973782663349));
#33278=CARTESIAN_POINT('Ctrl Pts',(-3.67531719541145,-3.27272078917271,
47.1877879220347));
#33279=CARTESIAN_POINT('Ctrl Pts',(-3.83581011916303,-3.07929999369034,
47.1736872977697));
#33280=CARTESIAN_POINT('Ctrl Pts',(-3.88517660059196,-3.01677482529704,
47.1692124523823));
#33281=CARTESIAN_POINT('Ctrl Pts',(-3.97679368312251,-2.89475633526866,
47.1606177250242));
#33282=CARTESIAN_POINT('Ctrl Pts',(-4.01928179313411,-2.83546749998651,
47.1565008465802));
#33283=CARTESIAN_POINT('Ctrl Pts',(-4.10051938974657,-2.71661000251498,
47.1483522454192));
#33284=CARTESIAN_POINT('Ctrl Pts',(-4.13932776346384,-2.65710268562874,
47.1443220575799));
#33285=CARTESIAN_POINT('Ctrl Pts',(-4.28959196379171,-2.4154074170201,47.1281360324337));
#33286=CARTESIAN_POINT('Ctrl Pts',(-4.39041649763644,-2.22688861774463,
47.1159074473785));
#33287=CARTESIAN_POINT('Ctrl Pts',(-4.49839469111282,-1.98894626880638,
47.1009579096944));
#33288=CARTESIAN_POINT('Ctrl Pts',(-4.51748837025478,-1.94518917148043,
47.0982285042523));
#33289=CARTESIAN_POINT('Ctrl Pts',(-4.55952006317209,-1.84490659050137,
47.0920206470637));
#33290=CARTESIAN_POINT('Ctrl Pts',(-4.58204975855493,-1.78821801594125,
47.0885451537726));
#33291=CARTESIAN_POINT('Ctrl Pts',(-4.6164545839381,-1.69672646292976,47.0829947330628));
#33292=CARTESIAN_POINT('Ctrl Pts',(-4.62900386931649,-1.66218435635961,
47.0809127692859));
#33293=CARTESIAN_POINT('Ctrl Pts',(-4.66091941758763,-1.57117057610563,
47.0754613878824));
#33294=CARTESIAN_POINT('Ctrl Pts',(-4.67964671979863,-1.51448126474898,
47.0720993421993));
#33295=CARTESIAN_POINT('Ctrl Pts',(-4.74976254563909,-1.28850137310328,
47.0588001798797));
#33296=CARTESIAN_POINT('Ctrl Pts',(-4.79303317872285,-1.11683193531472,
47.0489195370147));
#33297=CARTESIAN_POINT('Ctrl Pts',(-4.84215167289235,-0.865462227076943,
47.034549605177));
#33298=CARTESIAN_POINT('Ctrl Pts',(-4.85546229926689,-0.787364842118274,
47.030099255353));
#33299=CARTESIAN_POINT('Ctrl Pts',(-4.87736378605435,-0.637019507328562,
47.0215408617709));
#33300=CARTESIAN_POINT('Ctrl Pts',(-4.88624930102355,-0.564835339769297,
47.0174357407346));
#33301=CARTESIAN_POINT('Ctrl Pts',(-4.89980735586483,-0.430115987474027,
47.0097717378524));
#33302=CARTESIAN_POINT('Ctrl Pts',(-4.90489091934934,-0.367636843723732,
47.0062164186091));
#33303=CARTESIAN_POINT('Ctrl Pts',(-4.91509408357548,-0.203465495901944,
46.9968661112378));
#33304=CARTESIAN_POINT('Ctrl Pts',(-4.91825257506775,-0.101682306156651,
46.9910603738107));
#33305=CARTESIAN_POINT('Ctrl Pts',(-4.91824501973881,0.196839665486888,
46.9739978707272));
#33306=CARTESIAN_POINT('Ctrl Pts',(-4.90643805323138,0.393377564105095,
46.9627139993045));
#33307=CARTESIAN_POINT('Ctrl Pts',(-4.87745889323441,0.633749680902723,
46.9489218794627));
#33308=CARTESIAN_POINT('Ctrl Pts',(-4.87140144799517,0.678742889758802,
46.9463410435686));
#33309=CARTESIAN_POINT('Ctrl Pts',(-4.85893885155642,0.762522882634252,
46.9415395638995));
#33310=CARTESIAN_POINT('Ctrl Pts',(-4.85268996844676,0.801328902813746,
46.9393175718323));
#33311=CARTESIAN_POINT('Ctrl Pts',(-4.82751650861538,0.946545363256888,
46.9310025349431));
#33312=CARTESIAN_POINT('Ctrl Pts',(-4.80555118266694,1.05239826538985,46.9249403681993));
#33313=CARTESIAN_POINT('Ctrl Pts',(-4.77490049252517,1.17898241002546,46.9176411071331));
#33314=CARTESIAN_POINT('Ctrl Pts',(-4.76953983018175,1.20048484241867,46.9163994793669));
#33315=CARTESIAN_POINT('Ctrl Pts',(-4.76403458328184,1.22194826068645,46.9151580697526));
#33316=CARTESIAN_POINT('',(-4.91785582195738,6.53930245273875E-6,46.6398437988878));
#33317=CARTESIAN_POINT('Ctrl Pts',(-4.7640345870679,1.22194824592564,46.5701705954582));
#33318=CARTESIAN_POINT('Ctrl Pts',(-4.76723354040696,1.2094764211978,46.5709009832683));
#33319=CARTESIAN_POINT('Ctrl Pts',(-4.77038354248472,1.19699194120722,46.5716307886145));
#33320=CARTESIAN_POINT('Ctrl Pts',(-4.78152228235782,1.15210310833962,46.5742500147955));
#33321=CARTESIAN_POINT('Ctrl Pts',(-4.78923018167354,1.11962994056537,46.576135852302));
#33322=CARTESIAN_POINT('Ctrl Pts',(-4.80697392655666,1.0413378914593,46.5806642795432));
#33323=CARTESIAN_POINT('Ctrl Pts',(-4.81668604876316,0.995448892470532,
46.5833035425673));
#33324=CARTESIAN_POINT('Ctrl Pts',(-4.8745292050673,0.701444363990078,46.6001397299728));
#33325=CARTESIAN_POINT('Ctrl Pts',(-4.90413055987128,0.450069787444037,
46.614223605967));
#33326=CARTESIAN_POINT('Ctrl Pts',(-4.91692699994307,0.131721368016909,
46.6321721991386));
#33327=CARTESIAN_POINT('Ctrl Pts',(-4.91825008432671,0.0658606293943527,
46.6358900870717));
#33328=CARTESIAN_POINT('Ctrl Pts',(-4.91824999999597,-6.29693351562663E-6,
46.6396169269188));
#33329=CARTESIAN_POINT('Ctrl Pts',(-4.91782865331878,7.42403732347657E-6,
46.6398594359907));
#33330=CARTESIAN_POINT('Ctrl Pts',(-4.91780676097348,-0.417173566090727,
46.6634791213957));
#33331=CARTESIAN_POINT('Ctrl Pts',(-4.76226060784274,-1.65284746667128,
46.7334388053049));
#33332=CARTESIAN_POINT('Ctrl Pts',(-3.7390810765516,-3.50817654536093,46.8497384877184));
#33333=CARTESIAN_POINT('Ctrl Pts',(-1.60365005368828,-4.86994214271806,
46.9887584832308));
#33334=CARTESIAN_POINT('Ctrl Pts',(0.923083286691152,-5.04340631076602,
47.1277784787434));
#33335=CARTESIAN_POINT('Ctrl Pts',(3.22457756921184,-3.98624252566559,47.2667984742559));
#33336=CARTESIAN_POINT('Ctrl Pts',(4.73925138433377,-1.95640646877516,47.4058184697685));
#33337=CARTESIAN_POINT('Ctrl Pts',(5.09751327602456,0.550807048437444,47.5448384652809));
#33338=CARTESIAN_POINT('Ctrl Pts',(4.21194470665123,2.92361962201063,47.6838584607935));
#33339=CARTESIAN_POINT('Ctrl Pts',(2.29863091214187,4.58304767427664,47.8228784563059));
#33340=CARTESIAN_POINT('Ctrl Pts',(-0.175565656096785,5.12417862858086,
47.9618984518186));
#33341=CARTESIAN_POINT('Ctrl Pts',(-2.60692281934329,4.41497262009648,48.1009184473309));
#33342=CARTESIAN_POINT('Ctrl Pts',(-4.14805938556448,2.881354010624,48.2202605432668));
#33343=CARTESIAN_POINT('Ctrl Pts',(-4.64647847283068,1.67794619770932,48.2932626406984));
#33344=CARTESIAN_POINT('Ctrl Pts',(-4.76366299354682,1.22185269443844,48.3199247396258));
#33345=CARTESIAN_POINT('Origin',(0.,0.,-3.23514056400928));
#33346=CARTESIAN_POINT('',(-4.91825415174279,6.46578250284212E-5,48.3898594374466));
#33347=CARTESIAN_POINT('Ctrl Pts',(-4.76366299354682,1.22185269443844,48.3199247396258));
#33348=CARTESIAN_POINT('Ctrl Pts',(-4.85015075420195,0.885233954128829,
48.3396026392026));
#33349=CARTESIAN_POINT('Ctrl Pts',(-4.9107614377059,0.475756808800476,48.3629142046575));
#33350=CARTESIAN_POINT('Ctrl Pts',(-4.91864568349125,0.0642149472873671,
48.3862257701125));
#33351=CARTESIAN_POINT('Ctrl Pts',(-4.91860392675717,6.46881271033038E-5,
48.3898594359907));
#33352=CARTESIAN_POINT('',(-4.31106608169009,2.36725416924362,50.));
#33353=CARTESIAN_POINT('Ctrl Pts',(-4.91824999957499,6.4657465313589E-5,
48.3898594374639));
#33354=CARTESIAN_POINT('Ctrl Pts',(-4.91825188690336,-0.143497307078023,
48.3979918092232));
#33355=CARTESIAN_POINT('Ctrl Pts',(-4.9119636472632,-0.287087752773969,
48.4061241809826));
#33356=CARTESIAN_POINT('Ctrl Pts',(-4.89940385679968,-0.430145220217989,
48.4142565527419));
#33357=CARTESIAN_POINT('Ctrl Pts',(-4.88684656678358,-0.573174207276529,
48.4223873054799));
#33358=CARTESIAN_POINT('Ctrl Pts',(-4.86802024625112,-0.715670090689004,
48.430518058218));
#33359=CARTESIAN_POINT('Ctrl Pts',(-4.84299541970709,-0.857075508456625,
48.438648810956));
#33360=CARTESIAN_POINT('Ctrl Pts',(-4.81796978997819,-0.99848546470493,
48.4467798246548));
#33361=CARTESIAN_POINT('Ctrl Pts',(-4.78674531227144,-1.13880455141727,
48.4549108383536));
#33362=CARTESIAN_POINT('Ctrl Pts',(-4.74944389329373,-1.27748415526571,
48.4630418520524));
#33363=CARTESIAN_POINT('Ctrl Pts',(-4.71214345251239,-1.41616012236545,
48.4711726525226));
#33364=CARTESIAN_POINT('Ctrl Pts',(-4.66876647949925,-1.55319636631919,
48.4793034529928));
#33365=CARTESIAN_POINT('Ctrl Pts',(-4.61948514488079,-1.68805807326814,
48.487434253463));
#33366=CARTESIAN_POINT('Ctrl Pts',(-4.57019270843371,-1.82295016112231,
48.4955668855954));
#33367=CARTESIAN_POINT('Ctrl Pts',(-4.51499337112636,-1.95566641597054,
48.5036995177277));
#33368=CARTESIAN_POINT('Ctrl Pts',(-4.45410813183877,-2.08569024842802,
48.51183214986));
#33369=CARTESIAN_POINT('Ctrl Pts',(-4.4387700073343,-2.11844567082787,48.5138809111962));
#33370=CARTESIAN_POINT('Ctrl Pts',(-4.42307127439285,-2.15103032930286,
48.5159296725323));
#33371=CARTESIAN_POINT('Ctrl Pts',(-4.40701593818226,-2.18343618709307,
48.5179784338685));
#33372=CARTESIAN_POINT('Ctrl Pts',(-4.34309859665993,-2.31244602236111,
48.5261346864877));
#33373=CARTESIAN_POINT('Ctrl Pts',(-4.27350049521726,-2.43867143502133,
48.534290939107));
#33374=CARTESIAN_POINT('Ctrl Pts',(-4.19848925582428,-2.56161492641421,
48.5424471917262));
#33375=CARTESIAN_POINT('Ctrl Pts',(-4.12349330707571,-2.68453335642663,
48.5506017817365));
#33376=CARTESIAN_POINT('Ctrl Pts',(-4.04308659586943,-2.80417091427926,
48.5587563717468));
#33377=CARTESIAN_POINT('Ctrl Pts',(-3.9575814689975,-2.92005684512264,48.5669109617571));
#33378=CARTESIAN_POINT('Ctrl Pts',(-3.87207330801335,-3.03594688812785,
48.5750658411294));
#33379=CARTESIAN_POINT('Ctrl Pts',(-3.78146656500964,-3.14808476622646,
48.5832207205018));
#33380=CARTESIAN_POINT('Ctrl Pts',(-3.68611578484381,-3.25603032590688,
48.5913755998741));
#33381=CARTESIAN_POINT('Ctrl Pts',(-3.59077060912433,-3.36396954085581,
48.599529999926));
#33382=CARTESIAN_POINT('Ctrl Pts',(-3.49068217637334,-3.46771668016612,
48.6076843999778));
#33383=CARTESIAN_POINT('Ctrl Pts',(-3.38624399038185,-3.56686622963391,
48.6158388000297));
#33384=CARTESIAN_POINT('Ctrl Pts',(-3.28178005384405,-3.66604022566825,
48.6239952106513));
#33385=CARTESIAN_POINT('Ctrl Pts',(-3.17296446365347,-3.76061413599753,
48.6321516212729));
#33386=CARTESIAN_POINT('Ctrl Pts',(-3.0602265519251,-3.8502203201106,48.6403080318945));
#33387=CARTESIAN_POINT('Ctrl Pts',(-2.98332832443053,-3.91134045818315,
48.6458714977234));
#33388=CARTESIAN_POINT('Ctrl Pts',(-2.90460594879125,-3.97015012395728,
48.6514349635522));
#33389=CARTESIAN_POINT('Ctrl Pts',(-2.82420423355466,-4.02654361825027,
48.6569984293811));
#33390=CARTESIAN_POINT('Ctrl Pts',(-2.70632998692356,-4.10922022079686,
48.6651548392451));
#33391=CARTESIAN_POINT('Ctrl Pts',(-2.58480074625422,-4.18673270427483,
48.673311249109));
#33392=CARTESIAN_POINT('Ctrl Pts',(-2.4600896394939,-4.25877236162662,48.681467658973));
#33393=CARTESIAN_POINT('Ctrl Pts',(-2.3354039429029,-4.33079734073573,48.6896224069501));
#33394=CARTESIAN_POINT('Ctrl Pts',(-2.20753796315363,-4.39735155099705,
48.6977771549271));
#33395=CARTESIAN_POINT('Ctrl Pts',(-2.07699129460226,-4.45817117489295,
48.7059319029042));
#33396=CARTESIAN_POINT('Ctrl Pts',(-1.94644000136145,-4.51899295335837,
48.7140869397678));
#33397=CARTESIAN_POINT('Ctrl Pts',(-1.81320813102232,-4.57407959423216,
48.7222419766314));
#33398=CARTESIAN_POINT('Ctrl Pts',(-1.67781767950347,-4.62321434684199,
48.730397013495));
#33399=CARTESIAN_POINT('Ctrl Pts',(-1.54243519621796,-4.67234620768826,
48.7385515704042));
#33400=CARTESIAN_POINT('Ctrl Pts',(-1.40489470080638,-4.71552676779961,
48.7467061273135));
#33401=CARTESIAN_POINT('Ctrl Pts',(-1.26573581428016,-4.75258833804786,
48.7548606842228));
#33402=CARTESIAN_POINT('Ctrl Pts',(-1.12654265863381,-4.78965903503918,
48.7630172492646));
#33403=CARTESIAN_POINT('Ctrl Pts',(-0.985730638942556,-4.82060764474622,
48.7711738143064));
#33404=CARTESIAN_POINT('Ctrl Pts',(-0.843852704477646,-4.84531688082893,
48.7793303793482));
#33405=CARTESIAN_POINT('Ctrl Pts',(-0.747093614504557,-4.86216829050239,
48.7848930611967));
#33406=CARTESIAN_POINT('Ctrl Pts',(-0.649839026362427,-4.87611876961641,
48.7904557430452));
#33407=CARTESIAN_POINT('Ctrl Pts',(-0.552266597345409,-4.88714483803749,
48.7960184248937));
#33408=CARTESIAN_POINT('Ctrl Pts',(-0.409205056356983,-4.90331135510851,
48.8041744772262));
#33409=CARTESIAN_POINT('Ctrl Pts',(-0.265406350851102,-4.91319481873329,
48.8123305295588));
#33410=CARTESIAN_POINT('Ctrl Pts',(-0.121433605261592,-4.91675064875301,
48.8204865818913));
#33411=CARTESIAN_POINT('Ctrl Pts',(0.0225097812274147,-4.92030575366348,
48.8286409710316));
#33412=CARTESIAN_POINT('Ctrl Pts',(0.166626802610623,-4.91753579085466,
48.8367953601718));
#33413=CARTESIAN_POINT('Ctrl Pts',(0.310352583167036,-4.90844826158141,
48.8449497493121));
#33414=CARTESIAN_POINT('Ctrl Pts',(0.454083483381406,-4.89936040860115,
48.8531044289199));
#33415=CARTESIAN_POINT('Ctrl Pts',(0.597422780632983,-4.88395455621873,
48.8612591085278));
#33416=CARTESIAN_POINT('Ctrl Pts',(0.739808459343981,-4.86229025316086,
48.8694137881357));
#33417=CARTESIAN_POINT('Ctrl Pts',(0.882185787764231,-4.84062722061861,
48.8775679895076));
#33418=CARTESIAN_POINT('Ctrl Pts',(1.02360927877759,-4.81270652298323,48.8857221908795));
#33419=CARTESIAN_POINT('Ctrl Pts',(1.16352492632272,-4.77863922140244,48.8938763922515));
#33420=CARTESIAN_POINT('Ctrl Pts',(1.30347513317182,-4.7445635051643,48.9020326077193));
#33421=CARTESIAN_POINT('Ctrl Pts',(1.44191642694179,-4.70433823023442,48.910188823187));
#33422=CARTESIAN_POINT('Ctrl Pts',(1.57830722573228,-4.65812509103193,48.9183450386548));
#33423=CARTESIAN_POINT('Ctrl Pts',(1.67135788468709,-4.62659684210829,48.9239094992386));
#33424=CARTESIAN_POINT('Ctrl Pts',(1.76345441903967,-4.59228262112032,48.9294739598223));
#33425=CARTESIAN_POINT('Ctrl Pts',(1.85442944131458,-4.555246920825,48.9350384204061));
#33426=CARTESIAN_POINT('Ctrl Pts',(1.98778541037635,-4.50095804483178,48.9431950991833));
#33427=CARTESIAN_POINT('Ctrl Pts',(2.11878067919415,-4.44079895903165,48.9513517779606));
#33428=CARTESIAN_POINT('Ctrl Pts',(2.24689941917647,-4.3750001214405,48.9595084567379));
#33429=CARTESIAN_POINT('Ctrl Pts',(2.37499206212136,-4.30921468668744,48.9676634740474));
#33430=CARTESIAN_POINT('Ctrl Pts',(2.50020904767986,-4.23779194466744,48.9758184913569));
#33431=CARTESIAN_POINT('Ctrl Pts',(2.6220579407557,-4.16100891825768,48.9839735086665));
#33432=CARTESIAN_POINT('Ctrl Pts',(2.74391111994757,-4.0842231909538,48.9921288128342));
#33433=CARTESIAN_POINT('Ctrl Pts',(2.86239568451947,-4.00207697715491,49.0002841170019));
#33434=CARTESIAN_POINT('Ctrl Pts',(2.97704662494939,-3.91489162753932,49.0084394211696));
#33435=CARTESIAN_POINT('Ctrl Pts',(3.09169079322723,-3.82771142775019,49.0165942436234));
#33436=CARTESIAN_POINT('Ctrl Pts',(3.20250152461738,-3.73549289091029,49.0247490660771));
#33437=CARTESIAN_POINT('Ctrl Pts',(3.30904549887002,-3.63859876173618,49.0329038885308));
#33438=CARTESIAN_POINT('Ctrl Pts',(3.41561564176688,-3.5416808340506,49.0410607139195));
#33439=CARTESIAN_POINT('Ctrl Pts',(3.51791668563332,-3.44008524433254,49.0492175393082));
#33440=CARTESIAN_POINT('Ctrl Pts',(3.61555045472144,-3.33421324630918,49.0573743646968));
#33441=CARTESIAN_POINT('Ctrl Pts',(3.68211747995647,-3.26202936946075,49.0629357151041));
#33442=CARTESIAN_POINT('Ctrl Pts',(3.7465156353158,-3.18785837437165,49.0684970655114));
#33443=CARTESIAN_POINT('Ctrl Pts',(3.80862902171563,-3.11183676266051,49.0740584159187));
#33444=CARTESIAN_POINT('Ctrl Pts',(3.89972024128471,-3.00034869662916,49.0822143098478));
#33445=CARTESIAN_POINT('Ctrl Pts',(3.98592987250361,-2.88483728265233,49.0903702037769));
#33446=CARTESIAN_POINT('Ctrl Pts',(4.06691538033361,-2.76575167932805,49.098526097706));
#33447=CARTESIAN_POINT('Ctrl Pts',(4.14788438100405,-2.64669034905097,49.1066803292309));
#33448=CARTESIAN_POINT('Ctrl Pts',(4.22363119443135,-2.52405655939287,49.1148345607558));
#33449=CARTESIAN_POINT('Ctrl Pts',(4.29385611314292,-2.39832915633471,49.1229887922808));
#33450=CARTESIAN_POINT('Ctrl Pts',(4.36408355692555,-2.27259723250767,49.1311433170067));
#33451=CARTESIAN_POINT('Ctrl Pts',(4.42878854219891,-2.14377176307623,49.1392978417326));
#33452=CARTESIAN_POINT('Ctrl Pts',(4.48771665879655,-2.01235738696186,49.1474523664585));
#33453=CARTESIAN_POINT('Ctrl Pts',(4.54664133311361,-1.88095068740634,49.1556064148386));
#33454=CARTESIAN_POINT('Ctrl Pts',(4.59978967780052,-1.74695568954819,49.1637604632187));
#33455=CARTESIAN_POINT('Ctrl Pts',(4.64695492019639,-1.61089820664204,49.1719145115987));
#33456=CARTESIAN_POINT('Ctrl Pts',(4.69413183789641,-1.47480704400874,49.1800705784354));
#33457=CARTESIAN_POINT('Ctrl Pts',(4.73532258392123,-1.33665269246272,49.1882266452721));
#33458=CARTESIAN_POINT('Ctrl Pts',(4.7703696757342,-1.19697795273578,49.1963827121088));
#33459=CARTESIAN_POINT('Ctrl Pts',(4.79428380488269,-1.10167190616176,49.2019479452162));
#33460=CARTESIAN_POINT('Ctrl Pts',(4.81533852993245,-1.00565832347219,49.2075131783236));
#33461=CARTESIAN_POINT('Ctrl Pts',(4.83349736403111,-0.909112916201438,
49.2130784114311));
#33462=CARTESIAN_POINT('Ctrl Pts',(4.86011027114623,-0.767619583417664,
49.2212346086272));
#33463=CARTESIAN_POINT('Ctrl Pts',(4.88051089537211,-0.624930332658238,
49.2293908058235));
#33464=CARTESIAN_POINT('Ctrl Pts',(4.89461347930164,-0.481603520272367,
49.2375470030197));
#33465=CARTESIAN_POINT('Ctrl Pts',(4.90871318301751,-0.338305979957791,
49.2457015344509));
#33466=CARTESIAN_POINT('Ctrl Pts',(4.91651737970788,-0.194371470640131,
49.2538560658821));
#33467=CARTESIAN_POINT('Ctrl Pts',(4.91799212469945,-0.050363914603593,
49.2620105973133));
#33468=CARTESIAN_POINT('Ctrl Pts',(4.91946692127142,0.0936486782139966,
49.2701654139559));
#33469=CARTESIAN_POINT('Ctrl Pts',(4.91461181596314,0.237733988262807,49.2783202305984));
#33470=CARTESIAN_POINT('Ctrl Pts',(4.9034449811488,0.381327129046287,49.286475047241));
#33471=CARTESIAN_POINT('Ctrl Pts',(4.89227880567297,0.524911791465909,49.2946293823877));
#33472=CARTESIAN_POINT('Ctrl Pts',(4.87480167315109,0.668004009156202,49.3027837175344));
#33473=CARTESIAN_POINT('Ctrl Pts',(4.85108371705545,0.810043105408263,49.3109380526811));
#33474=CARTESIAN_POINT('Ctrl Pts',(4.82735992108153,0.952117174784864,49.319094395603));
#33475=CARTESIAN_POINT('Ctrl Pts',(4.79739228592106,1.09313727429167,49.3272507385249));
#33476=CARTESIAN_POINT('Ctrl Pts',(4.7613023531058,1.23255140453011,49.3354070814469));
#33477=CARTESIAN_POINT('Ctrl Pts',(4.73668393357037,1.32765148590034,49.3409708566125));
#33478=CARTESIAN_POINT('Ctrl Pts',(4.70921777841567,1.42200447474435,49.3465346317781));
#33479=CARTESIAN_POINT('Ctrl Pts',(4.67895590890541,1.51543876980205,49.3520984069438));
#33480=CARTESIAN_POINT('Ctrl Pts',(4.63458299103438,1.6524412870962,49.360256559182));
#33481=CARTESIAN_POINT('Ctrl Pts',(4.5841804662064,1.78751890601388,49.3684147114202));
#33482=CARTESIAN_POINT('Ctrl Pts',(4.5279404776491,1.92014012336779,49.3765728636584));
#33483=CARTESIAN_POINT('Ctrl Pts',(4.47171186823887,2.05273450721095,49.3847293652417));
#33484=CARTESIAN_POINT('Ctrl Pts',(4.40964828181284,2.18287317337993,49.3928858668249));
#33485=CARTESIAN_POINT('Ctrl Pts',(4.34199001409317,2.31004454069942,49.4010423684082));
#33486=CARTESIAN_POINT('Ctrl Pts',(4.27432935420594,2.43722040436842,49.4091991583778));
#33487=CARTESIAN_POINT('Ctrl Pts',(4.20107377094131,2.56142846234591,49.4173559483474));
#33488=CARTESIAN_POINT('Ctrl Pts',(4.12250977738952,2.68218123881064,49.425512738317));
#33489=CARTESIAN_POINT('Ctrl Pts',(4.0439504489463,2.80292684500836,49.4336690439386));
#33490=CARTESIAN_POINT('Ctrl Pts',(3.96008352394967,2.9202173004152,49.4418253495602));
#33491=CARTESIAN_POINT('Ctrl Pts',(3.87123912075788,3.03359369929688,49.4499816551819));
#33492=CARTESIAN_POINT('Ctrl Pts',(3.78237309431381,3.14699769211119,49.4581399459128));
#33493=CARTESIAN_POINT('Ctrl Pts',(3.68852737507418,3.25648546142182,49.4662982366438));
#33494=CARTESIAN_POINT('Ctrl Pts',(3.59007306298733,3.36163032841399,49.4744565273747));
#33495=CARTESIAN_POINT('Ctrl Pts',(3.52304785295607,3.43321029931098,49.4800104857352));
#33496=CARTESIAN_POINT('Ctrl Pts',(3.45388761708271,3.50277821283592,49.4855644440957));
#33497=CARTESIAN_POINT('Ctrl Pts',(3.38271944840214,3.57020898490578,49.4911184024561));
#33498=CARTESIAN_POINT('Ctrl Pts',(3.27828225345075,3.66916166022317,49.4992686730448));
#33499=CARTESIAN_POINT('Ctrl Pts',(3.16947995222353,3.76354777596328,49.5074189436334));
#33500=CARTESIAN_POINT('Ctrl Pts',(3.05673468831527,3.85299313621892,49.515569214222));
#33501=CARTESIAN_POINT('Ctrl Pts',(2.94401279067063,3.94241995907624,49.523717795681));
#33502=CARTESIAN_POINT('Ctrl Pts',(2.82734982328878,4.02690786064281,49.5318663771399));
#33503=CARTESIAN_POINT('Ctrl Pts',(2.70720069172927,4.10612316878105,49.5400149585989));
#33504=CARTESIAN_POINT('Ctrl Pts',(2.58704701179802,4.1853414756981,49.548163848531));
#33505=CARTESIAN_POINT('Ctrl Pts',(2.46340718173827,4.25928660186803,49.556312738463));
#33506=CARTESIAN_POINT('Ctrl Pts',(2.33676516282422,4.32766815228607,49.5644616283951));
#33507=CARTESIAN_POINT('Ctrl Pts',(2.21013021263356,4.39604588588035,49.5726100634841));
#33508=CARTESIAN_POINT('Ctrl Pts',(2.08049370471521,4.45886050647418,49.580758498573));
#33509=CARTESIAN_POINT('Ctrl Pts',(1.94836421109051,4.51586757594171,49.588906933662));
#33510=CARTESIAN_POINT('Ctrl Pts',(1.81620060637184,4.57288936258896,49.5970574723845));
#33511=CARTESIAN_POINT('Ctrl Pts',(1.68154303816524,4.62410046898825,49.605208011107));
#33512=CARTESIAN_POINT('Ctrl Pts',(1.5449206338762,4.66930436976682,49.6133585498296));
#33513=CARTESIAN_POINT('Ctrl Pts',(1.45116391936385,4.70032541087788,49.6189518325426));
#33514=CARTESIAN_POINT('Ctrl Pts',(1.35648231503136,4.72851845203959,49.6245451152557));
#33515=CARTESIAN_POINT('Ctrl Pts',(1.26105114876189,4.75383351230418,49.6301383979688));
#33516=CARTESIAN_POINT('Ctrl Pts',(1.12165256809271,4.79081182461438,49.6383086394314));
#33517=CARTESIAN_POINT('Ctrl Pts',(0.98060213796819,4.82166090769783,49.6464788808941));
#33518=CARTESIAN_POINT('Ctrl Pts',(0.838452342310928,4.8462542991648,49.6546491223567));
#33519=CARTESIAN_POINT('Ctrl Pts',(0.696330650913473,4.87084282830284,49.6628177484911));
#33520=CARTESIAN_POINT('Ctrl Pts',(0.55311035489733,4.88917807673463,49.6709863746254));
#33521=CARTESIAN_POINT('Ctrl Pts',(0.409353248986643,4.90118485471055,49.6791550007598));
#33522=CARTESIAN_POINT('Ctrl Pts',(0.265592281209922,4.91319195523448,49.6873238463347));
#33523=CARTESIAN_POINT('Ctrl Pts',(0.121294805525717,4.9188702137094,49.6954926919096));
#33524=CARTESIAN_POINT('Ctrl Pts',(-0.0229726286740002,4.9181963483407,
49.7036615374845));
#33525=CARTESIAN_POINT('Ctrl Pts',(-0.167230310106315,4.91752252852665,
49.7118298308291));
#33526=CARTESIAN_POINT('Ctrl Pts',(-0.311457621791795,4.91049744605797,
49.7199981241736));
#33527=CARTESIAN_POINT('Ctrl Pts',(-0.455088397425796,4.89714994798285,
49.7281664175182));
#33528=CARTESIAN_POINT('Ctrl Pts',(-0.598750248365985,4.8837995621033,49.7363364781179));
#33529=CARTESIAN_POINT('Ctrl Pts',(-0.741814974285452,4.86412405760869,
49.7445065387176));
#33530=CARTESIAN_POINT('Ctrl Pts',(-0.883721287240841,4.83820418636682,
49.7526765993172));
#33531=CARTESIAN_POINT('Ctrl Pts',(-0.979145738184204,4.8207744509994,49.7581705307052));
#33532=CARTESIAN_POINT('Ctrl Pts',(-1.07404648628848,4.80052218270611,49.7636644620932));
#33533=CARTESIAN_POINT('Ctrl Pts',(-1.16825532506712,4.77748496156213,49.7691583934811));
#33534=CARTESIAN_POINT('Ctrl Pts',(-1.30767583788311,4.74339196957339,49.7772889122458));
#33535=CARTESIAN_POINT('Ctrl Pts',(-1.44563187930691,4.70318465095805,49.7854194310104));
#33536=CARTESIAN_POINT('Ctrl Pts',(-1.5815826097383,4.6570140123338,49.7935499497751));
#33537=CARTESIAN_POINT('Ctrl Pts',(-1.71750497273023,4.61085300766144,49.8016787720281));
#33538=CARTESIAN_POINT('Ctrl Pts',(-1.85142253869643,4.55873127390083,49.8098075942811));
#33539=CARTESIAN_POINT('Ctrl Pts',(-1.98281074732252,4.50084932016195,49.8179364165341));
#33540=CARTESIAN_POINT('Ctrl Pts',(-2.11420682945525,4.44296389781694,49.826065725911));
#33541=CARTESIAN_POINT('Ctrl Pts',(-2.24307293941015,4.37931769817334,49.8341950352879));
#33542=CARTESIAN_POINT('Ctrl Pts',(-2.36890512983529,4.31015910939956,49.8423243446648));
#33543=CARTESIAN_POINT('Ctrl Pts',(-2.49473248588189,4.24100317764699,49.8504533417197));
#33544=CARTESIAN_POINT('Ctrl Pts',(-2.61752585952728,4.1663354454027,49.8585823387746));
#33545=CARTESIAN_POINT('Ctrl Pts',(-2.73680662682732,4.08644987120288,49.8667113358296));
#33546=CARTESIAN_POINT('Ctrl Pts',(-2.85612413052588,4.00653969363778,49.874842836474));
#33547=CARTESIAN_POINT('Ctrl Pts',(-2.97192658454216,3.92140865181147,49.8829743371184));
#33548=CARTESIAN_POINT('Ctrl Pts',(-3.08376452537185,3.83139392578708,49.8911058377628));
#33549=CARTESIAN_POINT('Ctrl Pts',(-3.16203457899332,3.76839690187567,49.8967966881731));
#33550=CARTESIAN_POINT('Ctrl Pts',(-3.23836345535582,3.70300878338029,49.9024875385834));
#33551=CARTESIAN_POINT('Ctrl Pts',(-3.31260678046568,3.63535684362798,49.9081783889938));
#33552=CARTESIAN_POINT('Ctrl Pts',(-3.41989988008897,3.53758931636796,49.9164025489315));
#33553=CARTESIAN_POINT('Ctrl Pts',(-3.52287846090169,3.43505347941445,49.9246267088693));
#33554=CARTESIAN_POINT('Ctrl Pts',(-3.62113200122419,3.32815055131377,49.9328508688071));
#33555=CARTESIAN_POINT('Ctrl Pts',(-3.71936169908124,3.22127356456196,49.9410730330484));
#33556=CARTESIAN_POINT('Ctrl Pts',(-3.81286842630019,3.11003183946856,49.9492951972896));
#33557=CARTESIAN_POINT('Ctrl Pts',(-3.90127974942257,2.99486216364716,49.9575173615309));
#33558=CARTESIAN_POINT('Ctrl Pts',(-3.98968144240252,2.87970503260333,49.9657386301785));
#33559=CARTESIAN_POINT('Ctrl Pts',(-4.07298864057679,2.76062105963968,49.9739598988262));
#33560=CARTESIAN_POINT('Ctrl Pts',(-4.15086999848057,2.63807909627705,49.9821811674739));
#33561=CARTESIAN_POINT('Ctrl Pts',(-4.20713685675021,2.54954633991283,49.988120778316));
#33562=CARTESIAN_POINT('Ctrl Pts',(-4.26057248301015,2.45920933123667,49.994060389158));
#33563=CARTESIAN_POINT('Ctrl Pts',(-4.31106608169009,2.36725416924362,50.));
#33564=CARTESIAN_POINT('',(0.837162017642341,4.84647736182859,50.));
#33565=CARTESIAN_POINT('Origin',(0.,0.,50.));
#33566=CARTESIAN_POINT('',(-4.91824999932842,-8.12775897282569E-5,48.7351405640092));
#33567=CARTESIAN_POINT('Ctrl Pts',(-4.91824999932841,-8.12775897283124E-5,
48.7351405640092));
#33568=CARTESIAN_POINT('Ctrl Pts',(-4.91824860461297,-0.0844779637138754,
48.7399212201507));
#33569=CARTESIAN_POINT('Ctrl Pts',(-4.91607448844467,-0.168867401146295,
48.7447018762922));
#33570=CARTESIAN_POINT('Ctrl Pts',(-4.91173094479186,-0.253144599930679,
48.7494825324338));
#33571=CARTESIAN_POINT('Ctrl Pts',(-4.90432050159678,-0.396928441915993,
48.7576387255341));
#33572=CARTESIAN_POINT('Ctrl Pts',(-4.89059073704431,-0.540413569487469,
48.7657949186345));
#33573=CARTESIAN_POINT('Ctrl Pts',(-4.87058963142793,-0.683037118117827,
48.7739511117348));
#33574=CARTESIAN_POINT('Ctrl Pts',(-4.85059259870388,-0.825631623835872,
48.7821056439622));
#33575=CARTESIAN_POINT('Ctrl Pts',(-4.82432681901249,-0.967364569392464,
48.7902601761895));
#33576=CARTESIAN_POINT('Ctrl Pts',(-4.7918919408917,-1.1076798677042,48.7984147084169));
#33577=CARTESIAN_POINT('Ctrl Pts',(-4.75945590785336,-1.248000162261,48.8065695310049));
#33578=CARTESIAN_POINT('Ctrl Pts',(-4.72085040855073,-1.38690238166367,
48.8147243535928));
#33579=CARTESIAN_POINT('Ctrl Pts',(-4.67622597313651,-1.52384176037524,
48.8228791761808));
#33580=CARTESIAN_POINT('Ctrl Pts',(-4.63160414837477,-1.66077312775566,
48.8310335216892));
#33581=CARTESIAN_POINT('Ctrl Pts',(-4.58096419657989,-1.7957415662676,48.8391878671976));
#33582=CARTESIAN_POINT('Ctrl Pts',(-4.5245061608825,-1.92821862418044,48.847342212706));
#33583=CARTESIAN_POINT('Ctrl Pts',(-4.46803421536716,-2.06072832105663,
48.8554985672369));
#33584=CARTESIAN_POINT('Ctrl Pts',(-4.40574145271102,-2.19074510270008,
48.8636549217677));
#33585=CARTESIAN_POINT('Ctrl Pts',(-4.3378758403449,-2.31776104382053,48.8718112762986));
#33586=CARTESIAN_POINT('Ctrl Pts',(-4.29178636058946,-2.40402120478847,
48.8773504901054));
#33587=CARTESIAN_POINT('Ctrl Pts',(-4.24312758724043,-2.48889776854284,
48.8828897039122));
#33588=CARTESIAN_POINT('Ctrl Pts',(-4.1919892239971,-2.57223820988496,48.888428917719));
#33589=CARTESIAN_POINT('Ctrl Pts',(-4.11668498514456,-2.69496189720833,
48.8965857348933));
#33590=CARTESIAN_POINT('Ctrl Pts',(-4.03597375155277,-2.81439932341442,
48.9047425520675));
#33591=CARTESIAN_POINT('Ctrl Pts',(-3.95016701024448,-2.93007912071947,
48.9128993692417));
#33592=CARTESIAN_POINT('Ctrl Pts',(-3.86437772267667,-3.0457353878784,48.9210545272576));
#33593=CARTESIAN_POINT('Ctrl Pts',(-3.77349519428314,-3.15763528238476,
48.9292096852735));
#33594=CARTESIAN_POINT('Ctrl Pts',(-3.67787303964822,-3.26533810909816,
48.9373648432894));
#33595=CARTESIAN_POINT('Ctrl Pts',(-3.58224752263747,-3.37304472298183,
48.9455202880663));
#33596=CARTESIAN_POINT('Ctrl Pts',(-3.48188226520706,-3.47655372109064,
48.9536757328432));
#33597=CARTESIAN_POINT('Ctrl Pts',(-3.37717014484713,-3.57545869438499,
48.9618311776201));
#33598=CARTESIAN_POINT('Ctrl Pts',(-3.27246419451462,-3.67435783983061,
48.9699861418478));
#33599=CARTESIAN_POINT('Ctrl Pts',(-3.16341213755547,-3.76865327414801,
48.9781411060756));
#33600=CARTESIAN_POINT('Ctrl Pts',(-3.05044252510817,-3.85797660225042,
48.9862960703034));
#33601=CARTESIAN_POINT('Ctrl Pts',(-2.9374452359176,-3.94732181392635,48.9944530324388));
#33602=CARTESIAN_POINT('Ctrl Pts',(-2.82052873581696,-4.03169227751469,
49.0026099945742));
#33603=CARTESIAN_POINT('Ctrl Pts',(-2.70015383907519,-4.11076055102064,
49.0107669567096));
#33604=CARTESIAN_POINT('Ctrl Pts',(-2.61845561461897,-4.16442404508047,
49.0163030721411));
#33605=CARTESIAN_POINT('Ctrl Pts',(-2.53516500631167,-4.21564604350739,
49.0218391875726));
#33606=CARTESIAN_POINT('Ctrl Pts',(-2.45043348771288,-4.26433567918794,
49.0273753030041));
#33607=CARTESIAN_POINT('Ctrl Pts',(-2.32560348256834,-4.33606728004911,
49.035531339025));
#33608=CARTESIAN_POINT('Ctrl Pts',(-2.19759824966692,-4.40232731187191,
49.0436873750459));
#33609=CARTESIAN_POINT('Ctrl Pts',(-2.06691673278157,-4.46285091418564,
49.0518434110668));
#33610=CARTESIAN_POINT('Ctrl Pts',(-1.93626181488615,-4.52336219749108,
49.0599977870035));
#33611=CARTESIAN_POINT('Ctrl Pts',(-1.8029320032343,-4.57813923999919,49.0681521629402));
#33612=CARTESIAN_POINT('Ctrl Pts',(-1.66744856132577,-4.62696427021353,
49.0763065388769));
#33613=CARTESIAN_POINT('Ctrl Pts',(-1.53196024992732,-4.67579105527694,
49.0844612078949));
#33614=CARTESIAN_POINT('Ctrl Pts',(-1.3943184669733,-4.71866528299151,49.0926158769128));
#33615=CARTESIAN_POINT('Ctrl Pts',(-1.2550625510186,-4.75541807368508,49.1007705459307));
#33616=CARTESIAN_POINT('Ctrl Pts',(-1.11581474995482,-4.7921687226751,49.1089247397498));
#33617=CARTESIAN_POINT('Ctrl Pts',(-0.974953327942705,-4.82279856382775,
49.1170789335689));
#33618=CARTESIAN_POINT('Ctrl Pts',(-0.833030761240178,-4.84718916624136,
49.125233127388));
#33619=CARTESIAN_POINT('Ctrl Pts',(-0.691073152419967,-4.87158579094149,
49.13338933456));
#33620=CARTESIAN_POINT('Ctrl Pts',(-0.548054205331753,-4.88974004165502,
49.1415455417321));
#33621=CARTESIAN_POINT('Ctrl Pts',(-0.40453513299909,-4.90158488538854,
49.1497017489041));
#33622=CARTESIAN_POINT('Ctrl Pts',(-0.307051983766232,-4.9096303155223,
49.1552417286991));
#33623=CARTESIAN_POINT('Ctrl Pts',(-0.209338267113324,-4.91476590902321,
49.1607817084942));
#33624=CARTESIAN_POINT('Ctrl Pts',(-0.111570856204851,-4.91698434068543,
49.1663216882892));
#33625=CARTESIAN_POINT('Ctrl Pts',(0.032368985038175,-4.92025046687513,
49.1744780238695));
#33626=CARTESIAN_POINT('Ctrl Pts',(0.17647929533059,-4.91719231805076,49.1826343594499));
#33627=CARTESIAN_POINT('Ctrl Pts',(0.320195185024482,-4.90781602201907,
49.1907906950302));
#33628=CARTESIAN_POINT('Ctrl Pts',(0.463881764555866,-4.89844163823774,
49.1989453671652));
#33629=CARTESIAN_POINT('Ctrl Pts',(0.607173750227318,-4.88275169961299,
49.2071000393002));
#33630=CARTESIAN_POINT('Ctrl Pts',(0.74950918126488,-4.86080436241777,49.2152547114352));
#33631=CARTESIAN_POINT('Ctrl Pts',(0.891849589093414,-4.83885625782888,
49.2234096687002));
#33632=CARTESIAN_POINT('Ctrl Pts',(1.03323304406454,-4.81065036414039,49.2315646259652));
#33633=CARTESIAN_POINT('Ctrl Pts',(1.17310510440446,-4.77629641841042,49.2397195832302));
#33634=CARTESIAN_POINT('Ctrl Pts',(1.31296892638229,-4.74194449610273,49.2478740601742));
#33635=CARTESIAN_POINT('Ctrl Pts',(1.45132120705093,-4.70144532694967,49.2560285371182));
#33636=CARTESIAN_POINT('Ctrl Pts',(1.5876201028899,-4.65495923412868,49.2641830140622));
#33637=CARTESIAN_POINT('Ctrl Pts',(1.72395247403347,-4.60846172422241,49.2723394937634));
#33638=CARTESIAN_POINT('Ctrl Pts',(1.8582301356656,-4.5559744603208,49.2804959734646));
#33639=CARTESIAN_POINT('Ctrl Pts',(1.98992816161218,-4.49770707962655,49.2886524531658));
#33640=CARTESIAN_POINT('Ctrl Pts',(2.0793558104611,-4.45814145347065,49.294190993302));
#33641=CARTESIAN_POINT('Ctrl Pts',(2.16759437950105,-4.41591169874794,49.2997295334382));
#33642=CARTESIAN_POINT('Ctrl Pts',(2.25448517276978,-4.37109593446097,49.3052680735744));
#33643=CARTESIAN_POINT('Ctrl Pts',(2.38247563376097,-4.30508214732678,49.313426363752));
#33644=CARTESIAN_POINT('Ctrl Pts',(2.50758830220511,-4.23343076051948,49.3215846539296));
#33645=CARTESIAN_POINT('Ctrl Pts',(2.62932987891126,-4.15641762222764,49.3297429441072));
#33646=CARTESIAN_POINT('Ctrl Pts',(2.75104685793632,-4.07942004431104,49.337899585916));
#33647=CARTESIAN_POINT('Ctrl Pts',(2.86939382167824,-3.99706305474322,49.3460562277248));
#33648=CARTESIAN_POINT('Ctrl Pts',(2.98390494230295,-3.90966678347401,49.3542128695336));
#33649=CARTESIAN_POINT('Ctrl Pts',(3.09842010979685,-3.82226742358532,49.3623697996014));
#33650=CARTESIAN_POINT('Ctrl Pts',(3.20909889490924,-3.72982862549775,49.3705267296692));
#33651=CARTESIAN_POINT('Ctrl Pts',(3.31550675515293,-3.63271221252597,49.378683659737));
#33652=CARTESIAN_POINT('Ctrl Pts',(3.42190831197147,-3.53560155256941,49.3868401066018));
#33653=CARTESIAN_POINT('Ctrl Pts',(3.52403920376839,-3.43381405815351,49.3949965534665));
#33654=CARTESIAN_POINT('Ctrl Pts',(3.62150015463472,-3.32774994440398,49.4031530003313));
#33655=CARTESIAN_POINT('Ctrl Pts',(3.71898476532931,-3.22166008230402,49.4113114272725));
#33656=CARTESIAN_POINT('Ctrl Pts',(3.81179694326111,-3.11129177243436,49.4194698542138));
#33657=CARTESIAN_POINT('Ctrl Pts',(3.89957586233266,-2.99708043876244,49.427628281155));
#33658=CARTESIAN_POINT('Ctrl Pts',(3.95906105316276,-2.91968277825017,49.4331570070564));
#33659=CARTESIAN_POINT('Ctrl Pts',(4.01623559033989,-2.84052098032081,49.4386857329579));
#33660=CARTESIAN_POINT('Ctrl Pts',(4.07099804335122,-2.75973875457996,49.4442144588593));
#33661=CARTESIAN_POINT('Ctrl Pts',(4.15172859067097,-2.64064998227064,49.4523648802423));
#33662=CARTESIAN_POINT('Ctrl Pts',(4.22724559219509,-2.51799334936182,49.4605153016252));
#33663=CARTESIAN_POINT('Ctrl Pts',(4.2972481714216,-2.39224606086283,49.4686657230081));
#33664=CARTESIAN_POINT('Ctrl Pts',(4.36723626350179,-2.26652479596736,49.4768144576482));
#33665=CARTESIAN_POINT('Ctrl Pts',(4.43171204672463,-2.13771444450357,49.4849631922884));
#33666=CARTESIAN_POINT('Ctrl Pts',(4.49041994060349,-2.00631797567847,49.4931119269285));
#33667=CARTESIAN_POINT('Ctrl Pts',(4.54913005609664,-1.8749165345702,49.5012609699316));
#33668=CARTESIAN_POINT('Ctrl Pts',(4.60207170512697,-1.74092908514969,49.5094100129348));
#33669=CARTESIAN_POINT('Ctrl Pts',(4.64903671980356,-1.60488025734576,49.517559055938));
#33670=CARTESIAN_POINT('Ctrl Pts',(4.69599911974273,-1.46883900394509,49.5257076452501));
#33671=CARTESIAN_POINT('Ctrl Pts',(4.73698544253774,-1.33073691938958,49.5338562345622));
#33672=CARTESIAN_POINT('Ctrl Pts',(4.77183685689096,-1.19111547455192,49.5420048238743));
#33673=CARTESIAN_POINT('Ctrl Pts',(4.80669724594076,-1.05145807535979,49.5501555115551));
#33674=CARTESIAN_POINT('Ctrl Pts',(4.83541948825201,-0.910280859824225,
49.5583061992359));
#33675=CARTESIAN_POINT('Ctrl Pts',(4.8578953623635,-0.768137820203664,49.5664568869167));
#33676=CARTESIAN_POINT('Ctrl Pts',(4.87324932407909,-0.671035532762169,
49.5720248726594));
#33677=CARTESIAN_POINT('Ctrl Pts',(4.88568936452691,-0.573482777099811,
49.577592858402));
#33678=CARTESIAN_POINT('Ctrl Pts',(4.89519482048859,-0.475658209181462,
49.5831608441447));
#33679=CARTESIAN_POINT('Ctrl Pts',(4.90914294322574,-0.33211232505609,49.5913311990283));
#33680=CARTESIAN_POINT('Ctrl Pts',(4.91677519099054,-0.187927578512104,
49.5995015539119));
#33681=CARTESIAN_POINT('Ctrl Pts',(4.91805612251975,-0.0436696490248933,
49.6076719087955));
#33682=CARTESIAN_POINT('Ctrl Pts',(4.91933680114459,0.100559798486057,49.6158406505418));
#33683=CARTESIAN_POINT('Ctrl Pts',(4.91426866240652,0.244862068010121,49.624009392288));
#33684=CARTESIAN_POINT('Ctrl Pts',(4.90286836852894,0.388670584657962,49.6321781340343));
#33685=CARTESIAN_POINT('Ctrl Pts',(4.89146776839561,0.532482964555806,49.6403470952244));
#33686=CARTESIAN_POINT('Ctrl Pts',(4.87373469525807,0.675801233489329,49.6485160564145));
#33687=CARTESIAN_POINT('Ctrl Pts',(4.84973780482396,0.818062520203257,49.6566850176046));
#33688=CARTESIAN_POINT('Ctrl Pts',(4.82574253298665,0.960314211354579,49.664853427796));
#33689=CARTESIAN_POINT('Ctrl Pts',(4.7954843449171,1.10150873532644,49.6730218379874));
#33690=CARTESIAN_POINT('Ctrl Pts',(4.75908327686338,1.24109202977835,49.6811902481789));
#33691=CARTESIAN_POINT('Ctrl Pts',(4.72267435320067,1.38070544729643,49.6893604211712));
#33692=CARTESIAN_POINT('Ctrl Pts',(4.68011998404698,1.51870661870121,49.6975305941636));
#33693=CARTESIAN_POINT('Ctrl Pts',(4.63159063780015,1.6545546912514,49.7057007671559));
#33694=CARTESIAN_POINT('Ctrl Pts',(4.59910683404554,1.74548651849501,49.7111695879139));
#33695=CARTESIAN_POINT('Ctrl Pts',(4.56394699150573,1.83545393997024,49.7166384086718));
#33696=CARTESIAN_POINT('Ctrl Pts',(4.52617449794241,1.92429921703351,49.7221072294298));
#33697=CARTESIAN_POINT('Ctrl Pts',(4.47001670612233,2.05638884371259,49.7302379316592));
#33698=CARTESIAN_POINT('Ctrl Pts',(4.40806101688729,2.18604583523466,49.7383686338887));
#33699=CARTESIAN_POINT('Ctrl Pts',(4.34054380093662,2.31276081224381,49.7464993361181));
#33700=CARTESIAN_POINT('Ctrl Pts',(4.2730406525832,2.4394493874644,49.7546283442693));
#33701=CARTESIAN_POINT('Ctrl Pts',(4.1999784481678,2.5631968720442,49.7627573524206));
#33702=CARTESIAN_POINT('Ctrl Pts',(4.12163978233728,2.68351794612123,49.7708863605718));
#33703=CARTESIAN_POINT('Ctrl Pts',(4.04329642595676,2.80384622445695,49.7790158554497));
#33704=CARTESIAN_POINT('Ctrl Pts',(3.95967615792387,2.92074739588798,49.7871453503276));
#33705=CARTESIAN_POINT('Ctrl Pts',(3.87110549478319,3.03376421476018,49.7952748452055));
#33706=CARTESIAN_POINT('Ctrl Pts',(3.78253822332834,3.14677670581624,49.8034040287762));
#33707=CARTESIAN_POINT('Ctrl Pts',(3.68902114658794,3.2559048763766,49.8115332123468));
#33708=CARTESIAN_POINT('Ctrl Pts',(3.59092166438334,3.36072383018337,49.8196623959174));
#33709=CARTESIAN_POINT('Ctrl Pts',(3.49279204407795,3.46557498644548,49.827794076934));
#33710=CARTESIAN_POINT('Ctrl Pts',(3.39007743703124,3.5661140331609,49.8359257579506));
#33711=CARTESIAN_POINT('Ctrl Pts',(3.28318318799768,3.66195183154413,49.8440574389671));
#33712=CARTESIAN_POINT('Ctrl Pts',(3.20870931069034,3.72872261203726,49.849722830883));
#33713=CARTESIAN_POINT('Ctrl Pts',(3.13220742683228,3.79321216257162,49.8553882227989));
#33714=CARTESIAN_POINT('Ctrl Pts',(3.05382444009089,3.85530016361937,49.8610536147148));
#33715=CARTESIAN_POINT('Ctrl Pts',(2.94028011452916,3.94523983672345,49.8692604097207));
#33716=CARTESIAN_POINT('Ctrl Pts',(2.82274158545749,4.03017446421762,49.8774672047265));
#33717=CARTESIAN_POINT('Ctrl Pts',(2.70166900979517,4.10976491103961,49.8856739997324));
#33718=CARTESIAN_POINT('Ctrl Pts',(2.58062228977396,4.18933836093213,49.893879042137));
#33719=CARTESIAN_POINT('Ctrl Pts',(2.45604330140261,4.26356972828012,49.9020840845417));
#33720=CARTESIAN_POINT('Ctrl Pts',(2.32842119384962,4.33216317865936,49.9102891269463));
#33721=CARTESIAN_POINT('Ctrl Pts',(2.20080501859814,4.40075344058608,49.9184937879532));
#33722=CARTESIAN_POINT('Ctrl Pts',(2.07014629201985,4.46370615109296,49.92669844896));
#33723=CARTESIAN_POINT('Ctrl Pts',(1.93695922718213,4.52077117478136,49.9349031099669));
#33724=CARTESIAN_POINT('Ctrl Pts',(1.80378819378023,4.57782932967761,49.9431067833967));
#33725=CARTESIAN_POINT('Ctrl Pts',(1.66808972996679,4.62900108541544,49.9513104568264));
#33726=CARTESIAN_POINT('Ctrl Pts',(1.53039860575751,4.67408420655806,49.9595141302562));
#33727=CARTESIAN_POINT('Ctrl Pts',(1.39269508346662,4.71917138710696,49.9677185423669));
#33728=CARTESIAN_POINT('Ctrl Pts',(1.25299885180337,4.75816873474349,49.9759229544776));
#33729=CARTESIAN_POINT('Ctrl Pts',(1.11186100265542,4.79092351987319,49.9841273665884));
#33730=CARTESIAN_POINT('Ctrl Pts',(1.02084374227571,4.8120464916687,49.9894182443922));
#33731=CARTESIAN_POINT('Ctrl Pts',(0.929227268209053,4.8305743615327,49.9947091221961));
#33732=CARTESIAN_POINT('Ctrl Pts',(0.837162017642339,4.84647736182859,50.));
#33733=CARTESIAN_POINT('Ctrl Pts',(-4.91824999915337,-9.12569049791451E-5,
48.7349629410195));
#33734=CARTESIAN_POINT('Ctrl Pts',(-4.91825434592466,0.234176033562846,
48.7218012036652));
#33735=CARTESIAN_POINT('Ctrl Pts',(-4.9015207571834,0.468144306462426,48.7087390737667));
#33736=CARTESIAN_POINT('Ctrl Pts',(-4.85907259687595,0.763339949708897,
48.6919547342511));
#33737=CARTESIAN_POINT('Ctrl Pts',(-4.84873434829882,0.826468084567931,
48.6883485203186));
#33738=CARTESIAN_POINT('Ctrl Pts',(-4.82568931602746,0.951806148915575,
48.6811469871145));
#33739=CARTESIAN_POINT('Ctrl Pts',(-4.81300330664162,1.01400758264125,48.6775524728086));
#33740=CARTESIAN_POINT('Ctrl Pts',(-4.78816591077663,1.12479159538779,48.6711086002473));
#33741=CARTESIAN_POINT('Ctrl Pts',(-4.7764703200144,1.17346480007204,48.6682628776392));
#33742=CARTESIAN_POINT('Ctrl Pts',(-4.76403458580012,1.22194825086837,48.6654127926075));
#33743=CARTESIAN_POINT('Origin',(0.,0.,0.));
#33744=CARTESIAN_POINT('',(-4.03656765912811,4.32587940999471,49.0832499999999));
#33745=CARTESIAN_POINT('Ctrl Pts',(-5.91653912833173,0.000142916515667024,
47.5616248077951));
#33746=CARTESIAN_POINT('Ctrl Pts',(-5.91592149880519,-0.686681391260685,
47.5939532561295));
#33747=CARTESIAN_POINT('Ctrl Pts',(-5.62516687896037,-2.35799619906392,
47.6725971662253));
#33748=CARTESIAN_POINT('Ctrl Pts',(-4.08414406137617,-4.62189440864751,
47.7975565380834));
#33749=CARTESIAN_POINT('Ctrl Pts',(-1.37510285831354,-6.01258952044505,
47.9365029233684));
#33750=CARTESIAN_POINT('Ctrl Pts',(1.66912564744111,-5.93768980797298,48.0754493086537));
#33751=CARTESIAN_POINT('Ctrl Pts',(4.30649751429276,-4.41545237791594,48.2143956939387));
#33752=CARTESIAN_POINT('Ctrl Pts',(5.8941419046702,-1.81692926751613,48.3533420792238));
#33753=CARTESIAN_POINT('Ctrl Pts',(6.04506355860129,1.22447831006187,48.492288464509));
#33754=CARTESIAN_POINT('Ctrl Pts',(4.72247474170802,3.96741385956337,48.631234849794));
#33755=CARTESIAN_POINT('Ctrl Pts',(2.24876208132675,5.74327526323482,48.7701812350792));
#33756=CARTESIAN_POINT('Ctrl Pts',(-0.7730959231624,6.11918790880795,48.9091276203643));
#33757=CARTESIAN_POINT('Ctrl Pts',(-2.90114233776988,5.28126301364285,49.0134838753379));
#33758=CARTESIAN_POINT('Ctrl Pts',(-3.8546249267777,4.4960048839609,49.0715246685497));
#33759=CARTESIAN_POINT('Ctrl Pts',(-4.03656765912811,4.32587940999471,49.0832499999999));
#33760=CARTESIAN_POINT('',(0.902187534995306,5.84756258745463,49.0832469945976));
#33761=CARTESIAN_POINT('Origin',(0.,0.,49.08325));
#33762=CARTESIAN_POINT('Ctrl Pts',(0.902187534995306,5.84756258745463,49.0832469945976));
#33763=CARTESIAN_POINT('Ctrl Pts',(1.0757113845097,5.82079056890589,49.0749812014674));
#33764=CARTESIAN_POINT('Ctrl Pts',(1.24800634179856,5.786296037608,49.0667154083371));
#33765=CARTESIAN_POINT('Ctrl Pts',(1.41841873069125,5.74421612292959,49.0584496152068));
#33766=CARTESIAN_POINT('Ctrl Pts',(1.45137406665876,5.7360784650121,49.0568511281988));
#33767=CARTESIAN_POINT('Ctrl Pts',(1.48425903291376,5.7276572809102,49.0552526411908));
#33768=CARTESIAN_POINT('Ctrl Pts',(1.51706895429147,5.71895378110586,49.0536541541828));
#33769=CARTESIAN_POINT('Ctrl Pts',(1.67680621552835,5.67658021958721,49.0458718149983));
#33770=CARTESIAN_POINT('Ctrl Pts',(1.83479720312141,5.62750197905755,49.0380894758137));
#33771=CARTESIAN_POINT('Ctrl Pts',(1.99047581665468,5.5718880629292,49.0303071366292));
#33772=CARTESIAN_POINT('Ctrl Pts',(2.1461224191251,5.51628558228658,49.0225263976705));
#33773=CARTESIAN_POINT('Ctrl Pts',(2.29945729458024,5.45415021512252,49.0147456587119));
#33774=CARTESIAN_POINT('Ctrl Pts',(2.44993138878728,5.38570021006877,49.0069649197533));
#33775=CARTESIAN_POINT('Ctrl Pts',(2.60041021113751,5.31724805420344,48.9991839363111));
#33776=CARTESIAN_POINT('Ctrl Pts',(2.74802777889052,5.24248099225811,48.9914029528689));
#33777=CARTESIAN_POINT('Ctrl Pts',(2.89225616972135,5.1616649262819,48.9836219694266));
#33778=CARTESIAN_POINT('Ctrl Pts',(3.03647469212574,5.08085438992021,48.9758415183766));
#33779=CARTESIAN_POINT('Ctrl Pts',(3.17730422203144,4.99399583444173,48.9680610673265));
#33780=CARTESIAN_POINT('Ctrl Pts',(3.31424242478615,4.90140058679635,48.9602806162765));
#33781=CARTESIAN_POINT('Ctrl Pts',(3.45121716393948,4.80878063386925,48.952498089329));
#33782=CARTESIAN_POINT('Ctrl Pts',(3.58429823450697,4.7104211082961,48.9447155623815));
#33783=CARTESIAN_POINT('Ctrl Pts',(3.71301247910061,4.60667655610236,48.9369330354341));
#33784=CARTESIAN_POINT('Ctrl Pts',(3.83594526161443,4.50759190147001,48.9295000765128));
#33785=CARTESIAN_POINT('Ctrl Pts',(3.9548947117549,4.40359555872854,48.9220671175916));
#33786=CARTESIAN_POINT('Ctrl Pts',(4.06947700835253,4.29503055181102,48.9146341586704));
#33787=CARTESIAN_POINT('Ctrl Pts',(4.18955912618769,4.18125454678624,48.9068444260891));
#33788=CARTESIAN_POINT('Ctrl Pts',(4.3048878997653,4.06241941215262,48.8990546935078));
#33789=CARTESIAN_POINT('Ctrl Pts',(4.41504675538643,3.93894563433563,48.8912649609265));
#33790=CARTESIAN_POINT('Ctrl Pts',(4.52518422084792,3.81549583211103,48.883476740921));
#33791=CARTESIAN_POINT('Ctrl Pts',(4.63015355899246,3.68740942199132,48.8756885209156));
#33792=CARTESIAN_POINT('Ctrl Pts',(4.72957676690374,3.55514193365952,48.8679003009101));
#33793=CARTESIAN_POINT('Ctrl Pts',(4.82900391645889,3.42286920156877,48.8601117721399));
#33794=CARTESIAN_POINT('Ctrl Pts',(4.92288430087925,3.28641531243443,48.8523232433696));
#33795=CARTESIAN_POINT('Ctrl Pts',(5.01088130159669,3.14626749400121,48.8445347145993));
#33796=CARTESIAN_POINT('Ctrl Pts',(5.09887251503693,3.00612889263526,48.8367466980553));
#33797=CARTESIAN_POINT('Ctrl Pts',(5.18098094941818,2.86229711859535,48.8289586815112));
#33798=CARTESIAN_POINT('Ctrl Pts',(5.25691420862224,2.71528701350071,48.8211706649672));
#33799=CARTESIAN_POINT('Ctrl Pts',(5.33286733050105,2.56823845340056,48.8133806112284));
#33800=CARTESIAN_POINT('Ctrl Pts',(5.4026419011453,2.41801018389847,48.8055905574896));
#33801=CARTESIAN_POINT('Ctrl Pts',(5.46599183768833,2.26514100947922,48.7978005037508));
#33802=CARTESIAN_POINT('Ctrl Pts',(5.52613276935194,2.12001545649662,48.7904050568865));
#33803=CARTESIAN_POINT('Ctrl Pts',(5.58048372723525,1.97251016469156,48.7830096100221));
#33804=CARTESIAN_POINT('Ctrl Pts',(5.62887457408974,1.82310218903551,48.7756141631578));
#33805=CARTESIAN_POINT('Ctrl Pts',(5.67983320173127,1.66576612461353,48.7678262890557));
#33806=CARTESIAN_POINT('Ctrl Pts',(5.72420011388111,1.50626403321614,48.7600384149535));
#33807=CARTESIAN_POINT('Ctrl Pts',(5.76181081107359,1.34516420555095,48.7522505408513));
#33808=CARTESIAN_POINT('Ctrl Pts',(5.79941412039692,1.18409602272447,48.7444641965212));
#33809=CARTESIAN_POINT('Ctrl Pts',(5.83026379015604,1.02143104084788,48.7366778521911));
#33810=CARTESIAN_POINT('Ctrl Pts',(5.85424595748507,0.857749865502559,48.7288915078611));
#33811=CARTESIAN_POINT('Ctrl Pts',(5.87822904954059,0.694062378787835,48.7211048632979));
#33812=CARTESIAN_POINT('Ctrl Pts',(5.89534405906009,0.529358935806454,48.7133182187348));
#33813=CARTESIAN_POINT('Ctrl Pts',(5.90552863021208,0.36422817058195,48.7055315741717));
#33814=CARTESIAN_POINT('Ctrl Pts',(5.91571253028362,0.19910828613257,48.6977454426852));
#33815=CARTESIAN_POINT('Ctrl Pts',(5.91896688628404,0.0335614547822753,
48.6899593111986));
#33816=CARTESIAN_POINT('Ctrl Pts',(5.91528138719896,-0.131820608243138,
48.6821731797121));
#33817=CARTESIAN_POINT('Ctrl Pts',(5.91159491591334,-0.297246297525582,
48.6743849943162));
#33818=CARTESIAN_POINT('Ctrl Pts',(5.90096493665034,-0.462506811887508,
48.6665968089203));
#33819=CARTESIAN_POINT('Ctrl Pts',(5.8834332717793,-0.627011562110531,48.6588086235243));
#33820=CARTESIAN_POINT('Ctrl Pts',(5.86676458812731,-0.783418706605302,
48.651403804898));
#33821=CARTESIAN_POINT('Ctrl Pts',(5.84385736427122,-0.939142439080653,
48.6439989862717));
#33822=CARTESIAN_POINT('Ctrl Pts',(5.81479093755537,-1.09368044465644,48.6365941676453));
#33823=CARTESIAN_POINT('Ctrl Pts',(5.78422191898618,-1.25620730797797,48.6288065561751));
#33824=CARTESIAN_POINT('Ctrl Pts',(5.74682905763876,-1.41748092584339,48.6210189447049));
#33825=CARTESIAN_POINT('Ctrl Pts',(5.70273990443529,-1.57692363317358,48.6132313332347));
#33826=CARTESIAN_POINT('Ctrl Pts',(5.6586594545948,-1.73633486591978,48.605445259068));
#33827=CARTESIAN_POINT('Ctrl Pts',(5.60788543554517,-1.89391560142245,48.5976591849012));
#33828=CARTESIAN_POINT('Ctrl Pts',(5.55059575249572,-2.04910159701183,48.5898731107345));
#33829=CARTESIAN_POINT('Ctrl Pts',(5.49330392747658,-2.2042933947576,48.5820867454589));
#33830=CARTESIAN_POINT('Ctrl Pts',(5.42949605793907,-2.35708997222679,48.5743003801833));
#33831=CARTESIAN_POINT('Ctrl Pts',(5.35939911575957,-2.50694469035429,48.5665140149077));
#33832=CARTESIAN_POINT('Ctrl Pts',(5.2893068326131,-2.65678944830293,48.5587281671573));
#33833=CARTESIAN_POINT('Ctrl Pts',(5.21292644883726,-2.80369244871058,48.5509423194069));
#33834=CARTESIAN_POINT('Ctrl Pts',(5.13053210744219,-2.94712925692185,48.5431564716565));
#33835=CARTESIAN_POINT('Ctrl Pts',(5.04811608039854,-3.09060381675739,48.5353685747222));
#33836=CARTESIAN_POINT('Ctrl Pts',(4.95968309050393,-3.23061008316695,48.5275806777879));
#33837=CARTESIAN_POINT('Ctrl Pts',(4.865552515652,-3.36664956298283,48.5197927808536));
#33838=CARTESIAN_POINT('Ctrl Pts',(4.77603539145568,-3.49602158721023,48.5123865779467));
#33839=CARTESIAN_POINT('Ctrl Pts',(4.68136595057938,-3.62180613137823,48.5049803750398));
#33840=CARTESIAN_POINT('Ctrl Pts',(4.58185447348852,-3.74359989131761,48.4975741721329));
#33841=CARTESIAN_POINT('Ctrl Pts',(4.47720858649184,-3.87167774135172,48.4897858376098));
#33842=CARTESIAN_POINT('Ctrl Pts',(4.36717040269952,-3.99538786321501,48.4819975030867));
#33843=CARTESIAN_POINT('Ctrl Pts',(4.2521285355429,-4.1142840786365,48.4742091685636));
#33844=CARTESIAN_POINT('Ctrl Pts',(4.1371092096297,-4.23315699759559,48.4664223600827));
#33845=CARTESIAN_POINT('Ctrl Pts',(4.017088378608,-4.34721766268525,48.4586355516018));
#33846=CARTESIAN_POINT('Ctrl Pts',(3.89249243811587,-4.45605578754472,48.4508487431209));
#33847=CARTESIAN_POINT('Ctrl Pts',(3.76789167283227,-4.56489812699781,48.4430616331075));
#33848=CARTESIAN_POINT('Ctrl Pts',(3.63871568159011,-4.66851730840554,48.4352745230942));
#33849=CARTESIAN_POINT('Ctrl Pts',(3.5054255112133,-4.76654199056664,48.4274874130808));
#33850=CARTESIAN_POINT('Ctrl Pts',(3.37214412699704,-4.86456021118153,48.4197008163745));
#33851=CARTESIAN_POINT('Ctrl Pts',(3.23474936382851,-4.95698448132655,48.4119142196683));
#33852=CARTESIAN_POINT('Ctrl Pts',(3.09373305327206,-5.04348553657011,48.4041276229621));
#33853=CARTESIAN_POINT('Ctrl Pts',(2.9526796341123,-5.13000935466524,48.396338977204));
#33854=CARTESIAN_POINT('Ctrl Pts',(2.8080030347374,-5.21060667441763,48.3885503314459));
#33855=CARTESIAN_POINT('Ctrl Pts',(2.66022238318807,-5.28499266172482,48.3807616856879));
#33856=CARTESIAN_POINT('Ctrl Pts',(2.51976834871897,-5.35569076675905,48.3733591826653));
#33857=CARTESIAN_POINT('Ctrl Pts',(2.37651082322848,-5.42077838556117,48.3659566796428));
#33858=CARTESIAN_POINT('Ctrl Pts',(2.23091453197799,-5.48005026560062,48.3585541766202));
#33859=CARTESIAN_POINT('Ctrl Pts',(2.07774094308078,-5.54240684424937,48.3507664236146));
#33860=CARTESIAN_POINT('Ctrl Pts',(1.9219238572207,-5.59834851440998,48.342978670609));
#33861=CARTESIAN_POINT('Ctrl Pts',(1.76401794960577,-5.64766954025894,48.3351909176035));
#33862=CARTESIAN_POINT('Ctrl Pts',(1.60614314965164,-5.69698084980428,48.3274046987949));
#33863=CARTESIAN_POINT('Ctrl Pts',(1.44618065387223,-5.73967402222281,48.3196184799864));
#33864=CARTESIAN_POINT('Ctrl Pts',(1.28470113377979,-5.77559291842534,48.3118322611779));
#33865=CARTESIAN_POINT('Ctrl Pts',(1.123215504986,-5.81151317342439,48.30404574782));
#33866=CARTESIAN_POINT('Ctrl Pts',(0.960213048135258,-5.84065856614888,
48.2962592344622));
#33867=CARTESIAN_POINT('Ctrl Pts',(0.796276219423017,-5.862923736915,48.2884727211043));
#33868=CARTESIAN_POINT('Ctrl Pts',(0.632350253164033,-5.88518743239105,
48.2806867236808));
#33869=CARTESIAN_POINT('Ctrl Pts',(0.467490355659226,-5.90057177529173,
48.2729007262572));
#33870=CARTESIAN_POINT('Ctrl Pts',(0.302285873648315,-5.90902308449482,
48.2651147288337));
#33871=CARTESIAN_POINT('Ctrl Pts',(0.137037885705147,-5.91747661931602,
48.2573266809992));
#33872=CARTESIAN_POINT('Ctrl Pts',(-0.0285545487879778,-5.91899345383947,
48.2495386331648));
#33873=CARTESIAN_POINT('Ctrl Pts',(-0.193899382391169,-5.91357198248303,
48.2417505853303));
#33874=CARTESIAN_POINT('Ctrl Pts',(-0.351121822789253,-5.90841683527564,
48.2343451172562));
#33875=CARTESIAN_POINT('Ctrl Pts',(-0.508120141164401,-5.89698870428187,
48.226939649182));
#33876=CARTESIAN_POINT('Ctrl Pts',(-0.664387412158191,-5.87932988775641,
48.2195341811079));
#33877=CARTESIAN_POINT('Ctrl Pts',(-0.828728543247588,-5.86075869326994,
48.2117460947619));
#33878=CARTESIAN_POINT('Ctrl Pts',(-0.992319878645803,-5.83528928235357,
48.2039580084159));
#33879=CARTESIAN_POINT('Ctrl Pts',(-1.15457589028596,-5.80300655488777,
48.1961699220699));
#33880=CARTESIAN_POINT('Ctrl Pts',(-1.31680002986572,-5.77073016874041,
48.1883833655431));
#33881=CARTESIAN_POINT('Ctrl Pts',(-1.47768905585395,-5.73164319875144,
48.1805968090163));
#33882=CARTESIAN_POINT('Ctrl Pts',(-1.63666713806711,-5.68588174707065,
48.1728102524895));
#33883=CARTESIAN_POINT('Ctrl Pts',(-1.79565130644826,-5.64011854350132,
48.1650233978695));
#33884=CARTESIAN_POINT('Ctrl Pts',(-1.95272407652092,-5.58768043153087,
48.1572365432494));
#33885=CARTESIAN_POINT('Ctrl Pts',(-2.10732357918337,-5.52875373797005,
48.1494496886294));
#33886=CARTESIAN_POINT('Ctrl Pts',(-2.26191286346188,-5.46983093921852,
48.141663348688));
#33887=CARTESIAN_POINT('Ctrl Pts',(-2.41402890890177,-5.40442053102927,
48.1338770087467));
#33888=CARTESIAN_POINT('Ctrl Pts',(-2.5631285345683,-5.33275751162396,48.1260906688053));
#33889=CARTESIAN_POINT('Ctrl Pts',(-2.71226740054379,-5.26107563181568,
48.118302279641));
#33890=CARTESIAN_POINT('Ctrl Pts',(-2.85838797140062,-5.18313798933969,
48.1105138904766));
#33891=CARTESIAN_POINT('Ctrl Pts',(-3.0009696227234,-5.09922659684695,48.1027255013122));
#33892=CARTESIAN_POINT('Ctrl Pts',(-3.13651010510691,-5.01945903552036,
48.0953217294065));
#33893=CARTESIAN_POINT('Ctrl Pts',(-3.26885253438473,-4.9342936286528,48.0879179575009));
#33894=CARTESIAN_POINT('Ctrl Pts',(-3.39757238832685,-4.84400995339388,
48.0805141855952));
#33895=CARTESIAN_POINT('Ctrl Pts',(-3.53297126245669,-4.74904163570251,
48.0727262465194));
#33896=CARTESIAN_POINT('Ctrl Pts',(-3.66441005731167,-4.64837580729459,
48.0649383074436));
#33897=CARTESIAN_POINT('Ctrl Pts',(-3.79141533198079,-4.54236726200348,
48.0571503683679));
#33898=CARTESIAN_POINT('Ctrl Pts',(-3.91839562909804,-4.43637956493262,
48.0493639609108));
#33899=CARTESIAN_POINT('Ctrl Pts',(-4.04094390058947,-4.32505145213363,
48.0415775534537));
#33900=CARTESIAN_POINT('Ctrl Pts',(-4.15861972835657,-4.20877803137959,
48.0337911459966));
#33901=CARTESIAN_POINT('Ctrl Pts',(-4.27630004069902,-4.09250017949534,
48.0260044418029));
#33902=CARTESIAN_POINT('Ctrl Pts',(-4.38910730767105,-3.97127686431734,
48.0182177376092));
#33903=CARTESIAN_POINT('Ctrl Pts',(-4.49663740936991,-3.84554060843921,
48.0104310334154));
#33904=CARTESIAN_POINT('Ctrl Pts',(-4.60416039755778,-3.71981267047602,
48.0026448443408));
#33905=CARTESIAN_POINT('Ctrl Pts',(-4.70640671145677,-3.58957263220266,
47.9948586552661));
#33906=CARTESIAN_POINT('Ctrl Pts',(-4.80301193638849,-3.45528680450837,
47.9870724661915));
#33907=CARTESIAN_POINT('Ctrl Pts',(-4.89964259538731,-3.32096562225894,
47.9792842271816));
#33908=CARTESIAN_POINT('Ctrl Pts',(-4.99062900939446,-3.1825967805922,47.9714959881716));
#33909=CARTESIAN_POINT('Ctrl Pts',(-5.07564907232607,-3.04067707214947,
47.9637077491617));
#33910=CARTESIAN_POINT('Ctrl Pts',(-5.15648027556416,-2.90574961619296,
47.9563032294688));
#33911=CARTESIAN_POINT('Ctrl Pts',(-5.23191875230041,-2.76761299210775,
47.9488987097758));
#33912=CARTESIAN_POINT('Ctrl Pts',(-5.30172552274323,-2.62671601890899,
47.9414941900828));
#33913=CARTESIAN_POINT('Ctrl Pts',(-5.37493451551398,-2.47895204949891,
47.9337287910357));
#33914=CARTESIAN_POINT('Ctrl Pts',(-5.44197671386717,-2.32809613211981,
47.9259633919887));
#33915=CARTESIAN_POINT('Ctrl Pts',(-5.50260701658285,-2.17468309956951,
47.9181979929416));
#33916=CARTESIAN_POINT('Ctrl Pts',(-5.56322478575962,-2.0213017806694,47.9104341991633));
#33917=CARTESIAN_POINT('Ctrl Pts',(-5.61743318505499,-1.86536470170965,
47.902670405385));
#33918=CARTESIAN_POINT('Ctrl Pts',(-5.66503538115071,-1.70742633598366,
47.8949066116067));
#33919=CARTESIAN_POINT('Ctrl Pts',(-5.71263811119004,-1.549486198697,47.8871427307436));
#33920=CARTESIAN_POINT('Ctrl Pts',(-5.75363439281445,-1.38954503810943,
47.8793788498805));
#33921=CARTESIAN_POINT('Ctrl Pts',(-5.78787717610237,-1.22817277158113,
47.8716149690174));
#33922=CARTESIAN_POINT('Ctrl Pts',(-5.82211830257874,-1.06680831292969,
47.8638514638039));
#33923=CARTESIAN_POINT('Ctrl Pts',(-5.84960651834727,-0.904013203300888,
47.8560879585904));
#33924=CARTESIAN_POINT('Ctrl Pts',(-5.870245801473,-0.74036801172702,47.8483244533769));
#33925=CARTESIAN_POINT('Ctrl Pts',(-5.89088955153219,-0.576687402635144,
47.840559267918));
#33926=CARTESIAN_POINT('Ctrl Pts',(-5.90468136710913,-0.412156664851667,
47.832794082459));
#33927=CARTESIAN_POINT('Ctrl Pts',(-5.91157696882471,-0.247362697594452,
47.8250288970001));
#33928=CARTESIAN_POINT('Ctrl Pts',(-5.91502652397537,-0.16492378914296,
47.8211443287491));
#33929=CARTESIAN_POINT('Ctrl Pts',(-5.91675108445212,-0.0824190692800998,
47.8172597604981));
#33930=CARTESIAN_POINT('Ctrl Pts',(-5.91674999948831,7.78145712749811E-5,
47.8133751922472));
#33931=CARTESIAN_POINT('Origin',(0.,0.,49.5));
#33932=CARTESIAN_POINT('',(1.67563808492399,4.71079034076956,50.0000691378445));
#33933=CARTESIAN_POINT('Ctrl Pts',(1.67563808492399,4.71079034076956,50.0000691378444));
#33934=CARTESIAN_POINT('Ctrl Pts',(1.81473787532752,4.66673395805934,49.9949609527894));
#33935=CARTESIAN_POINT('Ctrl Pts',(1.95192304800988,4.61660905950312,49.9898325023651));
#33936=CARTESIAN_POINT('Ctrl Pts',(2.08679675191645,4.5605717909821,49.9846699266638));
#33937=CARTESIAN_POINT('Ctrl Pts',(2.18013465240617,4.52179180020974,49.9810972215098));
#33938=CARTESIAN_POINT('Ctrl Pts',(2.27236538682205,4.48017983818195,49.9775087411235));
#33939=CARTESIAN_POINT('Ctrl Pts',(2.36335535052691,4.43578180111657,49.9739072133534));
#33940=CARTESIAN_POINT('Ctrl Pts',(2.39724229344457,4.41924685938859,49.9725659141486));
#33941=CARTESIAN_POINT('Ctrl Pts',(2.43095712394704,4.40232543880356,49.9712228642745));
#33942=CARTESIAN_POINT('Ctrl Pts',(2.4644928777425,4.38501972948132,49.9698784137574));
#33943=CARTESIAN_POINT('Ctrl Pts',(2.48261127171451,4.37566995725381,49.9691520461828));
#33944=CARTESIAN_POINT('Ctrl Pts',(2.50067739438694,4.36620794637243,49.9684252705303));
#33945=CARTESIAN_POINT('Ctrl Pts',(2.51867750380479,4.35664094393442,49.9676986693424));
#33946=CARTESIAN_POINT('Ctrl Pts',(2.6509623677971,4.28633194819731,49.9623587940626));
#33947=CARTESIAN_POINT('Ctrl Pts',(2.77985412600453,4.2102669796089,49.9570193910659));
#33948=CARTESIAN_POINT('Ctrl Pts',(2.90498713229767,4.12869881484235,49.9517226559453));
#33949=CARTESIAN_POINT('Ctrl Pts',(2.98517938741253,4.0764253558088,49.9483282107334));
#33950=CARTESIAN_POINT('Ctrl Pts',(3.0638282861637,4.02189100982338,49.9449518083139));
#33951=CARTESIAN_POINT('Ctrl Pts',(3.14084006697321,3.96515302750838,49.941609459733));
#33952=CARTESIAN_POINT('Ctrl Pts',(3.26052055661263,3.87697912173403,49.9364152685259));
#33953=CARTESIAN_POINT('Ctrl Pts',(3.3762503040121,3.783482753799,49.9313021101912));
#33954=CARTESIAN_POINT('Ctrl Pts',(3.48774777220362,3.68497444840038,49.9262024865122));
#33955=CARTESIAN_POINT('Ctrl Pts',(3.59964773861427,3.58611053477017,49.9210844535412));
#33956=CARTESIAN_POINT('Ctrl Pts',(3.70728451516587,3.48219804431622,49.9159798531581));
#33957=CARTESIAN_POINT('Ctrl Pts',(3.81034263019071,3.37354157002801,49.9108454843505));
#33958=CARTESIAN_POINT('Ctrl Pts',(3.82681372888809,3.35617572249937,49.910024892053));
#33959=CARTESIAN_POINT('Ctrl Pts',(3.84316781368502,3.33868868374835,49.9092035945216));
#33960=CARTESIAN_POINT('Ctrl Pts',(3.85940353090415,3.32108168337155,49.9083814791383));
#33961=CARTESIAN_POINT('Ctrl Pts',(3.87395088755691,3.30530564400049,49.9076448559557));
#33962=CARTESIAN_POINT('Ctrl Pts',(3.88839828689456,3.28943859217021,49.9069078245672));
#33963=CARTESIAN_POINT('Ctrl Pts',(3.90273991934431,3.2734873277252,49.9061705797287));
#33964=CARTESIAN_POINT('Ctrl Pts',(4.00336138882482,3.16157261549479,49.900998040321));
#33965=CARTESIAN_POINT('Ctrl Pts',(4.09885594019099,3.04542909728232,49.8958086469949));
#33966=CARTESIAN_POINT('Ctrl Pts',(4.18899320504064,2.92546460240762,49.8905961980074));
#33967=CARTESIAN_POINT('Ctrl Pts',(4.27967435974525,2.8047762396429,49.8853522970102));
#33968=CARTESIAN_POINT('Ctrl Pts',(4.36493356340819,2.68022087265818,49.8800851496014));
#33969=CARTESIAN_POINT('Ctrl Pts',(4.44453028409552,2.55218579792693,49.8748169014774));
#33970=CARTESIAN_POINT('Ctrl Pts',(4.52372110061123,2.42480363917638,49.8695755188306));
#33971=CARTESIAN_POINT('Ctrl Pts',(4.59730749734601,2.29397740000137,49.8643332430544));
#33972=CARTESIAN_POINT('Ctrl Pts',(4.66504193211966,2.16005750620798,49.8591377514506));
#33973=CARTESIAN_POINT('Ctrl Pts',(4.68953272611782,2.11163598261943,49.8572592133775));
#33974=CARTESIAN_POINT('Ctrl Pts',(4.71325833516671,2.06280970337978,49.8553870226302));
#33975=CARTESIAN_POINT('Ctrl Pts',(4.73620649163542,2.0135941395332,49.8535241873519));
#33976=CARTESIAN_POINT('Ctrl Pts',(4.78178682276434,1.91584067947285,49.8498241668757));
#33977=CARTESIAN_POINT('Ctrl Pts',(4.82430078597844,1.81655097495366,49.8461607180028));
#33978=CARTESIAN_POINT('Ctrl Pts',(4.8636946286286,1.71586513965779,49.8425084955917));
#33979=CARTESIAN_POINT('Ctrl Pts',(4.87286993785393,1.69241417343309,49.8416578481878));
#33980=CARTESIAN_POINT('Ctrl Pts',(4.88187594172209,1.66888748460883,49.8408078339904));
#33981=CARTESIAN_POINT('Ctrl Pts',(4.89071188208244,1.64528687215975,49.839958177956));
#33982=CARTESIAN_POINT('Ctrl Pts',(4.89798164868161,1.6258694771678,49.839259123774));
#33983=CARTESIAN_POINT('Ctrl Pts',(4.90513662158331,1.60640097331495,49.8385602749155));
#33984=CARTESIAN_POINT('Ctrl Pts',(4.91217064536634,1.58689872257296,49.8378620703334));
#33985=CARTESIAN_POINT('Ctrl Pts',(4.96311473550224,1.44565319223368,49.8328053064864));
#33986=CARTESIAN_POINT('Ctrl Pts',(5.00779051564247,1.30244333780008,49.8277731701466));
#33987=CARTESIAN_POINT('Ctrl Pts',(5.04617351021521,1.15771482827818,49.8227255511406));
#33988=CARTESIAN_POINT('Ctrl Pts',(5.08523210610634,1.01043886843539,49.8175890860689));
#33989=CARTESIAN_POINT('Ctrl Pts',(5.11777433764025,0.861590382504143,49.8124364914983));
#33990=CARTESIAN_POINT('Ctrl Pts',(5.14375382774835,0.711627275063704,49.8072534416659));
#33991=CARTESIAN_POINT('Ctrl Pts',(5.16973623733982,0.561647315298723,49.8020698093807));
#33992=CARTESIAN_POINT('Ctrl Pts',(5.18915456037088,0.410552554862994,49.7968557639674));
#33993=CARTESIAN_POINT('Ctrl Pts',(5.20194190393592,0.258788407666574,49.7916249163614));
#33994=CARTESIAN_POINT('Ctrl Pts',(5.21263748941908,0.131849892144523,49.7872497326155));
#33995=CARTESIAN_POINT('Ctrl Pts',(5.21869385085329,0.00444285787804401,
49.7828633223158));
#33996=CARTESIAN_POINT('Ctrl Pts',(5.22005878849942,-0.123179295803443,
49.7784880643338));
#33997=CARTESIAN_POINT('Ctrl Pts',(5.22077192299229,-0.189857623640299,
49.7762021376535));
#33998=CARTESIAN_POINT('Ctrl Pts',(5.22020421945982,-0.256594784247294,
49.7739194680061));
#33999=CARTESIAN_POINT('Ctrl Pts',(5.21834663224238,-0.323355354262235,
49.771644593243));
#34000=CARTESIAN_POINT('Ctrl Pts',(5.21760990549823,-0.349832871400289,
49.7707423685388));
#34001=CARTESIAN_POINT('Ctrl Pts',(5.21666999205992,-0.376318760520563,
49.7698412213317));
#34002=CARTESIAN_POINT('Ctrl Pts',(5.21552778162834,-0.40278134925187,49.7689424724782));
#34003=CARTESIAN_POINT('Ctrl Pts',(5.21403770096407,-0.437303352120437,
49.7677700017568));
#34004=CARTESIAN_POINT('Ctrl Pts',(5.21220321919947,-0.471794424074401,
49.7666013129027));
#34005=CARTESIAN_POINT('Ctrl Pts',(5.21002489504197,-0.506249741277439,
49.7654371522064));
#34006=CARTESIAN_POINT('Ctrl Pts',(5.20048560553725,-0.657136029089896,
49.76033907446));
#34007=CARTESIAN_POINT('Ctrl Pts',(5.18435463935589,-0.807337611433697,
49.7553259977829));
#34008=CARTESIAN_POINT('Ctrl Pts',(5.16180066510662,-0.956461402467586,
49.7503329133453));
#34009=CARTESIAN_POINT('Ctrl Pts',(5.13892017184147,-1.1077440925476,49.7452675428885));
#34010=CARTESIAN_POINT('Ctrl Pts',(5.1094289591262,-1.25791749088514,49.7402225599689));
#34011=CARTESIAN_POINT('Ctrl Pts',(5.0734771776897,-1.40656178859565,49.7351555827664));
#34012=CARTESIAN_POINT('Ctrl Pts',(5.03735518795703,-1.55590982035319,49.7300646167233));
#34013=CARTESIAN_POINT('Ctrl Pts',(4.99471115982055,-1.70371415190665,49.7249513647013));
#34014=CARTESIAN_POINT('Ctrl Pts',(4.94567556523468,-1.8495408292695,49.7198003753935));
#34015=CARTESIAN_POINT('Ctrl Pts',(4.91220116110093,-1.94909017037065,49.7162840257044));
#34016=CARTESIAN_POINT('Ctrl Pts',(4.87574775360055,-2.04771773028405,49.7127506702632));
#34017=CARTESIAN_POINT('Ctrl Pts',(4.8363511645014,-2.14528350432509,49.7092029050148));
#34018=CARTESIAN_POINT('Ctrl Pts',(4.81834271520086,-2.18988148439041,49.7075811973476));
#34019=CARTESIAN_POINT('Ctrl Pts',(4.79971923269632,-2.23425758647001,49.7059565627866));
#34020=CARTESIAN_POINT('Ctrl Pts',(4.78048379291373,-2.27839832664545,49.704329671404));
#34021=CARTESIAN_POINT('Ctrl Pts',(4.77194664210255,-2.29798904877367,49.7036076178798));
#34022=CARTESIAN_POINT('Ctrl Pts',(4.7632889450894,-2.31753340840308,49.7028851232796));
#34023=CARTESIAN_POINT('Ctrl Pts',(4.75451095611775,-2.33703022197421,49.7021622627468));
#34024=CARTESIAN_POINT('Ctrl Pts',(4.74667071160333,-2.35444420895271,49.7015166247373));
#34025=CARTESIAN_POINT('Ctrl Pts',(4.73873635227771,-2.37181609008569,49.7008708493076));
#34026=CARTESIAN_POINT('Ctrl Pts',(4.73071159737849,-2.3891379247781,49.7002252650528));
#34027=CARTESIAN_POINT('Ctrl Pts',(4.66523858368199,-2.53046469853094,49.6949580204724));
#34028=CARTESIAN_POINT('Ctrl Pts',(4.59368613047665,-2.6686038217097,49.6896960901462));
#34029=CARTESIAN_POINT('Ctrl Pts',(4.51629355623815,-2.80317176969319,49.6844869056202));
#34030=CARTESIAN_POINT('Ctrl Pts',(4.48067498182562,-2.86510430670922,49.6820894698391));
#34031=CARTESIAN_POINT('Ctrl Pts',(4.44381883724951,-2.92628069281049,49.6797035477704));
#34032=CARTESIAN_POINT('Ctrl Pts',(4.40574537996631,-2.98666472899764,49.6773353894376));
#34033=CARTESIAN_POINT('Ctrl Pts',(4.32349081779372,-3.11711945555011,49.6722191788092));
#34034=CARTESIAN_POINT('Ctrl Pts',(4.23555519682983,-3.24387869280854,49.6671843479792));
#34035=CARTESIAN_POINT('Ctrl Pts',(4.14224309128914,-3.36664706312078,49.6621642705163));
#34036=CARTESIAN_POINT('Ctrl Pts',(4.04832514101874,-3.49021252797609,49.6571115993459));
#34037=CARTESIAN_POINT('Ctrl Pts',(3.94896027663346,-3.60973488258529,49.6520736777843));
#34038=CARTESIAN_POINT('Ctrl Pts',(3.84444539643511,-3.72488498895488,49.6470075110166));
#34039=CARTESIAN_POINT('Ctrl Pts',(3.79544021921852,-3.7788768354598,49.6446320750999));
#34040=CARTESIAN_POINT('Ctrl Pts',(3.74530265014764,-3.83190706666856,49.6422508029622));
#34041=CARTESIAN_POINT('Ctrl Pts',(3.69406254468819,-3.88393986178611,49.6398612952612));
#34042=CARTESIAN_POINT('Ctrl Pts',(3.65781405006707,-3.92074912431648,49.6381708995004));
#34043=CARTESIAN_POINT('Ctrl Pts',(3.62101378289051,-3.95705919634303,49.6364764096212));
#34044=CARTESIAN_POINT('Ctrl Pts',(3.58367218371391,-3.99285705051874,49.6347773814871));
#34045=CARTESIAN_POINT('Ctrl Pts',(3.5629338467586,-4.01273804058193,49.6338337952799));
#34046=CARTESIAN_POINT('Ctrl Pts',(3.5420240329473,-4.03246511448107,49.6328886149264));
#34047=CARTESIAN_POINT('Ctrl Pts',(3.52096943456868,-4.05201320692815,49.6319429224079));
#34048=CARTESIAN_POINT('Ctrl Pts',(3.40614714622976,-4.15861969103541,49.6267855417209));
#34049=CARTESIAN_POINT('Ctrl Pts',(3.2869131976001,-4.26001078709387,49.621605694337));
#34050=CARTESIAN_POINT('Ctrl Pts',(3.16366579501986,-4.35593771903587,49.6164161867119));
#34051=CARTESIAN_POINT('Ctrl Pts',(3.03981531919331,-4.45233403990652,49.6112012858278));
#34052=CARTESIAN_POINT('Ctrl Pts',(2.91191230951189,-4.54321295118199,49.6059767851582));
#34053=CARTESIAN_POINT('Ctrl Pts',(2.78032667834594,-4.62831864044268,49.6007824755997));
#34054=CARTESIAN_POINT('Ctrl Pts',(2.68229691010553,-4.6917213913376,49.5969127752557));
#34055=CARTESIAN_POINT('Ctrl Pts',(2.5822225803561,-4.75191998217825,49.5930604106771));
#34056=CARTESIAN_POINT('Ctrl Pts',(2.48024286974118,-4.80880497922347,49.5892505120726));
#34057=CARTESIAN_POINT('Ctrl Pts',(2.34350335530138,-4.88507923836746,49.5841420088017));
#34058=CARTESIAN_POINT('Ctrl Pts',(2.20333578698035,-4.95539857695016,49.5791090270458));
#34059=CARTESIAN_POINT('Ctrl Pts',(2.06013087428636,-5.01960377050101,49.5740842955298));
#34060=CARTESIAN_POINT('Ctrl Pts',(2.01243378737825,-5.04098851659063,49.5724107142867));
#34061=CARTESIAN_POINT('Ctrl Pts',(1.96439981353058,-5.06169468099203,49.5707382348701));
#34062=CARTESIAN_POINT('Ctrl Pts',(1.91604359986973,-5.08171549901325,49.5690649525599));
#34063=CARTESIAN_POINT('Ctrl Pts',(1.87554041937874,-5.09848494278274,49.5676634107457));
#34064=CARTESIAN_POINT('Ctrl Pts',(1.83481116554692,-5.11477355733233,49.5662613106286));
#34065=CARTESIAN_POINT('Ctrl Pts',(1.79386451568791,-5.13057715241704,49.5648577003405));
#34066=CARTESIAN_POINT('Ctrl Pts',(1.77567815094702,-5.1375962845174,49.5642342899091));
#34067=CARTESIAN_POINT('Ctrl Pts',(1.75745120137326,-5.14451880655941,49.563610662824));
#34068=CARTESIAN_POINT('Ctrl Pts',(1.7391946641175,-5.15134072548734,49.5629870931035));
#34069=CARTESIAN_POINT('Ctrl Pts',(1.59001261215237,-5.20708557182655,49.5578916355613));
#34070=CARTESIAN_POINT('Ctrl Pts',(1.43866498273231,-5.25618865327407,49.5527910414675));
#34071=CARTESIAN_POINT('Ctrl Pts',(1.28563400442455,-5.29859710524125,49.5476623291469));
#34072=CARTESIAN_POINT('Ctrl Pts',(1.13288844745672,-5.34092646030062,49.5425431824971));
#34073=CARTESIAN_POINT('Ctrl Pts',(0.978465894027958,-5.37658617453509,
49.5373960864726));
#34074=CARTESIAN_POINT('Ctrl Pts',(0.822827740101826,-5.40550619246802,
49.5322268987557));
#34075=CARTESIAN_POINT('Ctrl Pts',(0.666753346477603,-5.434507270601,49.5270432222721));
#34076=CARTESIAN_POINT('Ctrl Pts',(0.509456618531798,-5.45673116976558,
49.5218374346355));
#34077=CARTESIAN_POINT('Ctrl Pts',(0.351383211732529,-5.47208668410592,
49.5166431048256));
#34078=CARTESIAN_POINT('Ctrl Pts',(0.19330980493326,-5.48744219844627,49.5114487750157));
#34079=CARTESIAN_POINT('Ctrl Pts',(0.0344597161104908,-5.49592995853461,
49.5062660817186));
#34080=CARTESIAN_POINT('Ctrl Pts',(-0.124741716672891,-5.49743085582899,
49.5011540746717));
#34081=CARTESIAN_POINT('Ctrl Pts',(-0.180692942040016,-5.49795834506889,
49.4993574635901));
#34082=CARTESIAN_POINT('Ctrl Pts',(-0.236687812261172,-5.49762253264645,
49.4975698016442));
#34083=CARTESIAN_POINT('Ctrl Pts',(-0.292708187959222,-5.49642372103878,
49.4957878125479));
#34084=CARTESIAN_POINT('Ctrl Pts',(-0.310662081935003,-5.49603951553797,
49.4952167052873));
#34085=CARTESIAN_POINT('Ctrl Pts',(-0.328616265529814,-5.49556668586931,
49.4946462573012));
#34086=CARTESIAN_POINT('Ctrl Pts',(-0.346561355889629,-5.49500566096314,
49.4940766453379));
#34087=CARTESIAN_POINT('Ctrl Pts',(-0.503655794107246,-5.49009435147994,
49.4890901632658));
#34088=CARTESIAN_POINT('Ctrl Pts',(-0.660246401114815,-5.47842251008643,
49.4841595921883));
#34089=CARTESIAN_POINT('Ctrl Pts',(-0.815916987885523,-5.46014480646224,
49.4792299596291));
#34090=CARTESIAN_POINT('Ctrl Pts',(-0.973868778975,-5.44159926048382,49.4742280879957));
#34091=CARTESIAN_POINT('Ctrl Pts',(-1.13087330605085,-5.41625257091423,
49.4692270433391));
#34092=CARTESIAN_POINT('Ctrl Pts',(-1.28649294986338,-5.38424187213397,
49.4641961154961));
#34093=CARTESIAN_POINT('Ctrl Pts',(-1.44300002932614,-5.35204862933427,
49.459136498314));
#34094=CARTESIAN_POINT('Ctrl Pts',(-1.59810631725191,-5.3131151399391,49.4540466189856));
#34095=CARTESIAN_POINT('Ctrl Pts',(-1.75136501543228,-5.26755851017518,
49.4489233408825));
#34096=CARTESIAN_POINT('Ctrl Pts',(-1.90361219626974,-5.22230255712089,
49.4438338767471));
#34097=CARTESIAN_POINT('Ctrl Pts',(-2.05403612331965,-5.17051080101936,
49.4387115327372));
#34098=CARTESIAN_POINT('Ctrl Pts',(-2.20219753609186,-5.11227467177507,
49.4335804768557));
#34099=CARTESIAN_POINT('Ctrl Pts',(-2.25665635950895,-5.09086915856033,
49.4316944846735));
#34100=CARTESIAN_POINT('Ctrl Pts',(-2.3108094940984,-5.06859274266779,49.4298075756852));
#34101=CARTESIAN_POINT('Ctrl Pts',(-2.36463504949088,-5.04544904547062,
49.4279218429996));
#34102=CARTESIAN_POINT('Ctrl Pts',(-2.38837021496942,-5.03524349387428,
49.427090301606));
#34103=CARTESIAN_POINT('Ctrl Pts',(-2.41204483876381,-5.02486780300145,
49.4262588832171));
#34104=CARTESIAN_POINT('Ctrl Pts',(-2.43563327483403,-5.0143331018827,49.4254286347634));
#34105=CARTESIAN_POINT('Ctrl Pts',(-2.55373048104147,-4.96159036104766,
49.421271936009));
#34106=CARTESIAN_POINT('Ctrl Pts',(-2.66978375591747,-4.90481436355621,
49.4171397528067));
#34107=CARTESIAN_POINT('Ctrl Pts',(-2.78359497648946,-4.84411571837135,
49.413063622511));
#34108=CARTESIAN_POINT('Ctrl Pts',(-2.924248586175,-4.76910129092416,49.4080261364287));
#34109=CARTESIAN_POINT('Ctrl Pts',(-3.0614810489766,-4.68809507551227,49.403073459607));
#34110=CARTESIAN_POINT('Ctrl Pts',(-3.19498666686176,-4.60140279590078,
49.3981389260757));
#34111=CARTESIAN_POINT('Ctrl Pts',(-3.3299447733608,-4.51376733838381,49.3931507067604));
#34112=CARTESIAN_POINT('Ctrl Pts',(-3.46109428099897,-4.42032105177208,
49.3881808356728));
#34113=CARTESIAN_POINT('Ctrl Pts',(-3.58809628381318,-4.32136180668214,
49.3831857066336));
#34114=CARTESIAN_POINT('Ctrl Pts',(-3.70950179427866,-4.22676331690086,
49.3784106938195));
#34115=CARTESIAN_POINT('Ctrl Pts',(-3.82711700729642,-4.12712681810338,
49.3736127057868));
#34116=CARTESIAN_POINT('Ctrl Pts',(-3.94062874722527,-4.02270054491346,
49.3687768116061));
#34117=CARTESIAN_POINT('Ctrl Pts',(-3.98572004581248,-3.98121834873086,
49.3668558054743));
#34118=CARTESIAN_POINT('Ctrl Pts',(-4.03016364557377,-3.93898021007131,
49.3649290738369));
#34119=CARTESIAN_POINT('Ctrl Pts',(-4.07393922780361,-3.89600120334253,
49.3629966996388));
#34120=CARTESIAN_POINT('Ctrl Pts',(-4.10700497887908,-3.8635371431159,49.3615370867458));
#34121=CARTESIAN_POINT('Ctrl Pts',(-4.13968958544803,-3.83065037589362,
49.3600742663872));
#34122=CARTESIAN_POINT('Ctrl Pts',(-4.17198414223093,-3.79734728864012,
49.3586084949218));
#34123=CARTESIAN_POINT('Ctrl Pts',(-4.18608658919232,-3.78280443472203,
49.3579684191193));
#34124=CARTESIAN_POINT('Ctrl Pts',(-4.20011079548223,-3.76818613348426,
49.3573279572478));
#34125=CARTESIAN_POINT('Ctrl Pts',(-4.21405108877795,-3.75349847141212,
49.3566873776368));
#34126=CARTESIAN_POINT('Ctrl Pts',(-4.32957559830332,-3.6317804471952,49.3513788347101));
#34127=CARTESIAN_POINT('Ctrl Pts',(-4.43944604389779,-3.50519034747474,
49.3460548328354));
#34128=CARTESIAN_POINT('Ctrl Pts',(-4.54337101560959,-3.37414716019543,
49.3407518834976));
#34129=CARTESIAN_POINT('Ctrl Pts',(-4.64729598732139,-3.24310397291613,
49.3354489341598));
#34130=CARTESIAN_POINT('Ctrl Pts',(-4.74527612649365,-3.10760807449447,
49.3301673120086));
#34131=CARTESIAN_POINT('Ctrl Pts',(-4.8370174576042,-2.96803270750451,49.3249708337327));
#34132=CARTESIAN_POINT('Ctrl Pts',(-4.92609830595216,-2.83250500205884,
49.3199250524297));
#34133=CARTESIAN_POINT('Ctrl Pts',(-5.00929931953407,-2.69312714851096,
49.3149596075419));
#34134=CARTESIAN_POINT('Ctrl Pts',(-5.08645441034632,-2.55029552791752,
49.3100065247623));
#34135=CARTESIAN_POINT('Ctrl Pts',(-5.16378621091767,-2.40713677737061,
49.3050420978439));
#34136=CARTESIAN_POINT('Ctrl Pts',(-5.23504395172591,-2.26050815104089,
49.3000898940267));
#34137=CARTESIAN_POINT('Ctrl Pts',(-5.3000273093003,-2.1108115805684,49.2951060476122));
#34138=CARTESIAN_POINT('Ctrl Pts',(-5.31786155570052,-2.06972836137618,
49.2937382644091));
#34139=CARTESIAN_POINT('Ctrl Pts',(-5.33522304787959,-2.02841409497743,
49.2923682492653));
#34140=CARTESIAN_POINT('Ctrl Pts',(-5.35210726416258,-1.98687715762331,
49.2909954452123));
#34141=CARTESIAN_POINT('Ctrl Pts',(-5.36297878413954,-1.96013208182836,
49.2901115151301));
#34142=CARTESIAN_POINT('Ctrl Pts',(-5.37365434333545,-1.93328954670697,
49.2892262632332));
#34143=CARTESIAN_POINT('Ctrl Pts',(-5.38412129062111,-1.90638177843231,
49.2883405601123));
#34144=CARTESIAN_POINT('Ctrl Pts',(-5.44359691541729,-1.75348559138468,
49.283307789328));
#34145=CARTESIAN_POINT('Ctrl Pts',(-5.49640364515274,-1.59833076538052,
49.2782530325609));
#34146=CARTESIAN_POINT('Ctrl Pts',(-5.54246661452835,-1.44139155837415,
49.27317314757));
#34147=CARTESIAN_POINT('Ctrl Pts',(-5.58879486804785,-1.28354851291058,
49.2680640066939));
#34148=CARTESIAN_POINT('Ctrl Pts',(-5.62830171747107,-1.12390060961607,
49.2629295393757));
#34149=CARTESIAN_POINT('Ctrl Pts',(-5.66089528402405,-0.962905702878125,
49.2577946040462));
#34150=CARTESIAN_POINT('Ctrl Pts',(-5.69333557172059,-0.802667912277112,
49.252683816949));
#34151=CARTESIAN_POINT('Ctrl Pts',(-5.71892794727571,-0.641095804455549,
49.2475727597972));
#34152=CARTESIAN_POINT('Ctrl Pts',(-5.73756064484128,-0.478615090618444,
49.2425114365551));
#34153=CARTESIAN_POINT('Ctrl Pts',(-5.74450339795431,-0.418072945401361,
49.2406255304713));
#34154=CARTESIAN_POINT('Ctrl Pts',(-5.75047962292998,-0.357404389991355,
49.2387467691439));
#34155=CARTESIAN_POINT('Ctrl Pts',(-5.75548252324649,-0.296630523360118,
49.2368785590806));
#34156=CARTESIAN_POINT('Ctrl Pts',(-5.76537892967853,-0.17641168097307,
49.2331829895276));
#34157=CARTESIAN_POINT('Ctrl Pts',(-5.77146731689194,-0.0557799619614495,
49.2295283245924));
#34158=CARTESIAN_POINT('Ctrl Pts',(-5.77374672853297,0.065096445717814,
49.2258863162828));
#34159=CARTESIAN_POINT('Ctrl Pts',(-5.77459391555212,0.110022479112958,
49.2245326940989));
#34160=CARTESIAN_POINT('Ctrl Pts',(-5.77491484307218,0.154982237612365,
49.2231808830343));
#34161=CARTESIAN_POINT('Ctrl Pts',(-5.77470914469647,0.199966813322252,
49.2218296639618));
#34162=CARTESIAN_POINT('Ctrl Pts',(-5.77458352980315,0.227437777343764,
49.221004508007));
#34163=CARTESIAN_POINT('Ctrl Pts',(-5.77426136385812,0.254922353169247,
49.2201794445654));
#34164=CARTESIAN_POINT('Ctrl Pts',(-5.77374329813058,0.282389833044242,
49.2193550800525));
#34165=CARTESIAN_POINT('Ctrl Pts',(-5.77065780153438,0.445980688713763,
49.2144453287152));
#34166=CARTESIAN_POINT('Ctrl Pts',(-5.76062670170217,0.609147527714891,
49.2095527300581));
#34167=CARTESIAN_POINT('Ctrl Pts',(-5.74378571552021,0.771448622323782,
49.2046391550914));
#34168=CARTESIAN_POINT('Ctrl Pts',(-5.72666463659201,0.936449045749695,
49.1996438594528));
#34169=CARTESIAN_POINT('Ctrl Pts',(-5.70250521466273,1.10055459203251,49.1946267993558));
#34170=CARTESIAN_POINT('Ctrl Pts',(-5.67142703313475,1.26330529042377,49.1895761902436));
#34171=CARTESIAN_POINT('Ctrl Pts',(-5.64034926925677,1.42605380165904,49.1845256490049));
#34172=CARTESIAN_POINT('Ctrl Pts',(-5.60235308985842,1.58744747929261,49.1794416145631));
#34173=CARTESIAN_POINT('Ctrl Pts',(-5.55753454842355,1.74703145364951,49.1743404530506));
#34174=CARTESIAN_POINT('Ctrl Pts',(-5.5200120235029,1.88063673090842,49.1700697103212));
#34175=CARTESIAN_POINT('Ctrl Pts',(-5.47770730015332,2.01297368705868,49.1657874941309));
#34176=CARTESIAN_POINT('Ctrl Pts',(-5.43066194318534,2.14377785630578,49.1615179508413));
#34177=CARTESIAN_POINT('Ctrl Pts',(-5.40713926470134,2.20917994092934,49.1593831791965));
#34178=CARTESIAN_POINT('Ctrl Pts',(-5.38243120004108,2.27419885983428,49.1572517781467));
#34179=CARTESIAN_POINT('Ctrl Pts',(-5.35654143278953,2.33880167648566,49.155127939542));
#34180=CARTESIAN_POINT('Ctrl Pts',(-5.34671655063384,2.36331773545052,49.1543219661314));
#34181=CARTESIAN_POINT('Ctrl Pts',(-5.33672147795149,2.38777387113981,49.1535170895802));
#34182=CARTESIAN_POINT('Ctrl Pts',(-5.3265563732068,2.41216828423402,49.1527135670967));
#34183=CARTESIAN_POINT('Ctrl Pts',(-5.31673784757985,2.43573097012222,49.1519374407022));
#34184=CARTESIAN_POINT('Ctrl Pts',(-5.306759648629,2.4592382882221,49.1511625043726));
#34185=CARTESIAN_POINT('Ctrl Pts',(-5.29663156396569,2.48266680522254,49.150389723225));
#34186=CARTESIAN_POINT('Ctrl Pts',(-5.28961442410136,2.49889901358878,49.1498543097113));
#34187=CARTESIAN_POINT('Ctrl Pts',(-5.28252441466418,2.51509565043687,49.1493198567731));
#34188=CARTESIAN_POINT('Ctrl Pts',(-5.27536177146622,2.53125625338851,49.1487864472261));
#34189=CARTESIAN_POINT('Ctrl Pts',(-5.20905723135039,2.68085484668549,49.1438486786215));
#34190=CARTESIAN_POINT('Ctrl Pts',(-5.1365305147677,2.82736721515206,49.1389984596951));
#34191=CARTESIAN_POINT('Ctrl Pts',(-5.05808337360841,2.97048046784585,49.1341699969887));
#34192=CARTESIAN_POINT('Ctrl Pts',(-4.97795812668693,3.11665513451141,49.129238245992));
#34193=CARTESIAN_POINT('Ctrl Pts',(-4.89165612942615,3.25928352807764,49.1243289773594));
#34194=CARTESIAN_POINT('Ctrl Pts',(-4.79947735049932,3.39801430845291,49.1193976432336));
#34195=CARTESIAN_POINT('Ctrl Pts',(-4.70691216791804,3.53732663353017,49.1144456374787));
#34196=CARTESIAN_POINT('Ctrl Pts',(-4.60842069933321,3.67270845509946,49.1094712986947));
#34197=CARTESIAN_POINT('Ctrl Pts',(-4.50428872136281,3.80378869777911,49.104457163013));
#34198=CARTESIAN_POINT('Ctrl Pts',(-4.4008671297137,3.93397471360161,49.0994772336671));
#34199=CARTESIAN_POINT('Ctrl Pts',(-4.291881788178,4.05991762763984,49.0944580775447));
#34200=CARTESIAN_POINT('Ctrl Pts',(-4.1775954660098,4.18124012170818,49.0894101112488));
#34201=CARTESIAN_POINT('Ctrl Pts',(-4.13145291568673,4.23022349243586,49.0873720192495));
#34202=CARTESIAN_POINT('Ctrl Pts',(-4.08444604836479,4.27845353024594,49.0853295426084));
#34203=CARTESIAN_POINT('Ctrl Pts',(-4.03659128039468,4.32590472425831,49.0832846233473));
#34204=CARTESIAN_POINT('',(-4.72583710973184,1.63293098821764,50.));
#34205=CARTESIAN_POINT('Origin',(0.,0.,50.));
#34206=CARTESIAN_POINT('Ctrl Pts',(0.902188245823411,5.84749488262084,49.083316804731));
#34207=CARTESIAN_POINT('Ctrl Pts',(0.570773072266766,5.86193985911904,49.1195756242143));
#34208=CARTESIAN_POINT('Ctrl Pts',(0.239586412830494,5.84829261175139,49.1560808085295));
#34209=CARTESIAN_POINT('Ctrl Pts',(-0.403141186164292,5.76508832621516,
49.229396259483));
#34210=CARTESIAN_POINT('Ctrl Pts',(-0.712291744810658,5.6984338729017,49.2658262564742));
#34211=CARTESIAN_POINT('Ctrl Pts',(-1.41949250323092,5.48319083688572,49.3516406277647));
#34212=CARTESIAN_POINT('Ctrl Pts',(-2.04693271827507,5.24616261480877,49.4260186478511));
#34213=CARTESIAN_POINT('Ctrl Pts',(-2.95875165016973,4.57432864164807,49.5617463576736));
#34214=CARTESIAN_POINT('Ctrl Pts',(-3.20150736272193,4.35877003192118,49.6014258895003));
#34215=CARTESIAN_POINT('Ctrl Pts',(-3.75505974601525,3.76967225965931,49.7008828051444));
#34216=CARTESIAN_POINT('Ctrl Pts',(-4.04010787119168,3.37408581464056,49.7592710513533));
#34217=CARTESIAN_POINT('Ctrl Pts',(-4.47964495834608,2.52220292271381,49.8796783199167));
#34218=CARTESIAN_POINT('Ctrl Pts',(-4.6331687113469,2.08624253568,49.9395418565637));
#34219=CARTESIAN_POINT('Ctrl Pts',(-4.72583710973167,1.63293098821788,50.0000000000001));
#34220=CARTESIAN_POINT('Ctrl Pts',(3.43704063106228,-4.81656042341828,-0.576723952463529));
#34221=CARTESIAN_POINT('Ctrl Pts',(4.23851061681899,-4.24464230409036,-0.530378404645798));
#34222=CARTESIAN_POINT('Ctrl Pts',(5.54954235425666,-2.69365781311748,-0.437692858323896));
#34223=CARTESIAN_POINT('Ctrl Pts',(6.16159033410026,0.291989391379818,-0.298667313497819));
#34224=CARTESIAN_POINT('Ctrl Pts',(5.27018942791115,3.20546788220774,-0.159647317985302));
#34225=CARTESIAN_POINT('Ctrl Pts',(3.09280338018427,5.33718340530576,-0.0206273224727845));
#34226=CARTESIAN_POINT('Ctrl Pts',(0.160760791193982,6.16638660286929,0.118392673039733));
#34227=CARTESIAN_POINT('Ctrl Pts',(-2.8105137177503,5.49104909633203,0.257412668552251));
#34228=CARTESIAN_POINT('Ctrl Pts',(-5.09599974900626,3.47580295946428,0.396432664064767));
#34229=CARTESIAN_POINT('Ctrl Pts',(-6.13802598467403,0.61246246229798,0.535452659577285));
#34230=CARTESIAN_POINT('Ctrl Pts',(-5.68232839089761,-2.40033714446484,
0.674472655089802));
#34231=CARTESIAN_POINT('Ctrl Pts',(-3.8401015449425,-4.82742989807141,0.813492650602319));
#34232=CARTESIAN_POINT('Ctrl Pts',(-1.06086171213873,-6.0765981420124,0.952512646114838));
#34233=CARTESIAN_POINT('Ctrl Pts',(1.97723602956149,-5.84303022933689,1.09153264162736));
#34234=CARTESIAN_POINT('Ctrl Pts',(4.53287379508907,-4.1837212419108,1.23055263713987));
#34235=CARTESIAN_POINT('Ctrl Pts',(5.98245724399727,-1.50355324653343,1.36957263265239));
#34236=CARTESIAN_POINT('Ctrl Pts',(5.97227747058842,1.54349246619894,1.50859262816491));
#34237=CARTESIAN_POINT('Ctrl Pts',(4.50481839510344,4.21391487875842,1.64761262367743));
#34238=CARTESIAN_POINT('Ctrl Pts',(1.93815075286798,5.85611123715929,1.78663261918994));
#34239=CARTESIAN_POINT('Ctrl Pts',(-1.10143982170116,6.06937374228201,1.92565261470246));
#34240=CARTESIAN_POINT('Ctrl Pts',(-3.87227103928215,4.80166473547632,2.06467261021498));
#34241=CARTESIAN_POINT('Ctrl Pts',(-5.69823985920696,2.3623144936764,2.20369260572749));
#34242=CARTESIAN_POINT('Ctrl Pts',(-6.13379656062603,-0.653457732117191,
2.34271260124001));
#34243=CARTESIAN_POINT('Ctrl Pts',(-5.0726621295139,-3.50978149923841,2.48173259675253));
#34244=CARTESIAN_POINT('Ctrl Pts',(-2.77376111232836,-5.5096929631069,2.62075259226505));
#34245=CARTESIAN_POINT('Ctrl Pts',(0.201957862492829,-6.16519912697854,
2.75977258777756));
#34246=CARTESIAN_POINT('Ctrl Pts',(3.12839764474893,-5.31635170311109,2.89879258329009));
#34247=CARTESIAN_POINT('Ctrl Pts',(5.29148556685501,-3.17027565837135,3.03781257880259));
#34248=CARTESIAN_POINT('Ctrl Pts',(6.16341238700176,-0.25062921257097,3.17683257431512));
#34249=CARTESIAN_POINT('Ctrl Pts',(5.53142159669249,2.73017259053316,3.31585256982763));
#34250=CARTESIAN_POINT('Ctrl Pts',(3.54972356179769,5.04479235342969,3.45487256534015));
#34251=CARTESIAN_POINT('Ctrl Pts',(0.701867067655108,6.12844595911452,3.59389256085267));
#34252=CARTESIAN_POINT('Ctrl Pts',(-2.31725011406836,5.7167140179715,3.73291255636519));
#34253=CARTESIAN_POINT('Ctrl Pts',(-4.77094135387005,3.91006212896485,3.8719325518777));
#34254=CARTESIAN_POINT('Ctrl Pts',(-6.06048807923677,1.14932654013476,4.01095254739023));
#34255=CARTESIAN_POINT('Ctrl Pts',(-5.87123147651013,-1.89185311366029,
4.14997254290273));
#34256=CARTESIAN_POINT('Ctrl Pts',(-4.24935153817855,-4.47140679869429,
4.28899253841526));
#34257=CARTESIAN_POINT('Ctrl Pts',(-1.59059880763312,-5.95990458712096,
4.42801253392777));
#34258=CARTESIAN_POINT('Ctrl Pts',(1.45627164208546,-5.99414215371037,4.56703252944029));
#34259=CARTESIAN_POINT('Ctrl Pts',(4.14780118150638,-4.56576528230742,4.7060525249528));
#34260=CARTESIAN_POINT('Ctrl Pts',(5.82723695697856,-2.0233083555536,4.84507252046533));
#34261=CARTESIAN_POINT('Ctrl Pts',(6.08478438073663,1.01285057850268,4.98409251597784));
#34262=CARTESIAN_POINT('Ctrl Pts',(4.8576000014916,3.80186657839784,5.12311251149037));
#34263=CARTESIAN_POINT('Ctrl Pts',(2.44512576525259,5.66319938255113,5.26213250700287));
#34264=CARTESIAN_POINT('Ctrl Pts',(-0.563977005188219,6.14267020049495,
5.4011525025154));
#34265=CARTESIAN_POINT('Ctrl Pts',(-3.43546526977796,5.123284652894,5.54017249802791));
#34266=CARTESIAN_POINT('Ctrl Pts',(-5.46867493236823,2.8537802540695,5.67919249354042));
#34267=CARTESIAN_POINT('Ctrl Pts',(-6.16748799446796,-0.112067357082,5.81821248905295));
#34268=CARTESIAN_POINT('Ctrl Pts',(-5.36138896814329,-3.05056971510259,
5.95723248456547));
#34269=CARTESIAN_POINT('Ctrl Pts',(-3.24707189970145,-5.24471079589703,
6.09625248007797));
#34270=CARTESIAN_POINT('Ctrl Pts',(-0.340445586681124,-6.15910416026057,
6.23527247559051));
#34271=CARTESIAN_POINT('Ctrl Pts',(2.64925193447237,-5.57063115294167,6.37429247110302));
#34272=CARTESIAN_POINT('Ctrl Pts',(4.99251264617518,-3.62288348311266,6.51331246661553));
#34273=CARTESIAN_POINT('Ctrl Pts',(6.11756383082583,-0.791125799226151,
6.65233246212806));
#34274=CARTESIAN_POINT('Ctrl Pts',(5.74988478738761,2.23367235426287,6.79135245764057));
#34275=CARTESIAN_POINT('Ctrl Pts',(3.97919188622503,4.7134381492739,6.93037245315309));
#34276=CARTESIAN_POINT('Ctrl Pts',(1.23754711987656,6.04309063149933,7.0693924486656));
#34277=CARTESIAN_POINT('Ctrl Pts',(-1.80606817683494,5.89818488986686,7.20841244417813));
#34278=CARTESIAN_POINT('Ctrl Pts',(-4.40898965553244,4.3140789830319,7.34743243969063));
#34279=CARTESIAN_POINT('Ctrl Pts',(-5.93608547614997,1.67730631497977,7.48645243520317));
#34280=CARTESIAN_POINT('Ctrl Pts',(-6.01473311186767,-1.36874133693413,
7.62547243071567));
#34281=CARTESIAN_POINT('Ctrl Pts',(-4.62574196550504,-4.08080611190917,
7.76449242622819));
#34282=CARTESIAN_POINT('Ctrl Pts',(-2.10803601530903,-5.79712440892808,
7.9035124217407));
#34283=CARTESIAN_POINT('Ctrl Pts',(0.924046109614526,-6.09890203575495,
8.04253241725323));
#34284=CARTESIAN_POINT('Ctrl Pts',(3.73065423898791,-4.91250304870655,8.18155241276573));
#34285=CARTESIAN_POINT('Ctrl Pts',(5.6269555032291,-2.527417460395,8.32057240827827));
#34286=CARTESIAN_POINT('Ctrl Pts',(6.15023855236694,0.474376436397263,8.45959240379077));
#34287=CARTESIAN_POINT('Ctrl Pts',(5.17281850286031,3.36041902013657,8.59861239930329));
#34288=CARTESIAN_POINT('Ctrl Pts',(2.93319298118051,5.42649483456707,8.73763239481581));
#34289=CARTESIAN_POINT('Ctrl Pts',(-0.0221530378913636,6.16846630025178,
8.87665239032833));
#34290=CARTESIAN_POINT('Ctrl Pts',(-2.97209355401811,5.40528696375999,9.01567238584084));
#34291=CARTESIAN_POINT('Ctrl Pts',(-5.1968215490371,3.32317815379998,9.15469238135336));
#34292=CARTESIAN_POINT('Ctrl Pts',(-6.15348715341253,0.430189617746093,
9.29371237686589));
#34293=CARTESIAN_POINT('Ctrl Pts',(-5.60865697677616,-2.56776832508109,
9.43273237237838));
#34294=CARTESIAN_POINT('Ctrl Pts',(-3.69527355905571,-4.93917205391485,
9.57175236789092));
#34295=CARTESIAN_POINT('Ctrl Pts',(-0.880216420357442,-6.10538174955201,
9.71077236340343));
#34296=CARTESIAN_POINT('Ctrl Pts',(2.14961994979028,-5.78183373385064,9.84979235891595));
#34297=CARTESIAN_POINT('Ctrl Pts',(4.65493336166727,-4.04747608428597,9.98881235442845));
#34298=CARTESIAN_POINT('Ctrl Pts',(6.02440905597324,-1.32550472678798,10.127832349941));
#34299=CARTESIAN_POINT('Ctrl Pts',(5.92388496721038,1.71989945918022,10.2668523454535));
#34300=CARTESIAN_POINT('Ctrl Pts',(4.37788970678303,4.34563562320553,10.405872340966));
#34301=CARTESIAN_POINT('Ctrl Pts',(1.76365740277551,5.91100497547285,10.5448923364785));
#34302=CARTESIAN_POINT('Ctrl Pts',(-1.28092018081044,6.03404596807335,10.6839123319911));
#34303=CARTESIAN_POINT('Ctrl Pts',(-4.01294389057655,4.68473570071077,10.8229323275036));
#34304=CARTESIAN_POINT('Ctrl Pts',(-5.7657799997321,2.19231572751711,10.9619523230161));
#34305=CARTESIAN_POINT('Ctrl Pts',(-6.1117237033288,-0.835045285357961,
11.1009723185286));
#34306=CARTESIAN_POINT('Ctrl Pts',(-4.9663622125742,-3.65864915343695,11.2399923140411));
#34307=CARTESIAN_POINT('Ctrl Pts',(-2.6091720914435,-5.58951592283822,11.3790123095536));
#34308=CARTESIAN_POINT('Ctrl Pts',(0.384675064887725,-6.15650000803081,
11.5180323050662));
#34309=CARTESIAN_POINT('Ctrl Pts',(3.28465869756325,-5.22125315369325,11.6570523005787));
#34310=CARTESIAN_POINT('Ctrl Pts',(5.38316163262817,-3.01198241884472,11.7960722960912));
#34311=CARTESIAN_POINT('Ctrl Pts',(6.1681338365184,-0.0677659887136258,
11.9350922916037));
#34312=CARTESIAN_POINT('Ctrl Pts',(5.44803636180983,2.89298583730161,12.0741122871163));
#34313=CARTESIAN_POINT('Ctrl Pts',(3.39857824847212,5.14782800251152,12.2131322826287));
#34314=CARTESIAN_POINT('Ctrl Pts',(0.519842235579626,6.14656256004421,12.3521522781413));
#34315=CARTESIAN_POINT('Ctrl Pts',(-2.48573907723061,5.64549098789099,12.4911722736538));
#34316=CARTESIAN_POINT('Ctrl Pts',(-4.88478191127144,3.76687840708258,12.6301922691663));
#34317=CARTESIAN_POINT('Ctrl Pts',(-6.0919023039256,0.969119999719169,12.7692122646788));
#34318=CARTESIAN_POINT('Ctrl Pts',(-5.81255406836334,-2.06511076138364,
12.9082322601914));
#34319=CARTESIAN_POINT('Ctrl Pts',(-4.11490021308256,-4.59543942303701,
13.0472522557038));
#34320=CARTESIAN_POINT('Ctrl Pts',(-1.41318067029944,-6.00444732240376,
13.1862722512164));
#34321=CARTESIAN_POINT('Ctrl Pts',(1.63336527113562,-5.94832624739747,13.3252922467289));
#34322=CARTESIAN_POINT('Ctrl Pts',(4.28135816414165,-4.44077014995906,13.4643122422414));
#34323=CARTESIAN_POINT('Ctrl Pts',(5.88466841457579,-1.84963372182813,13.6033322377539));
#34324=CARTESIAN_POINT('Ctrl Pts',(6.052076618438,1.19282683528906,13.7423522332665));
#34325=CARTESIAN_POINT('Ctrl Pts',(4.74273395203871,3.94422893790522,13.881372228779));
#34326=CARTESIAN_POINT('Ctrl Pts',(2.27612958314307,5.73321038992733,14.0203922242915));
#34327=CARTESIAN_POINT('Ctrl Pts',(-0.745867017981445,6.12324665891528,
14.159412219804));
#34328=CARTESIAN_POINT('Ctrl Pts',(-3.58586662248042,5.01916604828039,14.2984322153165));
#34329=CARTESIAN_POINT('Ctrl Pts',(-5.55088859710986,2.69037228593095,14.437452210829));
#34330=CARTESIAN_POINT('Ctrl Pts',(-6.16145323695721,-0.294891951771045,
14.5764722063416));
#34331=CARTESIAN_POINT('Ctrl Pts',(-5.26857831326169,-3.20820040076339,
14.7154922018541));
#34332=CARTESIAN_POINT('Ctrl Pts',(-3.09013182468434,-5.33868453464922,
14.8545121973666));
#34333=CARTESIAN_POINT('Ctrl Pts',(-0.157670615370865,-6.16649067391479,
14.9935321928791));
#34334=CARTESIAN_POINT('Ctrl Pts',(2.81326337496362,-5.48962807825065,15.1325521883917));
#34335=CARTESIAN_POINT('Ctrl Pts',(5.09774056721409,-3.47325616155927,15.2715721839041));
#34336=CARTESIAN_POINT('Ctrl Pts',(6.13833185159848,-0.609384389430206,
15.4105921794167));
#34337=CARTESIAN_POINT('Ctrl Pts',(5.68112535923535,2.40318162174289,15.5496121749292));
#34338=CARTESIAN_POINT('Ctrl Pts',(3.83768281150632,4.82935377588954,15.6886321704417));
#34339=CARTESIAN_POINT('Ctrl Pts',(1.05781764572689,6.07712835826415,15.8276521659542));
#34340=CARTESIAN_POINT('Ctrl Pts',(-1.98016274684031,5.84203926300189,15.9666721614667));
#34341=CARTESIAN_POINT('Ctrl Pts',(-4.53496897555987,4.18144994531072,16.1056921569792));
#34342=CARTESIAN_POINT('Ctrl Pts',(-5.98320967256359,1.50055631969322,16.2447121524918));
#34343=CARTESIAN_POINT('Ctrl Pts',(-5.97150353677324,-1.54648400080129,
16.3837321480043));
#34344=CARTESIAN_POINT('Ctrl Pts',(-4.50270695076721,-4.21617093699274,
16.5227521435168));
#34345=CARTESIAN_POINT('Ctrl Pts',(-1.93521700258198,-5.8570813898517,16.6617721390293));
#34346=CARTESIAN_POINT('Ctrl Pts',(1.10448001978357,-6.06882123153488,16.8007921345418));
#34347=CARTESIAN_POINT('Ctrl Pts',(3.8746758554932,-4.79972439513851,16.9398121300543));
#34348=CARTESIAN_POINT('Ctrl Pts',(5.69942250039969,-2.35945977214434,17.0788321255669));
#34349=CARTESIAN_POINT('Ctrl Pts',(6.13346845394157,0.656530257439375,17.2178521210794));
#34350=CARTESIAN_POINT('Ctrl Pts',(5.07090333526315,3.5123221120573,17.3568721165919));
#34351=CARTESIAN_POINT('Ctrl Pts',(2.77100078920524,5.51108173416558,17.4958921121044));
#34352=CARTESIAN_POINT('Ctrl Pts',(-0.20504617552828,6.16509718660872,17.6349121076169));
#34353=CARTESIAN_POINT('Ctrl Pts',(-3.13106037675837,5.31478392519616,17.7739321031294));
#34354=CARTESIAN_POINT('Ctrl Pts',(-5.29307299180025,3.16762459232536,17.912952098642));
#34355=CARTESIAN_POINT('Ctrl Pts',(-6.16353716160514,0.247541737778197,
18.0519720941545));
#34356=CARTESIAN_POINT('Ctrl Pts',(-5.53005327504208,-2.73294310764532,
18.190992089667));
#34357=CARTESIAN_POINT('Ctrl Pts',(-3.54719602436282,-5.0465698864847,18.3300120851795));
#34358=CARTESIAN_POINT('Ctrl Pts',(-0.698797052019465,-6.12879677706142,
18.469032080692));
#34359=CARTESIAN_POINT('Ctrl Pts',(2.3201135016813,-5.71555251867621,18.6080520762046));
#34360=CARTESIAN_POINT('Ctrl Pts',(4.77289942598214,-3.90767172673052,18.747072071717));
#34361=CARTESIAN_POINT('Ctrl Pts',(6.06106305196034,-1.14629051055608,18.8860920672296));
#34362=CARTESIAN_POINT('Ctrl Pts',(5.87028305230372,1.89479395720625,19.0251120627421));
#34363=CARTESIAN_POINT('Ctrl Pts',(4.24711113947134,4.47353486891608,19.1641320582546));
#34364=CARTESIAN_POINT('Ctrl Pts',(1.58761310806277,5.96070061935146,19.3031520537671));
#34365=CARTESIAN_POINT('Ctrl Pts',(-1.45927411003053,5.99341191027483,19.4421720492797));
#34366=CARTESIAN_POINT('Ctrl Pts',(-4.15008779373199,4.56368694793438,19.5811920447921));
#34367=CARTESIAN_POINT('Ctrl Pts',(-5.82824976341114,2.0203890590002,19.7202120403047));
#34368=CARTESIAN_POINT('Ctrl Pts',(-6.08427624921397,-1.01589850756883,
19.8592320358172));
#34369=CARTESIAN_POINT('Ctrl Pts',(-4.85569491981417,-3.8042994230371,19.9982520313297));
#34370=CARTESIAN_POINT('Ctrl Pts',(-2.44228858725531,-5.66442351091372,
20.1372720268422));
#34371=CARTESIAN_POINT('Ctrl Pts',(0.567053987364875,-6.14238691632522,
20.2762920223548));
#34372=CARTESIAN_POINT('Ctrl Pts',(3.43803125002338,-5.12156307959712,20.4153120178673));
#34373=CARTESIAN_POINT('Ctrl Pts',(5.47010379277291,-2.851040468096,20.5543320133798));
#34374=CARTESIAN_POINT('Ctrl Pts',(6.16743108266357,0.1151568279563,20.6933520088923));
#34375=CARTESIAN_POINT('Ctrl Pts',(5.35986017102552,3.05325501743365,20.8323720044048));
#34376=CARTESIAN_POINT('Ctrl Pts',(3.24444425492609,5.24633669631551,20.9713919999173));
#34377=CARTESIAN_POINT('Ctrl Pts',(0.337360258753054,6.1592739271966,21.1104119954299));
#34378=CARTESIAN_POINT('Ctrl Pts',(-2.65204210301827,5.56930336202366,21.2494319909424));
#34379=CARTESIAN_POINT('Ctrl Pts',(-4.99432683384769,3.62038212501645,21.3884519864549));
#34380=CARTESIAN_POINT('Ctrl Pts',(-6.1179593625907,0.78806122358511,21.5274719819674));
#34381=CARTESIAN_POINT('Ctrl Pts',(-5.74876515060713,-2.2365523686233,21.6664919774799));
#34382=CARTESIAN_POINT('Ctrl Pts',(-3.97683028044616,-4.71543085782797,
21.8055119729925));
#34383=CARTESIAN_POINT('Ctrl Pts',(-1.23451979414715,-6.04370979881467,
21.944531968505));
#34384=CARTESIAN_POINT('Ctrl Pts',(1.80902253293984,-5.89727943459912,22.0835519640175));
#34385=CARTESIAN_POINT('Ctrl Pts',(4.4111501575588,-4.31186984287546,22.22257195953));
#34386=CARTESIAN_POINT('Ctrl Pts',(5.93692494583333,-1.67433253625779,22.3615919550425));
#34387=CARTESIAN_POINT('Ctrl Pts',(6.01404671247788,1.37175413050724,22.5006119505551));
#34388=CARTESIAN_POINT('Ctrl Pts',(4.62369718350338,4.08312277671056,22.6396319460675));
#34389=CARTESIAN_POINT('Ctrl Pts',(2.10513179242921,5.79817966183642,22.7786519415801));
#34390=CARTESIAN_POINT('Ctrl Pts',(-0.927101121791352,6.09843838735811,
22.9176719370926));
#34391=CARTESIAN_POINT('Ctrl Pts',(-3.73311459519142,4.91063363259758,23.0566919326051));
#34392=CARTESIAN_POINT('Ctrl Pts',(-5.62822085858694,2.52459842774975,23.1957119281177));
#34393=CARTESIAN_POINT('Ctrl Pts',(-6.15000015093573,-0.477457221036609,
23.3347319236301));
#34394=CARTESIAN_POINT('Ctrl Pts',(-5.17113451632943,-3.36300982283073,
23.4737519191427));
#34395=CARTESIAN_POINT('Ctrl Pts',(-2.93047431455525,-5.4279634805479,23.6127719146552));
#34396=CARTESIAN_POINT('Ctrl Pts',(0.0252430101103464,-6.16845442917999,
23.7517919101677));
#34397=CARTESIAN_POINT('Ctrl Pts',(2.97480085605505,-5.40379747226373,23.8908119056802));
#34398=CARTESIAN_POINT('Ctrl Pts',(5.19848557943377,-3.32057448867644,24.0298319011927));
#34399=CARTESIAN_POINT('Ctrl Pts',(6.15370187660606,-0.427107092290141,
24.1688518967053));
#34400=CARTESIAN_POINT('Ctrl Pts',(5.60736999874005,2.57057755215821,24.3078718922178));
#34401=CARTESIAN_POINT('Ctrl Pts',(3.69279891182468,4.94102251070121,24.4468918877303));
#34402=CARTESIAN_POINT('Ctrl Pts',(0.8771579359188,6.10582191108489,24.5859118832428));
#34403=CARTESIAN_POINT('Ctrl Pts',(-2.152515978909,5.78075619750316,24.7249318787553));
#34404=CARTESIAN_POINT('Ctrl Pts',(-4.65696028322234,4.04514377679203,24.8639518742678));
#34405=CARTESIAN_POINT('Ctrl Pts',(-6.0250722863103,1.32248674820017,25.0029718697804));
#34406=CARTESIAN_POINT('Ctrl Pts',(-5.92302267328619,-1.72286670005763,
25.1419918652929));
#34407=CARTESIAN_POINT('Ctrl Pts',(-4.37571229460911,-4.34782809793997,
25.2810118608054));
#34408=CARTESIAN_POINT('Ctrl Pts',(-1.76069617681569,-5.91188770422582,
25.4200318563179));
#34409=CARTESIAN_POINT('Ctrl Pts',(1.28394265980739,-6.03340355858585,25.5590518518304));
#34410=CARTESIAN_POINT('Ctrl Pts',(4.01529011567363,-4.68272490558683,25.698071847343));
#34411=CARTESIAN_POINT('Ctrl Pts',(5.76687747488004,-2.18942719544423,25.8370918428554));
#34412=CARTESIAN_POINT('Ctrl Pts',(6.11130463658083,0.838106731470015,25.976111838368));
#34413=CARTESIAN_POINT('Ctrl Pts',(4.96452885927568,3.66113649839072,26.1151318338805));
#34414=CARTESIAN_POINT('Ctrl Pts',(2.60637180318128,5.59082223630937,26.254151829393));
#34415=CARTESIAN_POINT('Ctrl Pts',(-0.387758997337801,6.15630653999729,
26.3931718249055));
#34416=CARTESIAN_POINT('Ctrl Pts',(-3.28727377217307,5.21960711176738,26.532191820418));
#34417=CARTESIAN_POINT('Ctrl Pts',(-5.38466975210494,3.00928544927126,26.6712118159306));
#34418=CARTESIAN_POINT('Ctrl Pts',(-6.16816700870177,0.0646761717542413,
26.8102318114431));
#34419=CARTESIAN_POINT('Ctrl Pts',(-5.44658649244489,-2.89571456375564,
26.9492518069556));
#34420=CARTESIAN_POINT('Ctrl Pts',(-3.39599911626685,-5.14952980928789,
27.0882718024682));
#34421=CARTESIAN_POINT('Ctrl Pts',(-0.516763167617664,-6.14682219386762,
27.2272917979806));
#34422=CARTESIAN_POINT('Ctrl Pts',(2.48856676589174,-5.64424509621337,27.3663117934932));
#34423=CARTESIAN_POINT('Ctrl Pts',(4.88666824395851,-3.76443099656735,27.5053317890056));
#34424=CARTESIAN_POINT('Ctrl Pts',(6.09238700169426,-0.966068256396196,
27.6443517845182));
#34425=CARTESIAN_POINT('Ctrl Pts',(5.81151886142015,2.06802218986825,27.7833717800307));
#34426=CARTESIAN_POINT('Ctrl Pts',(4.11259769947784,4.59750012688192,27.9223917755432));
#34427=CARTESIAN_POINT('Ctrl Pts',(1.41017268015921,6.0051544748293,28.0614117710557));
#34428=CARTESIAN_POINT('Ctrl Pts',(-1.63634476626115,5.94750729805012,28.2004317665683));
#34429=CARTESIAN_POINT('Ctrl Pts',(-4.28358214569388,4.43862492845726,28.3394517620808));
#34430=CARTESIAN_POINT('Ctrl Pts',(-5.88559421482269,1.84668567787679,28.4784717575933));
#34431=CARTESIAN_POINT('Ctrl Pts',(-6.05147833536176,-1.19585835744747,
28.6174917531058));
#34432=CARTESIAN_POINT('Ctrl Pts',(-4.74075757107689,-3.94660422473637,
28.7565117486183));
#34433=CARTESIAN_POINT('Ctrl Pts',(-2.27325735567634,-5.73434985410667,
28.8955317441309));
#34434=CARTESIAN_POINT('Ctrl Pts',(0.748934247486209,-6.12287226286585,
29.0345517396433));
#34435=CARTESIAN_POINT('Ctrl Pts',(3.58838042763567,-5.01736914737103,29.1735717351559));
#34436=CARTESIAN_POINT('Ctrl Pts',(5.55223559110895,-2.68759133709957,29.3125917306684));
#34437=CARTESIAN_POINT('Ctrl Pts',(6.16130474343239,0.297978376710887,29.4516117261809));
#34438=CARTESIAN_POINT('Ctrl Pts',(5.26697056571692,3.21083919159792,29.5906317216934));
#34439=CARTESIAN_POINT('Ctrl Pts',(3.08745712525581,5.34023180715378,29.729651717206));
#34440=CARTESIAN_POINT('Ctrl Pts',(0.154581610242292,6.16656888230436,29.8686717127185));
#34441=CARTESIAN_POINT('Ctrl Pts',(-2.81601294599354,5.48821813910729,30.007691708231));
#34442=CARTESIAN_POINT('Ctrl Pts',(-5.09947978874435,3.47070211032544,30.1467117037435));
#34443=CARTESIAN_POINT('Ctrl Pts',(-6.1386363408808,0.606309433249525,30.285731699256));
#34444=CARTESIAN_POINT('Ctrl Pts',(-5.67992081866231,-2.40602717111763,
30.4247516947685));
#34445=CARTESIAN_POINT('Ctrl Pts',(-3.83526315776992,-4.83127558364066,
30.5637716902811));
#34446=CARTESIAN_POINT('Ctrl Pts',(-1.05477329200035,-6.07765748927269,
30.7027916857935));
#34447=CARTESIAN_POINT('Ctrl Pts',(1.98308895602633,-5.84104660543947,30.8418116813061));
#34448=CARTESIAN_POINT('Ctrl Pts',(4.53706302380495,-4.17917771486826,30.9808316768186));
#34449=CARTESIAN_POINT('Ctrl Pts',(5.98396059681105,-1.49755895718416,31.1198516723311));
#34450=CARTESIAN_POINT('Ctrl Pts',(5.97072810602557,1.5494751170464,31.2588716678436));
#34451=CARTESIAN_POINT('Ctrl Pts',(4.50059437578687,4.21842595277733,31.3978916633562));
#34452=CARTESIAN_POINT('Ctrl Pts',(1.93228276708425,5.8580500648645,31.5369116588686));
#34453=CARTESIAN_POINT('Ctrl Pts',(-1.10751994091965,6.06826720200214,31.6759316543812));
#34454=CARTESIAN_POINT('Ctrl Pts',(-3.87707969932138,4.79778284831023,31.8149516498937));
#34455=CARTESIAN_POINT('Ctrl Pts',(-5.70060371147976,2.35660445961832,31.9539716454062));
#34456=CARTESIAN_POINT('Ctrl Pts',(-6.13313880814805,-0.659602618565238,
32.0929916409187));
#34457=CARTESIAN_POINT('Ctrl Pts',(-5.06914326857582,-3.51486184324249,
32.2320116364313));
#34458=CARTESIAN_POINT('Ctrl Pts',(-2.76823977074293,-5.51246912246289,
32.3710316319438));
#34459=CARTESIAN_POINT('Ctrl Pts',(0.208134437107512,-6.16499369914678,
32.5100516274563));
#34460=CARTESIAN_POINT('Ctrl Pts',(3.13372232308735,-5.31321481367108,32.6490716229688));
#34461=CARTESIAN_POINT('Ctrl Pts',(5.29465908854464,-3.16497273140251,32.7880916184813));
#34462=CARTESIAN_POINT('Ctrl Pts',(6.16366038958201,-0.24445420087921,32.9271116139939));
#34463=CARTESIAN_POINT('Ctrl Pts',(5.5286835657256,2.73571293898048,33.0661316095063));
#34464=CARTESIAN_POINT('Ctrl Pts',(3.54466759682403,5.04834615319267,33.2051516050189));
#34465=CARTESIAN_POINT('Ctrl Pts',(0.695726861033372,6.12914605710014,33.3441716005314));
#34466=CARTESIAN_POINT('Ctrl Pts',(-2.32297630710416,5.71438958516676,33.4831915960439));
#34467=CARTESIAN_POINT('Ctrl Pts',(-4.7748563004224,3.90528034393773,33.6222115915565));
#34468=CARTESIAN_POINT('Ctrl Pts',(-6.06163650377092,1.14325419333651,33.761231587069));
#34469=CARTESIAN_POINT('Ctrl Pts',(-5.86933315505708,-1.89773432528826,
33.9002515825815));
#34470=CARTESIAN_POINT('Ctrl Pts',(-4.24486967502917,-4.47566181658616,
34.039271578094));
#34471=CARTESIAN_POINT('Ctrl Pts',(-1.5846270101099,-5.96149515585307,34.1782915736065));
#34472=CARTESIAN_POINT('Ctrl Pts',(1.46227621179747,-5.99268016290215,34.317311569119));
#34473=CARTESIAN_POINT('Ctrl Pts',(4.15237336456894,-4.56160746838747,34.4563315646316));
#34474=CARTESIAN_POINT('Ctrl Pts',(5.82926110735099,-2.01746925546705,34.595351560144));
#34475=CARTESIAN_POINT('Ctrl Pts',(6.08376659095337,1.01894618171386,34.7343715556566));
#34476=CARTESIAN_POINT('Ctrl Pts',(4.85378861968884,3.80673131305699,34.8733915511691));
#34477=CARTESIAN_POINT('Ctrl Pts',(2.43945079641032,5.66564621789277,35.0124115466816));
#34478=CARTESIAN_POINT('Ctrl Pts',(-0.570130827249739,6.14210209083577,
35.1514315421941));
#34479=CARTESIAN_POINT('Ctrl Pts',(-3.44059636755775,5.1198402211376,35.2904515377066));
#34480=CARTESIAN_POINT('Ctrl Pts',(-5.47153128055505,2.84829996670597,35.4294715332192));
#34481=CARTESIAN_POINT('Ctrl Pts',(-6.16737262325507,-0.118246269934136,
35.5684915287317));
#34482=CARTESIAN_POINT('Ctrl Pts',(-5.3583300289488,-3.05593955360628,35.7075115242442));
#34483=CARTESIAN_POINT('Ctrl Pts',(-3.24181579601662,-5.24796128026178,
35.8465315197567));
#34484=CARTESIAN_POINT('Ctrl Pts',(-0.334274846170438,-6.15944214857542,
35.9855515152693));
#34485=CARTESIAN_POINT('Ctrl Pts',(2.65483160608277,-5.56797417359075,36.1245715107817));
#34486=CARTESIAN_POINT('Ctrl Pts',(4.9961397682852,-3.61787985845148,36.2635915062943));
#34487=CARTESIAN_POINT('Ctrl Pts',(6.11835335916549,-0.784996450194473,
36.4026115018067));
#34488=CARTESIAN_POINT('Ctrl Pts',(5.74764407127912,2.23943182176189,36.5416314973193));
#34489=CARTESIAN_POINT('Ctrl Pts',(3.97446767675429,4.71742238313097,36.6806514928318));
#34490=CARTESIAN_POINT('Ctrl Pts',(1.23149215863742,6.04432744957155,36.8196714883444));
#34491=CARTESIAN_POINT('Ctrl Pts',(-1.81197643510369,5.89637249951686,36.9586914838568));
#34492=CARTESIAN_POINT('Ctrl Pts',(-4.41330955268765,4.30965962073406,37.0977114793694));
#34493=CARTESIAN_POINT('Ctrl Pts',(-5.93776292575391,1.67135833739262,37.2367314748819));
#34494=CARTESIAN_POINT('Ctrl Pts',(-6.01335880397298,-1.37476657986381,
37.3757514703944));
#34495=CARTESIAN_POINT('Ctrl Pts',(-4.62165124126933,-4.08543841692705,
37.5147714659069));
#34496=CARTESIAN_POINT('Ctrl Pts',(-2.10222704130489,-5.7992334597976,37.6537914614195));
#34497=CARTESIAN_POINT('Ctrl Pts',(0.930155901329192,-6.0979732086696,37.7928114569319));
#34498=CARTESIAN_POINT('Ctrl Pts',(3.73557401463809,-4.90876298425484,37.9318314524445));
#34499=CARTESIAN_POINT('Ctrl Pts',(5.62948480164565,-2.52177876160262,38.070851447957));
#34500=CARTESIAN_POINT('Ctrl Pts',(6.14976020627442,0.480537885866896,38.2098714434695));
#34501=CARTESIAN_POINT('Ctrl Pts',(5.16944923219678,3.36559978163918,38.348891438982));
#34502=CARTESIAN_POINT('Ctrl Pts',(2.92775491258089,5.42943076448057,38.4879114344945));
#34503=CARTESIAN_POINT('Ctrl Pts',(-0.0283329759951614,6.16844101024732,
38.6269314300071));
#34504=CARTESIAN_POINT('Ctrl Pts',(-2.97750741162013,5.40230662478325,38.7659514255196));
#34505=CARTESIAN_POINT('Ctrl Pts',(-5.20014830536553,3.31796999031538,38.9049714210321));
#34506=CARTESIAN_POINT('Ctrl Pts',(-6.15391505564063,0.424024459659371,
39.0439914165446));
#34507=CARTESIAN_POINT('Ctrl Pts',(-5.60608161363686,-2.57338613419603,
39.1830114120571));
#34508=CARTESIAN_POINT('Ctrl Pts',(-3.69032333795313,-4.94287172762838,
39.3220314075697));
#34509=CARTESIAN_POINT('Ctrl Pts',(-0.874099231373308,-6.10626054047339,
39.4610514030821));
#34510=CARTESIAN_POINT('Ctrl Pts',(2.15541146789322,-5.77967721058055,39.6000713985947));
#34511=CARTESIAN_POINT('Ctrl Pts',(4.65898603619837,-4.04281045424319,39.7390913941072));
#34512=CARTESIAN_POINT('Ctrl Pts',(6.02573400476567,-1.3194684377584,39.8781113896197));
#34513=CARTESIAN_POINT('Ctrl Pts',(5.92215889308766,1.72583350861328,40.0171313851323));
#34514=CARTESIAN_POINT('Ctrl Pts',(4.37353378443007,4.35001948166654,40.1561513806447));
#34515=CARTESIAN_POINT('Ctrl Pts',(1.75773450904124,5.91276894949864,40.2951713761573));
#34516=CARTESIAN_POINT('Ctrl Pts',(-1.28696481662245,6.03275963512601,40.4341913716697));
#34517=CARTESIAN_POINT('Ctrl Pts',(-4.01763533320709,4.68071293541866,40.5732113671824));
#34518=CARTESIAN_POINT('Ctrl Pts',(-5.76797350293554,2.18653811397452,40.7122313626948));
#34519=CARTESIAN_POINT('Ctrl Pts',(-6.11088403631264,-0.841167967274665,
40.8512513582074));
#34520=CARTESIAN_POINT('Ctrl Pts',(-4.96269426021928,-3.66362292464934,
40.9902713537199));
#34521=CARTESIAN_POINT('Ctrl Pts',(-2.6035708608976,-5.5921271468659,41.1292913492324));
#34522=CARTESIAN_POINT('Ctrl Pts',(0.390842832486891,-6.15611152715116,
41.2683113447449));
#34523=CARTESIAN_POINT('Ctrl Pts',(3.28988802190165,-5.21795976007649,41.4073313402574));
#34524=CARTESIAN_POINT('Ctrl Pts',(5.38617652039734,-3.00658772457253,41.54635133577));
#34525=CARTESIAN_POINT('Ctrl Pts',(6.16819863309635,-0.061586338565383,
41.6853713312824));
#34526=CARTESIAN_POINT('Ctrl Pts',(5.44513525635857,2.89844256358317,41.8243913267949));
#34527=CARTESIAN_POINT('Ctrl Pts',(3.39341913189756,5.15123032388393,41.9634113223075));
#34528=CARTESIAN_POINT('Ctrl Pts',(0.513683969983391,6.14708028525834,42.10243131782));
#34529=CARTESIAN_POINT('Ctrl Pts',(-2.49139383009257,5.64299778821561,42.2414513133325));
#34530=CARTESIAN_POINT('Ctrl Pts',(-4.8885533504256,3.76198264143688,42.3804713088451));
#34531=CARTESIAN_POINT('Ctrl Pts',(-6.09287017068981,0.963016270655894,
42.5194913043575));
#34532=CARTESIAN_POINT('Ctrl Pts',(-5.81048219618248,-2.07093309942065,
42.6585112998701));
#34533=CARTESIAN_POINT('Ctrl Pts',(-4.1102941538918,-4.59955967706829,42.7975312953826));
#34534=CARTESIAN_POINT('Ctrl Pts',(-1.40716433616188,-6.00586012037109,
42.9365512908951));
#34535=CARTESIAN_POINT('Ctrl Pts',(1.63932385077592,-5.94668685628449,43.0755712864076));
#34536=CARTESIAN_POINT('Ctrl Pts',(4.28580505235956,-4.43647859316362,43.2145912819201));
#34537=CARTESIAN_POINT('Ctrl Pts',(5.88651853818737,-1.84373717053327,43.3536112774327));
#34538=CARTESIAN_POINT('Ctrl Pts',(6.05087853377761,1.19888957952724,43.4926312729452));
#34539=CARTESIAN_POINT('Ctrl Pts',(4.73878000050854,3.94897852123938,43.6316512684577));
#34540=CARTESIAN_POINT('Ctrl Pts',(2.27038455777718,5.73548787935574,43.7706712639702));
#34541=CARTESIAN_POINT('Ctrl Pts',(-0.75200128905964,6.12249633039352,43.9096912594827));
#34542=CARTESIAN_POINT('Ctrl Pts',(-3.59089333235252,5.0155709874446,44.0487112549953));
#34543=CARTESIAN_POINT('Ctrl Pts',(-5.55358119187607,2.68480971386613,44.1877312505077));
#34544=CARTESIAN_POINT('Ctrl Pts',(-6.16115470384076,-0.301064726878676,
44.3267512460203));
#34545=CARTESIAN_POINT('Ctrl Pts',(-5.26536149652208,-3.21347717673118,
44.4657712415327));
#34546=CARTESIAN_POINT('Ctrl Pts',(-3.08478165108631,-5.34177773962483,
44.6047912370454));
#34547=CARTESIAN_POINT('Ctrl Pts',(-0.151492566324147,-6.16664554330616,
44.7438112325578));
#34548=CARTESIAN_POINT('Ctrl Pts',(2.81876181039641,-5.48680682279593,44.8828312280704));
#34549=CARTESIAN_POINT('Ctrl Pts',(5.10121773065381,-3.46814718818215,45.0218512235828));
#34550=CARTESIAN_POINT('Ctrl Pts',(6.13893928978386,-0.603234324926554,
45.1608712190954));
#34551=CARTESIAN_POINT('Ctrl Pts',(5.67871485281819,2.40887211674427,45.2998912146079));
#34552=CARTESIAN_POINT('Ctrl Pts',(3.83284254164173,4.83319617907093,45.4389112101205));
#34553=CARTESIAN_POINT('Ctrl Pts',(1.05172867360261,6.07818509520536,45.5779312056329));
#34554=CARTESIAN_POINT('Ctrl Pts',(-1.98601466760215,5.84005248217085,45.7169512011455));
#34555=CARTESIAN_POINT('Ctrl Pts',(-4.53915593353827,4.176904435742,45.8559711966579));
#34556=CARTESIAN_POINT('Ctrl Pts',(-5.98471001952974,1.49456121888098,45.9949911921705));
#34557=CARTESIAN_POINT('Ctrl Pts',(-5.96995117696109,-1.55246584446183,
46.134011187683));
#34558=CARTESIAN_POINT('Ctrl Pts',(-4.49848067160452,-4.22067991005896,
46.2730311831955));
#34559=CARTESIAN_POINT('Ctrl Pts',(-1.92934804644225,-5.85901726984058,
46.412051178708));
#34560=CARTESIAN_POINT('Ctrl Pts',(1.11055958361069,-6.06771164987773,46.5510711742206));
#34561=CARTESIAN_POINT('Ctrl Pts',(3.879482571308,-4.79584009731413,46.6900911697331));
#34562=CARTESIAN_POINT('Ctrl Pts',(5.7017834900662,-2.35374855623714,46.8291111652456));
#34563=CARTESIAN_POINT('Ctrl Pts',(6.1328076273202,0.662674815135318,46.9681311607581));
#34564=CARTESIAN_POINT('Ctrl Pts',(5.06738192214114,3.51740069056444,47.1071511562706));
#34565=CARTESIAN_POINT('Ctrl Pts',(2.76547807274594,5.51385513116234,47.2461711517831));
#34566=CARTESIAN_POINT('Ctrl Pts',(-0.211222675940933,6.16488865755735,
47.3851911472957));
#34567=CARTESIAN_POINT('Ctrl Pts',(-3.13638342552245,5.31164438281825,47.5242111428081));
#34568=CARTESIAN_POINT('Ctrl Pts',(-5.29624396900741,3.16232004910531,47.6632311383208));
#34569=CARTESIAN_POINT('Ctrl Pts',(-6.16378185167675,0.241366655694626,
47.8022511338331));
#34570=CARTESIAN_POINT('Ctrl Pts',(-5.5273128969791,-2.73848218739485,47.9412711293458));
#34571=CARTESIAN_POINT('Ctrl Pts',(-3.5421374446362,-5.05012095098419,48.0802911248582));
#34572=CARTESIAN_POINT('Ctrl Pts',(-0.692658125609615,-6.12949419366117,
48.2193111203708));
#34573=CARTESIAN_POINT('Ctrl Pts',(2.3258417114082,-5.71322444769426,48.3583311158833));
#34574=CARTESIAN_POINT('Ctrl Pts',(4.7768057663147,-3.90288948418925,48.4973511113958));
#34575=CARTESIAN_POINT('Ctrl Pts',(6.06222055645793,-1.14021465560235,48.6363711069083));
#34576=CARTESIAN_POINT('Ctrl Pts',(5.86835812258636,1.900668491112,48.7753911024208));
#34577=CARTESIAN_POINT('Ctrl Pts',(4.24267335475951,4.47779881807613,48.9144110979333));
#34578=CARTESIAN_POINT('Ctrl Pts',(1.58155006867202,5.96226637531529,49.0534310934459));
#34579=CARTESIAN_POINT('Ctrl Pts',(-1.46509874999526,5.99198956129919,49.1924510889584));
#34580=CARTESIAN_POINT('Ctrl Pts',(-4.15503569018137,4.55944298225233,49.3314710844709));
#34581=CARTESIAN_POINT('Ctrl Pts',(-5.27116507023042,2.86295887331669,49.4241510814793));
#34582=CARTESIAN_POINT('Ctrl Pts',(-5.5926845116257,1.9324550623107,49.4704910799834));
#34583=CARTESIAN_POINT('Ctrl Pts',(3.24353530767675,-4.54538816146824,-0.3843885632452));
#34584=CARTESIAN_POINT('Ctrl Pts',(3.99988254819268,-4.00566902158514,-0.338043015427469));
#34585=CARTESIAN_POINT('Ctrl Pts',(5.23710322327956,-2.54200492850901,-0.245357469105566));
#34586=CARTESIAN_POINT('Ctrl Pts',(5.81469291328025,0.275550394094319,-0.106331924279489));
#34587=CARTESIAN_POINT('Ctrl Pts',(4.97347786147395,3.02500010026102,0.0326880712330279));
#34588=CARTESIAN_POINT('Ctrl Pts',(2.91867860759893,5.03670007919148,0.171708066745545));
#34589=CARTESIAN_POINT('Ctrl Pts',(0.151709961649961,5.81921915220708,0.310728062258062));
#34590=CARTESIAN_POINT('Ctrl Pts',(-2.65228184789175,5.18190313468451,0.449748057770581));
#34591=CARTESIAN_POINT('Ctrl Pts',(-4.80909505824059,3.28011531771315,0.588768053283096));
#34592=CARTESIAN_POINT('Ctrl Pts',(-5.79245523628694,0.577980837100627,
0.727788048795615));
#34593=CARTESIAN_POINT('Ctrl Pts',(-5.36241340853576,-2.26519820802741,
0.866808044308132));
#34594=CARTESIAN_POINT('Ctrl Pts',(-3.62390389962763,-4.55564568490122,
1.00582803982065));
#34595=CARTESIAN_POINT('Ctrl Pts',(-1.00113521754353,-5.73448578002076,
1.14484803533317));
#34596=CARTESIAN_POINT('Ctrl Pts',(1.86591767799704,-5.51406773646999,1.28386803084568));
#34597=CARTESIAN_POINT('Ctrl Pts',(4.27767308501967,-3.94817781406936,1.42288802635821));
#34598=CARTESIAN_POINT('Ctrl Pts',(5.645645012807,-1.41890322681348,1.56190802187072));
#34599=CARTESIAN_POINT('Ctrl Pts',(5.63603836045111,1.45659386915713,1.70092801738324));
#34600=CARTESIAN_POINT('Ctrl Pts',(4.25119720352968,3.97667154972591,1.83994801289576));
#34601=CARTESIAN_POINT('Ctrl Pts',(1.82903290165202,5.52641228379608,1.97896800840828));
#34602=CARTESIAN_POINT('Ctrl Pts',(-1.03942878029484,5.72766811386036,2.11798800392079));
#34603=CARTESIAN_POINT('Ctrl Pts',(-3.65426225203626,4.53133110047943,2.25700799943331));
#34604=CARTESIAN_POINT('Ctrl Pts',(-5.37742906147621,2.22931623176881,2.39602799494583));
#34605=CARTESIAN_POINT('Ctrl Pts',(-5.78846392873392,-0.616668073994028,
2.53504799045834));
#34606=CARTESIAN_POINT('Ctrl Pts',(-4.78707134629015,-3.31218086633208,
2.67406798597086));
#34607=CARTESIAN_POINT('Ctrl Pts',(-2.61759841346924,-5.19949735210785,
2.81308798148338));
#34608=CARTESIAN_POINT('Ctrl Pts',(0.190587638603466,-5.81809853118683,
2.95210797699589));
#34609=CARTESIAN_POINT('Ctrl Pts',(2.95226891573283,-5.01704120144163,3.09112797250841));
#34610=CARTESIAN_POINT('Ctrl Pts',(4.99357502819268,-2.9917891979699,3.23014796802093));
#34611=CARTESIAN_POINT('Ctrl Pts',(5.8164123846374,-0.236518792580586,3.36916796353344));
#34612=CARTESIAN_POINT('Ctrl Pts',(5.22000266402811,2.57646392463758,3.50818795904597));
#34613=CARTESIAN_POINT('Ctrl Pts',(3.34987419151473,4.76077063807932,3.64720795455848));
#34614=CARTESIAN_POINT('Ctrl Pts',(0.662351964844652,5.78341456598765,3.786227950071));
#34615=CARTESIAN_POINT('Ctrl Pts',(-2.18678897589165,5.3948631254471,3.92524794558351));
#34616=CARTESIAN_POINT('Ctrl Pts',(-4.50233744468419,3.68992570407515,4.06426794109604));
#34617=CARTESIAN_POINT('Ctrl Pts',(-5.71928271347876,1.08461947737435,4.20328793660855));
#34618=CARTESIAN_POINT('Ctrl Pts',(-5.54068125395366,-1.78534181866763,
4.34230793212107));
#34619=CARTESIAN_POINT('Ctrl Pts',(-4.01011312588206,-4.2196666793748,4.48132792763359));
#34620=CARTESIAN_POINT('Ctrl Pts',(-1.50104812444773,-5.62436207009194,
4.6203479231461));
#34621=CARTESIAN_POINT('Ctrl Pts',(1.37428357581349,-5.65667206232133,4.75936791865862));
#34622=CARTESIAN_POINT('Ctrl Pts',(3.91428005239532,-4.3087127821215,4.89838791417113));
#34623=CARTESIAN_POINT('Ctrl Pts',(5.49916362505065,-1.90939613289568,5.03740790968366));
#34624=CARTESIAN_POINT('Ctrl Pts',(5.74221113365761,0.95582710983514,5.17642790519617));
#34625=CARTESIAN_POINT('Ctrl Pts',(4.58411721206192,3.58782156098583,5.31544790070869));
#34626=CARTESIAN_POINT('Ctrl Pts',(2.30746523030072,5.34436136300218,5.45446789622121));
#34627=CARTESIAN_POINT('Ctrl Pts',(-0.532225110321242,5.79683798284382,
5.59348789173372));
#34628=CARTESIAN_POINT('Ctrl Pts',(-3.24204863920333,4.83484382254867,5.73250788724625));
#34629=CARTESIAN_POINT('Ctrl Pts',(-5.16078863573428,2.69311247902369,5.87152788275876));
#34630=CARTESIAN_POINT('Ctrl Pts',(-5.8202585354793,-0.105757966969696,
6.01054787827129));
#34631=CARTESIAN_POINT('Ctrl Pts',(-5.05954286929301,-2.87882269707314,
6.14956787378379));
#34632=CARTESIAN_POINT('Ctrl Pts',(-3.06426181234631,-4.94943367596671,
6.28858786929631));
#34633=CARTESIAN_POINT('Ctrl Pts',(-0.321278506504521,-5.81234671098133,
6.42760786480884));
#34634=CARTESIAN_POINT('Ctrl Pts',(2.50009910000284,-5.25700472299219,6.56662786032134));
#34635=CARTESIAN_POINT('Ctrl Pts',(4.71143427736757,-3.41891521062502,6.70564785583387));
#34636=CARTESIAN_POINT('Ctrl Pts',(5.77314510131853,-0.746585431494017,
6.84466785134638));
#34637=CARTESIAN_POINT('Ctrl Pts',(5.42616638116412,2.10791664240345,6.98368784685891));
#34638=CARTESIAN_POINT('Ctrl Pts',(3.7551634572917,4.44807166943365,7.12270784237141));
#34639=CARTESIAN_POINT('Ctrl Pts',(1.16787324012308,5.70286474172425,7.26172783788393));
#34640=CARTESIAN_POINT('Ctrl Pts',(-1.70438657218461,5.56611719064143,7.40074783339646));
#34641=CARTESIAN_POINT('Ctrl Pts',(-4.16076362020811,4.07119641679812,7.53976782890896));
#34642=CARTESIAN_POINT('Ctrl Pts',(-5.6018839746241,1.58287400074895,7.67878782442149));
#34643=CARTESIAN_POINT('Ctrl Pts',(-5.67610374991866,-1.29168122520867,
7.81780781993401));
#34644=CARTESIAN_POINT('Ctrl Pts',(-4.36531277917439,-3.85105680396615,
7.95682781544651));
#34645=CARTESIAN_POINT('Ctrl Pts',(-1.98935362698809,-5.47074641289345,
8.09584781095906));
#34646=CARTESIAN_POINT('Ctrl Pts',(0.872022330888087,-5.75553396496188,
8.23486780647155));
#34647=CARTESIAN_POINT('Ctrl Pts',(3.52061847495569,-4.63592921874331,8.37388780198407));
#34648=CARTESIAN_POINT('Ctrl Pts',(5.31015801340958,-2.38512390454236,8.51290779749659));
#34649=CARTESIAN_POINT('Ctrl Pts',(5.80398023664667,0.447669051881049,8.6519277930091));
#34650=CARTESIAN_POINT('Ctrl Pts',(4.88158891768631,3.17122749201622,8.79094778852162));
#34651=CARTESIAN_POINT('Ctrl Pts',(2.76805427108038,5.12098327665214,8.92996778403414));
#34652=CARTESIAN_POINT('Ctrl Pts',(-0.0209058222714769,5.82118176266575,
9.06898777954667));
#34653=CARTESIAN_POINT('Ctrl Pts',(-2.80476474239316,5.10096940857573,9.20800777505916));
#34654=CARTESIAN_POINT('Ctrl Pts',(-4.90424059281125,3.13608328575942,9.34702777057171));
#34655=CARTESIAN_POINT('Ctrl Pts',(-5.80704594151402,0.405969950295367,
9.4860477660842));
#34656=CARTESIAN_POINT('Ctrl Pts',(-5.29288969365446,-2.42320301629962,
9.62506776159673));
#34657=CARTESIAN_POINT('Ctrl Pts',(-3.48722972664344,-4.66109675945605,
9.76408775710924));
#34658=CARTESIAN_POINT('Ctrl Pts',(-0.83066025231826,-5.76164887099307,
9.90310775262178));
#34659=CARTESIAN_POINT('Ctrl Pts',(2.02859638673404,-5.45631660253753,10.0421277481342));
#34660=CARTESIAN_POINT('Ctrl Pts',(4.39286070027743,-3.81960325627614,10.1811477436468));
#34661=CARTESIAN_POINT('Ctrl Pts',(5.68523493855165,-1.25087883540689,10.3201677391593));
#34662=CARTESIAN_POINT('Ctrl Pts',(5.59037035411014,1.62306915172573,10.4591877346718));
#34663=CARTESIAN_POINT('Ctrl Pts',(4.13141459799293,4.10097641871886,10.5982077301843));
#34664=CARTESIAN_POINT('Ctrl Pts',(1.66436352391329,5.57821550566704,10.7372277256968));
#34665=CARTESIAN_POINT('Ctrl Pts',(-1.20880439853578,5.69432929268037,10.8762477212093));
#34666=CARTESIAN_POINT('Ctrl Pts',(-3.78701522442807,4.42098516818901,11.0152677167219));
#34667=CARTESIAN_POINT('Ctrl Pts',(-5.44116669335026,2.06888839297171,11.1542877122344));
#34668=CARTESIAN_POINT('Ctrl Pts',(-5.76763377289058,-0.788032251376195,
11.2933077077469));
#34669=CARTESIAN_POINT('Ctrl Pts',(-4.68675611269034,-3.45266727437747,
11.4323277032594));
#34670=CARTESIAN_POINT('Ctrl Pts',(-2.46227575138857,-5.27482628069598,
11.5713476987719));
#34671=CARTESIAN_POINT('Ctrl Pts',(0.363017865913463,-5.8098891724735,11.7103676942845));
#34672=CARTESIAN_POINT('Ctrl Pts',(3.0997324741899,-4.92729669858126,11.849387689797));
#34673=CARTESIAN_POINT('Ctrl Pts',(5.08008973317371,-2.8424078648745,11.9884076853095));
#34674=CARTESIAN_POINT('Ctrl Pts',(5.82086801663436,-0.063950764813749,
12.127427680822));
#34675=CARTESIAN_POINT('Ctrl Pts',(5.14131201631318,2.73011078865145,12.2664476763345));
#34676=CARTESIAN_POINT('Ctrl Pts',(3.20723835650867,4.85800538204074,12.405467671847));
#34677=CARTESIAN_POINT('Ctrl Pts',(0.490575127418006,5.8005112026231,12.5444876673595));
#34678=CARTESIAN_POINT('Ctrl Pts',(-2.34579201357227,5.32764995063094,12.6835076628721));
#34679=CARTESIAN_POINT('Ctrl Pts',(-4.60976878082841,3.55480322306271,12.8225276583846));
#34680=CARTESIAN_POINT('Ctrl Pts',(-5.74892831790386,0.914558561821075,
12.9615476538971));
#34681=CARTESIAN_POINT('Ctrl Pts',(-5.48530738279048,-1.94884506405755,
13.1005676494096));
#34682=CARTESIAN_POINT('Ctrl Pts',(-3.88323140787979,-4.33671626928177,
13.2395876449221));
#34683=CARTESIAN_POINT('Ctrl Pts',(-1.33361862493489,-5.66639705020959,
13.3786076404346));
#34684=CARTESIAN_POINT('Ctrl Pts',(1.5414068368531,-5.61343559067883,13.5176276359472));
#34685=CARTESIAN_POINT('Ctrl Pts',(4.04031777940071,-4.19075487339164,13.6566476314597));
#34686=CARTESIAN_POINT('Ctrl Pts',(5.55336169265697,-1.74549937780777,13.7956676269722));
#34687=CARTESIAN_POINT('Ctrl Pts',(5.711344817766,1.12567070672322,13.9346876224847));
#34688=CARTESIAN_POINT('Ctrl Pts',(4.47571811904957,3.72216892230976,14.0737076179972));
#34689=CARTESIAN_POINT('Ctrl Pts',(2.14798353009009,5.41043075196965,14.2127276135098));
#34690=CARTESIAN_POINT('Ctrl Pts',(-0.703874718788708,5.7785079862926,14.3517476090223));
#34691=CARTESIAN_POINT('Ctrl Pts',(-3.38398239855548,4.73658709343171,14.4907676045348));
#34692=CARTESIAN_POINT('Ctrl Pts',(-5.23837367268526,2.53890437644177,14.6297876000473));
#34693=CARTESIAN_POINT('Ctrl Pts',(-5.81456353470378,-0.278289540389685,
14.7688075955598));
#34694=CARTESIAN_POINT('Ctrl Pts',(-4.97195745254918,-3.02757877807298,
14.9078275910723));
#34695=CARTESIAN_POINT('Ctrl Pts',(-2.91615746062379,-5.03811669498091,
15.0468475865849));
#34696=CARTESIAN_POINT('Ctrl Pts',(-0.148793762668019,-5.81931736405468,
15.1858675820974));
#34697=CARTESIAN_POINT('Ctrl Pts',(2.65487669945529,-5.18056211989457,15.3248875776099));
#34698=CARTESIAN_POINT('Ctrl Pts',(4.81073786841581,-3.27771190448267,15.4639075731224));
#34699=CARTESIAN_POINT('Ctrl Pts',(5.79274388290926,-0.575076059677866,
15.6029275686349));
#34700=CARTESIAN_POINT('Ctrl Pts',(5.36127810753363,2.26788254128779,15.7419475641475));
#34701=CARTESIAN_POINT('Ctrl Pts',(3.62162134083876,4.55746124843408,15.88096755966));
#34702=CARTESIAN_POINT('Ctrl Pts',(0.998262532013878,5.73498614510745,16.0199875551725));
#34703=CARTESIAN_POINT('Ctrl Pts',(-1.86867962114769,5.51313256152113,16.159007550685));
#34704=CARTESIAN_POINT('Ctrl Pts',(-4.27965030686907,3.94603439142549,16.2980275461975));
#34705=CARTESIAN_POINT('Ctrl Pts',(-5.64635507965907,1.41607502689844,16.43704754171));
#34706=CARTESIAN_POINT('Ctrl Pts',(-5.63530799909529,-1.45941698041719,
16.5760675372226));
#34707=CARTESIAN_POINT('Ctrl Pts',(-4.24920463347018,-3.97880059192374,
16.7150875327351));
#34708=CARTESIAN_POINT('Ctrl Pts',(-1.82626432145237,-5.52732781691002,
16.8541075282476));
#34709=CARTESIAN_POINT('Ctrl Pts',(1.04229781528194,-5.72714670945801,16.9931275237601));
#34710=CARTESIAN_POINT('Ctrl Pts',(3.65653167713951,-4.52950000126642,17.1321475192726));
#34711=CARTESIAN_POINT('Ctrl Pts',(5.37854511999187,-2.22662223100573,17.2711675147851));
#34712=CARTESIAN_POINT('Ctrl Pts',(5.78815429444966,0.619567616197914,17.4101875102977));
#34713=CARTESIAN_POINT('Ctrl Pts',(4.78541157212288,3.31457844269668,17.5492075058102));
#34714=CARTESIAN_POINT('Ctrl Pts',(2.61499349648643,5.20080793538185,17.6882275013227));
#34715=CARTESIAN_POINT('Ctrl Pts',(-0.193502079672655,5.81800233005794,
17.8272474968352));
#34716=CARTESIAN_POINT('Ctrl Pts',(-2.95478173597983,5.01556168939405,17.9662674923477));
#34717=CARTESIAN_POINT('Ctrl Pts',(-4.99507308114313,2.98928738689283,18.1052874878603));
#34718=CARTESIAN_POINT('Ctrl Pts',(-5.81653013443292,0.233605142561025,
18.2443074833728));
#34719=CARTESIAN_POINT('Ctrl Pts',(-5.21871137886108,-2.57907846168803,
18.3833274788853));
#34720=CARTESIAN_POINT('Ctrl Pts',(-3.34748895439027,-4.76244809605651,
18.5223474743978));
#34721=CARTESIAN_POINT('Ctrl Pts',(-0.659454791032004,-5.78374563289069,
18.6613674699103));
#34722=CARTESIAN_POINT('Ctrl Pts',(2.18949115483542,-5.39376701854044,18.8003874654228));
#34723=CARTESIAN_POINT('Ctrl Pts',(4.50418527737289,-3.687669881442,18.9394074609354));
#34724=CARTESIAN_POINT('Ctrl Pts',(5.71982531524873,-1.08175437620428,19.0784274564479));
#34725=CARTESIAN_POINT('Ctrl Pts',(5.53978622601238,1.78811709277684,19.2174474519604));
#34726=CARTESIAN_POINT('Ctrl Pts',(4.00799886158025,4.22167493928282,19.3564674474729));
#34727=CARTESIAN_POINT('Ctrl Pts',(1.49823051970747,5.62511328572272,19.4954874429854));
#34728=CARTESIAN_POINT('Ctrl Pts',(-1.37711700486929,5.6559829315776,19.6345074384979));
#34729=CARTESIAN_POINT('Ctrl Pts',(-3.91643792839529,4.30675145793487,19.7735274340104));
#34730=CARTESIAN_POINT('Ctrl Pts',(-5.50011941049998,1.90664119268375,19.912547429523));
#34731=CARTESIAN_POINT('Ctrl Pts',(-5.74173160993018,-0.958703440551738,
20.0515674250355));
#34732=CARTESIAN_POINT('Ctrl Pts',(-4.58231938644739,-3.59011743651731,
20.190587420548));
#34733=CARTESIAN_POINT('Ctrl Pts',(-2.30478778537174,-5.34551657296078,
20.3296074160606));
#34734=CARTESIAN_POINT('Ctrl Pts',(0.535128858458774,-5.79657064756757,
20.468627411573));
#34735=CARTESIAN_POINT('Ctrl Pts',(3.24447015480882,-4.83321917379629,20.6076474070856));
#34736=CARTESIAN_POINT('Ctrl Pts',(5.16213705132485,-2.69052694294937,20.7466674025981));
#34737=CARTESIAN_POINT('Ctrl Pts',(5.82020482780844,0.108673500691432,20.8856873981106));
#34738=CARTESIAN_POINT('Ctrl Pts',(5.05810014342445,2.88135681693307,21.0247073936231));
#34739=CARTESIAN_POINT('Ctrl Pts',(3.06178210392277,4.95096803822197,21.1637273891357));
#34740=CARTESIAN_POINT('Ctrl Pts',(0.318366882481225,5.81250692004203,21.3027473846481));
#34741=CARTESIAN_POINT('Ctrl Pts',(-2.50273218211169,5.25575168667811,21.4417673801607));
#34742=CARTESIAN_POINT('Ctrl Pts',(-4.71314632630798,3.41655467894293,21.5807873756732));
#34743=CARTESIAN_POINT('Ctrl Pts',(-5.7735183646524,0.743693391404382,21.7198073711857));
#34744=CARTESIAN_POINT('Ctrl Pts',(-5.4251097799135,-2.11063451200913,21.8588273666982));
#34745=CARTESIAN_POINT('Ctrl Pts',(-3.7529348098741,-4.44995218853332,21.9978473622107));
#34746=CARTESIAN_POINT('Ctrl Pts',(-1.16501635277576,-5.70344904993131,
22.1368673577233));
#34747=CARTESIAN_POINT('Ctrl Pts',(1.70717459809594,-5.56526271248836,22.2758873532358));
#34748=CARTESIAN_POINT('Ctrl Pts',(4.16280248601068,-4.06911165119126,22.4149073487483));
#34749=CARTESIAN_POINT('Ctrl Pts',(5.60267618217995,-1.5800676457135,22.5539273442608));
#34750=CARTESIAN_POINT('Ctrl Pts',(5.67545599480169,1.29452439855982,22.6929473397733));
#34751=CARTESIAN_POINT('Ctrl Pts',(4.36338311836127,3.85324304058244,22.8319673352858));
#34752=CARTESIAN_POINT('Ctrl Pts',(1.9866129118022,5.47174225508275,22.9709873307984));
#34753=CARTESIAN_POINT('Ctrl Pts',(-0.874905345936364,5.75509641996111,
23.1100073263109));
#34754=CARTESIAN_POINT('Ctrl Pts',(-3.52294031315086,4.63416505072638,23.2490273218234));
#34755=CARTESIAN_POINT('Ctrl Pts',(-5.31135212928438,2.38246358338242,23.3880473173359));
#34756=CARTESIAN_POINT('Ctrl Pts',(-5.80375525721159,-0.450576388402698,
23.5270673128484));
#34757=CARTESIAN_POINT('Ctrl Pts',(-4.87999973956568,-3.17367243256704,
23.666087308361));
#34758=CARTESIAN_POINT('Ctrl Pts',(-2.76548866533538,-5.12236923789166,
23.8051073038735));
#34759=CARTESIAN_POINT('Ctrl Pts',(0.0238218291122001,-5.82117055993508,
23.944127299386));
#34760=CARTESIAN_POINT('Ctrl Pts',(2.80731962337594,-5.09956377542292,24.0831472948985));
#34761=CARTESIAN_POINT('Ctrl Pts',(4.90581093832766,-3.13362620693373,24.222167290411));
#34762=CARTESIAN_POINT('Ctrl Pts',(5.80724857579574,-0.403060970965061,
24.3611872859235));
#34763=CARTESIAN_POINT('Ctrl Pts',(5.29167517245777,2.42585408394472,24.5002072814361));
#34764=CARTESIAN_POINT('Ctrl Pts',(3.48489440200532,4.66284303555988,24.6392272769485));
#34765=CARTESIAN_POINT('Ctrl Pts',(0.827773960496438,5.76206425143987,24.7782472724611));
#34766=CARTESIAN_POINT('Ctrl Pts',(-2.03132936946743,5.4552997314663,24.9172672679736));
#34767=CARTESIAN_POINT('Ctrl Pts',(-4.39477350618678,3.81740225765061,25.0562872634861));
#34768=CARTESIAN_POINT('Ctrl Pts',(-5.6858608290331,1.24803076895726,25.1953072589986));
#34769=CARTESIAN_POINT('Ctrl Pts',(-5.58955660731777,-1.62586933699712,
25.3343272545112));
#34770=CARTESIAN_POINT('Ctrl Pts',(-4.12935977408376,-4.10304545716667,
25.4733472500237));
#34771=CARTESIAN_POINT('Ctrl Pts',(-1.66156901491974,-5.57904853680768,
25.6123672455362));
#34772=CARTESIAN_POINT('Ctrl Pts',(1.21165671202161,-5.69372305083503,25.7513872410487));
#34773=CARTESIAN_POINT('Ctrl Pts',(3.78922935709598,-4.41908758079302,25.8904072365612));
#34774=CARTESIAN_POINT('Ctrl Pts',(5.44220238066783,-2.06616248520063,26.0294272320737));
#34775=CARTESIAN_POINT('Ctrl Pts',(5.76723829959271,0.790921338129275,26.1684472275863));
#34776=CARTESIAN_POINT('Ctrl Pts',(4.6850259771483,3.45501458185676,26.3074672230988));
#34777=CARTESIAN_POINT('Ctrl Pts',(2.45963311930325,5.27605904874309,26.4464872186113));
#34778=CARTESIAN_POINT('Ctrl Pts',(-0.365928173024152,5.80970659668666,
26.5855072141238));
#34779=CARTESIAN_POINT('Ctrl Pts',(-3.102200320148,4.9257433287851,26.7245272096363));
#34780=CARTESIAN_POINT('Ctrl Pts',(-5.08151294555208,2.83986273463768,26.8635472051489));
#34781=CARTESIAN_POINT('Ctrl Pts',(-5.82089932122442,0.0610349044915131,
27.0025672006613));
#34782=CARTESIAN_POINT('Ctrl Pts',(-5.13994377456644,-2.73268588785704,
27.1415871961739));
#34783=CARTESIAN_POINT('Ctrl Pts',(-3.2048044293984,-4.85961137712736,27.2806071916864));
#34784=CARTESIAN_POINT('Ctrl Pts',(-0.48766941092484,-5.80075621906708,
27.4196271871989));
#34785=CARTESIAN_POINT('Ctrl Pts',(2.34846050341454,-5.32647420263152,27.5586471827114));
#34786=CARTESIAN_POINT('Ctrl Pts',(4.6115489130204,-3.5524936017138,27.697667178224));
#34787=CARTESIAN_POINT('Ctrl Pts',(5.7493857271972,-0.911678631590233,27.8366871737365));
#34788=CARTESIAN_POINT('Ctrl Pts',(5.48433045797889,1.95159257917282,27.975707169249));
#34789=CARTESIAN_POINT('Ctrl Pts',(3.88105852574804,4.33866095553867,28.1147271647615));
#34790=CARTESIAN_POINT('Ctrl Pts',(1.33077998458343,5.66706438996677,28.253747160274));
#34791=CARTESIAN_POINT('Ctrl Pts',(-1.54421858645868,5.61266274816444,28.3927671557865));
#34792=CARTESIAN_POINT('Ctrl Pts',(-4.04241655083305,4.18873042782036,28.531787151299));
#34793=CARTESIAN_POINT('Ctrl Pts',(-5.55423537036727,1.74271730867587,28.6708071468116));
#34794=CARTESIAN_POINT('Ctrl Pts',(-5.71078021801578,-1.12853155424069,
28.8098271423241));
#34795=CARTESIAN_POINT('Ctrl Pts',(-4.47385300829901,-3.72441048053663,
28.9488471378366));
#34796=CARTESIAN_POINT('Ctrl Pts',(-2.14527300897614,-5.41150606433697,
29.0878671333492));
#34797=CARTESIAN_POINT('Ctrl Pts',(0.706769263329594,-5.77815466873377,
29.2268871288616));
#34798=CARTESIAN_POINT('Ctrl Pts',(3.38635467652741,-4.73489135801003,29.3659071243742));
#34799=CARTESIAN_POINT('Ctrl Pts',(5.23964483094734,-2.53627999497769,29.5049271198867));
#34800=CARTESIAN_POINT('Ctrl Pts',(5.81442340136165,0.281202199663012,29.6439471153992));
#34801=CARTESIAN_POINT('Ctrl Pts',(4.97044022116119,3.03006900503279,29.7829671109117));
#34802=CARTESIAN_POINT('Ctrl Pts',(2.91363334672317,5.03957685607234,29.9219871064243));
#34803=CARTESIAN_POINT('Ctrl Pts',(0.145878668470538,5.81939116931338,30.0610071019367));
#34804=CARTESIAN_POINT('Ctrl Pts',(-2.65747146968753,5.17923156029867,30.2000270974493));
#34805=CARTESIAN_POINT('Ctrl Pts',(-4.81237917180638,3.27530164628564,30.3390470929618));
#34806=CARTESIAN_POINT('Ctrl Pts',(-5.79303122945065,0.57217422347277,30.4780670884743));
#34807=CARTESIAN_POINT('Ctrl Pts',(-5.36014138257237,-2.27056788628583,
30.6170870839868));
#34808=CARTESIAN_POINT('Ctrl Pts',(-3.61933791356257,-4.55927485844469,
30.7561070794994));
#34809=CARTESIAN_POINT('Ctrl Pts',(-0.995389575345323,-5.73548548605007,
30.8951270750118));
#34810=CARTESIAN_POINT('Ctrl Pts',(1.87144108481115,-5.51219579056096,31.0341470705244));
#34811=CARTESIAN_POINT('Ctrl Pts',(4.28162646023702,-3.94389008751453,31.1731670660369));
#34812=CARTESIAN_POINT('Ctrl Pts',(5.64706372688543,-1.4132464158427,31.3121870615494));
#34813=CARTESIAN_POINT('Ctrl Pts',(5.63457622508423,1.46223969687353,31.4512070570619));
#34814=CARTESIAN_POINT('Ctrl Pts',(4.24721099642181,3.98092865036174,31.5902270525745));
#34815=CARTESIAN_POINT('Ctrl Pts',(1.8234952833584,5.52824195553766,31.7292470480869));
#34816=CARTESIAN_POINT('Ctrl Pts',(-1.04516658891478,5.72662387177763,31.8682670435995));
#34817=CARTESIAN_POINT('Ctrl Pts',(-3.65880018460502,4.52766776348834,32.0072870391119));
#34818=CARTESIAN_POINT('Ctrl Pts',(-5.37965982891017,2.22392767252164,32.1463070346245));
#34819=CARTESIAN_POINT('Ctrl Pts',(-5.78784320770817,-0.622467003449729,
32.285327030137));
#34820=CARTESIAN_POINT('Ctrl Pts',(-4.7837505971572,-3.31697518706355,32.4243470256496));
#34821=CARTESIAN_POINT('Ctrl Pts',(-2.61238792331202,-5.2021172137439,32.563367021162));
#34822=CARTESIAN_POINT('Ctrl Pts',(0.19641647218261,-5.81790466893816,32.7023870166746));
#34823=CARTESIAN_POINT('Ctrl Pts',(2.95729381478017,-5.01408091881854,32.8414070121871));
#34824=CARTESIAN_POINT('Ctrl Pts',(4.99656988067041,-2.98678482569044,32.9804270076996));
#34825=CARTESIAN_POINT('Ctrl Pts',(5.81664642467701,-0.230691433931826,
33.1194470032122));
#34826=CARTESIAN_POINT('Ctrl Pts',(5.21741878415356,2.58169235157071,33.2584669987246));
#34827=CARTESIAN_POINT('Ctrl Pts',(3.34510287727474,4.76412435898198,33.3974869942372));
#34828=CARTESIAN_POINT('Ctrl Pts',(0.656557451741129,5.78407524846973,33.5365069897497));
#34829=CARTESIAN_POINT('Ctrl Pts',(-2.1921927843664,5.39266955816591,33.6755269852622));
#34830=CARTESIAN_POINT('Ctrl Pts',(-4.5060319798187,3.68541313345579,33.8145469807748));
#34831=CARTESIAN_POINT('Ctrl Pts',(-5.72036648173308,1.07888900358752,33.9535669762872));
#34832=CARTESIAN_POINT('Ctrl Pts',(-5.53888980796299,-1.79089191819071,
34.0925869717998));
#34833=CARTESIAN_POINT('Ctrl Pts',(-4.00588359154434,-4.22368213983876,
34.2316069673123));
#34834=CARTESIAN_POINT('Ctrl Pts',(-1.49541253901362,-5.62586308983412,
34.3706269628248));
#34835=CARTESIAN_POINT('Ctrl Pts',(1.37995008836278,-5.65529238156834,34.5096469583373));
#34836=CARTESIAN_POINT('Ctrl Pts',(3.91859482163678,-4.30478905304764,34.6486669538498));
#34837=CARTESIAN_POINT('Ctrl Pts',(5.5010738157949,-1.90388577403503,34.7876869493624));
#34838=CARTESIAN_POINT('Ctrl Pts',(5.74125064542016,0.961579530699287,34.9267069448748));
#34839=CARTESIAN_POINT('Ctrl Pts',(4.58052041098353,3.59241241117446,35.0657269403874));
#34840=CARTESIAN_POINT('Ctrl Pts',(2.30210976209836,5.34667044155973,35.2047469358999));
#34841=CARTESIAN_POINT('Ctrl Pts',(-0.53803247231554,5.79630185774787,35.3437669314124));
#34842=CARTESIAN_POINT('Ctrl Pts',(-3.24689085627389,4.83159331223588,35.482786926925));
#34843=CARTESIAN_POINT('Ctrl Pts',(-5.1634841715715,2.68794073173646,35.6218069224374));
#34844=CARTESIAN_POINT('Ctrl Pts',(-5.82014965966356,-0.111589007143574,
35.76082691795));
#34845=CARTESIAN_POINT('Ctrl Pts',(-5.05665614831808,-2.88389021376926,
35.8998469134625));
#34846=CARTESIAN_POINT('Ctrl Pts',(-3.05930162720085,-4.95250115812238,
36.038866908975));
#34847=CARTESIAN_POINT('Ctrl Pts',(-0.315455178569425,-5.81266567056034,
36.1778869044875));
#34848=CARTESIAN_POINT('Ctrl Pts',(2.50536463620572,-5.25449733152917,36.3169069));
#34849=CARTESIAN_POINT('Ctrl Pts',(4.7148571925705,-3.41419328993885,36.4559268955126));
#34850=CARTESIAN_POINT('Ctrl Pts',(5.77389017922739,-0.740801164698446,
36.594946891025));
#34851=CARTESIAN_POINT('Ctrl Pts',(5.42405181733073,2.11335185198976,36.7339668865376));
#34852=CARTESIAN_POINT('Ctrl Pts',(3.750705220726,4.45183159099891,36.8729868820501));
#34853=CARTESIAN_POINT('Ctrl Pts',(1.16215917308872,5.70403192696209,37.0120068775626));
#34854=CARTESIAN_POINT('Ctrl Pts',(-1.7099621956231,5.5644068378343,37.1510268730751));
#34855=CARTESIAN_POINT('Ctrl Pts',(-4.16484030723409,4.06702586451518,37.2900468685877));
#34856=CARTESIAN_POINT('Ctrl Pts',(-5.60346698384665,1.57726089418894,37.4290668641001));
#34857=CARTESIAN_POINT('Ctrl Pts',(-5.67480681553278,-1.29736724707385,
37.5680868596127));
#34858=CARTESIAN_POINT('Ctrl Pts',(-4.36145236263682,-3.85542831029796,
37.7071068551252));
#34859=CARTESIAN_POINT('Ctrl Pts',(-1.98387169811197,-5.47273672423838,
37.8461268506377));
#34860=CARTESIAN_POINT('Ctrl Pts',(0.877788141443237,-5.75465743082409,
37.9851468461503));
#34861=CARTESIAN_POINT('Ctrl Pts',(3.52526126732858,-4.63239971985041,38.1241668416627));
#34862=CARTESIAN_POINT('Ctrl Pts',(5.31254491237248,-2.37980266438677,38.2631868371753));
#34863=CARTESIAN_POINT('Ctrl Pts',(5.80352882143023,0.453483611860533,38.4022068326878));
#34864=CARTESIAN_POINT('Ctrl Pts',(4.87840933689825,3.17611657674293,38.5412268282003));
#34865=CARTESIAN_POINT('Ctrl Pts',(2.76292236564143,5.12375391376631,38.6802468237129));
#34866=CARTESIAN_POINT('Ctrl Pts',(-0.026737829975367,5.82115789648808,
38.8192668192253));
#34867=CARTESIAN_POINT('Ctrl Pts',(-2.80987379991321,5.09815686262776,38.9582868147379));
#34868=CARTESIAN_POINT('Ctrl Pts',(-4.90738005282049,3.1311683417818,39.0973068102503));
#34869=CARTESIAN_POINT('Ctrl Pts',(-5.80744975285464,0.400151890493876,
39.2363268057629));
#34870=CARTESIAN_POINT('Ctrl Pts',(-5.29045932341185,-2.42850454286624,
39.3753468012754));
#34871=CARTESIAN_POINT('Ctrl Pts',(-3.48255820289654,-4.66458814160855,
39.514366796788));
#34872=CARTESIAN_POINT('Ctrl Pts',(-0.824887460959776,-5.76247818600198,
39.6533867923004));
#34873=CARTESIAN_POINT('Ctrl Pts',(2.03406184247587,-5.4542814914873,39.792406787813));
#34874=CARTESIAN_POINT('Ctrl Pts',(4.39668520930807,-3.81520030111772,39.9314267833255));
#34875=CARTESIAN_POINT('Ctrl Pts',(5.68648529275177,-1.24518238933703,40.0704467788382));
#34876=CARTESIAN_POINT('Ctrl Pts',(5.5887414579283,1.62866911428645,40.2094667743506));
#34877=CARTESIAN_POINT('Ctrl Pts',(4.12730391398715,4.10511346603033,40.3484867698631));
#34878=CARTESIAN_POINT('Ctrl Pts',(1.65877408898573,5.5798801679881,40.4875067653756));
#34879=CARTESIAN_POINT('Ctrl Pts',(-1.21450872146438,5.69311538025396,40.6265267608882));
#34880=CARTESIAN_POINT('Ctrl Pts',(-3.79144253892607,4.41718888450776,40.7655467564006));
#34881=CARTESIAN_POINT('Ctrl Pts',(-5.44323670236427,2.06343605896375,40.9045667519131));
#34882=CARTESIAN_POINT('Ctrl Pts',(-5.76684137911178,-0.793810226415255,
41.0435867474256));
#34883=CARTESIAN_POINT('Ctrl Pts',(-4.68329466598454,-3.45736102236341,
41.1826067429381));
#34884=CARTESIAN_POINT('Ctrl Pts',(-2.45698987001788,-5.27729049285965,
41.3216267384507));
#34885=CARTESIAN_POINT('Ctrl Pts',(0.368838388311899,-5.80952256306013,
41.4606467339632));
#34886=CARTESIAN_POINT('Ctrl Pts',(3.10466738766565,-4.92418872296366,41.5996667294757));
#34887=CARTESIAN_POINT('Ctrl Pts',(5.08293488281772,-2.83731689178915,41.7386867249883));
#34888=CARTESIAN_POINT('Ctrl Pts',(5.8209291651662,-0.0581190288535307,
41.8777067205007));
#34889=CARTESIAN_POINT('Ctrl Pts',(5.13857424304467,2.73526030134519,42.0167267160134));
#34890=CARTESIAN_POINT('Ctrl Pts',(3.20236969810097,4.86121615278336,42.1557467115258));
#34891=CARTESIAN_POINT('Ctrl Pts',(0.484763572059907,5.80099977991734,42.2947667070383));
#34892=CARTESIAN_POINT('Ctrl Pts',(-2.35112840395363,5.32529711805075,42.4337867025508));
#34893=CARTESIAN_POINT('Ctrl Pts',(-4.61332788802856,3.5501830889315,42.5728066980634));
#34894=CARTESIAN_POINT('Ctrl Pts',(-5.74984169378732,0.90879847259015,42.7118266935758));
#34895=CARTESIAN_POINT('Ctrl Pts',(-5.48335215697474,-1.95433960457174,
42.8508466890884));
#34896=CARTESIAN_POINT('Ctrl Pts',(-3.87888466973552,-4.34060455308798,
42.9898666846009));
#34897=CARTESIAN_POINT('Ctrl Pts',(-1.32794101029701,-5.66773030767773,
43.1288866801135));
#34898=CARTESIAN_POINT('Ctrl Pts',(1.54702994857086,-5.61188849725491,43.2679066756258));
#34899=CARTESIAN_POINT('Ctrl Pts',(4.04451430789495,-4.18670493116369,43.4069266711385));
#34900=CARTESIAN_POINT('Ctrl Pts',(5.55510765434376,-1.73993480224076,43.5459466666509));
#34901=CARTESIAN_POINT('Ctrl Pts',(5.71021418524961,1.13139211857394,43.6849666621635));
#34902=CARTESIAN_POINT('Ctrl Pts',(4.47198677491675,3.72665110419086,43.8239866576759));
#34903=CARTESIAN_POINT('Ctrl Pts',(2.1425619495451,5.41258001878576,43.9630066531885));
#34904=CARTESIAN_POINT('Ctrl Pts',(-0.709663630519674,5.77779990125263,
44.102026648701));
#34905=CARTESIAN_POINT('Ctrl Pts',(-3.3887261047556,4.73319443445388,44.2410466442136));
#34906=CARTESIAN_POINT('Ctrl Pts',(-5.24091467441638,2.53365497708039,44.3800666397261));
#34907=CARTESIAN_POINT('Ctrl Pts',(-5.81428180899623,-0.284114788373957,
44.5190866352387));
#34908=CARTESIAN_POINT('Ctrl Pts',(-4.96892174253198,-3.03255847165228,
44.658106630751));
#34909=CARTESIAN_POINT('Ctrl Pts',(-2.91110850169949,-5.04103575257413,
44.7971266262637));
#34910=CARTESIAN_POINT('Ctrl Pts',(-0.142963537667334,-5.81946351430219,
44.9361466217762));
#34911=CARTESIAN_POINT('Ctrl Pts',(2.66006557307581,-5.17789970106932,45.0751666172887));
#34912=CARTESIAN_POINT('Ctrl Pts',(4.81401926761876,-3.27289056621134,45.2141866128011));
#34913=CARTESIAN_POINT('Ctrl Pts',(5.79331712233613,-0.569272243690995,
45.3532066083137));
#34914=CARTESIAN_POINT('Ctrl Pts',(5.35900331258278,2.27325266152679,45.4922266038261));
#34915=CARTESIAN_POINT('Ctrl Pts',(3.61705357807721,4.56108732438807,45.6312465993388));
#34916=CARTESIAN_POINT('Ctrl Pts',(0.992516368906552,5.73598338777858,45.7702665948512));
#34917=CARTESIAN_POINT('Ctrl Pts',(-1.87420207887986,5.51125763641381,45.9092865903637));
#34918=CARTESIAN_POINT('Ctrl Pts',(-4.28360153919141,3.94174479396065,46.0483065858762));
#34919=CARTESIAN_POINT('Ctrl Pts',(-5.64777095711903,1.41041745015005,46.1873265813888));
#34920=CARTESIAN_POINT('Ctrl Pts',(-5.63384303711158,-1.46506204639129,
46.3263465769013));
#34921=CARTESIAN_POINT('Ctrl Pts',(-4.24521629374547,-3.98305570989048,
46.4653665724138));
#34922=CARTESIAN_POINT('Ctrl Pts',(-1.82072578743378,-5.52915470689165,
46.6043865679263));
#34923=CARTESIAN_POINT('Ctrl Pts',(1.04803509977905,-5.72609959722744,46.7434065634389));
#34924=CARTESIAN_POINT('Ctrl Pts',(3.66106777494364,-4.52583438933708,46.8824265589513));
#34925=CARTESIAN_POINT('Ctrl Pts',(5.38077318598422,-2.22123255644752,47.0214465544639));
#34926=CARTESIAN_POINT('Ctrl Pts',(5.78753067235475,0.625366235410245,47.1604665499763));
#34927=CARTESIAN_POINT('Ctrl Pts',(4.78208841449392,3.31937109732865,47.299486545489));
#34928=CARTESIAN_POINT('Ctrl Pts',(2.60978170886072,5.20342519017945,47.4385065410014));
#34929=CARTESIAN_POINT('Ctrl Pts',(-0.199330843227342,5.81780554118826,
47.5775265365139));
#34930=CARTESIAN_POINT('Ctrl Pts',(-2.95980509719784,5.01259890319342,47.7165465320265));
#34931=CARTESIAN_POINT('Ctrl Pts',(-4.99806553239269,2.98428148935706,47.855566527539));
#34932=CARTESIAN_POINT('Ctrl Pts',(-5.81676104845808,0.227777717483519,
47.9945865230515));
#34933=CARTESIAN_POINT('Ctrl Pts',(-5.21612528403191,-2.58430569135105,
48.1336065185641));
#34934=CARTESIAN_POINT('Ctrl Pts',(-3.34271517260787,-4.76579923569095,
48.2726265140765));
#34935=CARTESIAN_POINT('Ctrl Pts',(-0.653661486064455,-5.78440378494888,
48.4116465095892));
#34936=CARTESIAN_POINT('Ctrl Pts',(2.19489686646158,-5.39157001791135,48.5506665051015));
#34937=CARTESIAN_POINT('Ctrl Pts',(4.50787169081764,-3.68315687906655,48.6896865006141));
#34938=CARTESIAN_POINT('Ctrl Pts',(5.7209176522647,-1.07602059177106,48.8287064961267));
#34939=CARTESIAN_POINT('Ctrl Pts',(5.53796966980217,1.79366089053333,48.9677264916392));
#34940=CARTESIAN_POINT('Ctrl Pts',(4.00381092406488,4.22569882818473,49.1067464871517));
#34941=CARTESIAN_POINT('Ctrl Pts',(1.49250882932127,5.626590889655,49.2457664826643));
#34942=CARTESIAN_POINT('Ctrl Pts',(-1.3826137177127,5.65464066082273,49.3847864781767));
#34943=CARTESIAN_POINT('Ctrl Pts',(-3.92110725836691,4.30274642744152,49.5238064736894));
#34944=CARTESIAN_POINT('Ctrl Pts',(-4.97439857514882,2.70177434217856,49.6164864706976));
#34945=CARTESIAN_POINT('Ctrl Pts',(-5.27781647799386,1.82365787836681,49.6628264692018));
#34946=CARTESIAN_POINT('Ctrl Pts',(3.05002998429121,-4.27421589951819,-0.19205317402687));
#34947=CARTESIAN_POINT('Ctrl Pts',(3.76125447956637,-3.76669573907992,-0.145707626209139));
#34948=CARTESIAN_POINT('Ctrl Pts',(4.92466409230247,-2.39035204390054,-0.0530220798872355));
#34949=CARTESIAN_POINT('Ctrl Pts',(5.46779549246023,0.259111396808819,0.0860034649388399));
#34950=CARTESIAN_POINT('Ctrl Pts',(4.67676629503674,2.8445323183143,0.225023460451358));
#34951=CARTESIAN_POINT('Ctrl Pts',(2.7445538350136,4.7362167530772,0.364043455963875));
#34952=CARTESIAN_POINT('Ctrl Pts',(0.142659132105948,5.47205170154488,0.503063451476392));
#34953=CARTESIAN_POINT('Ctrl Pts',(-2.49404997803322,4.87275717303697,0.64208344698891));
#34954=CARTESIAN_POINT('Ctrl Pts',(-4.5221903674749,3.08442767596202,0.781103442501426));
#34955=CARTESIAN_POINT('Ctrl Pts',(-5.44688448789985,0.543499211903274,
0.920123438013945));
#34956=CARTESIAN_POINT('Ctrl Pts',(-5.04249842617391,-2.13005927158998,
1.05914343352647));
#34957=CARTESIAN_POINT('Ctrl Pts',(-3.40770625431275,-4.28386147173102,
1.19816342903898));
#34958=CARTESIAN_POINT('Ctrl Pts',(-0.941408722948332,-5.39237341802913,
1.3371834245515));
#34959=CARTESIAN_POINT('Ctrl Pts',(1.7545993264326,-5.18510524360307,1.47620342006402));
#34960=CARTESIAN_POINT('Ctrl Pts',(4.02247237495026,-3.71263438622792,1.61522341557653));
#34961=CARTESIAN_POINT('Ctrl Pts',(5.30883278161673,-1.33425320709353,1.75424341108905));
#34962=CARTESIAN_POINT('Ctrl Pts',(5.29979925031378,1.36969527211531,1.89326340660157));
#34963=CARTESIAN_POINT('Ctrl Pts',(3.99757601195593,3.73942822069339,2.03228340211409));
#34964=CARTESIAN_POINT('Ctrl Pts',(1.71991505043604,5.19671333043287,2.17130339762661));
#34965=CARTESIAN_POINT('Ctrl Pts',(-0.977417738888497,5.38596248543875,
2.31032339313912));
#34966=CARTESIAN_POINT('Ctrl Pts',(-3.43625346479038,4.26099746548253,2.44934338865164));
#34967=CARTESIAN_POINT('Ctrl Pts',(-5.05661826374546,2.09631796986123,2.58836338416416));
#34968=CARTESIAN_POINT('Ctrl Pts',(-5.44313129684181,-0.57987841587087,
2.72738337967668));
#34969=CARTESIAN_POINT('Ctrl Pts',(-4.50148056306639,-3.11458023342574,
2.86640337518919));
#34970=CARTESIAN_POINT('Ctrl Pts',(-2.46143571461011,-4.8893017411088,3.00542337070171));
#34971=CARTESIAN_POINT('Ctrl Pts',(0.179217414714102,-5.47099793539511,
3.14444336621423));
#34972=CARTESIAN_POINT('Ctrl Pts',(2.77614018671673,-4.71773069977217,3.28346336172674));
#34973=CARTESIAN_POINT('Ctrl Pts',(4.69566448953035,-2.81330273756845,3.42248335723926));
#34974=CARTESIAN_POINT('Ctrl Pts',(5.46941238227303,-0.2224083725902,3.56150335275178));
#34975=CARTESIAN_POINT('Ctrl Pts',(4.90858373136372,2.42275525874201,3.7005233482643));
#34976=CARTESIAN_POINT('Ctrl Pts',(3.15002482123177,4.47674892272896,3.83954334377682));
#34977=CARTESIAN_POINT('Ctrl Pts',(0.622836862034194,5.43838317286077,3.97856333928933));
#34978=CARTESIAN_POINT('Ctrl Pts',(-2.05632783771493,5.0730122329227,4.11758333480185));
#34979=CARTESIAN_POINT('Ctrl Pts',(-4.23373353549831,3.46978927918545,4.25660333031437));
#34980=CARTESIAN_POINT('Ctrl Pts',(-5.37807734772074,1.01991241461394,4.39562332582688));
#34981=CARTESIAN_POINT('Ctrl Pts',(-5.2101310313972,-1.67883052367498,4.5346433213394));
#34982=CARTESIAN_POINT('Ctrl Pts',(-3.77087471358557,-3.9679265600553,4.67366331685192));
#34983=CARTESIAN_POINT('Ctrl Pts',(-1.41149744126235,-5.28881955306291,
4.81268331236443));
#34984=CARTESIAN_POINT('Ctrl Pts',(1.29229550954153,-5.3192019709323,4.95170330787695));
#34985=CARTESIAN_POINT('Ctrl Pts',(3.68075892328426,-4.05166028193557,5.09072330338947));
#34986=CARTESIAN_POINT('Ctrl Pts',(5.17109029312276,-1.79548391023775,5.22974329890198));
#34987=CARTESIAN_POINT('Ctrl Pts',(5.39963788657859,0.898803641167593,5.36876329441451));
#34988=CARTESIAN_POINT('Ctrl Pts',(4.31063442263225,3.37377654357382,5.50778328992702));
#34989=CARTESIAN_POINT('Ctrl Pts',(2.16980469534884,5.0255233434532,5.64680328543954));
#34990=CARTESIAN_POINT('Ctrl Pts',(-0.500473215454255,5.45100576519269,
5.78582328095206));
#34991=CARTESIAN_POINT('Ctrl Pts',(-3.0486320086287,4.54640299220334,5.92484327646457));
#34992=CARTESIAN_POINT('Ctrl Pts',(-4.85290233910033,2.53244470397788,6.06386327197709));
#34993=CARTESIAN_POINT('Ctrl Pts',(-5.47302907649065,-0.099448576857391,
6.20288326748962));
#34994=CARTESIAN_POINT('Ctrl Pts',(-4.75769677044274,-2.70707567904368,
6.34190326300212));
#34995=CARTESIAN_POINT('Ctrl Pts',(-2.88145172499117,-4.65415655603638,
6.48092325851464));
#34996=CARTESIAN_POINT('Ctrl Pts',(-0.302111426327919,-5.46558926170208,
6.61994325402716));
#34997=CARTESIAN_POINT('Ctrl Pts',(2.35094626553332,-4.94337829304272,6.75896324953968));
#34998=CARTESIAN_POINT('Ctrl Pts',(4.43035590855997,-3.21494693813735,6.8979832450522));
#34999=CARTESIAN_POINT('Ctrl Pts',(5.42872637181122,-0.70204506376189,7.03700324056471));
#35000=CARTESIAN_POINT('Ctrl Pts',(5.10244797494064,1.98216093054403,7.17602323607723));
#35001=CARTESIAN_POINT('Ctrl Pts',(3.53113502835836,4.1827051895934,7.31504323158974));
#35002=CARTESIAN_POINT('Ctrl Pts',(1.09819936036962,5.36263885194919,7.45406322710226));
#35003=CARTESIAN_POINT('Ctrl Pts',(-1.60270496753428,5.23404949141599,7.59308322261479));
#35004=CARTESIAN_POINT('Ctrl Pts',(-3.91253758488377,3.82831385056435,7.73210321812729));
#35005=CARTESIAN_POINT('Ctrl Pts',(-5.26768247309822,1.4884416865181,7.87112321363982));
#35006=CARTESIAN_POINT('Ctrl Pts',(-5.33747438796964,-1.21462111348319,
8.01014320915234));
#35007=CARTESIAN_POINT('Ctrl Pts',(-4.10488359284374,-3.62130749602312,
8.14916320466484));
#35008=CARTESIAN_POINT('Ctrl Pts',(-1.87067123866715,-5.14436841685882,
8.28818320017738));
#35009=CARTESIAN_POINT('Ctrl Pts',(0.819998552161644,-5.41216589416879,
8.42720319568988));
#35010=CARTESIAN_POINT('Ctrl Pts',(3.31058271092346,-4.35935538878005,8.56622319120241));
#35011=CARTESIAN_POINT('Ctrl Pts',(4.99336052359004,-2.24283034868973,8.70524318671491));
#35012=CARTESIAN_POINT('Ctrl Pts',(5.45772192092638,0.420961667364843,8.84426318222745));
#35013=CARTESIAN_POINT('Ctrl Pts',(4.59035933251229,2.98203596389586,8.98328317773994));
#35014=CARTESIAN_POINT('Ctrl Pts',(2.60291556098025,4.81547171873721,9.12230317325249));
#35015=CARTESIAN_POINT('Ctrl Pts',(-0.0196586066515966,5.47389722507973,
9.26132316876499));
#35016=CARTESIAN_POINT('Ctrl Pts',(-2.6374359307682,4.79665185339147,9.40034316427751));
#35017=CARTESIAN_POINT('Ctrl Pts',(-4.61165963658542,2.94898841771886,9.53936315979002));
#35018=CARTESIAN_POINT('Ctrl Pts',(-5.46060472961549,0.381750282844645,
9.67838315530255));
#35019=CARTESIAN_POINT('Ctrl Pts',(-4.97712241053276,-2.27863770751815,
9.81740315081505));
#35020=CARTESIAN_POINT('Ctrl Pts',(-3.27918589423115,-4.38302146499723,
9.95642314632758));
#35021=CARTESIAN_POINT('Ctrl Pts',(-0.781104084279084,-5.41791599243413,
10.0954431418401));
#35022=CARTESIAN_POINT('Ctrl Pts',(1.90757282367781,-5.13079947122442,10.2344631373526));
#35023=CARTESIAN_POINT('Ctrl Pts',(4.1307880388876,-3.59173042826634,10.3734831328651));
#35024=CARTESIAN_POINT('Ctrl Pts',(5.34606082113004,-1.1762529440258,10.5125031283776));
#35025=CARTESIAN_POINT('Ctrl Pts',(5.25685574100989,1.52623884427124,10.6515231238902));
#35026=CARTESIAN_POINT('Ctrl Pts',(3.88493948920281,3.8563172142322,10.7905431194027));
#35027=CARTESIAN_POINT('Ctrl Pts',(1.56506964505107,5.24542603586122,10.9295631149152));
#35028=CARTESIAN_POINT('Ctrl Pts',(-1.13668861626112,5.3546126172874,11.0685831104277));
#35029=CARTESIAN_POINT('Ctrl Pts',(-3.56108655827961,4.15723463566725,11.2076031059403));
#35030=CARTESIAN_POINT('Ctrl Pts',(-5.11655338696839,1.94546105842631,11.3466231014528));
#35031=CARTESIAN_POINT('Ctrl Pts',(-5.42354384245238,-0.74101921739443,
11.4856430969653));
#35032=CARTESIAN_POINT('Ctrl Pts',(-4.40715001280646,-3.24668539531798,
11.6246630924778));
#35033=CARTESIAN_POINT('Ctrl Pts',(-2.31537941133364,-4.96013663855375,
11.7636830879903));
#35034=CARTESIAN_POINT('Ctrl Pts',(0.341360666939199,-5.4632783369162,11.9027030835028));
#35035=CARTESIAN_POINT('Ctrl Pts',(2.91480625081657,-4.63334024346925,12.0417230790154));
#35036=CARTESIAN_POINT('Ctrl Pts',(4.77701783371922,-2.67283331090427,12.1807430745279));
#35037=CARTESIAN_POINT('Ctrl Pts',(5.47360219675033,-0.060135540913871,
12.3197630700404));
#35038=CARTESIAN_POINT('Ctrl Pts',(4.83458767081651,2.56723574000129,12.4587830655529));
#35039=CARTESIAN_POINT('Ctrl Pts',(3.01589846454521,4.56818276156996,12.5978030610654));
#35040=CARTESIAN_POINT('Ctrl Pts',(0.461308019256385,5.45445984520197,12.7368230565779));
#35041=CARTESIAN_POINT('Ctrl Pts',(-2.20584494991392,5.00980891337088,12.8758430520905));
#35042=CARTESIAN_POINT('Ctrl Pts',(-4.33475565038537,3.34272803904282,13.014863047603));
#35043=CARTESIAN_POINT('Ctrl Pts',(-5.40595433188213,0.85999712392298,13.1538830431155));
#35044=CARTESIAN_POINT('Ctrl Pts',(-5.15806069721761,-1.83257936673147,
13.292903038628));
#35045=CARTESIAN_POINT('Ctrl Pts',(-3.65156260267703,-4.07799311552651,
13.4319230341405));
#35046=CARTESIAN_POINT('Ctrl Pts',(-1.25405657957035,-5.32834677801541,
13.570943029653));
#35047=CARTESIAN_POINT('Ctrl Pts',(1.44944840257059,-5.27854493396018,13.7099630251656));
#35048=CARTESIAN_POINT('Ctrl Pts',(3.79927739465977,-3.94073959682421,13.8489830206781));
#35049=CARTESIAN_POINT('Ctrl Pts',(5.22205497073815,-1.64136503378741,13.9880030161906));
#35050=CARTESIAN_POINT('Ctrl Pts',(5.37061301709398,1.05851457815739,14.1270230117031));
#35051=CARTESIAN_POINT('Ctrl Pts',(4.20870228606042,3.5001089067143,14.2660430072156));
#35052=CARTESIAN_POINT('Ctrl Pts',(2.01983747703712,5.08765111401199,14.4050630027282));
#35053=CARTESIAN_POINT('Ctrl Pts',(-0.661882419595964,5.43376931366991,
14.5440829982406));
#35054=CARTESIAN_POINT('Ctrl Pts',(-3.18209817463055,4.45400813858303,14.6831029937532));
#35055=CARTESIAN_POINT('Ctrl Pts',(-4.92585874826066,2.38743646695259,14.8221229892657));
#35056=CARTESIAN_POINT('Ctrl Pts',(-5.46767383245036,-0.261687129008328,
14.9611429847782));
#35057=CARTESIAN_POINT('Ctrl Pts',(-4.67533659183668,-2.84695715538257,
15.1001629802908));
#35058=CARTESIAN_POINT('Ctrl Pts',(-2.74218309656324,-4.73754885531261,
15.2391829758032));
#35059=CARTESIAN_POINT('Ctrl Pts',(-0.139916909965175,-5.47214405419455,
15.3782029713158));
#35060=CARTESIAN_POINT('Ctrl Pts',(2.49649002394695,-4.8714961615385,15.5172229668283));
#35061=CARTESIAN_POINT('Ctrl Pts',(4.52373516961751,-3.08216764740608,15.6562429623408));
#35062=CARTESIAN_POINT('Ctrl Pts',(5.44715591422003,-0.540767729925525,
15.7952629578533));
#35063=CARTESIAN_POINT('Ctrl Pts',(5.0414308558319,2.13258346083268,15.9342829533659));
#35064=CARTESIAN_POINT('Ctrl Pts',(3.4055598701712,4.28556872097864,16.0733029488783));
#35065=CARTESIAN_POINT('Ctrl Pts',(0.938707418300856,5.39284393195074,16.2123229443909));
#35066=CARTESIAN_POINT('Ctrl Pts',(-1.75719649545506,5.18422586004037,16.3513429399034));
#35067=CARTESIAN_POINT('Ctrl Pts',(-4.02433163817825,3.71061883754025,16.4903629354159));
#35068=CARTESIAN_POINT('Ctrl Pts',(-5.30950048675456,1.33159373410367,16.6293829309284));
#35069=CARTESIAN_POINT('Ctrl Pts',(-5.29911246141731,-1.3723499600331,16.768402926441));
#35070=CARTESIAN_POINT('Ctrl Pts',(-3.99570231617316,-3.74143024685473,
16.9074229219534));
#35071=CARTESIAN_POINT('Ctrl Pts',(-1.71731164032274,-5.19757424396833,
17.046442917466));
#35072=CARTESIAN_POINT('Ctrl Pts',(0.980115610780298,-5.38547218738113,
17.1854629129785));
#35073=CARTESIAN_POINT('Ctrl Pts',(3.43838749878582,-4.25927560739433,17.324482908491));
#35074=CARTESIAN_POINT('Ctrl Pts',(5.05766773958404,-2.09378468986712,17.4635029040035));
#35075=CARTESIAN_POINT('Ctrl Pts',(5.44284013495777,0.582604974956452,17.6025228995161));
#35076=CARTESIAN_POINT('Ctrl Pts',(4.49991980898261,3.11683477333606,17.7415428950285));
#35077=CARTESIAN_POINT('Ctrl Pts',(2.45898620376762,4.89053413659811,17.8805628905411));
#35078=CARTESIAN_POINT('Ctrl Pts',(-0.181957983817034,5.47090747350714,
18.0195828860536));
#35079=CARTESIAN_POINT('Ctrl Pts',(-2.77850309520129,4.71633945359194,18.1586028815661));
#35080=CARTESIAN_POINT('Ctrl Pts',(-4.697073170486,2.81095018146029,18.2976228770786));
#35081=CARTESIAN_POINT('Ctrl Pts',(-5.46952310726072,0.219668547343855,
18.4366428725912));
#35082=CARTESIAN_POINT('Ctrl Pts',(-4.90736948268007,-2.42521381573074,
18.5756628681037));
#35083=CARTESIAN_POINT('Ctrl Pts',(-3.14778188441772,-4.47832630562831,
18.7146828636162));
#35084=CARTESIAN_POINT('Ctrl Pts',(-0.620112530044538,-5.43869448871995,
18.8537028591287));
#35085=CARTESIAN_POINT('Ctrl Pts',(2.05886880798953,-5.0719815184047,18.9927228546412));
#35086=CARTESIAN_POINT('Ctrl Pts',(4.23547112876366,-3.46766803615348,19.1317428501537));
#35087=CARTESIAN_POINT('Ctrl Pts',(5.3785875785371,-1.01721824185249,19.2707628456663));
#35088=CARTESIAN_POINT('Ctrl Pts',(5.20928939972103,1.68144022834744,19.4097828411788));
#35089=CARTESIAN_POINT('Ctrl Pts',(3.76888658368916,3.96981500964954,19.5488028366913));
#35090=CARTESIAN_POINT('Ctrl Pts',(1.40884793135217,5.28952595209399,19.6878228322038));
#35091=CARTESIAN_POINT('Ctrl Pts',(-1.29495989970804,5.31855395288035,19.8268428277163));
#35092=CARTESIAN_POINT('Ctrl Pts',(-3.68278806305859,4.04981596793535,19.9658628232288));
#35093=CARTESIAN_POINT('Ctrl Pts',(-5.17198905758884,1.79289332636729,20.1048828187414));
#35094=CARTESIAN_POINT('Ctrl Pts',(-5.39918697064639,-0.901508373534651,
20.2439028142538));
#35095=CARTESIAN_POINT('Ctrl Pts',(-4.3089438530806,-3.37593544999751,20.3829228097664));
#35096=CARTESIAN_POINT('Ctrl Pts',(-2.16728698348817,-5.02660963500785,
20.5219428052789));
#35097=CARTESIAN_POINT('Ctrl Pts',(0.503203729552668,-5.45075437880991,
20.6609628007914));
#35098=CARTESIAN_POINT('Ctrl Pts',(3.05090905959427,-4.54487526799544,20.7999827963039));
#35099=CARTESIAN_POINT('Ctrl Pts',(4.85417030987677,-2.53001341780274,20.9390027918165));
#35100=CARTESIAN_POINT('Ctrl Pts',(5.47297857295331,0.102190173426562,21.0780227873289));
#35101=CARTESIAN_POINT('Ctrl Pts',(4.75634011582337,2.70945861643248,21.2170427828415));
#35102=CARTESIAN_POINT('Ctrl Pts',(2.87911995291945,4.65559938012842,21.356062778354));
#35103=CARTESIAN_POINT('Ctrl Pts',(0.299373506209391,5.46573991288745,21.4950827738665));
#35104=CARTESIAN_POINT('Ctrl Pts',(-2.3534222612051,4.94220001133254,21.634102769379));
#35105=CARTESIAN_POINT('Ctrl Pts',(-4.43196581876828,3.2127272328694,21.7731227648916));
#35106=CARTESIAN_POINT('Ctrl Pts',(-5.42907736671412,0.69932555922365,21.9121427604041));
#35107=CARTESIAN_POINT('Ctrl Pts',(-5.10145440921986,-1.98471665539497,
22.0511627559166));
#35108=CARTESIAN_POINT('Ctrl Pts',(-3.52903933930205,-4.18447351923866,
22.1901827514291));
#35109=CARTESIAN_POINT('Ctrl Pts',(-1.09551291140435,-5.36318830104793,
22.3292027469416));
#35110=CARTESIAN_POINT('Ctrl Pts',(1.60532666325203,-5.23324599037759,22.4682227424542));
#35111=CARTESIAN_POINT('Ctrl Pts',(3.91445481446258,-3.82635345950707,22.6072427379667));
#35112=CARTESIAN_POINT('Ctrl Pts',(5.26842741852657,-1.48580275516922,22.7462627334792));
#35113=CARTESIAN_POINT('Ctrl Pts',(5.33686527712551,1.21729466661241,22.8852827289917));
#35114=CARTESIAN_POINT('Ctrl Pts',(4.10306905321916,3.62336330445434,23.0243027245042));
#35115=CARTESIAN_POINT('Ctrl Pts',(1.8680940311752,5.14530484832907,23.1633227200167));
#35116=CARTESIAN_POINT('Ctrl Pts',(-0.822709570081384,5.41175445256412,
23.3023427155292));
#35117=CARTESIAN_POINT('Ctrl Pts',(-3.3127660311103,4.35769646885517,23.4413627110418));
#35118=CARTESIAN_POINT('Ctrl Pts',(-4.99448339998182,2.24032873901511,23.5803827065543));
#35119=CARTESIAN_POINT('Ctrl Pts',(-5.45751036348743,-0.423695555768791,
23.7194027020668));
#35120=CARTESIAN_POINT('Ctrl Pts',(-4.58886496280194,-2.98433504230336,
23.8584226975793));
#35121=CARTESIAN_POINT('Ctrl Pts',(-2.60050301611552,-4.81677499523542,
23.9974426930919));
#35122=CARTESIAN_POINT('Ctrl Pts',(0.0224006481140536,-5.47388669069018,
24.1364626886043));
#35123=CARTESIAN_POINT('Ctrl Pts',(2.63983839069682,-4.7953300785821,24.2754826841169));
#35124=CARTESIAN_POINT('Ctrl Pts',(4.61313629722153,-2.94667792519104,24.4145026796294));
#35125=CARTESIAN_POINT('Ctrl Pts',(5.46079527498544,-0.379014849639979,
24.5535226751419));
#35126=CARTESIAN_POINT('Ctrl Pts',(4.97598034617548,2.28113061573125,24.6925426706544));
#35127=CARTESIAN_POINT('Ctrl Pts',(3.27698989218598,4.38466356041853,24.8315626661669));
#35128=CARTESIAN_POINT('Ctrl Pts',(0.778389985074074,5.41830659179484,24.9705826616795));
#35129=CARTESIAN_POINT('Ctrl Pts',(-1.91014276002585,5.12984326542945,25.109602657192));
#35130=CARTESIAN_POINT('Ctrl Pts',(-4.13258672915122,3.58966073850917,25.2486226527045));
#35131=CARTESIAN_POINT('Ctrl Pts',(-5.3466493717559,1.17357478971434,25.387642648217));
#35132=CARTESIAN_POINT('Ctrl Pts',(-5.25609054134937,-1.52887197393661,
25.5266626437296));
#35133=CARTESIAN_POINT('Ctrl Pts',(-3.88300725355842,-3.85826281639337,
25.665682639242));
#35134=CARTESIAN_POINT('Ctrl Pts',(-1.56244185302379,-5.24620936938954,
25.8047026347546));
#35135=CARTESIAN_POINT('Ctrl Pts',(1.13937076423583,-5.35404254308423,25.9437226302671));
#35136=CARTESIAN_POINT('Ctrl Pts',(3.56316859851835,-4.1554502559992,26.0827426257796));
#35137=CARTESIAN_POINT('Ctrl Pts',(5.11752728645563,-1.94289777495703,26.2217626212921));
#35138=CARTESIAN_POINT('Ctrl Pts',(5.42317196260459,0.74373594478854,26.3607826168046));
#35139=CARTESIAN_POINT('Ctrl Pts',(4.40552309502093,3.24889266532279,26.4998026123171));
#35140=CARTESIAN_POINT('Ctrl Pts',(2.31289443542522,4.96129586117681,26.6388226078297));
#35141=CARTESIAN_POINT('Ctrl Pts',(-0.344097348710505,5.46310665337603,
26.7778426033422));
#35142=CARTESIAN_POINT('Ctrl Pts',(-2.91712686812292,4.63187954580281,26.9168625988547));
#35143=CARTESIAN_POINT('Ctrl Pts',(-4.7783561389992,2.67044002000411,27.0558825943672));
#35144=CARTESIAN_POINT('Ctrl Pts',(-5.47363163374707,0.0573936372287894,
27.1949025898798));
#35145=CARTESIAN_POINT('Ctrl Pts',(-4.83330105668796,-2.56965721195845,
27.3339225853923));
#35146=CARTESIAN_POINT('Ctrl Pts',(-3.01360974252997,-4.56969294496682,
27.4729425809048));
#35147=CARTESIAN_POINT('Ctrl Pts',(-0.458575654232012,-5.45469024426655,
27.6119625764173));
#35148=CARTESIAN_POINT('Ctrl Pts',(2.20835424093734,-5.00870330904966,27.7509825719298));
#35149=CARTESIAN_POINT('Ctrl Pts',(4.33642958208229,-3.34055620686025,27.8900025674423));
#35150=CARTESIAN_POINT('Ctrl Pts',(5.40638445270014,-0.85728900678427,28.0290225629549));
#35151=CARTESIAN_POINT('Ctrl Pts',(5.15714205453761,1.83516296847739,28.1680425584673));
#35152=CARTESIAN_POINT('Ctrl Pts',(3.64951935201825,4.07982178419541,28.3070625539799));
#35153=CARTESIAN_POINT('Ctrl Pts',(1.25138728900764,5.32897430510424,28.4460825494924));
#35154=CARTESIAN_POINT('Ctrl Pts',(-1.45209240665622,5.27781819827875,28.5851025450049));
#35155=CARTESIAN_POINT('Ctrl Pts',(-3.80125095597222,3.93883592718345,28.7241225405174));
#35156=CARTESIAN_POINT('Ctrl Pts',(-5.22287652591183,1.63874893947494,28.86314253603));
#35157=CARTESIAN_POINT('Ctrl Pts',(-5.37008210066978,-1.06120475103391,
29.0021625315424));
#35158=CARTESIAN_POINT('Ctrl Pts',(-4.20694844552114,-3.50221673633691,
29.141182527055));
#35159=CARTESIAN_POINT('Ctrl Pts',(-2.01728866227594,-5.08866227456726,
29.2802025225675));
#35160=CARTESIAN_POINT('Ctrl Pts',(0.664604279172973,-5.43343707460167,
29.41922251808));
#35161=CARTESIAN_POINT('Ctrl Pts',(3.18432892541915,-4.45241356864901,29.5582425135925));
#35162=CARTESIAN_POINT('Ctrl Pts',(4.92705407078572,-2.38496865285581,29.6972625091051));
#35163=CARTESIAN_POINT('Ctrl Pts',(5.4675420592909,0.264426022615144,29.8362825046176));
#35164=CARTESIAN_POINT('Ctrl Pts',(4.67390987660545,2.84929881846764,29.9753025001301));
#35165=CARTESIAN_POINT('Ctrl Pts',(2.73980956819053,4.73892190499091,30.1143224956426));
#35166=CARTESIAN_POINT('Ctrl Pts',(0.137175726698781,5.47221345632237,30.2533424911551));
#35167=CARTESIAN_POINT('Ctrl Pts',(-2.49892999338152,4.87024498149005,30.3923624866676));
#35168=CARTESIAN_POINT('Ctrl Pts',(-4.52527855486839,3.07990118224584,30.5313824821802));
#35169=CARTESIAN_POINT('Ctrl Pts',(-5.44742611802051,0.538039013696014,
30.6704024776926));
#35170=CARTESIAN_POINT('Ctrl Pts',(-5.04036194648243,-2.13510860145403,
30.8094224732052));
#35171=CARTESIAN_POINT('Ctrl Pts',(-3.4034126693552,-4.28727413324872,30.9484424687177));
#35172=CARTESIAN_POINT('Ctrl Pts',(-0.936005858690288,-5.39331348282746,
31.0874624642302));
#35173=CARTESIAN_POINT('Ctrl Pts',(1.75979321359596,-5.18334497568246,31.2264824597427));
#35174=CARTESIAN_POINT('Ctrl Pts',(4.0261898966691,-3.7086024601608,31.3655024552553));
#35175=CARTESIAN_POINT('Ctrl Pts',(5.31016685695979,-1.32893387450125,31.5045224507678));
#35176=CARTESIAN_POINT('Ctrl Pts',(5.29842434414289,1.37500427670065,31.6435424462803));
#35177=CARTESIAN_POINT('Ctrl Pts',(3.99382761705674,3.74343134794615,31.7825624417928));
#35178=CARTESIAN_POINT('Ctrl Pts',(1.71470779963254,5.19843384621083,31.9215824373054));
#35179=CARTESIAN_POINT('Ctrl Pts',(-0.982813236909919,5.38498054155311,
32.0606024328178));
#35180=CARTESIAN_POINT('Ctrl Pts',(-3.44052066988868,4.25755267866645,32.1996224283304));
#35181=CARTESIAN_POINT('Ctrl Pts',(-5.05871594634058,2.09125088542497,32.3386424238428));
#35182=CARTESIAN_POINT('Ctrl Pts',(-5.44254760726829,-0.585331388334223,
32.4776624193555));
#35183=CARTESIAN_POINT('Ctrl Pts',(-4.49835792573859,-3.11908853088459,
32.6166824148679));
#35184=CARTESIAN_POINT('Ctrl Pts',(-2.4565360758811,-4.89176530502493,32.7557024103805));
#35185=CARTESIAN_POINT('Ctrl Pts',(0.184698507257711,-5.47081563872953,
32.8947224058929));
#35186=CARTESIAN_POINT('Ctrl Pts',(2.78086530647299,-4.71494702396602,33.0337424014054));
#35187=CARTESIAN_POINT('Ctrl Pts',(4.69848067279618,-2.80859691997837,33.172762396918));
#35188=CARTESIAN_POINT('Ctrl Pts',(5.46963245977199,-0.216928666984451,
33.3117823924305));
#35189=CARTESIAN_POINT('Ctrl Pts',(4.90615400258152,2.42767176416095,33.4508023879431));
#35190=CARTESIAN_POINT('Ctrl Pts',(3.14553815772543,4.47990256477127,33.5898223834555));
#35191=CARTESIAN_POINT('Ctrl Pts',(0.617388042448883,5.43900443983934,33.728842378968));
#35192=CARTESIAN_POINT('Ctrl Pts',(-2.06140926162863,5.07094953116503,33.8678623744806));
#35193=CARTESIAN_POINT('Ctrl Pts',(-4.237207659215,3.46554592297388,34.0068823699931));
#35194=CARTESIAN_POINT('Ctrl Pts',(-5.37909645969521,1.01452381383852,34.1459023655056));
#35195=CARTESIAN_POINT('Ctrl Pts',(-5.20844646086891,-1.68404951109316,
34.2849223610181));
#35196=CARTESIAN_POINT('Ctrl Pts',(-3.76689750805951,-3.97170246309136,
34.4239423565306));
#35197=CARTESIAN_POINT('Ctrl Pts',(-1.40619806791734,-5.29023102381516,
34.5629623520432));
#35198=CARTESIAN_POINT('Ctrl Pts',(1.29762396492809,-5.31790460023452,34.7019823475557));
#35199=CARTESIAN_POINT('Ctrl Pts',(3.68481627870462,-4.04797063770782,34.8410023430682));
#35200=CARTESIAN_POINT('Ctrl Pts',(5.17288652423882,-1.79030229260299,34.9800223385807));
#35201=CARTESIAN_POINT('Ctrl Pts',(5.39873469988693,0.90421287968471,35.1190423340932));
#35202=CARTESIAN_POINT('Ctrl Pts',(4.30725220227824,3.37809350929193,35.2580623296057));
#35203=CARTESIAN_POINT('Ctrl Pts',(2.1647687277864,5.0276946652267,35.3970823251183));
#35204=CARTESIAN_POINT('Ctrl Pts',(-0.505934117381339,5.45050162465994,
35.5361023206308));
#35205=CARTESIAN_POINT('Ctrl Pts',(-3.05318534499002,4.54334640333416,35.6751223161433));
#35206=CARTESIAN_POINT('Ctrl Pts',(-4.85543706258792,2.52758149676695,35.8141423116559));
#35207=CARTESIAN_POINT('Ctrl Pts',(-5.47292669607204,-0.10493174435301,
35.9531623071683));
#35208=CARTESIAN_POINT('Ctrl Pts',(-4.75498226768737,-2.71184087393226,
36.0921823026809));
#35209=CARTESIAN_POINT('Ctrl Pts',(-2.87678745838508,-4.65704103598298,
36.2312022981934));
#35210=CARTESIAN_POINT('Ctrl Pts',(-0.296635510968414,-5.46588919254529,
36.3702222937059));
#35211=CARTESIAN_POINT('Ctrl Pts',(2.35589766632866,-4.94102048946757,36.5092422892184));
#35212=CARTESIAN_POINT('Ctrl Pts',(4.43357461685579,-3.21050672142625,36.6482622847309));
#35213=CARTESIAN_POINT('Ctrl Pts',(5.4294269992893,-0.696605879202412,36.7872822802435));
#35214=CARTESIAN_POINT('Ctrl Pts',(5.10045956338232,1.98727188221763,36.926302275756));
#35215=CARTESIAN_POINT('Ctrl Pts',(3.52694276469771,4.18624079886686,37.0653222712684));
#35216=CARTESIAN_POINT('Ctrl Pts',(1.09282618754001,5.36373640435264,37.2043422667811));
#35217=CARTESIAN_POINT('Ctrl Pts',(-1.60794795614249,5.23244117615174,37.3433622622934));
#35218=CARTESIAN_POINT('Ctrl Pts',(-3.91637106178054,3.8243921082963,37.4823822578061));
#35219=CARTESIAN_POINT('Ctrl Pts',(-5.26917104193937,1.48316345098525,37.6214022533185));
#35220=CARTESIAN_POINT('Ctrl Pts',(-5.33625482709259,-1.21996791428387,
37.7604222488311));
#35221=CARTESIAN_POINT('Ctrl Pts',(-4.1012534840043,-3.62541820366888,37.8994422443435));
#35222=CARTESIAN_POINT('Ctrl Pts',(-1.86551635491906,-5.14623998867916,
38.0384622398561));
#35223=CARTESIAN_POINT('Ctrl Pts',(0.825420381557286,-5.41134165297858,
38.1774822353686));
#35224=CARTESIAN_POINT('Ctrl Pts',(3.31494852001907,-4.35603645544599,38.3165022308812));
#35225=CARTESIAN_POINT('Ctrl Pts',(4.9956050230993,-2.23782656717092,38.4555222263936));
#35226=CARTESIAN_POINT('Ctrl Pts',(5.45729743658602,0.426429337854175,38.5945422219062));
#35227=CARTESIAN_POINT('Ctrl Pts',(4.58736944159972,2.98663337184665,38.7335622174186));
#35228=CARTESIAN_POINT('Ctrl Pts',(2.59808981870197,4.81807706305204,38.8725822129312));
#35229=CARTESIAN_POINT('Ctrl Pts',(-0.0251426839555714,5.47387478272882,
39.0116022084437));
#35230=CARTESIAN_POINT('Ctrl Pts',(-2.6422401882063,4.79400710047229,39.1506222039563));
#35231=CARTESIAN_POINT('Ctrl Pts',(-4.61461180027545,2.94436669324823,39.2896421994687));
#35232=CARTESIAN_POINT('Ctrl Pts',(-5.46098445006866,0.376279321328379,
39.4286621949813));
#35233=CARTESIAN_POINT('Ctrl Pts',(-4.97483703318683,-2.28362295153644,
39.5676821904938));
#35234=CARTESIAN_POINT('Ctrl Pts',(-3.27479306783995,-4.38630455558871,
39.7067021860063));
#35235=CARTESIAN_POINT('Ctrl Pts',(-0.775675690546239,-5.41869583153057,
39.8457221815188));
#35236=CARTESIAN_POINT('Ctrl Pts',(1.91271221705852,-5.12888577239404,39.9847421770314));
#35237=CARTESIAN_POINT('Ctrl Pts',(4.13438438241777,-3.58759014799223,40.1237621725439));
#35238=CARTESIAN_POINT('Ctrl Pts',(5.34723658073789,-1.17089634091565,40.2627821680564));
#35239=CARTESIAN_POINT('Ctrl Pts',(5.25532402276895,1.53150471995962,40.4018021635689));
#35240=CARTESIAN_POINT('Ctrl Pts',(3.88107404354422,3.86020745039412,40.5408221590814));
#35241=CARTESIAN_POINT('Ctrl Pts',(1.55981366893021,5.24699138647753,40.679842154594));
#35242=CARTESIAN_POINT('Ctrl Pts',(-1.14205262630631,5.35347112538193,40.8188621501064));
#35243=CARTESIAN_POINT('Ctrl Pts',(-3.56524974464505,4.15366483359686,40.957882145619));
#35244=CARTESIAN_POINT('Ctrl Pts',(-5.118499901793,1.94033400395298,41.0969021411315));
#35245=CARTESIAN_POINT('Ctrl Pts',(-5.4227987219109,-0.746452485555846,
41.235922136644));
#35246=CARTESIAN_POINT('Ctrl Pts',(-4.40389507174982,-3.25109912007749,
41.3749421321565));
#35247=CARTESIAN_POINT('Ctrl Pts',(-2.31040887913814,-4.96245383885338,
41.513962127669));
#35248=CARTESIAN_POINT('Ctrl Pts',(0.346833944136911,-5.4629335989691,41.6529821231815));
#35249=CARTESIAN_POINT('Ctrl Pts',(2.91944675342964,-4.63041768585082,41.7920021186941));
#35250=CARTESIAN_POINT('Ctrl Pts',(4.77969324523812,-2.66804605900577,41.9310221142067));
#35251=CARTESIAN_POINT('Ctrl Pts',(5.47365969723602,-0.0546517191416722,
42.070042109719));
#35252=CARTESIAN_POINT('Ctrl Pts',(4.83201322973078,2.57207803910722,42.2090621052317));
#35253=CARTESIAN_POINT('Ctrl Pts',(3.01132026430437,4.57120198168282,42.3480821007441));
#35254=CARTESIAN_POINT('Ctrl Pts',(0.455843174136428,5.45491927457632,42.4871020962567));
#35255=CARTESIAN_POINT('Ctrl Pts',(-2.21086297781468,5.00759644788588,42.6261220917692));
#35256=CARTESIAN_POINT('Ctrl Pts',(-4.33810242563154,3.3383835364261,42.7651420872817));
#35257=CARTESIAN_POINT('Ctrl Pts',(-5.40681321688483,0.854580674524409,
42.9041620827942));
#35258=CARTESIAN_POINT('Ctrl Pts',(-5.156222117767,-1.83774610972284,43.0431820783068));
#35259=CARTESIAN_POINT('Ctrl Pts',(-3.64747518557922,-4.08164942910766,
43.1822020738192));
#35260=CARTESIAN_POINT('Ctrl Pts',(-1.24871768443212,-5.32960049498436,
43.3212220693318));
#35261=CARTESIAN_POINT('Ctrl Pts',(1.45473604636581,-5.27709013822532,43.4602420648443));
#35262=CARTESIAN_POINT('Ctrl Pts',(3.80322356343032,-3.93693126916376,43.5992620603568));
#35263=CARTESIAN_POINT('Ctrl Pts',(5.22369677050014,-1.63613243394826,43.7382820558693));
#35264=CARTESIAN_POINT('Ctrl Pts',(5.36954983672162,1.06389465762065,43.8773020513818));
#35265=CARTESIAN_POINT('Ctrl Pts',(4.20519354932497,3.50432368714232,44.0163220468944));
#35266=CARTESIAN_POINT('Ctrl Pts',(2.014739341313,5.08967215821577,44.1553420424069));
#35267=CARTESIAN_POINT('Ctrl Pts',(-0.667325971979708,5.43310347211171,
44.2943620379194));
#35268=CARTESIAN_POINT('Ctrl Pts',(-3.18655887715868,4.45081788146317,44.4333820334319));
#35269=CARTESIAN_POINT('Ctrl Pts',(-4.92824815695669,2.38250024029464,44.5724020289444));
#35270=CARTESIAN_POINT('Ctrl Pts',(-5.46740891415169,-0.267164849869239,
44.711422024457));
#35271=CARTESIAN_POINT('Ctrl Pts',(-4.67248198854188,-2.85163976657336,
44.8504420199694));
#35272=CARTESIAN_POINT('Ctrl Pts',(-2.73743535231266,-4.74029376552342,
44.989462015482));
#35273=CARTESIAN_POINT('Ctrl Pts',(-0.134434509010523,-5.47228148529823,
45.1284820109945));
#35274=CARTESIAN_POINT('Ctrl Pts',(2.50136933575522,-4.86899257934269,45.267502006507));
#35275=CARTESIAN_POINT('Ctrl Pts',(4.5268208045837,-3.07763394424053,45.4065220020195));
#35276=CARTESIAN_POINT('Ctrl Pts',(5.44769495488841,-0.535310162455436,
45.5455419975321));
#35277=CARTESIAN_POINT('Ctrl Pts',(5.03929177234735,2.1376332063093,45.6845619930446));
#35278=CARTESIAN_POINT('Ctrl Pts',(3.40126461451271,4.28897846970521,45.8235819885571));
#35279=CARTESIAN_POINT('Ctrl Pts',(0.93330406421049,5.39378168035181,45.9626019840697));
#35280=CARTESIAN_POINT('Ctrl Pts',(-1.76238949015754,5.18246279065678,46.101621979582));
#35281=CARTESIAN_POINT('Ctrl Pts',(-4.02804714484456,3.70658515217929,46.2406419750947));
#35282=CARTESIAN_POINT('Ctrl Pts',(-5.31083189470833,1.32627368141911,46.3796619706071));
#35283=CARTESIAN_POINT('Ctrl Pts',(-5.29773489726207,-1.37765824832074,
46.5186819661197));
#35284=CARTESIAN_POINT('Ctrl Pts',(-3.99195191588644,-3.74543150972201,
46.6577019616322));
#35285=CARTESIAN_POINT('Ctrl Pts',(-1.71210352842529,-5.19929214394272,
46.7967219571447));
#35286=CARTESIAN_POINT('Ctrl Pts',(0.985510615947398,-5.38448754457717,
46.9357419526573));
#35287=CARTESIAN_POINT('Ctrl Pts',(3.44265297857929,-4.25582868136,47.0747619481697));
#35288=CARTESIAN_POINT('Ctrl Pts',(5.05976288190223,-2.0887165566579,47.2137819436824));
#35289=CARTESIAN_POINT('Ctrl Pts',(5.44225371738929,0.588057655685179,47.3528019391947));
#35290=CARTESIAN_POINT('Ctrl Pts',(4.49679490684671,3.12134150409286,47.4918219347074));
#35291=CARTESIAN_POINT('Ctrl Pts',(2.4540853449755,4.89299524919655,47.6308419302197));
#35292=CARTESIAN_POINT('Ctrl Pts',(-0.187439010513757,5.47072242481917,
47.7698619257324));
#35293=CARTESIAN_POINT('Ctrl Pts',(-2.78322676887322,4.71355342356861,47.9088819212448));
#35294=CARTESIAN_POINT('Ctrl Pts',(-4.69988709577799,2.80624292960881,48.0479019167574));
#35295=CARTESIAN_POINT('Ctrl Pts',(-5.4697402452394,0.214188779272411,48.1869219122698));
#35296=CARTESIAN_POINT('Ctrl Pts',(-4.90493767108471,-2.43012919530724,
48.3259419077824));
#35297=CARTESIAN_POINT('Ctrl Pts',(-3.14329290057951,-4.4814775203977,48.4649619032949));
#35298=CARTESIAN_POINT('Ctrl Pts',(-0.614664846519301,-5.43931337623658,
48.6039818988075));
#35299=CARTESIAN_POINT('Ctrl Pts',(2.06395202151498,-5.06991558812843,48.7430018943199));
#35300=CARTESIAN_POINT('Ctrl Pts',(4.23893761532058,-3.46342427394386,48.8820218898325));
#35301=CARTESIAN_POINT('Ctrl Pts',(5.37961474807146,-1.01182652793978,49.0210418853449));
#35302=CARTESIAN_POINT('Ctrl Pts',(5.207581217018,1.68665328995466,49.1600618808576));
#35303=CARTESIAN_POINT('Ctrl Pts',(3.76494849337024,3.97359883829332,49.29908187637));
#35304=CARTESIAN_POINT('Ctrl Pts',(1.40346758997053,5.29091540399473,49.4381018718826));
#35305=CARTESIAN_POINT('Ctrl Pts',(-1.30012868543015,5.31729176034627,49.577121867395));
#35306=CARTESIAN_POINT('Ctrl Pts',(-3.68717882655246,4.04604987263071,49.7161418629077));
#35307=CARTESIAN_POINT('Ctrl Pts',(-4.67763208006722,2.54058981104043,49.8088218599159));
#35308=CARTESIAN_POINT('Ctrl Pts',(-4.96294844436203,1.71486069442291,49.8551618584201));
#35309=CARTESIAN_POINT('Ctrl Pts',(2.85652466090568,-4.00304363756816,0.000282215191459768));
#35310=CARTESIAN_POINT('Ctrl Pts',(3.52262641094007,-3.5277224565747,0.0466277630091907));
#35311=CARTESIAN_POINT('Ctrl Pts',(4.61222496132538,-2.23869915929206,0.139313309331095));
#35312=CARTESIAN_POINT('Ctrl Pts',(5.12089807164022,0.242672399523322,0.27833885415717));
#35313=CARTESIAN_POINT('Ctrl Pts',(4.38005472859954,2.66406453636758,0.417358849669687));
#35314=CARTESIAN_POINT('Ctrl Pts',(2.57042906242826,4.43573342696293,0.556378845182204));
#35315=CARTESIAN_POINT('Ctrl Pts',(0.133608302561927,5.12488425088266,0.695398840694722));
#35316=CARTESIAN_POINT('Ctrl Pts',(-2.33581810817467,4.56361121138943,0.83441883620724));
#35317=CARTESIAN_POINT('Ctrl Pts',(-4.23528567670923,2.8887400342109,0.973438831719756));
#35318=CARTESIAN_POINT('Ctrl Pts',(-5.10131373951276,0.509017586705921,
1.11245882723228));
#35319=CARTESIAN_POINT('Ctrl Pts',(-4.72258344381205,-1.99492033515254,
1.2514788227448));
#35320=CARTESIAN_POINT('Ctrl Pts',(-3.19150860899786,-4.01207725856082,
1.39049881825731));
#35321=CARTESIAN_POINT('Ctrl Pts',(-0.881682228353137,-5.05026105603751,
1.52951881376983));
#35322=CARTESIAN_POINT('Ctrl Pts',(1.64328097486816,-4.85614275073615,1.66853880928235));
#35323=CARTESIAN_POINT('Ctrl Pts',(3.76727166488086,-3.47709095838648,1.80755880479487));
#35324=CARTESIAN_POINT('Ctrl Pts',(4.97202055042645,-1.24960318737358,1.94657880030738));
#35325=CARTESIAN_POINT('Ctrl Pts',(4.96356014017646,1.2827966750735,2.0855987958199));
#35326=CARTESIAN_POINT('Ctrl Pts',(3.74395482038217,3.50218489166088,2.22461879133242));
#35327=CARTESIAN_POINT('Ctrl Pts',(1.61079719922008,4.86701437706966,2.36363878684493));
#35328=CARTESIAN_POINT('Ctrl Pts',(-0.915406697482164,5.04425685701712,
2.50265878235745));
#35329=CARTESIAN_POINT('Ctrl Pts',(-3.21824467754449,3.99066383048563,2.64167877786997));
#35330=CARTESIAN_POINT('Ctrl Pts',(-4.73580746601471,1.96331970795363,2.78069877338249));
#35331=CARTESIAN_POINT('Ctrl Pts',(-5.09779866494969,-0.543088757747706,
2.91971876889501));
#35332=CARTESIAN_POINT('Ctrl Pts',(-4.21588977984263,-2.91697960051942,
3.05873876440752));
#35333=CARTESIAN_POINT('Ctrl Pts',(-2.30527301575098,-4.57910613010975,
3.19775875992004));
#35334=CARTESIAN_POINT('Ctrl Pts',(0.167847190824738,-5.12389733960339,
3.33677875543256));
#35335=CARTESIAN_POINT('Ctrl Pts',(2.60001145770063,-4.41842019810271,3.47579875094507));
#35336=CARTESIAN_POINT('Ctrl Pts',(4.39775395086801,-2.63481627716698,3.61481874645759));
#35337=CARTESIAN_POINT('Ctrl Pts',(5.12241237990866,-0.208297952599817,
3.75383874197011));
#35338=CARTESIAN_POINT('Ctrl Pts',(4.59716479869933,2.26904659284643,3.89285873748263));
#35339=CARTESIAN_POINT('Ctrl Pts',(2.9501754509488,4.19272720737859,4.03187873299514));
#35340=CARTESIAN_POINT('Ctrl Pts',(0.583321759223736,5.09335177973389,4.17089872850766));
#35341=CARTESIAN_POINT('Ctrl Pts',(-1.92586669953822,4.7511613403983,4.30991872402018));
#35342=CARTESIAN_POINT('Ctrl Pts',(-3.96512962631244,3.24965285429574,4.44893871953269));
#35343=CARTESIAN_POINT('Ctrl Pts',(-5.03687198196272,0.955205351853525,
4.58795871504521));
#35344=CARTESIAN_POINT('Ctrl Pts',(-4.87958080884073,-1.57231922868232,
4.72697871055773));
#35345=CARTESIAN_POINT('Ctrl Pts',(-3.53163630128907,-3.7161864407358,4.86599870607025));
#35346=CARTESIAN_POINT('Ctrl Pts',(-1.32194675807696,-4.9532770360339,5.00501870158276));
#35347=CARTESIAN_POINT('Ctrl Pts',(1.21030744326956,-4.98173187954325,5.14403869709529));
#35348=CARTESIAN_POINT('Ctrl Pts',(3.44723779417319,-3.79460778174965,5.2830586926078));
#35349=CARTESIAN_POINT('Ctrl Pts',(4.84301696119486,-1.68157168757982,5.42207868812032));
#35350=CARTESIAN_POINT('Ctrl Pts',(5.05706463949957,0.841780172500049,5.56109868363283));
#35351=CARTESIAN_POINT('Ctrl Pts',(4.03715163320258,3.1597315261618,5.70011867914535));
#35352=CARTESIAN_POINT('Ctrl Pts',(2.03214416039696,4.70668532390425,5.83913867465787));
#35353=CARTESIAN_POINT('Ctrl Pts',(-0.468721320587276,5.10517354754156,
5.97815867017038));
#35354=CARTESIAN_POINT('Ctrl Pts',(-2.85521537805407,4.25796216185801,6.11717866568291));
#35355=CARTESIAN_POINT('Ctrl Pts',(-4.54501604246637,2.37177692893208,6.25619866119542));
#35356=CARTESIAN_POINT('Ctrl Pts',(-5.125799617502,-0.0931391867450908,
6.39521865670794));
#35357=CARTESIAN_POINT('Ctrl Pts',(-4.45585067159246,-2.5353286610142,6.53423865222046));
#35358=CARTESIAN_POINT('Ctrl Pts',(-2.69864163763604,-4.35887943610605,
6.67325864773297));
#35359=CARTESIAN_POINT('Ctrl Pts',(-0.282944346151318,-5.11883181242284,
6.81227864324549));
#35360=CARTESIAN_POINT('Ctrl Pts',(2.2017934310638,-4.62975186309325,6.95129863875801));
#35361=CARTESIAN_POINT('Ctrl Pts',(4.14927753975237,-3.0109786656497,7.09031863427053));
#35362=CARTESIAN_POINT('Ctrl Pts',(5.08430764230391,-0.657504696029762,
7.22933862978304));
#35363=CARTESIAN_POINT('Ctrl Pts',(4.77872956871716,1.8564052186846,7.36835862529557));
#35364=CARTESIAN_POINT('Ctrl Pts',(3.30710659942503,3.91733870975315,7.50737862080806));
#35365=CARTESIAN_POINT('Ctrl Pts',(1.02852548061614,5.02241296217411,7.6463986163206));
#35366=CARTESIAN_POINT('Ctrl Pts',(-1.50102336288394,4.90198179219056,7.78541861183311));
#35367=CARTESIAN_POINT('Ctrl Pts',(-3.66431154955944,3.58543128433058,7.92443860734562));
#35368=CARTESIAN_POINT('Ctrl Pts',(-4.93348097157235,1.39400937228727,8.06345860285816));
#35369=CARTESIAN_POINT('Ctrl Pts',(-4.99884502602062,-1.13756100175772,
8.20247859837064));
#35370=CARTESIAN_POINT('Ctrl Pts',(-3.8444544065131,-3.39155818808009,8.34149859388319));
#35371=CARTESIAN_POINT('Ctrl Pts',(-1.7519888503462,-4.8179904208242,8.4805185893957));
#35372=CARTESIAN_POINT('Ctrl Pts',(0.767974773435199,-5.0687978233757,8.61953858490822));
#35373=CARTESIAN_POINT('Ctrl Pts',(3.10054694689124,-4.08278155881679,8.75855858042073));
#35374=CARTESIAN_POINT('Ctrl Pts',(4.6765630337705,-2.10053679283709,8.89757857593325));
#35375=CARTESIAN_POINT('Ctrl Pts',(5.11146360520611,0.394254282848632,9.03659857144578));
#35376=CARTESIAN_POINT('Ctrl Pts',(4.29912974733827,2.79284443577551,9.17561856695828));
#35377=CARTESIAN_POINT('Ctrl Pts',(2.43777685088012,4.50996016082228,9.3146385624708));
#35378=CARTESIAN_POINT('Ctrl Pts',(-0.018411391031715,5.1266126874937,9.45365855798332));
#35379=CARTESIAN_POINT('Ctrl Pts',(-2.47010711914323,4.49233429820722,9.59267855349584));
#35380=CARTESIAN_POINT('Ctrl Pts',(-4.31907868035958,2.76189354967829,9.73169854900835));
#35381=CARTESIAN_POINT('Ctrl Pts',(-5.11416351771696,0.357530615393925,
9.87071854452088));
#35382=CARTESIAN_POINT('Ctrl Pts',(-4.66135512741105,-2.13407239873668,
10.0097385400333));
#35383=CARTESIAN_POINT('Ctrl Pts',(-3.07114206181887,-4.10494617053842,
10.1487585355459));
#35384=CARTESIAN_POINT('Ctrl Pts',(-0.731547916239905,-5.0741831138752,
10.2877785310584));
#35385=CARTESIAN_POINT('Ctrl Pts',(1.78654926062158,-4.80528233991131,10.4267985265709));
#35386=CARTESIAN_POINT('Ctrl Pts',(3.86871537749776,-3.36385760025652,10.5658185220834));
#35387=CARTESIAN_POINT('Ctrl Pts',(5.00688670370844,-1.10162705264471,10.704838517596));
#35388=CARTESIAN_POINT('Ctrl Pts',(4.92334112790964,1.42940853681676,10.8438585131084));
#35389=CARTESIAN_POINT('Ctrl Pts',(3.63846438041272,3.61165800974553,10.982878508621));
#35390=CARTESIAN_POINT('Ctrl Pts',(1.46577576618884,4.9126365660554,11.1218985041335));
#35391=CARTESIAN_POINT('Ctrl Pts',(-1.06457283398646,5.01489594189442,11.260918499646));
#35392=CARTESIAN_POINT('Ctrl Pts',(-3.33515789213115,3.89348410314547,11.3999384951585));
#35393=CARTESIAN_POINT('Ctrl Pts',(-4.79194008058653,1.82203372388092,11.538958490671));
#35394=CARTESIAN_POINT('Ctrl Pts',(-5.07945391201418,-0.694006183412673,
11.6779784861835));
#35395=CARTESIAN_POINT('Ctrl Pts',(-4.1275439129226,-3.04070351625848,11.8169984816961));
#35396=CARTESIAN_POINT('Ctrl Pts',(-2.1684830712787,-4.64544699641152,11.9560184772086));
#35397=CARTESIAN_POINT('Ctrl Pts',(0.31970346796494,-5.11666750135889,12.0950384727211));
#35398=CARTESIAN_POINT('Ctrl Pts',(2.72988002744322,-4.33938378835726,12.2340584682336));
#35399=CARTESIAN_POINT('Ctrl Pts',(4.47394593426475,-2.50325875693404,12.3730784637462));
#35400=CARTESIAN_POINT('Ctrl Pts',(5.12633637686628,-0.056320317013998,
12.5120984592586));
#35401=CARTESIAN_POINT('Ctrl Pts',(4.52786332531986,2.40436069135114,12.6511184547712));
#35402=CARTESIAN_POINT('Ctrl Pts',(2.82455857258174,4.27836014109916,12.7901384502837));
#35403=CARTESIAN_POINT('Ctrl Pts',(0.432040911094763,5.10840848778086,12.9291584457962));
#35404=CARTESIAN_POINT('Ctrl Pts',(-2.06589788625557,4.69196787611082,13.0681784413087));
#35405=CARTESIAN_POINT('Ctrl Pts',(-4.05974251994234,3.13065285502295,13.2071984368212));
#35406=CARTESIAN_POINT('Ctrl Pts',(-5.06298034586039,0.805435686024888,
13.3462184323338));
#35407=CARTESIAN_POINT('Ctrl Pts',(-4.83081401164476,-1.71631366940539,
13.4852384278463));
#35408=CARTESIAN_POINT('Ctrl Pts',(-3.41989379747425,-3.81926996177125,
13.6242584233588));
#35409=CARTESIAN_POINT('Ctrl Pts',(-1.1744945342058,-4.99029650582126,13.7632784188713));
#35410=CARTESIAN_POINT('Ctrl Pts',(1.35748996828809,-4.94365427724152,13.9022984143838));
#35411=CARTESIAN_POINT('Ctrl Pts',(3.55823700991883,-3.6907243202568,14.0413184098964));
#35412=CARTESIAN_POINT('Ctrl Pts',(4.89074824881934,-1.53723068976704,14.1803384054088));
#35413=CARTESIAN_POINT('Ctrl Pts',(5.02988121642198,0.991358449591552,14.3193584009214));
#35414=CARTESIAN_POINT('Ctrl Pts',(3.94168645307127,3.27804889111885,14.4583783964339));
#35415=CARTESIAN_POINT('Ctrl Pts',(1.89169142398414,4.76487147605431,14.5973983919464));
#35416=CARTESIAN_POINT('Ctrl Pts',(-0.619890120403223,5.08903064104723,
14.7364183874589));
#35417=CARTESIAN_POINT('Ctrl Pts',(-2.98021395070562,4.17142918373435,14.8754383829715));
#35418=CARTESIAN_POINT('Ctrl Pts',(-4.61334382383605,2.2359685574634,15.014458378484));
#35419=CARTESIAN_POINT('Ctrl Pts',(-5.12078413019695,-0.245084717626975,
15.1534783739965));
#35420=CARTESIAN_POINT('Ctrl Pts',(-4.37871573112417,-2.66633553269217,
15.292498369509));
#35421=CARTESIAN_POINT('Ctrl Pts',(-2.5682087325027,-4.4369810156443,15.4315183650215));
#35422=CARTESIAN_POINT('Ctrl Pts',(-0.131040057262327,-5.12497074433441,
15.570538360534));
#35423=CARTESIAN_POINT('Ctrl Pts',(2.33810334843862,-4.56243020318243,15.7095583560466));
#35424=CARTESIAN_POINT('Ctrl Pts',(4.23673247081922,-2.88662339032947,15.8485783515591));
#35425=CARTESIAN_POINT('Ctrl Pts',(5.1015679455308,-0.506459400173185,15.9875983470716));
#35426=CARTESIAN_POINT('Ctrl Pts',(4.72158360413018,1.99728438037758,16.1266183425841));
#35427=CARTESIAN_POINT('Ctrl Pts',(3.18949839950364,4.01367619352319,16.2656383380966));
#35428=CARTESIAN_POINT('Ctrl Pts',(0.879152304587834,5.05070171879402,16.4046583336091));
#35429=CARTESIAN_POINT('Ctrl Pts',(-1.64571336976244,4.85531915855964,16.5436783291217));
#35430=CARTESIAN_POINT('Ctrl Pts',(-3.76901296948745,3.475203283655,16.6826983246342));
#35431=CARTESIAN_POINT('Ctrl Pts',(-4.97264589385004,1.24711244130889,16.8217183201467));
#35432=CARTESIAN_POINT('Ctrl Pts',(-4.96291692373935,-1.28528293964901,
16.9607383156592));
#35433=CARTESIAN_POINT('Ctrl Pts',(-3.74219999887612,-3.50405990178573,
17.0997583111718));
#35434=CARTESIAN_POINT('Ctrl Pts',(-1.60835895919313,-4.86782067102664,
17.2387783066842));
#35435=CARTESIAN_POINT('Ctrl Pts',(0.91793340627866,-5.04379766530427,17.3777983021968));
#35436=CARTESIAN_POINT('Ctrl Pts',(3.22024332043214,-3.98905121352225,17.5168182977093));
#35437=CARTESIAN_POINT('Ctrl Pts',(4.7367903591762,-1.96094714872851,17.6558382932218));
#35438=CARTESIAN_POINT('Ctrl Pts',(5.09752597546587,0.545642333714995,17.7948582887343));
#35439=CARTESIAN_POINT('Ctrl Pts',(4.21442804584234,2.91909110397544,17.9338782842469));
#35440=CARTESIAN_POINT('Ctrl Pts',(2.30297891104881,4.58026033781438,18.0728982797593));
#35441=CARTESIAN_POINT('Ctrl Pts',(-0.170413887961411,5.12381261695634,
18.2119182752719));
#35442=CARTESIAN_POINT('Ctrl Pts',(-2.60222445442275,4.41711721778983,18.3509382707844));
#35443=CARTESIAN_POINT('Ctrl Pts',(-4.39907325982889,2.63261297602774,18.4899582662969));
#35444=CARTESIAN_POINT('Ctrl Pts',(-5.12251608008851,0.205731952126684,
18.6289782618094));
#35445=CARTESIAN_POINT('Ctrl Pts',(-4.59602758649907,-2.27134916977346,
18.767998257322));
#35446=CARTESIAN_POINT('Ctrl Pts',(-2.94807481444516,-4.19420451520013,
18.9070182528345));
#35447=CARTESIAN_POINT('Ctrl Pts',(-0.580770269057073,-5.09364334454921,
19.046038248347));
#35448=CARTESIAN_POINT('Ctrl Pts',(1.92824646114365,-4.75019601826895,19.1850582438595));
#35449=CARTESIAN_POINT('Ctrl Pts',(3.96675698015443,-3.24766619086495,19.324078239372));
#35450=CARTESIAN_POINT('Ctrl Pts',(5.03734984182548,-0.952682107500701,
19.4630982348845));
#35451=CARTESIAN_POINT('Ctrl Pts',(4.87879257342969,1.57476336391802,19.602118230397));
#35452=CARTESIAN_POINT('Ctrl Pts',(3.52977430579807,3.71795508001628,19.7411382259096));
#35453=CARTESIAN_POINT('Ctrl Pts',(1.31946534299687,4.95393861846523,19.8801582214221));
#35454=CARTESIAN_POINT('Ctrl Pts',(-1.2128027945468,4.9811249741831,20.0191782169346));
#35455=CARTESIAN_POINT('Ctrl Pts',(-3.44913819772191,3.79288047793584,20.1581982124471));
#35456=CARTESIAN_POINT('Ctrl Pts',(-4.84385870467769,1.67914546005085,20.2972182079597));
#35457=CARTESIAN_POINT('Ctrl Pts',(-5.05664233136262,-0.844313306517566,
20.4362382034721));
#35458=CARTESIAN_POINT('Ctrl Pts',(-4.03556831971381,-3.16175346347771,
20.5752581989847));
#35459=CARTESIAN_POINT('Ctrl Pts',(-2.02978618160459,-4.70770269705492,
20.7142781944972));
#35460=CARTESIAN_POINT('Ctrl Pts',(0.471278600646567,-5.10493811005225,
20.8532981900097));
#35461=CARTESIAN_POINT('Ctrl Pts',(2.85734796437971,-4.2565313621946,20.9923181855222));
#35462=CARTESIAN_POINT('Ctrl Pts',(4.5462035684287,-2.36949989265611,21.1313381810348));
#35463=CARTESIAN_POINT('Ctrl Pts',(5.12575231809818,0.0957068461616923,
21.2703581765473));
#35464=CARTESIAN_POINT('Ctrl Pts',(4.4545800882223,2.53756041593189,21.4093781720598));
#35465=CARTESIAN_POINT('Ctrl Pts',(2.69645780191612,4.36023072203488,21.5483981675723));
#35466=CARTESIAN_POINT('Ctrl Pts',(0.280380129937561,5.11897290573287,21.6874181630848));
#35467=CARTESIAN_POINT('Ctrl Pts',(-2.20411234029851,4.62864833598698,21.8264381585973));
#35468=CARTESIAN_POINT('Ctrl Pts',(-4.15078531122857,3.00889978679588,21.9654581541098));
#35469=CARTESIAN_POINT('Ctrl Pts',(-5.08463636877582,0.654957727042922,
22.1044781496224));
#35470=CARTESIAN_POINT('Ctrl Pts',(-4.77779903852622,-1.8587987987808,22.2434981451349));
#35471=CARTESIAN_POINT('Ctrl Pts',(-3.30514386873,-3.918994849944,22.3825181406474));
#35472=CARTESIAN_POINT('Ctrl Pts',(-1.02600947003294,-5.02292755216456,
22.5215381361599));
#35473=CARTESIAN_POINT('Ctrl Pts',(1.50347872840812,-4.90122926826684,22.6605581316724));
#35474=CARTESIAN_POINT('Ctrl Pts',(3.6661071429145,-3.58359526782287,22.799578127185));
#35475=CARTESIAN_POINT('Ctrl Pts',(4.93417865487318,-1.39153786462493,22.9385981226975));
#35476=CARTESIAN_POINT('Ctrl Pts',(4.99827455944932,1.140064934665,23.07761811821));
#35477=CARTESIAN_POINT('Ctrl Pts',(3.84275498807705,3.39348356832622,23.2166381137225));
#35478=CARTESIAN_POINT('Ctrl Pts',(1.74957515054818,4.8188674415754,23.355658109235));
#35479=CARTESIAN_POINT('Ctrl Pts',(-0.770513794226398,5.06841248516712,
23.4946781047475));
#35480=CARTESIAN_POINT('Ctrl Pts',(-3.10259174906973,4.08122788698396,23.6336981002601));
#35481=CARTESIAN_POINT('Ctrl Pts',(-4.67761467067925,2.09819389464779,23.7727180957726));
#35482=CARTESIAN_POINT('Ctrl Pts',(-5.11126546976328,-0.39681472313488,
23.9117380912851));
#35483=CARTESIAN_POINT('Ctrl Pts',(-4.29773018603819,-2.79499765203967,
24.0507580867976));
#35484=CARTESIAN_POINT('Ctrl Pts',(-2.43551736689566,-4.51118075257917,
24.1897780823101));
#35485=CARTESIAN_POINT('Ctrl Pts',(0.0209794671159091,-5.12660282144528,
24.3287980778226));
#35486=CARTESIAN_POINT('Ctrl Pts',(2.47235715801771,-4.4910963817413,24.4678180733352));
#35487=CARTESIAN_POINT('Ctrl Pts',(4.32046165611542,-2.75972964344834,24.6068380688477));
#35488=CARTESIAN_POINT('Ctrl Pts',(5.11434197417513,-0.354968728314899,
24.7458580643602));
#35489=CARTESIAN_POINT('Ctrl Pts',(4.66028551989319,2.13640714751776,24.8848780598727));
#35490=CARTESIAN_POINT('Ctrl Pts',(3.06908538236661,4.10648408527718,25.0238980553852));
#35491=CARTESIAN_POINT('Ctrl Pts',(0.729006009651713,5.07454893214982,25.1629180508977));
#35492=CARTESIAN_POINT('Ctrl Pts',(-1.78895615058429,4.80438679939259,25.3019380464103));
#35493=CARTESIAN_POINT('Ctrl Pts',(-3.87039995211566,3.36191921936774,25.4409580419228));
#35494=CARTESIAN_POINT('Ctrl Pts',(-5.00743791447871,1.09911881047142,25.5799780374353));
#35495=CARTESIAN_POINT('Ctrl Pts',(-4.92262447538095,-1.43187461087609,
25.7189980329478));
#35496=CARTESIAN_POINT('Ctrl Pts',(-3.63665473303307,-3.61348017562008,
25.8580180284603));
#35497=CARTESIAN_POINT('Ctrl Pts',(-1.46331469112785,-4.91337020197141,
25.9970380239728));
#35498=CARTESIAN_POINT('Ctrl Pts',(1.06708481645005,-5.0143620353334,26.1360580194854));
#35499=CARTESIAN_POINT('Ctrl Pts',(3.33710783994068,-3.89181293120539,26.2750780149979));
#35500=CARTESIAN_POINT('Ctrl Pts',(4.79285219224344,-1.81963306471342,26.4140980105104));
#35501=CARTESIAN_POINT('Ctrl Pts',(5.07910562561647,0.696550551447801,26.5531180060229));
#35502=CARTESIAN_POINT('Ctrl Pts',(4.12602021289356,3.04277074878882,26.6921380015354));
#35503=CARTESIAN_POINT('Ctrl Pts',(2.1661557515472,4.64653267361053,26.831157997048));
#35504=CARTESIAN_POINT('Ctrl Pts',(-0.322266524396859,5.11650671006541,
26.9701779925605));
#35505=CARTESIAN_POINT('Ctrl Pts',(-2.73205341609784,4.33801576282051,27.109197988073));
#35506=CARTESIAN_POINT('Ctrl Pts',(-4.47519933244633,2.50101730537053,27.2482179835855));
#35507=CARTESIAN_POINT('Ctrl Pts',(-5.12636394626974,0.0537523699660611,
27.387237979098));
#35508=CARTESIAN_POINT('Ctrl Pts',(-4.52665833880949,-2.40662853605985,
27.5262579746105));
#35509=CARTESIAN_POINT('Ctrl Pts',(-2.82241505566153,-4.27977451280629,
27.6652779701231));
#35510=CARTESIAN_POINT('Ctrl Pts',(-0.429481897539188,-5.10862426946603,
27.8042979656356));
#35511=CARTESIAN_POINT('Ctrl Pts',(2.06824797846015,-4.6909324154678,27.9433179611481));
#35512=CARTESIAN_POINT('Ctrl Pts',(4.06131025114418,-3.1286188120067,28.0823379566606));
#35513=CARTESIAN_POINT('Ctrl Pts',(5.06338317820308,-0.802899381978309,
28.2213579521732));
#35514=CARTESIAN_POINT('Ctrl Pts',(4.82995365109632,1.71873335778196,28.3603779476856));
#35515=CARTESIAN_POINT('Ctrl Pts',(3.41798017828845,3.82098261285214,28.4993979431982));
#35516=CARTESIAN_POINT('Ctrl Pts',(1.17199459343186,4.9908842202417,28.6384179387107));
#35517=CARTESIAN_POINT('Ctrl Pts',(-1.35996622685374,4.94297364839307,28.7774379342232));
#35518=CARTESIAN_POINT('Ctrl Pts',(-3.5600853611114,3.68894142654656,28.9164579297357));
#35519=CARTESIAN_POINT('Ctrl Pts',(-4.89151768145639,1.53478057027402,29.0554779252482));
#35520=CARTESIAN_POINT('Ctrl Pts',(-5.0293839833238,-0.993877947827136,
29.1944979207607));
#35521=CARTESIAN_POINT('Ctrl Pts',(-3.94004388274326,-3.28002299213719,
29.3335179162733));
#35522=CARTESIAN_POINT('Ctrl Pts',(-1.88930431557573,-4.76581848479756,
29.4725379117858));
#35523=CARTESIAN_POINT('Ctrl Pts',(0.622439295016351,-5.08871948046958,
29.6115579072983));
#35524=CARTESIAN_POINT('Ctrl Pts',(2.9823031743109,-4.169935779288,29.7505779028108));
#35525=CARTESIAN_POINT('Ctrl Pts',(4.6144633106241,-2.23365731073393,29.8895978983234));
#35526=CARTESIAN_POINT('Ctrl Pts',(5.12066071722015,0.247649845567273,30.0286178938358));
#35527=CARTESIAN_POINT('Ctrl Pts',(4.37737953204971,2.6685286319025,30.1676378893484));
#35528=CARTESIAN_POINT('Ctrl Pts',(2.5659857896579,4.43826695390947,30.3066578848609));
#35529=CARTESIAN_POINT('Ctrl Pts',(0.128472784927027,5.12503574333136,30.4456778803734));
#35530=CARTESIAN_POINT('Ctrl Pts',(-2.34038851707551,4.56125840268145,30.5846978758859));
#35531=CARTESIAN_POINT('Ctrl Pts',(-4.2381779379304,2.88450071820604,30.7237178713985));
#35532=CARTESIAN_POINT('Ctrl Pts',(-5.10182100659037,0.503903803919262,
30.8627378669109));
#35533=CARTESIAN_POINT('Ctrl Pts',(-4.72058251039248,-1.99964931662224,
31.0017578624235));
#35534=CARTESIAN_POINT('Ctrl Pts',(-3.18748742514785,-4.01527340805273,
31.140777857936));
#35535=CARTESIAN_POINT('Ctrl Pts',(-0.876622142035253,-5.05114147960484,
31.2797978534485));
#35536=CARTESIAN_POINT('Ctrl Pts',(1.64814534238077,-4.85449416080395,31.418817848961));
#35537=CARTESIAN_POINT('Ctrl Pts',(3.77075333310117,-3.47331483280705,31.5578378444735));
#35538=CARTESIAN_POINT('Ctrl Pts',(4.97326998703416,-1.24462133315979,31.6968578399861));
#35539=CARTESIAN_POINT('Ctrl Pts',(4.96227246320154,1.28776885652777,31.8358778354985));
#35540=CARTESIAN_POINT('Ctrl Pts',(3.74044423769168,3.50593404553055,31.9748978310111));
#35541=CARTESIAN_POINT('Ctrl Pts',(1.60592031590668,4.86862573688399,32.1139178265236));
#35542=CARTESIAN_POINT('Ctrl Pts',(-0.920459884905055,5.0433372113286,32.2529378220362));
#35543=CARTESIAN_POINT('Ctrl Pts',(-3.22224115517232,3.98743759384455,32.3919578175486));
#35544=CARTESIAN_POINT('Ctrl Pts',(-4.73777206377099,1.95857409832829,32.5309778130612));
#35545=CARTESIAN_POINT('Ctrl Pts',(-5.09725200682841,-0.548195773218716,
32.6699978085737));
#35546=CARTESIAN_POINT('Ctrl Pts',(-4.21296525431996,-2.92120187470564,
32.8090178040862));
#35547=CARTESIAN_POINT('Ctrl Pts',(-2.3006842284502,-4.58141339630595,32.9480377995987));
#35548=CARTESIAN_POINT('Ctrl Pts',(0.172980542332811,-5.12372660852091,
33.0870577951112));
#35549=CARTESIAN_POINT('Ctrl Pts',(2.6044367981658,-4.41581312911349,33.2260777906237));
#35550=CARTESIAN_POINT('Ctrl Pts',(4.40039146492194,-2.6304090142663,33.3650977861363));
#35551=CARTESIAN_POINT('Ctrl Pts',(5.12261849486698,-0.203165900037072,
33.5041177816488));
#35552=CARTESIAN_POINT('Ctrl Pts',(4.59488922100946,2.2736511767512,33.6431377771613));
#35553=CARTESIAN_POINT('Ctrl Pts',(2.94597343817613,4.19568077056057,33.7821577726738));
#35554=CARTESIAN_POINT('Ctrl Pts',(0.578218633156638,5.09393363120894,33.9211777681863));
#35555=CARTESIAN_POINT('Ctrl Pts',(-1.93062573889086,4.74922950416415,34.0601977636989));
#35556=CARTESIAN_POINT('Ctrl Pts',(-3.9683833386113,3.24567871249196,34.1992177592113));
#35557=CARTESIAN_POINT('Ctrl Pts',(-5.03782643765737,0.950158624089521,
34.3382377547239));
#35558=CARTESIAN_POINT('Ctrl Pts',(-4.87800311377481,-1.57720710399561,
34.4772577502364));
#35559=CARTESIAN_POINT('Ctrl Pts',(-3.52791142457468,-3.71972278634396,
34.6162777457489));
#35560=CARTESIAN_POINT('Ctrl Pts',(-1.31698359682106,-4.95459895779621,
34.7552977412614));
#35561=CARTESIAN_POINT('Ctrl Pts',(1.21529784149338,-4.98051681890069,34.894317736774));
#35562=CARTESIAN_POINT('Ctrl Pts',(3.45103773577246,-3.79115222236799,35.0333377322865));
#35563=CARTESIAN_POINT('Ctrl Pts',(4.84469923268273,-1.67671881117096,35.172357727799));
#35564=CARTESIAN_POINT('Ctrl Pts',(5.05621875435371,0.846846228670134,35.3113777233115));
#35565=CARTESIAN_POINT('Ctrl Pts',(4.03398399357292,3.1637746074094,35.450397718824));
#35566=CARTESIAN_POINT('Ctrl Pts',(2.02742769347443,4.70871888889366,35.5894177143365));
#35567=CARTESIAN_POINT('Ctrl Pts',(-0.473835762447141,5.10470139157202,
35.7284377098491));
#35568=CARTESIAN_POINT('Ctrl Pts',(-2.85947983370614,4.25509949443244,35.8674577053615));
#35569=CARTESIAN_POINT('Ctrl Pts',(-4.54738995360437,2.36722226179743,36.0064777008742));
#35570=CARTESIAN_POINT('Ctrl Pts',(-5.1257037324805,-0.0982744815624442,
36.1454976963866));
#35571=CARTESIAN_POINT('Ctrl Pts',(-4.45330838705666,-2.53979153409525,
36.2845176918992));
#35572=CARTESIAN_POINT('Ctrl Pts',(-2.6942732895693,-4.36158091384358,36.4235376874117));
#35573=CARTESIAN_POINT('Ctrl Pts',(-0.277815843367409,-5.11911271453023,
36.5625576829242));
#35574=CARTESIAN_POINT('Ctrl Pts',(2.2064306964516,-4.62754364740596,36.7015776784367));
#35575=CARTESIAN_POINT('Ctrl Pts',(4.15229204114108,-3.00682015291364,36.8405976739492));
#35576=CARTESIAN_POINT('Ctrl Pts',(5.0849638193512,-0.652410593706373,36.9796176694617));
#35577=CARTESIAN_POINT('Ctrl Pts',(4.77686730943394,1.86119191244549,37.1186376649743));
#35578=CARTESIAN_POINT('Ctrl Pts',(3.30318030866942,3.92065000673483,37.2576576604868));
#35579=CARTESIAN_POINT('Ctrl Pts',(1.02349320199129,5.02344088174318,37.3966776559993));
#35580=CARTESIAN_POINT('Ctrl Pts',(-1.50593371666188,4.9004755144692,37.5356976515118));
#35581=CARTESIAN_POINT('Ctrl Pts',(-3.66790181632699,3.58175835207742,37.6747176470243));
#35582=CARTESIAN_POINT('Ctrl Pts',(-4.9348751000321,1.38906600778156,37.8137376425368));
#35583=CARTESIAN_POINT('Ctrl Pts',(-4.9977028386524,-1.1425685814939,37.9527576380494));
#35584=CARTESIAN_POINT('Ctrl Pts',(-3.84105460537178,-3.39540809703979,
38.0917776335618));
#35585=CARTESIAN_POINT('Ctrl Pts',(-1.74716101172614,-4.81974325311994,
38.2307976290744));
#35586=CARTESIAN_POINT('Ctrl Pts',(0.773052621671329,-5.06802587513306,
38.3698176245869));
#35587=CARTESIAN_POINT('Ctrl Pts',(3.10463577270955,-4.07967319104157,38.5088376200994));
#35588=CARTESIAN_POINT('Ctrl Pts',(4.67866513382612,-2.09585046995506,38.6478576156119));
#35589=CARTESIAN_POINT('Ctrl Pts',(5.11106605174182,0.39937506384781,38.7868776111245));
#35590=CARTESIAN_POINT('Ctrl Pts',(4.29632954630119,2.79715016695038,38.925897606637));
#35591=CARTESIAN_POINT('Ctrl Pts',(2.43325727176251,4.51240021233776,39.0649176021495));
#35592=CARTESIAN_POINT('Ctrl Pts',(-0.0235475379357751,5.12659166896957,
39.203937597662));
#35593=CARTESIAN_POINT('Ctrl Pts',(-2.47460657649937,4.48985733831679,39.3429575931745));
#35594=CARTESIAN_POINT('Ctrl Pts',(-4.3218435477304,2.75756504471465,39.481977588687));
#35595=CARTESIAN_POINT('Ctrl Pts',(-5.11451914728269,0.352406752162877,
39.6209975841996));
#35596=CARTESIAN_POINT('Ctrl Pts',(-4.6592147429618,-2.13874136020663,39.7600175797121));
#35597=CARTESIAN_POINT('Ctrl Pts',(-3.06702793278336,-4.10802096956888,
39.8990375752246));
#35598=CARTESIAN_POINT('Ctrl Pts',(-0.726463920132707,-5.07491347705914,
40.0380575707372));
#35599=CARTESIAN_POINT('Ctrl Pts',(1.79136259164118,-4.8034900533008,40.1770775662496));
#35600=CARTESIAN_POINT('Ctrl Pts',(3.87208355552747,-3.35997999486676,40.3160975617622));
#35601=CARTESIAN_POINT('Ctrl Pts',(5.007987868724,-1.09661029249428,40.4551175572747));
#35602=CARTESIAN_POINT('Ctrl Pts',(4.92190658760959,1.4343403256328,40.5941375527873));
#35603=CARTESIAN_POINT('Ctrl Pts',(3.6348441731013,3.61530143475791,40.7331575482997));
#35604=CARTESIAN_POINT('Ctrl Pts',(1.46085324887469,4.91410260496699,40.8721775438122));
#35605=CARTESIAN_POINT('Ctrl Pts',(-1.06959653114824,5.01382687050987,41.0111975393247));
#35606=CARTESIAN_POINT('Ctrl Pts',(-3.33905695036404,3.89014078268597,41.1502175348373));
#35607=CARTESIAN_POINT('Ctrl Pts',(-4.79376310122173,1.81723194894219,41.2892375303498));
#35608=CARTESIAN_POINT('Ctrl Pts',(-5.07875606471003,-0.699094744696433,
41.4282575258623));
#35609=CARTESIAN_POINT('Ctrl Pts',(-4.12449547751508,-3.04483721779157,
41.5672775213748));
#35610=CARTESIAN_POINT('Ctrl Pts',(-2.16382788825841,-4.64761718484712,
41.7062975168873));
#35611=CARTESIAN_POINT('Ctrl Pts',(0.324829499961922,-5.11634463487808,
41.8453175123999));
#35612=CARTESIAN_POINT('Ctrl Pts',(2.73422611919363,-4.33664664873797,41.9843375079123));
#35613=CARTESIAN_POINT('Ctrl Pts',(4.47645160765851,-2.49877522622239,42.1233575034249));
#35614=CARTESIAN_POINT('Ctrl Pts',(5.12639022930584,-0.0511844094298134,
42.2623774989373));
#35615=CARTESIAN_POINT('Ctrl Pts',(4.5254522164169,2.40889577686924,42.4013974944501));
#35616=CARTESIAN_POINT('Ctrl Pts',(2.82027083050778,4.28118781058226,42.5404174899624));
#35617=CARTESIAN_POINT('Ctrl Pts',(0.426922776212946,5.10883876923531,42.6794374854749));
#35618=CARTESIAN_POINT('Ctrl Pts',(-2.07059755167574,4.68989577772102,42.8184574809875));
#35619=CARTESIAN_POINT('Ctrl Pts',(-4.06287696323452,3.12658398392071,42.9574774765));
#35620=CARTESIAN_POINT('Ctrl Pts',(-5.06378473998233,0.800362876458667,
43.0964974720124));
#35621=CARTESIAN_POINT('Ctrl Pts',(-4.82909207855925,-1.72115261487393,
43.2355174675251));
#35622=CARTESIAN_POINT('Ctrl Pts',(-3.41606570142293,-3.82269430512735,
43.3745374630375));
#35623=CARTESIAN_POINT('Ctrl Pts',(-1.16949435856725,-4.99147068229099,
43.5135574585502));
#35624=CARTESIAN_POINT('Ctrl Pts',(1.36244214416074,-4.94229177919573,43.6525774540626));
#35625=CARTESIAN_POINT('Ctrl Pts',(3.5619328189657,-3.68715760716384,43.7915974495751));
#35626=CARTESIAN_POINT('Ctrl Pts',(4.89228588665652,-1.53233006565575,43.9306174450876));
#35627=CARTESIAN_POINT('Ctrl Pts',(5.02888548819363,0.996397196667345,44.0696374406001));
#35628=CARTESIAN_POINT('Ctrl Pts',(3.93840032373318,3.28199627009378,44.2086574361127));
#35629=CARTESIAN_POINT('Ctrl Pts',(1.88691673308091,4.76676429764577,44.3476774316251));
#35630=CARTESIAN_POINT('Ctrl Pts',(-0.624988313439745,5.08840704297079,
44.4866974271377));
#35631=CARTESIAN_POINT('Ctrl Pts',(-2.98439164956176,4.16844132847245,44.6257174226502));
#35632=CARTESIAN_POINT('Ctrl Pts',(-4.61558163949699,2.23134550350889,44.7647374181627));
#35633=CARTESIAN_POINT('Ctrl Pts',(-5.12053601930716,-0.250214911364518,
44.9037574136753));
#35634=CARTESIAN_POINT('Ctrl Pts',(-4.37604223455179,-2.67072106149444,
45.0427774091877));
#35635=CARTESIAN_POINT('Ctrl Pts',(-2.56376220292584,-4.43955177847271,
45.1817974047002));
#35636=CARTESIAN_POINT('Ctrl Pts',(-0.125905480353708,-5.12509945629427,
45.3208174002128));
#35637=CARTESIAN_POINT('Ctrl Pts',(2.34267309843463,-4.56008545761606,45.4598373957253));
#35638=CARTESIAN_POINT('Ctrl Pts',(4.23962234154865,-2.88237732226971,45.5988573912378));
#35639=CARTESIAN_POINT('Ctrl Pts',(5.10207278744068,-0.501348081219873,
45.7378773867503));
#35640=CARTESIAN_POINT('Ctrl Pts',(4.71958023211192,2.00201375109182,45.8768973822628));
#35641=CARTESIAN_POINT('Ctrl Pts',(3.18547565094819,4.01686961502235,46.0159173777754));
#35642=CARTESIAN_POINT('Ctrl Pts',(0.874091759514427,5.05157997292503,46.1549373732879));
#35643=CARTESIAN_POINT('Ctrl Pts',(-1.65057690143524,4.85366794489974,46.2939573688004));
#35644=CARTESIAN_POINT('Ctrl Pts',(-3.77249275049772,3.47142551039794,46.4329773643129));
#35645=CARTESIAN_POINT('Ctrl Pts',(-4.97389283229761,1.24212991268819,46.5719973598255));
#35646=CARTESIAN_POINT('Ctrl Pts',(-4.96162675741255,-1.29025445025019,
46.711017355338));
#35647=CARTESIAN_POINT('Ctrl Pts',(-3.7386875380274,-3.50780730955351,46.8500373508505));
#35648=CARTESIAN_POINT('Ctrl Pts',(-1.60348126941681,-4.86942958099378,
46.9890573463629));
#35649=CARTESIAN_POINT('Ctrl Pts',(0.922986132115756,-5.04287549192688,
47.1280773418756));
#35650=CARTESIAN_POINT('Ctrl Pts',(3.22423818221493,-3.98582297338294,47.267097337388));
#35651=CARTESIAN_POINT('Ctrl Pts',(4.73875257782023,-1.95620055686828,47.4061173329006));
#35652=CARTESIAN_POINT('Ctrl Pts',(5.09697676242384,0.550749075960109,47.545137328413));
#35653=CARTESIAN_POINT('Ctrl Pts',(4.21150139919949,2.92331191085705,47.6841573239256));
#35654=CARTESIAN_POINT('Ctrl Pts',(2.29838898109027,4.58256530821365,47.823177319438));
#35655=CARTESIAN_POINT('Ctrl Pts',(-0.17554717780017,5.12363930845007,47.9621973149507));
#35656=CARTESIAN_POINT('Ctrl Pts',(-2.6066484405486,4.41450794394377,48.101217310463));
#35657=CARTESIAN_POINT('Ctrl Pts',(-4.40170865916328,2.62820436986058,48.2402373059757));
#35658=CARTESIAN_POINT('Ctrl Pts',(-5.12271944202073,0.200599841061302,
48.3792573014881));
#35659=CARTESIAN_POINT('Ctrl Pts',(-4.59375005813751,-2.27595269926343,
48.5182772970008));
#35660=CARTESIAN_POINT('Ctrl Pts',(-2.94387062855117,-4.19715580510446,
48.6572972925132));
#35661=CARTESIAN_POINT('Ctrl Pts',(-0.575668206974144,-5.0942229675243,
48.7963172880258));
#35662=CARTESIAN_POINT('Ctrl Pts',(1.93300717656837,-4.74826115834551,48.9353372835382));
#35663=CARTESIAN_POINT('Ctrl Pts',(3.97000353982352,-3.24369166882115,49.0743572790508));
#35664=CARTESIAN_POINT('Ctrl Pts',(5.03831184387823,-0.947632464108493,
49.2133772745632));
#35665=CARTESIAN_POINT('Ctrl Pts',(4.87719276423381,1.57964568937599,49.3523972700758));
#35666=CARTESIAN_POINT('Ctrl Pts',(3.5260860626756,3.72149884840192,49.4914172655884));
#35667=CARTESIAN_POINT('Ctrl Pts',(1.31442635061977,4.95523991833443,49.6304372611009));
#35668=CARTESIAN_POINT('Ctrl Pts',(-1.21764365314759,4.9799428598698,49.7694572566133));
#35669=CARTESIAN_POINT('Ctrl Pts',(-3.45325039473801,3.78935331781989,49.9084772521259));
#35670=CARTESIAN_POINT('Ctrl Pts',(-4.38086558498562,2.3794052799023,50.0011572491342));
#35671=CARTESIAN_POINT('Ctrl Pts',(-4.6480804107302,1.60606351047903,50.0474972476384));
#35672=CARTESIAN_POINT('Origin',(-1.24911029906066,0.239195630269012,50.0000000000009));
#35673=CARTESIAN_POINT('Ctrl Pts',(2.58414624548329,5.32290476454751,4.9705248597598E-16));
#35674=CARTESIAN_POINT('Ctrl Pts',(2.70878071728787,5.24948204733452,-4.65901245328114E-15));
#35675=CARTESIAN_POINT('Ctrl Pts',(2.83052932791161,5.1715483667422,-4.68175003979269E-15));
#35676=CARTESIAN_POINT('Ctrl Pts',(2.94911242871282,5.08918295133373,-4.26395030395099E-15));
#35677=CARTESIAN_POINT('Ctrl Pts',(3.08549346351464,4.9944554521421,-3.77346057385956E-15));
#35678=CARTESIAN_POINT('Ctrl Pts',(3.21768860761213,4.89386633309252,-5.25738578620774E-16));
#35679=CARTESIAN_POINT('Ctrl Pts',(3.34538553148986,4.78775621336396,-2.98372437868011E-16));
#35680=CARTESIAN_POINT('Ctrl Pts',(3.47264577986623,4.68200895037717,-7.17838038905828E-17));
#35681=CARTESIAN_POINT('Ctrl Pts',(3.59543895347339,4.57077773595461,-3.19213500403142E-15));
#35682=CARTESIAN_POINT('Ctrl Pts',(3.71341282312126,4.45437143214694,-2.91433543964104E-16));
#35683=CARTESIAN_POINT('Ctrl Pts',(3.73983681572441,4.42829854566831,3.58270616402455E-16));
#35684=CARTESIAN_POINT('Ctrl Pts',(3.76601984852167,4.4019649171396,-2.99970839866107E-16));
#35685=CARTESIAN_POINT('Ctrl Pts',(3.79195443328246,4.37537715898866,5.41233724504764E-16));
#35686=CARTESIAN_POINT('Ctrl Pts',(3.81284818670717,4.35395718762434,1.21893575481746E-15));
#35687=CARTESIAN_POINT('Ctrl Pts',(3.8335749053755,4.3323781688725,2.30923463697903E-15));
#35688=CARTESIAN_POINT('Ctrl Pts',(3.85412745579704,4.31064779303087,2.44249065417534E-15));
#35689=CARTESIAN_POINT('Ctrl Pts',(3.96643270305237,4.19190655742792,3.17064115873798E-15));
#35690=CARTESIAN_POINT('Ctrl Pts',(4.07359664990735,4.06859126704819,1.94796900594839E-16));
#35691=CARTESIAN_POINT('Ctrl Pts',(4.17531676305532,3.94102919401566,5.41233724504764E-16));
#35692=CARTESIAN_POINT('Ctrl Pts',(4.27565036298719,3.81520587740661,8.82948382659753E-16));
#35693=CARTESIAN_POINT('Ctrl Pts',(4.37068783456493,3.68525011334924,3.32318783145209E-15));
#35694=CARTESIAN_POINT('Ctrl Pts',(4.46009412989579,3.55145356956696,3.99680288865056E-15));
#35695=CARTESIAN_POINT('Ctrl Pts',(4.54136308663149,3.42983455506927,4.60910868588099E-15));
#35696=CARTESIAN_POINT('Ctrl Pts',(4.61797895440299,3.30504150753519,1.83714078762577E-15));
#35697=CARTESIAN_POINT('Ctrl Pts',(4.68965400613746,3.17728361173429,6.60582699651968E-15));
#35698=CARTESIAN_POINT('Ctrl Pts',(4.69964533897967,3.15947446295409,6.42785852502324E-15));
#35699=CARTESIAN_POINT('Ctrl Pts',(4.70953894956037,3.14161057967267,3.94720314365333E-15));
#35700=CARTESIAN_POINT('Ctrl Pts',(4.71933011212868,3.12370005744086,3.46944695195361E-15));
#35701=CARTESIAN_POINT('Ctrl Pts',(4.75402963607211,3.06022581822917,1.32476286234967E-15));
#35702=CARTESIAN_POINT('Ctrl Pts',(4.78745810107654,2.99613834286576,2.98636140275833E-15));
#35703=CARTESIAN_POINT('Ctrl Pts',(4.81959019617709,2.93146624165117,3.99680288865056E-15));
#35704=CARTESIAN_POINT('Ctrl Pts',(4.89045936985516,2.78882822322252,6.09530346681891E-15));
#35705=CARTESIAN_POINT('Ctrl Pts',(4.95502572040444,2.64334740391261,2.50127599806969E-15));
#35706=CARTESIAN_POINT('Ctrl Pts',(5.01322356048623,2.49546111471738,3.3584246494911E-15));
#35707=CARTESIAN_POINT('Ctrl Pts',(5.07162447994012,2.34705878137496,3.35050327570378E-15));
#35708=CARTESIAN_POINT('Ctrl Pts',(5.12361247993031,2.19623337590386,3.66742926385365E-15));
#35709=CARTESIAN_POINT('Ctrl Pts',(5.16907007421431,2.04341570254536,2.1094237467878E-15));
#35710=CARTESIAN_POINT('Ctrl Pts',(5.21390629682536,1.89268693368885,1.53361017081258E-15));
#35711=CARTESIAN_POINT('Ctrl Pts',(5.25238939607452,1.74001924954489,2.50364342773557E-15));
#35712=CARTESIAN_POINT('Ctrl Pts',(5.28435659849648,1.58582660018576,3.60822483003176E-16));
#35713=CARTESIAN_POINT('Ctrl Pts',(5.30699058850528,1.47665236470033,-5.6045551921697E-16));
#35714=CARTESIAN_POINT('Ctrl Pts',(5.32635701224097,1.36671363152776,4.68892524957503E-15));
#35715=CARTESIAN_POINT('Ctrl Pts',(5.34238266598432,1.25616051768223,2.96984659087229E-15));
#35716=CARTESIAN_POINT('Ctrl Pts',(5.34800745436866,1.21735786534933,2.97246100623852E-15));
#35717=CARTESIAN_POINT('Ctrl Pts',(5.35322057164304,1.1784795614691,4.18116876452651E-15));
#35718=CARTESIAN_POINT('Ctrl Pts',(5.35801847245224,1.13953222602327,3.60822483003176E-15));
#35719=CARTESIAN_POINT('Ctrl Pts',(5.36104530259073,1.11496169540385,3.24677426288584E-15));
#35720=CARTESIAN_POINT('Ctrl Pts',(5.36390609156444,1.09036950507184,4.23502775416862E-15));
#35721=CARTESIAN_POINT('Ctrl Pts',(5.36659871116989,1.06577233689814,4.21884749357559E-15));
#35722=CARTESIAN_POINT('Ctrl Pts',(5.38350200775575,0.911360169664405,4.11727364219028E-15));
#35723=CARTESIAN_POINT('Ctrl Pts',(5.3938040052084,0.756577139039222,3.41788756861821E-15));
#35724=CARTESIAN_POINT('Ctrl Pts',(5.39741303532708,0.601823960215616,4.16333634234434E-15));
#35725=CARTESIAN_POINT('Ctrl Pts',(5.40010692670364,0.486311415232869,4.71976229534865E-15));
#35726=CARTESIAN_POINT('Ctrl Pts',(5.39907072069453,0.370815309359756,4.64881586728296E-15));
#35727=CARTESIAN_POINT('Ctrl Pts',(5.39424738914643,0.255503721863896,4.38538094726937E-15));
#35728=CARTESIAN_POINT('Ctrl Pts',(5.38775683563753,0.10033378975928,3.28400669008254E-15));
#35729=CARTESIAN_POINT('Ctrl Pts',(5.37441019776384,-0.0545030548216875,
3.88956332774984E-15));
#35730=CARTESIAN_POINT('Ctrl Pts',(5.35430867040058,-0.20856819236625,3.44169137633799E-15));
#35731=CARTESIAN_POINT('Ctrl Pts',(5.33439409683937,-0.361200450572585,
2.99798484791265E-15));
#35732=CARTESIAN_POINT('Ctrl Pts',(5.30784933644905,-0.513075978006889,
4.82803955867264E-15));
#35733=CARTESIAN_POINT('Ctrl Pts',(5.27472800412706,-0.663744430058508,
4.16333634234434E-15));
#35734=CARTESIAN_POINT('Ctrl Pts',(5.25927971775813,-0.734018456822544,
3.85330878861071E-15));
#35735=CARTESIAN_POINT('Ctrl Pts',(5.24240013898647,-0.804029489193217,
4.0102305330087E-15));
#35736=CARTESIAN_POINT('Ctrl Pts',(5.22409165812288,-0.873729395676655,
3.38618022510673E-15));
#35737=CARTESIAN_POINT('Ctrl Pts',(5.21856569074994,-0.894766608539603,
2.56437578661977E-15));
#35738=CARTESIAN_POINT('Ctrl Pts',(5.21290953948652,-0.915775466103714,
3.85815002206143E-15));
#35739=CARTESIAN_POINT('Ctrl Pts',(5.20712323720842,-0.93675461242177,4.66293670342566E-15));
#35740=CARTESIAN_POINT('Ctrl Pts',(5.20151158363336,-0.957100542478549,
5.44343240527273E-15));
#35741=CARTESIAN_POINT('Ctrl Pts',(5.19577955606844,-0.977411034412793,
5.45443632467064E-15));
#35742=CARTESIAN_POINT('Ctrl Pts',(5.18992938606291,-0.997678452611402,
5.32907051820075E-15));
#35743=CARTESIAN_POINT('Ctrl Pts',(5.14784463105866,-1.14347751975841,3.61622417999283E-15));
#35744=CARTESIAN_POINT('Ctrl Pts',(5.09962047179063,-1.28715624957652,8.5620977488092E-16));
#35745=CARTESIAN_POINT('Ctrl Pts',(5.04538459586395,-1.4283155996208,8.88178419700125E-16));
#35746=CARTESIAN_POINT('Ctrl Pts',(4.99037672763084,-1.57148420885657,1.49259684713777E-16));
#35747=CARTESIAN_POINT('Ctrl Pts',(4.92918455837232,-1.71206201410615,1.64585842454949E-15));
#35748=CARTESIAN_POINT('Ctrl Pts',(4.86189305225203,-1.84960649198228,1.83186799063151E-15));
#35749=CARTESIAN_POINT('Ctrl Pts',(4.79460154613173,-1.98715096985842,1.32090672371618E-15));
#35750=CARTESIAN_POINT('Ctrl Pts',(4.72121037278009,-2.12166286716527,2.86036616442949E-17));
#35751=CARTESIAN_POINT('Ctrl Pts',(4.64176094100255,-2.25266201421487,4.9960036108132E-16));
#35752=CARTESIAN_POINT('Ctrl Pts',(4.58721573082958,-2.34259816414614,6.83092991782841E-16));
#35753=CARTESIAN_POINT('Ctrl Pts',(4.52981397660194,-2.43087776084676,-2.86988927465527E-15));
#35754=CARTESIAN_POINT('Ctrl Pts',(4.46964647785047,-2.51737751627479,-6.66133814775094E-16));
#35755=CARTESIAN_POINT('Ctrl Pts',(4.43875608755086,-2.56178706065407,7.73849861614024E-16));
#35756=CARTESIAN_POINT('Ctrl Pts',(4.40713658096766,-2.60572729308483,-3.02645681402354E-15));
#35757=CARTESIAN_POINT('Ctrl Pts',(4.37479966267197,-2.6491803912438,-2.22044604925031E-15));
#35758=CARTESIAN_POINT('Ctrl Pts',(4.35422501482126,-2.67682780601809,-4.76874351599547E-16));
#35759=CARTESIAN_POINT('Ctrl Pts',(4.33335993315775,-2.70427800064961,-3.53144676016607E-15));
#35760=CARTESIAN_POINT('Ctrl Pts',(4.31220736271508,-2.73152621065158,-1.72084568816899E-15));
#35761=CARTESIAN_POINT('Ctrl Pts',(4.29999903121887,-2.74725267667535,-6.7584653999294E-16));
#35762=CARTESIAN_POINT('Ctrl Pts',(4.28770074273341,-2.7629043558843,-9.60893281977405E-16));
#35763=CARTESIAN_POINT('Ctrl Pts',(4.27531513424813,-2.77847828895174,-1.27675647831893E-15));
#35764=CARTESIAN_POINT('Ctrl Pts',(4.2326472946748,-2.83212975697908,-2.36489035600746E-15));
#35765=CARTESIAN_POINT('Ctrl Pts',(4.18893635069837,-2.8848676535937,-1.97050552418505E-15));
#35766=CARTESIAN_POINT('Ctrl Pts',(4.14421478376096,-2.93666546386691,-1.60982338570648E-15));
#35767=CARTESIAN_POINT('Ctrl Pts',(4.04793402946876,-3.048180613834,-8.3331328709926E-16));
#35768=CARTESIAN_POINT('Ctrl Pts',(3.94697122462269,-3.15534114389694,1.76209427040427E-15));
#35769=CARTESIAN_POINT('Ctrl Pts',(3.84162425024921,-3.25785439519544,6.66133814775094E-16));
#35770=CARTESIAN_POINT('Ctrl Pts',(3.73693153910005,-3.35973098226387,-4.23020117689046E-16));
#35771=CARTESIAN_POINT('Ctrl Pts',(3.62790829687089,-3.45701825449416,-4.73077726807451E-16));
#35772=CARTESIAN_POINT('Ctrl Pts',(3.51481945591763,-3.54938593120666,-3.33066907387547E-16));
#35773=CARTESIAN_POINT('Ctrl Pts',(3.40416108084475,-3.63976847406503,-1.96065151608371E-16));
#35774=CARTESIAN_POINT('Ctrl Pts',(3.2896093651333,-3.72544086154151,1.01954794998456E-15));
#35775=CARTESIAN_POINT('Ctrl Pts',(3.17139556349596,-3.80604757063947,0.));
#35776=CARTESIAN_POINT('Ctrl Pts',(3.06930259849605,-3.87566192883381,-8.8051201917039E-16));
#35777=CARTESIAN_POINT('Ctrl Pts',(2.96447778034216,-3.94149744951773,1.6904407368494E-15));
#35778=CARTESIAN_POINT('Ctrl Pts',(2.85706463458463,-4.00329423553976,1.11022302462516E-16));
#35779=CARTESIAN_POINT('Ctrl Pts',(-2.14763659377329,4.42399807618489,-0.576782495683815));
#35780=CARTESIAN_POINT('Ctrl Pts',(-2.88330608755926,4.0668662016747,-0.530467033922107));
#35781=CARTESIAN_POINT('Ctrl Pts',(-4.17230160089297,2.9788793155184,-0.437836110398691));
#35782=CARTESIAN_POINT('Ctrl Pts',(-5.08888703583058,0.619198826710665,
-0.298889725113564));
#35783=CARTESIAN_POINT('Ctrl Pts',(-4.76496251935548,-1.89075243704101,
-0.159943339828439));
#35784=CARTESIAN_POINT('Ctrl Pts',(-3.27959572109872,-3.9401495754155,-0.0209969545433121));
#35785=CARTESIAN_POINT('Ctrl Pts',(-0.994793592359738,-5.02895297143194,
0.117949430741813));
#35786=CARTESIAN_POINT('Ctrl Pts',(1.53248373837111,-4.89201169135806,0.256895816026939));
#35787=CARTESIAN_POINT('Ctrl Pts',(3.68621665053458,-3.56257803960143,0.395842201312065));
#35788=CARTESIAN_POINT('Ctrl Pts',(4.9414155898574,-1.36477265986452,0.534788586597191));
#35789=CARTESIAN_POINT('Ctrl Pts',(4.99212435123777,1.16571333689883,0.673734971882318));
#35790=CARTESIAN_POINT('Ctrl Pts',(3.82598040849633,3.41204582749421,0.812681357167443));
#35791=CARTESIAN_POINT('Ctrl Pts',(1.7272374644813,4.8266802929848,0.951627742452569));
#35792=CARTESIAN_POINT('Ctrl Pts',(-0.792527301558058,5.06478893033327,
1.09057412773769));
#35793=CARTESIAN_POINT('Ctrl Pts',(-3.11910999962733,4.06833403048449,1.22952051302282));
#35794=CARTESIAN_POINT('Ctrl Pts',(-4.68539612420164,2.08020462550141,1.36846689830795));
#35795=CARTESIAN_POINT('Ctrl Pts',(-5.10959655165582,-0.414983494631241,
1.50741328359307));
#35796=CARTESIAN_POINT('Ctrl Pts',(-4.28831062073647,-2.80901768900255,
1.6463596688782));
#35797=CARTESIAN_POINT('Ctrl Pts',(-2.42173032831516,-4.51834155710065,
1.78530605416333));
#35798=CARTESIAN_POINT('Ctrl Pts',(0.035157255613399,-5.12630005696805,
1.92425243944845));
#35799=CARTESIAN_POINT('Ctrl Pts',(2.48347510733904,-4.48470061981063,2.06319882473358));
#35800=CARTESIAN_POINT('Ctrl Pts',(4.3264351051218,-2.74993591880546,2.2021452100187));
#35801=CARTESIAN_POINT('Ctrl Pts',(5.11480773945644,-0.344862379916521,
2.34109159530383));
#35802=CARTESIAN_POINT('Ctrl Pts',(4.65642375300045,2.14427286129782,2.48003798058896));
#35803=CARTESIAN_POINT('Ctrl Pts',(3.06301623538964,4.11073227238675,2.61898436587408));
#35804=CARTESIAN_POINT('Ctrl Pts',(0.722985195410011,5.07518282222839,2.75793075115921));
#35805=CARTESIAN_POINT('Ctrl Pts',(-1.7932766287375,4.80253549758407,2.89687713644433));
#35806=CARTESIAN_POINT('Ctrl Pts',(-3.87241947927127,3.35924926864857,3.03582352172946));
#35807=CARTESIAN_POINT('Ctrl Pts',(-5.00764324831504,1.09713142788837,3.17476990701458));
#35808=CARTESIAN_POINT('Ctrl Pts',(-4.92223220735804,-1.43241696768481,
3.31371629229971));
#35809=CARTESIAN_POINT('Ctrl Pts',(-3.63700566890923,-3.61280750064991,
3.45266267758483));
#35810=CARTESIAN_POINT('Ctrl Pts',(-1.46524318859916,-4.91256050046432,
3.59160906286996));
#35811=CARTESIAN_POINT('Ctrl Pts',(1.06367868834549,-5.01485552338266,3.73055544815509));
#35812=CARTESIAN_POINT('Ctrl Pts',(3.33332426119376,-3.89475771289902,3.86950183344021));
#35813=CARTESIAN_POINT('Ctrl Pts',(4.79045755541376,-1.82529577938104,4.00844821872534));
#35814=CARTESIAN_POINT('Ctrl Pts',(5.07989599637985,0.68908993492224,4.14739460401047));
#35815=CARTESIAN_POINT('Ctrl Pts',(4.13108770591761,3.03550698211419,4.28634098929559));
#35816=CARTESIAN_POINT('Ctrl Pts',(2.17530882929733,4.64200600706508,4.42528737458072));
#35817=CARTESIAN_POINT('Ctrl Pts',(-0.310711030532882,5.11699588899118,
4.56423375986584));
#35818=CARTESIAN_POINT('Ctrl Pts',(-2.72099372600968,4.34469577939161,4.70318014515097));
#35819=CARTESIAN_POINT('Ctrl Pts',(-4.46802237261035,2.51335718717033,4.84212653043609));
#35820=CARTESIAN_POINT('Ctrl Pts',(-5.12595114339145,0.0693768550111596,
4.98107291572122));
#35821=CARTESIAN_POINT('Ctrl Pts',(-4.53440704045836,-2.39151438713821,
5.12001930100635));
#35822=CARTESIAN_POINT('Ctrl Pts',(-2.83758151034357,-4.26946360150824,
5.25896568629147));
#35823=CARTESIAN_POINT('Ctrl Pts',(-0.449083152114085,-5.10671250364994,
5.3979120715766));
#35824=CARTESIAN_POINT('Ctrl Pts',(2.04888117660792,-4.69917803414481,5.53685845686173));
#35825=CARTESIAN_POINT('Ctrl Pts',(4.0474218120441,-3.14619849148731,5.67580484214685));
#35826=CARTESIAN_POINT('Ctrl Pts',(5.05938578664962,-0.826319390003141,
5.81475122743198));
#35827=CARTESIAN_POINT('Ctrl Pts',(4.83810248260642,1.69497865480515,5.9536976127171));
#35828=CARTESIAN_POINT('Ctrl Pts',(3.43751066719364,3.80311828443151,6.09264399800223));
#35829=CARTESIAN_POINT('Ctrl Pts',(1.19901068379161,4.98423130007035,6.23159038328735));
#35830=CARTESIAN_POINT('Ctrl Pts',(-1.33175336588475,4.95041626986075,6.37053676857248));
#35831=CARTESIAN_POINT('Ctrl Pts',(-3.53789674349407,3.70991575441024,6.50948315385761));
#35832=CARTESIAN_POINT('Ctrl Pts',(-4.88166241063757,1.56510714681635,6.64842953914273));
#35833=CARTESIAN_POINT('Ctrl Pts',(-5.03550164459886,-0.961203131335693,
6.78737592442786));
#35834=CARTESIAN_POINT('Ctrl Pts',(-3.96191546336068,-3.25321596787409,
6.92632230971299));
#35835=CARTESIAN_POINT('Ctrl Pts',(-1.92259516547955,-4.75224327051151,
7.0652686949981));
#35836=CARTESIAN_POINT('Ctrl Pts',(0.585366061509484,-5.09289061795758,
7.20421508028325));
#35837=CARTESIAN_POINT('Ctrl Pts',(2.95064176641898,-4.19212373847805,7.34316146556836));
#35838=CARTESIAN_POINT('Ctrl Pts',(4.59668571432242,-2.26950847458025,7.48210785085349));
#35839=CARTESIAN_POINT('Ctrl Pts',(5.12226753756436,0.206309345551128,7.62105423613861));
#35840=CARTESIAN_POINT('Ctrl Pts',(4.39927438202509,2.63183836587758,7.76000062142375));
#35841=CARTESIAN_POINT('Ctrl Pts',(2.60393897221896,4.41584534391849,7.89894700670886));
#35842=CARTESIAN_POINT('Ctrl Pts',(0.173882118610286,5.12347082369706,8.037893391994));
#35843=CARTESIAN_POINT('Ctrl Pts',(-2.29855925727532,4.58222801846888,8.17683977727911));
#35844=CARTESIAN_POINT('Ctrl Pts',(-4.21071682236168,2.92404721479112,8.31578616256425));
#35845=CARTESIAN_POINT('Ctrl Pts',(-5.09649385800896,0.553117191673102,
8.45473254784938));
#35846=CARTESIAN_POINT('Ctrl Pts',(-4.73997836130483,-1.95263755131597,
8.59367893313449));
#35847=CARTESIAN_POINT('Ctrl Pts',(-3.22807253434404,-3.98242840305523,
8.73262531841964));
#35848=CARTESIAN_POINT('Ctrl Pts',(-0.929309994703741,-5.04148501993124,
8.87157170370474));
#35849=CARTESIAN_POINT('Ctrl Pts',(1.59597589585668,-4.87165774786078,9.01051808898988));
#35850=CARTESIAN_POINT('Ctrl Pts',(3.73223572409388,-3.51434272265025,9.149464474275));
#35851=CARTESIAN_POINT('Ctrl Pts',(4.95874687055243,-1.3003913819439,9.28841085956013));
#35852=CARTESIAN_POINT('Ctrl Pts',(4.97654191163832,1.23053601091333,9.42735724484525));
#35853=CARTESIAN_POINT('Ctrl Pts',(3.78128322873188,3.46151490196971,9.56630363013038));
#35854=CARTESIAN_POINT('Ctrl Pts',(1.6643203215817,4.84873448846372,9.7052500154155));
#35855=CARTESIAN_POINT('Ctrl Pts',(-0.858327898755408,5.05405396594313,
9.84419640070063));
#35856=CARTESIAN_POINT('Ctrl Pts',(-3.17175496261903,4.02742581924844,9.98314278598575));
#35857=CARTESIAN_POINT('Ctrl Pts',(-4.71205296672362,2.01909512188963,10.1220891712709));
#35858=CARTESIAN_POINT('Ctrl Pts',(-5.10376757689243,-0.481398788437435,
10.261035556556));
#35859=CARTESIAN_POINT('Ctrl Pts',(-4.25141665411314,-2.86454965144206,
10.3999819418411));
#35860=CARTESIAN_POINT('Ctrl Pts',(-2.36276444098316,-4.54945408470871,
10.5389283271262));
#35861=CARTESIAN_POINT('Ctrl Pts',(0.10182187557482,-5.12540930834815,10.6778747124114));
#35862=CARTESIAN_POINT('Ctrl Pts',(2.54158866734169,-4.45202373292053,10.8168210976965));
#35863=CARTESIAN_POINT('Ctrl Pts',(4.36183217315665,-2.69343801964384,10.9557674829816));
#35864=CARTESIAN_POINT('Ctrl Pts',(5.11886012587774,-0.278315080702345,
11.0947138682668));
#35865=CARTESIAN_POINT('Ctrl Pts',(4.62814367122823,2.20464836899615,11.2336602535518));
#35866=CARTESIAN_POINT('Ctrl Pts',(3.00929707817369,4.15021919514412,11.372606638837));
#35867=CARTESIAN_POINT('Ctrl Pts',(0.656921240898197,5.08415605147049,11.5115530241221));
#35868=CARTESIAN_POINT('Ctrl Pts',(-1.85558200448324,4.77880776942172,11.6504994094073));
#35869=CARTESIAN_POINT('Ctrl Pts',(-3.91577907005585,3.30860432009629,11.7894457946923));
#35870=CARTESIAN_POINT('Ctrl Pts',(-5.02148796540853,1.03191418524254,11.9283921799775));
#35871=CARTESIAN_POINT('Ctrl Pts',(-4.90318734078181,-1.49630951799562,
12.0673385652626));
#35872=CARTESIAN_POINT('Ctrl Pts',(-3.5897134876814,-3.65980127176404,12.2062849505478));
#35873=CARTESIAN_POINT('Ctrl Pts',(-1.40123136747207,-4.93120055638176,
12.3452313358328));
#35874=CARTESIAN_POINT('Ctrl Pts',(1.12880698971214,-5.00059826944982,12.484177721118));
#35875=CARTESIAN_POINT('Ctrl Pts',(3.38369373622936,-3.85107841673595,12.6231241064031));
#35876=CARTESIAN_POINT('Ctrl Pts',(4.81379042562212,-1.76284145930265,12.7620704916883));
#35877=CARTESIAN_POINT('Ctrl Pts',(5.07050477321974,0.755095766908508,12.9010168769733));
#35878=CARTESIAN_POINT('Ctrl Pts',(4.09126154085794,3.08897511753399,13.0399632622585));
#35879=CARTESIAN_POINT('Ctrl Pts',(2.11475552319577,4.66990335548396,13.1789096475436));
#35880=CARTESIAN_POINT('Ctrl Pts',(-0.377231346088842,5.11252235046219,
13.3178560328287));
#35881=CARTESIAN_POINT('Ctrl Pts',(-2.77726643493942,4.30894179837768,13.4568024181139));
#35882=CARTESIAN_POINT('Ctrl Pts',(-4.50033075749474,2.45503795196616,13.595748803399));
#35883=CARTESIAN_POINT('Ctrl Pts',(-5.12641989497035,0.00270793271152465,
13.7346951886841));
#35884=CARTESIAN_POINT('Ctrl Pts',(-4.50292189849674,-2.45028215691293,
13.8736415739692));
#35885=CARTESIAN_POINT('Ctrl Pts',(-2.7818171150605,-4.30600531941193,14.0125879592544));
#35886=CARTESIAN_POINT('Ctrl Pts',(-0.382632317267694,-5.1121209670967,
14.1515343445395));
#35887=CARTESIAN_POINT('Ctrl Pts',(2.10982077116202,-4.67213490665891,14.2904807298246));
#35888=CARTESIAN_POINT('Ctrl Pts',(4.08799587522889,-3.09329565294991,14.4294271151098));
#35889=CARTESIAN_POINT('Ctrl Pts',(5.06970421418836,-0.760452137276422,
14.5683735003949));
#35890=CARTESIAN_POINT('Ctrl Pts',(4.81565011293228,1.75775489254407,14.70731988568));
#35891=CARTESIAN_POINT('Ctrl Pts',(3.38776036301521,3.84750152634543,14.8462662709651));
#35892=CARTESIAN_POINT('Ctrl Pts',(1.13408929801697,4.99940293800877,14.9852126562503));
#35893=CARTESIAN_POINT('Ctrl Pts',(-1.39602096325972,4.93267815112508,15.1241590415354));
#35894=CARTESIAN_POINT('Ctrl Pts',(-3.58584504623797,3.66359162254993,15.2631054268205));
#35895=CARTESIAN_POINT('Ctrl Pts',(-4.90160381152525,1.50148871034336,15.4020518121056));
#35896=CARTESIAN_POINT('Ctrl Pts',(-5.02257534047868,-1.02660860198166,
15.5409981973908));
#35897=CARTESIAN_POINT('Ctrl Pts',(-3.91927229705261,-3.30446560490549,
15.6799445826759));
#35898=CARTESIAN_POINT('Ctrl Pts',(-1.86062959414104,-4.77684475211974,
15.818890967961));
#35899=CARTESIAN_POINT('Ctrl Pts',(0.651549660500337,-5.08484722605797,
15.9578373532461));
#35900=CARTESIAN_POINT('Ctrl Pts',(3.00491085310802,-4.15339608481073,16.0967837385313));
#35901=CARTESIAN_POINT('Ctrl Pts',(4.62581196292139,-2.20953659307574,16.2357301238164));
#35902=CARTESIAN_POINT('Ctrl Pts',(5.11915129836543,0.272907048078267,16.3746765091015));
#35903=CARTESIAN_POINT('Ctrl Pts',(4.36467525187932,2.6888284099361,16.5136228943866));
#35904=CARTESIAN_POINT('Ctrl Pts',(2.54629063950183,4.44933615853341,16.6525692796718));
#35905=CARTESIAN_POINT('Ctrl Pts',(0.107236615018882,5.12529887722137,16.7915156649569));
#35906=CARTESIAN_POINT('Ctrl Pts',(-2.35795680053252,4.55194771490949,16.930462050242));
#35907=CARTESIAN_POINT('Ctrl Pts',(-4.24838799591456,2.86903950976915,17.0694084355271));
#35908=CARTESIAN_POINT('Ctrl Pts',(-5.10325614954743,0.486790452406175,
17.2083548208123));
#35909=CARTESIAN_POINT('Ctrl Pts',(-4.7141834328707,-2.01411589380919,17.3473012060974));
#35910=CARTESIAN_POINT('Ctrl Pts',(-3.1760080118737,-4.02407273554559,17.4862475913825));
#35911=CARTESIAN_POINT('Ctrl Pts',(-0.863666831873859,-5.05314435534632,
17.6251939766677));
#35912=CARTESIAN_POINT('Ctrl Pts',(1.65919689275546,-4.85049007251,17.7641403619528));
#35913=CARTESIAN_POINT('Ctrl Pts',(3.77762416224581,-3.46550774941626,17.9030867472379));
#35914=CARTESIAN_POINT('Ctrl Pts',(4.97523912085433,-1.23579284783815,18.042033132523));
#35915=CARTESIAN_POINT('Ctrl Pts',(4.96011791638736,1.2951519323927,18.1809795178082));
#35916=CARTESIAN_POINT('Ctrl Pts',(3.73594640816555,3.51039779907668,18.3199259030933));
#35917=CARTESIAN_POINT('Ctrl Pts',(1.60112172279223,4.86996894253445,18.4588722883784));
#35918=CARTESIAN_POINT('Ctrl Pts',(-0.923983342588718,5.04246398649172,
18.5978186736635));
#35919=CARTESIAN_POINT('Ctrl Pts',(-3.22386345165755,3.98583651414782,18.7367650589486));
#35920=CARTESIAN_POINT('Ctrl Pts',(-4.73791283024863,1.95764406504679,18.8757114442338));
#35921=CARTESIAN_POINT('Ctrl Pts',(-5.09707536075682,-0.54773263478927,
19.0146578295189));
#35922=CARTESIAN_POINT('Ctrl Pts',(-4.21380361509104,-2.91959712390135,
19.153604214804));
#35923=CARTESIAN_POINT('Ctrl Pts',(-2.30339892084015,-4.57979712257211,
19.2925506000892));
#35924=CARTESIAN_POINT('Ctrl Pts',(0.168469273241985,-5.12365166423526,
19.4314969853743));
#35925=CARTESIAN_POINT('Ctrl Pts',(2.59927234963534,-4.41859384022433,19.5704433706594));
#35926=CARTESIAN_POINT('Ctrl Pts',(4.3964914917667,-2.63648456002883,19.7093897559445));
#35927=CARTESIAN_POINT('Ctrl Pts',(5.12204672122891,-0.211720707526411,
19.8483361412297));
#35928=CARTESIAN_POINT('Ctrl Pts',(4.59908079685158,2.26465098778562,19.9872825265148));
#35929=CARTESIAN_POINT('Ctrl Pts',(2.95506893603482,4.18900416038578,20.1262289117999));
#35930=CARTESIAN_POINT('Ctrl Pts',(0.59074617637326,5.09226935928841,20.265175297085));
#35931=CARTESIAN_POINT('Ctrl Pts',(-1.91757353175325,4.75427176576673,20.4041216823702));
#35932=CARTESIAN_POINT('Ctrl Pts',(-3.9584763558217,3.25739976251733,20.5430680676553));
#35933=CARTESIAN_POINT('Ctrl Pts',(-5.03448336065964,0.9665224072357,20.6820144529404));
#35934=CARTESIAN_POINT('Ctrl Pts',(-4.88331316143473,-1.55994898628306,
20.8209608382255));
#35935=CARTESIAN_POINT('Ctrl Pts',(-3.54181415134507,-3.7061760332962,20.9599072235107));
#35936=CARTESIAN_POINT('Ctrl Pts',(-1.33698254559689,-4.94900656144409,
21.0988536087958));
#35937=CARTESIAN_POINT('Ctrl Pts',(1.19374436750442,-4.98549522690562,21.2377999940809));
#35938=CARTESIAN_POINT('Ctrl Pts',(3.43349090181907,-3.80674775885835,21.376746379366));
#35939=CARTESIAN_POINT('Ctrl Pts',(4.83630910342842,-1.70008897665469,21.5156927646512));
#35940=CARTESIAN_POINT('Ctrl Pts',(5.06025593763869,0.820973883896323,21.6546391499363));
#35941=CARTESIAN_POINT('Ctrl Pts',(4.05074339011407,3.14192079147367,21.7935855352214));
#35942=CARTESIAN_POINT('Ctrl Pts',(2.05384453266536,4.69701084819781,21.9325319205066));
#35943=CARTESIAN_POINT('Ctrl Pts',(-0.443687857683883,5.10718409276494,
22.0714783057917));
#35944=CARTESIAN_POINT('Ctrl Pts',(-2.83306940401134,4.27245901378845,22.2104246910768));
#35945=CARTESIAN_POINT('Ctrl Pts',(-4.53187796775673,2.39630347781925,22.3493710763619));
#35946=CARTESIAN_POINT('Ctrl Pts',(-5.12602157678528,-0.063961447601001,
22.488317461647));
#35947=CARTESIAN_POINT('Ctrl Pts',(-4.47067514365369,-2.50863549212803,
22.6272638469322));
#35948=CARTESIAN_POINT('Ctrl Pts',(-2.72558221022914,-4.34181873040893,
22.7662102322173));
#35949=CARTESIAN_POINT('Ctrl Pts',(-0.316116764953832,-5.11666477926417,
22.9051566175024));
#35950=CARTESIAN_POINT('Ctrl Pts',(2.17040351593876,-4.64430154602909,23.0441030027875));
#35951=CARTESIAN_POINT('Ctrl Pts',(4.12787850507594,-3.03986962216792,23.1830493880727));
#35952=CARTESIAN_POINT('Ctrl Pts',(5.07916516471065,-0.694456263588383,
23.3219957733578));
#35953=CARTESIAN_POINT('Ctrl Pts',(4.79238323631331,1.82023382804259,23.460942158643));
#35954=CARTESIAN_POINT('Ctrl Pts',(3.33743706157193,3.89123401153074,23.599888543928));
#35955=CARTESIAN_POINT('Ctrl Pts',(1.06897609523158,5.01372898951177,23.7388349292132));
#35956=CARTESIAN_POINT('Ctrl Pts',(-1.46005244116113,4.91410573161657,23.8777813144983));
#35957=CARTESIAN_POINT('Ctrl Pts',(-3.63318684817203,3.61664784001942,24.0167276997835));
#35958=CARTESIAN_POINT('Ctrl Pts',(-4.92071616747572,1.43761631584731,24.1556740850685));
#35959=CARTESIAN_POINT('Ctrl Pts',(-5.00879953060122,-1.09184043463153,
24.2946204703537));
#35960=CARTESIAN_POINT('Ctrl Pts',(-3.87596623488826,-3.35515633293791,
24.4335668556388));
#35961=CARTESIAN_POINT('Ctrl Pts',(-1.7983493205939,-4.80063829022421,24.572513240924));
#35962=CARTESIAN_POINT('Ctrl Pts',(0.717623058020787,-5.075943795891,24.7114596262091));
#35963=CARTESIAN_POINT('Ctrl Pts',(3.05867169673505,-4.11396593617877,24.8504060114942));
#35964=CARTESIAN_POINT('Ctrl Pts',(4.65415581332253,-2.14919099611072,24.9893523967793));
#35965=CARTESIAN_POINT('Ctrl Pts',(5.1151692187947,0.339458591793783,25.1282987820644));
#35966=CARTESIAN_POINT('Ctrl Pts',(4.32933789154216,2.74536367232189,25.2672451673496));
#35967=CARTESIAN_POINT('Ctrl Pts',(2.48821163359192,4.48207442362409,25.4061915526347));
#35968=CARTESIAN_POINT('Ctrl Pts',(0.0405729736962985,5.12626005058783,
25.5451379379198));
#35969=CARTESIAN_POINT('Ctrl Pts',(-2.41695552490853,4.52089750636546,25.684084323205));
#35970=CARTESIAN_POINT('Ctrl Pts',(-4.28534060780991,2.81354654262248,25.8230307084901));
#35971=CARTESIAN_POINT('Ctrl Pts',(-5.10915528917953,0.420381378626828,
25.9619770937752));
#35972=CARTESIAN_POINT('Ctrl Pts',(-4.6875911593107,-2.07525357380717,26.1009234790603));
#35973=CARTESIAN_POINT('Ctrl Pts',(-3.12340630739848,-4.06503644649722,
26.2398698643455));
#35974=CARTESIAN_POINT('Ctrl Pts',(-0.797877590608867,-5.06394901463785,
26.3788162496306));
#35975=CARTESIAN_POINT('Ctrl Pts',(1.722137257266,-4.82850199747124,26.5177626349157));
#35976=CARTESIAN_POINT('Ctrl Pts',(3.82237366255062,-3.41608662892009,26.6567090202008));
#35977=CARTESIAN_POINT('Ctrl Pts',(4.99088987172806,-1.17098529483918,26.795655405486));
#35978=CARTESIAN_POINT('Ctrl Pts',(4.9428549792707,1.35954879513255,26.9346017907711));
#35979=CARTESIAN_POINT('Ctrl Pts',(3.68997769902266,3.55868695633134,27.0735481760562));
#35980=CARTESIAN_POINT('Ctrl Pts',(1.53765231430271,4.89037970231012,27.2124945613413));
#35981=CARTESIAN_POINT('Ctrl Pts',(-0.989482506204021,5.03002113736749,
27.3514409466265));
#35982=CARTESIAN_POINT('Ctrl Pts',(-3.2754266645425,3.94357305468675,27.4903873319116));
#35983=CARTESIAN_POINT('Ctrl Pts',(-4.76297133511717,1.89586189721181,27.6293337171967));
#35984=CARTESIAN_POINT('Ctrl Pts',(-5.08952103811793,-0.613973839021256,
27.7682801024819));
#35985=CARTESIAN_POINT('Ctrl Pts',(-4.17547786392657,-2.97415078304826,
27.9072264877669));
#35986=CARTESIAN_POINT('Ctrl Pts',(-2.24364380959848,-4.60936554507209,
28.0461728730521));
#35987=CARTESIAN_POINT('Ctrl Pts',(0.23508817644013,-5.12102741856997,28.1851192583372));
#35988=CARTESIAN_POINT('Ctrl Pts',(2.65651639754307,-4.38441659768233,28.3240656436223));
#35989=CARTESIAN_POINT('Ctrl Pts',(4.43040719886656,-2.57908517204815,28.4630120289075));
#35990=CARTESIAN_POINT('Ctrl Pts',(5.12436698648373,-0.145090524442568,
28.6019584141926));
#35991=CARTESIAN_POINT('Ctrl Pts',(4.5692400455193,2.3242705692045,28.7409047994777));
#35992=CARTESIAN_POINT('Ctrl Pts',(2.90034098097046,4.22708060800249,28.8798511847629));
#35993=CARTESIAN_POINT('Ctrl Pts',(0.524471194526165,5.09952137347807,29.018797570048));
#35994=CARTESIAN_POINT('Ctrl Pts',(-1.97924072546044,4.72893163654605,29.1577439553331));
#35995=CARTESIAN_POINT('Ctrl Pts',(-4.0005041148555,3.20564425653746,29.2966903406182));
#35996=CARTESIAN_POINT('Ctrl Pts',(-5.0466272360609,0.90096715406042,29.4356367259034));
#35997=CARTESIAN_POINT('Ctrl Pts',(-4.86261303078498,-1.62332460872357,
29.5745831111885));
#35998=CARTESIAN_POINT('Ctrl Pts',(-3.49331576147361,-3.75192394153818,
29.7135294964736));
#35999=CARTESIAN_POINT('Ctrl Pts',(-1.27250758985748,-4.96597550398736,
29.8524758817587));
#36000=CARTESIAN_POINT('Ctrl Pts',(1.25847983837766,-4.96954895024129,29.9914222670439));
#36001=CARTESIAN_POINT('Ctrl Pts',(3.48270733539568,-3.76177323724179,30.130368652329));
#36002=CARTESIAN_POINT('Ctrl Pts',(4.8580097800802,-1.63704894523421,30.2693150376141));
#36003=CARTESIAN_POINT('Ctrl Pts',(5.04915122309893,0.886713143426884,30.4082614228992));
#36004=CARTESIAN_POINT('Ctrl Pts',(4.00954010682405,3.19433504883518,30.5472078081844));
#36005=CARTESIAN_POINT('Ctrl Pts',(1.99258616003768,4.7233239003136,30.6861541934695));
#36006=CARTESIAN_POINT('Ctrl Pts',(-0.510069325031026,5.1009820187989,30.8251005787546));
#36007=CARTESIAN_POINT('Ctrl Pts',(-2.88839319485177,4.23525359623026,30.9640469640397));
#36008=CARTESIAN_POINT('Ctrl Pts',(-4.56265866758056,2.33716369893069,31.1029933493249));
#36009=CARTESIAN_POINT('Ctrl Pts',(-5.12475625620675,-0.13062000963517,
31.24193973461));
#36010=CARTESIAN_POINT('Ctrl Pts',(-4.43767223006419,-2.56656452304717,
31.3808861198952));
#36011=CARTESIAN_POINT('Ctrl Pts',(-2.66888630727981,-4.376897777109,31.5198325051802));
#36012=CARTESIAN_POINT('Ctrl Pts',(-0.249547745445644,-5.1203431716234,
31.6587788904654));
#36013=CARTESIAN_POINT('Ctrl Pts',(2.23061916412508,-4.61568265991991,31.7977252757505));
#36014=CARTESIAN_POINT('Ctrl Pts',(4.16706295593753,-2.98592943548579,31.9366716610356));
#36015=CARTESIAN_POINT('Ctrl Pts',(5.08776703801517,-0.62834293131509,32.0756180463208));
#36016=CARTESIAN_POINT('Ctrl Pts',(4.76830578805043,1.88240489377079,32.2145644316058));
#36017=CARTESIAN_POINT('Ctrl Pts',(3.28654927442038,3.9343083431849,32.353510816891));
#36018=CARTESIAN_POINT('Ctrl Pts',(1.00368208851879,5.02720703150705,32.4924572021761));
#36019=CARTESIAN_POINT('Ctrl Pts',(-1.52383696946585,4.89470215262752,32.6314035874613));
#36020=CARTESIAN_POINT('Ctrl Pts',(-3.67991414202303,3.56909234677198,32.7703499727464));
#36021=CARTESIAN_POINT('Ctrl Pts',(-4.93899624587321,1.37350076654429,32.9092963580315));
#36022=CARTESIAN_POINT('Ctrl Pts',(-4.99417654497228,-1.15688759613717,
33.0482427433167));
#36023=CARTESIAN_POINT('Ctrl Pts',(-3.83200460154611,-3.40527957826912,
33.1871891286017));
#36024=CARTESIAN_POINT('Ctrl Pts',(-1.73576487876693,-4.82361986044573,
33.3261355138869));
#36025=CARTESIAN_POINT('Ctrl Pts',(0.783575078582641,-5.06618183336047,
33.465081899172));
#36026=CARTESIAN_POINT('Ctrl Pts',(3.1119152043264,-4.07383996169826,33.6040282844571));
#36027=CARTESIAN_POINT('Ctrl Pts',(4.6817124715184,-2.08848189038745,33.7429746697423));
#36028=CARTESIAN_POINT('Ctrl Pts',(5.11032197237104,0.405952720337242,33.8819210550274));
#36029=CARTESIAN_POINT('Ctrl Pts',(4.29326827788569,2.80143459080304,34.0208674403125));
#36030=CARTESIAN_POINT('Ctrl Pts',(2.42971177782606,4.51405460192282,34.1598138255976));
#36031=CARTESIAN_POINT('Ctrl Pts',(-0.0260975300371019,5.126354181226,34.2987602108827));
#36032=CARTESIAN_POINT('Ctrl Pts',(-2.47554545150775,4.48908264459084,34.4377065961679));
#36033=CARTESIAN_POINT('Ctrl Pts',(-4.32156840797594,2.75757769929185,34.576652981453));
#36034=CARTESIAN_POINT('Ctrl Pts',(-5.11419027913967,0.353901202598625,
34.7155993667381));
#36035=CARTESIAN_POINT('Ctrl Pts',(-4.66020603837503,-2.13604025063673,
34.8545457520232));
#36036=CARTESIAN_POINT('Ctrl Pts',(-3.07027631783819,-4.1053126074112,34.9934921373084));
#36037=CARTESIAN_POINT('Ctrl Pts',(-0.731953398335376,-5.07389717033296,
35.1324385225935));
#36038=CARTESIAN_POINT('Ctrl Pts',(1.78478634381352,-4.80569724175214,35.2713849078787));
#36039=CARTESIAN_POINT('Ctrl Pts',(3.86647665619062,-3.36608772012562,35.4103312931637));
#36040=CARTESIAN_POINT('Ctrl Pts',(5.00569647604503,-1.10597968433321,35.5492776784489));
#36041=CARTESIAN_POINT('Ctrl Pts',(4.92475602009802,1.42371570720972,35.688224063734));
#36042=CARTESIAN_POINT('Ctrl Pts',(3.6433848763349,3.60637420622729,35.8271704490192));
#36043=CARTESIAN_POINT('Ctrl Pts',(1.47392283116901,4.90996331556623,35.9661168343042));
#36044=CARTESIAN_POINT('Ctrl Pts',(-1.05481431123771,5.01672752312256,36.1050632195895));
#36045=CARTESIAN_POINT('Ctrl Pts',(-3.32643588000179,3.90064258920041,36.2440096048745));
#36046=CARTESIAN_POINT('Ctrl Pts',(-4.78722424299679,1.83375906806513,36.3829559901597));
#36047=CARTESIAN_POINT('Ctrl Pts',(-5.08110588669488,-0.680111197262768,
36.5219023754447));
#36048=CARTESIAN_POINT('Ctrl Pts',(-4.13644588294086,-3.02820140181411,
36.6608487607299));
#36049=CARTESIAN_POINT('Ctrl Pts',(-2.18350921408743,-4.63815435108003,
36.799795146015));
#36050=CARTESIAN_POINT('Ctrl Pts',(0.30166731741563,-5.11753701521061,36.9387415313002));
#36051=CARTESIAN_POINT('Ctrl Pts',(2.71331112895062,-4.34949778594726,37.0776879165853));
#36052=CARTESIAN_POINT('Ctrl Pts',(4.46357355803887,-2.52124956408992,37.2166343018704));
#36053=CARTESIAN_POINT('Ctrl Pts',(5.12582052919834,-0.0784358011124148,
37.3555806871555));
#36054=CARTESIAN_POINT('Ctrl Pts',(4.53862646442101,2.38349702934671,37.4945270724407));
#36055=CARTESIAN_POINT('Ctrl Pts',(2.84512246952923,4.26444209783968,37.6334734577258));
#36056=CARTESIAN_POINT('Ctrl Pts',(0.458107504940694,5.10591086745201,37.7724198430109));
#36057=CARTESIAN_POINT('Ctrl Pts',(-2.04057315537071,4.70279166772542,37.911366228296));
#36058=CARTESIAN_POINT('Ctrl Pts',(-4.04185523868785,3.15334655595275,38.0503126135812));
#36059=CARTESIAN_POINT('Ctrl Pts',(-5.05791753762779,0.835259513567289,
38.1892589988663));
#36060=CARTESIAN_POINT('Ctrl Pts',(-4.84109045000053,-1.68642566612377,
38.3282053841514));
#36061=CARTESIAN_POINT('Ctrl Pts',(-3.44422652096274,-3.79703725880379,
38.4671517694365));
#36062=CARTESIAN_POINT('Ctrl Pts',(-1.20781740538567,-4.9821045139273,38.6060981547217));
#36063=CARTESIAN_POINT('Ctrl Pts',(1.32300245313715,-4.9527621365699,38.7450445400067));
#36064=CARTESIAN_POINT('Ctrl Pts',(3.53133471261537,-3.71616245876376,38.883990925292));
#36065=CARTESIAN_POINT('Ctrl Pts',(4.87888878517958,-1.57373202747361,39.022937310577));
#36066=CARTESIAN_POINT('Ctrl Pts',(5.03719250782395,0.952302426527237,39.1618836958622));
#36067=CARTESIAN_POINT('Ctrl Pts',(3.96765866000753,3.24620902440288,39.3008300811473));
#36068=CARTESIAN_POINT('Ctrl Pts',(1.93099076639979,4.74883806130785,39.4397764664324));
#36069=CARTESIAN_POINT('Ctrl Pts',(-0.57636452053578,5.09391717756727,39.5787228517175));
#36070=CARTESIAN_POINT('Ctrl Pts',(-2.94322845013388,4.19733183853384,39.7176692370027));
#36071=CARTESIAN_POINT('Ctrl Pts',(-4.59266765079613,2.2776286180539,39.8566156222878));
#36072=CARTESIAN_POINT('Ctrl Pts',(-5.12262414724796,-0.197256478929643,
39.995562007573));
#36073=CARTESIAN_POINT('Ctrl Pts',(-4.40391873975792,-2.62405945170006,
40.134508392858));
#36074=CARTESIAN_POINT('Ctrl Pts',(-2.61173899561465,-4.41123652633059,
40.2734547781432));
#36075=CARTESIAN_POINT('Ctrl Pts',(-0.182936518059435,-5.12315552202035,
40.4124011634283));
#36076=CARTESIAN_POINT('Ctrl Pts',(2.29045753099789,-4.58628308885772,40.5513475487134));
#36077=CARTESIAN_POINT('Ctrl Pts',(4.20554260025436,-2.93148421621083,40.6902939339986));
#36078=CARTESIAN_POINT('Ctrl Pts',(5.09550837920273,-0.562123322698978,
40.8292403192837));
#36079=CARTESIAN_POINT('Ctrl Pts',(4.74342184054261,1.94425757427114,40.9681867045688));
#36080=CARTESIAN_POINT('Ctrl Pts',(3.23510560859279,3.9767172358239,41.1071330898539));
#36081=CARTESIAN_POINT('Ctrl Pts',(0.938218321542545,5.03983478435249,41.2460794751391));
#36082=CARTESIAN_POINT('Ctrl Pts',(-1.58736375981927,4.87447069603047,41.3850258604242));
#36083=CARTESIAN_POINT('Ctrl Pts',(-3.72601902445393,3.52093318622417,41.5239722457093));
#36084=CARTESIAN_POINT('Ctrl Pts',(-4.95644095487116,1.30915290677719,41.6629186309945));
#36085=CARTESIAN_POINT('Ctrl Pts',(-4.97870885688693,-1.22173908458518,
41.8018650162796));
#36086=CARTESIAN_POINT('Ctrl Pts',(-3.78739483258627,-3.45482686317944,
41.9408114015646));
#36087=CARTESIAN_POINT('Ctrl Pts',(-1.6728868540352,-4.84578557573935,42.0797577868498));
#36088=CARTESIAN_POINT('Ctrl Pts',(0.849394567227056,-5.05556298958016,
42.218704172135));
#36089=CARTESIAN_POINT('Ctrl Pts',(3.16463237040904,-4.03302494817558,42.35765055742));
#36090=CARTESIAN_POINT('Ctrl Pts',(4.7084772766451,-2.02741954409147,42.4965969427052));
#36091=CARTESIAN_POINT('Ctrl Pts',(5.10461037894552,0.47237818705881,42.6355433279903));
#36092=CARTESIAN_POINT('Ctrl Pts',(4.25647251163379,2.85703168168524,42.7744897132754));
#36093=CARTESIAN_POINT('Ctrl Pts',(2.37080096672289,4.54527128438262,42.9134360985606));
#36094=CARTESIAN_POINT('Ctrl Pts',(-0.0927636196998844,5.12558125321486,
43.0523824838456));
#36095=CARTESIAN_POINT('Ctrl Pts',(-2.53371667057728,4.45650851067134,43.1913288691309));
#36096=CARTESIAN_POINT('Ctrl Pts',(-4.35706526893369,2.70114244620665,43.3302752544159));
#36097=CARTESIAN_POINT('Ctrl Pts',(-5.11836026782228,0.287361168611337,
43.4692216397011));
#36098=CARTESIAN_POINT('Ctrl Pts',(-4.63203270191418,-2.19646564299215,
43.6081680249862));
#36099=CARTESIAN_POINT('Ctrl Pts',(-3.01662702946576,-4.14489440607887,
43.7471144102713));
#36100=CARTESIAN_POINT('Ctrl Pts',(-0.665905405305666,-5.08298713982556,
43.8860607955565));
#36101=CARTESIAN_POINT('Ctrl Pts',(1.8471335560889,-4.78207966249181,44.0250071808416));
#36102=CARTESIAN_POINT('Ctrl Pts',(3.90992568369618,-3.31551947972265,44.1639535661266));
#36103=CARTESIAN_POINT('Ctrl Pts',(5.01965642945332,-1.04078701120603,44.3028999514119));
#36104=CARTESIAN_POINT('Ctrl Pts',(4.90582410008189,1.48764181559379,44.4418463366969));
#36105=CARTESIAN_POINT('Ctrl Pts',(3.59617582069531,3.65345148306281,44.5807927219821));
#36106=CARTESIAN_POINT('Ctrl Pts',(1.40994405243592,4.92871646997956,44.7197391072672));
#36107=CARTESIAN_POINT('Ctrl Pts',(-1.11996770763229,5.00258539220554,44.8586854925523));
#36108=CARTESIAN_POINT('Ctrl Pts',(-3.37688247046485,3.85705237883987,44.9976318778374));
#36109=CARTESIAN_POINT('Ctrl Pts',(-4.81066745181167,1.77134608152317,45.1365782631226));
#36110=CARTESIAN_POINT('Ctrl Pts',(-5.07183132980518,-0.746133523207451,
45.2755246484077));
#36111=CARTESIAN_POINT('Ctrl Pts',(-4.09671427390505,-3.0817398382131,45.4144710336929));
#36112=CARTESIAN_POINT('Ctrl Pts',(-2.12300530532106,-4.66615867132998,
45.5534174189779));
#36113=CARTESIAN_POINT('Ctrl Pts',(0.368195435139699,-5.11318104451468,
45.6923638042631));
#36114=CARTESIAN_POINT('Ctrl Pts',(2.7696469377403,-4.31384331110022,45.8313101895482));
#36115=CARTESIAN_POINT('Ctrl Pts',(4.49598495960815,-2.46298751832151,45.9702565748334));
#36116=CARTESIAN_POINT('Ctrl Pts',(5.12640710352584,-0.011767811352088,
46.1092029601185));
#36117=CARTESIAN_POINT('Ctrl Pts',(4.50724523145763,2.44232035080534,46.2481493454036));
#36118=CARTESIAN_POINT('Ctrl Pts',(2.78942274123745,4.30108231065426,46.3870957306888));
#36119=CARTESIAN_POINT('Ctrl Pts',(0.391666332192212,5.11143676053596,46.5260421159738));
#36120=CARTESIAN_POINT('Ctrl Pts',(-2.10156044784752,4.67585628049741,46.664988501259));
#36121=CARTESIAN_POINT('Ctrl Pts',(-4.08252273333974,3.10051550637416,46.803934886544));
#36122=CARTESIAN_POINT('Ctrl Pts',(-5.06835235565692,0.769410599168003,
46.9428812718293));
#36123=CARTESIAN_POINT('Ctrl Pts',(-4.81874905953264,-1.74924148531259,
47.0818276571143));
#36124=CARTESIAN_POINT('Ctrl Pts',(-3.39455473229958,-3.84150835555375,
47.2207740423995));
#36125=CARTESIAN_POINT('Ctrl Pts',(-1.14292293438725,-4.99739086165512,
47.3597204276846));
#36126=CARTESIAN_POINT('Ctrl Pts',(1.38730129989963,-4.93513762827236,47.4986668129698));
#36127=CARTESIAN_POINT('Ctrl Pts',(3.57936480620948,-3.66992313186164,47.6376131982548));
#36128=CARTESIAN_POINT('Ctrl Pts',(4.89894259229508,-1.510148944458,47.7765595835401));
#36129=CARTESIAN_POINT('Ctrl Pts',(5.0243818047371,1.01773066266865,47.915505968825));
#36130=CARTESIAN_POINT('Ctrl Pts',(3.92510615240954,3.29753389928866,48.0544523541103));
#36131=CARTESIAN_POINT('Ctrl Pts',(1.86906873270474,4.77354910373812,48.1933987393953));
#36132=CARTESIAN_POINT('Ctrl Pts',(-0.642562158693535,5.08599059227959,
48.3323451246805));
#36133=CARTESIAN_POINT('Ctrl Pts',(-2.99756603670477,4.15870048993547,48.4712915099656));
#36134=CARTESIAN_POINT('Ctrl Pts',(-4.62189956542536,2.21770765030908,48.6102378952508));
#36135=CARTESIAN_POINT('Ctrl Pts',(-5.11962615001036,-0.263858307003834,
48.7491842805358));
#36136=CARTESIAN_POINT('Ctrl Pts',(-4.3694193284947,-2.68111304807841,48.8881306658211));
#36137=CARTESIAN_POINT('Ctrl Pts',(-2.55415199717266,-4.44482430004468,
49.0270770511061));
#36138=CARTESIAN_POINT('Ctrl Pts',(-0.11629033496576,-5.12511086267891,
49.1660234363912));
#36139=CARTESIAN_POINT('Ctrl Pts',(2.34990065829377,-4.55608924149042,49.3049698216764));
#36140=CARTESIAN_POINT('Ctrl Pts',(4.24332623397428,-2.87657943442583,49.4439162069614));
#36141=CARTESIAN_POINT('Ctrl Pts',(5.10235796277362,-0.495737641055859,
49.5828625922466));
#36142=CARTESIAN_POINT('Ctrl Pts',(4.71779440725493,2.00564064112161,49.7218089775318));
#36143=CARTESIAN_POINT('Ctrl Pts',(3.18293456305578,4.01883138234242,49.8607609007809));
#36144=CARTESIAN_POINT('Ctrl Pts',(1.64272913283473,4.70685298774121,49.9533973622685));
#36145=CARTESIAN_POINT('Ctrl Pts',(0.836785021106394,4.84601823601536,49.9997183619944));
#36146=CARTESIAN_POINT('Ctrl Pts',(-2.29311987939507,4.72368461420244,-0.384448231563372));
#36147=CARTESIAN_POINT('Ctrl Pts',(-3.07862444090061,4.34236023028229,-0.338132769801664));
#36148=CARTESIAN_POINT('Ctrl Pts',(-4.45493794042212,3.18067190535823,-0.245501846278247));
#36149=CARTESIAN_POINT('Ctrl Pts',(-5.43361388965546,0.661144042220643,
-0.106555460993121));
#36150=CARTESIAN_POINT('Ctrl Pts',(-5.08774636704661,-2.01883410487796,
0.0323909242920052));
#36151=CARTESIAN_POINT('Ctrl Pts',(-3.50175917389135,-4.2070596791708,0.171337309577131));
#36152=CARTESIAN_POINT('Ctrl Pts',(-1.06218201400962,-5.36961982523882,
0.310283694862257));
#36153=CARTESIAN_POINT('Ctrl Pts',(1.63629588706826,-5.22340199091913,0.449230080147383));
#36154=CARTESIAN_POINT('Ctrl Pts',(3.93592505622498,-3.80391102861263,0.588176465432509));
#36155=CARTESIAN_POINT('Ctrl Pts',(5.27615256431546,-1.4572238740315,0.727122850717634));
#36156=CARTESIAN_POINT('Ctrl Pts',(5.33029639345207,1.24468005167587,0.866069236002761));
#36157=CARTESIAN_POINT('Ctrl Pts',(4.08515656621609,3.64318159744485,1.00501562128788));
#36158=CARTESIAN_POINT('Ctrl Pts',(1.84424244666043,5.1536449711362,1.14396200657301));
#36159=CARTESIAN_POINT('Ctrl Pts',(-0.846213980258722,5.4078833517554,1.28290839185814));
#36160=CARTESIAN_POINT('Ctrl Pts',(-3.33040197159187,4.34392749144419,1.42185477714326));
#36161=CARTESIAN_POINT('Ctrl Pts',(-5.00279005600775,2.221119994778,1.56080116242839));
#36162=CARTESIAN_POINT('Ctrl Pts',(-5.45572629105949,-0.443094936973425,
1.69974754771351));
#36163=CARTESIAN_POINT('Ctrl Pts',(-4.57880553997945,-2.99930366380419,
1.83869393299864));
#36164=CARTESIAN_POINT('Ctrl Pts',(-2.58578102761624,-4.82441902718766,
1.97764031828376));
#36165=CARTESIAN_POINT('Ctrl Pts',(0.0375388471149513,-5.47356131035378,
2.11658670356889));
#36166=CARTESIAN_POINT('Ctrl Pts',(2.65170846647585,-4.78849921548164,2.25553308885402));
#36167=CARTESIAN_POINT('Ctrl Pts',(4.61951261923543,-2.93621962894386,2.39447947413914));
#36168=CARTESIAN_POINT('Ctrl Pts',(5.46129049050343,-0.368223740149896,
2.53342585942427));
#36169=CARTESIAN_POINT('Ctrl Pts',(4.97185506423708,2.28952828394974,2.6723722447094));
#36170=CARTESIAN_POINT('Ctrl Pts',(3.27050835352976,4.38919783729295,2.81131862999452));
#36171=CARTESIAN_POINT('Ctrl Pts',(0.771961014684566,5.4189813374193,2.95026501527965));
#36172=CARTESIAN_POINT('Ctrl Pts',(-1.91475517717252,5.12786458050685,3.08921140056477));
#36173=CARTESIAN_POINT('Ctrl Pts',(-4.13474147116859,3.58680854112624,3.2281577858499));
#36174=CARTESIAN_POINT('Ctrl Pts',(-5.34686655783527,1.17145232805873,3.36710417113502));
#36175=CARTESIAN_POINT('Ctrl Pts',(-5.255669678202,-1.5294504823136,3.50605055642015));
#36176=CARTESIAN_POINT('Ctrl Pts',(-3.8833804681057,-3.85754308908115,3.64499694170528));
#36177=CARTESIAN_POINT('Ctrl Pts',(-1.56450038785265,-5.24534279915276,
3.7839433269904));
#36178=CARTESIAN_POINT('Ctrl Pts',(1.13573346282413,-5.35456740041784,3.92288971227553));
#36179=CARTESIAN_POINT('Ctrl Pts',(3.55912734490322,-4.15859292152604,4.06183609756065));
#36180=CARTESIAN_POINT('Ctrl Pts',(5.11496846513371,-1.9489433406052,4.20078248284578));
#36181=CARTESIAN_POINT('Ctrl Pts',(5.42401378721696,0.735769651645315,4.33972886813091));
#36182=CARTESIAN_POINT('Ctrl Pts',(4.41093217047509,3.24113559291651,4.47867525341603));
#36183=CARTESIAN_POINT('Ctrl Pts',(2.32266666285525,4.9564606441959,4.61762163870116));
#36184=CARTESIAN_POINT('Ctrl Pts',(-0.331758940468846,5.46362686771537,
4.75656802398628));
#36185=CARTESIAN_POINT('Ctrl Pts',(-2.90531685989736,4.63901029184008,4.89551440927141));
#36186=CARTESIAN_POINT('Ctrl Pts',(-4.77069116531186,2.68361479154843,5.03446079455654));
#36187=CARTESIAN_POINT('Ctrl Pts',(-5.47318876098439,0.0740765201418065,
5.17340717984166));
#36188=CARTESIAN_POINT('Ctrl Pts',(-4.84157280421231,-2.55351822506004,
5.31235356512679));
#36189=CARTESIAN_POINT('Ctrl Pts',(-3.02980243009377,-4.55868180275834,
5.45129995041191));
#36190=CARTESIAN_POINT('Ctrl Pts',(-0.479504543086973,-5.45264687444191,
5.59024633569704));
#36191=CARTESIAN_POINT('Ctrl Pts',(2.18767466070378,-5.0175055678212,5.72919272098216));
#36192=CARTESIAN_POINT('Ctrl Pts',(4.32159865612501,-3.35932546794452,5.86813910626729));
#36193=CARTESIAN_POINT('Ctrl Pts',(5.40211419312394,-0.88229518226665,6.00708549155243));
#36194=CARTESIAN_POINT('Ctrl Pts',(5.16584091255546,1.80979838942637,6.14603187683754));
#36195=CARTESIAN_POINT('Ctrl Pts',(3.6703714536382,4.06074573650209,6.28497826212267));
#36196=CARTESIAN_POINT('Ctrl Pts',(1.28023299778984,5.3218686582414,6.42392464740779));
#36197=CARTESIAN_POINT('Ctrl Pts',(-1.42196781644337,5.28576296036829,6.56287103269293));
#36198=CARTESIAN_POINT('Ctrl Pts',(-3.7775577941236,3.96122956369082,6.70181741797804));
#36199=CARTESIAN_POINT('Ctrl Pts',(-5.21235163844033,1.67112924139653,6.84076380326317));
#36200=CARTESIAN_POINT('Ctrl Pts',(-5.37661211279168,-1.02631609788793,
6.9797101885483));
#36201=CARTESIAN_POINT('Ctrl Pts',(-4.23030001251415,-3.47359242691553,
7.11865657383343));
#36202=CARTESIAN_POINT('Ctrl Pts',(-2.05283389506973,-5.07416550217421,
7.25760295911855));
#36203=CARTESIAN_POINT('Ctrl Pts',(0.62501940796803,-5.43788867887764,7.39654934440369));
#36204=CARTESIAN_POINT('Ctrl Pts',(3.15052151335387,-4.47610285159943,7.5354957296888));
#36205=CARTESIAN_POINT('Ctrl Pts',(4.9080703045409,-2.42324749662225,7.67444211497394));
#36206=CARTESIAN_POINT('Ctrl Pts',(5.46925562361168,0.220284969514861,7.81338850025905));
#36207=CARTESIAN_POINT('Ctrl Pts',(4.69728610956982,2.81012201675383,7.95233488554419));
#36208=CARTESIAN_POINT('Ctrl Pts',(2.78033268721492,4.71497960680705,8.09128127082931));
#36209=CARTESIAN_POINT('Ctrl Pts',(0.185661086243624,5.47054042168203,8.23022765611444));
#36210=CARTESIAN_POINT('Ctrl Pts',(-2.45426621156841,4.89263322832968,8.36917404139956));
#36211=CARTESIAN_POINT('Ctrl Pts',(-4.49595545161403,3.12212541729256,8.50812042668468));
#36212=CARTESIAN_POINT('Ctrl Pts',(-5.44173600640782,0.590585963909393,
8.64706681196982));
#36213=CARTESIAN_POINT('Ctrl Pts',(-5.06106975441018,-2.0849113854542,8.78601319725493));
#36214=CARTESIAN_POINT('Ctrl Pts',(-3.44674574930196,-4.25220252150235,
8.92495958254008));
#36215=CARTESIAN_POINT('Ctrl Pts',(-0.99226248479567,-5.38300080860752,
9.06390596782517));
#36216=CARTESIAN_POINT('Ctrl Pts',(1.70408907374516,-5.20166924870704,9.20285235311033));
#36217=CARTESIAN_POINT('Ctrl Pts',(3.98506151288443,-3.75240819777504,9.34179873839543));
#36218=CARTESIAN_POINT('Ctrl Pts',(5.29465788519347,-1.38848133691482,9.48074512368058));
#36219=CARTESIAN_POINT('Ctrl Pts',(5.31365838210577,1.31389388554757,9.61969150896568));
#36220=CARTESIAN_POINT('Ctrl Pts',(4.03743154990377,3.69600176191026,9.75863789425084));
#36221=CARTESIAN_POINT('Ctrl Pts',(1.7770632266955,5.17719314228556,9.89758427953593));
#36222=CARTESIAN_POINT('Ctrl Pts',(-0.916471982914659,5.39642118896724,
10.0365306648211));
#36223=CARTESIAN_POINT('Ctrl Pts',(-3.38661316278514,4.30024811259217,10.1754770501062));
#36224=CARTESIAN_POINT('Ctrl Pts',(-5.0312526626174,2.15587086559178,10.3144234353914));
#36225=CARTESIAN_POINT('Ctrl Pts',(-5.44950245507848,-0.514009276468483,
10.4533698206764));
#36226=CARTESIAN_POINT('Ctrl Pts',(-4.53941233512393,-3.05859742299095,
10.5923162059616));
#36227=CARTESIAN_POINT('Ctrl Pts',(-2.52282072565491,-4.85763915193463,
10.7312625912467));
#36228=CARTESIAN_POINT('Ctrl Pts',(0.108719402395609,-5.47261022143409,
10.8702089765319));
#36229=CARTESIAN_POINT('Ctrl Pts',(2.7137587035089,-4.75360876001925,11.0091553618169));
#36230=CARTESIAN_POINT('Ctrl Pts',(4.65730752393128,-2.87589449940974,11.1481017471021));
#36231=CARTESIAN_POINT('Ctrl Pts',(5.46561739007695,-0.297168453054067,
11.2870481323872));
#36232=CARTESIAN_POINT('Ctrl Pts',(4.94165925834944,2.35399369552495,11.4259945176723));
#36233=CARTESIAN_POINT('Ctrl Pts',(3.21315020100368,4.43135964800785,11.5649409029575));
#36234=CARTESIAN_POINT('Ctrl Pts',(0.701421814597499,5.42856242316589,11.7038872882426));
#36235=CARTESIAN_POINT('Ctrl Pts',(-1.98128118819784,5.10252950971334,11.8428336735277));
#36236=CARTESIAN_POINT('Ctrl Pts',(-4.1810382887395,3.53273284756947,11.9817800588128));
#36237=CARTESIAN_POINT('Ctrl Pts',(-5.3616491314251,1.10181719703885,12.120726444098));
#36238=CARTESIAN_POINT('Ctrl Pts',(-5.23533469123401,-1.59767118486996,
12.2596728293831));
#36239=CARTESIAN_POINT('Ctrl Pts',(-3.83288466205176,-3.90772027038919,
12.3986192146682));
#36240=CARTESIAN_POINT('Ctrl Pts',(-1.49615233494258,-5.26524555313881,
12.5375655999534));
#36241=CARTESIAN_POINT('Ctrl Pts',(1.2052736275839,-5.33934434428544,12.6765119852385));
#36242=CARTESIAN_POINT('Ctrl Pts',(3.61290890406165,-4.1119547413796,12.8154583705236));
#36243=CARTESIAN_POINT('Ctrl Pts',(5.13988192985733,-1.88225829559289,12.9544047558087));
#36244=CARTESIAN_POINT('Ctrl Pts',(5.4139863921806,0.806246791922473,13.0933511410939));
#36245=CARTESIAN_POINT('Ctrl Pts',(4.36840813680796,3.29822571915148,13.232297526379));
#36246=CARTESIAN_POINT('Ctrl Pts',(2.25801140861569,4.98624778994821,13.3712439116641));
#36247=CARTESIAN_POINT('Ctrl Pts',(-0.402785416003514,5.45885028672311,
13.5101902969492));
#36248=CARTESIAN_POINT('Ctrl Pts',(-2.96540154456344,4.60083429648395,13.6491366822344));
#36249=CARTESIAN_POINT('Ctrl Pts',(-4.80518815603382,2.6213449466475,13.7880830675195));
#36250=CARTESIAN_POINT('Ctrl Pts',(-5.47368926631531,0.00289137107776702,
13.9270294528046));
#36251=CARTESIAN_POINT('Ctrl Pts',(-4.80795482380209,-2.61626698876096,
14.0659758380897));
#36252=CARTESIAN_POINT('Ctrl Pts',(-2.97026049280476,-4.59769889717513,
14.2049222233749));
#36253=CARTESIAN_POINT('Ctrl Pts',(-0.408552254962224,-5.45842171320313,
14.34386860866));
#36254=CARTESIAN_POINT('Ctrl Pts',(2.25274237100424,-4.9886305088756,14.4828149939451));
#36255=CARTESIAN_POINT('Ctrl Pts',(4.36492125136605,-3.30283893242996,14.6217613792302));
#36256=CARTESIAN_POINT('Ctrl Pts',(5.41313160239223,-0.811966008761832,
14.7607077645154));
#36257=CARTESIAN_POINT('Ctrl Pts',(5.14186759444916,1.87682715915871,14.8996541498005));
#36258=CARTESIAN_POINT('Ctrl Pts',(3.61725100865776,4.10813554846558,15.0386005350856));
#36259=CARTESIAN_POINT('Ctrl Pts',(1.21091376531386,5.33806803976639,15.1775469203707));
#36260=CARTESIAN_POINT('Ctrl Pts',(-1.49058897216811,5.26682324178939,15.3164933056559));
#36261=CARTESIAN_POINT('Ctrl Pts',(-3.82875416809305,3.91176738374259,15.455439690941));
#36262=CARTESIAN_POINT('Ctrl Pts',(-5.23364389194872,1.60320122145348,15.5943860762261));
#36263=CARTESIAN_POINT('Ctrl Pts',(-5.36281016648893,-1.09615220768151,
15.7333324615112));
#36264=CARTESIAN_POINT('Ctrl Pts',(-4.18476815080863,-3.52831377121986,
15.8722788467964));
#36265=CARTESIAN_POINT('Ctrl Pts',(-1.98667070717921,-5.10043351544144,
16.0112252320815));
#36266=CARTESIAN_POINT('Ctrl Pts',(0.695686357383897,-5.42930041868675,
16.1501716173666));
#36267=CARTESIAN_POINT('Ctrl Pts',(3.20846684818567,-4.43475174370513,16.2891180026517));
#36268=CARTESIAN_POINT('Ctrl Pts',(4.93916959753494,-2.35921305332702,16.4280643879369));
#36269=CARTESIAN_POINT('Ctrl Pts',(5.46592828691201,0.291394074299996,16.567010773222));
#36270=CARTESIAN_POINT('Ctrl Pts',(4.66034319596094,2.87097262962618,16.7059571585071));
#36271=CARTESIAN_POINT('Ctrl Pts',(2.71877919247985,4.75073912636138,16.8449035437923));
#36272=CARTESIAN_POINT('Ctrl Pts',(0.114500942297094,5.47249230958027,16.9838499290774));
#36273=CARTESIAN_POINT('Ctrl Pts',(-2.51768741030621,4.8603017034118,17.1227963143625));
#36274=CARTESIAN_POINT('Ctrl Pts',(-4.53617851225878,3.06339142930247,17.2617426996476));
#36275=CARTESIAN_POINT('Ctrl Pts',(-5.44895638307774,0.519766177736342,
17.4006890849328));
#36276=CARTESIAN_POINT('Ctrl Pts',(-5.03352744890496,-2.15055433907689,
17.5396354702179));
#36277=CARTESIAN_POINT('Ctrl Pts',(-3.39115431831494,-4.29666788727916,
17.678581855503));
#36278=CARTESIAN_POINT('Ctrl Pts',(-0.92217258128593,-5.39544996033942,
17.8175282407881));
#36279=CARTESIAN_POINT('Ctrl Pts',(1.77159273111631,-5.1790676515429,17.9564746260733));
#36280=CARTESIAN_POINT('Ctrl Pts',(4.03352461419432,-3.70026508927276,18.0954210113584));
#36281=CARTESIAN_POINT('Ctrl Pts',(5.31226733882865,-1.31950682643796,18.2343673966435));
#36282=CARTESIAN_POINT('Ctrl Pts',(5.2961218071944,1.382886961238,18.3733137819286));
#36283=CARTESIAN_POINT('Ctrl Pts',(3.989023562812,3.74819604070184,18.5122601672138));
#36284=CARTESIAN_POINT('Ctrl Pts',(1.70958348470646,5.19986604183425,18.6512065524989));
#36285=CARTESIAN_POINT('Ctrl Pts',(-0.986574999356629,5.38404609144894,
18.790152937784));
#36286=CARTESIAN_POINT('Ctrl Pts',(-3.44225153868445,4.25584150182154,18.9290993230691));
#36287=CARTESIAN_POINT('Ctrl Pts',(-5.05886430198859,2.0902570459797,19.0680457083543));
#36288=CARTESIAN_POINT('Ctrl Pts',(-5.44235690079696,-0.584836651168256,
19.2069920936394));
#36289=CARTESIAN_POINT('Ctrl Pts',(-4.49925134710757,-3.11737387230869,
19.3459384789245));
#36290=CARTESIAN_POINT('Ctrl Pts',(-2.45943371931255,-4.89003766084787,
19.4848848642096));
#36291=CARTESIAN_POINT('Ctrl Pts',(0.179881568724695,-5.47073351255893,
19.6238312494948));
#36292=CARTESIAN_POINT('Ctrl Pts',(2.77534994244003,-4.71791428930203,19.7627776347799));
#36293=CARTESIAN_POINT('Ctrl Pts',(4.69431470323778,-2.81508294925169,19.901724020065));
#36294=CARTESIAN_POINT('Ctrl Pts',(5.46901984893268,-0.226062903154081,
20.0406704053501));
#36295=CARTESIAN_POINT('Ctrl Pts',(4.91062763261785,2.41806095828293,20.1796167906353));
#36296=CARTESIAN_POINT('Ctrl Pts',(3.15524858435129,4.47277194982611,20.3185631759204));
#36297=CARTESIAN_POINT('Ctrl Pts',(0.630763977781736,5.43722533545695,20.4575095612055));
#36298=CARTESIAN_POINT('Ctrl Pts',(-2.04747209030348,5.07633140994857,20.5964559464906));
#36299=CARTESIAN_POINT('Ctrl Pts',(-4.22662793601492,3.47805963644969,20.7354023317758));
#36300=CARTESIAN_POINT('Ctrl Pts',(-5.37552484916865,1.03199570743896,20.8743487170609));
#36301=CARTESIAN_POINT('Ctrl Pts',(-5.21411421292796,-1.66562166134591,
21.013295102346));
#36302=CARTESIAN_POINT('Ctrl Pts',(-3.78174057152866,-3.9572365097194,21.1522414876312));
#36303=CARTESIAN_POINT('Ctrl Pts',(-1.4275512265908,-5.28425775673948,21.2911878729163));
#36304=CARTESIAN_POINT('Ctrl Pts',(1.27460993539455,-5.3232182048828,21.4301342582014));
#36305=CARTESIAN_POINT('Ctrl Pts',(3.66607938489734,-4.06462107555339,21.5690806434865));
#36306=CARTESIAN_POINT('Ctrl Pts',(5.16392604788226,-1.81525489014774,21.7080270287717));
#36307=CARTESIAN_POINT('Ctrl Pts',(5.40304328910642,0.876587565645492,21.8469734140568));
#36308=CARTESIAN_POINT('Ctrl Pts',(4.32514524157863,3.35475799178598,21.9859197993419));
#36309=CARTESIAN_POINT('Ctrl Pts',(2.19297424000723,5.01519157429372,22.124866184627));
#36310=CARTESIAN_POINT('Ctrl Pts',(-0.47374376542617,5.45315040952677,22.2638125699122));
#36311=CARTESIAN_POINT('Ctrl Pts',(-3.02498466867256,4.56188012758973,22.4027589551973));
#36312=CARTESIAN_POINT('Ctrl Pts',(-4.83887240931995,2.55863173405716,22.5417053404824));
#36313=CARTESIAN_POINT('Ctrl Pts',(-5.47326396561445,-0.0682942670254661,
22.6806517257675));
#36314=CARTESIAN_POINT('Ctrl Pts',(-4.77352363800884,-2.67857324364538,
22.8195981110527));
#36315=CARTESIAN_POINT('Ctrl Pts',(-2.91021617312862,-4.63593834836731,
22.9585444963378));
#36316=CARTESIAN_POINT('Ctrl Pts',(-0.337530865336959,-5.4632733282481,
23.0974908816229));
#36317=CARTESIAN_POINT('Ctrl Pts',(2.31742905812749,-4.95891168551614,23.2364372669081));
#36318=CARTESIAN_POINT('Ctrl Pts',(4.4075055748079,-3.2457937630477,23.3753836521932));
#36319=CARTESIAN_POINT('Ctrl Pts',(5.42323344819965,-0.741499501369069,
23.5143300374783));
#36320=CARTESIAN_POINT('Ctrl Pts',(5.11702459379388,1.94353848706702,23.6532764227634));
#36321=CARTESIAN_POINT('Ctrl Pts',(3.56351875094202,4.15483052071765,23.7922228080486));
#36322=CARTESIAN_POINT('Ctrl Pts',(1.14138972192999,5.35336455389269,23.9311691933337));
#36323=CARTESIAN_POINT('Ctrl Pts',(-1.55895801342421,5.24699270597763,24.0701155786188));
#36324=CARTESIAN_POINT('Ctrl Pts',(-3.87930295621489,3.86164357730029,24.2090619639039));
#36325=CARTESIAN_POINT('Ctrl Pts',(-5.25405094009607,1.53500204008914,24.348008349189));
#36326=CARTESIAN_POINT('Ctrl Pts',(-5.34810116796638,-1.16580291704848,
24.4869547344742));
#36327=CARTESIAN_POINT('Ctrl Pts',(-4.13852848794609,-3.58243834540955,
24.6259011197593));
#36328=CARTESIAN_POINT('Ctrl Pts',(-1.92017149880326,-5.12583885421554,
24.7648475050444));
#36329=CARTESIAN_POINT('Ctrl Pts',(0.766235640159479,-5.41979386028211,
24.9037938903296));
#36330=CARTESIAN_POINT('Ctrl Pts',(3.26586951100659,-4.39265055305789,25.0427402756147));
#36331=CARTESIAN_POINT('Ctrl Pts',(4.96943349180918,-2.29477957867138,25.1816866608998));
#36332=CARTESIAN_POINT('Ctrl Pts',(5.46167645685312,0.362453893424401,25.3206330461849));
#36333=CARTESIAN_POINT('Ctrl Pts',(4.62261204362843,2.93133765341074,25.4595794314701));
#36334=CARTESIAN_POINT('Ctrl Pts',(2.65676585027213,4.78569511785174,25.5985258167552));
#36335=CARTESIAN_POINT('Ctrl Pts',(0.0433214319493474,5.47351859389697,
25.7374722020403));
#36336=CARTESIAN_POINT('Ctrl Pts',(-2.58068277372936,4.82714811929141,25.8764185873254));
#36337=CARTESIAN_POINT('Ctrl Pts',(-4.5756343350821,3.00413930699294,26.0153649726106));
#36338=CARTESIAN_POINT('Ctrl Pts',(-5.45525513697349,0.448858479619654,
26.1543113578957));
#36339=CARTESIAN_POINT('Ctrl Pts',(-5.00513378523042,-2.21583355334896,
26.2932577431808));
#36340=CARTESIAN_POINT('Ctrl Pts',(-3.33498931601805,-4.34040652545905,
26.4322041284659));
#36341=CARTESIAN_POINT('Ctrl Pts',(-0.851926703825804,-5.40698653923892,
26.5711505137511));
#36342=CARTESIAN_POINT('Ctrl Pts',(1.83879674574985,-5.15559007990567,26.7100968990362));
#36343=CARTESIAN_POINT('Ctrl Pts',(4.08130549529846,-3.64749612724247,26.8490432843213));
#36344=CARTESIAN_POINT('Ctrl Pts',(5.32897828893076,-1.25030913789616,26.9879896696064));
#36345=CARTESIAN_POINT('Ctrl Pts',(5.27768945956457,1.45164613890688,27.1269360548916));
#36346=CARTESIAN_POINT('Ctrl Pts',(3.93994088231041,3.79975635904478,27.2658824401767));
#36347=CARTESIAN_POINT('Ctrl Pts',(1.64181458806782,5.22165944912245,27.4048288254618));
#36348=CARTESIAN_POINT('Ctrl Pts',(-1.05651114898524,5.37076034991994,27.5437752107469));
#36349=CARTESIAN_POINT('Ctrl Pts',(-3.49730770081858,4.21071506872612,27.6827215960321));
#36350=CARTESIAN_POINT('Ctrl Pts',(-5.08562029777881,2.02428968554951,27.8216679813172));
#36351=CARTESIAN_POINT('Ctrl Pts',(-5.43429083996117,-0.655565108068201,
27.9606143666024));
#36352=CARTESIAN_POINT('Ctrl Pts',(-4.45832936703756,-3.1756230568524,28.0995607518874));
#36353=CARTESIAN_POINT('Ctrl Pts',(-2.3956307305383,-4.92160908109355,28.2385071371726));
#36354=CARTESIAN_POINT('Ctrl Pts',(0.251013310337818,-5.46793149758073,
28.3774535224577));
#36355=CARTESIAN_POINT('Ctrl Pts',(2.83647176566412,-4.68142184243126,28.5163999077429));
#36356=CARTESIAN_POINT('Ctrl Pts',(4.7305278979654,-2.75379526304575,28.6553462930279));
#36357=CARTESIAN_POINT('Ctrl Pts',(5.47149729153014,-0.15491911754329,28.7942926783131));
#36358=CARTESIAN_POINT('Ctrl Pts',(4.87876543568261,2.48171923629383,28.9332390635982));
#36359=CARTESIAN_POINT('Ctrl Pts',(3.0968132968913,4.51342773824943,29.0721854488833));
#36360=CARTESIAN_POINT('Ctrl Pts',(0.559999455133565,5.44496860913378,29.2111318341684));
#36361=CARTESIAN_POINT('Ctrl Pts',(-2.11331668813089,5.04927471226013,29.3500782194536));
#36362=CARTESIAN_POINT('Ctrl Pts',(-4.27150270207461,3.42279815507304,29.4890246047387));
#36363=CARTESIAN_POINT('Ctrl Pts',(-5.38849136416299,0.961999668681364,
29.6279709900239));
#36364=CARTESIAN_POINT('Ctrl Pts',(-5.1920118324616,-1.73329041876452,29.7669173753089));
#36365=CARTESIAN_POINT('Ctrl Pts',(-3.72995684691932,-4.00608343202207,
29.9058637605941));
#36366=CARTESIAN_POINT('Ctrl Pts',(-1.35870866581594,-5.30237619427732,
30.0448101458792));
#36367=CARTESIAN_POINT('Ctrl Pts',(1.34373065888744,-5.30619170974514,30.1837565311644));
#36368=CARTESIAN_POINT('Ctrl Pts',(3.71862979428907,-4.0165999299442,30.3227029164495));
#36369=CARTESIAN_POINT('Ctrl Pts',(5.18709675244689,-1.74794445705719,30.4616493017346));
#36370=CARTESIAN_POINT('Ctrl Pts',(5.39118632888328,0.946780075553036,30.6005956870197));
#36371=CARTESIAN_POINT('Ctrl Pts',(4.28115080216432,3.41072284909372,30.7395420723048));
#36372=CARTESIAN_POINT('Ctrl Pts',(2.12756615725283,5.04328710175364,30.87848845759));
#36373=CARTESIAN_POINT('Ctrl Pts',(-0.544621987020308,5.44652820018919,
31.0174348428751));
#36374=CARTESIAN_POINT('Ctrl Pts',(-3.08405615448515,4.52215437376749,31.1563812281602));
#36375=CARTESIAN_POINT('Ctrl Pts',(-4.87173822790043,2.49548576093229,31.2953276134453));
#36376=CARTESIAN_POINT('Ctrl Pts',(-5.4719129308161,-0.13946835400816,31.4342739987305));
#36377=CARTESIAN_POINT('Ctrl Pts',(-4.73828507043673,-2.74042645139009,
31.5732203840156));
#36378=CARTESIAN_POINT('Ctrl Pts',(-2.84967962681054,-4.67339368861035,
31.7121667693007));
#36379=CARTESIAN_POINT('Ctrl Pts',(-0.266452386590298,-5.46720089898684,
31.8511131545859));
#36380=CARTESIAN_POINT('Ctrl Pts',(2.38172378113,-4.92835412430985,31.990059539871));
#36381=CARTESIAN_POINT('Ctrl Pts',(4.44934442384521,-3.18819960827417,32.1290059251561));
#36382=CARTESIAN_POINT('Ctrl Pts',(5.43241802194542,-0.670907578616172,
32.2679523104412));
#36383=CARTESIAN_POINT('Ctrl Pts',(5.09131611247224,2.00992108976518,32.4068986957263));
#36384=CARTESIAN_POINT('Ctrl Pts',(3.50918376862985,4.20082275538816,32.5458450810115));
#36385=CARTESIAN_POINT('Ctrl Pts',(1.07167262676009,5.36775561340635,32.6847914662966));
#36386=CARTESIAN_POINT('Ctrl Pts',(-1.62706337644393,5.22627470702,32.8237378515817));
#36387=CARTESIAN_POINT('Ctrl Pts',(-3.92919560879436,3.81086662217839,32.9626842368669));
#36388=CARTESIAN_POINT('Ctrl Pts',(-5.27356933128557,1.46654323234143,33.101630622152));
#36389=CARTESIAN_POINT('Ctrl Pts',(-5.33248760506705,-1.23525644544303,
33.2405770074371));
#36390=CARTESIAN_POINT('Ctrl Pts',(-4.09158884478678,-3.63595699499023,
33.3795233927222));
#36391=CARTESIAN_POINT('Ctrl Pts',(-1.85334751745077,-5.15037722150147,
33.5184697780074));
#36392=CARTESIAN_POINT('Ctrl Pts',(0.83665532376664,-5.40937061157905,33.6574161632925));
#36393=CARTESIAN_POINT('Ctrl Pts',(3.32271979287475,-4.3498064005471,33.7963625485776));
#36394=CARTESIAN_POINT('Ctrl Pts',(4.9988568686048,-2.22995797077088,33.9353089338628));
#36395=CARTESIAN_POINT('Ctrl Pts',(5.4565008525788,0.433452408009289,34.0742553191479));
#36396=CARTESIAN_POINT('Ctrl Pts',(4.58409903432438,2.99120687811935,34.213201704433));
#36397=CARTESIAN_POINT('Ctrl Pts',(2.59430314937227,4.8198416689098,34.3521480897182));
#36398=CARTESIAN_POINT('Ctrl Pts',(-0.0278654056765308,5.473619101049,34.4910944750032));
#36399=CARTESIAN_POINT('Ctrl Pts',(-2.64324164696075,4.79317808348222,34.6300408602884));
#36400=CARTESIAN_POINT('Ctrl Pts',(-4.6143162466254,2.94437907211879,34.7689872455735));
#36401=CARTESIAN_POINT('Ctrl Pts',(-5.46063120273975,0.377874862708882,
34.9079336308586));
#36402=CARTESIAN_POINT('Ctrl Pts',(-4.97589356581932,-2.28073798710854,
35.0468800161437));
#36403=CARTESIAN_POINT('Ctrl Pts',(-3.2782602420183,-4.38341103819895,35.1858264014289));
#36404=CARTESIAN_POINT('Ctrl Pts',(-0.781536733626139,-5.41760859403806,
35.324772786714));
#36405=CARTESIAN_POINT('Ctrl Pts',(1.90568975092798,-5.13124050473276,35.4637191719991));
#36406=CARTESIAN_POINT('Ctrl Pts',(4.12839607465902,-3.59411023689345,35.6026655572843));
#36407=CARTESIAN_POINT('Ctrl Pts',(5.34478790905178,-1.18089997521211,35.7416119425694));
#36408=CARTESIAN_POINT('Ctrl Pts',(5.25836445681711,1.52015978880005,35.8805583278545));
#36409=CARTESIAN_POINT('Ctrl Pts',(3.89019181011998,3.85067399615672,36.0195047131396));
#36410=CARTESIAN_POINT('Ctrl Pts',(1.57376799904008,5.24256967806815,36.1584510984248));
#36411=CARTESIAN_POINT('Ctrl Pts',(-1.12626860297622,5.35656621149707,36.2973974837099));
#36412=CARTESIAN_POINT('Ctrl Pts',(-3.55177233712678,4.16487644587724,36.436343868995));
#36413=CARTESIAN_POINT('Ctrl Pts',(-5.11151612454633,1.9579799418546,36.5752902542801));
#36414=CARTESIAN_POINT('Ctrl Pts',(-5.42530563684426,-0.726182684335063,
36.7142366395653));
#36415=CARTESIAN_POINT('Ctrl Pts',(-4.4166533163547,-3.23333512450152,36.8531830248503));
#36416=CARTESIAN_POINT('Ctrl Pts',(-2.33142255080919,-4.95234807276109,
36.9921294101355));
#36417=CARTESIAN_POINT('Ctrl Pts',(0.32210259619121,-5.46420465042526,37.1310757954206));
#36418=CARTESIAN_POINT('Ctrl Pts',(2.89711383518983,-4.64413759164755,37.2700221807058));
#36419=CARTESIAN_POINT('Ctrl Pts',(4.76594098310544,-2.69204180683697,37.4089685659909));
#36420=CARTESIAN_POINT('Ctrl Pts',(5.47304929884092,-0.0837491293026769,
37.547914951276));
#36421=CARTESIAN_POINT('Ctrl Pts',(4.84607805663556,2.54495776255665,37.6868613365611));
#36422=CARTESIAN_POINT('Ctrl Pts',(3.03785422222122,4.55332013686002,37.8258077218463));
#36423=CARTESIAN_POINT('Ctrl Pts',(0.489140215586399,5.45179093451851,37.9647541071314));
#36424=CARTESIAN_POINT('Ctrl Pts',(-2.17880384489038,5.02136399294982,38.1037004924165));
#36425=CARTESIAN_POINT('Ctrl Pts',(-4.3156549969136,3.36695775022748,38.2426468777017));
#36426=CARTESIAN_POINT('Ctrl Pts',(-5.40054648328439,0.89184091971992,38.3815932629867));
#36427=CARTESIAN_POINT('Ctrl Pts',(-5.16903128817595,-1.80066601180235,
38.520539648272));
#36428=CARTESIAN_POINT('Ctrl Pts',(-3.67754224679271,-4.05425277545157,
38.659486033557));
#36429=CARTESIAN_POINT('Ctrl Pts',(-1.28963629647555,-5.3195978012454,38.7984324188422));
#36430=CARTESIAN_POINT('Ctrl Pts',(1.41262410715728,-5.28826773869103,38.9373788041273));
#36431=CARTESIAN_POINT('Ctrl Pts',(3.77055124399274,-3.96789942672782,39.0763251894124));
#36432=CARTESIAN_POINT('Ctrl Pts',(5.20939012451653,-1.68033838103866,39.2152715746975));
#36433=CARTESIAN_POINT('Ctrl Pts',(5.37841751696762,1.0168124494606,39.3542179599827));
#36434=CARTESIAN_POINT('Ctrl Pts',(4.23643225967382,3.46611082531952,39.4931643452678));
#36435=CARTESIAN_POINT('Ctrl Pts',(2.06179822331107,5.07052962032108,39.6321107305529));
#36436=CARTESIAN_POINT('Ctrl Pts',(-0.61540809262174,5.43898477877421,39.771057115838));
#36437=CARTESIAN_POINT('Ctrl Pts',(-3.14260601079868,4.48166375413128,39.9100035011232));
#36438=CARTESIAN_POINT('Ctrl Pts',(-4.90378005293337,2.43191770762393,40.0489498864083));
#36439=CARTESIAN_POINT('Ctrl Pts',(-5.4696363904309,-0.210618851664463,
40.1878962716934));
#36440=CARTESIAN_POINT('Ctrl Pts',(-4.70224508124829,-2.80181615029938,
40.3268426569785));
#36441=CARTESIAN_POINT('Ctrl Pts',(-2.78866109284938,-4.71005858280236,
40.4657890422636));
#36442=CARTESIAN_POINT('Ctrl Pts',(-0.195328840757133,-5.47020376111992,
40.6047354275488));
#36443=CARTESIAN_POINT('Ctrl Pts',(2.44561566536424,-4.89696299368569,40.7436818128338));
#36444=CARTESIAN_POINT('Ctrl Pts',(4.49043072196045,-3.13006620943965,40.8826281981191));
#36445=CARTESIAN_POINT('Ctrl Pts',(5.4406837701739,-0.600202180243085,41.0215745834041));
#36446=CARTESIAN_POINT('Ctrl Pts',(5.06474649875199,2.07596373946694,41.1605209686893));
#36447=CARTESIAN_POINT('Ctrl Pts',(3.45425525180338,4.24610447346635,41.2994673539744));
#36448=CARTESIAN_POINT('Ctrl Pts',(1.00177427157815,5.38123878423976,41.4384137392595));
#36449=CARTESIAN_POINT('Ctrl Pts',(-1.69489354205759,5.20467274910667,41.5773601245447));
#36450=CARTESIAN_POINT('Ctrl Pts',(-3.97842368711355,3.75944510666346,41.7163065098298));
#36451=CARTESIAN_POINT('Ctrl Pts',(-5.2921957642256,1.39783637716104,41.8552528951149));
#36452=CARTESIAN_POINT('Ctrl Pts',(-5.31597211862969,-1.30450104566994,
41.9941992804001));
#36453=CARTESIAN_POINT('Ctrl Pts',(-4.04395716058395,-3.6888606679521,42.1331456656852));
#36454=CARTESIAN_POINT('Ctrl Pts',(-1.7862100655618,-5.17404446694148,42.2720920509703));
#36455=CARTESIAN_POINT('Ctrl Pts',(0.906933497597219,-5.39803243553966,
42.4110384362554));
#36456=CARTESIAN_POINT('Ctrl Pts',(3.37900807827648,-4.30622653272497,42.5499848215406));
#36457=CARTESIAN_POINT('Ctrl Pts',(5.02743475132581,-2.16475919338935,42.6889312068257));
#36458=CARTESIAN_POINT('Ctrl Pts',(5.45040234947773,0.504377609544291,42.8278775921108));
#36459=CARTESIAN_POINT('Ctrl Pts',(4.54481068204241,3.05057017762177,42.9668239773959));
#36460=CARTESIAN_POINT('Ctrl Pts',(2.53140165456461,4.8531730040737,43.105770362681));
#36461=CARTESIAN_POINT('Ctrl Pts',(-0.0990475302177512,5.47279381403684,
43.2447167479662));
#36462=CARTESIAN_POINT('Ctrl Pts',(-2.70535344894986,4.75839734159067,43.3836631332513));
#36463=CARTESIAN_POINT('Ctrl Pts',(-4.65221770432746,2.88412083237583,43.5226095185365));
#36464=CARTESIAN_POINT('Ctrl Pts',(-5.46508367108224,0.306827332994467,
43.6615559038215));
#36465=CARTESIAN_POINT('Ctrl Pts',(-4.94581173628886,-2.34525666258288,
43.8005022891067));
#36466=CARTESIAN_POINT('Ctrl Pts',(-3.2209766913287,-4.42567415182356,43.9394486743917));
#36467=CARTESIAN_POINT('Ctrl Pts',(-0.711014576269677,-5.42731432814925,
44.078395059677));
#36468=CARTESIAN_POINT('Ctrl Pts',(1.97226043253588,-5.10602304445011,44.217341444962));
#36469=CARTESIAN_POINT('Ctrl Pts',(4.17478838749362,-3.54011644778115,44.3562878302472));
#36470=CARTESIAN_POINT('Ctrl Pts',(5.35969352519225,-1.11129107807733,44.4952342155323));
#36471=CARTESIAN_POINT('Ctrl Pts',(5.2381500675345,1.58841632269079,44.6341806008175));
#36472=CARTESIAN_POINT('Ctrl Pts',(3.83978476067387,3.90094033995637,44.7731269861025));
#36473=CARTESIAN_POINT('Ctrl Pts',(1.50545522685244,5.26259319196769,44.9120733713877));
#36474=CARTESIAN_POINT('Ctrl Pts',(-1.19583556272895,5.34146607694132,45.0510197566728));
#36475=CARTESIAN_POINT('Ctrl Pts',(-3.60563623559729,4.11833338630442,45.189966141958));
#36476=CARTESIAN_POINT('Ctrl Pts',(-5.13654740233609,1.89133903035833,45.328912527243));
#36477=CARTESIAN_POINT('Ctrl Pts',(-5.41540281118094,-0.796677435889682,
45.4678589125282));
#36478=CARTESIAN_POINT('Ctrl Pts',(-4.37423024404137,-3.29050031398198,
45.6068052978133));
#36479=CARTESIAN_POINT('Ctrl Pts',(-2.26682004013511,-4.982249436735,45.7457516830984));
#36480=CARTESIAN_POINT('Ctrl Pts',(0.393137402421516,-5.45955360144152,
45.8846980683836));
#36481=CARTESIAN_POINT('Ctrl Pts',(2.95726589417037,-4.60606784311644,46.0236444536686));
#36482=CARTESIAN_POINT('Ctrl Pts',(4.80054796897683,-2.62983302544764,46.1625908389539));
#36483=CARTESIAN_POINT('Ctrl Pts',(5.47367560836416,-0.0125649759491998,
46.3015372242389));
#36484=CARTESIAN_POINT('Ctrl Pts',(4.81257102413439,2.60776584107418,46.4404836095241));
#36485=CARTESIAN_POINT('Ctrl Pts',(2.97838133253723,4.59244239834222,46.5794299948092));
#36486=CARTESIAN_POINT('Ctrl Pts',(0.418198244080788,5.45769115773086,46.7183763800943));
#36487=CARTESIAN_POINT('Ctrl Pts',(-2.24392248422375,4.99260397270669,46.8573227653795));
#36488=CARTESIAN_POINT('Ctrl Pts',(-4.35907735277298,3.31054786673546,46.9962691506646));
#36489=CARTESIAN_POINT('Ctrl Pts',(-5.41168816746401,0.82153132680118,47.1352155359497));
#36490=CARTESIAN_POINT('Ctrl Pts',(-5.14517646713044,-1.8677370442759,47.2741619212348));
#36491=CARTESIAN_POINT('Ctrl Pts',(-3.62450563605566,-4.10173639363517,
47.41310830652));
#36492=CARTESIAN_POINT('Ctrl Pts',(-1.22034580201261,-5.3359196631282,47.5520546918051));
#36493=CARTESIAN_POINT('Ctrl Pts',(1.48127862913772,-5.26944932664737,47.6910010770902));
#36494=CARTESIAN_POINT('Ctrl Pts',(3.82183494941533,-3.91852779651975,47.8299474623754));
#36495=CARTESIAN_POINT('Ctrl Pts',(5.23080239877533,-1.61244810943541,47.9688938476604));
#36496=CARTESIAN_POINT('Ctrl Pts',(5.36473900264045,1.08667286690954,48.1078402329456));
#36497=CARTESIAN_POINT('Ctrl Pts',(4.190997198,3.52091250417398,48.2467866182307));
#36498=CARTESIAN_POINT('Ctrl Pts',(1.99568152235226,5.09691461618197,48.3857330035158));
#36499=CARTESIAN_POINT('Ctrl Pts',(-0.686090032233244,5.43052123780479,
48.5246793888009));
#36500=CARTESIAN_POINT('Ctrl Pts',(-3.20062448577036,4.44041547511814,48.6636257740861));
#36501=CARTESIAN_POINT('Ctrl Pts',(-4.9349921698918,2.36793762704299,48.8025721593712));
#36502=CARTESIAN_POINT('Ctrl Pts',(-5.46643530553421,-0.281732361465787,
48.9415185446563));
#36503=CARTESIAN_POINT('Ctrl Pts',(-4.66540864158968,-2.86273462059622,
49.0804649299415));
#36504=CARTESIAN_POINT('Ctrl Pts',(-2.72717308724132,-4.7459216295728,49.2194113152266));
#36505=CARTESIAN_POINT('Ctrl Pts',(-0.124167971278091,-5.47229155872411,
49.3583577005117));
#36506=CARTESIAN_POINT('Ctrl Pts',(2.50908553605409,-4.86472378159826,49.4973040857969));
#36507=CARTESIAN_POINT('Ctrl Pts',(4.53077386094875,-3.07144211682079,49.6362504710819));
#36508=CARTESIAN_POINT('Ctrl Pts',(5.44799735213535,-0.529319458871882,
49.7751968563671));
#36509=CARTESIAN_POINT('Ctrl Pts',(5.03738303470027,2.14150496336914,49.9141432416522));
#36510=CARTESIAN_POINT('Ctrl Pts',(3.39855008175896,4.29107147899482,50.0530951649014));
#36511=CARTESIAN_POINT('Ctrl Pts',(1.75400942686783,5.02570043128944,50.145731626389));
#36512=CARTESIAN_POINT('Ctrl Pts',(0.893469766832245,5.17429288788272,50.1920526261149));
#36513=CARTESIAN_POINT('Ctrl Pts',(-2.43860316501687,5.02337115222,-0.192113967442929));
#36514=CARTESIAN_POINT('Ctrl Pts',(-3.27394279424196,4.61785425888989,-0.14579850568122));
#36515=CARTESIAN_POINT('Ctrl Pts',(-4.73757427995125,3.38246449519804,-0.0531675821578035));
#36516=CARTESIAN_POINT('Ctrl Pts',(-5.77834074348035,0.703089257730629,
0.0857788031273231));
#36517=CARTESIAN_POINT('Ctrl Pts',(-5.41053021473772,-2.14691577271492,
0.224725188412448));
#36518=CARTESIAN_POINT('Ctrl Pts',(-3.72392262668397,-4.47396978292609,
0.363671573697576));
#36519=CARTESIAN_POINT('Ctrl Pts',(-1.1295704356595,-5.71028667904572,0.5026179589827));
#36520=CARTESIAN_POINT('Ctrl Pts',(1.74010803576541,-5.55479229048019,0.641564344267827));
#36521=CARTESIAN_POINT('Ctrl Pts',(4.18563346191538,-4.04524401762382,0.780510729552951));
#36522=CARTESIAN_POINT('Ctrl Pts',(5.61088953877353,-1.54967508819847,0.919457114838079));
#36523=CARTESIAN_POINT('Ctrl Pts',(5.66846843566637,1.3236467664529,1.05840350012321));
#36524=CARTESIAN_POINT('Ctrl Pts',(4.34433272393584,3.87431736739548,1.19734988540833));
#36525=CARTESIAN_POINT('Ctrl Pts',(1.96124742883955,5.48060964928763,1.33629627069346));
#36526=CARTESIAN_POINT('Ctrl Pts',(-0.899900658959379,5.75097777317752,
1.47524265597859));
#36527=CARTESIAN_POINT('Ctrl Pts',(-3.5416939435564,4.61952095240389,1.61418904126371));
#36528=CARTESIAN_POINT('Ctrl Pts',(-5.32018398781385,2.36203536405459,1.75313542654884));
#36529=CARTESIAN_POINT('Ctrl Pts',(-5.80185603046317,-0.471206379315615,
1.89208181183396));
#36530=CARTESIAN_POINT('Ctrl Pts',(-4.86930045922241,-3.18958963860582,
2.03102819711909));
#36531=CARTESIAN_POINT('Ctrl Pts',(-2.74983172691733,-5.13049649727467,
2.16997458240422));
#36532=CARTESIAN_POINT('Ctrl Pts',(0.0399204386165095,-5.8208225637395,
2.30892096768934));
#36533=CARTESIAN_POINT('Ctrl Pts',(2.81994182561266,-5.09229781115264,2.44786735297447));
#36534=CARTESIAN_POINT('Ctrl Pts',(4.91259013334905,-3.12250333908225,2.58681373825959));
#36535=CARTESIAN_POINT('Ctrl Pts',(5.80777324155042,-0.391585100383275,
2.72576012354472));
#36536=CARTESIAN_POINT('Ctrl Pts',(5.28728637547375,2.43478370660165,2.86470650882985));
#36537=CARTESIAN_POINT('Ctrl Pts',(3.47800047166986,4.66766340219916,3.00365289411497));
#36538=CARTESIAN_POINT('Ctrl Pts',(0.820936833959134,5.76277985261022,3.1425992794001));
#36539=CARTESIAN_POINT('Ctrl Pts',(-2.03623372560755,5.45319366342964,3.28154566468522));
#36540=CARTESIAN_POINT('Ctrl Pts',(-4.39706346306589,3.81436781360389,3.42049204997035));
#36541=CARTESIAN_POINT('Ctrl Pts',(-5.68608986735551,1.24577322822909,3.55943843525547));
#36542=CARTESIAN_POINT('Ctrl Pts',(-5.58910714904596,-1.62648399694239,
3.6983848205406));
#36543=CARTESIAN_POINT('Ctrl Pts',(-4.12975526730215,-4.10227867751238,
3.83733120582573));
#36544=CARTESIAN_POINT('Ctrl Pts',(-1.66375758710614,-5.57812509784119,
3.97627759111085));
#36545=CARTESIAN_POINT('Ctrl Pts',(1.20778823730278,-5.69427927745301,4.11522397639598));
#36546=CARTESIAN_POINT('Ctrl Pts',(3.78493042861267,-4.42242813015308,4.2541703616811));
#36547=CARTESIAN_POINT('Ctrl Pts',(5.43947937485367,-2.07259090182936,4.39311674696624));
#36548=CARTESIAN_POINT('Ctrl Pts',(5.76813157805406,0.782449368368389,4.53206313225135));
#36549=CARTESIAN_POINT('Ctrl Pts',(4.69077663503258,3.44676420371884,4.67100951753648));
#36550=CARTESIAN_POINT('Ctrl Pts',(2.47002449641317,5.2709152813267,4.80995590282161));
#36551=CARTESIAN_POINT('Ctrl Pts',(-0.35280685040481,5.81025784643955,4.94890228810673));
#36552=CARTESIAN_POINT('Ctrl Pts',(-3.08963999378505,4.93332480428855,5.08784867339187));
#36553=CARTESIAN_POINT('Ctrl Pts',(-5.07335995801337,2.85387239592652,5.22679505867698));
#36554=CARTESIAN_POINT('Ctrl Pts',(-5.82042637857731,0.0787761852724543,
5.36574144396212));
#36555=CARTESIAN_POINT('Ctrl Pts',(-5.14873856796628,-2.71552206298188,
5.50468782924723));
#36556=CARTESIAN_POINT('Ctrl Pts',(-3.22202334984397,-4.84790000400844,
5.64363421453237));
#36557=CARTESIAN_POINT('Ctrl Pts',(-0.509925934059868,-5.79858124523387,
5.78258059981748));
#36558=CARTESIAN_POINT('Ctrl Pts',(2.32646814479965,-5.33583310149757,5.92152698510262));
#36559=CARTESIAN_POINT('Ctrl Pts',(4.59577550020591,-3.57245244440173,6.06047337038773));
#36560=CARTESIAN_POINT('Ctrl Pts',(5.74484259959826,-0.938270974530154,
6.19941975567287));
#36561=CARTESIAN_POINT('Ctrl Pts',(5.49357934250451,1.9246181240476,6.33836614095799));
#36562=CARTESIAN_POINT('Ctrl Pts',(3.90323224008275,4.31837318857267,6.47731252624312));
#36563=CARTESIAN_POINT('Ctrl Pts',(1.36145531178806,5.65950601641247,6.61625891152824));
#36564=CARTESIAN_POINT('Ctrl Pts',(-1.51218226700198,5.62110965087584,6.75520529681338));
#36565=CARTESIAN_POINT('Ctrl Pts',(-4.01721884475313,4.21254337297139,6.89415168209848));
#36566=CARTESIAN_POINT('Ctrl Pts',(-5.5430408662431,1.7771513359767,7.03309806738364));
#36567=CARTESIAN_POINT('Ctrl Pts',(-5.71772258098449,-1.09142906444016,
7.17204445266874));
#36568=CARTESIAN_POINT('Ctrl Pts',(-4.49868456166763,-3.69396888595697,
7.31099083795388));
#36569=CARTESIAN_POINT('Ctrl Pts',(-2.18307262465992,-5.39608773383692,
7.449937223239));
#36570=CARTESIAN_POINT('Ctrl Pts',(0.664672754426577,-5.78288673979767,
7.58888360852413));
#36571=CARTESIAN_POINT('Ctrl Pts',(3.35040126028876,-4.7600819647208,7.72782999380925));
#36572=CARTESIAN_POINT('Ctrl Pts',(5.21945489475937,-2.57698651866424,7.86677637909439));
#36573=CARTESIAN_POINT('Ctrl Pts',(5.816243709659,0.234260593478593,8.0057227643795));
#36574=CARTESIAN_POINT('Ctrl Pts',(4.99529783711454,2.98840566763009,8.14466914966463));
#36575=CARTESIAN_POINT('Ctrl Pts',(2.95672640221087,5.01411386969561,8.28361553494976));
#36576=CARTESIAN_POINT('Ctrl Pts',(0.197440053876959,5.817610019667,8.42256192023489));
#36577=CARTESIAN_POINT('Ctrl Pts',(-2.60997316586149,5.20303843819049,8.56150830552));
#36578=CARTESIAN_POINT('Ctrl Pts',(-4.78119408086637,3.320203619794,8.70045469080513));
#36579=CARTESIAN_POINT('Ctrl Pts',(-5.78697815480668,0.628054736145685,
8.83940107609027));
#36580=CARTESIAN_POINT('Ctrl Pts',(-5.38216114751552,-2.21718521959242,
8.97834746137538));
#36581=CARTESIAN_POINT('Ctrl Pts',(-3.6654189642599,-4.52197663994948,9.11729384666053));
#36582=CARTESIAN_POINT('Ctrl Pts',(-1.05521497488759,-5.7245165972838,9.25624023194561));
#36583=CARTESIAN_POINT('Ctrl Pts',(1.81220225163365,-5.53168074955333,9.39518661723079));
#36584=CARTESIAN_POINT('Ctrl Pts',(4.23788730167498,-3.99047367289983,9.53413300251587));
#36585=CARTESIAN_POINT('Ctrl Pts',(5.63056889983452,-1.47657129188572,9.67307938780103));
#36586=CARTESIAN_POINT('Ctrl Pts',(5.65077485257319,1.3972517601818,9.81202577308613));
#36587=CARTESIAN_POINT('Ctrl Pts',(4.29357987107567,3.93048862185081,9.95097215837128));
#36588=CARTESIAN_POINT('Ctrl Pts',(1.8898061318093,5.5056517961074,10.0899185436564));
#36589=CARTESIAN_POINT('Ctrl Pts',(-0.974616067073906,5.73878841199136,
10.2288649289416));
#36590=CARTESIAN_POINT('Ctrl Pts',(-3.60147136295125,4.5730704059359,10.3678113142267));
#36591=CARTESIAN_POINT('Ctrl Pts',(-5.35045235851118,2.29264660929394,10.5067576995118));
#36592=CARTESIAN_POINT('Ctrl Pts',(-5.79523733326456,-0.546619764499533,
10.6457040847969));
#36593=CARTESIAN_POINT('Ctrl Pts',(-4.82740801613472,-3.25264519453983,
10.7846504700821));
#36594=CARTESIAN_POINT('Ctrl Pts',(-2.68287701032666,-5.16582421916052,
10.9235968553672));
#36595=CARTESIAN_POINT('Ctrl Pts',(0.115616929216404,-5.81981113452004,
11.0625432406523));
#36596=CARTESIAN_POINT('Ctrl Pts',(2.88592873967612,-5.05519378711798,11.2014896259374));
#36597=CARTESIAN_POINT('Ctrl Pts',(4.95278287470592,-3.05835097917565,11.3404360112226));
#36598=CARTESIAN_POINT('Ctrl Pts',(5.81237465427617,-0.316021825405791,
11.4793823965077));
#36599=CARTESIAN_POINT('Ctrl Pts',(5.25517484547065,2.50333902205377,11.6183287817928));
#36600=CARTESIAN_POINT('Ctrl Pts',(3.41700332383366,4.71250010087157,11.757275167078));
#36601=CARTESIAN_POINT('Ctrl Pts',(0.745922388296798,5.77296879486129,11.8962215523631));
#36602=CARTESIAN_POINT('Ctrl Pts',(-2.10698037191245,5.42625125000498,12.0351679376482));
#36603=CARTESIAN_POINT('Ctrl Pts',(-4.44629750742316,3.75686137504265,12.1741143229333));
#36604=CARTESIAN_POINT('Ctrl Pts',(-5.70181029744169,1.17172020883517,12.3130607082185));
#36605=CARTESIAN_POINT('Ctrl Pts',(-5.56748204168621,-1.69903285174431,
12.4520070935035));
#36606=CARTESIAN_POINT('Ctrl Pts',(-4.07605583642212,-4.15563926901433,
12.5909534787887));
#36607=CARTESIAN_POINT('Ctrl Pts',(-1.5910733024131,-5.59929054989586,12.7298998640738));
#36608=CARTESIAN_POINT('Ctrl Pts',(1.28174026545566,-5.67809041912107,12.868846249359));
#36609=CARTESIAN_POINT('Ctrl Pts',(3.84212407189394,-4.37283106602324,13.0077926346441));
#36610=CARTESIAN_POINT('Ctrl Pts',(5.46597343409255,-2.00167513188312,13.1467390199292));
#36611=CARTESIAN_POINT('Ctrl Pts',(5.75746801114147,0.857397816936438,13.2856854052143));
#36612=CARTESIAN_POINT('Ctrl Pts',(4.64555473275797,3.50747632076895,13.4246317904995));
#36613=CARTESIAN_POINT('Ctrl Pts',(2.40126729403563,5.30259222441247,13.5635781757846));
#36614=CARTESIAN_POINT('Ctrl Pts',(-0.428339485918187,5.80517822298404,
13.7025245610697));
#36615=CARTESIAN_POINT('Ctrl Pts',(-3.15353665418747,4.89272679459021,13.8414709463548));
#36616=CARTESIAN_POINT('Ctrl Pts',(-5.1100455545729,2.78765194132884,13.98041733164));
#36617=CARTESIAN_POINT('Ctrl Pts',(-5.82095863766027,0.00307480944400744,
14.1193637169251));
#36618=CARTESIAN_POINT('Ctrl Pts',(-5.11298774910743,-2.78225182060899,
14.2583101022102));
#36619=CARTESIAN_POINT('Ctrl Pts',(-3.15870387054901,-4.88939247493832,
14.3972564874954));
#36620=CARTESIAN_POINT('Ctrl Pts',(-0.434472192656758,-5.80472245930956,
14.5362028727805));
#36621=CARTESIAN_POINT('Ctrl Pts',(2.39566397084646,-5.30512611109228,14.6751492580656));
#36622=CARTESIAN_POINT('Ctrl Pts',(4.6418466275032,-3.51238221191002,14.8140956433507));
#36623=CARTESIAN_POINT('Ctrl Pts',(5.75655899059612,-0.863479880247238,
14.9530420286359));
#36624=CARTESIAN_POINT('Ctrl Pts',(5.46808507596602,1.99589942577334,15.091988413921));
#36625=CARTESIAN_POINT('Ctrl Pts',(3.8467416543003,4.36876957058571,15.2309347992061));
#36626=CARTESIAN_POINT('Ctrl Pts',(1.28773823261074,5.67673314152403,15.3698811844912));
#36627=CARTESIAN_POINT('Ctrl Pts',(-1.58515698107652,5.60096833245369,15.5088275697763));
#36628=CARTESIAN_POINT('Ctrl Pts',(-4.07166328994811,4.15994314493526,15.6477739550615));
#36629=CARTESIAN_POINT('Ctrl Pts',(-5.5656839723722,1.7049137325636,15.7867203403466));
#36630=CARTESIAN_POINT('Ctrl Pts',(-5.70304499249917,-1.16569581338135,
15.9256667256317));
#36631=CARTESIAN_POINT('Ctrl Pts',(-4.45026400456468,-3.75216193753426,
16.0646131109168));
#36632=CARTESIAN_POINT('Ctrl Pts',(-2.11271182021736,-5.42402227876312,
16.203559496202));
#36633=CARTESIAN_POINT('Ctrl Pts',(0.739823054267452,-5.77375361131554,
16.3425058814871));
#36634=CARTESIAN_POINT('Ctrl Pts',(3.41202284326333,-4.71610740259953,16.4814522667722));
#36635=CARTESIAN_POINT('Ctrl Pts',(5.2525272321485,-2.50888951357832,16.6203986520574));
#36636=CARTESIAN_POINT('Ctrl Pts',(5.81270527545858,0.309881100521729,16.7593450373425));
#36637=CARTESIAN_POINT('Ctrl Pts',(4.95601114004255,3.05311684931627,16.8982914226276));
#36638=CARTESIAN_POINT('Ctrl Pts',(2.89126774545787,5.05214209418933,17.0372378079127));
#36639=CARTESIAN_POINT('Ctrl Pts',(0.121765269575306,5.81968574193917,17.1761841931979));
#36640=CARTESIAN_POINT('Ctrl Pts',(-2.67741802007991,5.1686556919141,17.315130578483));
#36641=CARTESIAN_POINT('Ctrl Pts',(-4.82396902860301,3.25774334883577,17.4540769637681));
#36642=CARTESIAN_POINT('Ctrl Pts',(-5.79465661660804,0.552741903066509,
17.5930233490532));
#36643=CARTESIAN_POINT('Ctrl Pts',(-5.35287146493922,-2.28699278434459,
17.7319697343384));
#36644=CARTESIAN_POINT('Ctrl Pts',(-3.60630062475619,-4.56926303901273,
17.8709161196235));
#36645=CARTESIAN_POINT('Ctrl Pts',(-0.980678330697991,-5.73775556533251,
18.0098625049086));
#36646=CARTESIAN_POINT('Ctrl Pts',(1.88398856947714,-5.5076452305758,18.1488088901936));
#36647=CARTESIAN_POINT('Ctrl Pts',(4.28942506614282,-3.93502242912927,18.2877552754789));
#36648=CARTESIAN_POINT('Ctrl Pts',(5.64929555680298,-1.40322080503777,18.426701660764));
#36649=CARTESIAN_POINT('Ctrl Pts',(5.63212569800144,1.47062199008331,18.5656480460491));
#36650=CARTESIAN_POINT('Ctrl Pts',(4.24210071745844,3.985994282327,18.7045944313342));
#36651=CARTESIAN_POINT('Ctrl Pts',(1.81804524662069,5.52976314113405,18.8435408166194));
#36652=CARTESIAN_POINT('Ctrl Pts',(-1.04916665612453,5.72562819640615,18.9824872019045));
#36653=CARTESIAN_POINT('Ctrl Pts',(-3.66063962571136,4.52584648949526,19.1214335871896));
#36654=CARTESIAN_POINT('Ctrl Pts',(-5.37981577372854,2.22287002691262,19.2603799724748));
#36655=CARTESIAN_POINT('Ctrl Pts',(-5.78763844083714,-0.621940667547248,
19.3993263577599));
#36656=CARTESIAN_POINT('Ctrl Pts',(-4.78469907912408,-3.31515062071602,
19.538272743045));
#36657=CARTESIAN_POINT('Ctrl Pts',(-2.61546851778496,-5.20027819912362,
19.6772191283301));
#36658=CARTESIAN_POINT('Ctrl Pts',(0.191293864207407,-5.8178153608826,19.8161655136153));
#36659=CARTESIAN_POINT('Ctrl Pts',(2.9514275352447,-5.01723473837972,19.9551118989004));
#36660=CARTESIAN_POINT('Ctrl Pts',(4.99213791470887,-2.99368133847456,20.0940582841855));
#36661=CARTESIAN_POINT('Ctrl Pts',(5.81599297663645,-0.24040509878175,20.2330046694706));
#36662=CARTESIAN_POINT('Ctrl Pts',(5.22217446838412,2.57147092878024,20.3719510547558));
#36663=CARTESIAN_POINT('Ctrl Pts',(3.35542823266775,4.75653973926645,20.5108974400409));
#36664=CARTESIAN_POINT('Ctrl Pts',(0.670781779190222,5.78218131162548,20.649843825326));
#36665=CARTESIAN_POINT('Ctrl Pts',(-2.1773706488537,5.3983910541304,20.7887902106111));
#36666=CARTESIAN_POINT('Ctrl Pts',(-4.49477951620812,3.69871951038204,20.9277365958963));
#36667=CARTESIAN_POINT('Ctrl Pts',(-5.71656633767768,1.09746900764223,21.0666829811814));
#36668=CARTESIAN_POINT('Ctrl Pts',(-5.54491526442117,-1.77129433640875,
21.2056293664665));
#36669=CARTESIAN_POINT('Ctrl Pts',(-4.02166699171225,-4.20829698614261,
21.3445757517516));
#36670=CARTESIAN_POINT('Ctrl Pts',(-1.51811990758472,-5.61950895203485,
21.4835221370368));
#36671=CARTESIAN_POINT('Ctrl Pts',(1.35547550328467,-5.66094118285996,21.6224685223219));
#36672=CARTESIAN_POINT('Ctrl Pts',(3.89866786797563,-4.32249439224843,21.761414907607));
#36673=CARTESIAN_POINT('Ctrl Pts',(5.49154299233608,-1.93042080364079,21.9003612928921));
#36674=CARTESIAN_POINT('Ctrl Pts',(5.74583064057415,0.932201247394659,22.0393076781773));
#36675=CARTESIAN_POINT('Ctrl Pts',(4.59954709304317,3.56759519209829,22.1782540634624));
#36676=CARTESIAN_POINT('Ctrl Pts',(2.33210394734911,5.33337230038963,22.3172004487475));
#36677=CARTESIAN_POINT('Ctrl Pts',(-0.503799673168457,5.79911672628859,
22.4561468340326));
#36678=CARTESIAN_POINT('Ctrl Pts',(-3.21689993333379,4.85130124139101,22.5950932193178));
#36679=CARTESIAN_POINT('Ctrl Pts',(-5.14586685088318,2.72095999029507,22.7340396046029));
#36680=CARTESIAN_POINT('Ctrl Pts',(-5.82050635444362,-0.0726270864499248,
22.872985989888));
#36681=CARTESIAN_POINT('Ctrl Pts',(-5.07637213236399,-2.84851099516275,
23.0119323751731));
#36682=CARTESIAN_POINT('Ctrl Pts',(-3.0948501360281,-4.9300579663257,23.1508787604583));
#36683=CARTESIAN_POINT('Ctrl Pts',(-0.358944965720083,-5.80988187723202,
23.2898251457433));
#36684=CARTESIAN_POINT('Ctrl Pts',(2.46445460031621,-5.2735218250032,23.4287715310286));
#36685=CARTESIAN_POINT('Ctrl Pts',(4.68713264453987,-3.45171790392748,23.5677179163136));
#36686=CARTESIAN_POINT('Ctrl Pts',(5.76730173168865,-0.788542739149756,
23.7066643015988));
#36687=CARTESIAN_POINT('Ctrl Pts',(5.44166595127444,2.06684314609144,23.8456106868839));
#36688=CARTESIAN_POINT('Ctrl Pts',(3.7896004403121,4.41842702990455,23.984557072169));
#36689=CARTESIAN_POINT('Ctrl Pts',(1.21380334862841,5.69300011827361,24.1235034574541));
#36690=CARTESIAN_POINT('Ctrl Pts',(-1.65786358568728,5.5798796803387,24.2624498427393));
#36691=CARTESIAN_POINT('Ctrl Pts',(-4.12541906425775,4.10663931458115,24.4013962280244));
#36692=CARTESIAN_POINT('Ctrl Pts',(-5.58738571271641,1.63238776433096,24.5403426133096));
#36693=CARTESIAN_POINT('Ctrl Pts',(-5.68740280533154,-1.23976539946543,
24.6792889985946));
#36694=CARTESIAN_POINT('Ctrl Pts',(-4.40109074100391,-3.80972035788119,
24.8182353838798));
#36695=CARTESIAN_POINT('Ctrl Pts',(-2.04199367701263,-5.45103941820688,
24.9571817691649));
#36696=CARTESIAN_POINT('Ctrl Pts',(0.814848222298178,-5.76364392467321,
25.0961281544501));
#36697=CARTESIAN_POINT('Ctrl Pts',(3.47306732527811,-4.671335169937,25.2350745397351));
#36698=CARTESIAN_POINT('Ctrl Pts',(5.28471117029584,-2.44036816123203,25.3740209250203));
#36699=CARTESIAN_POINT('Ctrl Pts',(5.80818369491154,0.385449195055016,25.5129673103054));
#36700=CARTESIAN_POINT('Ctrl Pts',(4.91588619571472,3.11731163449957,25.6519136955906));
#36701=CARTESIAN_POINT('Ctrl Pts',(2.82532006695232,5.08931581207938,25.7908600808756));
#36702=CARTESIAN_POINT('Ctrl Pts',(0.0460698902024037,5.82077713720612,
25.9298064661608));
#36703=CARTESIAN_POINT('Ctrl Pts',(-2.7444100225502,5.13339873221737,26.0687528514459));
#36704=CARTESIAN_POINT('Ctrl Pts',(-4.86592806235428,3.19473207136341,26.2076992367311));
#36705=CARTESIAN_POINT('Ctrl Pts',(-5.80135498476745,0.477335580612477,
26.3466456220161));
#36706=CARTESIAN_POINT('Ctrl Pts',(-5.32267641115013,-2.35641353289075,
26.4855920073013));
#36707=CARTESIAN_POINT('Ctrl Pts',(-3.54657232463761,-4.6157766044209,26.6245383925864));
#36708=CARTESIAN_POINT('Ctrl Pts',(-0.905975817042736,-5.75002406383996,
26.7634847778716));
#36709=CARTESIAN_POINT('Ctrl Pts',(1.95545623423369,-5.48267816234013,26.9024311631566));
#36710=CARTESIAN_POINT('Ctrl Pts',(4.34023732804627,-3.87890562556482,27.0413775484418));
#36711=CARTESIAN_POINT('Ctrl Pts',(5.66706670613347,-1.32963298095314,27.1803239337269));
#36712=CARTESIAN_POINT('Ctrl Pts',(5.61252393985844,1.5437434826812,27.3192703190121));
#36713=CARTESIAN_POINT('Ctrl Pts',(4.18990406559815,4.04082576175822,27.4582167042971));
#36714=CARTESIAN_POINT('Ctrl Pts',(1.74597686183295,5.55293919593477,27.5971630895823));
#36715=CARTESIAN_POINT('Ctrl Pts',(-1.12353979176645,5.7114995624724,27.7361094748674));
#36716=CARTESIAN_POINT('Ctrl Pts',(-3.71918873709466,4.47785708276549,27.8750558601526));
#36717=CARTESIAN_POINT('Ctrl Pts',(-5.40826926044047,2.15271747388722,28.0140022454376));
#36718=CARTESIAN_POINT('Ctrl Pts',(-5.7790606418044,-0.697156377115153,
28.1529486307229));
#36719=CARTESIAN_POINT('Ctrl Pts',(-4.74118087014855,-3.37709533065652,
28.2918950160079));
#36720=CARTESIAN_POINT('Ctrl Pts',(-2.5476176514781,-5.23385261711504,28.4308414012931));
#36721=CARTESIAN_POINT('Ctrl Pts',(0.266938444235501,-5.81483557659147,
28.5697877865781));
#36722=CARTESIAN_POINT('Ctrl Pts',(3.01642713378518,-4.97842708718019,28.7087341718633));
#36723=CARTESIAN_POINT('Ctrl Pts',(5.03064859706422,-2.92850535404333,28.8476805571484));
#36724=CARTESIAN_POINT('Ctrl Pts',(5.81862759657655,-0.16474771064401,28.9866269424335));
#36725=CARTESIAN_POINT('Ctrl Pts',(5.1882908258459,2.63916790338318,29.1255733277187));
#36726=CARTESIAN_POINT('Ctrl Pts',(3.29328561281214,4.79977486849638,29.2645197130038));
#36727=CARTESIAN_POINT('Ctrl Pts',(0.595527715740968,5.79041584478949,29.4034660982889));
#36728=CARTESIAN_POINT('Ctrl Pts',(-2.24739265080135,5.36961778797418,29.542412483574));
#36729=CARTESIAN_POINT('Ctrl Pts',(-4.54250128929371,3.63995205360863,29.6813588688592));
#36730=CARTESIAN_POINT('Ctrl Pts',(-5.73035549226509,1.0230321833023,29.8203052541443));
#36731=CARTESIAN_POINT('Ctrl Pts',(-5.52141063413822,-1.84325622880545,
29.9592516394294));
#36732=CARTESIAN_POINT('Ctrl Pts',(-3.96659793236503,-4.26024292250597,
30.0981980247146));
#36733=CARTESIAN_POINT('Ctrl Pts',(-1.44490974177441,-5.63877688456727,
30.2371444099997));
#36734=CARTESIAN_POINT('Ctrl Pts',(1.42898147939723,-5.64283446924899,30.3760907952848));
#36735=CARTESIAN_POINT('Ctrl Pts',(3.95455225318248,-4.27142662264661,30.5150371805699));
#36736=CARTESIAN_POINT('Ctrl Pts',(5.51618372481357,-1.85883996888017,30.6539835658551));
#36737=CARTESIAN_POINT('Ctrl Pts',(5.73322143466762,1.00684700767919,30.7929299511402));
#36738=CARTESIAN_POINT('Ctrl Pts',(4.55276149750459,3.62711064935227,30.9318763364253));
#36739=CARTESIAN_POINT('Ctrl Pts',(2.26254615446798,5.36325030319366,31.0708227217104));
#36740=CARTESIAN_POINT('Ctrl Pts',(-0.579174649009589,5.79207438157948,
31.2097691069956));
#36741=CARTESIAN_POINT('Ctrl Pts',(-3.27971911411854,4.8090551513047,31.3487154922807));
#36742=CARTESIAN_POINT('Ctrl Pts',(-5.18081778822028,2.6538078229339,31.4876618775658));
#36743=CARTESIAN_POINT('Ctrl Pts',(-5.81906960542543,-0.148316698381154,
31.626608262851));
#36744=CARTESIAN_POINT('Ctrl Pts',(-5.03889791080926,-2.91428837973299,
31.7655546481361));
#36745=CARTESIAN_POINT('Ctrl Pts',(-3.03047294634127,-4.9698896001117,31.9045010334212));
#36746=CARTESIAN_POINT('Ctrl Pts',(-0.283357027734952,-5.81405862635028,
32.0434474187063));
#36747=CARTESIAN_POINT('Ctrl Pts',(2.53282839813492,-5.2410255886998,32.1823938039914));
#36748=CARTESIAN_POINT('Ctrl Pts',(4.7316258917529,-3.39046978106256,32.3213401892766));
#36749=CARTESIAN_POINT('Ctrl Pts',(5.77706900587568,-0.713472225917252,
32.4602865745617));
#36750=CARTESIAN_POINT('Ctrl Pts',(5.41432643689403,2.13743728575958,32.5992329598468));
#36751=CARTESIAN_POINT('Ctrl Pts',(3.73181826283932,4.46733716759143,32.7381793451319));
#36752=CARTESIAN_POINT('Ctrl Pts',(1.13966316500139,5.70830419530563,32.8771257304171));
#36753=CARTESIAN_POINT('Ctrl Pts',(-1.73028978342203,5.55784726141247,33.0160721157022));
#36754=CARTESIAN_POINT('Ctrl Pts',(-4.17847707556568,4.05264089758481,33.1550185009873));
#36755=CARTESIAN_POINT('Ctrl Pts',(-5.60814241669793,1.55958569813855,33.2939648862725));
#36756=CARTESIAN_POINT('Ctrl Pts',(-5.67079866516178,-1.31362529474889,
33.4329112715576));
#36757=CARTESIAN_POINT('Ctrl Pts',(-4.35117308802745,-3.86663441171134,
33.5718576568427));
#36758=CARTESIAN_POINT('Ctrl Pts',(-1.97093015613459,-5.47713458255719,
33.7108040421278));
#36759=CARTESIAN_POINT('Ctrl Pts',(0.889735568950635,-5.75255938979764,
33.8497504274129));
#36760=CARTESIAN_POINT('Ctrl Pts',(3.53352438142312,-4.62577283939593,33.9886968126981));
#36761=CARTESIAN_POINT('Ctrl Pts',(5.31600126569122,-2.37143405115432,34.1276431979832));
#36762=CARTESIAN_POINT('Ctrl Pts',(5.80267973278655,0.460952095681341,34.2665895832684));
#36763=CARTESIAN_POINT('Ctrl Pts',(4.87492979076306,3.18097916543565,34.4055359685534));
#36764=CARTESIAN_POINT('Ctrl Pts',(2.75889452091848,5.12562873589677,34.5444823538386));
#36765=CARTESIAN_POINT('Ctrl Pts',(-0.0296332813159625,5.82088402087201,
34.6834287391237));
#36766=CARTESIAN_POINT('Ctrl Pts',(-2.81093784241375,5.0972735223736,34.8223751244088));
#36767=CARTESIAN_POINT('Ctrl Pts',(-4.90706408527485,3.13118044494573,34.961321509694));
#36768=CARTESIAN_POINT('Ctrl Pts',(-5.80707212633982,0.401848522819139,
35.1002678949791));
#36769=CARTESIAN_POINT('Ctrl Pts',(-5.29158109326361,-2.42543572358036,
35.2392142802642));
#36770=CARTESIAN_POINT('Ctrl Pts',(-3.48624416619839,-4.66150946898669,
35.3781606655493));
#36771=CARTESIAN_POINT('Ctrl Pts',(-0.831120068916907,-5.76132001774319,
35.5171070508345));
#36772=CARTESIAN_POINT('Ctrl Pts',(2.02659315804246,-5.45678376771338,35.6560534361196));
#36773=CARTESIAN_POINT('Ctrl Pts',(4.39031549312739,-3.8221327536613,35.7949998214048));
#36774=CARTESIAN_POINT('Ctrl Pts',(5.68387934205856,-1.255820266091,35.9339462066898));
#36775=CARTESIAN_POINT('Ctrl Pts',(5.59197289353619,1.61660387039037,36.072892591975));
#36776=CARTESIAN_POINT('Ctrl Pts',(4.13699874390506,4.09497378608617,36.2118389772602));
#36777=CARTESIAN_POINT('Ctrl Pts',(1.67361316691114,5.57517604057006,36.3507853625452));
#36778=CARTESIAN_POINT('Ctrl Pts',(-1.19772289471474,5.69640489987157,36.4897317478304));
#36779=CARTESIAN_POINT('Ctrl Pts',(-3.77710879425175,4.42911030255408,36.6286781331154));
#36780=CARTESIAN_POINT('Ctrl Pts',(-5.43580800609587,2.08220081564407,36.7676245184007));
#36781=CARTESIAN_POINT('Ctrl Pts',(-5.76950538699365,-0.772254171407353,
36.9065709036857));
#36782=CARTESIAN_POINT('Ctrl Pts',(-4.69686074976853,-3.43846884718893,
37.0455172889708));
#36783=CARTESIAN_POINT('Ctrl Pts',(-2.47933588753095,-5.26654179444213,
37.184463674256));
#36784=CARTESIAN_POINT('Ctrl Pts',(0.342537874966791,-5.81087228563992,
37.3234100595411));
#36785=CARTESIAN_POINT('Ctrl Pts',(3.08091654142906,-4.93877739734782,37.4623564448262));
#36786=CARTESIAN_POINT('Ctrl Pts',(5.06830840817201,-2.86283404958403,37.6013028301114));
#36787=CARTESIAN_POINT('Ctrl Pts',(5.8202780684835,-0.0890624574929409,
37.7402492153965));
#36788=CARTESIAN_POINT('Ctrl Pts',(5.1535296488501,2.7064184957666,37.8791956006816));
#36789=CARTESIAN_POINT('Ctrl Pts',(3.2305859749132,4.84219817588035,38.0181419859667));
#36790=CARTESIAN_POINT('Ctrl Pts',(0.520172926232102,5.79767100158503,38.1570883712518));
#36791=CARTESIAN_POINT('Ctrl Pts',(-2.31703453441006,5.3399363181742,38.296034756537));
#36792=CARTESIAN_POINT('Ctrl Pts',(-4.58945475513934,3.58056894450221,38.4349811418222));
#36793=CARTESIAN_POINT('Ctrl Pts',(-5.74317542894098,0.948422325872549,
38.5739275271072));
#36794=CARTESIAN_POINT('Ctrl Pts',(-5.49697212635136,-1.91490635748093,
38.7128739123924));
#36795=CARTESIAN_POINT('Ctrl Pts',(-3.91085797262269,-4.31146829209936,
38.8518202976775));
#36796=CARTESIAN_POINT('Ctrl Pts',(-1.37145518756544,-5.6570910885635,38.9907666829627));
#36797=CARTESIAN_POINT('Ctrl Pts',(1.50224576117741,-5.62377334081214,39.1297130682477));
#36798=CARTESIAN_POINT('Ctrl Pts',(4.00976777537009,-4.21963639469189,39.2686594535329));
#36799=CARTESIAN_POINT('Ctrl Pts',(5.5398914638535,-1.78694473460368,39.407605838818));
#36800=CARTESIAN_POINT('Ctrl Pts',(5.71964252611128,1.08132247239395,39.5465522241031));
#36801=CARTESIAN_POINT('Ctrl Pts',(4.5052058593401,3.68601262623616,39.6854986093882));
#36802=CARTESIAN_POINT('Ctrl Pts',(2.19260568022234,5.39222117933431,39.8244449946734));
#36803=CARTESIAN_POINT('Ctrl Pts',(-0.654451664707701,5.78405237998118,
39.9633913799585));
#36804=CARTESIAN_POINT('Ctrl Pts',(-3.34198357146349,4.76599566972871,40.1023377652437));
#36805=CARTESIAN_POINT('Ctrl Pts',(-5.21489245507062,2.58620679719397,40.2412841505287));
#36806=CARTESIAN_POINT('Ctrl Pts',(-5.81664863361382,-0.223981224399285,
40.3802305358138));
#36807=CARTESIAN_POINT('Ctrl Pts',(-5.00057142273866,-2.9795728488987,40.519176921099));
#36808=CARTESIAN_POINT('Ctrl Pts',(-2.96558319008412,-5.00888063927413,
40.6581233063842));
#36809=CARTESIAN_POINT('Ctrl Pts',(-0.207721163454829,-5.81725200021949,
40.7970696916693));
#36810=CARTESIAN_POINT('Ctrl Pts',(2.60077379973059,-5.20764289851364,40.9360160769543));
#36811=CARTESIAN_POINT('Ctrl Pts',(4.77531884366656,-3.32864820266846,41.0749624622396));
#36812=CARTESIAN_POINT('Ctrl Pts',(5.78585916114505,-0.63828103778719,41.2139088475246));
#36813=CARTESIAN_POINT('Ctrl Pts',(5.38607115696136,2.20766990466273,41.3528552328098));
#36814=CARTESIAN_POINT('Ctrl Pts',(3.67340489501397,4.51549171110879,41.4918016180949));
#36815=CARTESIAN_POINT('Ctrl Pts',(1.06533022161374,5.72264278412703,41.6307480033799));
#36816=CARTESIAN_POINT('Ctrl Pts',(-1.80242332429591,5.53487480218286,41.7696943886652));
#36817=CARTESIAN_POINT('Ctrl Pts',(-4.23082834977319,3.99795702710274,41.9086407739503));
#36818=CARTESIAN_POINT('Ctrl Pts',(-5.62795057358003,1.48651984754489,42.0475871592354));
#36819=CARTESIAN_POINT('Ctrl Pts',(-5.65323538037245,-1.38726300675469,
42.1865335445205));
#36820=CARTESIAN_POINT('Ctrl Pts',(-4.30051948858164,-3.92289447272474,
42.3254799298057));
#36821=CARTESIAN_POINT('Ctrl Pts',(-1.8995332770884,-5.50230335814362,42.4644263150907));
#36822=CARTESIAN_POINT('Ctrl Pts',(0.964472427967387,-5.74050188149918,
42.603372700376));
#36823=CARTESIAN_POINT('Ctrl Pts',(3.59338378614392,-4.57942811727434,42.7423190856609));
#36824=CARTESIAN_POINT('Ctrl Pts',(5.3463922260065,-2.30209884268725,42.8812654709462));
#36825=CARTESIAN_POINT('Ctrl Pts',(5.79619432000995,0.536377032029781,43.0202118562312));
#36826=CARTESIAN_POINT('Ctrl Pts',(4.83314885245102,3.24410867355829,43.1591582415163));
#36827=CARTESIAN_POINT('Ctrl Pts',(2.69200234240633,5.16107472376478,43.2981046268015));
#36828=CARTESIAN_POINT('Ctrl Pts',(-0.105331440735626,5.82000637485882,
43.4370510120867));
#36829=CARTESIAN_POINT('Ctrl Pts',(-2.87699022732243,5.06028617251001,43.5759973973718));
#36830=CARTESIAN_POINT('Ctrl Pts',(-4.94737013972126,3.06709921854501,43.7149437826568));
#36831=CARTESIAN_POINT('Ctrl Pts',(-5.81180707434219,0.326293497377598,
43.853890167942));
#36832=CARTESIAN_POINT('Ctrl Pts',(-5.25959077066355,-2.49404768217361,
43.9928365532272));
#36833=CARTESIAN_POINT('Ctrl Pts',(-3.42532635319164,-4.70645389756827,
44.1317829385122));
#36834=CARTESIAN_POINT('Ctrl Pts',(-0.756123747233696,-5.77164151647293,
44.2707293237974));
#36835=CARTESIAN_POINT('Ctrl Pts',(2.09738730898287,-5.42996642640841,44.4096757090826));
#36836=CARTESIAN_POINT('Ctrl Pts',(4.43965109129104,-3.76471341583966,44.5486220943676));
#36837=CARTESIAN_POINT('Ctrl Pts',(5.69973062093118,-1.18179514494863,44.6875684796528));
#36838=CARTESIAN_POINT('Ctrl Pts',(5.57047603498711,1.68919082978778,44.8265148649379));
#36839=CARTESIAN_POINT('Ctrl Pts',(4.08339370065241,4.14842919684994,44.965461250223));
#36840=CARTESIAN_POINT('Ctrl Pts',(1.60096640126895,5.59646991395581,45.1044076355082));
#36841=CARTESIAN_POINT('Ctrl Pts',(-1.27170341782562,5.68034676167709,45.2433540207932));
#36842=CARTESIAN_POINT('Ctrl Pts',(-3.83439000072971,4.37961439376897,45.3823004060785));
#36843=CARTESIAN_POINT('Ctrl Pts',(-5.46242735286052,2.01133197919349,45.5212467913633));
#36844=CARTESIAN_POINT('Ctrl Pts',(-5.75897429255667,-0.84722134857191,
45.6601931766487));
#36845=CARTESIAN_POINT('Ctrl Pts',(-4.65174621417769,-3.49926078975088,
45.7991395619337));
#36846=CARTESIAN_POINT('Ctrl Pts',(-2.41063477494917,-5.29834020214,45.938085947219));
#36847=CARTESIAN_POINT('Ctrl Pts',(0.418079369703333,-5.80592615836837,
46.0770323325039));
#36848=CARTESIAN_POINT('Ctrl Pts',(3.14488485060045,-4.89829237513266,46.2159787177892));
#36849=CARTESIAN_POINT('Ctrl Pts',(5.10511097834549,-2.79667853257378,46.3549251030743));
#36850=CARTESIAN_POINT('Ctrl Pts',(5.82094411320247,-0.0133621405463012,
46.4938714883593));
#36851=CARTESIAN_POINT('Ctrl Pts',(5.11789681681116,2.77321133134302,46.6328178736445));
#36852=CARTESIAN_POINT('Ctrl Pts',(3.167339923837,4.8838024860302,46.7717642589297));
#36853=CARTESIAN_POINT('Ctrl Pts',(0.444730155969368,5.80394555492573,46.9107106442148));
#36854=CARTESIAN_POINT('Ctrl Pts',(-2.38628452059998,5.30935166491599,47.0496570294999));
#36855=CARTESIAN_POINT('Ctrl Pts',(-4.63563197220621,3.52058022709674,47.188603414785));
#36856=CARTESIAN_POINT('Ctrl Pts',(-5.75502397927113,0.873652054434358,
47.3275498000702));
#36857=CARTESIAN_POINT('Ctrl Pts',(-5.47160387472823,-1.98623260323923,
47.4664961853552));
#36858=CARTESIAN_POINT('Ctrl Pts',(-3.85445653981176,-4.36196443171659,
47.6054425706403));
#36859=CARTESIAN_POINT('Ctrl Pts',(-1.29776866963795,-5.67444846460127,
47.7443889559256));
#36860=CARTESIAN_POINT('Ctrl Pts',(1.57525595837582,-5.60376102502237,47.8833353412107));
#36861=CARTESIAN_POINT('Ctrl Pts',(4.06430509262118,-4.16713246117787,48.0222817264957));
#36862=CARTESIAN_POINT('Ctrl Pts',(5.5626622052556,-1.71474727441282,48.161228111781));
#36863=CARTESIAN_POINT('Ctrl Pts',(5.70509620054379,1.15561507115043,48.300174497066));
#36864=CARTESIAN_POINT('Ctrl Pts',(4.45688824359047,3.74429110905929,48.4391208823512));
#36865=CARTESIAN_POINT('Ctrl Pts',(2.12229431199977,5.42028012862584,48.5780672676363));
#36866=CARTESIAN_POINT('Ctrl Pts',(-0.729617905772954,5.77505188332996,
48.7170136529215));
#36867=CARTESIAN_POINT('Ctrl Pts',(-3.40368293483593,4.72213046030083,48.8559600382065));
#36868=CARTESIAN_POINT('Ctrl Pts',(-5.24808477435825,2.51816760377688,48.9949064234917));
#36869=CARTESIAN_POINT('Ctrl Pts',(-5.81324446105805,-0.29960641592774,
49.1338528087768));
#36870=CARTESIAN_POINT('Ctrl Pts',(-4.96139795468468,-3.04435619311404,
49.272799194062));
#36871=CARTESIAN_POINT('Ctrl Pts',(-2.90019417731,-5.04701895910092,49.4117455793471));
#36872=CARTESIAN_POINT('Ctrl Pts',(-0.132045607590425,-5.81947225476929,
49.5506919646322));
#36873=CARTESIAN_POINT('Ctrl Pts',(2.66827041381441,-5.17335832170609,49.6896383499173));
#36874=CARTESIAN_POINT('Ctrl Pts',(4.81822148792321,-3.26630479921574,49.8285847352024));
#36875=CARTESIAN_POINT('Ctrl Pts',(5.79363674149707,-0.562901276687905,
49.9675311204876));
#36876=CARTESIAN_POINT('Ctrl Pts',(5.35697166214563,2.27736928561665,50.1064775057727));
#36877=CARTESIAN_POINT('Ctrl Pts',(3.61416560046215,4.56331157564723,50.2454294290219));
#36878=CARTESIAN_POINT('Ctrl Pts',(1.86528972090092,5.34454787483767,50.3380658905095));
#36879=CARTESIAN_POINT('Ctrl Pts',(0.950154512558094,5.50256753975008,50.3843868902353));
#36880=CARTESIAN_POINT('Ctrl Pts',(-2.58408645063866,5.32305769023755,0.000220296677514235));
#36881=CARTESIAN_POINT('Ctrl Pts',(-3.4692611475833,4.8933482874975,0.0465357584392229));
#36882=CARTESIAN_POINT('Ctrl Pts',(-5.02021061948039,3.58425708503786,0.13916668196264));
#36883=CARTESIAN_POINT('Ctrl Pts',(-6.12306759730524,0.745034473240605,
0.278113067247767));
#36884=CARTESIAN_POINT('Ctrl Pts',(-5.73331406242883,-2.27499744055186,
0.417059452532892));
#36885=CARTESIAN_POINT('Ctrl Pts',(-3.9460860794766,-4.7408798866814,0.556005837818019));
#36886=CARTESIAN_POINT('Ctrl Pts',(-1.19695885730938,-6.05095353285258,
0.694952223103144));
#36887=CARTESIAN_POINT('Ctrl Pts',(1.84392018446255,-5.88618259004128,0.83389860838827));
#36888=CARTESIAN_POINT('Ctrl Pts',(4.43534186760578,-4.286577006635,0.972844993673396));
#36889=CARTESIAN_POINT('Ctrl Pts',(5.94562651323158,-1.64212630236546,1.11179137895852));
#36890=CARTESIAN_POINT('Ctrl Pts',(6.00664047788067,1.40261348122994,1.25073776424365));
#36891=CARTESIAN_POINT('Ctrl Pts',(4.60350888165559,4.10545313734612,1.38968414952877));
#36892=CARTESIAN_POINT('Ctrl Pts',(2.07825241101868,5.80757432743904,1.5286305348139));
#36893=CARTESIAN_POINT('Ctrl Pts',(-0.953587337660047,6.09407219459964,
1.66757692009903));
#36894=CARTESIAN_POINT('Ctrl Pts',(-3.75298591552093,4.8951144133636,1.80652330538415));
#36895=CARTESIAN_POINT('Ctrl Pts',(-5.63757791961995,2.50295073333117,1.94546969066928));
#36896=CARTESIAN_POINT('Ctrl Pts',(-6.14798576986681,-0.499317821657796,
2.08441607595441));
#36897=CARTESIAN_POINT('Ctrl Pts',(-5.1597953784654,-3.37987561340746,2.22336246123953));
#36898=CARTESIAN_POINT('Ctrl Pts',(-2.9138824262184,-5.43657396736167,2.36230884652466));
#36899=CARTESIAN_POINT('Ctrl Pts',(0.0423020301180563,-6.16808381712523,
2.50125523180978));
#36900=CARTESIAN_POINT('Ctrl Pts',(2.98817518474946,-5.39609640682365,2.64020161709491));
#36901=CARTESIAN_POINT('Ctrl Pts',(5.20566764746265,-3.30878704922065,2.77914800238003));
#36902=CARTESIAN_POINT('Ctrl Pts',(6.15425599259743,-0.414946460616659,
2.91809438766516));
#36903=CARTESIAN_POINT('Ctrl Pts',(5.60271768671038,2.58003912925357,3.05704077295029));
#36904=CARTESIAN_POINT('Ctrl Pts',(3.68549258980999,4.94612896710534,3.19598715823541));
#36905=CARTESIAN_POINT('Ctrl Pts',(0.869912653233688,6.10657836780115,3.33493354352054));
#36906=CARTESIAN_POINT('Ctrl Pts',(-2.15771227404257,5.77852274635241,3.47387992880566));
#36907=CARTESIAN_POINT('Ctrl Pts',(-4.6593854549632,4.04192708608156,3.61282631409079));
#36908=CARTESIAN_POINT('Ctrl Pts',(-6.02531317687573,1.32009412839944,3.75177269937591));
#36909=CARTESIAN_POINT('Ctrl Pts',(-5.92254461988993,-1.72351751157118,
3.89071908466104));
#36910=CARTESIAN_POINT('Ctrl Pts',(-4.3761300664986,-4.34701426594362,4.02966546994617));
#36911=CARTESIAN_POINT('Ctrl Pts',(-1.76301478635964,-5.91090739652963,
4.16861185523129));
#36912=CARTESIAN_POINT('Ctrl Pts',(1.27984301178143,-6.03399115448819,4.30755824051643));
#36913=CARTESIAN_POINT('Ctrl Pts',(4.01073351232212,-4.6862633387801,4.44650462580154));
#36914=CARTESIAN_POINT('Ctrl Pts',(5.76399028457363,-2.19623846305353,4.58545101108668));
#36915=CARTESIAN_POINT('Ctrl Pts',(6.11224936889116,0.829129085091465,4.72439739637179));
#36916=CARTESIAN_POINT('Ctrl Pts',(4.97062109959005,3.65239281452117,4.86334378165692));
#36917=CARTESIAN_POINT('Ctrl Pts',(2.61738232997109,5.58536991845751,5.00229016694205));
#36918=CARTESIAN_POINT('Ctrl Pts',(-0.373854760340773,6.15688882516372,
5.14123655222717));
#36919=CARTESIAN_POINT('Ctrl Pts',(-3.27396312767273,5.22763931673701,5.2801829375123));
#36920=CARTESIAN_POINT('Ctrl Pts',(-5.37602875071488,3.0241300003046,5.41912932279743));
#36921=CARTESIAN_POINT('Ctrl Pts',(-6.16766399617026,0.0834758504031012,
5.55807570808255));
#36922=CARTESIAN_POINT('Ctrl Pts',(-5.45590433172023,-2.87752590090372,
5.69702209336768));
#36923=CARTESIAN_POINT('Ctrl Pts',(-3.41424426959418,-5.13711820525854,
5.83596847865281));
#36924=CARTESIAN_POINT('Ctrl Pts',(-0.540347325032756,-6.14451561602582,
5.97491486393793));
#36925=CARTESIAN_POINT('Ctrl Pts',(2.46526162889552,-5.65416063517396,6.11386124922306));
#36926=CARTESIAN_POINT('Ctrl Pts',(4.86995234428682,-3.78557942085893,6.25280763450818));
#36927=CARTESIAN_POINT('Ctrl Pts',(6.08757100607258,-0.994246766793666,
6.39175401979331));
#36928=CARTESIAN_POINT('Ctrl Pts',(5.82131777245357,2.03943785866883,6.53070040507843));
#36929=CARTESIAN_POINT('Ctrl Pts',(4.13609302652729,4.57600064064325,6.66964679036356));
#36930=CARTESIAN_POINT('Ctrl Pts',(1.44267762578629,5.99714337458352,6.80859317564868));
#36931=CARTESIAN_POINT('Ctrl Pts',(-1.6023967175606,5.95645634138339,6.94753956093381));
#36932=CARTESIAN_POINT('Ctrl Pts',(-4.25687989538264,4.46385718225195,7.08648594621893));
#36933=CARTESIAN_POINT('Ctrl Pts',(-5.87373009404587,1.88317343055689,7.22543233150407));
#36934=CARTESIAN_POINT('Ctrl Pts',(-6.05883304917731,-1.1565420309924,7.36437871678918));
#36935=CARTESIAN_POINT('Ctrl Pts',(-4.7670691108211,-3.91434534499841,7.50332510207432));
#36936=CARTESIAN_POINT('Ctrl Pts',(-2.31331135425011,-5.71800996549961,
7.64227148735944));
#36937=CARTESIAN_POINT('Ctrl Pts',(0.704326100885125,-6.12788480071773,
7.78121787264457));
#36938=CARTESIAN_POINT('Ctrl Pts',(3.55028100722364,-5.04406107784218,7.92016425792969));
#36939=CARTESIAN_POINT('Ctrl Pts',(5.53083948497785,-2.73072554070624,8.05911064321483));
#36940=CARTESIAN_POINT('Ctrl Pts',(6.16323179570631,0.248236217442325,8.19805702849994));
#36941=CARTESIAN_POINT('Ctrl Pts',(5.29330956465926,3.16668931850635,8.33700341378508));
#36942=CARTESIAN_POINT('Ctrl Pts',(3.13312011720682,5.31324813258417,8.4759497990702));
#36943=CARTESIAN_POINT('Ctrl Pts',(0.209219021510298,6.16467961765197,8.61489618435532));
#36944=CARTESIAN_POINT('Ctrl Pts',(-2.76568012015457,5.51344364805129,8.75384256964046));
#36945=CARTESIAN_POINT('Ctrl Pts',(-5.06643271011871,3.51828182229544,8.89278895492557));
#36946=CARTESIAN_POINT('Ctrl Pts',(-6.13222030320556,0.665523508381978,
9.03173534021072));
#36947=CARTESIAN_POINT('Ctrl Pts',(-5.70325254062085,-2.34945905373065,
9.17068172549582));
#36948=CARTESIAN_POINT('Ctrl Pts',(-3.88409217921783,-4.7917507583966,9.30962811078097));
#36949=CARTESIAN_POINT('Ctrl Pts',(-1.11816746497952,-6.06603238596007,
9.44857449606607));
#36950=CARTESIAN_POINT('Ctrl Pts',(1.92031542952214,-5.86169225039958,9.58752088135123));
#36951=CARTESIAN_POINT('Ctrl Pts',(4.49071309046551,-4.22853914802464,9.72646726663632));
#36952=CARTESIAN_POINT('Ctrl Pts',(5.96647991447557,-1.56466124685663,9.86541365192148));
#36953=CARTESIAN_POINT('Ctrl Pts',(5.98789132304063,1.48060963481603,10.0043600372065));
#36954=CARTESIAN_POINT('Ctrl Pts',(4.54972819224755,4.16497548179135,10.1433064224917));
#36955=CARTESIAN_POINT('Ctrl Pts',(2.0025490369231,5.83411044992925,10.2822528077768));
#36956=CARTESIAN_POINT('Ctrl Pts',(-1.03276015123316,6.08115563501546,10.421199193062));
#36957=CARTESIAN_POINT('Ctrl Pts',(-3.81632956311736,4.84589269927964,10.560145578347));
#36958=CARTESIAN_POINT('Ctrl Pts',(-5.66965205440495,2.4294223529961,10.6990919636322));
#36959=CARTESIAN_POINT('Ctrl Pts',(-6.14097221145061,-0.57923025253058,
10.8380383489173));
#36960=CARTESIAN_POINT('Ctrl Pts',(-5.11540369714552,-3.44669296608871,
10.9769847342025));
#36961=CARTESIAN_POINT('Ctrl Pts',(-2.84293329499841,-5.47400928638642,
11.1159311194876));
#36962=CARTESIAN_POINT('Ctrl Pts',(0.122514456037195,-6.16701204760598,
11.2548775047727));
#36963=CARTESIAN_POINT('Ctrl Pts',(3.05809877584333,-5.35677881421669,11.3938238900578));
#36964=CARTESIAN_POINT('Ctrl Pts',(5.24825822548055,-3.24080745894155,11.532770275343));
#36965=CARTESIAN_POINT('Ctrl Pts',(6.15913191847538,-0.334875197757514,
11.6717166606281));
#36966=CARTESIAN_POINT('Ctrl Pts',(5.56869043259187,2.65268434858258,11.8106630459132));
#36967=CARTESIAN_POINT('Ctrl Pts',(3.62085644666365,4.9936405537353,11.9496094311983));
#36968=CARTESIAN_POINT('Ctrl Pts',(0.7904229619961,6.1173751665567,12.0885558164834));
#36969=CARTESIAN_POINT('Ctrl Pts',(-2.23267955562705,5.7499729902966,12.2275022017686));
#36970=CARTESIAN_POINT('Ctrl Pts',(-4.7115567261068,3.98098990251583,12.3664485870537));
#36971=CARTESIAN_POINT('Ctrl Pts',(-6.04197146345827,1.24162322063148,12.5053949723388));
#36972=CARTESIAN_POINT('Ctrl Pts',(-5.89962939213839,-1.80039451861864,
12.644341357624));
#36973=CARTESIAN_POINT('Ctrl Pts',(-4.31922701079247,-4.40355826763949,
12.7832877429091));
#36974=CARTESIAN_POINT('Ctrl Pts',(-1.68599426988362,-5.93333554665289,
12.9222341281942));
#36975=CARTESIAN_POINT('Ctrl Pts',(1.35820690332742,-6.0168364939567,13.0611805134793));
#36976=CARTESIAN_POINT('Ctrl Pts',(4.07133923972621,-4.63370739066687,13.2001268987645));
#36977=CARTESIAN_POINT('Ctrl Pts',(5.79206493832777,-2.12109196817337,13.3390732840496));
#36978=CARTESIAN_POINT('Ctrl Pts',(6.10094963010233,0.908548841950409,13.4780196693347));
#36979=CARTESIAN_POINT('Ctrl Pts',(4.92270132870797,3.71672692238643,13.6169660546198));
#36980=CARTESIAN_POINT('Ctrl Pts',(2.54452317945555,5.61893665887672,13.755912439905));
#36981=CARTESIAN_POINT('Ctrl Pts',(-0.453893555832864,6.15150615924497,
13.8948588251901));
#36982=CARTESIAN_POINT('Ctrl Pts',(-3.34167176381149,5.18461929269647,14.0338052104752));
#36983=CARTESIAN_POINT('Ctrl Pts',(-5.41490295311199,2.95395893601018,14.1727515957603));
#36984=CARTESIAN_POINT('Ctrl Pts',(-6.16822800900523,0.00325824781025046,
14.3116979810455));
#36985=CARTESIAN_POINT('Ctrl Pts',(-5.41802067441278,-2.94823665245703,
14.4506443663306));
#36986=CARTESIAN_POINT('Ctrl Pts',(-3.34714724829327,-5.18108605270152,
14.5895907516157));
#36987=CARTESIAN_POINT('Ctrl Pts',(-0.46039213035129,-6.15102320541598,
14.7285371369008));
#36988=CARTESIAN_POINT('Ctrl Pts',(2.53858557068867,-5.62162171330895,14.867483522186));
#36989=CARTESIAN_POINT('Ctrl Pts',(4.91877200364035,-3.72192549139007,15.0064299074711));
#36990=CARTESIAN_POINT('Ctrl Pts',(6.0999863788,-0.914993751732644,15.1453762927562));
#36991=CARTESIAN_POINT('Ctrl Pts',(5.7943025574829,2.11497169238796,15.2843226780413));
#36992=CARTESIAN_POINT('Ctrl Pts',(4.07623229994285,4.62940359270587,15.4232690633265));
#36993=CARTESIAN_POINT('Ctrl Pts',(1.36456269990763,6.01539824328165,15.5622154486116));
#36994=CARTESIAN_POINT('Ctrl Pts',(-1.67972498998492,5.935113423118,15.7011618338967));
#36995=CARTESIAN_POINT('Ctrl Pts',(-4.31457241180318,4.40811890612791,15.8401082191819));
#36996=CARTESIAN_POINT('Ctrl Pts',(-5.89772405279568,1.80662624367373,15.979054604467));
#36997=CARTESIAN_POINT('Ctrl Pts',(-6.04327981850941,-1.2352394190812,16.1180009897521));
#36998=CARTESIAN_POINT('Ctrl Pts',(-4.71575985832071,-3.97601010384864,
16.2569473750372));
#36999=CARTESIAN_POINT('Ctrl Pts',(-2.23875293325552,-5.7476110420848,16.3958937603224));
#37000=CARTESIAN_POINT('Ctrl Pts',(0.783959751151009,-6.11820680394433,
16.5348401456075));
#37001=CARTESIAN_POINT('Ctrl Pts',(3.61557883834099,-4.99746306149393,16.6737865308926));
#37002=CARTESIAN_POINT('Ctrl Pts',(5.56588486676205,-2.6585659738296,16.8127329161777));
#37003=CARTESIAN_POINT('Ctrl Pts',(6.15948226400517,0.328368126743459,16.9516793014629));
#37004=CARTESIAN_POINT('Ctrl Pts',(5.25167908412416,3.23526106900636,17.090625686748));
#37005=CARTESIAN_POINT('Ctrl Pts',(3.0637562984359,5.3535450620173,17.2295720720331));
#37006=CARTESIAN_POINT('Ctrl Pts',(0.129029596853515,6.16687917429807,17.3685184573182));
#37007=CARTESIAN_POINT('Ctrl Pts',(-2.83714862985361,5.4770096804164,17.5074648426033));
#37008=CARTESIAN_POINT('Ctrl Pts',(-5.11175954494723,3.45209526836909,17.6464112278885));
#37009=CARTESIAN_POINT('Ctrl Pts',(-6.14035685013834,0.585717628396678,
17.7853576131736));
#37010=CARTESIAN_POINT('Ctrl Pts',(-5.67221548097349,-2.42343122961229,
17.9243039984588));
#37011=CARTESIAN_POINT('Ctrl Pts',(-3.82144693119744,-4.84185819074629,
18.0632503837439));
#37012=CARTESIAN_POINT('Ctrl Pts',(-1.03918408011006,-6.0800611703256,18.202196769029));
#37013=CARTESIAN_POINT('Ctrl Pts',(1.99638440783797,-5.8362228096087,18.3411431543141));
#37014=CARTESIAN_POINT('Ctrl Pts',(4.54532551809133,-4.16977976898578,18.4800895395992));
#37015=CARTESIAN_POINT('Ctrl Pts',(5.9863237747773,-1.48693478363758,18.6190359248844));
#37016=CARTESIAN_POINT('Ctrl Pts',(5.96812958880847,1.55835701892862,18.7579823101695));
#37017=CARTESIAN_POINT('Ctrl Pts',(4.49517787210488,4.22379252395216,18.8969286954546));
#37018=CARTESIAN_POINT('Ctrl Pts',(1.92650700853492,5.85966024043385,19.0358750807397));
#37019=CARTESIAN_POINT('Ctrl Pts',(-1.11175831289245,6.06721030136336,19.1748214660249));
#37020=CARTESIAN_POINT('Ctrl Pts',(-3.87902771273827,4.79585147716898,19.31376785131));
#37021=CARTESIAN_POINT('Ctrl Pts',(-5.70076724546849,2.35548300784553,19.4527142365951));
#37022=CARTESIAN_POINT('Ctrl Pts',(-6.13291998087729,-0.659044683926238,
19.5916606218803));
#37023=CARTESIAN_POINT('Ctrl Pts',(-5.07014681114061,-3.51292736912334,
19.7306070071654));
#37024=CARTESIAN_POINT('Ctrl Pts',(-2.77150331625738,-5.51051873739938,
19.8695533924505));
#37025=CARTESIAN_POINT('Ctrl Pts',(0.202706159690122,-6.16489720920625,
20.0084997777356));
#37026=CARTESIAN_POINT('Ctrl Pts',(3.12750512804936,-5.31655518745741,20.1474461630208));
#37027=CARTESIAN_POINT('Ctrl Pts',(5.28996112617996,-3.17227972769742,20.2863925483059));
#37028=CARTESIAN_POINT('Ctrl Pts',(6.16296610434022,-0.25474729440942,20.425338933591));
#37029=CARTESIAN_POINT('Ctrl Pts',(5.53372130415038,2.72488089927755,20.5642853188761));
#37030=CARTESIAN_POINT('Ctrl Pts',(3.55560788098422,5.04030752870678,20.7032317041613));
#37031=CARTESIAN_POINT('Ctrl Pts',(0.710799580598698,6.12713728779403,20.8421780894464));
#37032=CARTESIAN_POINT('Ctrl Pts',(-2.30726920740392,5.72045069831224,20.9811244747315));
#37033=CARTESIAN_POINT('Ctrl Pts',(-4.76293109640132,3.9193793843144,21.1200708600166));
#37034=CARTESIAN_POINT('Ctrl Pts',(-6.0576078261867,1.1629423078455,21.2590172453017));
#37035=CARTESIAN_POINT('Ctrl Pts',(-5.8757163159144,-1.87696701147159,21.3979636305869));
#37036=CARTESIAN_POINT('Ctrl Pts',(-4.26159341189583,-4.45935746256581,
21.536910015872));
#37037=CARTESIAN_POINT('Ctrl Pts',(-1.60868858857865,-5.95476014733023,
21.6758564011572));
#37038=CARTESIAN_POINT('Ctrl Pts',(1.43634107117479,-5.99866416083712,21.8148027864422));
#37039=CARTESIAN_POINT('Ctrl Pts',(4.1312563510539,-4.58036770894347,21.9537491717274));
#37040=CARTESIAN_POINT('Ctrl Pts',(5.81915993678993,-2.04558671713384,22.0926955570125));
#37041=CARTESIAN_POINT('Ctrl Pts',(6.08861799204188,0.987814929143823,22.2316419422977));
#37042=CARTESIAN_POINT('Ctrl Pts',(4.87394894450772,3.78043239241062,22.3705883275827));
#37043=CARTESIAN_POINT('Ctrl Pts',(2.471233654691,5.65155302648554,22.5095347128679));
#37044=CARTESIAN_POINT('Ctrl Pts',(-0.533855580910739,6.14508304305042,
22.648481098153));
#37045=CARTESIAN_POINT('Ctrl Pts',(-3.40881519799501,5.14072235519228,22.7874274834382));
#37046=CARTESIAN_POINT('Ctrl Pts',(-5.45286129244639,2.88328824653298,22.9263738687233));
#37047=CARTESIAN_POINT('Ctrl Pts',(-6.16774874327281,-0.0769599058743887,
23.0653202540084));
#37048=CARTESIAN_POINT('Ctrl Pts',(-5.37922062671915,-3.0184487466801,23.2042666392935));
#37049=CARTESIAN_POINT('Ctrl Pts',(-3.27948409892758,-5.22417758428409,
23.3432130245786));
#37050=CARTESIAN_POINT('Ctrl Pts',(-0.380359066103212,-6.15649042621594,
23.4821594098638));
#37051=CARTESIAN_POINT('Ctrl Pts',(2.61148014250494,-5.58813196449027,23.6211057951489));
#37052=CARTESIAN_POINT('Ctrl Pts',(4.96675971427183,-3.65764204480724,23.760052180434));
#37053=CARTESIAN_POINT('Ctrl Pts',(6.11137001517765,-0.835585976930445,
23.8989985657192));
#37054=CARTESIAN_POINT('Ctrl Pts',(5.766307308755,2.19014780511587,24.0379449510043));
#37055=CARTESIAN_POINT('Ctrl Pts',(4.01568212968219,4.68202353909146,24.1768913362894));
#37056=CARTESIAN_POINT('Ctrl Pts',(1.28621697532681,6.03263568265451,24.3158377215745));
#37057=CARTESIAN_POINT('Ctrl Pts',(-1.75676915795036,5.91276665469978,24.4547841068596));
#37058=CARTESIAN_POINT('Ctrl Pts',(-4.37153517230061,4.351635051862,24.5937304921448));
#37059=CARTESIAN_POINT('Ctrl Pts',(-5.92072048533674,1.72977348857279,24.7326768774299));
#37060=CARTESIAN_POINT('Ctrl Pts',(-6.02670444269671,-1.31372788188239,
24.871623262715));
#37061=CARTESIAN_POINT('Ctrl Pts',(-4.66365299406171,-4.03700237035283,
25.0105696480002));
#37062=CARTESIAN_POINT('Ctrl Pts',(-2.163815855222,-5.77623998219821,25.1495160332853));
#37063=CARTESIAN_POINT('Ctrl Pts',(0.863460804436876,-6.10749398906431,
25.2884624185704));
#37064=CARTESIAN_POINT('Ctrl Pts',(3.68026513954963,-4.95001978681612,25.4274088038556));
#37065=CARTESIAN_POINT('Ctrl Pts',(5.59998884878251,-2.58595674379267,25.5663551891406));
#37066=CARTESIAN_POINT('Ctrl Pts',(6.15469093296995,0.408444496685631,25.7053015744258));
#37067=CARTESIAN_POINT('Ctrl Pts',(5.209160347801,3.3032856155884,25.8442479597109));
#37068=CARTESIAN_POINT('Ctrl Pts',(2.99387428363253,5.39293650630704,25.983194344996));
#37069=CARTESIAN_POINT('Ctrl Pts',(0.0488183484554523,6.16803568051526,
26.1221407302812));
#37070=CARTESIAN_POINT('Ctrl Pts',(-2.90813727137102,5.43964934514331,26.2610871155663));
#37071=CARTESIAN_POINT('Ctrl Pts',(-5.15622178962649,3.38532483573388,26.4000335008514));
#37072=CARTESIAN_POINT('Ctrl Pts',(-6.1474548325614,0.505812681605302,26.5389798861365));
#37073=CARTESIAN_POINT('Ctrl Pts',(-5.64021903706985,-2.49699351243254,
26.6779262714217));
#37074=CARTESIAN_POINT('Ctrl Pts',(-3.75815533325717,-4.89114668338274,
26.8168726567068));
#37075=CARTESIAN_POINT('Ctrl Pts',(-0.960024930259674,-6.09306158844103,
26.9558190419919));
#37076=CARTESIAN_POINT('Ctrl Pts',(2.07211572271754,-5.80976624477457,27.0947654272771));
#37077=CARTESIAN_POINT('Ctrl Pts',(4.5991691607941,-4.11031512388719,27.2337118125622));
#37078=CARTESIAN_POINT('Ctrl Pts',(6.00515512333616,-1.40895682401013,27.3726581978473));
#37079=CARTESIAN_POINT('Ctrl Pts',(5.94735842015232,1.63584082645554,27.5116045831324));
#37080=CARTESIAN_POINT('Ctrl Pts',(4.43986724888588,4.28189516447166,27.6505509684176));
#37081=CARTESIAN_POINT('Ctrl Pts',(1.85013913559806,5.8842189427471,27.7894973537027));
#37082=CARTESIAN_POINT('Ctrl Pts',(-1.19056843454766,6.05223877502484,27.9284437389878));
#37083=CARTESIAN_POINT('Ctrl Pts',(-3.94106977337074,4.74499909680486,28.0673901242729));
#37084=CARTESIAN_POINT('Ctrl Pts',(-5.73091822310212,2.28114526222492,28.206336509558));
#37085=CARTESIAN_POINT('Ctrl Pts',(-6.12383044364763,-0.738747646162098,
28.3452828948432));
#37086=CARTESIAN_POINT('Ctrl Pts',(-5.02403237325955,-3.57856760446066,
28.4842292801283));
#37087=CARTESIAN_POINT('Ctrl Pts',(-2.69960457241791,-5.54609615313651,
28.6231756654135));
#37088=CARTESIAN_POINT('Ctrl Pts',(0.282863578133191,-6.16173965560222,
28.7621220506985));
#37089=CARTESIAN_POINT('Ctrl Pts',(3.19638250190623,-5.27543233192912,28.9010684359837));
#37090=CARTESIAN_POINT('Ctrl Pts',(5.33076929616305,-3.10321544504092,29.0400148212688));
#37091=CARTESIAN_POINT('Ctrl Pts',(6.16575790162297,-0.174576303744733,
29.178961206554));
#37092=CARTESIAN_POINT('Ctrl Pts',(5.4978162160092,2.79661657047253,29.3179075918391));
#37093=CARTESIAN_POINT('Ctrl Pts',(3.48975792873298,5.08612199874332,29.4568539771242));
#37094=CARTESIAN_POINT('Ctrl Pts',(0.631055976348368,6.13586308044519,29.5958003624093));
#37095=CARTESIAN_POINT('Ctrl Pts',(-2.38146861347181,5.68996086368824,29.7347467476945));
#37096=CARTESIAN_POINT('Ctrl Pts',(-4.81349987651282,3.85710595214422,29.8736931329796));
#37097=CARTESIAN_POINT('Ctrl Pts',(-6.07221962036718,1.08406469792324,30.0126395182647));
#37098=CARTESIAN_POINT('Ctrl Pts',(-5.85080943581484,-1.95322203884639,
30.1515859035498));
#37099=CARTESIAN_POINT('Ctrl Pts',(-4.20323901781073,-4.51440241298987,
30.290532288835));
#37100=CARTESIAN_POINT('Ctrl Pts',(-1.53111081773288,-5.97517757485722,
30.42947867412));
#37101=CARTESIAN_POINT('Ctrl Pts',(1.514232299907,-5.97947722875285,30.5684250594052));
#37102=CARTESIAN_POINT('Ctrl Pts',(4.19047471207587,-4.52625331534901,30.7073714446903));
#37103=CARTESIAN_POINT('Ctrl Pts',(5.84527069718027,-1.96973548070316,30.8463178299755));
#37104=CARTESIAN_POINT('Ctrl Pts',(6.07525654045197,1.06691393980534,30.9852642152606));
#37105=CARTESIAN_POINT('Ctrl Pts',(4.82437219284485,3.84349844961081,31.1242106005457));
#37106=CARTESIAN_POINT('Ctrl Pts',(2.39752615168313,5.6832135046337,31.2631569858308));
#37107=CARTESIAN_POINT('Ctrl Pts',(-0.613727310998874,6.13762056296976,
31.402103371116));
#37108=CARTESIAN_POINT('Ctrl Pts',(-3.47538207375193,5.09595592884191,31.5410497564011));
#37109=CARTESIAN_POINT('Ctrl Pts',(-5.48989734854015,2.81212988493551,31.6799961416862));
#37110=CARTESIAN_POINT('Ctrl Pts',(-6.16622628003476,-0.157165042754142,
31.8189425269713));
#37111=CARTESIAN_POINT('Ctrl Pts',(-5.33951075118179,-3.08815030807591,
31.9578889122565));
#37112=CARTESIAN_POINT('Ctrl Pts',(-3.21126626587201,-5.26638551161304,
32.0968352975416));
#37113=CARTESIAN_POINT('Ctrl Pts',(-0.300261668879607,-6.16091635371372,
32.2357816828267));
#37114=CARTESIAN_POINT('Ctrl Pts',(2.68393301513983,-5.55369705308975,32.3747280681118));
#37115=CARTESIAN_POINT('Ctrl Pts',(5.01390735966058,-3.59273995385092,32.513674453397));
#37116=CARTESIAN_POINT('Ctrl Pts',(6.12171998980593,-0.756036873218341,
32.652620838682));
#37117=CARTESIAN_POINT('Ctrl Pts',(5.73733676131583,2.26495348175397,32.7915672239672));
#37118=CARTESIAN_POINT('Ctrl Pts',(3.95445275704879,4.73385157979469,32.9305136092523));
#37119=CARTESIAN_POINT('Ctrl Pts',(1.20765370324269,6.04885277720492,33.0694599945375));
#37120=CARTESIAN_POINT('Ctrl Pts',(-1.83351619040011,5.88941981580495,33.2084063798226));
#37121=CARTESIAN_POINT('Ctrl Pts',(-4.427758542337,4.29441517299123,33.3473527651077));
#37122=CARTESIAN_POINT('Ctrl Pts',(-5.9427155021103,1.65262816393567,33.4862991503928));
#37123=CARTESIAN_POINT('Ctrl Pts',(-6.00910972525653,-1.39199414405475,
33.625245535678));
#37124=CARTESIAN_POINT('Ctrl Pts',(-4.61075733126812,-4.09731182843245,
33.764191920963));
#37125=CARTESIAN_POINT('Ctrl Pts',(-2.08851279481842,-5.80389194361292,
33.9031383062483));
#37126=CARTESIAN_POINT('Ctrl Pts',(0.942815814134629,-6.09574816801622,
34.0420846915333));
#37127=CARTESIAN_POINT('Ctrl Pts',(3.74432896997149,-4.90173927824479,34.1810310768185));
#37128=CARTESIAN_POINT('Ctrl Pts',(5.63314566277761,-2.51291013153774,34.3199774621036));
#37129=CARTESIAN_POINT('Ctrl Pts',(6.14885861299432,0.488451783353388,34.4589238473887));
#37130=CARTESIAN_POINT('Ctrl Pts',(5.16576054720173,3.37075145275196,34.5978702326739));
#37131=CARTESIAN_POINT('Ctrl Pts',(2.92348589246469,5.43141580288374,34.736816617959));
#37132=CARTESIAN_POINT('Ctrl Pts',(-0.0314011569553952,6.16814894069502,
34.8757630032441));
#37133=CARTESIAN_POINT('Ctrl Pts',(-2.97863403786675,5.40136896126499,35.0147093885292));
#37134=CARTESIAN_POINT('Ctrl Pts',(-5.19981192392431,3.31798181777267,35.1536557738144));
#37135=CARTESIAN_POINT('Ctrl Pts',(-6.1535130499399,0.425822182929395,35.2926021590995));
#37136=CARTESIAN_POINT('Ctrl Pts',(-5.60726862070789,-2.57013346005217,
35.4315485443846));
#37137=CARTESIAN_POINT('Ctrl Pts',(-3.69422809037848,-4.93960789977443,
35.5704949296698));
#37138=CARTESIAN_POINT('Ctrl Pts',(-0.880703404207672,-6.10503144144831,
35.7094413149548));
#37139=CARTESIAN_POINT('Ctrl Pts',(2.14749656515694,-5.78232703069399,35.84838770024));
#37140=CARTESIAN_POINT('Ctrl Pts',(4.65223491159577,-4.05015527042914,35.9873340855251));
#37141=CARTESIAN_POINT('Ctrl Pts',(6.02297077506532,-1.3307405569699,36.1262804708102));
#37142=CARTESIAN_POINT('Ctrl Pts',(5.92558133025528,1.71304795198071,36.2652268560954));
#37143=CARTESIAN_POINT('Ctrl Pts',(4.38380567769012,4.3392735760156,36.4041732413805));
#37144=CARTESIAN_POINT('Ctrl Pts',(1.77345833478221,5.90778240307198,36.5431196266656));
#37145=CARTESIAN_POINT('Ctrl Pts',(-1.26917718645326,6.03624358824607,36.6820660119508));
#37146=CARTESIAN_POINT('Ctrl Pts',(-4.00244525137675,4.69334415923093,36.8210123972359));
#37147=CARTESIAN_POINT('Ctrl Pts',(-5.7600998876454,2.20642168943353,36.959958782521));
#37148=CARTESIAN_POINT('Ctrl Pts',(-6.11370513714305,-0.818325658479648,
37.0989051678061));
#37149=CARTESIAN_POINT('Ctrl Pts',(-4.97706818318234,-3.64360256987634,
37.2378515530912));
#37150=CARTESIAN_POINT('Ctrl Pts',(-2.62724922425273,-5.58073551612318,
37.3767979383764));
#37151=CARTESIAN_POINT('Ctrl Pts',(0.362973153742378,-6.15753992085458,
37.5157443236615));
#37152=CARTESIAN_POINT('Ctrl Pts',(3.26471924766826,-5.23341720304809,37.6546907089466));
#37153=CARTESIAN_POINT('Ctrl Pts',(5.37067583323858,-3.03362629233108,37.7936370942318));
#37154=CARTESIAN_POINT('Ctrl Pts',(6.16750683812607,-0.0943757856832029,
37.9325834795169));
#37155=CARTESIAN_POINT('Ctrl Pts',(5.46098124106467,2.86787922897654,38.071529864802));
#37156=CARTESIAN_POINT('Ctrl Pts',(3.42331772760518,5.13107621490068,38.2104762500871));
#37157=CARTESIAN_POINT('Ctrl Pts',(0.551205636877804,6.14355106865155,38.3494226353723));
#37158=CARTESIAN_POINT('Ctrl Pts',(-2.45526522392973,5.65850864339859,38.4883690206574));
#37159=CARTESIAN_POINT('Ctrl Pts',(-4.8632545133651,3.79418013877694,38.6273154059425));
#37160=CARTESIAN_POINT('Ctrl Pts',(-6.08580437459756,1.00500373202518,38.7662617912276));
#37161=CARTESIAN_POINT('Ctrl Pts',(-5.82491296452679,-2.02914670315951,
38.9052081765128));
#37162=CARTESIAN_POINT('Ctrl Pts',(-4.14417369845267,-4.56868380874715,
39.0441545617979));
#37163=CARTESIAN_POINT('Ctrl Pts',(-1.45327407865533,-5.99458437588159,
39.183100947083));
#37164=CARTESIAN_POINT('Ctrl Pts',(1.59186741519754,-5.95927894293327,39.3220473323681));
#37165=CARTESIAN_POINT('Ctrl Pts',(4.24898430674745,-4.47137336265596,39.4609937176533));
#37166=CARTESIAN_POINT('Ctrl Pts',(5.87039280319046,-1.89355108816871,39.5999401029384));
#37167=CARTESIAN_POINT('Ctrl Pts',(6.06086753525496,1.14583249532731,39.7388864882236));
#37168=CARTESIAN_POINT('Ctrl Pts',(4.7739794590064,3.90591442715279,39.8778328735086));
#37169=CARTESIAN_POINT('Ctrl Pts',(2.32341313713361,5.71391273834754,40.0167792587938));
#37170=CARTESIAN_POINT('Ctrl Pts',(-0.693495236793662,6.12911998118813,
40.1557256440789));
#37171=CARTESIAN_POINT('Ctrl Pts',(-3.5413611321283,5.05032758532616,40.294672029364));
#37172=CARTESIAN_POINT('Ctrl Pts',(-5.52600485720787,2.74049588676401,40.4336184146491));
#37173=CARTESIAN_POINT('Ctrl Pts',(-6.16366087679677,-0.237343597134103,
40.5725647999343));
#37174=CARTESIAN_POINT('Ctrl Pts',(-5.29889776422902,-3.15732954749802,
40.7115111852194));
#37175=CARTESIAN_POINT('Ctrl Pts',(-3.14250528731887,-5.3077026957459,40.8504575705046));
#37176=CARTESIAN_POINT('Ctrl Pts',(-0.220113486152523,-6.16430023931905,
40.9894039557896));
#37177=CARTESIAN_POINT('Ctrl Pts',(2.75593193409692,-5.51832280334161,41.1283503410748));
#37178=CARTESIAN_POINT('Ctrl Pts',(5.06020696537266,-3.52723019589728,41.2672967263599));
#37179=CARTESIAN_POINT('Ctrl Pts',(6.1310345521162,-0.676359895331296,41.406243111645));
#37180=CARTESIAN_POINT('Ctrl Pts',(5.70739581517076,2.33937606985853,41.5451894969302));
#37181=CARTESIAN_POINT('Ctrl Pts',(3.89255453822456,4.78487894875124,41.6841358822153));
#37182=CARTESIAN_POINT('Ctrl Pts',(1.12888617164935,6.06404678401431,41.8230822675004));
#37183=CARTESIAN_POINT('Ctrl Pts',(-1.90995310653424,5.86507685525906,41.9620286527856));
#37184=CARTESIAN_POINT('Ctrl Pts',(-4.4832330124328,4.23646894754202,42.1009750380707));
#37185=CARTESIAN_POINT('Ctrl Pts',(-5.96370538293448,1.57520331792875,42.2399214233557));
#37186=CARTESIAN_POINT('Ctrl Pts',(-5.9904986421152,-1.47002496783944,42.3788678086409));
#37187=CARTESIAN_POINT('Ctrl Pts',(-4.55708181657933,-4.15692827749739,
42.517814193926));
#37188=CARTESIAN_POINT('Ctrl Pts',(-2.01285648861499,-5.83056224934576,
42.6567605792111));
#37189=CARTESIAN_POINT('Ctrl Pts',(1.02201135833755,-6.08297132745868,42.7957069644963));
#37190=CARTESIAN_POINT('Ctrl Pts',(3.80775949401135,-4.85262970182371,42.9346533497814));
#37191=CARTESIAN_POINT('Ctrl Pts',(5.6653497006872,-2.43943849198514,43.0735997350666));
#37192=CARTESIAN_POINT('Ctrl Pts',(6.14198629054217,0.568376454515263,43.2125461203516));
#37193=CARTESIAN_POINT('Ctrl Pts',(5.12148702285964,3.43764716949481,43.3514925056368));
#37194=CARTESIAN_POINT('Ctrl Pts',(2.85260303024805,5.46897644345585,43.4904388909219));
#37195=CARTESIAN_POINT('Ctrl Pts',(-0.111615351253502,6.16721893568081,
43.6293852762071));
#37196=CARTESIAN_POINT('Ctrl Pts',(-3.04862700569499,5.36217500342934,43.7683316614921));
#37197=CARTESIAN_POINT('Ctrl Pts',(-5.24252257511504,3.25007760471418,43.9072780467774));
#37198=CARTESIAN_POINT('Ctrl Pts',(-6.15853047760213,0.345759661760731,
44.0462244320624));
#37199=CARTESIAN_POINT('Ctrl Pts',(-5.57336980503824,-2.64283870176434,
44.1851708173476));
#37200=CARTESIAN_POINT('Ctrl Pts',(-3.62967601505457,-4.98723364331296,
44.3241172026326));
#37201=CARTESIAN_POINT('Ctrl Pts',(-0.801232918197713,-6.11596870479661,
44.4630635879178));
#37202=CARTESIAN_POINT('Ctrl Pts',(2.22251418542987,-5.7539098083667,44.6020099732029));
#37203=CARTESIAN_POINT('Ctrl Pts',(4.70451379508847,-3.98931038389815,44.7409563584881));
#37204=CARTESIAN_POINT('Ctrl Pts',(6.03976771667011,-1.25229921181993,44.8799027437731));
#37205=CARTESIAN_POINT('Ctrl Pts',(5.90280200243972,1.78996533688478,45.0188491290584));
#37206=CARTESIAN_POINT('Ctrl Pts',(4.32700264063096,4.39591805374351,45.1577955143434));
#37207=CARTESIAN_POINT('Ctrl Pts',(1.69647757568547,5.93034663594394,45.2967418996286));
#37208=CARTESIAN_POINT('Ctrl Pts',(-1.34757127292229,6.01922744641287,45.4356882849136));
#37209=CARTESIAN_POINT('Ctrl Pts',(-4.06314376586214,4.64089540123354,45.5746346701989));
#37210=CARTESIAN_POINT('Ctrl Pts',(-5.78830730338494,2.13132492802865,45.7135810554838));
#37211=CARTESIAN_POINT('Ctrl Pts',(-6.10254577393243,-0.897765261254136,
45.8525274407692));
#37212=CARTESIAN_POINT('Ctrl Pts',(-4.92926218431401,-3.70802126551977,
45.9914738260541));
#37213=CARTESIAN_POINT('Ctrl Pts',(-2.55444950976324,-5.61443096754502,
46.1304202113394));
#37214=CARTESIAN_POINT('Ctrl Pts',(0.443021336985154,-6.15229871529521,
46.2693665966244));
#37215=CARTESIAN_POINT('Ctrl Pts',(3.33250380703052,-5.19051690714888,46.4083129819096));
#37216=CARTESIAN_POINT('Ctrl Pts',(5.40967398771416,-2.96352403969991,46.5472593671947));
#37217=CARTESIAN_POINT('Ctrl Pts',(6.16821261804079,-0.0141593051434131,
46.6862057524798));
#37218=CARTESIAN_POINT('Ctrl Pts',(5.42322260948793,2.93865682161187,46.8251521377649));
#37219=CARTESIAN_POINT('Ctrl Pts',(3.35629851513677,5.17516257371816,46.9640985230501));
#37220=CARTESIAN_POINT('Ctrl Pts',(0.471262067857944,6.15019995212064,47.1030449083352));
#37221=CARTESIAN_POINT('Ctrl Pts',(-2.52864655697621,5.62609935712526,47.2419912936204));
#37222=CARTESIAN_POINT('Ctrl Pts',(-4.91218659163945,3.73061258745804,47.3809376789054));
#37223=CARTESIAN_POINT('Ctrl Pts',(-6.09835979107824,0.925772782067534,
47.5198840641906));
#37224=CARTESIAN_POINT('Ctrl Pts',(-5.79803128232603,-2.10472816220254,
47.6588304494757));
#37225=CARTESIAN_POINT('Ctrl Pts',(-4.08440744356784,-4.62219246979801,
47.7977768347608));
#37226=CARTESIAN_POINT('Ctrl Pts',(-1.3751915372633,-6.01297726607435,47.9367232200459));
#37227=CARTESIAN_POINT('Ctrl Pts',(1.66923328761391,-5.93807272339738,48.0756696053311));
#37228=CARTESIAN_POINT('Ctrl Pts',(4.30677523582703,-4.41573712583598,48.2146159906162));
#37229=CARTESIAN_POINT('Ctrl Pts',(5.89452201173586,-1.81704643939022,48.3535623759014));
#37230=CARTESIAN_POINT('Ctrl Pts',(6.04545339844714,1.22455727539131,48.4925087611865));
#37231=CARTESIAN_POINT('Ctrl Pts',(4.72277928918092,3.9676697139446,48.6314551464715));
#37232=CARTESIAN_POINT('Ctrl Pts',(2.24890710164729,5.7436456410697,48.7704015317568));
#37233=CARTESIAN_POINT('Ctrl Pts',(-0.773145779312667,6.11958252885515,
48.9093479170418));
#37234=CARTESIAN_POINT('Ctrl Pts',(-3.60674138390151,5.0038454454835,49.0482943023269));
#37235=CARTESIAN_POINT('Ctrl Pts',(-5.56117737882469,2.66839758051078,49.1872406876122));
#37236=CARTESIAN_POINT('Ctrl Pts',(-6.16005361658189,-0.317480470389693,
49.3261870728971));
#37237=CARTESIAN_POINT('Ctrl Pts',(-5.25738726777968,-3.22597776563184,
49.4651334581824));
#37238=CARTESIAN_POINT('Ctrl Pts',(-3.07321526737865,-5.34811628862904,
49.6040798434674));
#37239=CARTESIAN_POINT('Ctrl Pts',(-0.139923243902764,-6.16665295081448,
49.7430262287525));
#37240=CARTESIAN_POINT('Ctrl Pts',(2.82745529157474,-5.48199286181392,49.8819726140377));
#37241=CARTESIAN_POINT('Ctrl Pts',(5.10566911489767,-3.46116748161068,50.0209189993228));
#37242=CARTESIAN_POINT('Ctrl Pts',(6.13927613085879,-0.596483094503927,
50.159865384608));
#37243=CARTESIAN_POINT('Ctrl Pts',(5.67656028959098,2.41323360786418,50.2988117698931));
#37244=CARTESIAN_POINT('Ctrl Pts',(3.82978111916535,4.83555167229963,50.4377636931423));
#37245=CARTESIAN_POINT('Ctrl Pts',(1.97657001493401,5.6633953183859,50.5304001546298));
#37246=CARTESIAN_POINT('Ctrl Pts',(1.00683925828395,5.83084219161743,50.5767211543557));
#37247=CARTESIAN_POINT('',(-2.85720427747916,-4.00332290438391,-6.57838495879084E-5));
#37248=CARTESIAN_POINT('Ctrl Pts',(-2.85727392025667,-4.0034136718698,-1.90440111597079E-16));
#37249=CARTESIAN_POINT('Ctrl Pts',(-2.96392441703552,-3.94219184122042,
-3.79761926524811E-15));
#37250=CARTESIAN_POINT('Ctrl Pts',(-3.06811942088831,-3.87701250322895,
-4.52675719847336E-15));
#37251=CARTESIAN_POINT('Ctrl Pts',(-3.1696245436634,-3.8080049793148,-3.87190279838023E-15));
#37252=CARTESIAN_POINT('Ctrl Pts',(-3.28894064367922,-3.7268887912833,-2.80322714571153E-15));
#37253=CARTESIAN_POINT('Ctrl Pts',(-3.40454111778736,-3.64048431718383,
-1.35958250046822E-15));
#37254=CARTESIAN_POINT('Ctrl Pts',(-3.51620782247888,-3.54916472775186,
-2.47718512369488E-15));
#37255=CARTESIAN_POINT('Ctrl Pts',(-3.62942802187464,-3.45657471040703,
-3.61033570959694E-15));
#37256=CARTESIAN_POINT('Ctrl Pts',(-3.73860485228503,-3.35893149262313,
-9.2527721805512E-15));
#37257=CARTESIAN_POINT('Ctrl Pts',(-3.84348814314742,-3.25657606743181,
-3.27515792264421E-15));
#37258=CARTESIAN_POINT('Ctrl Pts',(-3.85907125732511,-3.24136853280597,
-2.38702936827464E-15));
#37259=CARTESIAN_POINT('Ctrl Pts',(-3.87455954225653,-3.22605689833688,
-1.45446846519406E-15));
#37260=CARTESIAN_POINT('Ctrl Pts',(-3.88995212208754,-3.2106422018724,-1.17961196366423E-15));
#37261=CARTESIAN_POINT('Ctrl Pts',(-3.90663484725527,-3.1939355063422,-9.37983998556092E-16));
#37262=CARTESIAN_POINT('Ctrl Pts',(-3.92319901111119,-3.17711387554321,
-2.16429627180207E-15));
#37263=CARTESIAN_POINT('Ctrl Pts',(-3.93964133836745,-3.16018139905906,
-1.87350135405495E-15));
#37264=CARTESIAN_POINT('Ctrl Pts',(-4.04344251084588,-3.05328589183402,
-1.39830370429894E-15));
#37265=CARTESIAN_POINT('Ctrl Pts',(-4.14242071302894,-2.9419456343137,-1.86698229125925E-15));
#37266=CARTESIAN_POINT('Ctrl Pts',(-4.23634450385737,-2.82655565829915,
-2.41473507855972E-15));
#37267=CARTESIAN_POINT('Ctrl Pts',(-4.33083320912257,-2.71047165723798,
-1.95593090836767E-15));
#37268=CARTESIAN_POINT('Ctrl Pts',(-4.42020713177466,-2.59028858558435,
-3.66802097409348E-15));
#37269=CARTESIAN_POINT('Ctrl Pts',(-4.50420315680805,-2.46636346404815,
-3.10862446895044E-15));
#37270=CARTESIAN_POINT('Ctrl Pts',(-4.56394529362918,-2.37822177444499,
-3.71351768609898E-15));
#37271=CARTESIAN_POINT('Ctrl Pts',(-4.62096632907673,-2.28818610926391,
-4.00301393197316E-15));
#37272=CARTESIAN_POINT('Ctrl Pts',(-4.6751605977512,-2.19637326218911,-2.13717932240343E-15));
#37273=CARTESIAN_POINT('Ctrl Pts',(-4.69349550832276,-2.16531129970469,
-2.68638171010596E-15));
#37274=CARTESIAN_POINT('Ctrl Pts',(-4.71151113780902,-2.13403784574948,
-3.5495951981545E-15));
#37275=CARTESIAN_POINT('Ctrl Pts',(-4.7291814375198,-2.10259654657166,-3.27515792264421E-15));
#37276=CARTESIAN_POINT('Ctrl Pts',(-4.76374095187582,-2.04110375651751,
-2.73841439717669E-15));
#37277=CARTESIAN_POINT('Ctrl Pts',(-4.79699068953928,-1.97895180212665,
-2.25062029132347E-15));
#37278=CARTESIAN_POINT('Ctrl Pts',(-4.82890821417569,-1.91618085442916,
-1.47104550762833E-15));
#37279=CARTESIAN_POINT('Ctrl Pts',(-4.89653151535774,-1.78318875212848,
-3.27759312618307E-16));
#37280=CARTESIAN_POINT('Ctrl Pts',(-4.95817727267847,-1.647420621107,-2.18395141942288E-15));
#37281=CARTESIAN_POINT('Ctrl Pts',(-5.01386176575433,-1.50932773275128,
-2.88657986402541E-15));
#37282=CARTESIAN_POINT('Ctrl Pts',(-5.07040880353274,-1.36909580563034,
-4.46478699491984E-15));
#37283=CARTESIAN_POINT('Ctrl Pts',(-5.12080880180208,-1.22646596455888,
-1.93984784978018E-15));
#37284=CARTESIAN_POINT('Ctrl Pts',(-5.1650385546073,-1.08187495549977,-8.88178419700125E-16));
#37285=CARTESIAN_POINT('Ctrl Pts',(-5.20789090131116,-0.941786809908098,
1.14310558333649E-15));
#37286=CARTESIAN_POINT('Ctrl Pts',(-5.24495133489085,-0.799856998147732,
-7.25711619033519E-17));
#37287=CARTESIAN_POINT('Ctrl Pts',(-5.27615924986373,-0.656459529145883,
6.38378239159465E-16));
#37288=CARTESIAN_POINT('Ctrl Pts',(-5.2995651860934,-0.548911427394497,
1.17159028995658E-15));
#37289=CARTESIAN_POINT('Ctrl Pts',(-5.31967830443972,-0.44053724444289,
-1.8825369533321E-16));
#37290=CARTESIAN_POINT('Ctrl Pts',(-5.33645757909966,-0.33148943554366,
8.32667268468867E-17));
#37291=CARTESIAN_POINT('Ctrl Pts',(-5.34173742775273,-0.297175918505209,
1.68704671238542E-16));
#37292=CARTESIAN_POINT('Ctrl Pts',(-5.34668707696921,-0.262795679428468,
-5.27690249084824E-16));
#37293=CARTESIAN_POINT('Ctrl Pts',(-5.35130496264844,-0.228353414454299,
-1.22124532708767E-15));
#37294=CARTESIAN_POINT('Ctrl Pts',(-5.35416327631062,-0.207034827687464,
-1.65053225461906E-15));
#37295=CARTESIAN_POINT('Ctrl Pts',(-5.3568934937129,-0.18569960650873,-1.7557947277759E-15));
#37296=CARTESIAN_POINT('Ctrl Pts',(-5.35949458805709,-0.164356971876369,
-1.55431223447522E-15));
#37297=CARTESIAN_POINT('Ctrl Pts',(-5.36550318946691,-0.115054882996834,
-1.08888198354834E-15));
#37298=CARTESIAN_POINT('Ctrl Pts',(-5.37082454994926,-0.0657002470660596,
-2.6297948742482E-15));
#37299=CARTESIAN_POINT('Ctrl Pts',(-5.37545897566846,-0.0163081375275379,
-2.55351295663786E-15));
#37300=CARTESIAN_POINT('Ctrl Pts',(-5.39010486966895,0.139782745052889,
-2.31244384750334E-15));
#37301=CARTESIAN_POINT('Ctrl Pts',(-5.39789366413514,0.296245517049997,
-1.69829426269487E-16));
#37302=CARTESIAN_POINT('Ctrl Pts',(-5.3988048329656,0.45261913524857,-4.44089209850063E-16));
#37303=CARTESIAN_POINT('Ctrl Pts',(-5.39920138612075,0.520675075713029,
-5.63450824156723E-16));
#37304=CARTESIAN_POINT('Ctrl Pts',(-5.39829465303725,0.588714457569937,
-4.03889576939982E-16));
#37305=CARTESIAN_POINT('Ctrl Pts',(-5.39608014451778,0.656700546464023,
-8.88178419700125E-16));
#37306=CARTESIAN_POINT('Ctrl Pts',(-5.39103330518352,0.81164005769026,-2.2239734044486E-15));
#37307=CARTESIAN_POINT('Ctrl Pts',(-5.37919775368595,0.966302252665731,
-2.50379637210522E-15));
#37308=CARTESIAN_POINT('Ctrl Pts',(-5.36076192524352,1.12029164381784,-1.55431223447522E-15));
#37309=CARTESIAN_POINT('Ctrl Pts',(-5.34439112180454,1.25703245056332,-7.11181249930206E-16));
#37310=CARTESIAN_POINT('Ctrl Pts',(-5.32281505665169,1.3932432519743,-1.27921867688379E-15));
#37311=CARTESIAN_POINT('Ctrl Pts',(-5.29613177430492,1.52864937240809,-9.99200722162641E-16));
#37312=CARTESIAN_POINT('Ctrl Pts',(-5.28279013313154,1.59635243262499,-8.59191744802064E-16));
#37313=CARTESIAN_POINT('Ctrl Pts',(-5.26817119586974,1.66385431563014,-1.01692553827192E-15));
#37314=CARTESIAN_POINT('Ctrl Pts',(-5.25228430581433,1.73112039267501,-6.66133814775094E-16));
#37315=CARTESIAN_POINT('Ctrl Pts',(-5.24284045247573,1.77110625296983,-4.57608069487945E-16));
#37316=CARTESIAN_POINT('Ctrl Pts',(-5.23294851526294,1.8110087825455,1.63983992970298E-15));
#37317=CARTESIAN_POINT('Ctrl Pts',(-5.22261013722243,1.85082063743615,7.7715611723761E-16));
#37318=CARTESIAN_POINT('Ctrl Pts',(-5.21644087173432,1.87457773951079,2.62363037458145E-16));
#37319=CARTESIAN_POINT('Ctrl Pts',(-5.21011245680572,1.89830284226968,-2.1845483731124E-15));
#37320=CARTESIAN_POINT('Ctrl Pts',(-5.20363101472144,1.9219741450254,-2.99760216648792E-15));
#37321=CARTESIAN_POINT('Ctrl Pts',(-5.2027022220642,1.92536625003855,-3.11411302678728E-15));
#37322=CARTESIAN_POINT('Ctrl Pts',(-5.20177026797345,1.9287573266952,-2.51008778115122E-15));
#37323=CARTESIAN_POINT('Ctrl Pts',(-5.2008351599293,1.93214735386067,-2.55351295663786E-15));
#37324=CARTESIAN_POINT('Ctrl Pts',(-5.15837246026862,2.08608646952665,-3.29752994359241E-15));
#37325=CARTESIAN_POINT('Ctrl Pts',(-5.10939283443341,2.2379254056552,-9.6917886872663E-16));
#37326=CARTESIAN_POINT('Ctrl Pts',(-5.05412742134996,2.38725197436616,-1.4432899320127E-15));
#37327=CARTESIAN_POINT('Ctrl Pts',(-4.99560914757004,2.54536773869149,1.84033906423277E-16));
#37328=CARTESIAN_POINT('Ctrl Pts',(-4.93004375984936,2.70066753913477,-2.81809918376493E-16));
#37329=CARTESIAN_POINT('Ctrl Pts',(-4.85764295714644,2.85266553503319,-8.88178419700125E-16));
#37330=CARTESIAN_POINT('Ctrl Pts',(-4.78524215444354,3.00466353093158,-1.1729133274605E-16));
#37331=CARTESIAN_POINT('Ctrl Pts',(-4.70600574477678,3.15336070488546,-8.50437032510622E-16));
#37332=CARTESIAN_POINT('Ctrl Pts',(-4.62008381109869,3.29826043492649,4.44089209850063E-16));
#37333=CARTESIAN_POINT('Ctrl Pts',(-4.55853244340741,3.40206136421584,1.38317739444463E-15));
#37334=CARTESIAN_POINT('Ctrl Pts',(-4.4935489092733,3.50391333587595,-2.37538502008119E-15));
#37335=CARTESIAN_POINT('Ctrl Pts',(-4.42526788724923,3.60369937507567,1.11022302462516E-16));
#37336=CARTESIAN_POINT('Ctrl Pts',(-4.39539494011371,3.64735576722555,1.16321000706569E-15));
#37337=CARTESIAN_POINT('Ctrl Pts',(-4.36489064048442,3.69061662547834,-4.70458545952692E-16));
#37338=CARTESIAN_POINT('Ctrl Pts',(-4.33376540259314,3.73347163408685,-1.60982338570648E-15));
#37339=CARTESIAN_POINT('Ctrl Pts',(-4.3144372096508,3.76008379614724,-1.89151283622047E-15));
#37340=CARTESIAN_POINT('Ctrl Pts',(-4.29486956173448,3.78653944869874,-2.67178752123484E-15));
#37341=CARTESIAN_POINT('Ctrl Pts',(-4.2750648569809,3.8128360516663,-1.49880108324396E-15));
#37342=CARTESIAN_POINT('Ctrl Pts',(-4.25977487047579,3.83313803089331,-5.93210869670195E-16));
#37343=CARTESIAN_POINT('Ctrl Pts',(-4.24434478058479,3.85334347519376,-6.91837681892335E-16));
#37344=CARTESIAN_POINT('Ctrl Pts',(-4.22878820767209,3.87343556296813,-7.7715611723761E-16));
#37345=CARTESIAN_POINT('Ctrl Pts',(-4.12984945342294,4.00121988576316,-1.31977561029168E-15));
#37346=CARTESIAN_POINT('Ctrl Pts',(-4.02566840201076,4.12459437000251,-1.20137809397138E-15));
#37347=CARTESIAN_POINT('Ctrl Pts',(-3.91664624574708,4.24332609595032,-7.21644966006352E-16));
#37348=CARTESIAN_POINT('Ctrl Pts',(-3.80538717710434,4.36449395485185,-2.32068692305071E-16));
#37349=CARTESIAN_POINT('Ctrl Pts',(-3.68908600787891,4.48082719185148,-2.27264911948676E-15));
#37350=CARTESIAN_POINT('Ctrl Pts',(-3.56811826615625,4.59205972744533,-9.99200722162641E-16));
#37351=CARTESIAN_POINT('Ctrl Pts',(-3.44670691496372,4.70370017183738,2.78917628988849E-16));
#37352=CARTESIAN_POINT('Ctrl Pts',(-3.32059424074317,4.81020303581451,2.41120170451567E-16));
#37353=CARTESIAN_POINT('Ctrl Pts',(-3.19011516755566,4.91127172518233,-3.33066907387547E-16));
#37354=CARTESIAN_POINT('Ctrl Pts',(-3.06067297799998,5.01153724767336,-9.02691068215667E-16));
#37355=CARTESIAN_POINT('Ctrl Pts',(-2.92693298103373,5.10645516017338,-1.40885470584828E-15));
#37356=CARTESIAN_POINT('Ctrl Pts',(-2.78918574631266,5.19570037385525,-7.7715611723761E-16));
#37357=CARTESIAN_POINT('Ctrl Pts',(-2.72171518373931,5.23941395392303,-4.67741127988239E-16));
#37358=CARTESIAN_POINT('Ctrl Pts',(-2.65328270595906,5.28176595923915,-2.19182071710708E-16));
#37359=CARTESIAN_POINT('Ctrl Pts',(-2.583919816344,5.32271443393357,-4.44089209850063E-16));
#37360=CARTESIAN_POINT('Ctrl Pts',(-2.85714359587721,-4.00323788139524,
-6.57838495876639E-5));
#37361=CARTESIAN_POINT('Ctrl Pts',(-2.85654553762487,-4.00366472045808,
-4.38558997250773E-5));
#37362=CARTESIAN_POINT('Ctrl Pts',(-2.85594738372198,-4.00409142550178,
-2.19279498625866E-5));
#37363=CARTESIAN_POINT('Ctrl Pts',(-2.85534913422859,-4.00451799648348,
0.));
#37364=CARTESIAN_POINT('Origin',(0.959402651837398,0.906858060794113,49.9999999999962));
#37365=CARTESIAN_POINT('Origin',(-2.88675134594813,-5.,-12.));
#37366=CARTESIAN_POINT('',(-2.88675134594813,-5.,-12.));
#37367=CARTESIAN_POINT('',(2.88675134594813,-5.,-12.));
#37368=CARTESIAN_POINT('',(-1.44337567297407,-5.,-12.));
#37369=CARTESIAN_POINT('',(-2.88675134594813,-5.,-6.));
#37370=CARTESIAN_POINT('',(-2.88675134594813,-5.,-12.));
#37371=CARTESIAN_POINT('',(2.88675134594813,-5.,-6.));
#37372=CARTESIAN_POINT('',(-2.88675134594813,-5.,-6.));
#37373=CARTESIAN_POINT('',(2.88675134594813,-5.,-12.));
#37374=CARTESIAN_POINT('Origin',(-5.77350269189626,7.07050159149938E-16,
-12.));
#37375=CARTESIAN_POINT('',(-5.77350269189626,7.07050159149938E-16,-12.));
#37376=CARTESIAN_POINT('',(-5.05181485540923,-1.25,-12.));
#37377=CARTESIAN_POINT('',(-5.77350269189626,1.11022302462516E-15,-6.));
#37378=CARTESIAN_POINT('',(-5.77350269189626,7.07050159149938E-16,-12.));
#37379=CARTESIAN_POINT('',(-5.77350269189626,7.07050159149938E-16,-6.));
#37380=CARTESIAN_POINT('Origin',(-2.88675134594813,5.,-12.));
#37381=CARTESIAN_POINT('',(-2.88675134594813,5.,-12.));
#37382=CARTESIAN_POINT('',(-3.60843918243516,3.75,-12.));
#37383=CARTESIAN_POINT('',(-2.88675134594813,5.,-6.));
#37384=CARTESIAN_POINT('',(-2.88675134594813,5.,-12.));
#37385=CARTESIAN_POINT('',(-2.88675134594813,5.,-6.));
#37386=CARTESIAN_POINT('Origin',(2.88675134594813,5.,-12.));
#37387=CARTESIAN_POINT('',(2.88675134594813,5.,-12.));
#37388=CARTESIAN_POINT('',(1.44337567297407,5.,-12.));
#37389=CARTESIAN_POINT('',(2.88675134594813,5.,-6.));
#37390=CARTESIAN_POINT('',(2.88675134594813,5.,-12.));
#37391=CARTESIAN_POINT('',(2.88675134594813,5.,-6.));
#37392=CARTESIAN_POINT('Origin',(5.77350269189626,0.,-12.));
#37393=CARTESIAN_POINT('',(5.77350269189626,0.,-12.));
#37394=CARTESIAN_POINT('',(5.05181485540923,1.25,-12.));
#37395=CARTESIAN_POINT('',(5.77350269189626,0.,-6.));
#37396=CARTESIAN_POINT('',(5.77350269189626,0.,-12.));
#37397=CARTESIAN_POINT('',(5.77350269189626,0.,-6.));
#37398=CARTESIAN_POINT('Origin',(2.88675134594813,-5.,-12.));
#37399=CARTESIAN_POINT('',(3.60843918243516,-3.75,-12.));
#37400=CARTESIAN_POINT('',(2.88675134594813,-5.,-6.));
#37401=CARTESIAN_POINT('Origin',(0.,0.,-6.));
#37402=CARTESIAN_POINT('Origin',(0.,0.,0.));
#37403=CARTESIAN_POINT('',(-9.,-1.10218211923262E-15,0.));
#37404=CARTESIAN_POINT('Origin',(0.,0.,0.));
#37405=CARTESIAN_POINT('Origin',(0.,0.,-12.));
#37406=CARTESIAN_POINT('',(-9.,-1.10218211923262E-15,-12.));
#37407=CARTESIAN_POINT('',(-9.,-1.10218211923262E-15,-12.));
#37408=CARTESIAN_POINT('Origin',(0.,0.,-12.));
#37409=CARTESIAN_POINT('Origin',(0.,0.,-12.));
#37410=CARTESIAN_POINT('Origin',(0.,0.,50.));
#37671=UNCERTAINTY_MEASURE_WITH_UNIT(LENGTH_MEASURE(0.01),#37702,
'DISTANCE_ACCURACY_VALUE',
'Maximum model space distance between geometric entities at asserted c
onnectivities');
#37681=UNCERTAINTY_MEASURE_WITH_UNIT(LENGTH_MEASURE(0.01),#37702,
'DISTANCE_ACCURACY_VALUE',
'Maximum model space distance between geometric entities at asserted c
onnectivities');
#37691=(
GEOMETRIC_REPRESENTATION_CONTEXT(3)
GLOBAL_UNCERTAINTY_ASSIGNED_CONTEXT((#37671))
GLOBAL_UNIT_ASSIGNED_CONTEXT((#37702,#37704,#37705))
REPRESENTATION_CONTEXT('','3D')
);
#37701=(
GEOMETRIC_REPRESENTATION_CONTEXT(3)
GLOBAL_UNCERTAINTY_ASSIGNED_CONTEXT((#37681))
GLOBAL_UNIT_ASSIGNED_CONTEXT((#37702,#37704,#37705))
REPRESENTATION_CONTEXT('','3D')
);
#37702=(
LENGTH_UNIT()
NAMED_UNIT(*)
SI_UNIT(.MILLI.,.METRE.)
);
#37704=(
NAMED_UNIT(*)
PLANE_ANGLE_UNIT()
SI_UNIT($,.RADIAN.)
);
#37705=(
NAMED_UNIT(*)
SI_UNIT($,.STERADIAN.)
SOLID_ANGLE_UNIT()
);
#37715=SHAPE_DEFINITION_REPRESENTATION(#37734,#37787);
#37734=PRODUCT_DEFINITION_SHAPE('',$,#37807);
#37787=SHAPE_REPRESENTATION('',(#4497),#37691);
#37797=PRODUCT_DEFINITION_CONTEXT('part definition',#37856,'design');
#37807=PRODUCT_DEFINITION('Socket head cap screw M12x50',
'Socket head cap screw M12x50',#37826,#37797);
#37826=PRODUCT_DEFINITION_FORMATION('',$,#37867);
#37856=APPLICATION_CONTEXT(
'Core Data for Automotive Mechanical Design Process');
#37857=PRODUCT_CONTEXT('part definition',#37856,'mechanical');
#37867=PRODUCT('Socket head cap screw M12x50',
'Socket head cap screw M12x50',$,(#37857));
#37883=PRESENTATION_STYLE_ASSIGNMENT((#37891));
#37891=SURFACE_STYLE_USAGE(.BOTH.,#37899);
#37899=SURFACE_SIDE_STYLE('',(#37907));
#37907=SURFACE_STYLE_FILL_AREA(#37915);
#37915=FILL_AREA_STYLE('Opaque(64,72,82)',(#37923));
#37923=FILL_AREA_STYLE_COLOUR('Opaque(64,72,82)',#37931);
#37931=COLOUR_RGB('Opaque(64,72,82)',0.250980392156863,0.282352941176471,
0.32156862745098);
ENDSEC;
END-ISO-10303-21;
